ISO-10303-21;
HEADER;
/* Generated by software containing ST-Developer
 * from STEP Tools, Inc. (www.steptools.com) 
 */

FILE_DESCRIPTION(
/* description */ (''),
/* implementation_level */ '2;1');

FILE_NAME(
/* name */ 'Screw.step',
/* time_stamp */ '2026-10-06T12:47:13-07:00',
/* author */ (''),
/* organization */ (''),
/* preprocessor_version */ 'ST-DEVELOPER v20.2',
/* originating_system */ 'Autodesk Translation Framework v15.15.0.0',
/* authorisation */ '');

FILE_SCHEMA (('AUTOMOTIVE_DESIGN { 1 0 10303 214 3 1 1 }'));
ENDSEC;

DATA;
#10=MECHANICAL_DESIGN_GEOMETRIC_PRESENTATION_REPRESENTATION('',(#71),#42667);
#53=SHAPE_REPRESENTATION_RELATIONSHIP('SRR','None',#42706,#62);
#62=ADVANCED_BREP_SHAPE_REPRESENTATION('',(#80),#42662);
#71=STYLED_ITEM('',(#42756),#80);
#80=MANIFOLD_SOLID_BREP('Body1',#4036);
#88=B_SPLINE_SURFACE_WITH_KNOTS('',3,3,((#31748,#31749,#31750,#31751,#31752,
#31753,#31754,#31755,#31756,#31757,#31758,#31759,#31760,#31761,#31762,#31763,
#31764,#31765,#31766,#31767,#31768,#31769,#31770,#31771,#31772,#31773,#31774,
#31775,#31776,#31777,#31778,#31779,#31780,#31781,#31782,#31783,#31784,#31785,
#31786,#31787,#31788,#31789,#31790,#31791,#31792,#31793,#31794,#31795,#31796,
#31797,#31798,#31799,#31800,#31801,#31802,#31803,#31804,#31805,#31806,#31807,
#31808,#31809,#31810,#31811,#31812,#31813,#31814,#31815,#31816,#31817,#31818,
#31819,#31820,#31821,#31822,#31823,#31824,#31825,#31826,#31827,#31828,#31829,
#31830,#31831,#31832,#31833,#31834,#31835,#31836,#31837,#31838,#31839,#31840,
#31841,#31842,#31843,#31844,#31845,#31846,#31847,#31848,#31849,#31850,#31851,
#31852,#31853,#31854,#31855,#31856,#31857,#31858,#31859,#31860,#31861,#31862,
#31863,#31864,#31865,#31866,#31867,#31868,#31869,#31870,#31871,#31872,#31873,
#31874,#31875,#31876,#31877,#31878,#31879,#31880,#31881,#31882,#31883,#31884,
#31885,#31886,#31887,#31888,#31889,#31890,#31891,#31892,#31893,#31894,#31895,
#31896,#31897,#31898,#31899,#31900,#31901,#31902,#31903,#31904,#31905,#31906,
#31907,#31908,#31909,#31910,#31911,#31912,#31913,#31914,#31915,#31916,#31917,
#31918,#31919,#31920,#31921,#31922,#31923,#31924,#31925,#31926,#31927,#31928),
(#31929,#31930,#31931,#31932,#31933,#31934,#31935,#31936,#31937,#31938,
#31939,#31940,#31941,#31942,#31943,#31944,#31945,#31946,#31947,#31948,#31949,
#31950,#31951,#31952,#31953,#31954,#31955,#31956,#31957,#31958,#31959,#31960,
#31961,#31962,#31963,#31964,#31965,#31966,#31967,#31968,#31969,#31970,#31971,
#31972,#31973,#31974,#31975,#31976,#31977,#31978,#31979,#31980,#31981,#31982,
#31983,#31984,#31985,#31986,#31987,#31988,#31989,#31990,#31991,#31992,#31993,
#31994,#31995,#31996,#31997,#31998,#31999,#32000,#32001,#32002,#32003,#32004,
#32005,#32006,#32007,#32008,#32009,#32010,#32011,#32012,#32013,#32014,#32015,
#32016,#32017,#32018,#32019,#32020,#32021,#32022,#32023,#32024,#32025,#32026,
#32027,#32028,#32029,#32030,#32031,#32032,#32033,#32034,#32035,#32036,#32037,
#32038,#32039,#32040,#32041,#32042,#32043,#32044,#32045,#32046,#32047,#32048,
#32049,#32050,#32051,#32052,#32053,#32054,#32055,#32056,#32057,#32058,#32059,
#32060,#32061,#32062,#32063,#32064,#32065,#32066,#32067,#32068,#32069,#32070,
#32071,#32072,#32073,#32074,#32075,#32076,#32077,#32078,#32079,#32080,#32081,
#32082,#32083,#32084,#32085,#32086,#32087,#32088,#32089,#32090,#32091,#32092,
#32093,#32094,#32095,#32096,#32097,#32098,#32099,#32100,#32101,#32102,#32103,
#32104,#32105,#32106,#32107,#32108,#32109),(#32110,#32111,#32112,#32113,
#32114,#32115,#32116,#32117,#32118,#32119,#32120,#32121,#32122,#32123,#32124,
#32125,#32126,#32127,#32128,#32129,#32130,#32131,#32132,#32133,#32134,#32135,
#32136,#32137,#32138,#32139,#32140,#32141,#32142,#32143,#32144,#32145,#32146,
#32147,#32148,#32149,#32150,#32151,#32152,#32153,#32154,#32155,#32156,#32157,
#32158,#32159,#32160,#32161,#32162,#32163,#32164,#32165,#32166,#32167,#32168,
#32169,#32170,#32171,#32172,#32173,#32174,#32175,#32176,#32177,#32178,#32179,
#32180,#32181,#32182,#32183,#32184,#32185,#32186,#32187,#32188,#32189,#32190,
#32191,#32192,#32193,#32194,#32195,#32196,#32197,#32198,#32199,#32200,#32201,
#32202,#32203,#32204,#32205,#32206,#32207,#32208,#32209,#32210,#32211,#32212,
#32213,#32214,#32215,#32216,#32217,#32218,#32219,#32220,#32221,#32222,#32223,
#32224,#32225,#32226,#32227,#32228,#32229,#32230,#32231,#32232,#32233,#32234,
#32235,#32236,#32237,#32238,#32239,#32240,#32241,#32242,#32243,#32244,#32245,
#32246,#32247,#32248,#32249,#32250,#32251,#32252,#32253,#32254,#32255,#32256,
#32257,#32258,#32259,#32260,#32261,#32262,#32263,#32264,#32265,#32266,#32267,
#32268,#32269,#32270,#32271,#32272,#32273,#32274,#32275,#32276,#32277,#32278,
#32279,#32280,#32281,#32282,#32283,#32284,#32285,#32286,#32287,#32288,#32289,
#32290),(#32291,#32292,#32293,#32294,#32295,#32296,#32297,#32298,#32299,
#32300,#32301,#32302,#32303,#32304,#32305,#32306,#32307,#32308,#32309,#32310,
#32311,#32312,#32313,#32314,#32315,#32316,#32317,#32318,#32319,#32320,#32321,
#32322,#32323,#32324,#32325,#32326,#32327,#32328,#32329,#32330,#32331,#32332,
#32333,#32334,#32335,#32336,#32337,#32338,#32339,#32340,#32341,#32342,#32343,
#32344,#32345,#32346,#32347,#32348,#32349,#32350,#32351,#32352,#32353,#32354,
#32355,#32356,#32357,#32358,#32359,#32360,#32361,#32362,#32363,#32364,#32365,
#32366,#32367,#32368,#32369,#32370,#32371,#32372,#32373,#32374,#32375,#32376,
#32377,#32378,#32379,#32380,#32381,#32382,#32383,#32384,#32385,#32386,#32387,
#32388,#32389,#32390,#32391,#32392,#32393,#32394,#32395,#32396,#32397,#32398,
#32399,#32400,#32401,#32402,#32403,#32404,#32405,#32406,#32407,#32408,#32409,
#32410,#32411,#32412,#32413,#32414,#32415,#32416,#32417,#32418,#32419,#32420,
#32421,#32422,#32423,#32424,#32425,#32426,#32427,#32428,#32429,#32430,#32431,
#32432,#32433,#32434,#32435,#32436,#32437,#32438,#32439,#32440,#32441,#32442,
#32443,#32444,#32445,#32446,#32447,#32448,#32449,#32450,#32451,#32452,#32453,
#32454,#32455,#32456,#32457,#32458,#32459,#32460,#32461,#32462,#32463,#32464,
#32465,#32466,#32467,#32468,#32469,#32470,#32471)),.UNSPECIFIED.,.F.,.F.,
 .F.,(4,4),(4,1,1,1,1,1,1,1,1,1,1,1,1,1,1,1,1,1,1,1,1,1,1,1,1,1,1,1,1,1,
1,1,1,1,1,1,1,1,1,1,1,1,1,1,1,1,1,1,1,1,1,1,1,1,1,1,1,1,1,1,1,1,1,1,1,1,
1,1,1,1,1,1,1,1,1,1,1,1,1,1,1,1,1,1,1,1,1,1,1,1,1,1,1,1,1,1,1,1,1,1,1,1,
1,1,1,1,1,1,1,1,1,1,1,1,1,1,1,1,1,1,1,1,1,1,1,1,1,1,1,1,1,1,1,1,1,1,1,1,
1,1,1,1,1,1,1,1,1,1,1,1,1,1,1,1,1,1,1,1,1,1,1,1,1,1,1,1,1,1,1,1,1,1,1,1,
1,1,1,1,4),(-0.000650925100349628,0.0823958707828885),(8.31473274985812,
9.3146787622095,10.3146247745609,11.3145707869122,12.3145167992636,13.314462811615,
14.3144088239664,15.3143548363177,16.3143008486691,17.3142468610205,18.3141928733718,
19.3141388857232,20.3140848980746,21.314030910426,22.3139769227773,23.3139229351287,
24.3138689474801,25.3138149598315,26.3137609721828,27.3137069845342,28.3136529968856,
29.3135990092369,30.3135450215883,31.3134910339397,32.3134370462911,33.3133830586424,
34.3133290709938,35.3132750833452,36.3132210956965,37.3131671080479,38.3131131203993,
39.3130591327507,40.313005145102,41.3129511574534,42.3128971698048,43.3128431821562,
44.3127891945075,45.3127352068589,46.3126812192103,47.3126272315616,48.312573243913,
49.3125192562644,50.3124652686158,51.3124112809671,52.3123572933185,53.3123033056699,
54.3122493180213,55.3121953303726,56.312141342724,57.3120873550754,58.3120333674267,
59.3119793797781,60.3119253921295,61.3118714044809,62.3118174168322,63.3117634291836,
64.311709441535,65.3116554538863,66.3116014662377,67.3115474785891,68.3114934909405,
69.3114395032918,70.3113855156432,71.3113315279946,72.311277540346,73.3112235526973,
74.3111695650487,75.3111155774001,76.3110615897514,77.3110076021028,78.3109536144542,
79.3108996268056,80.3108456391569,81.3107916515083,82.3107376638597,83.3106836762111,
84.3106296885624,85.3105757009138,86.3105217132652,87.3104677256165,88.3104137379679,
89.3103597503193,90.3103057626707,91.310251775022,92.3101977873734,93.3101437997248,
94.3100898120761,95.3100358244275,96.3099818367789,97.3099278491303,98.3098738614816,
99.309819873833,100.309765886184,101.309711898536,102.309657910887,103.309603923238,
104.30954993559,105.309495947941,106.309441960293,107.309387972644,108.309333984995,
109.309279997347,110.309226009698,111.309172022049,112.309118034401,113.309064046752,
114.309010059104,115.308956071455,116.308902083806,117.308848096158,118.308794108509,
119.30874012086,120.308686133212,121.308632145563,122.308578157915,123.308524170266,
124.308470182617,125.308416194969,126.30836220732,127.308308219671,128.308254232023,
129.308200244374,130.308146256726,131.308092269077,132.308038281428,133.30798429378,
134.307930306131,135.307876318482,136.307822330834,137.307768343185,138.307714355537,
139.307660367888,140.307606380239,141.307552392591,142.307498404942,143.307444417293,
144.307390429645,145.307336441996,146.307282454348,147.307228466699,148.30717447905,
149.307120491402,150.307066503753,151.307012516104,152.306958528456,153.306904540807,
154.306850553158,155.30679656551,156.306742577861,157.306688590213,158.306634602564,
159.306580614915,160.306526627267,161.306472639618,162.306418651969,163.306364664321,
164.306310676672,165.306256689024,166.306202701375,167.306148713726,168.306094726078,
169.306040738429,170.30598675078,171.305932763132,172.305878775483,173.305824787835,
174.305770800186,175.305716812537,176.305662824889,177.30560883724,178.305554849591,
179.305500861943,180.305446874294,181.305392886646,182.305338898997,183.305284911348,
184.3052309237,185.305176936051,186.305773873502),.UNSPECIFIED.);
#89=B_SPLINE_SURFACE_WITH_KNOTS('',3,3,((#32657,#32658,#32659,#32660,#32661,
#32662,#32663,#32664,#32665,#32666,#32667,#32668,#32669,#32670,#32671,#32672,
#32673,#32674,#32675,#32676,#32677,#32678,#32679,#32680,#32681,#32682,#32683,
#32684,#32685,#32686,#32687,#32688,#32689,#32690,#32691,#32692,#32693,#32694,
#32695,#32696,#32697,#32698,#32699,#32700,#32701,#32702,#32703,#32704,#32705,
#32706,#32707,#32708,#32709,#32710,#32711,#32712,#32713,#32714,#32715,#32716,
#32717,#32718,#32719,#32720,#32721,#32722,#32723,#32724,#32725,#32726,#32727,
#32728,#32729,#32730,#32731,#32732,#32733,#32734,#32735,#32736,#32737,#32738,
#32739,#32740,#32741,#32742,#32743,#32744,#32745,#32746,#32747,#32748,#32749,
#32750,#32751,#32752,#32753,#32754,#32755,#32756,#32757,#32758,#32759,#32760,
#32761,#32762,#32763,#32764,#32765,#32766,#32767,#32768,#32769,#32770,#32771,
#32772,#32773,#32774,#32775,#32776,#32777,#32778,#32779,#32780,#32781,#32782,
#32783,#32784,#32785,#32786,#32787,#32788,#32789,#32790,#32791,#32792,#32793,
#32794,#32795,#32796,#32797,#32798,#32799,#32800,#32801,#32802,#32803,#32804,
#32805,#32806,#32807,#32808,#32809,#32810,#32811,#32812,#32813,#32814,#32815,
#32816,#32817,#32818,#32819,#32820,#32821,#32822,#32823,#32824,#32825,#32826,
#32827,#32828,#32829,#32830,#32831,#32832,#32833,#32834,#32835,#32836,#32837),
(#32838,#32839,#32840,#32841,#32842,#32843,#32844,#32845,#32846,#32847,
#32848,#32849,#32850,#32851,#32852,#32853,#32854,#32855,#32856,#32857,#32858,
#32859,#32860,#32861,#32862,#32863,#32864,#32865,#32866,#32867,#32868,#32869,
#32870,#32871,#32872,#32873,#32874,#32875,#32876,#32877,#32878,#32879,#32880,
#32881,#32882,#32883,#32884,#32885,#32886,#32887,#32888,#32889,#32890,#32891,
#32892,#32893,#32894,#32895,#32896,#32897,#32898,#32899,#32900,#32901,#32902,
#32903,#32904,#32905,#32906,#32907,#32908,#32909,#32910,#32911,#32912,#32913,
#32914,#32915,#32916,#32917,#32918,#32919,#32920,#32921,#32922,#32923,#32924,
#32925,#32926,#32927,#32928,#32929,#32930,#32931,#32932,#32933,#32934,#32935,
#32936,#32937,#32938,#32939,#32940,#32941,#32942,#32943,#32944,#32945,#32946,
#32947,#32948,#32949,#32950,#32951,#32952,#32953,#32954,#32955,#32956,#32957,
#32958,#32959,#32960,#32961,#32962,#32963,#32964,#32965,#32966,#32967,#32968,
#32969,#32970,#32971,#32972,#32973,#32974,#32975,#32976,#32977,#32978,#32979,
#32980,#32981,#32982,#32983,#32984,#32985,#32986,#32987,#32988,#32989,#32990,
#32991,#32992,#32993,#32994,#32995,#32996,#32997,#32998,#32999,#33000,#33001,
#33002,#33003,#33004,#33005,#33006,#33007,#33008,#33009,#33010,#33011,#33012,
#33013,#33014,#33015,#33016,#33017,#33018),(#33019,#33020,#33021,#33022,
#33023,#33024,#33025,#33026,#33027,#33028,#33029,#33030,#33031,#33032,#33033,
#33034,#33035,#33036,#33037,#33038,#33039,#33040,#33041,#33042,#33043,#33044,
#33045,#33046,#33047,#33048,#33049,#33050,#33051,#33052,#33053,#33054,#33055,
#33056,#33057,#33058,#33059,#33060,#33061,#33062,#33063,#33064,#33065,#33066,
#33067,#33068,#33069,#33070,#33071,#33072,#33073,#33074,#33075,#33076,#33077,
#33078,#33079,#33080,#33081,#33082,#33083,#33084,#33085,#33086,#33087,#33088,
#33089,#33090,#33091,#33092,#33093,#33094,#33095,#33096,#33097,#33098,#33099,
#33100,#33101,#33102,#33103,#33104,#33105,#33106,#33107,#33108,#33109,#33110,
#33111,#33112,#33113,#33114,#33115,#33116,#33117,#33118,#33119,#33120,#33121,
#33122,#33123,#33124,#33125,#33126,#33127,#33128,#33129,#33130,#33131,#33132,
#33133,#33134,#33135,#33136,#33137,#33138,#33139,#33140,#33141,#33142,#33143,
#33144,#33145,#33146,#33147,#33148,#33149,#33150,#33151,#33152,#33153,#33154,
#33155,#33156,#33157,#33158,#33159,#33160,#33161,#33162,#33163,#33164,#33165,
#33166,#33167,#33168,#33169,#33170,#33171,#33172,#33173,#33174,#33175,#33176,
#33177,#33178,#33179,#33180,#33181,#33182,#33183,#33184,#33185,#33186,#33187,
#33188,#33189,#33190,#33191,#33192,#33193,#33194,#33195,#33196,#33197,#33198,
#33199),(#33200,#33201,#33202,#33203,#33204,#33205,#33206,#33207,#33208,
#33209,#33210,#33211,#33212,#33213,#33214,#33215,#33216,#33217,#33218,#33219,
#33220,#33221,#33222,#33223,#33224,#33225,#33226,#33227,#33228,#33229,#33230,
#33231,#33232,#33233,#33234,#33235,#33236,#33237,#33238,#33239,#33240,#33241,
#33242,#33243,#33244,#33245,#33246,#33247,#33248,#33249,#33250,#33251,#33252,
#33253,#33254,#33255,#33256,#33257,#33258,#33259,#33260,#33261,#33262,#33263,
#33264,#33265,#33266,#33267,#33268,#33269,#33270,#33271,#33272,#33273,#33274,
#33275,#33276,#33277,#33278,#33279,#33280,#33281,#33282,#33283,#33284,#33285,
#33286,#33287,#33288,#33289,#33290,#33291,#33292,#33293,#33294,#33295,#33296,
#33297,#33298,#33299,#33300,#33301,#33302,#33303,#33304,#33305,#33306,#33307,
#33308,#33309,#33310,#33311,#33312,#33313,#33314,#33315,#33316,#33317,#33318,
#33319,#33320,#33321,#33322,#33323,#33324,#33325,#33326,#33327,#33328,#33329,
#33330,#33331,#33332,#33333,#33334,#33335,#33336,#33337,#33338,#33339,#33340,
#33341,#33342,#33343,#33344,#33345,#33346,#33347,#33348,#33349,#33350,#33351,
#33352,#33353,#33354,#33355,#33356,#33357,#33358,#33359,#33360,#33361,#33362,
#33363,#33364,#33365,#33366,#33367,#33368,#33369,#33370,#33371,#33372,#33373,
#33374,#33375,#33376,#33377,#33378,#33379,#33380)),.UNSPECIFIED.,.F.,.F.,
 .F.,(4,4),(4,1,1,1,1,1,1,1,1,1,1,1,1,1,1,1,1,1,1,1,1,1,1,1,1,1,1,1,1,1,
1,1,1,1,1,1,1,1,1,1,1,1,1,1,1,1,1,1,1,1,1,1,1,1,1,1,1,1,1,1,1,1,1,1,1,1,
1,1,1,1,1,1,1,1,1,1,1,1,1,1,1,1,1,1,1,1,1,1,1,1,1,1,1,1,1,1,1,1,1,1,1,1,
1,1,1,1,1,1,1,1,1,1,1,1,1,1,1,1,1,1,1,1,1,1,1,1,1,1,1,1,1,1,1,1,1,1,1,1,
1,1,1,1,1,1,1,1,1,1,1,1,1,1,1,1,1,1,1,1,1,1,1,1,1,1,1,1,1,1,1,1,1,1,1,1,
1,1,1,1,4),(-0.00033399260015787,0.082683618112034),(11.6145432153813,12.6151602401062,
13.6151062524576,14.615052264809,15.6149982771603,16.6149442895117,17.6148903018631,
18.6148363142145,19.6147823265658,20.6147283389172,21.6146743512686,22.61462036362,
23.6145663759713,24.6145123883227,25.6144584006741,26.6144044130254,27.6143504253768,
28.6142964377282,29.6142424500796,30.6141884624309,31.6141344747823,32.6140804871337,
33.614026499485,34.6139725118364,35.6139185241878,36.6138645365392,37.6138105488905,
38.6137565612419,39.6137025735933,40.6136485859447,41.613594598296,42.6135406106474,
43.6134866229988,44.6134326353501,45.6133786477015,46.6133246600529,47.6132706724043,
48.6132166847556,49.613162697107,50.6131087094584,51.6130547218097,52.6130007341611,
53.6129467465125,54.6128927588639,55.6128387712152,56.6127847835666,57.612730795918,
58.6126768082694,59.6126228206207,60.6125688329721,61.6125148453235,62.6124608576748,
63.6124068700262,64.6123528823776,65.612298894729,66.6122449070803,67.6121909194317,
68.6121369317831,69.6120829441344,70.6120289564858,71.6119749688372,72.6119209811886,
73.6118669935399,74.6118130058913,75.6117590182427,76.6117050305941,77.6116510429454,
78.6115970552968,79.6115430676482,80.6114890799995,81.6114350923509,82.6113811047023,
83.6113271170537,84.611273129405,85.6112191417564,86.6111651541078,87.6111111664591,
88.6110571788105,89.6110031911619,90.6109492035133,91.6108952158646,92.610841228216,
93.6107872405674,94.6107332529187,95.6106792652701,96.6106252776215,97.6105712899729,
98.6105173023242,99.6104633146756,100.610409327027,101.610355339378,102.61030135173,
103.610247364081,104.610193376432,105.610139388784,106.610085401135,107.610031413487,
108.609977425838,109.609923438189,110.609869450541,111.609815462892,112.609761475243,
113.609707487595,114.609653499946,115.609599512298,116.609545524649,117.609491537,
118.609437549352,119.609383561703,120.609329574054,121.609275586406,122.609221598757,
123.609167611109,124.60911362346,125.609059635811,126.609005648163,127.608951660514,
128.608897672865,129.608843685217,130.608789697568,131.60873570992,132.608681722271,
133.608627734622,134.608573746974,135.608519759325,136.608465771676,137.608411784028,
138.608357796379,139.60830380873,140.608249821082,141.608195833433,142.608141845785,
143.608087858136,144.608033870487,145.607979882839,146.60792589519,147.607871907541,
148.607817919893,149.607763932244,150.607709944596,151.607655956947,152.607601969298,
153.60754798165,154.607493994001,155.607440006352,156.607386018704,157.607332031055,
158.607278043407,159.607224055758,160.607170068109,161.607116080461,162.607062092812,
163.607008105163,164.606954117515,165.606900129866,166.606846142218,167.606792154569,
168.60673816692,169.606684179272,170.606630191623,171.606576203974,172.606522216326,
173.606468228677,174.606414241029,175.60636025338,176.606306265731,177.606252278083,
178.606198290434,179.606144302785,180.606090315137,181.606036327488,182.605982339839,
183.605928352191,184.605874364542,185.605820376894,186.605766389245,187.605712401596,
188.605658413948,189.605604426299),.UNSPECIFIED.);
#152=B_SPLINE_CURVE_WITH_KNOTS('',3,(#11681,#11682,#11683,#11684,#11685,
#11686,#11687,#11688,#11689,#11690,#11691,#11692,#11693,#11694,#11695,#11696,
#11697,#11698,#11699,#11700,#11701,#11702,#11703,#11704,#11705,#11706,#11707,
#11708,#11709,#11710,#11711,#11712,#11713,#11714,#11715,#11716,#11717,#11718,
#11719,#11720,#11721,#11722,#11723,#11724,#11725,#11726,#11727,#11728,#11729,
#11730,#11731,#11732,#11733,#11734,#11735,#11736,#11737,#11738,#11739,#11740,
#11741,#11742,#11743,#11744,#11745,#11746,#11747,#11748,#11749,#11750,#11751,
#11752,#11753,#11754,#11755,#11756,#11757,#11758,#11759,#11760,#11761,#11762,
#11763,#11764,#11765,#11766,#11767,#11768,#11769,#11770,#11771,#11772,#11773,
#11774,#11775,#11776,#11777,#11778,#11779,#11780,#11781,#11782,#11783,#11784,
#11785,#11786,#11787,#11788,#11789,#11790,#11791,#11792),.UNSPECIFIED.,
 .F.,.F.,(4,3,3,3,3,3,3,3,3,3,3,3,3,3,3,3,3,3,3,3,3,3,3,3,3,3,3,3,3,3,3,
3,3,3,3,3,3,4),(10.3762723589309,10.4685607196145,10.560727614795,10.6549580113097,
10.7469711869423,10.838956356852,10.9309391472322,11.0268470571522,11.1189553523447,
11.2111259176515,11.3034309831953,11.3145707869122,11.4078036887453,11.500913534529,
11.5939277225349,11.6868775989975,11.779794413783,11.8727027895915,11.9656273355042,
12.0586527505373,12.151731115711,12.2449651361798,12.3145167992636,12.4074644695395,
12.5002843875549,12.5930043634112,12.6856547841058,12.778269017663,12.8708720387751,
12.9634888063115,13.0562045696504,13.1489717592456,13.2418953378247,13.314462811615,
13.4075374976835,13.5005018407416,13.5933639283471,13.6621109872984),
 .UNSPECIFIED.);
#153=B_SPLINE_CURVE_WITH_KNOTS('',3,(#11795,#11796,#11797,#11798,#11799,
#11800,#11801,#11802,#11803,#11804,#11805,#11806,#11807,#11808,#11809,#11810,
#11811,#11812,#11813,#11814,#11815,#11816,#11817,#11818,#11819,#11820,#11821,
#11822,#11823,#11824,#11825,#11826,#11827,#11828,#11829,#11830,#11831,#11832,
#11833,#11834,#11835,#11836,#11837,#11838,#11839,#11840,#11841,#11842,#11843,
#11844,#11845,#11846,#11847,#11848,#11849,#11850,#11851,#11852,#11853,#11854,
#11855,#11856,#11857,#11858,#11859,#11860,#11861,#11862,#11863,#11864),
 .UNSPECIFIED.,.F.,.F.,(4,3,3,3,3,3,3,3,3,3,3,3,3,3,3,3,3,3,3,3,3,3,3,4),
(11.6152142277549,11.7104627373194,11.8056562041118,11.900816792875,11.9959935195508,
12.0911845217967,12.1864099267108,12.2816898891895,12.3771113362023,12.4726110332727,
12.5682798807942,12.6151602401062,12.7072927880287,12.7992864602223,12.8911700806882,
12.9829719958292,13.0747303838343,13.1664710617718,13.25821982499,13.3500638544193,
13.4419557180476,13.5340072043485,13.6151062524576,13.661880832927),
 .UNSPECIFIED.);
#154=B_SPLINE_CURVE_WITH_KNOTS('',3,(#11870,#11871,#11872,#11873,#11874,
#11875,#11876,#11877,#11878,#11879,#11880,#11881,#11882,#11883,#11884,#11885,
#11886,#11887,#11888,#11889,#11890,#11891,#11892,#11893,#11894,#11895,#11896,
#11897,#11898,#11899,#11900,#11901,#11902,#11903,#11904,#11905,#11906,#11907,
#11908,#11909,#11910,#11911,#11912,#11913,#11914,#11915,#11916,#11917,#11918,
#11919,#11920,#11921,#11922,#11923,#11924,#11925,#11926,#11927,#11928,#11929,
#11930,#11931,#11932,#11933,#11934,#11935,#11936,#11937,#11938,#11939,#11940,
#11941,#11942,#11943,#11944,#11945,#11946,#11947,#11948,#11949,#11950,#11951,
#11952,#11953,#11954,#11955,#11956,#11957,#11958,#11959,#11960,#11961,#11962,
#11963,#11964,#11965,#11966,#11967,#11968,#11969,#11970,#11971,#11972,#11973,
#11974,#11975,#11976,#11977,#11978,#11979,#11980,#11981,#11982,#11983,#11984,
#11985,#11986,#11987,#11988,#11989,#11990,#11991,#11992,#11993,#11994,#11995,
#11996,#11997,#11998,#11999,#12000,#12001,#12002,#12003,#12004,#12005,#12006,
#12007,#12008,#12009,#12010,#12011,#12012,#12013,#12014,#12015,#12016,#12017,
#12018,#12019,#12020,#12021,#12022,#12023,#12024,#12025,#12026,#12027,#12028,
#12029,#12030,#12031,#12032,#12033,#12034,#12035,#12036,#12037,#12038,#12039,
#12040,#12041,#12042,#12043,#12044,#12045,#12046,#12047,#12048,#12049,#12050,
#12051,#12052,#12053,#12054,#12055,#12056,#12057,#12058,#12059,#12060,#12061,
#12062,#12063,#12064,#12065,#12066,#12067,#12068,#12069,#12070,#12071,#12072,
#12073),.UNSPECIFIED.,.F.,.F.,(4,2,2,2,2,2,2,2,2,2,2,2,2,2,2,2,2,2,2,2,
2,2,2,2,2,2,2,2,2,2,2,2,2,2,2,2,2,2,2,2,2,2,2,2,2,2,2,2,2,2,2,2,2,2,2,2,
2,2,2,2,2,2,2,2,2,2,2,2,2,2,2,2,2,2,2,2,2,2,2,2,2,2,2,2,2,2,2,2,2,2,2,2,
2,2,2,2,2,2,2,2,2,4),(-1.37022537659221,-1.34091059982744,-1.33432719131615,
-1.3303909319413,-1.32736015588578,-1.32409755164556,-1.31893198307468,
-1.30204871993472,-1.27436763409897,-1.20187882557325,-1.17377960928441,
-1.16957709291693,-1.1674464593617,-1.16576780553845,-1.16381408405481,
-1.16031516703387,-1.14355099392605,-1.06708577498172,-1.01778424944133,
-1.01119847934814,-1.00726192833468,-1.00423159012833,-1.00097011411607,
-0.995807742098134,-0.978947757724557,-0.951318348613338,-0.878272261227642,
-0.850624656984496,-0.846437417232639,-0.844310230135465,-0.84263193635636,
-0.840675834471548,-0.837166371180659,-0.820231465470602,-0.743896134944801,
-0.694656347337957,-0.688058434107688,-0.684117998593137,-0.681086638284101,
-0.67782599594984,-0.67266905232386,-0.655863294413673,-0.628358683882797,
-0.554289454404455,-0.527442810043846,-0.523282445163439,-0.521160607566312,
-0.519481936297915,-0.517519845927585,-0.513986917321571,-0.496687651642819,
-0.420510968432387,-0.371613687460086,-0.365020492697749,-0.361080668421583,
-0.358048465132614,-0.357989283934159,-0.357924385584965,-0.357868206524929,
-0.357819584317401,-0.357777508247663,-0.35774110059434,-0.35770959993251,
-0.357673452353779,-0.357638479118564,-0.35760463897588,-0.357571893371848,
-0.357540205087393,-0.357509538189687,-0.357479857999926,-0.35745113104381,
-0.357423325030654,-0.357396408793136,-0.357370352278429,-0.357345128720867,
-0.357320712405916,-0.357297072275671,-0.357274182330256,-0.357252017493811,
-0.353792555790826,-0.347636689923209,-0.340058218326234,-0.324125423490495,
-0.276678078069955,-0.208783494514185,-0.201629712397283,-0.198940634478145,
-0.197342528679399,-0.195628651904034,-0.193235011566351,-0.187440230609289,
-0.160248598865694,-0.0750892562821783,-0.0558604189753205,-0.0436152515609683,
-0.0388953015602837,-0.0360480651305796,-0.0331759803957967,-0.0302282624267043,
-0.0263905830487572,-0.0167964234972045,-0.000966734669669255),
 .UNSPECIFIED.);
#155=B_SPLINE_CURVE_WITH_KNOTS('',3,(#12074,#12075,#12076,#12077,#12078,
#12079,#12080,#12081,#12082,#12083,#12084,#12085,#12086,#12087,#12088,#12089,
#12090,#12091,#12092,#12093,#12094,#12095,#12096,#12097,#12098,#12099,#12100,
#12101,#12102,#12103,#12104,#12105,#12106,#12107,#12108,#12109,#12110,#12111,
#12112,#12113,#12114,#12115,#12116,#12117,#12118,#12119,#12120,#12121,#12122,
#12123,#12124,#12125,#12126,#12127,#12128,#12129,#12130,#12131,#12132,#12133,
#12134,#12135,#12136,#12137,#12138,#12139,#12140),.UNSPECIFIED.,.F.,.F.,
(4,3,3,3,3,3,3,3,3,3,3,3,3,3,3,3,3,3,3,3,3,3,4),(13.6621109872984,13.7548852435726,
13.8476426210203,13.9404079052831,14.0339081349539,14.1268150028064,14.2206119133864,
14.3144088239664,14.4074983292472,14.5004620657044,14.5933276454891,14.6861257703182,
14.7788889547583,14.8716420039164,14.9644097079295,15.0572768974958,15.1501960256872,
15.2432708035197,15.3143548363177,15.4182322755584,15.5217902671822,15.6247747852697,
15.7079632677622),.UNSPECIFIED.);
#156=B_SPLINE_CURVE_WITH_KNOTS('',3,(#12142,#12143,#12144,#12145,#12146,
#12147,#12148,#12149,#12150,#12151,#12152,#12153,#12154,#12155,#12156,#12157,
#12158,#12159,#12160,#12161,#12162,#12163,#12164,#12165,#12166,#12167,#12168,
#12169,#12170,#12171,#12172,#12173,#12174,#12175,#12176,#12177,#12178,#12179,
#12180,#12181,#12182,#12183,#12184,#12185,#12186,#12187,#12188,#12189,#12190,
#12191,#12192,#12193,#12194,#12195,#12196,#12197,#12198,#12199,#12200,#12201,
#12202,#12203,#12204,#12205,#12206,#12207,#12208,#12209,#12210,#12211),
 .UNSPECIFIED.,.F.,.F.,(4,3,3,3,3,3,3,3,3,3,3,3,3,3,3,3,3,3,3,3,3,3,3,4),
(13.661880832927,13.7550145535338,13.8480359180392,13.9439129613854,14.0367976849942,
14.1296597979391,14.222523956533,14.3154148117948,14.4084097402506,14.5014672535618,
14.5946633566942,14.615052264809,14.708285208079,14.8013950963811,14.894409327926,
14.9873592492917,15.0802761098038,15.173184532111,15.266109125244,15.3591345883359,
15.4522130021073,15.5454470715631,15.6149982771603,15.707963267949),
 .UNSPECIFIED.);
#157=B_SPLINE_CURVE_WITH_KNOTS('',3,(#12212,#12213,#12214,#12215,#12216,
#12217,#12218,#12219,#12220,#12221,#12222,#12223,#12224,#12225,#12226,#12227,
#12228,#12229,#12230,#12231,#12232,#12233,#12234,#12235,#12236,#12237,#12238,
#12239,#12240,#12241,#12242,#12243,#12244,#12245,#12246,#12247,#12248,#12249,
#12250,#12251,#12252,#12253,#12254,#12255,#12256,#12257,#12258,#12259,#12260,
#12261,#12262,#12263,#12264,#12265,#12266,#12267,#12268,#12269,#12270,#12271,
#12272,#12273,#12274,#12275,#12276,#12277,#12278,#12279,#12280,#12281,#12282,
#12283,#12284,#12285,#12286,#12287,#12288,#12289,#12290,#12291,#12292,#12293,
#12294,#12295,#12296,#12297,#12298,#12299,#12300,#12301,#12302,#12303,#12304,
#12305,#12306,#12307,#12308,#12309,#12310,#12311,#12312,#12313,#12314,#12315,
#12316,#12317,#12318,#12319,#12320,#12321,#12322,#12323,#12324,#12325,#12326,
#12327,#12328,#12329,#12330,#12331,#12332,#12333,#12334,#12335,#12336,#12337,
#12338,#12339,#12340,#12341,#12342,#12343,#12344,#12345,#12346,#12347,#12348,
#12349,#12350,#12351,#12352,#12353,#12354,#12355,#12356,#12357,#12358,#12359,
#12360,#12361,#12362,#12363,#12364,#12365,#12366,#12367,#12368,#12369),
 .UNSPECIFIED.,.F.,.F.,(4,2,2,2,2,2,2,2,2,2,2,2,2,2,2,2,2,2,2,2,2,2,2,2,
2,2,2,2,2,2,2,2,2,2,2,2,2,2,2,2,2,2,2,2,2,2,2,2,2,2,2,2,2,2,2,2,2,2,2,2,
2,2,2,2,2,2,2,2,2,2,2,2,2,2,2,2,2,2,4),(-4.06120255059993,-3.98563093651712,
-3.95648723998739,-3.93900363536026,-3.9337996512044,-3.93054568897629,
-3.927545495221,-3.92368079394536,-3.91728694917056,-3.87478652528743,-3.81154283654031,
-3.78641054291921,-3.77775083177261,-3.77363233946665,-3.77033862668475,
-3.76843724623808,-3.76843169727313,-3.7684261277979,-3.76842020266436,
-3.76841417858657,-3.76840805352903,-3.7684018254137,-3.76672725759988,
-3.76458526153515,-3.76018046412751,-3.70378742243041,-3.66048805565629,
-3.63238508052738,-3.61530721998266,-3.61011483988667,-3.60684262793018,
-3.60380790987669,-3.59987349968863,-3.59330806707067,-3.54518739555943,
-3.46818660168279,-3.45132555574338,-3.44781194086284,-3.44585052626606,
-3.44416849798318,-3.44203607305814,-3.43782912895715,-3.40949788501506,
-3.3373981623366,-3.30976078229524,-3.29289800496867,-3.2877355333589,-3.28447412216659,
-3.28144392589934,-3.27750767120283,-3.27092262666215,-3.22169970794755,
-3.14592784897398,-3.12832042484183,-3.12477302637789,-3.1228095549436,
-3.12113407500583,-3.1190219793966,-3.11489708395197,-3.0888726987146,-3.01373915889266,
-2.9864101678104,-2.96968546106006,-2.96454288763508,-2.96128898177692,
-2.9582622867068,-2.95432567725299,-2.94772929532905,-2.8975752535729,-2.81954364620963,
-2.80487885748976,-2.80152221963937,-2.79960157042717,-2.79792027503715,
-2.79574639791226,-2.79221594067299,-2.77172997379105,-2.76310662474663,
-2.69244553871344),.UNSPECIFIED.);
#158=B_SPLINE_CURVE_WITH_KNOTS('',3,(#12374,#12375,#12376,#12377,#12378,
#12379,#12380,#12381,#12382,#12383,#12384,#12385,#12386,#12387,#12388,#12389,
#12390,#12391,#12392,#12393,#12394,#12395,#12396,#12397,#12398,#12399,#12400,
#12401,#12402,#12403,#12404,#12405,#12406,#12407,#12408,#12409,#12410,#12411,
#12412,#12413,#12414,#12415,#12416,#12417,#12418,#12419,#12420,#12421,#12422,
#12423,#12424,#12425,#12426,#12427,#12428,#12429,#12430,#12431,#12432,#12433,
#12434,#12435,#12436,#12437,#12438,#12439,#12440,#12441,#12442,#12443,#12444,
#12445,#12446,#12447,#12448,#12449,#12450,#12451,#12452,#12453,#12454,#12455,
#12456,#12457,#12458,#12459,#12460,#12461,#12462,#12463,#12464,#12465,#12466,
#12467,#12468,#12469,#12470,#12471,#12472,#12473,#12474,#12475,#12476,#12477,
#12478,#12479,#12480,#12481,#12482,#12483,#12484,#12485,#12486,#12487,#12488,
#12489,#12490,#12491,#12492,#12493,#12494,#12495,#12496,#12497,#12498,#12499,
#12500,#12501,#12502,#12503,#12504,#12505,#12506,#12507,#12508,#12509,#12510,
#12511,#12512,#12513,#12514,#12515,#12516,#12517,#12518,#12519,#12520,#12521,
#12522,#12523,#12524,#12525,#12526,#12527,#12528,#12529,#12530,#12531,#12532,
#12533,#12534,#12535,#12536,#12537,#12538,#12539,#12540,#12541,#12542,#12543,
#12544,#12545,#12546,#12547,#12548,#12549,#12550,#12551,#12552,#12553,#12554,
#12555,#12556,#12557,#12558,#12559,#12560,#12561,#12562,#12563,#12564,#12565,
#12566,#12567,#12568,#12569,#12570,#12571,#12572,#12573,#12574,#12575,#12576,
#12577,#12578,#12579,#12580,#12581,#12582,#12583,#12584,#12585,#12586,#12587,
#12588,#12589),.UNSPECIFIED.,.F.,.F.,(4,2,2,2,2,2,2,2,2,2,2,2,2,2,2,2,2,
2,2,2,2,2,2,2,2,2,2,2,2,2,2,2,2,2,2,2,2,2,2,2,2,2,2,2,2,2,2,2,2,2,2,2,2,
2,2,2,2,2,2,2,2,2,2,2,2,2,2,2,2,2,2,2,2,2,2,2,2,2,2,2,2,2,2,2,2,2,2,2,2,
2,2,2,2,2,2,2,2,2,2,2,2,2,2,2,2,2,2,4),(-3.40022159451442,-3.3925401132152,
-3.3200050390171,-3.29235438762688,-3.27548412264847,-3.27032103375553,
-3.26705964286102,-3.26402975102361,-3.26009429546325,-3.25351143131809,
-3.20432783531026,-3.12804042133909,-3.11098569610243,-3.1074693544432,
-3.10551192600415,-3.10383397299881,-3.10170913726944,-3.09753242381139,
-3.07018138376164,-2.99683627903875,-2.96926380638888,-2.95242740298401,
-2.94726785950343,-2.94400713566057,-2.9409767780011,-2.93703917585256,
-2.93044932349352,-2.88092989287828,-2.80390463736647,-2.7878178537626,
-2.78436140521718,-2.78241699071641,-2.78073744627168,-2.77859408937043,
-2.77418488279155,-2.71819893788166,-2.67545672979554,-2.64679667237422,
-2.62948906307082,-2.62427798083233,-2.62100566616702,-2.61797889757186,
-2.614066204176,-2.60756229829595,-2.56201005594115,-2.4944036654252,-2.46825969003576,
-2.46258138440068,-2.46020576467742,-2.45849402512761,-2.45689066920433,
-2.45417405380509,-2.44683789853128,-2.39269897481404,-2.35094086384508,
-2.32325622336795,-2.30637011488509,-2.30120456608902,-2.29794217041142,
-2.29491172361986,-2.29097608412515,-2.28439409414145,-2.23531443419858,
-2.15923668276916,-2.14186746965592,-2.13833196816928,-2.13637011532168,
-2.13469222279945,-2.13257238790137,-2.12842018158147,-2.10178022082503,
-2.09186350730744,-2.03167536075008,-1.98694862586953,-1.98046071444936,
-1.9765524753541,-1.97352611548223,-1.97025122058457,-1.96502950273261,
-1.94762606752115,-1.9187391385546,-1.87617611232732,-1.82026864601881,
-1.81585648676625,-1.81371237128581,-1.81203256007626,-1.81008819935012,
-1.80663275527695,-1.79056621408816,-1.71355628532306,-1.66403361467725,
-1.65744290374154,-1.65350465165849,-1.6504737318586,-1.64721234376396,
-1.64205162508133,-1.62521044484006,-1.59762499205793,-1.52418393971989,
-1.49685097773187,-1.49267399540364,-1.49054880963011,-1.48887042187013,
-1.48691225260106,-1.48339422559622,-1.46632336136999,-1.39005788054266,
-1.37022537659221),.UNSPECIFIED.);
#159=B_SPLINE_CURVE_WITH_KNOTS('',3,(#12590,#12591,#12592,#12593,#12594,
#12595,#12596,#12597,#12598,#12599,#12600,#12601,#12602,#12603,#12604,#12605,
#12606,#12607,#12608,#12609,#12610,#12611,#12612,#12613,#12614,#12615,#12616,
#12617,#12618,#12619,#12620,#12621,#12622,#12623,#12624,#12625,#12626,#12627,
#12628,#12629,#12630,#12631,#12632,#12633,#12634,#12635,#12636,#12637,#12638,
#12639,#12640,#12641,#12642,#12643,#12644,#12645,#12646,#12647,#12648,#12649,
#12650,#12651,#12652,#12653,#12654,#12655,#12656,#12657,#12658,#12659,#12660,
#12661,#12662,#12663,#12664,#12665,#12666,#12667,#12668,#12669,#12670,#12671,
#12672,#12673,#12674,#12675,#12676,#12677,#12678,#12679,#12680,#12681,#12682,
#12683,#12684,#12685,#12686,#12687,#12688,#12689,#12690,#12691,#12692,#12693,
#12694,#12695,#12696,#12697,#12698,#12699,#12700,#12701,#12702,#12703,#12704,
#12705,#12706,#12707,#12708,#12709,#12710,#12711,#12712,#12713,#12714,#12715,
#12716,#12717,#12718,#12719,#12720,#12721,#12722,#12723,#12724,#12725,#12726,
#12727,#12728,#12729,#12730,#12731,#12732,#12733,#12734,#12735,#12736,#12737,
#12738,#12739,#12740,#12741,#12742,#12743,#12744,#12745,#12746,#12747,#12748,
#12749,#12750,#12751,#12752,#12753,#12754,#12755,#12756,#12757,#12758,#12759,
#12760,#12761,#12762,#12763,#12764,#12765,#12766,#12767,#12768,#12769,#12770,
#12771,#12772,#12773,#12774,#12775,#12776,#12777,#12778,#12779,#12780,#12781,
#12782,#12783,#12784,#12785,#12786,#12787,#12788,#12789,#12790,#12791,#12792,
#12793,#12794,#12795,#12796,#12797,#12798,#12799,#12800,#12801,#12802,#12803,
#12804,#12805,#12806,#12807,#12808,#12809,#12810,#12811),.UNSPECIFIED.,
 .F.,.F.,(4,2,2,2,2,2,2,2,2,2,2,2,2,2,2,2,2,2,2,2,2,2,2,2,2,2,2,2,2,2,2,
2,2,2,2,2,2,2,2,2,2,2,2,2,2,2,2,2,2,2,2,2,2,2,2,2,2,2,2,2,2,2,2,2,2,2,2,
2,2,2,2,2,2,2,2,2,2,2,2,2,2,2,2,2,2,2,2,2,2,2,2,2,2,2,2,2,2,2,2,2,2,2,2,
2,2,2,2,2,2,2,4),(-2.69244553871344,-2.69123390220975,-2.66351216289566,
-2.64661002537132,-2.64144315723391,-2.63818074862069,-2.63515085232453,
-2.63121671987635,-2.62463895963185,-2.57569886226652,-2.49956912753649,
-2.48221194837531,-2.47867692264336,-2.47671503442069,-2.47503737789983,
-2.47291794870337,-2.46876568067321,-2.44209528711233,-2.36786514684491,
-2.34040313139532,-2.32361626754396,-2.31846312957891,-2.31520444280347,
-2.31217459458479,-2.30823569593098,-2.30163938604602,-2.25173873785962,
-2.1739447321752,-2.15886500487573,-2.15547661035761,-2.15354760585632,
-2.15186677261722,-2.14970265785861,-2.14518476561153,-2.0977148457355,
-2.03153183178019,-2.00290916989459,-1.99711495885629,-1.99337526337154,
-1.99037851322074,-1.98697854965591,-1.98118591670721,-1.95745290307746,
-1.87805903643468,-1.83761200191641,-1.83311607563557,-1.83095618476786,
-1.82927563339033,-1.82734348673568,-1.82394164945751,-1.80867084322266,
-1.73105301696905,-1.68126353679017,-1.67466922392996,-1.67073064179387,
-1.66770053911554,-1.6644410886992,-1.65928569983533,-1.6424823358668,-1.61498019083181,
-1.54084252702486,-1.51406022810568,-1.50990364772197,-1.50778324838028,
-1.50610584586776,-1.50414570018307,-1.50061587033473,-1.48332583298547,
-1.40726644914206,-1.35815142411915,-1.35157078979615,-1.3476363163429,
-1.34460700185069,-1.34134606416725,-1.33618335185292,-1.31931176739594,
-1.29165341553657,-1.21889182349642,-1.1910209928546,-1.18682724618086,
-1.18469905141312,-1.18302118856845,-1.18106704238676,-1.17756453369895,
-1.16072947935636,-1.08434016724001,-1.03505412536001,-1.02847011594516,
-1.02453469032697,-1.02150526645892,-1.01824482560543,-1.01308421014322,
-0.99623121663964,-0.96861522334579,-0.895431670283169,-0.867901795449302,
-0.863719413968823,-0.861593638832768,-0.859915942506391,-0.857959975968885,
-0.854449260826696,-0.837479653525979,-0.761187883541069,-0.711973606440921,
-0.705378399957064,-0.701439648905281,-0.698409630433466,-0.69515048248527,
-0.689996026249312,-0.673199831892496,-0.662344722523992),.UNSPECIFIED.);
#160=B_SPLINE_CURVE_WITH_KNOTS('',3,(#12817,#12818,#12819,#12820,#12821,
#12822,#12823,#12824,#12825,#12826,#12827,#12828,#12829,#12830,#12831,#12832,
#12833,#12834,#12835,#12836,#12837,#12838,#12839,#12840,#12841,#12842,#12843,
#12844,#12845,#12846,#12847,#12848,#12849,#12850,#12851,#12852,#12853,#12854,
#12855,#12856,#12857,#12858,#12859,#12860,#12861,#12862,#12863,#12864,#12865,
#12866,#12867,#12868,#12869,#12870,#12871,#12872,#12873,#12874,#12875,#12876,
#12877,#12878,#12879,#12880,#12881,#12882,#12883,#12884,#12885,#12886,#12887,
#12888,#12889,#12890,#12891,#12892,#12893,#12894,#12895,#12896,#12897,#12898,
#12899,#12900,#12901,#12902,#12903,#12904,#12905,#12906,#12907,#12908,#12909,
#12910,#12911,#12912,#12913,#12914,#12915,#12916,#12917,#12918,#12919,#12920,
#12921,#12922,#12923,#12924,#12925,#12926,#12927,#12928,#12929,#12930,#12931,
#12932,#12933,#12934,#12935,#12936,#12937,#12938,#12939,#12940,#12941,#12942,
#12943,#12944,#12945,#12946,#12947,#12948,#12949,#12950,#12951,#12952,#12953,
#12954,#12955,#12956,#12957,#12958,#12959,#12960,#12961,#12962,#12963,#12964,
#12965,#12966,#12967,#12968,#12969,#12970,#12971,#12972,#12973,#12974),
 .UNSPECIFIED.,.F.,.F.,(4,2,2,2,2,2,2,2,2,2,2,2,2,2,2,2,2,2,2,2,2,2,2,2,
2,2,2,2,2,2,2,2,2,2,2,2,2,2,2,2,2,2,2,2,2,2,2,2,2,2,2,2,2,2,2,2,2,2,2,2,
2,2,2,2,2,2,2,2,2,2,2,2,2,2,2,2,2,2,4),(-1.36988642038638,-1.3413112663451,
-1.31332639502017,-1.30912817643698,-1.30699868518289,-1.30532029240606,
-1.30336605794606,-1.29986467780207,-1.28305909352352,-1.20662448920358,
-1.15736774933564,-1.15078323832296,-1.14684710852722,-1.14381689651347,
-1.14055535841533,-1.13539245967217,-1.11852678218158,-1.09088358878178,
-1.01805450344349,-0.990246337496509,-0.986053908400624,-0.983925649917715,
-0.982247352285227,-0.980292221850595,-0.976786736535938,-0.959913668674745,
-0.883529239114067,-0.834296324460669,-0.827712286680746,-0.823776293781452,
-0.820746101811455,-0.817484501228151,-0.812321324405555,-0.795453133645105,
-0.767804185329178,-0.695035676092615,-0.667178651308371,-0.662984483009059,
-0.660855853517954,-0.659177526655734,-0.657222664648347,-0.653718411777061,
-0.636865656306205,-0.560466115236699,-0.511225947278959,-0.50464176233137,
-0.500705725818408,-0.497675526209257,-0.494413942951445,-0.489250848012482,
-0.47238341260582,-0.444736199326516,-0.372935203092716,-0.344155914948134,
-0.339933756986813,-0.337799177424309,-0.336208633012441,-0.334334307168588,
-0.332334879940176,-0.329294205028423,-0.323654757567015,-0.310233371681277,
-0.208930142592438,-0.18583772763581,-0.179896465594955,-0.176428242222843,
-0.173436881472165,-0.169787214674185,-0.162839031221035,-0.11426220036506,
-0.0308869772400612,-0.0196703223883601,-0.0162071716242147,-0.0142404761879752,
-0.0125638474888604,-0.0109390323766698,-0.00886278152393431,-0.00528731446874136,
-0.000961764280122457),.UNSPECIFIED.);
#161=B_SPLINE_CURVE_WITH_KNOTS('',3,(#12975,#12976,#12977,#12978,#12979,
#12980,#12981,#12982,#12983,#12984,#12985,#12986,#12987,#12988,#12989,#12990,
#12991,#12992,#12993,#12994,#12995,#12996,#12997,#12998,#12999,#13000,#13001,
#13002,#13003,#13004,#13005,#13006,#13007,#13008,#13009,#13010,#13011,#13012,
#13013,#13014,#13015,#13016,#13017,#13018,#13019,#13020,#13021,#13022,#13023,
#13024,#13025,#13026,#13027,#13028,#13029,#13030,#13031,#13032,#13033,#13034,
#13035,#13036,#13037,#13038,#13039,#13040,#13041,#13042,#13043,#13044,#13045,
#13046,#13047,#13048,#13049,#13050,#13051,#13052,#13053,#13054,#13055,#13056,
#13057,#13058,#13059,#13060,#13061,#13062,#13063,#13064,#13065,#13066,#13067,
#13068),.UNSPECIFIED.,.F.,.F.,(4,2,2,2,2,2,2,2,2,2,2,2,2,2,2,2,2,2,2,2,
2,2,2,2,2,2,2,2,2,2,2,2,2,2,2,2,2,2,2,2,2,2,2,2,2,2,4),(-4.06143253580346,
-3.96549119249435,-3.9382033737247,-3.92149246432343,-3.91634736999491,
-3.91309020656234,-3.91005930184858,-3.90611550026312,-3.89950314368999,
-3.83153907990166,-3.76477803466754,-3.75874524557317,-3.75555607946893,
-3.7534952994355,-3.75157479538124,-3.75156849042742,-3.75156209358517,
-3.75155560294987,-3.7515490166095,-3.75154233261846,-3.7515355489364,-3.7515286634698,
-3.75152167405901,-3.75151457851469,-3.75150737455215,-3.74987537495363,
-3.74774297096556,-3.7435299674707,-3.71512361309314,-3.64275295956895,
-3.61528600507965,-3.59849634827436,-3.59334238005485,-3.5900831563305,
-3.58705279448121,-3.58311319904763,-3.57651562420591,-3.52656638707188,
-3.44833232271012,-3.43373212251742,-3.43037692763681,-3.42845490975064,
-3.42677231646694,-3.4245955666775,-3.4210563496417,-3.40040424022381,-3.40022159451442),
 .UNSPECIFIED.);
#162=B_SPLINE_CURVE_WITH_KNOTS('',3,(#13070,#13071,#13072,#13073,#13074,
#13075,#13076,#13077,#13078,#13079,#13080,#13081,#13082,#13083,#13084,#13085,
#13086,#13087,#13088,#13089,#13090,#13091,#13092,#13093,#13094,#13095,#13096,
#13097,#13098,#13099,#13100,#13101,#13102,#13103,#13104,#13105,#13106,#13107,
#13108,#13109,#13110,#13111,#13112,#13113,#13114,#13115,#13116,#13117,#13118,
#13119,#13120,#13121,#13122,#13123,#13124,#13125,#13126,#13127,#13128,#13129,
#13130,#13131,#13132,#13133,#13134,#13135,#13136,#13137,#13138,#13139,#13140,
#13141,#13142,#13143,#13144,#13145,#13146,#13147,#13148,#13149,#13150,#13151,
#13152,#13153,#13154,#13155,#13156,#13157,#13158,#13159,#13160,#13161,#13162,
#13163,#13164,#13165,#13166,#13167,#13168,#13169,#13170,#13171,#13172,#13173,
#13174,#13175,#13176,#13177,#13178,#13179,#13180,#13181,#13182,#13183,#13184,
#13185,#13186,#13187,#13188,#13189,#13190,#13191),.UNSPECIFIED.,.F.,.F.,
(4,2,2,2,2,2,2,2,2,2,2,2,2,2,2,2,2,2,2,2,2,2,2,2,2,2,2,2,2,2,2,2,2,2,2,
2,2,2,2,2,2,2,2,2,2,2,2,2,2,2,2,2,2,2,2,2,2,2,2,2,4),(-0.662344722523992,
-0.645714028626579,-0.571423472767882,-0.544750670504654,-0.540598227240143,
-0.538478802736249,-0.536801540409405,-0.534840810959558,-0.531308250736471,
-0.513971430648279,-0.437946925193404,-0.388871653187486,-0.382276442410484,
-0.378337696144331,-0.375307685860361,-0.375236453617864,-0.375175001757771,
-0.375121980981308,-0.375076228319364,-0.375036741775316,-0.37500265825663,
-0.374973234339956,-0.374937579532359,-0.374903097779416,-0.374869745847379,
-0.3748374835443,-0.374806272195281,-0.374776074601791,-0.374746854978714,
-0.374718578900171,-0.374691213247298,-0.37466472616437,-0.374639087009157,
-0.374614268603377,-0.374590244897587,-0.374566984420498,-0.374544460938557,
-0.374522649215573,-0.371071741422611,-0.364964378064538,-0.357446145143455,
-0.34168481445426,-0.295056650901346,-0.226075013085308,-0.218917170937421,
-0.216228308672131,-0.214630814899865,-0.212916245490462,-0.210521815706478,
-0.204728045970659,-0.177557726175298,-0.110034475114551,-0.0908275066279576,
-0.0641104113689985,-0.058437561695102,-0.0547350451309201,-0.0517409172081973,
-0.0489229383257218,-0.0455619196258216,-0.0406606372590674,-0.000962269056679762),
 .UNSPECIFIED.);
#163=B_SPLINE_CURVE_WITH_KNOTS('',3,(#13192,#13193,#13194,#13195,#13196,
#13197,#13198,#13199),.UNSPECIFIED.,.F.,.F.,(4,1,1,1,1,4),(28.2743413277526,
28.6142964377282,29.6142424500796,30.6141884624309,31.6141344747823,32.5106472410873),
 .UNSPECIFIED.);
#164=B_SPLINE_CURVE_WITH_KNOTS('',3,(#13204,#13205,#13206,#13207,#13208,
#13209,#13210,#13211,#13212,#13213,#13214,#13215,#13216,#13217,#13218,#13219,
#13220,#13221,#13222,#13223,#13224,#13225,#13226,#13227,#13228,#13229,#13230,
#13231,#13232,#13233,#13234,#13235,#13236,#13237,#13238,#13239,#13240,#13241,
#13242,#13243,#13244,#13245,#13246,#13247,#13248,#13249,#13250,#13251,#13252,
#13253,#13254,#13255,#13256,#13257,#13258,#13259,#13260,#13261,#13262,#13263,
#13264,#13265,#13266,#13267,#13268,#13269,#13270,#13271,#13272,#13273,#13274,
#13275,#13276,#13277,#13278,#13279,#13280,#13281,#13282,#13283,#13284,#13285,
#13286,#13287,#13288,#13289,#13290,#13291,#13292,#13293,#13294,#13295,#13296,
#13297,#13298,#13299,#13300,#13301,#13302,#13303,#13304,#13305,#13306,#13307,
#13308,#13309,#13310,#13311,#13312,#13313,#13314,#13315,#13316,#13317,#13318,
#13319,#13320,#13321,#13322,#13323,#13324,#13325,#13326,#13327,#13328,#13329,
#13330,#13331,#13332,#13333,#13334,#13335,#13336,#13337,#13338,#13339,#13340,
#13341,#13342,#13343,#13344,#13345,#13346,#13347,#13348,#13349,#13350,#13351,
#13352,#13353,#13354,#13355,#13356,#13357,#13358,#13359,#13360,#13361,#13362,
#13363,#13364,#13365,#13366,#13367,#13368,#13369,#13370,#13371,#13372,#13373,
#13374,#13375,#13376,#13377,#13378,#13379,#13380,#13381,#13382,#13383,#13384,
#13385,#13386,#13387,#13388,#13389,#13390,#13391,#13392,#13393,#13394,#13395,
#13396,#13397,#13398,#13399,#13400,#13401,#13402,#13403,#13404,#13405,#13406,
#13407,#13408,#13409,#13410,#13411,#13412,#13413,#13414,#13415,#13416,#13417,
#13418,#13419,#13420,#13421,#13422,#13423),.UNSPECIFIED.,.F.,.F.,(4,2,2,
2,2,2,2,2,2,2,2,2,2,2,2,2,2,2,2,2,2,2,2,2,2,2,2,2,2,2,2,2,2,2,2,2,2,2,2,
2,2,2,2,2,2,2,2,2,2,2,2,2,2,2,2,2,2,2,2,2,2,2,2,2,2,2,2,2,2,2,2,2,2,2,2,
2,2,2,2,2,2,2,2,2,2,2,2,2,2,2,2,2,2,2,2,2,2,2,2,2,2,2,2,2,2,2,2,2,2,4),
(-3.39981704860417,-3.39949957029591,-3.39290308880973,-3.34363862625196,
-3.26713372109305,-3.25038713773088,-3.24688975491302,-3.24493660514252,
-3.24325842520933,-3.24112829123458,-3.23692603631769,-3.20879373891644,
-3.13643276223271,-3.10876845785778,-3.09189253049485,-3.086729023892,-3.08346767212296,
-3.08043802567777,-3.0765031855718,-3.06992200454182,-3.02080523060401,
-2.94465027400736,-2.92742144649204,-2.92389489709134,-2.92193531909049,
-2.92025769523073,-2.91813606062682,-2.91397398964407,-2.88703691376175,
-2.81316510203951,-2.78565562204065,-2.76884704110681,-2.76369076189058,
-2.76043088517301,-2.75740047479573,-2.75346161034759,-2.74686701186692,
-2.69708932605819,-2.61938469249513,-2.60415005598616,-2.60075023644575,
-2.59881831473613,-2.59713716814004,-2.59497555505549,-2.59148693020392,
-2.57183182725261,-2.56242134371727,-2.49040724573827,-2.4627089495513,
-2.44581759615135,-2.44065197954643,-2.43738989560931,-2.43435998316739,
-2.43042538520751,-2.42384590304496,-2.37484858952389,-2.29892511217508,
-2.2813583025512,-2.27781168297495,-2.27584759086462,-2.27417016450779,
-2.27205396912217,-2.26791801437609,-2.24170629106371,-2.16585675567565,
-2.13911703470754,-2.12264675106471,-2.11752773573311,-2.11427580573156,
-2.11124192428133,-2.10728302503174,-2.10062041294131,-2.03647708621462,
-2.03071903932308,-1.96359321873984,-1.95657860119534,-1.95391099896981,
-1.95231722997155,-1.95059884869207,-1.94818612630463,-1.9422851200763,
-1.91415533048361,-1.88888017302048,-1.80868427644457,-1.79808778465268,
-1.7936350751821,-1.79083545880277,-1.78776045094286,-1.78349287729285,
-1.77324670208299,-1.72658686968809,-1.67283875181467,-1.66374855757199,
-1.63636339041546,-1.63218519025583,-1.63005996735404,-1.62838190255909,
-1.62642455720781,-1.62290890819997,-1.60586727707371,-1.52960738044998,
-1.48043483245754,-1.47385200532895,-1.46991636613453,-1.46688623012685,
-1.46362447666781,-1.45846060352996,-1.44158606679677,-1.41392256520755,
-1.36988642038638),.UNSPECIFIED.);
#165=B_SPLINE_CURVE_WITH_KNOTS('',3,(#13425,#13426,#13427,#13428,#13429,
#13430),.UNSPECIFIED.,.F.,.F.,(4,1,1,4),(32.5106472410873,32.6140804871337,
33.614026499485,34.5575121440499),.UNSPECIFIED.);
#166=B_SPLINE_CURVE_WITH_KNOTS('',3,(#13431,#13432,#13433,#13434,#13435,
#13436,#13437,#13438,#13439,#13440,#13441,#13442,#13443,#13444,#13445,#13446,
#13447,#13448,#13449,#13450,#13451,#13452,#13453,#13454,#13455,#13456,#13457,
#13458,#13459,#13460,#13461,#13462,#13463,#13464,#13465,#13466,#13467,#13468,
#13469,#13470,#13471,#13472,#13473,#13474,#13475,#13476,#13477,#13478,#13479,
#13480,#13481,#13482,#13483,#13484,#13485,#13486,#13487,#13488,#13489,#13490,
#13491,#13492,#13493,#13494,#13495,#13496,#13497,#13498,#13499,#13500,#13501,
#13502,#13503,#13504,#13505,#13506,#13507,#13508,#13509,#13510,#13511,#13512,
#13513,#13514,#13515,#13516,#13517,#13518,#13519,#13520,#13521,#13522,#13523,
#13524,#13525,#13526,#13527,#13528,#13529,#13530,#13531,#13532,#13533,#13534,
#13535,#13536,#13537,#13538,#13539,#13540,#13541,#13542,#13543,#13544,#13545,
#13546,#13547,#13548,#13549,#13550,#13551,#13552,#13553,#13554,#13555,#13556,
#13557,#13558,#13559,#13560,#13561,#13562,#13563,#13564,#13565,#13566,#13567,
#13568,#13569,#13570,#13571,#13572,#13573,#13574,#13575,#13576,#13577,#13578,
#13579,#13580,#13581,#13582,#13583,#13584,#13585,#13586,#13587,#13588,#13589,
#13590,#13591,#13592),.UNSPECIFIED.,.F.,.F.,(4,2,2,2,2,2,2,2,2,2,2,2,2,
2,2,2,2,2,2,2,2,2,2,2,2,2,2,2,2,2,2,2,2,2,2,2,2,2,2,2,2,2,2,2,2,2,2,2,2,
2,2,2,2,2,2,2,2,2,2,2,2,2,2,2,2,2,2,2,2,2,2,2,2,2,2,2,2,2,2,2,4),(-4.06085147293434,
-4.05310077188983,-4.04796490762521,-4.04572245654519,-4.04404186582043,
-4.04244042015484,-4.04083738496685,-4.03857436223626,-4.03249414860606,
-4.02032878775457,-3.93337662315455,-3.90664620310083,-3.89018244347752,
-3.88506615529543,-3.88181614393027,-3.87878418869646,-3.87482800649026,
-3.86817044713076,-3.80212119708593,-3.74694624012344,-3.73306234460286,
-3.72728776079619,-3.72419632428553,-3.72217634002965,-3.72028936261388,
-3.71867837800603,-3.71655666347782,-3.71225238564042,-3.68268555244652,
-3.61176490728404,-3.58415659727521,-3.56730666185997,-3.56214739635258,
-3.55888789026005,-3.55585939005812,-3.55192524019188,-3.54534348072126,
-3.49610042606097,-3.41978453366031,-3.40282543481444,-3.39931602836641,
-3.3973606943214,-3.39568345178764,-3.3935581594255,-3.38937649745657,-3.36183891339592,
-3.28874653477381,-3.26114796949512,-3.24430200803514,-3.23914298662774,
-3.23588341051888,-3.23285469050179,-3.22892003534876,-3.22233694632319,
-3.17304358878905,-3.0966243044284,-3.07979763755673,-3.07629610439543,
-3.07434241718201,-3.07266488956438,-3.07053705264485,-3.06634379496547,
-3.03846243566354,-2.96579113436638,-2.938149403629,-2.9212843159247,-2.91612299369249,
-2.91286278311782,-2.90983403881386,-2.90590015445412,-2.89932012257902,
-2.85019655859923,-2.77412278613023,-2.75681775538367,-2.7532874611796,
-2.7513274383532,-2.74965044806575,-2.74753094915117,-2.74337707861589,
-2.71664512289895,-2.69231343346385),.UNSPECIFIED.);
#167=B_SPLINE_CURVE_WITH_KNOTS('',3,(#13598,#13599,#13600,#13601,#13602,
#13603,#13604,#13605,#13606,#13607,#13608,#13609,#13610,#13611,#13612,#13613,
#13614,#13615,#13616,#13617,#13618,#13619,#13620,#13621,#13622,#13623,#13624,
#13625,#13626,#13627,#13628,#13629,#13630,#13631,#13632,#13633,#13634,#13635,
#13636,#13637,#13638,#13639,#13640,#13641,#13642,#13643,#13644,#13645,#13646,
#13647,#13648,#13649,#13650,#13651,#13652,#13653,#13654,#13655,#13656,#13657,
#13658,#13659,#13660,#13661,#13662,#13663,#13664,#13665,#13666,#13667,#13668,
#13669,#13670,#13671,#13672,#13673,#13674,#13675,#13676,#13677,#13678,#13679,
#13680,#13681,#13682,#13683,#13684,#13685,#13686,#13687,#13688,#13689,#13690,
#13691,#13692,#13693,#13694,#13695,#13696,#13697,#13698,#13699,#13700,#13701,
#13702,#13703,#13704,#13705,#13706,#13707,#13708,#13709,#13710,#13711,#13712,
#13713,#13714,#13715,#13716,#13717,#13718,#13719,#13720,#13721,#13722,#13723,
#13724,#13725,#13726,#13727,#13728,#13729,#13730,#13731,#13732,#13733,#13734,
#13735,#13736,#13737,#13738,#13739,#13740,#13741,#13742,#13743,#13744,#13745,
#13746,#13747,#13748,#13749,#13750,#13751,#13752,#13753,#13754,#13755,#13756,
#13757,#13758,#13759,#13760,#13761,#13762,#13763,#13764,#13765,#13766,#13767,
#13768,#13769,#13770,#13771,#13772,#13773,#13774,#13775,#13776,#13777,#13778,
#13779),.UNSPECIFIED.,.F.,.F.,(4,2,2,2,2,2,2,2,2,2,2,2,2,2,2,2,2,2,2,2,
2,2,2,2,2,2,2,2,2,2,2,2,2,2,2,2,2,2,2,2,2,2,2,2,2,2,2,2,2,2,2,2,2,2,2,2,
2,2,2,2,2,2,2,2,2,2,2,2,2,2,2,2,2,2,2,2,2,2,2,2,2,2,2,2,2,2,2,2,2,2,4),
(-1.36989260040055,-1.34694907025288,-1.29727439722468,-1.29068106761255,
-1.286742178582,-1.2837113098679,-1.28045050923884,-1.27529185373621,-1.25846753342456,
-1.23092008416594,-1.15715155332722,-1.13007914422047,-1.12591148078631,
-1.12378838841277,-1.12211033476853,-1.12015107721843,-1.11662718200838,
-1.09945141006572,-1.02328098131251,-0.974151816281154,-0.96756931407155,
-0.96363357310733,-0.960603185648537,-0.957340990987224,-0.952176055765177,
-0.935294788795801,-0.907616928940878,-0.835127854039516,-0.80703471412696,
-0.802832671510397,-0.800702246102006,-0.799023633445816,-0.797069735581214,
-0.793570427280163,-0.776802713138018,-0.700331202766069,-0.651082868466669,
-0.644482445262207,-0.640541479382043,-0.637510273701122,-0.634250350689317,
-0.62909572183803,-0.61230804644454,-0.584844443998596,-0.510423746113522,
-0.48384351450654,-0.479693475653538,-0.477574144930029,-0.475896353579631,
-0.473934272881937,-0.470397444343366,-0.453002478716234,-0.376989927622464,
-0.327967436876231,-0.320789114192507,-0.31701197919373,-0.314077215359215,
-0.314011445492452,-0.31395001612433,-0.313892464978884,-0.313838393819533,
-0.313787460593142,-0.313739368673774,-0.313693859328444,-0.313650705654848,
-0.313609707688398,-0.313570688401014,-0.313533490397462,-0.313497973192461,
-0.313464010937888,-0.313431490500467,-0.313400309848774,-0.313370376705422,
-0.313341607360951,-0.313313925675485,-0.309734378318534,-0.305877998963111,
-0.288584007343764,-0.259951770413244,-0.217139399379979,-0.161104772996814,
-0.156695254884214,-0.154551761741178,-0.15287212300594,-0.150927600882317,
-0.147470983225329,-0.131383103492649,-0.0543953119851398,-0.0142431875939723,
-0.00563614058459413,-0.000962618911395125),.UNSPECIFIED.);
#168=B_SPLINE_CURVE_WITH_KNOTS('',3,(#13780,#13781,#13782,#13783,#13784,
#13785,#13786,#13787,#13788,#13789,#13790,#13791,#13792,#13793,#13794,#13795,
#13796,#13797,#13798,#13799,#13800,#13801,#13802,#13803,#13804,#13805,#13806,
#13807,#13808,#13809,#13810,#13811,#13812,#13813,#13814,#13815,#13816,#13817,
#13818,#13819,#13820,#13821,#13822,#13823,#13824,#13825,#13826,#13827,#13828,
#13829,#13830,#13831,#13832,#13833,#13834,#13835,#13836,#13837,#13838,#13839,
#13840,#13841,#13842,#13843,#13844,#13845,#13846,#13847,#13848,#13849,#13850,
#13851,#13852,#13853,#13854,#13855,#13856,#13857),.UNSPECIFIED.,.F.,.F.,
(4,2,2,2,2,2,2,2,2,2,2,2,2,2,2,2,2,2,2,2,2,2,2,2,2,2,2,2,2,2,2,2,2,2,2,
2,2,2,4),(-4.0609098086769,-4.05711133593753,-4.05417360536516,-4.05128946276244,
-4.04842506637434,-4.04362140952887,-4.03084245516691,-3.93391530616202,
-3.90084440751831,-3.89442701347254,-3.89193235729023,-3.89019869557731,
-3.88862368915904,-3.88605254837563,-3.87962813169656,-3.80516967931925,
-3.74159650188201,-3.7365006198925,-3.7330591784387,-3.72977770511242,-3.72685566977004,
-3.72308032737714,-3.71590642563688,-3.66684648587034,-3.59076004029415,
-3.57345066016846,-3.56991965018618,-3.5679592390965,-3.56628191276532,
-3.56416194845147,-3.56000702082474,-3.53325930510304,-3.4591499057468,
-3.43167510792401,-3.41488225249231,-3.40972809161283,-3.40646892852742,
-3.40343874917258,-3.39981704860417),.UNSPECIFIED.);
#169=B_SPLINE_CURVE_WITH_KNOTS('',3,(#13858,#13859,#13860,#13861,#13862,
#13863,#13864,#13865,#13866,#13867,#13868,#13869,#13870,#13871,#13872,#13873,
#13874,#13875,#13876,#13877,#13878,#13879,#13880,#13881,#13882,#13883,#13884,
#13885,#13886,#13887,#13888,#13889,#13890,#13891,#13892,#13893,#13894,#13895,
#13896,#13897,#13898,#13899,#13900,#13901,#13902,#13903,#13904,#13905,#13906,
#13907,#13908,#13909,#13910,#13911,#13912,#13913,#13914,#13915,#13916,#13917,
#13918,#13919,#13920,#13921,#13922,#13923,#13924,#13925,#13926,#13927,#13928,
#13929,#13930,#13931,#13932,#13933,#13934,#13935,#13936,#13937,#13938,#13939,
#13940,#13941,#13942,#13943,#13944,#13945,#13946,#13947,#13948,#13949,#13950,
#13951,#13952,#13953,#13954,#13955,#13956,#13957,#13958,#13959,#13960,#13961,
#13962,#13963,#13964,#13965,#13966,#13967,#13968,#13969,#13970,#13971,#13972,
#13973,#13974,#13975,#13976,#13977,#13978,#13979,#13980,#13981,#13982,#13983,
#13984,#13985,#13986,#13987,#13988,#13989,#13990,#13991,#13992,#13993,#13994,
#13995,#13996,#13997,#13998,#13999,#14000,#14001,#14002,#14003,#14004,#14005,
#14006,#14007,#14008,#14009,#14010,#14011,#14012,#14013,#14014,#14015,#14016,
#14017,#14018,#14019,#14020,#14021,#14022,#14023,#14024,#14025,#14026,#14027,
#14028,#14029,#14030,#14031,#14032,#14033,#14034,#14035,#14036,#14037,#14038,
#14039,#14040,#14041,#14042,#14043,#14044,#14045,#14046,#14047,#14048,#14049,
#14050,#14051,#14052,#14053,#14054,#14055,#14056,#14057,#14058,#14059,#14060,
#14061,#14062,#14063,#14064,#14065,#14066,#14067,#14068,#14069),
 .UNSPECIFIED.,.F.,.F.,(4,2,2,2,2,2,2,2,2,2,2,2,2,2,2,2,2,2,2,2,2,2,2,2,
2,2,2,2,2,2,2,2,2,2,2,2,2,2,2,2,2,2,2,2,2,2,2,2,2,2,2,2,2,2,2,2,2,2,2,2,
2,2,2,2,2,2,2,2,2,2,2,2,2,2,2,2,2,2,2,2,2,2,2,2,2,2,2,2,2,2,2,2,2,2,2,2,
2,2,2,2,2,2,2,2,2,4),(-2.69231343346385,-2.64250090796024,-2.61502009310778,
-2.59822504553809,-2.59307125462505,-2.58981258871412,-2.58678306006822,
-2.58284500332925,-2.57625103693778,-2.52643937039689,-2.44876246795497,
-2.4335256364613,-2.43012637766502,-2.42819494839645,-2.42651435251194,
-2.42435364374961,-2.41985377925528,-2.37059577266759,-2.32147112749855,
-2.29267881511926,-2.27531589822419,-2.27010010604013,-2.26682753811948,
-2.26380238651174,-2.25989439124412,-2.25340399660443,-2.2083829963703,
-2.14090920941316,-2.1141736347455,-2.10842901595149,-2.10604276362931,
-2.10432963063252,-2.10272997071654,-2.10003013447172,-2.09280039695301,
-2.03153620018936,-1.961826828632,-1.95076205203216,-1.94623309039102,-1.94342036938971,
-1.94035875644004,-1.93616045256383,-1.92631918996058,-1.8830810832417,
-1.80824312733514,-1.78825875186903,-1.7847535240704,-1.78258718618012,
-1.78090593238775,-1.7789779189676,-1.77559458578027,-1.76059050459986,
-1.68275474821951,-1.63289141875531,-1.62629611977262,-1.62235743848731,
-1.61932754688473,-1.61606860761162,-1.61091463562352,-1.5941214073392,
-1.56664193409925,-1.49231135303828,-1.46567075175513,-1.46151963551514,
-1.45940055901531,-1.45772339337683,-1.45576256705092,-1.45222934083547,
-1.43487944453747,-1.358867986863,-1.3097724587627,-1.30319234920908,-1.29925808218646,
-1.29622886413424,-1.2929679686192,-1.28780519123183,-1.2709321980056,-1.24327018294436,
-1.17057353209847,-1.14265439142622,-1.1384591123928,-1.13633060376794,
-1.13465273026236,-1.13269883987765,-1.12919745761532,-1.11238054035069,
-1.03597847812415,-0.986689714546489,-0.980105733530443,-0.976170336867778,
-0.973140941759397,-0.969880537869576,-0.964719992859611,-0.947867318275063,
-0.920251879620666,-0.847074944040324,-0.819542446406734,-0.815360019889002,
-0.813234248561001,-0.811556582967808,-0.809600692896254,-0.80609015138467,
-0.789122092021607,-0.712831953229946,-0.663619336930725,-0.662240502390468),
 .UNSPECIFIED.);
#170=B_SPLINE_CURVE_WITH_KNOTS('',3,(#14074,#14075,#14076,#14077,#14078,
#14079,#14080,#14081,#14082,#14083,#14084,#14085,#14086,#14087,#14088,#14089,
#14090,#14091,#14092,#14093,#14094,#14095,#14096,#14097,#14098,#14099,#14100,
#14101,#14102,#14103,#14104,#14105,#14106,#14107,#14108,#14109,#14110,#14111,
#14112,#14113,#14114,#14115,#14116,#14117,#14118,#14119,#14120,#14121,#14122,
#14123,#14124,#14125,#14126,#14127,#14128,#14129,#14130,#14131,#14132,#14133,
#14134,#14135,#14136,#14137,#14138,#14139,#14140,#14141,#14142,#14143,#14144,
#14145,#14146,#14147,#14148,#14149,#14150,#14151,#14152,#14153,#14154,#14155,
#14156,#14157,#14158,#14159,#14160,#14161,#14162,#14163,#14164,#14165,#14166,
#14167,#14168,#14169,#14170,#14171,#14172,#14173,#14174,#14175,#14176,#14177,
#14178,#14179,#14180,#14181,#14182,#14183,#14184,#14185,#14186,#14187,#14188,
#14189,#14190,#14191,#14192,#14193,#14194,#14195,#14196,#14197,#14198,#14199,
#14200,#14201,#14202,#14203,#14204,#14205,#14206,#14207,#14208,#14209,#14210,
#14211,#14212,#14213,#14214,#14215,#14216,#14217,#14218,#14219,#14220,#14221,
#14222,#14223,#14224,#14225,#14226,#14227,#14228,#14229,#14230,#14231,#14232,
#14233,#14234,#14235,#14236,#14237,#14238,#14239,#14240,#14241,#14242,#14243,
#14244,#14245,#14246,#14247,#14248,#14249,#14250,#14251,#14252,#14253,#14254,
#14255,#14256,#14257,#14258,#14259,#14260,#14261,#14262,#14263,#14264,#14265,
#14266,#14267,#14268,#14269,#14270,#14271,#14272,#14273,#14274,#14275,#14276,
#14277,#14278,#14279,#14280,#14281,#14282,#14283,#14284,#14285,#14286,#14287,
#14288,#14289,#14290,#14291,#14292,#14293,#14294,#14295,#14296,#14297,#14298,
#14299,#14300,#14301),.UNSPECIFIED.,.F.,.F.,(4,2,2,2,2,2,2,2,2,2,2,2,2,
2,2,2,2,2,2,2,2,2,2,2,2,2,2,2,2,2,2,2,2,2,2,2,2,2,2,2,2,2,2,2,2,2,2,2,2,
2,2,2,2,2,2,2,2,2,2,2,2,2,2,2,2,2,2,2,2,2,2,2,2,2,2,2,2,2,2,2,2,2,2,2,2,
2,2,2,2,2,2,2,2,2,2,2,2,2,2,2,2,2,2,2,2,2,2,2,2,2,2,2,2,4),(-3.39991588284246,
-3.39040284696551,-3.38689701771358,-3.38494201102694,-3.38326400840224,
-3.38113637903207,-3.37694595249143,-3.3491808323736,-3.27636701760464,
-3.24874414704973,-3.23188624426278,-3.22672468256399,-3.2234637365705,
-3.22043389940239,-3.21649800573895,-3.20991328716416,-3.16062262439996,
-3.08411107232553,-3.06736478764203,-3.06386724474948,-3.0619139741981,
-3.06023567099159,-3.05810535544347,-3.05390266630649,-3.02576425173291,
-2.95340304389138,-2.92573630206508,-2.90885896452811,-2.90369506419902,
-2.9004334724363,-2.89740360904243,-2.8934684956751,-2.88688687634004,-2.83776838184286,
-2.76161152416422,-2.74437649931954,-2.74084940251167,-2.73888961936069,
-2.73721188076596,-2.73509017907659,-2.73092820990048,-2.70400051020518,
-2.63010853649165,-2.60259890823962,-2.58578991792256,-2.58063335541558,
-2.57737326315395,-2.57434262722422,-2.57040343381606,-2.5638082056094,
-2.51401906798455,-2.43628635191589,-2.42107779675773,-2.41767959355126,
-2.41574794175036,-2.41406661262627,-2.41190421795168,-2.40739823800769,
-2.3658438194634,-2.30700794897804,-2.27953082753528,-2.2627355829291,-2.25758020882409,
-2.2543201675795,-2.2512890950447,-2.24734864596555,-2.24074979664955,-2.19080413950868,
-2.11260225637664,-2.09793948662124,-2.09457925819915,-2.09265584853259,
-2.0909730130786,-2.08879723726757,-2.08526214730072,-2.06470505519974,
-2.03142818364736,-1.94831592242864,-1.93796263568773,-1.93399190062331,
-1.93113525016105,-1.92810055832378,-1.92406894905081,-1.91517481777322,
-1.87941363195954,-1.80918440574648,-1.80004154742277,-1.79251830471457,
-1.7754415385953,-1.77209921129998,-1.76998180359689,-1.7683041530891,-1.76634064031836,
-1.76279720824143,-1.74528870808485,-1.66935766903248,-1.62035207886556,
-1.61377204035047,-1.60983700933843,-1.60680672218784,-1.60354419568562,
-1.59837779704592,-1.58148333137201,-1.55377524021807,-1.48163442798051,
-1.47180014855695,-1.45257718007089,-1.44911104050935,-1.44695605148667,
-1.44527532218127,-1.44333850822202,-1.43991723989069,-1.42437016231373,
-1.36989260040055),.UNSPECIFIED.);
#171=B_SPLINE_CURVE_WITH_KNOTS('',3,(#14303,#14304,#14305,#14306,#14307,
#14308,#14309,#14310,#14311,#14312,#14313,#14314,#14315,#14316,#14317,#14318,
#14319,#14320,#14321,#14322,#14323,#14324,#14325,#14326,#14327,#14328,#14329,
#14330,#14331,#14332,#14333,#14334,#14335,#14336,#14337,#14338,#14339,#14340,
#14341,#14342,#14343,#14344,#14345,#14346,#14347,#14348,#14349,#14350,#14351,
#14352,#14353,#14354,#14355,#14356,#14357,#14358,#14359,#14360,#14361,#14362,
#14363,#14364,#14365,#14366,#14367,#14368,#14369,#14370,#14371,#14372,#14373,
#14374,#14375,#14376,#14377,#14378,#14379,#14380,#14381,#14382),
 .UNSPECIFIED.,.F.,.F.,(4,2,2,2,2,2,2,2,2,2,2,2,2,2,2,2,2,2,2,2,2,2,2,2,
2,2,2,2,2,2,2,2,2,2,2,2,2,2,2,4),(-0.662240502390468,-0.657023929679327,
-0.653085195757008,-0.650055270679035,-0.646796302300343,-0.641642298961981,
-0.624849099321322,-0.597369805596174,-0.523035054525191,-0.496396691937766,
-0.492245623831593,-0.490126544756246,-0.488449362968123,-0.486488501472852,
-0.482955170959465,-0.465603944879306,-0.389592518454238,-0.340518345836509,
-0.333343563923072,-0.329643268468981,-0.326711683522161,-0.323450021335688,
-0.320037521603015,-0.308539299509218,-0.250181783322074,-0.176853417000301,
-0.170311927293518,-0.167721023336038,-0.166142277370552,-0.16441218979227,
-0.161935838127768,-0.155636135072824,-0.12373585073483,-0.0337146530897698,
-0.023749165330492,-0.0122727340884673,-0.0077672268730303,-0.004928086174024,
-0.00247151203102761,-0.000962250865292755),.UNSPECIFIED.);
#172=B_SPLINE_CURVE_WITH_KNOTS('',3,(#14383,#14384,#14385,#14386,#14387,
#14388,#14389,#14390,#14391,#14392,#14393,#14394,#14395,#14396,#14397,#14398,
#14399,#14400,#14401,#14402,#14403,#14404,#14405,#14406,#14407,#14408,#14409,
#14410,#14411,#14412,#14413,#14414,#14415,#14416,#14417,#14418,#14419,#14420,
#14421,#14422,#14423,#14424,#14425,#14426,#14427,#14428,#14429,#14430,#14431,
#14432,#14433,#14434,#14435,#14436,#14437,#14438,#14439,#14440,#14441,#14442,
#14443,#14444,#14445,#14446,#14447,#14448,#14449,#14450,#14451,#14452,#14453,
#14454,#14455,#14456,#14457,#14458,#14459,#14460,#14461,#14462,#14463,#14464,
#14465,#14466,#14467,#14468,#14469,#14470,#14471,#14472,#14473,#14474,#14475,
#14476,#14477,#14478,#14479,#14480,#14481,#14482,#14483,#14484,#14485,#14486,
#14487,#14488,#14489,#14490,#14491,#14492,#14493,#14494,#14495,#14496,#14497,
#14498,#14499,#14500,#14501,#14502,#14503,#14504,#14505,#14506,#14507,#14508,
#14509,#14510,#14511,#14512,#14513,#14514,#14515,#14516,#14517,#14518,#14519,
#14520,#14521,#14522,#14523,#14524,#14525,#14526,#14527,#14528,#14529,#14530,
#14531,#14532,#14533,#14534,#14535,#14536,#14537,#14538,#14539,#14540,#14541,
#14542,#14543,#14544,#14545,#14546,#14547,#14548,#14549,#14550,#14551,#14552,
#14553,#14554,#14555,#14556,#14557,#14558,#14559,#14560,#14561,#14562,#14563,
#14564),.UNSPECIFIED.,.F.,.F.,(4,2,2,2,2,2,2,2,2,2,2,2,2,2,2,2,2,2,2,2,
2,2,2,2,2,2,2,2,2,2,2,2,2,2,2,2,2,2,2,2,2,2,2,2,2,2,2,2,2,2,2,2,2,2,2,2,
2,2,2,2,2,2,2,2,2,2,2,2,2,2,2,2,2,2,2,2,2,2,2,2,2,2,2,2,2,2,2,2,2,2,4),
(-4.06006550870592,-4.0592979539179,-4.05690831414429,-4.04988864926168,
-4.00079261892183,-3.92311550633048,-3.90791900336471,-3.90452337110743,
-3.90259317387311,-3.90091311683915,-3.89875240228628,-3.89425010106067,
-3.85281521416176,-3.79516080279116,-3.75651367782774,-3.74724431336817,
-3.74323583404368,-3.74313274029429,-3.74303270359105,-3.74293529208593,
-3.74284007719896,-3.74274662742569,-3.74265450090998,-3.74256323630275,
-3.74247234116765,-3.74238127681489,-3.74228943786694,-3.74219612378574,
-3.74210049780654,-3.74200152542122,-3.74189787807022,-3.74178777431335,
-3.74166870048804,-3.74153687676995,-3.74141647185602,-3.73854358165865,
-3.73484440097036,-3.72767081526953,-3.6786148649635,-3.60262224632263,
-3.58523119680468,-3.58169640628854,-3.57973566424315,-3.57805914823915,
-3.57594164255294,-3.57179583430777,-3.54526655032527,-3.47087245667017,
-3.44343455577428,-3.42665932795555,-3.4215084437827,-3.41825088115425,
-3.41522187038504,-3.41128376470012,-3.40468812234878,-3.35543216565346,
-3.27903782638549,-3.2621901185483,-3.25868756521093,-3.25673377981595,
-3.25505645985484,-3.25292926179518,-3.24873839710274,-3.22091943381247,
-3.14818227289282,-3.12055035179458,-3.10369004703682,-3.09852959671027,
-3.09526980055343,-3.0922413471849,-3.08830770720035,-3.08172778999415,
-3.03258070930082,-2.95645870697833,-2.93923310378528,-2.93570775579726,
-2.93374893395435,-2.93207202140456,-2.92995140406656,-2.92579170429336,
-2.89888776713552,-2.82498254972042,-2.79747486259023,-2.78066855746512,
-2.77551386788707,-2.77225522429316,-2.76922612439584,-2.76528920487724,
-2.75869842201576,-2.70901924957822,-2.69160338547236),.UNSPECIFIED.);
#173=B_SPLINE_CURVE_WITH_KNOTS('',3,(#14570,#14571,#14572,#14573,#14574,
#14575,#14576,#14577,#14578,#14579,#14580,#14581,#14582,#14583,#14584,#14585,
#14586,#14587,#14588,#14589,#14590,#14591,#14592,#14593,#14594,#14595,#14596,
#14597,#14598,#14599,#14600,#14601,#14602,#14603,#14604,#14605,#14606,#14607,
#14608,#14609,#14610,#14611,#14612,#14613,#14614,#14615,#14616,#14617,#14618,
#14619,#14620,#14621,#14622,#14623,#14624,#14625,#14626,#14627,#14628,#14629,
#14630,#14631,#14632,#14633,#14634,#14635,#14636,#14637,#14638,#14639,#14640,
#14641,#14642,#14643,#14644,#14645,#14646,#14647,#14648,#14649,#14650,#14651,
#14652,#14653,#14654,#14655,#14656,#14657,#14658,#14659,#14660,#14661,#14662,
#14663,#14664,#14665,#14666,#14667,#14668,#14669,#14670,#14671,#14672,#14673,
#14674,#14675,#14676,#14677,#14678,#14679,#14680,#14681,#14682,#14683,#14684,
#14685,#14686,#14687,#14688,#14689,#14690,#14691,#14692,#14693,#14694,#14695,
#14696,#14697,#14698,#14699,#14700,#14701,#14702,#14703,#14704,#14705,#14706,
#14707,#14708,#14709,#14710,#14711,#14712,#14713,#14714,#14715,#14716,#14717,
#14718,#14719,#14720,#14721,#14722,#14723,#14724,#14725),.UNSPECIFIED.,
 .F.,.F.,(4,2,2,2,2,2,2,2,2,2,2,2,2,2,2,2,2,2,2,2,2,2,2,2,2,2,2,2,2,2,2,
2,2,2,2,2,2,2,2,2,2,2,2,2,2,2,2,2,2,2,2,2,2,2,2,2,2,2,2,2,2,2,2,2,2,2,2,
2,2,2,2,2,2,2,2,2,2,4),(-1.36992615419562,-1.29786960198346,-1.27000623472678,
-1.2658121564844,-1.26368361046342,-1.26200536880233,-1.26005062826733,
-1.25654664849401,-1.23969626482832,-1.16329957818781,-1.1140614775962,
-1.10747762566089,-1.10354179120432,-1.10051174888973,-1.09725033664901,
-1.09208751607606,-1.07522100961626,-1.04757535235962,-0.974790884145844,
-0.946951072229813,-0.942757767494469,-0.940629385759145,-0.938951156192367,
-0.936996294856674,-0.933491763576773,-0.916632318306228,-0.8402423289104,
-0.791007413912739,-0.784423623193408,-0.780487805690802,-0.777457764946563,
-0.77419634308704,-0.769033483182266,-0.752166632294715,-0.724520190387477,
-0.651743874951846,-0.623897137704172,-0.619703790814916,-0.617575399580141,
-0.615897168643255,-0.613942312741393,-0.61043780866106,-0.593578828407068,
-0.517188456225025,-0.467953353339218,-0.461369556521858,-0.457433736398397,
-0.454403694235402,-0.451142271438742,-0.445979411307835,-0.429112570946092,
-0.401466157773912,-0.357735009114619,-0.30112070793025,-0.296719915350321,
-0.294578338139885,-0.292899088590012,-0.292892478182276,-0.292885973240311,
-0.292879571660865,-0.292873271404119,-0.292867070494959,-0.292860966976924,
-0.290939922527024,-0.28760362101891,-0.283428771869717,-0.27463130011459,
-0.248962733052717,-0.186448793622971,-0.144654555862752,-0.138251386563788,
-0.13436852232334,-0.131346504133501,-0.128060943473425,-0.122788705748904,
-0.104897435176136,-0.0748538664662228,-0.0009633702098371),
 .UNSPECIFIED.);
#174=B_SPLINE_CURVE_WITH_KNOTS('',3,(#14726,#14727,#14728,#14729,#14730,
#14731,#14732,#14733,#14734,#14735,#14736,#14737,#14738,#14739,#14740,#14741,
#14742,#14743,#14744,#14745,#14746,#14747,#14748,#14749,#14750,#14751,#14752,
#14753,#14754,#14755,#14756,#14757,#14758,#14759,#14760,#14761,#14762,#14763,
#14764,#14765,#14766,#14767,#14768,#14769,#14770,#14771,#14772,#14773,#14774,
#14775,#14776,#14777,#14778,#14779,#14780,#14781,#14782,#14783,#14784,#14785,
#14786,#14787,#14788,#14789,#14790,#14791,#14792,#14793,#14794,#14795,#14796,
#14797,#14798,#14799,#14800,#14801,#14802,#14803,#14804,#14805,#14806,#14807,
#14808,#14809,#14810,#14811,#14812,#14813,#14814,#14815),.UNSPECIFIED.,
 .F.,.F.,(4,2,2,2,2,2,2,2,2,2,2,2,2,2,2,2,2,2,2,2,2,2,2,2,2,2,2,2,2,2,2,
2,2,2,2,2,2,2,2,2,2,2,2,2,4),(-4.06063762530162,-4.03738770533439,-4.03445526959851,
-4.03250078196954,-4.03091014967505,-4.02923446840462,-4.02713968381193,
-4.02386997406795,-4.00790352707352,-3.99522786418767,-3.92512436701015,
-3.89564592231692,-3.87799147570487,-3.87274461236604,-3.86946504639217,
-3.86644189698296,-3.86254831866582,-3.85610745447437,-3.81293127607245,
-3.75042378113196,-3.72575725523217,-3.71718896198902,-3.71309254312229,
-3.709780503098,-3.70787879974509,-3.70787380863913,-3.70786878904772,-3.70786374080227,
-3.70785866372855,-3.70785355758587,-3.70617268426424,-3.70401080379363,
-3.69950564525158,-3.65768203768179,-3.59939529228445,-3.57176226710138,
-3.55490021929956,-3.54973839915619,-3.54647752275402,-3.54344791093525,
-3.53951253812888,-3.53292919354584,-3.48369066638352,-3.40728760675519,
-3.39991588284246),.UNSPECIFIED.);
#175=B_SPLINE_CURVE_WITH_KNOTS('',3,(#14816,#14817,#14818,#14819,#14820,
#14821,#14822,#14823,#14824,#14825,#14826,#14827,#14828,#14829,#14830,#14831,
#14832,#14833,#14834,#14835,#14836,#14837,#14838,#14839,#14840,#14841,#14842,
#14843,#14844,#14845,#14846,#14847,#14848,#14849,#14850,#14851,#14852,#14853,
#14854,#14855,#14856,#14857,#14858,#14859,#14860,#14861,#14862,#14863,#14864,
#14865,#14866,#14867,#14868,#14869,#14870,#14871,#14872,#14873,#14874,#14875,
#14876,#14877,#14878,#14879,#14880,#14881,#14882,#14883,#14884,#14885,#14886,
#14887,#14888,#14889,#14890,#14891,#14892,#14893,#14894,#14895,#14896,#14897,
#14898,#14899,#14900,#14901,#14902,#14903,#14904,#14905,#14906,#14907,#14908,
#14909,#14910,#14911,#14912,#14913,#14914,#14915,#14916,#14917,#14918,#14919,
#14920,#14921,#14922,#14923,#14924,#14925,#14926,#14927,#14928,#14929,#14930,
#14931,#14932,#14933,#14934,#14935,#14936,#14937,#14938,#14939,#14940,#14941,
#14942,#14943,#14944,#14945,#14946,#14947,#14948,#14949,#14950,#14951,#14952,
#14953,#14954,#14955,#14956,#14957,#14958,#14959,#14960,#14961,#14962,#14963,
#14964,#14965,#14966,#14967,#14968,#14969,#14970,#14971,#14972,#14973,#14974,
#14975,#14976,#14977,#14978,#14979,#14980,#14981,#14982,#14983,#14984,#14985,
#14986,#14987,#14988,#14989,#14990,#14991,#14992,#14993,#14994,#14995,#14996,
#14997,#14998,#14999,#15000,#15001,#15002,#15003,#15004,#15005,#15006,#15007,
#15008,#15009,#15010,#15011,#15012,#15013,#15014,#15015,#15016,#15017,#15018,
#15019,#15020,#15021,#15022,#15023,#15024,#15025,#15026,#15027,#15028,#15029,
#15030,#15031,#15032,#15033,#15034,#15035,#15036,#15037,#15038,#15039,#15040,
#15041),.UNSPECIFIED.,.F.,.F.,(4,2,2,2,2,2,2,2,2,2,2,2,2,2,2,2,2,2,2,2,
2,2,2,2,2,2,2,2,2,2,2,2,2,2,2,2,2,2,2,2,2,2,2,2,2,2,2,2,2,2,2,2,2,2,2,2,
2,2,2,2,2,2,2,2,2,2,2,2,2,2,2,2,2,2,2,2,2,2,2,2,2,2,2,2,2,2,2,2,2,2,2,2,
2,2,2,2,2,2,2,2,2,2,2,2,2,2,2,2,2,2,2,2,4),(-2.69160338547236,-2.63169763039443,
-2.61603620327971,-2.6126086148271,-2.61067108797478,-2.60899156713524,
-2.60684056011834,-2.60338555899897,-2.58434312529108,-2.57435193343334,
-2.50224056241301,-2.47454852745384,-2.45766141641091,-2.45249761626397,
-2.44923682113843,-2.44620821005473,-2.44227545821738,-2.4356994332569,
-2.38677994524135,-2.31108733551206,-2.29324310216633,-2.28968164861194,
-2.28771483513348,-2.28603843603407,-2.28392784197441,-2.27981558166157,
-2.25419228103839,-2.17815034654899,-2.15113320638569,-2.13454176865548,
-2.12941052990453,-2.12615680590718,-2.12312540723192,-2.11917569807003,
-2.11254179305805,-2.06060314336006,-2.0302492262792,-1.975946280875,-1.96861215431759,
-1.96589664490868,-1.96429404515234,-1.96258319875142,-1.96020902120597,
-1.954535131085,-1.92842248779088,-1.86059325504999,-1.81529831746807,-1.80880298356115,
-1.80489372650911,-1.80186862656731,-1.7985971393049,-1.79338528459779,
-1.77605625035436,-1.74733766376055,-1.70462100284471,-1.64863944958662,
-1.64423085205556,-1.64208817429198,-1.64040935585446,-1.6384660221207,
-1.63501212653966,-1.61894821253835,-1.54198442551393,-1.49244918587806,
-1.48586115261748,-1.48192487853785,-1.47889571040262,-1.47563643902858,
-1.47047957836215,-1.45365584825761,-1.42610503732193,-1.35238242333136,
-1.32529198141123,-1.32112526146239,-1.31900302705165,-1.3173258530745,
-1.31536788739084,-1.31184700577633,-1.29469998304932,-1.21855437731766,
-1.16939216187519,-1.16281153069785,-1.15887740574886,-1.15584856249118,
-1.15258833187219,-1.14742716450561,-1.13056442768403,-1.10292431826243,
-1.03004854267861,-1.00228710228514,-0.998097491470576,-0.995970370025444,
-0.9942928239992,-0.992338434980571,-0.988833973630052,-0.971960456269705,
-0.895613419525241,-0.846352700140486,-0.839770092228908,-0.835835388658402,
-0.832806452472319,-0.829546469028812,-0.824386432930255,-0.807534018756594,
-0.779917579449145,-0.706800711878549,-0.679232755252589,-0.675049604754214,
-0.6729238583611,-0.671246415025316,-0.669291016990579,-0.665781938503568,
-0.661808055719697),.UNSPECIFIED.);
#176=B_SPLINE_CURVE_WITH_KNOTS('',3,(#15046,#15047,#15048,#15049,#15050,
#15051,#15052,#15053,#15054,#15055,#15056,#15057,#15058,#15059,#15060,#15061,
#15062,#15063,#15064,#15065,#15066,#15067,#15068,#15069,#15070,#15071,#15072,
#15073,#15074,#15075,#15076,#15077,#15078,#15079,#15080,#15081,#15082,#15083,
#15084,#15085,#15086,#15087,#15088,#15089,#15090,#15091,#15092,#15093,#15094,
#15095,#15096,#15097,#15098,#15099,#15100,#15101,#15102,#15103,#15104,#15105,
#15106,#15107,#15108,#15109,#15110,#15111,#15112,#15113,#15114,#15115,#15116,
#15117,#15118,#15119,#15120,#15121,#15122,#15123,#15124,#15125,#15126,#15127,
#15128,#15129,#15130,#15131,#15132,#15133,#15134,#15135,#15136,#15137,#15138,
#15139,#15140,#15141,#15142,#15143,#15144,#15145,#15146,#15147,#15148,#15149,
#15150,#15151,#15152,#15153,#15154,#15155,#15156,#15157,#15158,#15159,#15160,
#15161,#15162,#15163,#15164,#15165,#15166,#15167,#15168,#15169,#15170,#15171,
#15172,#15173,#15174,#15175,#15176,#15177,#15178,#15179,#15180,#15181,#15182,
#15183,#15184,#15185,#15186,#15187,#15188,#15189,#15190,#15191,#15192,#15193,
#15194,#15195,#15196,#15197,#15198,#15199,#15200,#15201,#15202,#15203,#15204,
#15205,#15206,#15207,#15208,#15209,#15210,#15211,#15212,#15213,#15214,#15215,
#15216,#15217,#15218,#15219,#15220,#15221,#15222,#15223,#15224,#15225,#15226,
#15227,#15228,#15229,#15230,#15231,#15232,#15233,#15234,#15235,#15236,#15237,
#15238,#15239,#15240,#15241,#15242,#15243,#15244,#15245,#15246,#15247,#15248,
#15249,#15250,#15251,#15252,#15253,#15254,#15255,#15256,#15257,#15258,#15259,
#15260,#15261,#15262,#15263,#15264,#15265,#15266,#15267,#15268,#15269,#15270,
#15271,#15272,#15273,#15274,#15275,#15276,#15277),.UNSPECIFIED.,.F.,.F.,
(4,2,2,2,2,2,2,2,2,2,2,2,2,2,2,2,2,2,2,2,2,2,2,2,2,2,2,2,2,2,2,2,2,2,2,
2,2,2,2,2,2,2,2,2,2,2,2,2,2,2,2,2,2,2,2,2,2,2,2,2,2,2,2,2,2,2,2,2,2,2,2,
2,2,2,2,2,2,2,2,2,2,2,2,2,2,2,2,2,2,2,2,2,2,2,2,2,2,2,2,2,2,2,2,2,2,2,2,
2,2,2,2,2,2,2,2,4),(-3.39970068703626,-3.38822341450344,-3.37147224508822,
-3.36632248943194,-3.36306416816673,-3.36003342691036,-3.35609160446387,
-3.34948647033446,-3.29976259537378,-3.22214765718618,-3.20681025573698,
-3.20340356533925,-3.20147020024205,-3.19978937757082,-3.19763024820342,
-3.19314012417513,-3.15469551958324,-3.09608666142328,-3.06641567919309,
-3.04867903176444,-3.04342293528804,-3.04014094686719,-3.03711782984798,
-3.03322745010955,-3.02679868926118,-2.98409455781559,-2.9221363862561,
-2.89670505813259,-2.88354629257996,-2.88030061337599,-2.87840278215447,
-2.87671535732535,-2.87453456777442,-2.87090308380529,-2.84834499806466,
-2.84152974728029,-2.77016756950921,-2.72839145468897,-2.72164869208634,
-2.71804209643894,-2.7150805448175,-2.71158648043496,-2.70553332989776,
-2.68114216087857,-2.66895089149459,-2.60260511242225,-2.57465929545017,
-2.56066125965985,-2.55735023382665,-2.5554379177877,-2.55375349146361,
-2.55159693740608,-2.54804776866578,-2.52719625669397,-2.45410663409195,
-2.40571028839893,-2.39876675791672,-2.39511794686555,-2.39241538267134,
-2.38904782324688,-2.38340527241454,-2.36411630727703,-2.27772581888842,
-2.25108164116281,-2.23751202712445,-2.23423365472209,-2.23232848841202,
-2.23064250068112,-2.22847382980477,-2.22488384927387,-2.20319614940122,
-2.18702461353068,-2.10477793037042,-2.08063460603756,-2.07480929135583,
-2.0714012544123,-2.06840411055488,-2.06467272335975,-2.05890804313187,
-2.0307786704277,-1.96685490333648,-1.94420771690159,-1.9161254167198,-1.91192421517328,
-1.90979415316076,-1.90811579447316,-1.90616215509294,-1.90266321770517,
-1.88589553381497,-1.80943727698247,-1.76017008038009,-1.75358565287927,
-1.74964965273988,-1.74661958715082,-1.74335825256084,-1.73819577380495,
-1.72133234459799,-1.69369372928755,-1.62083562102662,-1.59305541313776,
-1.58886407900056,-1.58673611822124,-1.58505792246039,-1.58310275800837,
-1.57959683243826,-1.56271437411727,-1.4863415447981,-1.43711483893621,
-1.43053121675512,-1.4265954499599,-1.42356541899705,-1.42030397884951,
-1.41514102857145,-1.3982733321828,-1.37062494350533,-1.36992615419562),
 .UNSPECIFIED.);
#177=B_SPLINE_CURVE_WITH_KNOTS('',3,(#15279,#15280,#15281,#15282,#15283,
#15284,#15285,#15286,#15287,#15288,#15289,#15290,#15291,#15292,#15293,#15294,
#15295,#15296,#15297,#15298,#15299,#15300,#15301,#15302,#15303,#15304,#15305,
#15306,#15307,#15308,#15309,#15310,#15311,#15312,#15313,#15314,#15315,#15316,
#15317,#15318,#15319,#15320,#15321,#15322,#15323,#15324,#15325,#15326,#15327,
#15328,#15329,#15330,#15331,#15332,#15333,#15334,#15335,#15336,#15337,#15338,
#15339,#15340,#15341,#15342,#15343,#15344,#15345,#15346,#15347,#15348,#15349,
#15350,#15351,#15352,#15353,#15354,#15355,#15356,#15357,#15358,#15359,#15360,
#15361,#15362,#15363,#15364,#15365,#15366,#15367,#15368,#15369,#15370,#15371,
#15372,#15373,#15374,#15375,#15376,#15377,#15378,#15379,#15380,#15381,#15382,
#15383,#15384,#15385,#15386),.UNSPECIFIED.,.F.,.F.,(4,2,2,2,2,2,2,2,2,2,
2,2,2,2,2,2,2,2,2,2,2,2,2,2,2,2,2,2,2,2,2,2,2,2,2,2,2,2,2,2,2,2,2,2,2,2,
2,2,2,2,2,2,2,4),(-0.661808055719697,-0.648832150577172,-0.572541433096579,
-0.523307773563162,-0.516725694804676,-0.512791141391924,-0.509762223683841,
-0.506502164486976,-0.501341804656795,-0.484486508268001,-0.456863486888756,
-0.389214614274023,-0.356439867090687,-0.352056010808638,-0.349918244540708,
-0.348321158104792,-0.348315809881205,-0.348310492428431,-0.34830520551964,
-0.348299948981064,-0.348294722610798,-0.348289526212797,-0.348284359534354,
-0.348279222357803,-0.348274114517763,-0.348269035862146,-0.348263986144369,
-0.348258965155043,-0.348253972718448,-0.346351750232364,-0.343031734571514,
-0.33892635730641,-0.330331700068644,-0.305551107034789,-0.243159137770574,
-0.200065231136631,-0.193627565821907,-0.189735279233183,-0.18671277699546,
-0.183433564530137,-0.178186525865762,-0.160525001770526,-0.131024497779064,
-0.0548895685140513,-0.0425981494905788,-0.0418966775377889,-0.0313058078813465,
-0.028166581753517,-0.0262927986908994,-0.0246670930059718,-0.0230104890773531,
-0.0208364519660099,-0.017373362411351,-0.000961441519558661),
 .UNSPECIFIED.);
#178=B_SPLINE_CURVE_WITH_KNOTS('',3,(#15387,#15388,#15389,#15390,#15391,
#15392,#15393,#15394,#15395,#15396,#15397,#15398,#15399,#15400,#15401,#15402,
#15403,#15404,#15405,#15406,#15407,#15408,#15409,#15410,#15411,#15412,#15413,
#15414,#15415,#15416,#15417,#15418,#15419,#15420,#15421,#15422,#15423,#15424,
#15425,#15426,#15427,#15428,#15429,#15430,#15431,#15432,#15433,#15434,#15435,
#15436,#15437,#15438,#15439,#15440,#15441,#15442,#15443,#15444,#15445,#15446,
#15447,#15448,#15449,#15450,#15451,#15452,#15453,#15454,#15455,#15456,#15457,
#15458,#15459,#15460,#15461,#15462,#15463,#15464,#15465,#15466,#15467,#15468,
#15469,#15470,#15471,#15472,#15473,#15474,#15475,#15476,#15477,#15478,#15479,
#15480,#15481,#15482,#15483,#15484,#15485,#15486,#15487,#15488,#15489,#15490,
#15491,#15492,#15493,#15494,#15495,#15496,#15497,#15498,#15499,#15500,#15501,
#15502,#15503,#15504,#15505,#15506,#15507,#15508,#15509,#15510,#15511,#15512,
#15513,#15514,#15515,#15516,#15517,#15518,#15519,#15520,#15521,#15522,#15523,
#15524,#15525,#15526,#15527,#15528,#15529,#15530),.UNSPECIFIED.,.F.,.F.,
(4,2,2,2,2,2,2,2,2,2,2,2,2,2,2,2,2,2,2,2,2,2,2,2,2,2,2,2,2,2,2,2,2,2,2,
2,2,2,2,2,2,2,2,2,2,2,2,2,2,2,2,2,2,2,2,2,2,2,2,2,2,2,2,2,2,2,2,2,2,2,2,
4),(-4.06154323901497,-3.97971723338825,-3.9409087536146,-3.93161870694837,
-3.92751754463492,-3.92447353549115,-3.92163907437441,-3.91774791945187,
-3.90787067438528,-3.82027383305999,-3.80171307894705,-3.78045720960814,
-3.77270265519819,-3.76888882502671,-3.76579087781818,-3.76392446850604,
-3.76231566211645,-3.76015547690693,-3.75565646608519,-3.71467064316284,
-3.65549872007339,-3.62789111064862,-3.61104151951261,-3.60588231837622,
-3.60262284349152,-3.5995943657568,-3.59566023580679,-3.58907848922892,
-3.53983382886483,-3.46351440828317,-3.44656104949759,-3.44305200892795,
-3.4410967641527,-3.43941952734521,-3.4372941512235,-3.43311205032648,-3.40557409353817,
-3.33248391660804,-3.30488540748622,-3.28803950890903,-3.28288052085286,
-3.2796209690648,-3.27659227388823,-3.27265765418958,-3.26607463149876,
-3.21678235585174,-3.14036513428093,-3.12353665298247,-3.12003502926618,
-3.11808133182462,-3.11640382041477,-3.11427603619539,-3.11008297947165,
-3.08220694854588,-3.00952993261914,-2.98188901256543,-2.96502431710805,
-2.95986306452819,-2.95660288634488,-2.95357416412611,-2.94964029708805,
-2.94306026915623,-2.89393466180563,-2.81785675018311,-2.80055843400905,
-2.79702855490374,-2.79506863194744,-2.79339164691385,-2.79127205197907,
-2.78711768670855,-2.76037130570713,-2.69271526571019),.UNSPECIFIED.);
#179=B_SPLINE_CURVE_WITH_KNOTS('',3,(#15536,#15537,#15538,#15539,#15540,
#15541,#15542,#15543,#15544,#15545,#15546,#15547,#15548,#15549,#15550,#15551,
#15552,#15553,#15554,#15555,#15556,#15557,#15558,#15559,#15560,#15561,#15562,
#15563,#15564,#15565,#15566,#15567,#15568,#15569,#15570,#15571,#15572,#15573,
#15574,#15575,#15576,#15577,#15578,#15579,#15580,#15581,#15582,#15583,#15584,
#15585,#15586,#15587,#15588,#15589,#15590,#15591,#15592,#15593,#15594,#15595,
#15596,#15597,#15598,#15599,#15600,#15601,#15602,#15603,#15604,#15605,#15606,
#15607,#15608,#15609,#15610,#15611,#15612,#15613,#15614,#15615,#15616,#15617,
#15618,#15619,#15620,#15621,#15622,#15623,#15624,#15625,#15626,#15627,#15628,
#15629,#15630,#15631,#15632,#15633,#15634,#15635,#15636,#15637,#15638,#15639,
#15640,#15641,#15642,#15643,#15644,#15645,#15646,#15647,#15648,#15649,#15650,
#15651,#15652,#15653,#15654,#15655,#15656,#15657,#15658,#15659,#15660,#15661,
#15662,#15663,#15664,#15665,#15666,#15667,#15668,#15669,#15670,#15671,#15672,
#15673,#15674,#15675,#15676,#15677),.UNSPECIFIED.,.F.,.F.,(4,2,2,2,2,2,
2,2,2,2,2,2,2,2,2,2,2,2,2,2,2,2,2,2,2,2,2,2,2,2,2,2,2,2,2,2,2,2,2,2,2,2,
2,2,2,2,2,2,2,2,2,2,2,2,2,2,2,2,2,2,2,2,2,2,2,2,2,2,2,2,4),(-1.36961882394012,
-1.30315593555376,-1.25364920307832,-1.24705976090669,-1.24312220915139,
-1.24009179395163,-1.2368309148216,-1.23167092891767,-1.21483149344873,
-1.18724833492873,-1.11382929870891,-1.08649270731871,-1.08231619034621,
-1.08019133305969,-1.07851330353662,-1.07655570765878,-1.07303888099454,
-1.05597737726654,-0.979732518490505,-0.930567441324095,-0.923984792423174,
-0.920049215438583,-0.917019101398693,-0.913757346043541,-0.908593415447113,
-0.891718202841784,-0.864053095476609,-0.791461329552479,-0.763460987737648,
-0.759262283343022,-0.75713269499197,-0.755454302435665,-0.753500156353745,
-0.749999152986304,-0.733199537098949,-0.656760944098597,-0.607501131360064,
-0.6009173033429,-0.596981383293664,-0.59395121668842,-0.590689613147879,
-0.585526367143234,-0.568657372482014,-0.541006517204668,-0.46826047777152,
-0.440385557689011,-0.436190948455384,-0.434062232241406,-0.432383907460957,
-0.430429128763035,-0.426925226197747,-0.410077998389506,-0.333674856318948,
-0.284452516327641,-0.277857575520124,-0.273918413492927,-0.270887737321598,
-0.268085403544718,-0.26354363846413,-0.251056102059236,-0.232524046960948,
-0.196005841666166,-0.120601370192909,-0.114217157975272,-0.111652348357135,
-0.110078217528788,-0.10834273572402,-0.105840673203071,-0.0993779921424752,
-0.0658658239895591,-0.000963213376137151),.UNSPECIFIED.);
#180=B_SPLINE_CURVE_WITH_KNOTS('',3,(#15678,#15679,#15680,#15681,#15682,
#15683,#15684,#15685,#15686,#15687,#15688,#15689,#15690,#15691,#15692,#15693,
#15694,#15695,#15696,#15697,#15698,#15699,#15700,#15701,#15702,#15703,#15704,
#15705,#15706,#15707,#15708,#15709,#15710,#15711,#15712,#15713,#15714,#15715,
#15716,#15717,#15718,#15719,#15720,#15721,#15722,#15723,#15724,#15725,#15726,
#15727,#15728,#15729,#15730,#15731,#15732,#15733,#15734,#15735,#15736,#15737,
#15738,#15739,#15740,#15741,#15742,#15743,#15744,#15745,#15746,#15747,#15748,
#15749,#15750,#15751,#15752,#15753,#15754,#15755,#15756,#15757,#15758,#15759),
 .UNSPECIFIED.,.F.,.F.,(4,2,2,2,2,2,2,2,2,2,2,2,2,2,2,2,2,2,2,2,2,2,2,2,
2,2,2,2,2,2,2,2,2,2,2,2,2,2,2,2,4),(-4.06102161170475,-4.02199582972615,
-4.01663778008757,-4.01308748452359,-4.01022730211651,-4.00752733239566,
-4.00414887591018,-3.99845407020849,-3.97865998740159,-3.96660944868934,
-3.94585223754946,-3.86808864668337,-3.85295615226867,-3.84956401701976,
-3.84763412207103,-3.84595323132078,-3.84378997006057,-3.83927720957401,
-3.79651224000436,-3.7414405954293,-3.71233471562289,-3.70074635282836,
-3.69208785735269,-3.68811704164995,-3.68526437890688,-3.68244780870993,
-3.67789828083094,-3.66671097613844,-3.6641851664845,-3.55730709132919,
-3.53944397463258,-3.53255799146753,-3.52750558145803,-3.52524014707967,
-3.5235463740722,-3.5216733201392,-3.51853886765252,-3.5079953174975,-3.50579466494038,
-3.41560235753592,-3.39970068703626),.UNSPECIFIED.);
#181=B_SPLINE_CURVE_WITH_KNOTS('',3,(#15760,#15761,#15762,#15763,#15764,
#15765,#15766,#15767,#15768,#15769,#15770,#15771,#15772,#15773,#15774,#15775,
#15776,#15777,#15778,#15779,#15780,#15781,#15782,#15783,#15784,#15785,#15786,
#15787,#15788,#15789,#15790,#15791,#15792,#15793,#15794,#15795,#15796,#15797,
#15798,#15799,#15800,#15801,#15802,#15803,#15804,#15805,#15806,#15807,#15808,
#15809,#15810,#15811,#15812,#15813,#15814,#15815,#15816,#15817,#15818,#15819,
#15820,#15821,#15822,#15823,#15824,#15825,#15826,#15827,#15828,#15829,#15830,
#15831,#15832,#15833,#15834,#15835,#15836,#15837,#15838,#15839,#15840,#15841,
#15842,#15843,#15844,#15845,#15846,#15847,#15848,#15849,#15850,#15851,#15852,
#15853,#15854,#15855,#15856,#15857,#15858,#15859,#15860,#15861,#15862,#15863,
#15864,#15865,#15866,#15867,#15868,#15869,#15870,#15871,#15872,#15873,#15874,
#15875,#15876,#15877,#15878,#15879,#15880,#15881,#15882,#15883,#15884,#15885,
#15886,#15887,#15888,#15889,#15890,#15891,#15892,#15893,#15894,#15895,#15896,
#15897,#15898,#15899,#15900,#15901,#15902,#15903,#15904,#15905,#15906,#15907,
#15908,#15909,#15910,#15911,#15912,#15913,#15914,#15915,#15916,#15917,#15918,
#15919,#15920,#15921,#15922,#15923,#15924,#15925,#15926,#15927,#15928,#15929,
#15930,#15931,#15932,#15933,#15934,#15935,#15936,#15937,#15938,#15939,#15940,
#15941,#15942,#15943,#15944,#15945,#15946,#15947,#15948,#15949,#15950,#15951,
#15952,#15953,#15954,#15955,#15956,#15957,#15958,#15959,#15960,#15961,#15962,
#15963,#15964,#15965,#15966,#15967,#15968,#15969,#15970,#15971,#15972,#15973,
#15974,#15975,#15976,#15977,#15978,#15979,#15980,#15981,#15982,#15983,#15984,
#15985,#15986,#15987),.UNSPECIFIED.,.F.,.F.,(4,2,2,2,2,2,2,2,2,2,2,2,2,
2,2,2,2,2,2,2,2,2,2,2,2,2,2,2,2,2,2,2,2,2,2,2,2,2,2,2,2,2,2,2,2,2,2,2,2,
2,2,2,2,2,2,2,2,2,2,2,2,2,2,2,2,2,2,2,2,2,2,2,2,2,2,2,2,2,2,2,2,2,2,2,2,
2,2,2,2,2,2,2,2,2,2,2,2,2,2,2,2,2,2,2,2,2,2,2,2,2,2,2,2,4),(-2.69271526571019,
-2.68624721463361,-2.65876402825057,-2.64196798111432,-2.63681410617141,
-2.63355543861204,-2.63052594401115,-2.62658798210346,-2.6199942861044,
-2.57019414145632,-2.4925494406474,-2.47727445615202,-2.47387261079431,
-2.47194062244171,-2.47026012526584,-2.46810030952158,-2.46461647622999,
-2.44503892072068,-2.4401978299325,-2.43135039808765,-2.36099685825411,
-2.32523145639768,-2.31633787189987,-2.31230745805228,-2.30927405643316,
-2.30602496996308,-2.30091535062292,-2.28602584244716,-2.18138882295176,
-2.16360151354676,-2.15673574234555,-2.15169498153557,-2.1494317829581,
-2.14773844567741,-2.14586457914324,-2.14272604785922,-2.13214483596618,
-2.12833675454628,-2.03158982424865,-1.99849962339315,-1.99244100403821,
-1.98862018070773,-1.98561497893053,-1.9822646182488,-1.97669766881371,
-1.95571553615086,-1.8748323874128,-1.83271608318859,-1.82820635004418,
-1.826043559173,-1.82436258819426,-1.82243211625727,-1.81903786643855,-1.80387764838228,
-1.7261679426778,-1.67634625841352,-1.66975150667458,-1.66581288820987,
-1.66278289082836,-1.65952368621272,-1.65436897211488,-1.63757045203986,
-1.61007940440053,-1.53582075189944,-1.50912267008506,-1.50496931584516,
-1.50284970165496,-1.50117242468987,-1.49921183084357,-1.49567993431371,
-1.47835473980605,-1.40232125814328,-1.35321389968435,-1.34663328600624,
-1.34269877597881,-1.33966940497848,-1.33640837846621,-1.33124546542001,
-1.31437267194065,-1.28671164011955,-1.2139866990388,-1.18608639192274,
-1.1818915727963,-1.17976310322527,-1.17808516061701,-1.1761310750648,-1.17262905843022,
-1.15580366272312,-1.07940367470053,-1.0301152666782,-1.02353102547234,
-1.01959545674416,-1.01656591951338,-1.01330535314141,-1.00814453066496,
-0.991290768345315,-0.963673362337573,-0.890499311629776,-0.862960415142799,
-0.85877761718957,-0.856651707779826,-0.854973959360891,-0.853018002796683,
-0.849507416817777,-0.832540589674147,-0.756245304467527,-0.70702883626328,
-0.700433528011964,-0.696494726806326,-0.693464676183969,-0.690205500202847,
-0.685051014157872,-0.668254866052211,-0.662349049559275),.UNSPECIFIED.);
#182=B_SPLINE_CURVE_WITH_KNOTS('',3,(#15992,#15993,#15994,#15995,#15996,
#15997,#15998,#15999,#16000,#16001,#16002,#16003,#16004,#16005,#16006,#16007,
#16008,#16009,#16010,#16011,#16012,#16013,#16014,#16015,#16016,#16017,#16018,
#16019,#16020,#16021,#16022,#16023,#16024,#16025,#16026,#16027,#16028,#16029,
#16030,#16031,#16032,#16033,#16034,#16035,#16036,#16037,#16038,#16039,#16040,
#16041,#16042,#16043,#16044,#16045,#16046,#16047,#16048,#16049,#16050,#16051,
#16052,#16053,#16054,#16055,#16056,#16057,#16058,#16059,#16060,#16061,#16062,
#16063,#16064,#16065,#16066,#16067,#16068,#16069,#16070,#16071,#16072,#16073,
#16074,#16075,#16076,#16077,#16078,#16079,#16080,#16081,#16082,#16083,#16084,
#16085,#16086,#16087,#16088,#16089,#16090,#16091,#16092,#16093,#16094,#16095,
#16096,#16097,#16098,#16099,#16100,#16101,#16102,#16103,#16104,#16105,#16106,
#16107,#16108,#16109,#16110,#16111,#16112,#16113,#16114,#16115,#16116,#16117,
#16118,#16119,#16120,#16121,#16122,#16123,#16124,#16125,#16126,#16127,#16128,
#16129,#16130,#16131,#16132,#16133,#16134,#16135,#16136,#16137,#16138,#16139,
#16140,#16141,#16142,#16143,#16144,#16145,#16146,#16147,#16148,#16149,#16150,
#16151,#16152,#16153,#16154,#16155,#16156,#16157,#16158,#16159,#16160,#16161,
#16162,#16163,#16164,#16165,#16166,#16167,#16168,#16169,#16170,#16171,#16172,
#16173,#16174,#16175,#16176,#16177,#16178,#16179,#16180,#16181,#16182,#16183,
#16184,#16185,#16186,#16187,#16188,#16189,#16190,#16191,#16192,#16193,#16194,
#16195,#16196,#16197,#16198,#16199,#16200,#16201,#16202,#16203,#16204,#16205,
#16206,#16207,#16208,#16209,#16210,#16211,#16212,#16213,#16214,#16215,#16216,
#16217,#16218,#16219),.UNSPECIFIED.,.F.,.F.,(4,2,2,2,2,2,2,2,2,2,2,2,2,
2,2,2,2,2,2,2,2,2,2,2,2,2,2,2,2,2,2,2,2,2,2,2,2,2,2,2,2,2,2,2,2,2,2,2,2,
2,2,2,2,2,2,2,2,2,2,2,2,2,2,2,2,2,2,2,2,2,2,2,2,2,2,2,2,2,2,2,2,2,2,2,2,
2,2,2,2,2,2,2,2,2,2,2,2,2,2,2,2,2,2,2,2,2,2,2,2,2,2,2,2,4),(-3.39964083351492,
-3.36365087206928,-3.34678077620974,-3.3432756693511,-3.34132074014372,
-3.33964260244493,-3.3375145426246,-3.33332248596686,-3.30551171339091,
-3.23274707438292,-3.20511715466561,-3.18825585182105,-3.18309369335482,
-3.17983247271473,-3.1768024510124,-3.17286641792817,-3.1662816870958,-3.11700934454949,
-3.04053866167242,-3.02372963752752,-3.02022809592353,-3.01827387292569,
-3.01659554617584,-3.01446622347939,-3.01026858715903,-2.98229350650707,
-2.90972509345195,-2.88207473063289,-2.86520421687862,-2.86004084563294,
-2.85677922902745,-2.85374909486574,-2.84981327827797,-2.84322970839898,
-2.79403246661742,-2.717719295123,-2.70069023416851,-2.69717523709525,-2.69521800906385,
-2.69353988657468,-2.69141439938574,-2.68723509897752,-2.65981606356893,
-2.58654863464378,-2.55896508096669,-2.54212345194394,-2.53696306561767,
-2.5337019839676,-2.53067141446083,-2.52673370839752,-2.52014405970235,
-2.4706577015763,-2.39371343017052,-2.37751324304274,-2.37404934384091,
-2.37210320212424,-2.37042371508873,-2.36828243821504,-2.36388427273072,
-2.3070464387066,-2.26249989183244,-2.23555375468513,-2.218991567172,-2.21386183379691,
-2.2106072771075,-2.20757385386497,-2.20361971358468,-2.1969743579148,-2.13040400241445,
-2.08297340398918,-2.06429494999913,-2.05719346066002,-2.0520176405405,
-2.04972954812474,-2.04803212316265,-2.0461691242003,-2.04308095280988,
-2.03294629747931,-2.03090298239736,-2.00858613066327,-1.91910146310902,
-1.89732612426433,-1.89150265071687,-1.88806124926346,-1.88506732512373,
-1.88138184085324,-1.87426317867405,-1.81790382035216,-1.75704433491111,
-1.73244874736278,-1.72837642684058,-1.72627388458271,-1.72459728666606,
-1.72262251508973,-1.71902685373257,-1.70058567033811,-1.62115250355916,
-1.57650792932064,-1.57002050655558,-1.5661127055394,-1.56308676936036,
-1.55981241672749,-1.55459174376434,-1.53719345280849,-1.50831675095391,
-1.46575548046262,-1.40985460921982,-1.40544316768122,-1.40329937886659,
-1.40161981358235,-1.39967572403598,-1.39622072167918,-1.3801554698927,
-1.36961882394012),.UNSPECIFIED.);
#183=B_SPLINE_CURVE_WITH_KNOTS('',3,(#16221,#16222,#16223,#16224,#16225,
#16226,#16227,#16228,#16229,#16230,#16231,#16232,#16233,#16234,#16235,#16236,
#16237,#16238,#16239,#16240,#16241,#16242,#16243,#16244,#16245,#16246,#16247,
#16248,#16249,#16250,#16251,#16252,#16253,#16254,#16255,#16256,#16257,#16258,
#16259,#16260,#16261,#16262,#16263,#16264,#16265,#16266,#16267,#16268,#16269,
#16270,#16271,#16272,#16273,#16274,#16275,#16276,#16277,#16278,#16279,#16280,
#16281,#16282,#16283,#16284,#16285,#16286,#16287,#16288,#16289,#16290,#16291,
#16292,#16293,#16294,#16295,#16296,#16297,#16298,#16299,#16300,#16301,#16302,
#16303,#16304,#16305,#16306,#16307,#16308,#16309,#16310,#16311,#16312,#16313,
#16314,#16315,#16316,#16317,#16318,#16319,#16320,#16321,#16322,#16323,#16324,
#16325,#16326,#16327,#16328,#16329,#16330,#16331,#16332,#16333,#16334,#16335,
#16336,#16337,#16338,#16339,#16340,#16341,#16342),.UNSPECIFIED.,.F.,.F.,
(4,2,2,2,2,2,2,2,2,2,2,2,2,2,2,2,2,2,2,2,2,2,2,2,2,2,2,2,2,2,2,2,2,2,2,
2,2,2,2,2,2,2,2,2,2,2,2,2,2,2,2,2,2,2,2,2,2,2,2,2,4),(-0.662349049559275,
-0.64076935233397,-0.566466931283648,-0.539800645169952,-0.535648410883396,
-0.533529023672387,-0.53185174726018,-0.529890947402202,-0.526358160710187,
-0.509018246169802,-0.432994462499759,-0.383918563847769,-0.377323282030764,
-0.373384472547141,-0.370354401509297,-0.370298975441233,-0.370234676619521,
-0.370179135744734,-0.370131156433472,-0.370089705560998,-0.370053891319813,
-0.370022944097521,-0.369986958714127,-0.369952150661377,-0.369918477084106,
-0.369885898069153,-0.369854375178348,-0.369823871418894,-0.369794351172866,
-0.369765780142296,-0.369738125323371,-0.369711354947079,-0.369685438411946,
-0.369660348552099,-0.369636059309752,-0.369612539282026,-0.369589762222112,
-0.369567702865705,-0.366116070446883,-0.35999913953825,-0.352470758189602,
-0.336679856203082,-0.289908620168167,-0.221133027376399,-0.213965351312048,
-0.211274959536918,-0.209677145139871,-0.20796274220465,-0.205569383331507,
-0.199782212265901,-0.172671316670112,-0.0998764316644174,-0.0808381187294856,
-0.05849686903062,-0.0526228188635247,-0.0491704671463769,-0.0464777890897304,
-0.0436385767213315,-0.0401730278245112,-0.0350189293278793,-0.000961519009988408),
 .UNSPECIFIED.);
#184=B_SPLINE_CURVE_WITH_KNOTS('',3,(#16343,#16344,#16345,#16346,#16347,
#16348,#16349,#16350,#16351,#16352,#16353,#16354,#16355,#16356,#16357,#16358,
#16359,#16360,#16361,#16362,#16363,#16364,#16365,#16366,#16367,#16368,#16369,
#16370,#16371,#16372,#16373,#16374,#16375,#16376,#16377,#16378,#16379,#16380,
#16381,#16382,#16383,#16384,#16385,#16386,#16387,#16388,#16389,#16390,#16391,
#16392,#16393,#16394,#16395,#16396,#16397,#16398,#16399,#16400,#16401,#16402,
#16403,#16404,#16405,#16406,#16407,#16408,#16409,#16410,#16411,#16412,#16413,
#16414,#16415,#16416,#16417,#16418,#16419,#16420,#16421,#16422,#16423,#16424,
#16425,#16426,#16427,#16428,#16429,#16430,#16431,#16432,#16433,#16434,#16435,
#16436,#16437,#16438,#16439,#16440,#16441,#16442,#16443,#16444,#16445,#16446,
#16447,#16448,#16449,#16450,#16451,#16452,#16453,#16454,#16455,#16456,#16457,
#16458,#16459,#16460,#16461,#16462,#16463,#16464,#16465,#16466,#16467,#16468,
#16469,#16470,#16471,#16472,#16473,#16474,#16475,#16476,#16477,#16478,#16479,
#16480,#16481,#16482,#16483,#16484,#16485,#16486,#16487,#16488,#16489,#16490,
#16491,#16492,#16493,#16494,#16495,#16496,#16497,#16498,#16499,#16500,#16501,
#16502,#16503,#16504,#16505,#16506,#16507,#16508,#16509,#16510,#16511,#16512,
#16513,#16514,#16515,#16516,#16517,#16518,#16519,#16520,#16521,#16522,#16523,
#16524,#16525,#16526,#16527,#16528),.UNSPECIFIED.,.F.,.F.,(4,2,2,2,2,2,
2,2,2,2,2,2,2,2,2,2,2,2,2,2,2,2,2,2,2,2,2,2,2,2,2,2,2,2,2,2,2,2,2,2,2,2,
2,2,2,2,2,2,2,2,2,2,2,2,2,2,2,2,2,2,2,2,2,2,2,2,2,2,2,2,2,2,2,2,2,2,2,2,
2,2,2,2,2,2,2,2,2,2,2,2,2,2,4),(-4.05998649109244,-3.99044868653892,-3.95612417468513,
-3.94958391300245,-3.94707104933022,-3.94533430297176,-3.94376374512821,
-3.94121389091149,-3.93491224071497,-3.85853970920352,-3.82135288996109,
-3.80378814948435,-3.79566392369472,-3.78917575318832,-3.78563392535796,
-3.78560114851417,-3.78556784745785,-3.78553400521955,-3.78549960416932,
-3.78546462596605,-3.78542905154357,-3.78540460852495,-3.78537816989084,
-3.78534955275616,-3.78531855429528,-3.785284949052,-3.78524848581845,-3.7852088840022,
-3.78516582932394,-3.7851189688123,-3.78506790484846,-3.78501218741791,
-3.78495130647743,-3.78488468463758,-3.78483352903948,-3.78475309657443,
-3.78462521567022,-3.78159649199966,-3.77765922839595,-3.77106603115191,
-3.72190272564037,-3.64569823574233,-3.62860089635745,-3.62508347628936,
-3.62312652790441,-3.62144965938125,-3.6193270972924,-3.61515758637774,
-3.58796333120841,-3.51444776445119,-3.48689846473251,-3.47007455659889,
-3.46491833212194,-3.46165961012969,-3.4586310533177,-3.45469571475831,
-3.44810950833233,-3.39886746926262,-3.32253510474421,-3.30560476888439,
-3.30209723125821,-3.30014236860668,-3.29846517792746,-3.29633949836763,
-3.29215571008368,-3.26454875851421,-3.19154894760421,-3.16394290735498,
-3.14709393960933,-3.14193476460322,-3.13867526825463,-3.13564674437131,
-3.13171251726629,-3.12513052616731,-3.07587720907922,-2.99954021199146,
-2.98260909029999,-2.97910135939408,-2.97714638476761,-2.97546909538644,
-2.97334328734951,-2.96915923600524,-2.94155014115303,-2.86854670069039,
-2.84093897507871,-2.82408899006877,-2.81892950917996,-2.81566982087076,
-2.81264111952099,-2.80870666314254,-2.80212429125671,-2.75286835703161,
-2.69164525988063),.UNSPECIFIED.);
#185=B_SPLINE_CURVE_WITH_KNOTS('',3,(#16534,#16535,#16536,#16537,#16538,
#16539,#16540,#16541),.UNSPECIFIED.,.F.,.F.,(4,1,1,1,1,4),(78.5398167494604,
79.3108996268056,80.3108456391569,81.3107916515083,82.3107376638597,82.7769112748486),
 .UNSPECIFIED.);
#186=B_SPLINE_CURVE_WITH_KNOTS('',3,(#16542,#16543,#16544,#16545,#16546,
#16547,#16548,#16549,#16550,#16551,#16552,#16553,#16554,#16555,#16556,#16557,
#16558,#16559,#16560,#16561,#16562,#16563,#16564,#16565,#16566,#16567,#16568,
#16569,#16570,#16571,#16572,#16573,#16574,#16575,#16576,#16577,#16578,#16579,
#16580,#16581,#16582,#16583,#16584,#16585,#16586,#16587,#16588,#16589,#16590,
#16591,#16592,#16593,#16594,#16595,#16596,#16597,#16598,#16599,#16600,#16601,
#16602,#16603,#16604,#16605,#16606,#16607,#16608,#16609,#16610,#16611,#16612,
#16613,#16614,#16615,#16616,#16617,#16618,#16619),.UNSPECIFIED.,.F.,.F.,
(4,2,2,2,2,2,2,2,2,2,2,2,2,2,2,2,2,2,2,2,2,2,2,2,2,2,2,2,2,2,2,2,2,2,2,
2,2,2,4),(-4.06030800713201,-3.99779701166778,-3.99312814877567,-3.99046496624178,
-3.98808965641954,-3.98637825904871,-3.98477533221798,-3.98205964130569,
-3.97472713607147,-3.92005396922612,-3.88678614013887,-3.84270727902733,
-3.83245010789196,-3.82911518963075,-3.82585347827722,-3.82282375369924,
-3.81888917523367,-3.81230923142789,-3.76326775465827,-3.71118612747833,
-3.68340591382533,-3.6694906936369,-3.66619873825633,-3.66427581734111,
-3.66259343172322,-3.66041826683211,-3.65688422741131,-3.63633485598899,
-3.62776215225491,-3.55051218449303,-3.52626917547153,-3.51099361480606,
-3.50612870745672,-3.5028676261734,-3.4998378056662,-3.49590213574806,-3.48931823678396,
-3.44007079154322,-3.39964083351492),.UNSPECIFIED.);
#187=B_SPLINE_CURVE_WITH_KNOTS('',3,(#16620,#16621,#16622,#16623,#16624,
#16625,#16626,#16627,#16628,#16629,#16630,#16631,#16632,#16633,#16634,#16635,
#16636,#16637,#16638,#16639,#16640,#16641,#16642,#16643,#16644,#16645,#16646,
#16647,#16648,#16649,#16650,#16651,#16652,#16653,#16654,#16655,#16656,#16657,
#16658,#16659,#16660,#16661,#16662,#16663,#16664,#16665,#16666,#16667,#16668,
#16669,#16670,#16671,#16672,#16673,#16674,#16675,#16676,#16677,#16678,#16679,
#16680,#16681,#16682,#16683,#16684,#16685,#16686,#16687,#16688,#16689,#16690,
#16691,#16692,#16693,#16694,#16695,#16696,#16697,#16698,#16699,#16700,#16701,
#16702,#16703,#16704,#16705,#16706,#16707,#16708,#16709,#16710,#16711,#16712,
#16713,#16714,#16715,#16716,#16717,#16718,#16719,#16720,#16721,#16722,#16723,
#16724,#16725,#16726,#16727,#16728,#16729,#16730,#16731,#16732,#16733,#16734,
#16735,#16736,#16737,#16738,#16739,#16740,#16741,#16742,#16743,#16744,#16745,
#16746,#16747,#16748,#16749,#16750,#16751,#16752,#16753,#16754,#16755,#16756,
#16757,#16758,#16759,#16760,#16761,#16762,#16763,#16764,#16765,#16766,#16767,
#16768,#16769,#16770,#16771,#16772,#16773,#16774,#16775,#16776,#16777,#16778,
#16779,#16780,#16781,#16782,#16783,#16784,#16785,#16786,#16787,#16788,#16789,
#16790,#16791,#16792,#16793,#16794,#16795,#16796,#16797,#16798,#16799,#16800,
#16801,#16802,#16803,#16804,#16805,#16806,#16807,#16808,#16809,#16810,#16811,
#16812,#16813,#16814,#16815,#16816,#16817,#16818,#16819,#16820,#16821,#16822,
#16823,#16824,#16825,#16826,#16827,#16828,#16829,#16830,#16831,#16832,#16833,
#16834,#16835,#16836,#16837,#16838,#16839,#16840,#16841,#16842,#16843,#16844,
#16845),.UNSPECIFIED.,.F.,.F.,(4,2,2,2,2,2,2,2,2,2,2,2,2,2,2,2,2,2,2,2,
2,2,2,2,2,2,2,2,2,2,2,2,2,2,2,2,2,2,2,2,2,2,2,2,2,2,2,2,2,2,2,2,2,2,2,2,
2,2,2,2,2,2,2,2,2,2,2,2,2,2,2,2,2,2,2,2,2,2,2,2,2,2,2,2,2,2,2,2,2,2,2,2,
2,2,2,2,2,2,2,2,2,2,2,2,2,2,2,2,2,2,2,2,4),(-2.69164525988063,-2.67652744625314,
-2.65959456612067,-2.65608658319691,-2.65413148378648,-2.65245409704284,
-2.65032817806746,-2.64614394591702,-2.61853515913257,-2.5455250255624,
-2.51791592128734,-2.50106505291842,-2.49590528089034,-2.49264540388283,
-2.48961652392077,-2.48568183085011,-2.47909905269859,-2.42983922230729,
-2.35349174717579,-2.33656069266682,-2.33305267414528,-2.33109749712599,
-2.32942000805571,-2.3272939134671,-2.32310919728146,-2.29549168176191,
-2.22248614591935,-2.19487453263666,-2.17802228732432,-2.17286216975934,
-2.16960209198305,-2.16657303758154,-2.16263813508684,-2.15605504442876,
-2.10679602888215,-2.03045174837929,-2.01380491832151,-2.01049077376697,
-2.00838249328433,-2.00670618453229,-2.00473743880578,-2.00116731427396,
-1.98317011768556,-1.90762229780562,-1.85877966320953,-1.8522051012188,
-1.84827261098029,-1.84524385997702,-1.84198257919614,-1.83681729749719,
-1.81991911702346,-1.7921984464339,-1.72020846029211,-1.71111613148174,
-1.69110900349414,-1.68760281185066,-1.68543627544157,-1.68375512195578,
-1.68182750962024,-1.67844555674473,-1.66345853408425,-1.58561588569702,
-1.53575222944299,-1.52915738590937,-1.52521900312959,-1.52218935663289,
-1.51893069621455,-1.51377719761044,-1.49698580023694,-1.46950961555556,
-1.39517766611248,-1.36854480229695,-1.36439422904569,-1.36227536989895,
-1.36059834518428,-1.35863764771494,-1.35510456347838,-1.33775356205248,
-1.26175017341635,-1.21265962203328,-1.20608007213211,-1.2021461339271,
-1.19911716565885,-1.19585653569015,-1.19069417160215,-1.17382246525547,
-1.14616249481071,-1.07347428975496,-1.04555543473885,-1.04136043479394,
-1.0392320871024,-1.03755435039807,-1.03560063073145,-1.03209958271399,
-1.01528481095655,-0.938888458637008,-0.889603476585265,-0.883020031294518,
-0.879084956491885,-0.876055810106649,-0.872795674853165,-0.86763555705628,
-0.85078429566735,-0.823171191116063,-0.74999963593344,-0.722469906107444,
-0.718287840389341,-0.716162247404762,-0.714484719962632,-0.712528987965407,
-0.709018722734614,-0.69205185495633,-0.66172580755329),.UNSPECIFIED.);
#188=B_SPLINE_CURVE_WITH_KNOTS('',3,(#16851,#16852,#16853,#16854,#16855,
#16856,#16857,#16858,#16859,#16860,#16861,#16862,#16863,#16864,#16865,#16866,
#16867,#16868,#16869,#16870,#16871,#16872,#16873,#16874,#16875,#16876,#16877,
#16878,#16879,#16880,#16881,#16882,#16883,#16884,#16885,#16886,#16887,#16888,
#16889,#16890,#16891,#16892,#16893,#16894,#16895,#16896,#16897,#16898,#16899,
#16900,#16901,#16902,#16903,#16904,#16905,#16906,#16907,#16908,#16909,#16910,
#16911,#16912,#16913,#16914,#16915,#16916,#16917,#16918,#16919,#16920,#16921,
#16922,#16923,#16924,#16925,#16926,#16927,#16928,#16929,#16930,#16931,#16932,
#16933,#16934,#16935,#16936,#16937,#16938,#16939,#16940,#16941,#16942,#16943,
#16944,#16945,#16946,#16947,#16948,#16949,#16950,#16951,#16952,#16953,#16954,
#16955,#16956,#16957,#16958,#16959,#16960,#16961,#16962,#16963,#16964,#16965,
#16966,#16967,#16968,#16969,#16970,#16971,#16972,#16973,#16974,#16975,#16976,
#16977,#16978,#16979,#16980,#16981,#16982,#16983,#16984,#16985,#16986,#16987,
#16988,#16989,#16990,#16991,#16992,#16993,#16994,#16995,#16996,#16997,#16998,
#16999,#17000,#17001,#17002,#17003,#17004,#17005,#17006,#17007,#17008,#17009,
#17010,#17011,#17012,#17013,#17014,#17015,#17016,#17017,#17018,#17019,#17020,
#17021,#17022,#17023,#17024,#17025,#17026,#17027,#17028,#17029,#17030,#17031,
#17032,#17033,#17034,#17035,#17036,#17037,#17038,#17039,#17040),
 .UNSPECIFIED.,.F.,.F.,(4,2,2,2,2,2,2,2,2,2,2,2,2,2,2,2,2,2,2,2,2,2,2,2,
2,2,2,2,2,2,2,2,2,2,2,2,2,2,2,2,2,2,2,2,2,2,2,2,2,2,2,2,2,2,2,2,2,2,2,2,
2,2,2,2,2,2,2,2,2,2,2,2,2,2,2,2,2,2,2,2,2,2,2,2,2,2,2,2,2,2,2,2,2,2,4),
(-1.37000516159202,-1.32982235070187,-1.30088677921817,-1.29507105438874,
-1.29132394001103,-1.2883254321715,-1.28492796263422,-1.27915059295163,
-1.25563521732469,-1.17675103002816,-1.13557854015604,-1.13107525122225,
-1.1289133898409,-1.12723212717903,-1.12530014487673,-1.12190041465387,
-1.1066688211435,-1.02899722392388,-0.979233631022262,-0.972639024540158,
-0.968699933566932,-0.965669236953448,-0.962408943672752,-0.95725177657945,
-0.940438429841211,-0.912915163360214,-0.838971107817674,-0.812040641643707,
-0.807878264526655,-0.805756405411002,-0.80407856986728,-0.802118694677714,
-0.798591504142505,-0.781356576663223,-0.705236566564479,-0.656157545825954,
-0.649562872356873,-0.645623749486369,-0.64259303306983,-0.639332723147275,
-0.63417553965061,-0.617362227933496,-0.589839108652345,-0.515892035835737,
-0.488963362485876,-0.484801029417397,-0.482679172153062,-0.481001327390222,
-0.479041429115078,-0.47551416617306,-0.458278274677027,-0.382158419390071,
-0.333079370543377,-0.325901714702702,-0.32220015647419,-0.319325300356319,
-0.319201804662897,-0.319098681490327,-0.319010062672658,-0.318932276434972,
-0.318862866167265,-0.318800104331356,-0.31874272871045,-0.318689788455967,
-0.318640549072348,-0.318594431079622,-0.318550968963718,-0.318509782802414,
-0.318470558165119,-0.318433031537635,-0.318396979522895,-0.318362210721167,
-0.318328559515459,-0.318295881248411,-0.318264048433537,-0.318232947722156,
-0.318163601624379,-0.318094221438091,-0.318024701903007,-0.317954942841739,
-0.314230023579432,-0.306387687448059,-0.24462636351261,-0.16918610614987,
-0.162802602600097,-0.160237844753108,-0.15866367422278,-0.156928082368122,
-0.154425746987008,-0.147961734233512,-0.0990691438969175,-0.0207871264132375,
-0.00677755631971555,-0.00293676047487332,-0.00101485485105488),
 .UNSPECIFIED.);
#189=B_SPLINE_CURVE_WITH_KNOTS('',3,(#17041,#17042,#17043,#17044,#17045,
#17046),.UNSPECIFIED.,.F.,.F.,(4,1,1,4),(82.7769112748486,83.3106836762111,
84.3106296885624,84.8230016469246),.UNSPECIFIED.);
#190=B_SPLINE_CURVE_WITH_KNOTS('',3,(#17048,#17049,#17050,#17051,#17052,
#17053,#17054,#17055,#17056,#17057,#17058,#17059,#17060,#17061,#17062,#17063,
#17064,#17065,#17066,#17067,#17068,#17069,#17070,#17071,#17072,#17073,#17074,
#17075,#17076,#17077,#17078,#17079,#17080,#17081,#17082,#17083,#17084,#17085,
#17086,#17087,#17088,#17089,#17090,#17091,#17092,#17093,#17094,#17095,#17096,
#17097,#17098,#17099,#17100,#17101,#17102,#17103,#17104,#17105,#17106,#17107,
#17108,#17109,#17110,#17111,#17112,#17113,#17114,#17115,#17116,#17117,#17118,
#17119,#17120,#17121,#17122,#17123),.UNSPECIFIED.,.F.,.F.,(4,2,2,2,2,2,
2,2,2,2,2,2,2,2,2,2,2,2,2,2,2,2,2,2,2,2,2,2,2,2,2,2,2,2,2,2,2,4),(-0.66172580755329,
-0.615768135562443,-0.566537092661659,-0.559954712151595,-0.556019943285156,
-0.552990839211819,-0.549730559234709,-0.544569806894018,-0.52804181333161,
-0.501027722968988,-0.423398787581568,-0.4222793957237,-0.399108186475157,
-0.395451222298192,-0.393263280845654,-0.391575308553205,-0.389682444530973,
-0.386522450347328,-0.374257392356896,-0.351272631358261,-0.29881050401711,
-0.243668379532499,-0.236993498479392,-0.233031688399543,-0.229998136996049,
-0.226749065290884,-0.221639837704353,-0.205642210257806,-0.164450525013423,
-0.131305979381181,-0.0767137492516896,-0.0722792425654901,-0.0701313490448679,
-0.0684519482407693,-0.066511922119817,-0.0644633838945868,-0.0613034965144324,
-0.000962151141444392),.UNSPECIFIED.);
#191=B_SPLINE_CURVE_WITH_KNOTS('',3,(#17124,#17125,#17126,#17127,#17128,
#17129,#17130,#17131,#17132,#17133,#17134,#17135,#17136,#17137,#17138,#17139,
#17140,#17141,#17142,#17143,#17144,#17145,#17146,#17147,#17148,#17149,#17150,
#17151,#17152,#17153,#17154,#17155,#17156,#17157,#17158,#17159,#17160,#17161,
#17162,#17163,#17164,#17165,#17166,#17167,#17168,#17169,#17170,#17171,#17172,
#17173,#17174,#17175,#17176,#17177,#17178,#17179,#17180,#17181,#17182,#17183,
#17184,#17185,#17186,#17187,#17188,#17189,#17190,#17191,#17192,#17193,#17194,
#17195,#17196,#17197,#17198,#17199,#17200,#17201,#17202,#17203,#17204,#17205,
#17206,#17207,#17208,#17209,#17210,#17211,#17212,#17213,#17214,#17215,#17216,
#17217,#17218,#17219,#17220,#17221,#17222,#17223,#17224,#17225,#17226,#17227,
#17228,#17229,#17230,#17231,#17232,#17233,#17234,#17235,#17236,#17237,#17238,
#17239,#17240,#17241,#17242,#17243,#17244,#17245,#17246,#17247,#17248,#17249,
#17250,#17251,#17252,#17253,#17254,#17255,#17256,#17257,#17258,#17259,#17260,
#17261,#17262,#17263,#17264,#17265,#17266,#17267,#17268,#17269,#17270,#17271,
#17272,#17273),.UNSPECIFIED.,.F.,.F.,(4,2,2,2,2,2,2,2,2,2,2,2,2,2,2,2,2,
2,2,2,2,2,2,2,2,2,2,2,2,2,2,2,2,2,2,2,2,2,2,2,2,2,2,2,2,2,2,2,2,2,2,2,2,
2,2,2,2,2,2,2,2,2,2,2,2,2,2,2,2,2,2,2,2,2,4),(-4.06115038023093,-3.99429509258559,
-3.98279511263255,-3.97679793062009,-3.97165267525303,-3.96839642445301,
-3.96536707786196,-3.96142632143306,-3.95482134705909,-3.8860872897746,
-3.85413284097312,-3.8182929323426,-3.81083640844067,-3.80879905270211,
-3.80686710321459,-3.80518722628126,-3.80302897507252,-3.79853953745811,
-3.75860831996345,-3.69128076668005,-3.65665186120019,-3.65021792731777,
-3.64656568227414,-3.64357572969109,-3.64011310782554,-3.63419116237318,
-3.61129640472461,-3.60184646027432,-3.52563564692273,-3.50157524369334,
-3.48893334798986,-3.48570807793765,-3.48381544371097,-3.4821280323054,
-3.47994130355179,-3.47628740115911,-3.45316911977267,-3.44248572875624,
-3.37541484079659,-3.3478082031626,-3.3309590937197,-3.32579998517169,-3.32254055612835,
-3.31951211225338,-3.31557801389033,-3.30899629283811,-3.25974954865934,
-3.18342551933013,-3.16647983977272,-3.16297129204163,-3.16101616893573,
-3.15933894190941,-3.15721345666721,-3.15303077504045,-3.12546002509056,
-3.0524112953787,-3.02480899577556,-3.00796149928777,-3.00280237468692,
-2.99954281795653,-2.99651417431887,-2.99257970127295,-2.98599709957066,
-2.9367226200479,-2.86034245058973,-2.8434655504661,-2.83996101611495,-2.83800669816343,
-2.83632927564846,-2.83420240347714,-2.83001355703396,-2.80226401775156,
-2.72943180907567,-2.70180606633594,-2.69239263445687),.UNSPECIFIED.);
#192=B_SPLINE_CURVE_WITH_KNOTS('',3,(#17278,#17279,#17280,#17281,#17282,
#17283,#17284,#17285,#17286,#17287,#17288,#17289,#17290,#17291,#17292,#17293,
#17294,#17295,#17296,#17297,#17298,#17299,#17300,#17301,#17302,#17303,#17304,
#17305,#17306,#17307,#17308,#17309,#17310,#17311,#17312,#17313,#17314,#17315,
#17316,#17317,#17318,#17319,#17320,#17321,#17322,#17323,#17324,#17325,#17326,
#17327,#17328,#17329,#17330,#17331,#17332,#17333,#17334,#17335,#17336,#17337,
#17338,#17339,#17340,#17341,#17342,#17343,#17344,#17345,#17346,#17347,#17348,
#17349,#17350,#17351,#17352,#17353,#17354,#17355,#17356,#17357,#17358,#17359,
#17360,#17361,#17362,#17363,#17364,#17365,#17366,#17367,#17368,#17369,#17370,
#17371,#17372,#17373,#17374,#17375,#17376,#17377,#17378,#17379,#17380,#17381,
#17382,#17383,#17384,#17385,#17386,#17387,#17388,#17389,#17390,#17391,#17392,
#17393,#17394,#17395,#17396,#17397,#17398,#17399,#17400,#17401,#17402,#17403,
#17404,#17405,#17406,#17407,#17408,#17409,#17410,#17411,#17412,#17413,#17414,
#17415,#17416,#17417,#17418,#17419,#17420,#17421,#17422,#17423,#17424,#17425,
#17426,#17427,#17428,#17429,#17430,#17431,#17432,#17433,#17434,#17435,#17436,
#17437,#17438,#17439,#17440,#17441,#17442,#17443,#17444,#17445,#17446,#17447,
#17448,#17449,#17450,#17451,#17452,#17453,#17454,#17455,#17456,#17457,#17458,
#17459,#17460,#17461,#17462,#17463,#17464,#17465,#17466,#17467,#17468,#17469,
#17470,#17471,#17472,#17473,#17474,#17475,#17476,#17477,#17478,#17479,#17480,
#17481,#17482,#17483,#17484,#17485,#17486,#17487,#17488,#17489,#17490,#17491,
#17492,#17493,#17494,#17495,#17496,#17497,#17498,#17499,#17500,#17501,#17502,
#17503,#17504,#17505),.UNSPECIFIED.,.F.,.F.,(4,2,2,2,2,2,2,2,2,2,2,2,2,
2,2,2,2,2,2,2,2,2,2,2,2,2,2,2,2,2,2,2,2,2,2,2,2,2,2,2,2,2,2,2,2,2,2,2,2,
2,2,2,2,2,2,2,2,2,2,2,2,2,2,2,2,2,2,2,2,2,2,2,2,2,2,2,2,2,2,2,2,2,2,2,2,
2,2,2,2,2,2,2,2,2,2,2,2,2,2,2,2,2,2,2,2,2,2,2,2,2,2,2,2,4),(-3.39962357914392,
-3.39506088796122,-3.3915554724998,-3.38960072794962,-3.38792296976071,
-3.38579567531718,-3.3816059838441,-3.35384994273638,-3.2810404240971,-3.25342214272944,
-3.23656693633569,-3.23140614882391,-3.2281456800974,-3.2251162781971,-3.22118093836022,
-3.21459712076029,-3.16531107070317,-3.08880520796687,-3.07206850046493,
-3.06857190097623,-3.06661900812461,-3.06494093677447,-3.06281079620667,
-3.05860809086884,-3.03045428610733,-2.958127260132,-2.93046241794374,-2.91358660328308,
-2.908423347958,-2.90516220481268,-2.90213278659885,-2.89819829177458,-2.89161779584987,
-2.84251503884156,-2.76638617725541,-2.7491301790426,-2.74560220543741,
-2.74364240355827,-2.74196493690716,-2.7398439479749,-2.73568448003327,
-2.70881402666259,-2.6348625953276,-2.6073657257391,-2.59056300616248,-2.58540761273744,
-2.58214808518325,-2.57911785369498,-2.57517901465898,-2.56858400175031,
-2.5187643998977,-2.44093339664959,-2.42585876816632,-2.42247013236351,
-2.42054075582029,-2.41885936595049,-2.41669421477148,-2.41217316321173,
-2.3676139551844,-2.31372474348187,-2.28500958960437,-2.26767905490894,
-2.26246596759375,-2.25919349503569,-2.25616733200127,-2.25225647748129,
-2.24575792849089,-2.20040242075149,-2.13257354208228,-2.10646078717017,
-2.10078641632752,-2.09841165534728,-2.0967002468842,-2.09509698618824,
-2.0923800448108,-2.08504017463944,-2.0313624349916,-2.00076102426971,-1.94853200347732,
-1.94189176875138,-1.93793945320682,-1.93490673759133,-1.93165226422132,
-1.92652123554799,-1.90994253883999,-1.88295325472521,-1.80682085236967,
-1.78117681975093,-1.77706251318236,-1.77495098808381,-1.77327390651068,
-1.77130631613008,-1.7677435062251,-1.74989199927299,-1.67421247374382,
-1.62534480071989,-1.6187681644757,-1.6148343465868,-1.61180451299719,-1.60854200104179,
-1.60337461461672,-1.5864678405104,-1.55873028604816,-1.48699834313129,
-1.47913249852733,-1.4577920244589,-1.4542188432688,-1.45205514353547,-1.45036978714444,
-1.44846166020954,-1.44516987713201,-1.43142620396899,-1.40426158146784,
-1.37000516159202),.UNSPECIFIED.);
#193=B_SPLINE_CURVE_WITH_KNOTS('',3,(#17506,#17507,#17508,#17509,#17510,
#17511,#17512,#17513,#17514,#17515,#17516,#17517,#17518,#17519,#17520,#17521,
#17522,#17523,#17524,#17525,#17526,#17527,#17528,#17529,#17530,#17531,#17532,
#17533,#17534,#17535,#17536,#17537,#17538,#17539,#17540,#17541,#17542,#17543,
#17544,#17545,#17546,#17547,#17548,#17549,#17550,#17551,#17552,#17553,#17554,
#17555,#17556,#17557,#17558,#17559,#17560,#17561,#17562,#17563,#17564,#17565,
#17566,#17567,#17568,#17569,#17570,#17571,#17572,#17573,#17574,#17575,#17576,
#17577,#17578,#17579,#17580,#17581,#17582,#17583,#17584,#17585,#17586,#17587,
#17588,#17589,#17590,#17591,#17592,#17593,#17594,#17595,#17596,#17597,#17598,
#17599,#17600,#17601,#17602,#17603,#17604,#17605,#17606,#17607,#17608,#17609,
#17610,#17611,#17612,#17613,#17614,#17615,#17616,#17617,#17618,#17619,#17620,
#17621,#17622,#17623,#17624,#17625,#17626,#17627,#17628,#17629,#17630,#17631,
#17632,#17633,#17634,#17635,#17636,#17637,#17638,#17639,#17640,#17641,#17642,
#17643,#17644,#17645,#17646,#17647,#17648,#17649,#17650,#17651,#17652,#17653,
#17654,#17655,#17656,#17657,#17658,#17659,#17660,#17661,#17662,#17663,#17664,
#17665,#17666,#17667,#17668,#17669,#17670,#17671,#17672,#17673,#17674,#17675,
#17676,#17677,#17678,#17679,#17680,#17681,#17682,#17683,#17684,#17685,#17686,
#17687,#17688,#17689,#17690,#17691,#17692,#17693,#17694,#17695,#17696,#17697,
#17698,#17699,#17700,#17701,#17702,#17703,#17704,#17705,#17706,#17707,#17708,
#17709,#17710,#17711,#17712,#17713,#17714,#17715,#17716,#17717,#17718,#17719,
#17720,#17721,#17722,#17723,#17724,#17725,#17726,#17727),.UNSPECIFIED.,
 .F.,.F.,(4,2,2,2,2,2,2,2,2,2,2,2,2,2,2,2,2,2,2,2,2,2,2,2,2,2,2,2,2,2,2,
2,2,2,2,2,2,2,2,2,2,2,2,2,2,2,2,2,2,2,2,2,2,2,2,2,2,2,2,2,2,2,2,2,2,2,2,
2,2,2,2,2,2,2,2,2,2,2,2,2,2,2,2,2,2,2,2,2,2,2,2,2,2,2,2,2,2,2,2,2,2,2,2,
2,2,2,2,2,2,2,4),(-2.69239263445687,-2.68494805292635,-2.67978757582851,
-2.67652759501388,-2.67349885434821,-2.66956467689721,-2.66298349870764,
-2.61379696160392,-2.53759830361569,-2.52046772848944,-2.51694780762479,
-2.5149900667759,-2.51331288826232,-2.51119040705332,-2.5070224745021,-2.4798927647365,
-2.40627172202468,-2.37872696173466,-2.36190404259822,-2.35674724051752,
-2.35348795018369,-2.35045872477708,-2.34652231798558,-2.33993388396048,
-2.29039816588765,-2.21343866888421,-2.1973098812984,-2.19385165876666,
-2.19190731894903,-2.19022852360582,-2.18808704585153,-2.18368484504786,
-2.12738993921722,-2.07809390211431,-2.04143874025707,-2.03489625227751,
-2.03133286737907,-2.0286435069976,-2.02521479706254,-2.01929254210226,
-1.99380399589262,-1.90047394336956,-1.87536059273919,-1.87126783657065,
-1.86916122492772,-1.86748481286403,-1.86551428325093,-1.86193667845401,
-1.84381164453842,-1.76748207762536,-1.71950776176137,-1.71295045618029,
-1.7090227353855,-1.70599440352357,-1.7027303611341,-1.69755383773739,-1.68055691677225,
-1.6526106382063,-1.58404448324062,-1.57658767255684,-1.55222016781284,
-1.54815818923646,-1.54605823947949,-1.5443822550099,-1.54240654249387,
-1.53880490824678,-1.52023993554453,-1.43952662179443,-1.39620611486845,
-1.38976139100435,-1.38586671757373,-1.38284347951215,-1.37956458761676,
-1.37432049682264,-1.35669203415515,-1.32727163504134,-1.27006636671304,
-1.22975110607695,-1.22525614736234,-1.22309631817013,-1.22141572200668,
-1.21948350592894,-1.21608101054728,-1.20079837103807,-1.12319518883931,
-1.07341206272411,-1.06681839394118,-1.06288020816388,-1.05985041866396,
-1.05659131471602,-1.05143649823933,-1.03463531258242,-1.00713753647854,
-0.932945791112551,-0.906202381460083,-0.902047574576181,-0.899927721240331,
-0.898250515854938,-0.896290306607768,-0.892759858318587,-0.875456810432336,
-0.7994125013577,-0.750300164886178,-0.743719777385732,-0.739785450825536,
-0.736756249290266,-0.733495432987769,-0.728332911989022,-0.711461930755637,
-0.683804411334442,-0.662325194366873),.UNSPECIFIED.);
#194=B_SPLINE_CURVE_WITH_KNOTS('',3,(#17733,#17734,#17735,#17736,#17737,
#17738,#17739,#17740,#17741,#17742,#17743,#17744,#17745,#17746,#17747,#17748,
#17749,#17750,#17751,#17752,#17753,#17754,#17755,#17756,#17757,#17758,#17759,
#17760,#17761,#17762,#17763,#17764,#17765,#17766,#17767,#17768,#17769,#17770,
#17771,#17772,#17773,#17774,#17775,#17776,#17777,#17778,#17779,#17780,#17781,
#17782,#17783,#17784,#17785,#17786,#17787,#17788,#17789,#17790,#17791,#17792,
#17793,#17794,#17795,#17796,#17797,#17798,#17799,#17800,#17801,#17802,#17803,
#17804,#17805,#17806,#17807,#17808,#17809,#17810,#17811,#17812,#17813,#17814,
#17815,#17816,#17817,#17818,#17819,#17820,#17821,#17822,#17823,#17824,#17825,
#17826,#17827,#17828,#17829,#17830,#17831,#17832,#17833,#17834,#17835,#17836,
#17837,#17838,#17839,#17840,#17841,#17842,#17843,#17844,#17845,#17846,#17847,
#17848,#17849,#17850,#17851,#17852,#17853,#17854,#17855,#17856,#17857,#17858,
#17859,#17860,#17861,#17862,#17863,#17864,#17865,#17866,#17867,#17868,#17869,
#17870,#17871,#17872,#17873,#17874,#17875,#17876),.UNSPECIFIED.,.F.,.F.,
(4,2,2,2,2,2,2,2,2,2,2,2,2,2,2,2,2,2,2,2,2,2,2,2,2,2,2,2,2,2,2,2,2,2,2,
2,2,2,2,2,2,2,2,2,2,2,2,2,2,2,2,2,2,2,2,2,2,2,2,2,2,2,2,2,2,2,2,2,2,2,2,
4),(-1.37004935497571,-1.30316814073184,-1.27508590256901,-1.27088446362104,
-1.26875426131253,-1.26707578184677,-1.2651219901352,-1.26162275082394,
-1.24485306745913,-1.16838984102694,-1.11911934000211,-1.11253443969424,
-1.10859815524532,-1.10556786980449,-1.10230629761672,-1.09714344070059,
-1.08027875778301,-1.05263806889375,-0.979775356429106,-0.951992575268294,
-0.947800918301569,-0.945672799035891,-0.943994481073714,-0.942039177454788,
-0.938533010293787,-0.921649541242461,-0.845271004511879,-0.796040646420658,
-0.789456544497113,-0.78552049137532,-0.782490240252348,-0.77922856340077,
-0.774065238989404,-0.757196325440682,-0.729545946934489,-0.656785124254543,
-0.628922400823095,-0.624726474804089,-0.622597445431669,-0.620919056340561,
-0.618964412410942,-0.615461271852217,-0.598627651596522,-0.522212035718397,
-0.472963998196164,-0.466379541122371,-0.462443383869284,-0.459413115819201,
-0.456151483035575,-0.450988361150219,-0.434121298566828,-0.406475166261227,
-0.350586438844927,-0.306303489975825,-0.301784112712283,-0.299619152640829,
-0.298007594518476,-0.296141552441799,-0.293047574959632,-0.289240971296497,
-0.281509140178125,-0.260352216935445,-0.239235334321867,-0.154554828047918,
-0.144354980870009,-0.140409077232606,-0.137559226511286,-0.134521501711864,
-0.13046826243361,-0.121453444454761,-0.0678787593783522,-0.000963316407824259),
 .UNSPECIFIED.);
#195=B_SPLINE_CURVE_WITH_KNOTS('',3,(#17877,#17878,#17879,#17880,#17881,
#17882,#17883,#17884,#17885,#17886,#17887,#17888,#17889,#17890,#17891,#17892,
#17893,#17894,#17895,#17896,#17897,#17898,#17899,#17900,#17901,#17902,#17903,
#17904,#17905,#17906,#17907,#17908,#17909,#17910,#17911,#17912,#17913,#17914,
#17915,#17916,#17917,#17918,#17919,#17920,#17921,#17922,#17923,#17924,#17925,
#17926,#17927,#17928,#17929,#17930,#17931,#17932,#17933,#17934,#17935,#17936,
#17937,#17938,#17939,#17940,#17941,#17942,#17943,#17944,#17945,#17946,#17947,
#17948,#17949,#17950,#17951,#17952,#17953,#17954,#17955,#17956,#17957,#17958,
#17959,#17960,#17961,#17962,#17963,#17964,#17965,#17966,#17967,#17968,#17969,
#17970,#17971,#17972,#17973,#17974,#17975,#17976,#17977,#17978,#17979,#17980,
#17981,#17982,#17983,#17984),.UNSPECIFIED.,.F.,.F.,(4,2,2,2,2,2,2,2,2,2,
2,2,2,2,2,2,2,2,2,2,2,2,2,2,2,2,2,2,2,2,2,2,2,2,2,2,2,2,2,2,2,2,2,2,2,2,
2,2,2,2,2,2,2,4),(-4.06031153053636,-4.04337786345749,-4.03987712903709,
-4.03768755233355,-4.03602554017982,-4.03440578151757,-4.03254341866112,
-4.02945553836437,-4.01931539272372,-4.01724335198028,-4.00491278016662,
-3.92971739228819,-3.90024592326161,-3.88259511281969,-3.87734908052151,
-3.87406997879228,-3.87104721993485,-3.86715409244408,-3.86071386128505,
-3.81753542449335,-3.75502227978076,-3.73037489300684,-3.72181138694382,
-3.71771675965949,-3.71440415088888,-3.71250338171311,-3.71249836360561,
-3.71249331681531,-3.71248824113156,-3.71248313638129,-3.71247800235655,
-3.71247283886091,-3.71246764571772,-3.71246242269704,-3.7124571695903,
-3.71245188615722,-3.71244657221248,-3.71244122758163,-3.71243585200552,
-3.7108368205494,-3.70869548668606,-3.70429402468919,-3.67063532828294,
-3.60402318881109,-3.57639402337472,-3.55953435347856,-3.55437327240694,
-3.55111286546653,-3.54808369158684,-3.5441488901654,-3.53756650697364,
-3.48833563132933,-3.41194473479421,-3.39962357914392),.UNSPECIFIED.);
#196=B_SPLINE_CURVE_WITH_KNOTS('',3,(#17986,#17987,#17988,#17989,#17990,
#17991,#17992,#17993,#17994,#17995,#17996,#17997,#17998,#17999,#18000,#18001,
#18002,#18003,#18004,#18005,#18006,#18007,#18008,#18009,#18010,#18011,#18012,
#18013,#18014,#18015,#18016,#18017,#18018,#18019,#18020,#18021,#18022,#18023,
#18024,#18025,#18026,#18027,#18028,#18029,#18030,#18031,#18032,#18033,#18034,
#18035,#18036,#18037,#18038,#18039,#18040,#18041,#18042,#18043,#18044,#18045,
#18046,#18047,#18048,#18049,#18050,#18051,#18052,#18053,#18054,#18055,#18056,
#18057,#18058,#18059,#18060,#18061),.UNSPECIFIED.,.F.,.F.,(4,2,2,2,2,2,
2,2,2,2,2,2,2,2,2,2,2,2,2,2,2,2,2,2,2,2,2,2,2,2,2,2,2,2,2,2,2,4),(-0.662325194366873,
-0.621620560052431,-0.608018603129565,-0.583038657207035,-0.578951600005077,
-0.576846344508726,-0.575170178549449,-0.573198969096297,-0.569623919237428,
-0.551709241105021,-0.476114929834138,-0.42724563765023,-0.42067035999194,
-0.416737597903866,-0.413708728920349,-0.410447411189627,-0.405282263178068,
-0.388696553075173,-0.361559940071661,-0.301674190535358,-0.26057087022593,
-0.256069367877931,-0.253908347764074,-0.252227737227905,-0.250296533647604,
-0.248260527748304,-0.240825517343258,-0.203497007398002,-0.171011365616584,
-0.104354867742704,-0.0977149872544985,-0.0937633978297387,-0.0907315478861691,
-0.0874783116247841,-0.0823498995925742,-0.0763773277259736,-0.0649442964123356,
-0.000962519665250632),.UNSPECIFIED.);
#197=B_SPLINE_CURVE_WITH_KNOTS('',3,(#18062,#18063,#18064,#18065,#18066,
#18067,#18068,#18069,#18070,#18071,#18072,#18073,#18074,#18075,#18076,#18077,
#18078,#18079,#18080,#18081,#18082,#18083,#18084,#18085,#18086,#18087,#18088,
#18089,#18090,#18091,#18092,#18093,#18094,#18095,#18096,#18097,#18098,#18099,
#18100,#18101,#18102,#18103,#18104,#18105,#18106,#18107,#18108,#18109,#18110,
#18111,#18112,#18113,#18114,#18115,#18116,#18117,#18118,#18119,#18120,#18121,
#18122,#18123,#18124,#18125,#18126,#18127,#18128,#18129,#18130,#18131,#18132,
#18133,#18134,#18135,#18136,#18137,#18138,#18139,#18140,#18141,#18142,#18143,
#18144,#18145,#18146,#18147,#18148,#18149,#18150,#18151,#18152,#18153,#18154,
#18155,#18156,#18157,#18158,#18159,#18160,#18161,#18162,#18163,#18164,#18165,
#18166,#18167,#18168,#18169,#18170,#18171,#18172,#18173,#18174,#18175,#18176,
#18177,#18178,#18179,#18180,#18181,#18182,#18183,#18184,#18185,#18186,#18187,
#18188,#18189,#18190,#18191,#18192,#18193,#18194,#18195,#18196,#18197,#18198,
#18199,#18200,#18201,#18202,#18203,#18204,#18205,#18206,#18207,#18208,#18209,
#18210,#18211,#18212,#18213,#18214,#18215),.UNSPECIFIED.,.F.,.F.,(4,2,2,
2,2,2,2,2,2,2,2,2,2,2,2,2,2,2,2,2,2,2,2,2,2,2,2,2,2,2,2,2,2,2,2,2,2,2,2,
2,2,2,2,2,2,2,2,2,2,2,2,2,2,2,2,2,2,2,2,2,2,2,2,2,2,2,2,2,2,2,2,2,2,2,2,
2,4),(-4.06032274020453,-4.0029643398074,-3.99696048208845,-3.99378252294505,
-3.99172667450296,-3.98978165610366,-3.98810331451559,-3.98596376197808,
-3.98157005092537,-3.92462360203421,-3.89235197403768,-3.85324049661156,
-3.83678405184572,-3.83162472556174,-3.82836505943201,-3.82533632658513,
-3.82140175531127,-3.81481902818917,-3.76554685382997,-3.68917231439229,
-3.67230747717275,-3.6688197833286,-3.66685353860644,-3.66517720869091,
-3.66306617230716,-3.65895148834677,-3.63326063075447,-3.55733803239008,
-3.53029632549652,-3.51375363272254,-3.50859229192791,-3.50533207760003,
-3.50230333530921,-3.4983694613703,-3.49178946412029,-3.44266758315225,
-3.36659708823063,-3.34928753844733,-3.34575697895428,-3.3437968986097,
-3.34211991421794,-3.34000049329885,-3.33584698625794,-3.30912508433863,
-3.23496745662917,-3.20748843670299,-3.19069417538195,-3.18554047188149,
-3.18228182566897,-3.17925229075347,-3.17531419091688,-3.16872007524078,
-3.11890072808387,-3.04120185447702,-3.02599161240632,-3.0225941742133,
-3.02066314539534,-3.01898249002419,-3.01682117035122,-3.01231817897828,
-2.97099042824152,-2.89189611096141,-2.86875351755784,-2.86300673510385,
-2.85961678094982,-2.85661848955385,-2.85286316036893,-2.84701836752918,
-2.81766043200606,-2.74380101561582,-2.71651328172788,-2.70273126574828,
-2.69943726530728,-2.69752905649933,-2.69584443467197,-2.69368276982011,
-2.69185776365183),.UNSPECIFIED.);
#198=B_SPLINE_CURVE_WITH_KNOTS('',3,(#18220,#18221,#18222,#18223,#18224,
#18225,#18226,#18227,#18228,#18229,#18230,#18231,#18232,#18233,#18234,#18235,
#18236,#18237,#18238,#18239,#18240,#18241,#18242,#18243,#18244,#18245,#18246,
#18247,#18248,#18249,#18250,#18251,#18252,#18253,#18254,#18255,#18256,#18257,
#18258,#18259,#18260,#18261,#18262,#18263,#18264,#18265,#18266,#18267,#18268,
#18269,#18270,#18271,#18272,#18273,#18274,#18275,#18276,#18277,#18278,#18279,
#18280,#18281,#18282,#18283,#18284,#18285,#18286,#18287,#18288,#18289,#18290,
#18291,#18292,#18293,#18294,#18295,#18296,#18297,#18298,#18299,#18300,#18301,
#18302,#18303,#18304,#18305,#18306,#18307,#18308,#18309,#18310,#18311,#18312,
#18313,#18314,#18315,#18316,#18317,#18318,#18319,#18320,#18321,#18322,#18323,
#18324,#18325,#18326,#18327,#18328,#18329,#18330,#18331,#18332,#18333,#18334,
#18335,#18336,#18337,#18338,#18339,#18340,#18341,#18342,#18343,#18344,#18345,
#18346,#18347,#18348,#18349,#18350,#18351,#18352,#18353,#18354,#18355,#18356,
#18357,#18358,#18359,#18360,#18361,#18362,#18363,#18364,#18365,#18366,#18367,
#18368,#18369,#18370,#18371,#18372,#18373,#18374,#18375,#18376,#18377,#18378,
#18379,#18380,#18381,#18382,#18383,#18384,#18385,#18386,#18387,#18388,#18389,
#18390,#18391,#18392,#18393,#18394,#18395,#18396,#18397,#18398,#18399,#18400,
#18401,#18402,#18403,#18404,#18405,#18406,#18407,#18408,#18409,#18410,#18411,
#18412,#18413,#18414,#18415,#18416,#18417,#18418,#18419,#18420,#18421,#18422,
#18423,#18424,#18425,#18426,#18427,#18428,#18429,#18430,#18431,#18432,#18433,
#18434,#18435,#18436,#18437,#18438,#18439,#18440,#18441,#18442,#18443),
 .UNSPECIFIED.,.F.,.F.,(4,2,2,2,2,2,2,2,2,2,2,2,2,2,2,2,2,2,2,2,2,2,2,2,
2,2,2,2,2,2,2,2,2,2,2,2,2,2,2,2,2,2,2,2,2,2,2,2,2,2,2,2,2,2,2,2,2,2,2,2,
2,2,2,2,2,2,2,2,2,2,2,2,2,2,2,2,2,2,2,2,2,2,2,2,2,2,2,2,2,2,2,2,2,2,2,2,
2,2,2,2,2,2,2,2,2,2,2,2,2,2,2,4),(-3.39991501201283,-3.39345442372656,-3.37665005401964,
-3.37149486401831,-3.36823562909115,-3.36520578297209,-3.3612676059447,
-3.35467405689956,-3.30553505650724,-3.22928879242379,-3.21220158311604,
-3.2086837866258,-3.20672627421138,-3.2050486941596,-3.20292490283201,-3.19875196737591,
-3.17149249005129,-3.09805189021828,-3.07049681717889,-3.05366894177034,
-3.04851097485566,-3.04525100791085,-3.0422211882679,-3.03828405016965,
-3.03169445596438,-2.98213317121262,-2.90499601432808,-2.88907364817869,
-2.8856282865663,-2.88368652823139,-2.88200701387048,-2.87986075446862,
-2.87642247903201,-2.85769637695237,-2.84740651144653,-2.77524290204827,
-2.74756181080354,-2.73067861535782,-2.72551434636221,-2.72225284941904,
-2.71922330010793,-2.71528891535136,-2.70870922083855,-2.65966344348674,
-2.58364611166234,-2.56622778027109,-2.56269012550498,-2.56072814470679,
-2.55905077458164,-2.55693241659781,-2.55278559079498,-2.52626970400944,
-2.45183508084819,-2.42440177563854,-2.40762658908115,-2.40247403801786,
-2.3992150103115,-2.39618434659084,-2.39224367012597,-2.38564276453107,
-2.33586123923847,-2.25811321899252,-2.24293244070949,-2.23953634468984,
-2.23760525727645,-2.23592401148195,-2.23376118932813,-2.22925246092525,
-2.18727835725855,-2.10664200274483,-2.08540275664059,-2.07981265642086,
-2.07645674546735,-2.07345186214115,-2.06963865725166,-2.06360633982676,
-2.03102102860358,-1.93972231387027,-1.92057209399014,-1.91711005558114,
-1.91495638976978,-1.91327589711605,-1.91133845490602,-1.90791391122118,
-1.89231500458797,-1.81494268268359,-1.7652879232096,-1.75869541543018,
-1.75475692013079,-1.75172629759428,-1.74846570593911,-1.74330726207455,
-1.72648256991856,-1.69893343246994,-1.62520298955981,-1.59810754751318,
-1.59393932164531,-1.59181620342651,-1.59013826432075,-1.58817929600144,
-1.58465630998329,-1.56749261689379,-1.49132017802214,-1.44219083683902,
-1.43560875957085,-1.43167329690249,-1.42864313788405,-1.42538120308981,
-1.4202167090565,-1.40333715081822,-1.37566236463397,-1.37004935497571),
 .UNSPECIFIED.);
#199=B_SPLINE_CURVE_WITH_KNOTS('',3,(#18444,#18445,#18446,#18447,#18448,
#18449,#18450,#18451,#18452,#18453,#18454,#18455,#18456,#18457,#18458,#18459,
#18460,#18461,#18462,#18463,#18464,#18465,#18466,#18467,#18468,#18469,#18470,
#18471,#18472,#18473,#18474,#18475,#18476,#18477,#18478,#18479,#18480,#18481,
#18482,#18483,#18484,#18485,#18486,#18487,#18488,#18489,#18490,#18491,#18492,
#18493,#18494,#18495,#18496,#18497,#18498,#18499,#18500,#18501,#18502,#18503,
#18504,#18505,#18506,#18507,#18508,#18509,#18510,#18511,#18512,#18513,#18514,
#18515,#18516,#18517,#18518,#18519,#18520,#18521,#18522,#18523,#18524,#18525,
#18526,#18527,#18528,#18529,#18530,#18531,#18532,#18533,#18534,#18535,#18536,
#18537,#18538,#18539,#18540,#18541,#18542,#18543,#18544,#18545,#18546,#18547,
#18548,#18549,#18550,#18551,#18552,#18553,#18554,#18555,#18556,#18557,#18558,
#18559,#18560,#18561,#18562,#18563,#18564,#18565,#18566,#18567,#18568,#18569,
#18570,#18571,#18572,#18573,#18574,#18575,#18576,#18577,#18578,#18579,#18580,
#18581,#18582,#18583,#18584,#18585,#18586,#18587,#18588,#18589,#18590,#18591,
#18592,#18593,#18594,#18595,#18596,#18597,#18598,#18599,#18600,#18601,#18602,
#18603,#18604,#18605,#18606,#18607,#18608,#18609,#18610,#18611,#18612,#18613,
#18614,#18615,#18616,#18617,#18618,#18619,#18620,#18621,#18622,#18623,#18624,
#18625,#18626,#18627,#18628,#18629,#18630,#18631,#18632,#18633,#18634,#18635,
#18636,#18637,#18638,#18639,#18640,#18641,#18642,#18643,#18644,#18645,#18646,
#18647,#18648,#18649,#18650,#18651,#18652,#18653,#18654,#18655,#18656,#18657,
#18658,#18659),.UNSPECIFIED.,.F.,.F.,(4,2,2,2,2,2,2,2,2,2,2,2,2,2,2,2,2,
2,2,2,2,2,2,2,2,2,2,2,2,2,2,2,2,2,2,2,2,2,2,2,2,2,2,2,2,2,2,2,2,2,2,2,2,
2,2,2,2,2,2,2,2,2,2,2,2,2,2,2,2,2,2,2,2,2,2,2,2,2,2,2,2,2,2,2,2,2,2,2,2,
2,2,2,2,2,2,2,2,2,2,2,2,2,2,2,2,2,2,4),(-2.69185776365183,-2.69011522243236,
-2.66887324319072,-2.66578991693006,-2.59970034798892,-2.55286621498866,
-2.54260066877817,-2.53833082283421,-2.53525625018545,-2.53245844063289,
-2.52801166844107,-2.51744500526503,-2.43681858930947,-2.38241246471018,
-2.37741566449612,-2.37516066407725,-2.37346863349736,-2.3715910242174,
-2.36843513621108,-2.35769589049127,-2.35462114311805,-2.26430705004553,
-2.23770937025894,-2.22130331938517,-2.21619268735876,-2.21294337196981,
-2.20991004527207,-2.20594917554656,-2.19927726951026,-2.14453930563011,
-2.10359019015327,-2.0582639461155,-2.053956505212,-2.05183387784789,-2.0501565999447,
-2.04819875093182,-2.04477239962098,-2.03083609207311,-1.95379076131783,
-1.90228984726655,-1.89566395175114,-1.89171654248501,-1.88868549094888,
-1.88543075170768,-1.88029497582514,-1.8636632269489,-1.83655074693802,
-1.76056834394419,-1.73495980715647,-1.73084790252123,-1.72873734218499,
-1.72706089257217,-1.72509392070327,-1.72153194599341,-1.70367925176042,
-1.6280315823551,-1.57913246929307,-1.57255679112061,-1.56862398571894,
-1.56559519817769,-1.56233408129141,-1.55716949276554,-1.54027747389885,
-1.51257088787475,-1.44041285476932,-1.43041110572576,-1.4113661222423,
-1.4079107040605,-1.40575947822954,-1.40407980613193,-1.40214211369403,
-1.39871427561739,-1.38305180528749,-1.30576441560168,-1.25609922269104,
-1.24950829419693,-1.24557105796173,-1.24254159773214,-1.23928245321785,
-1.23412673238752,-1.21731510452061,-1.18979262820455,-1.11581588114309,
-1.08891594602433,-1.08475576897062,-1.08263485989711,-1.08095769287635,
-1.07899853584173,-1.07547250829191,-1.05824120998824,-0.982151646551871,
-0.933017011339356,-0.92643659949887,-0.922502418317421,-0.919473422223947,
-0.91621291918644,-0.911051090528244,-0.89418413186103,-0.86653500112858,
-0.793732316900753,-0.765906651706445,-0.761714723678455,-0.759587035115249,
-0.75790935535832,-0.755955170659562,-0.752451970165263,-0.735601654619297,
-0.661806132235414),.UNSPECIFIED.);
#200=B_SPLINE_CURVE_WITH_KNOTS('',3,(#18665,#18666,#18667,#18668,#18669,
#18670,#18671,#18672,#18673,#18674,#18675,#18676,#18677,#18678,#18679,#18680,
#18681,#18682,#18683,#18684,#18685,#18686,#18687,#18688,#18689,#18690,#18691,
#18692,#18693,#18694,#18695,#18696,#18697,#18698,#18699,#18700,#18701,#18702,
#18703,#18704,#18705,#18706,#18707,#18708,#18709,#18710,#18711,#18712,#18713,
#18714,#18715,#18716,#18717,#18718,#18719,#18720,#18721,#18722,#18723,#18724,
#18725,#18726,#18727,#18728,#18729,#18730,#18731,#18732,#18733,#18734,#18735,
#18736,#18737,#18738,#18739,#18740,#18741,#18742,#18743,#18744,#18745,#18746,
#18747,#18748,#18749,#18750,#18751,#18752,#18753,#18754,#18755,#18756,#18757,
#18758,#18759,#18760,#18761,#18762,#18763,#18764,#18765,#18766,#18767,#18768,
#18769,#18770,#18771,#18772,#18773,#18774,#18775,#18776,#18777,#18778,#18779,
#18780,#18781,#18782,#18783,#18784,#18785,#18786,#18787,#18788,#18789,#18790,
#18791,#18792,#18793,#18794,#18795,#18796,#18797,#18798,#18799,#18800,#18801,
#18802,#18803,#18804,#18805,#18806,#18807,#18808,#18809,#18810,#18811,#18812,
#18813,#18814,#18815,#18816,#18817,#18818,#18819,#18820,#18821,#18822,#18823,
#18824,#18825,#18826,#18827,#18828,#18829,#18830,#18831,#18832,#18833,#18834,
#18835,#18836,#18837,#18838,#18839,#18840,#18841,#18842,#18843,#18844,#18845,
#18846,#18847,#18848,#18849,#18850),.UNSPECIFIED.,.F.,.F.,(4,2,2,2,2,2,
2,2,2,2,2,2,2,2,2,2,2,2,2,2,2,2,2,2,2,2,2,2,2,2,2,2,2,2,2,2,2,2,2,2,2,2,
2,2,2,2,2,2,2,2,2,2,2,2,2,2,2,2,2,2,2,2,2,2,2,2,2,2,2,2,2,2,2,2,2,2,2,2,
2,2,2,2,2,2,2,2,2,2,2,2,2,2,4),(-1.36964398461014,-1.30787036768949,-1.25862000725445,
-1.2520356836026,-1.24809963001014,-1.24506945573577,-1.24180793764911,
-1.23664502665887,-1.21977891576258,-1.19213461110797,-1.11932109461955,
-1.09150126983046,-1.08730849104993,-1.08518017131057,-1.08350188516868,
-1.08154683679123,-1.07804166930726,-1.0611734016892,-0.984786360060719,
-0.935552333209351,-0.928968333089632,-0.925032372734004,-0.922002211681342,
-0.918740650150646,-0.913577547455394,-0.896709709080528,-0.869061450526312,
-0.796289558865995,-0.768436007700299,-0.76424211652404,-0.76211355924542,
-0.760435254081098,-0.758480376837962,-0.754975996212281,-0.738120704482538,
-0.661723985771594,-0.612490423452113,-0.605903513901242,-0.601966703963024,
-0.598936408806204,-0.595675214938031,-0.590513785297814,-0.573661179874451,
-0.546047837680169,-0.472918049055438,-0.445352232790946,-0.441167919476765,
-0.439041401817279,-0.437363250721846,-0.435406881119683,-0.431895666438514,
-0.414927493372728,-0.338614211363969,-0.289438801861166,-0.282842694337029,
-0.278903197516473,-0.275872475145974,-0.275744229622131,-0.275663461074198,
-0.275612027540513,-0.275545308692106,-0.275484326182795,-0.27542850359385,
-0.275377333937562,-0.27533036756179,-0.275287207698183,-0.275247502029057,
-0.275210936783149,-0.275177231737833,-0.275146135974347,-0.275117424244362,
-0.275090893867485,-0.275066362062654,-0.275030741949859,-0.274995717425154,
-0.274961269477776,-0.274927379821316,-0.274894030862295,-0.274861205675903,
-0.271315827317332,-0.264820300500427,-0.256683991552925,-0.23908598672357,
-0.20187095921567,-0.125478243713695,-0.119168203703918,-0.116615849001147,
-0.115044020776078,-0.113306101322337,-0.110791914038808,-0.104250209816162,
-0.0699368801188113,-0.00096324508092347),.UNSPECIFIED.);
#201=B_SPLINE_CURVE_WITH_KNOTS('',3,(#18851,#18852,#18853,#18854,#18855,
#18856,#18857,#18858,#18859,#18860,#18861,#18862,#18863,#18864,#18865,#18866,
#18867,#18868,#18869,#18870,#18871,#18872,#18873,#18874,#18875,#18876,#18877,
#18878,#18879,#18880,#18881,#18882,#18883,#18884,#18885,#18886,#18887,#18888,
#18889,#18890,#18891,#18892,#18893,#18894,#18895,#18896,#18897,#18898,#18899,
#18900,#18901,#18902,#18903,#18904,#18905,#18906,#18907,#18908,#18909,#18910,
#18911,#18912,#18913,#18914,#18915,#18916,#18917,#18918,#18919,#18920,#18921,
#18922,#18923,#18924,#18925,#18926,#18927,#18928,#18929,#18930,#18931,#18932,
#18933,#18934,#18935,#18936,#18937,#18938,#18939,#18940,#18941,#18942,#18943,
#18944,#18945,#18946,#18947,#18948,#18949,#18950,#18951,#18952,#18953,#18954,
#18955,#18956,#18957,#18958,#18959,#18960,#18961,#18962,#18963,#18964,#18965,
#18966,#18967,#18968,#18969,#18970,#18971,#18972),.UNSPECIFIED.,.F.,.F.,
(4,2,2,2,2,2,2,2,2,2,2,2,2,2,2,2,2,2,2,2,2,2,2,2,2,2,2,2,2,2,2,2,2,2,2,
2,2,2,2,2,2,2,2,2,2,2,2,2,2,2,2,2,2,2,2,2,2,2,2,2,4),(-4.06096075769659,
-4.02702016228667,-4.02161774880303,-4.01804907544626,-4.01518409485397,
-4.01219364805124,-4.00872859622936,-4.0027979321248,-3.97981170917957,
-3.9607497434034,-3.88878313622104,-3.86163760844338,-3.85584747678854,
-3.8534538355195,-3.85173957147312,-3.85014213452476,-3.84745286779896,
-3.84029096437282,-3.77158348104996,-3.72486017122474,-3.70908029182896,
-3.70155565958667,-3.69544145550076,-3.69199045646421,-3.69196840230189,
-3.69194563088792,-3.69192211695931,-3.69189783427802,-3.69187275351379,
-3.69184684426837,-3.69182008162368,-3.69179243499257,-3.69176387258149,
-3.69173436137362,-3.69170386705747,-3.69167235397824,-3.69163978510591,
-3.6916061219818,-3.6915713246456,-3.69153535089833,-3.69150443643219,-3.69146865913723,
-3.69142724960061,-3.69137931607739,-3.69132382527268,-3.69125958038549,
-3.69120454515646,-3.68817479713999,-3.68423640456368,-3.67764173760504,
-3.6285632828689,-3.55242734410894,-3.53519541240001,-3.53166915373654,
-3.52970986445656,-3.52803256597843,-3.52591144305972,-3.52175067559592,
-3.49483322852289,-3.42095634108256,-3.39991501201283),.UNSPECIFIED.);
#202=B_SPLINE_CURVE_WITH_KNOTS('',3,(#18974,#18975,#18976,#18977,#18978,
#18979,#18980,#18981,#18982,#18983,#18984,#18985,#18986,#18987,#18988,#18989,
#18990,#18991,#18992,#18993,#18994,#18995,#18996,#18997,#18998,#18999,#19000,
#19001,#19002,#19003,#19004,#19005,#19006,#19007,#19008,#19009,#19010,#19011,
#19012,#19013,#19014,#19015,#19016,#19017,#19018,#19019,#19020,#19021,#19022,
#19023,#19024,#19025,#19026,#19027,#19028,#19029,#19030,#19031,#19032,#19033,
#19034,#19035,#19036,#19037,#19038,#19039,#19040,#19041,#19042,#19043,#19044,
#19045,#19046,#19047),.UNSPECIFIED.,.F.,.F.,(4,2,2,2,2,2,2,2,2,2,2,2,2,
2,2,2,2,2,2,2,2,2,2,2,2,2,2,2,2,2,2,2,2,2,2,2,4),(-0.661806132235414,-0.659232099503259,
-0.609956994452256,-0.60337542136454,-0.599440900228318,-0.596411849531053,
-0.593151491739137,-0.587990327919851,-0.571129437951296,-0.543494225960171,
-0.470546102915199,-0.442837739933146,-0.438649694709232,-0.43652283227735,
-0.434845214607481,-0.432890425073598,-0.429384457480762,-0.412488561200852,
-0.336152749283856,-0.286917691182195,-0.280323175420384,-0.276384876704873,
-0.273355229687206,-0.270553938311786,-0.266011484641358,-0.253517352890303,
-0.234974049864926,-0.198665794027236,-0.123059326398487,-0.116682576387896,
-0.114119564698602,-0.112546173871279,-0.110811188703143,-0.108309325613893,
-0.101844355914692,-0.0529083787368607,-0.0009632262016002),
 .UNSPECIFIED.);
#203=B_SPLINE_CURVE_WITH_KNOTS('',3,(#19048,#19049,#19050,#19051,#19052,
#19053,#19054,#19055),.UNSPECIFIED.,.F.,.F.,(4,1,1,1,1,4),(109.955742875643,
110.609869450541,111.609815462892,112.609761475243,113.609707487595,114.192220932897),
 .UNSPECIFIED.);
#204=B_SPLINE_CURVE_WITH_KNOTS('',3,(#19060,#19061,#19062,#19063,#19064,
#19065,#19066,#19067,#19068,#19069,#19070,#19071,#19072,#19073,#19074,#19075,
#19076,#19077,#19078,#19079,#19080,#19081,#19082,#19083,#19084,#19085,#19086,
#19087,#19088,#19089,#19090,#19091,#19092,#19093,#19094,#19095,#19096,#19097,
#19098,#19099,#19100,#19101,#19102,#19103,#19104,#19105,#19106,#19107,#19108,
#19109,#19110,#19111,#19112,#19113,#19114,#19115,#19116,#19117,#19118,#19119,
#19120,#19121,#19122,#19123,#19124,#19125,#19126,#19127,#19128,#19129,#19130,
#19131,#19132,#19133,#19134,#19135,#19136,#19137,#19138,#19139,#19140,#19141,
#19142,#19143,#19144,#19145,#19146,#19147,#19148,#19149,#19150,#19151,#19152,
#19153,#19154,#19155,#19156,#19157,#19158,#19159,#19160,#19161,#19162,#19163,
#19164,#19165,#19166,#19167,#19168,#19169,#19170,#19171,#19172,#19173,#19174,
#19175,#19176,#19177,#19178,#19179,#19180,#19181,#19182,#19183,#19184,#19185,
#19186,#19187,#19188,#19189,#19190,#19191,#19192,#19193,#19194,#19195,#19196,
#19197,#19198,#19199,#19200,#19201,#19202,#19203,#19204,#19205,#19206,#19207,
#19208,#19209,#19210,#19211,#19212,#19213,#19214,#19215,#19216,#19217,#19218,
#19219,#19220,#19221,#19222,#19223,#19224,#19225,#19226,#19227,#19228,#19229,
#19230,#19231,#19232,#19233,#19234,#19235,#19236,#19237,#19238,#19239,#19240,
#19241,#19242,#19243,#19244,#19245,#19246,#19247,#19248,#19249,#19250,#19251,
#19252,#19253,#19254,#19255,#19256,#19257,#19258,#19259,#19260,#19261,#19262,
#19263,#19264,#19265,#19266,#19267,#19268,#19269,#19270,#19271,#19272,#19273,
#19274,#19275,#19276,#19277,#19278,#19279,#19280,#19281,#19282,#19283),
 .UNSPECIFIED.,.F.,.F.,(4,2,2,2,2,2,2,2,2,2,2,2,2,2,2,2,2,2,2,2,2,2,2,2,
2,2,2,2,2,2,2,2,2,2,2,2,2,2,2,2,2,2,2,2,2,2,2,2,2,2,2,2,2,2,2,2,2,2,2,2,
2,2,2,2,2,2,2,2,2,2,2,2,2,2,2,2,2,2,2,2,2,2,2,2,2,2,2,2,2,2,2,2,2,2,2,2,
2,2,2,2,2,2,2,2,2,2,2,2,2,2,2,4),(-3.39957621942377,-3.36840457402077,-3.35166715085571,
-3.34817048919824,-3.34621757395302,-3.34453949102032,-3.34240934561185,
-3.33820666059612,-3.31005425626266,-3.23772473101716,-3.21005985651988,
-3.19318399210446,-3.1880207067793,-3.18475954128355,-3.18173009996059,
-3.17779557179278,-3.17121501276587,-3.12211117812336,-3.0459803515002,
-3.02872615917451,-3.02519827356027,-3.02323848199042,-3.02156100045507,
-3.01943996233688,-3.01528030713941,-2.98840527157683,-2.91445906518644,
-2.88696126161422,-2.87015809802642,-2.86500263108062,-2.86174307153667,
-2.85871282032469,-2.85477396988832,-2.84817896930698,-2.79836212890475,
-2.72053977426467,-2.70545398054485,-2.70206455449886,-2.70013499531584,
-2.69845361887413,-2.6962887114841,-2.69176895887232,-2.64771555107662,
-2.59371778131214,-2.55418936333725,-2.54480517609524,-2.54068580713233,
-2.53763729196339,-2.53480505555941,-2.53092695068876,-2.52113495693993,
-2.4328015752523,-2.41310204462584,-2.38612393470597,-2.38035138889777,
-2.37796006629271,-2.37624566443678,-2.37464667622878,-2.37195182770506,
-2.36475777447206,-2.27243897285695,-2.24220878385379,-2.22423773717541,
-2.21895734552988,-2.21567003355091,-2.21264864466204,-2.20876969365635,
-2.20237959461258,-2.16107688477461,-2.07840245512471,-2.05965259231551,
-2.05604042559745,-2.05406215894052,-2.05238592155259,-2.05028804676869,
-2.04700914838919,-2.03091324113586,-1.95416082996037,-1.9047595121799,
-1.89817218983878,-1.89423526586641,-1.89120496046708,-1.8879438319143,
-1.88278266828884,-1.86593238656111,-1.83832433332555,-1.76514368924867,
-1.7376186902314,-1.73343576532241,-1.73130954748688,-1.72963142370578,
-1.72767484525042,-1.72416265627099,-1.70717818267533,-1.6308771854719,
-1.58168466051326,-1.57510149395278,-1.57116577769228,-1.56813565593813,
-1.56487399031081,-1.55971041075653,-1.54283821829316,-1.51517997197715,
-1.4425154598664,-1.41457483342667,-1.4103780916217,-1.40824892812153,-1.40657057713253,
-1.40461614273153,-1.40111378751317,-1.38429176281064,-1.36964398461014),
 .UNSPECIFIED.);
#205=B_SPLINE_CURVE_WITH_KNOTS('',3,(#19285,#19286,#19287,#19288,#19289,
#19290),.UNSPECIFIED.,.F.,.F.,(4,1,1,4),(114.192220932897,114.609653499946,
115.609599512298,116.238928182823),.UNSPECIFIED.);
#206=B_SPLINE_CURVE_WITH_KNOTS('',3,(#19291,#19292,#19293,#19294,#19295,
#19296,#19297,#19298,#19299,#19300,#19301,#19302,#19303,#19304,#19305,#19306,
#19307,#19308,#19309,#19310,#19311,#19312,#19313,#19314,#19315,#19316,#19317,
#19318,#19319,#19320,#19321,#19322,#19323,#19324,#19325,#19326,#19327,#19328,
#19329,#19330,#19331,#19332,#19333,#19334,#19335,#19336,#19337,#19338,#19339,
#19340,#19341,#19342,#19343,#19344,#19345,#19346,#19347,#19348,#19349,#19350,
#19351,#19352,#19353,#19354,#19355,#19356,#19357,#19358,#19359,#19360,#19361,
#19362,#19363,#19364,#19365,#19366,#19367,#19368,#19369,#19370,#19371,#19372,
#19373,#19374,#19375,#19376,#19377,#19378,#19379,#19380,#19381,#19382,#19383,
#19384,#19385,#19386,#19387,#19388,#19389,#19390,#19391,#19392,#19393,#19394,
#19395,#19396,#19397,#19398,#19399,#19400,#19401,#19402,#19403,#19404,#19405,
#19406,#19407,#19408,#19409,#19410,#19411,#19412,#19413,#19414,#19415,#19416,
#19417,#19418,#19419,#19420,#19421,#19422,#19423,#19424,#19425,#19426,#19427,
#19428,#19429,#19430,#19431,#19432,#19433,#19434,#19435,#19436,#19437,#19438,
#19439,#19440,#19441,#19442,#19443,#19444,#19445,#19446,#19447,#19448,#19449,
#19450,#19451,#19452,#19453,#19454,#19455,#19456,#19457,#19458,#19459,#19460,
#19461,#19462,#19463,#19464,#19465,#19466,#19467,#19468,#19469,#19470,#19471,
#19472,#19473,#19474,#19475,#19476,#19477,#19478,#19479,#19480),
 .UNSPECIFIED.,.F.,.F.,(4,2,2,2,2,2,2,2,2,2,2,2,2,2,2,2,2,2,2,2,2,2,2,2,
2,2,2,2,2,2,2,2,2,2,2,2,2,2,2,2,2,2,2,2,2,2,2,2,2,2,2,2,2,2,2,2,2,2,2,2,
2,2,2,2,2,2,2,2,2,2,2,2,2,2,2,2,2,2,2,2,2,2,2,2,2,2,2,2,2,2,2,2,2,2,4),
(-4.06040871516838,-3.98561996845687,-3.95150132255625,-3.94498018359608,
-3.94246973479271,-3.94073306247043,-3.93916136612688,-3.93660734122501,
-3.93028386314145,-3.85406055927773,-3.81663656903841,-3.79911177686931,
-3.79099999589345,-3.78451420574077,-3.78097493073977,-3.78094221922002,
-3.78090898252618,-3.78087520346131,-3.78084086414446,-3.78080594597525,
-3.78077042959487,-3.78074621756581,-3.78072001943858,-3.78069165202857,
-3.78066091199668,-3.78062757310575,-3.7805913830117,-3.78055205953629,
-3.78050928626375,-3.78046270733438,-3.78041192131598,-3.78035647317105,
-3.78029584627666,-3.7802294546284,-3.78017959401717,-3.78010083951496,
-3.77997499628559,-3.77694531454117,-3.77300702978469,-3.76641261758707,
-3.71738910161496,-3.64145606542709,-3.62394226675987,-3.62039952805431,
-3.61843667768679,-3.61675976645174,-3.61464355992879,-3.61050564369955,
-3.58421685958437,-3.50945136624098,-3.48205857617288,-3.46530159294761,
-3.46015167638995,-3.4568936522188,-3.45386346979838,-3.44992278447107,
-3.44332048862746,-3.39435577650409,-3.31850475123958,-3.3008691130312,
-3.29731921487219,-3.29535474861058,-3.29367789171355,-3.29156358497465,
-3.28743481430705,-3.26139297492324,-3.18542649623018,-3.15863614682001,
-3.14214428787527,-3.13702374619963,-3.13377208554197,-3.13073932471084,
-3.12678314106674,-3.12012791486282,-3.05394667575203,-3.00685862797471,
-2.98770205543889,-2.98047704821159,-2.9752315416193,-2.97293153549146,
-2.97123283850945,-2.96937644408859,-2.96631571418806,-2.9564082552727,
-2.85545011160786,-2.82140468195996,-2.81498172230503,-2.81144413211794,
-2.80875175576088,-2.80529961745094,-2.79942549166939,-2.77707903443562,
-2.7584321187987,-2.6934347578505,-2.69158011258058),.UNSPECIFIED.);
#207=B_SPLINE_CURVE_WITH_KNOTS('',3,(#19486,#19487,#19488,#19489,#19490,
#19491,#19492,#19493,#19494,#19495,#19496,#19497,#19498,#19499,#19500,#19501,
#19502,#19503,#19504,#19505,#19506,#19507,#19508,#19509,#19510,#19511,#19512,
#19513,#19514,#19515,#19516,#19517,#19518,#19519,#19520,#19521,#19522,#19523,
#19524,#19525,#19526,#19527,#19528,#19529,#19530,#19531,#19532,#19533,#19534,
#19535,#19536,#19537,#19538,#19539,#19540,#19541,#19542,#19543,#19544,#19545,
#19546,#19547,#19548,#19549,#19550,#19551,#19552,#19553,#19554,#19555,#19556,
#19557,#19558,#19559,#19560,#19561,#19562,#19563,#19564,#19565,#19566,#19567,
#19568,#19569,#19570,#19571,#19572,#19573,#19574,#19575,#19576,#19577,#19578,
#19579,#19580,#19581,#19582,#19583,#19584,#19585,#19586,#19587,#19588,#19589,
#19590,#19591,#19592,#19593,#19594,#19595,#19596,#19597,#19598,#19599,#19600,
#19601,#19602,#19603,#19604,#19605,#19606,#19607,#19608,#19609,#19610,#19611,
#19612,#19613,#19614,#19615,#19616,#19617,#19618,#19619,#19620,#19621,#19622,
#19623,#19624,#19625,#19626,#19627,#19628,#19629,#19630,#19631,#19632,#19633,
#19634,#19635,#19636,#19637,#19638,#19639),.UNSPECIFIED.,.F.,.F.,(4,2,2,
2,2,2,2,2,2,2,2,2,2,2,2,2,2,2,2,2,2,2,2,2,2,2,2,2,2,2,2,2,2,2,2,2,2,2,2,
2,2,2,2,2,2,2,2,2,2,2,2,2,2,2,2,2,2,2,2,2,2,2,2,2,2,2,2,2,2,2,2,2,2,2,2,
2,4),(-1.37009647383181,-1.36007120758124,-1.33238914503019,-1.25997509255448,
-1.23182677303776,-1.22762319405347,-1.22549253035165,-1.22381400741873,
-1.22186053234231,-1.2183627697852,-1.20161741699309,-1.12513556989821,
-1.07585628150257,-1.06927117945961,-1.06533482674828,-1.06230451934517,
-1.05904295364416,-1.05388017120111,-1.0370163065357,-1.00937754466157,
-0.936493073653841,-0.908727439832827,-0.90453633532472,-0.902408327938482,
-0.900730011415827,-0.898774609752667,-0.895268018965813,-0.878377755431324,
-0.80200383629688,-0.752775629770619,-0.746191544205418,-0.742255486244925,
-0.739225222851115,-0.735963524374353,-0.730800147787975,-0.71393090304407,
-0.686279817812463,-0.620043075587636,-0.607262979997527,-0.58527957811466,
-0.581674570659246,-0.579501484128356,-0.577814948772835,-0.575912393791931,
-0.572645820972912,-0.559502906135828,-0.53401869230696,-0.458125570387648,
-0.44329668618723,-0.440093210829008,-0.425657403656021,-0.420609276839719,
-0.417372941001814,-0.414332837504097,-0.410265374369678,-0.402539003607289,
-0.391838479710758,-0.365907843819049,-0.302577484777825,-0.263031189715583,
-0.258542730139443,-0.256383818323119,-0.254702897566626,-0.252769103630285,
-0.250729654327291,-0.243258628350318,-0.207137910367097,-0.175092905464798,
-0.106765832952291,-0.100163181064056,-0.096221743753303,-0.0931906767397102,
-0.0899313955779809,-0.0847788291937528,-0.0787717256972496,-0.0672476008797058,
-0.000962604047633078),.UNSPECIFIED.);
#208=B_SPLINE_CURVE_WITH_KNOTS('',3,(#19640,#19641,#19642,#19643,#19644,
#19645,#19646,#19647,#19648,#19649,#19650,#19651,#19652,#19653,#19654,#19655,
#19656,#19657,#19658,#19659,#19660,#19661,#19662,#19663,#19664,#19665,#19666,
#19667,#19668,#19669,#19670,#19671,#19672,#19673,#19674,#19675,#19676,#19677,
#19678,#19679,#19680,#19681,#19682,#19683,#19684,#19685,#19686,#19687,#19688,
#19689,#19690,#19691,#19692,#19693,#19694,#19695,#19696,#19697,#19698,#19699,
#19700,#19701,#19702,#19703,#19704,#19705,#19706,#19707,#19708,#19709,#19710,
#19711),.UNSPECIFIED.,.F.,.F.,(4,2,2,2,2,2,2,2,2,2,2,2,2,2,2,2,2,2,2,2,
2,2,2,2,2,2,2,2,2,2,2,2,2,2,2,4),(-4.06018374265953,-3.99925922791561,-3.99609684884804,
-3.99404731745362,-3.99210665623675,-3.99042738853674,-3.98828053155481,
-3.98385106327984,-3.92884133292906,-3.89601345881533,-3.85565089620048,
-3.8391579704278,-3.83399405823387,-3.83073297516012,-3.82770394030177,
-3.82377040811831,-3.8171925455825,-3.76819390702086,-3.69226326691795,
-3.67476651114301,-3.67124089224966,-3.66926603801155,-3.667590045921,-3.66548912856324,
-3.6614224700408,-3.63693574670112,-3.55970402444907,-3.53269462731506,
-3.51616674635414,-3.51100591816946,-3.507745424725,-3.50471600053358,-3.50078063269799,
-3.49419677036822,-3.44491056152456,-3.39957621942377),.UNSPECIFIED.);
#209=B_SPLINE_CURVE_WITH_KNOTS('',3,(#19712,#19713,#19714,#19715,#19716,
#19717,#19718,#19719,#19720,#19721,#19722,#19723,#19724,#19725,#19726,#19727,
#19728,#19729,#19730,#19731,#19732,#19733,#19734,#19735,#19736,#19737,#19738,
#19739,#19740,#19741,#19742,#19743,#19744,#19745,#19746,#19747,#19748,#19749,
#19750,#19751,#19752,#19753,#19754,#19755,#19756,#19757,#19758,#19759,#19760,
#19761,#19762,#19763,#19764,#19765,#19766,#19767,#19768,#19769,#19770,#19771,
#19772,#19773,#19774,#19775,#19776,#19777,#19778,#19779,#19780,#19781,#19782,
#19783,#19784,#19785,#19786,#19787,#19788,#19789,#19790,#19791,#19792,#19793,
#19794,#19795,#19796,#19797,#19798,#19799,#19800,#19801,#19802,#19803,#19804,
#19805,#19806,#19807,#19808,#19809,#19810,#19811,#19812,#19813,#19814,#19815,
#19816,#19817,#19818,#19819,#19820,#19821,#19822,#19823,#19824,#19825,#19826,
#19827,#19828,#19829,#19830,#19831,#19832,#19833,#19834,#19835,#19836,#19837,
#19838,#19839,#19840,#19841,#19842,#19843,#19844,#19845,#19846,#19847,#19848,
#19849,#19850,#19851,#19852,#19853,#19854,#19855,#19856,#19857,#19858,#19859,
#19860,#19861,#19862,#19863,#19864,#19865,#19866,#19867,#19868,#19869,#19870,
#19871,#19872,#19873,#19874,#19875,#19876,#19877,#19878,#19879,#19880,#19881,
#19882,#19883,#19884,#19885,#19886,#19887,#19888,#19889,#19890,#19891,#19892,
#19893,#19894,#19895,#19896,#19897,#19898,#19899,#19900,#19901,#19902,#19903,
#19904,#19905,#19906,#19907,#19908,#19909,#19910,#19911,#19912,#19913,#19914,
#19915,#19916,#19917,#19918,#19919,#19920,#19921,#19922,#19923,#19924,#19925,
#19926,#19927,#19928,#19929,#19930,#19931,#19932,#19933,#19934,#19935,#19936,
#19937,#19938,#19939,#19940,#19941),.UNSPECIFIED.,.F.,.F.,(4,2,2,2,2,2,
2,2,2,2,2,2,2,2,2,2,2,2,2,2,2,2,2,2,2,2,2,2,2,2,2,2,2,2,2,2,2,2,2,2,2,2,
2,2,2,2,2,2,2,2,2,2,2,2,2,2,2,2,2,2,2,2,2,2,2,2,2,2,2,2,2,2,2,2,2,2,2,2,
2,2,2,2,2,2,2,2,2,2,2,2,2,2,2,2,2,2,2,2,2,2,2,2,2,2,2,2,2,2,2,2,2,2,2,2,
4),(-2.69158011258058,-2.66747209160962,-2.65413313474391,-2.65087378958829,
-2.64897332994243,-2.6472872208842,-2.64511289033625,-2.64150211020656,
-2.61940237791487,-2.54942804121769,-2.49935068933227,-2.49236649225764,
-2.48870993803168,-2.48571902440178,-2.48225817200146,-2.4763462828739,
-2.45357720940759,-2.43987264941951,-2.37311790935624,-2.34519909737869,
-2.33121087227542,-2.32790133799036,-2.32598975616248,-2.32430590310611,
-2.32215002397714,-2.31860186046939,-2.29775462982861,-2.28945186031621,
-2.21556297611123,-2.18920249973549,-2.17290226605099,-2.16780376808769,
-2.1645572262376,-2.16152303366808,-2.15755606719589,-2.15086279605703,
-2.08931745444593,-2.03040424951123,-2.00929526812745,-2.00573424087948,
-2.00357456515292,-2.00189026147102,-1.99998099971362,-1.99668198218777,
-1.98283236802072,-1.955341990993,-1.88355481478565,-1.87477445821375,-1.85163947967053,
-1.84569554271565,-1.84222729717398,-1.83923685216028,-1.83558948254433,
-1.82864932423041,-1.7803278063186,-1.70611978857024,-1.68614963516126,
-1.68264534752024,-1.68047938643621,-1.67879829421352,-1.67687031887543,
-1.67348670425153,-1.65847573703791,-1.58065340231378,-1.53079657214752,
-1.52420187538904,-1.52026354006071,-1.51723390660095,-1.5139752371275,
-1.50882167510734,-1.49202963367777,-1.46455195147587,-1.39023152181972,
-1.36359030114698,-1.35943943139079,-1.35732051167427,-1.35564348621507,
-1.35368284235094,-1.35014999158018,-1.33280287108105,-1.25679689637712,
-1.20770503148704,-1.20112546841894,-1.19719153114086,-1.19416256873165,
-1.19090195013919,-1.18573961487041,-1.16886809959988,-1.14120854121272,
-1.06851675826252,-1.04060101605438,-1.03640612562779,-1.03427780417039,
-1.03260007306797,-1.03064634261255,-1.02714523230519,-1.01032934196678,
-0.933934032562123,-0.884649574755044,-0.878066153089346,-0.874131089913014,
-0.871101951019273,-0.867841822392571,-0.862681712024551,-0.845830447507494,
-0.818217309940156,-0.74504688778659,-0.717516456535309,-0.713334374753202,
-0.711208781245367,-0.709531257331113,-0.707575533978588,-0.704065295549147,
-0.687098775447949,-0.661728295761303),.UNSPECIFIED.);
#210=B_SPLINE_CURVE_WITH_KNOTS('',3,(#19946,#19947,#19948,#19949,#19950,
#19951,#19952,#19953,#19954,#19955,#19956,#19957,#19958,#19959,#19960,#19961,
#19962,#19963,#19964,#19965,#19966,#19967,#19968,#19969,#19970,#19971,#19972,
#19973,#19974,#19975,#19976,#19977,#19978,#19979,#19980,#19981,#19982,#19983,
#19984,#19985,#19986,#19987,#19988,#19989,#19990,#19991,#19992,#19993,#19994,
#19995,#19996,#19997,#19998,#19999,#20000,#20001,#20002,#20003,#20004,#20005,
#20006,#20007,#20008,#20009,#20010,#20011,#20012,#20013,#20014,#20015,#20016,
#20017,#20018,#20019,#20020,#20021,#20022,#20023,#20024,#20025,#20026,#20027,
#20028,#20029,#20030,#20031,#20032,#20033,#20034,#20035,#20036,#20037,#20038,
#20039,#20040,#20041,#20042,#20043,#20044,#20045,#20046,#20047,#20048,#20049,
#20050,#20051,#20052,#20053,#20054,#20055,#20056,#20057,#20058,#20059,#20060,
#20061,#20062,#20063,#20064,#20065,#20066,#20067,#20068,#20069,#20070,#20071,
#20072,#20073,#20074,#20075,#20076,#20077,#20078,#20079,#20080,#20081,#20082,
#20083,#20084,#20085,#20086,#20087,#20088,#20089,#20090,#20091,#20092,#20093,
#20094,#20095,#20096,#20097,#20098,#20099,#20100,#20101,#20102,#20103,#20104,
#20105,#20106,#20107,#20108,#20109,#20110,#20111,#20112,#20113,#20114,#20115,
#20116,#20117,#20118,#20119,#20120,#20121,#20122,#20123,#20124,#20125,#20126,
#20127,#20128,#20129,#20130,#20131,#20132,#20133,#20134,#20135,#20136,#20137,
#20138,#20139,#20140,#20141,#20142,#20143,#20144,#20145,#20146,#20147,#20148,
#20149,#20150,#20151,#20152,#20153,#20154,#20155,#20156,#20157,#20158,#20159,
#20160,#20161,#20162,#20163,#20164,#20165,#20166,#20167),.UNSPECIFIED.,
 .F.,.F.,(4,2,2,2,2,2,2,2,2,2,2,2,2,2,2,2,2,2,2,2,2,2,2,2,2,2,2,2,2,2,2,
2,2,2,2,2,2,2,2,2,2,2,2,2,2,2,2,2,2,2,2,2,2,2,2,2,2,2,2,2,2,2,2,2,2,2,2,
2,2,2,2,2,2,2,2,2,2,2,2,2,2,2,2,2,2,2,2,2,2,2,2,2,2,2,2,2,2,2,2,2,2,2,2,
2,2,2,2,2,2,2,4),(-3.39989171054498,-3.37782329442216,-3.35020252442917,
-3.3333459486215,-3.32818481540107,-3.32492414522188,-3.32189456784869,
-3.31795901667933,-3.31137488213135,-3.26208951110153,-3.18558680582082,
-3.16883886382238,-3.16534143070497,-3.16338828577502,-3.16171013045796,
-3.15958005406527,-3.15537799249585,-3.12725035584433,-3.05488510752912,
-3.02722163448309,-3.01034613369993,-3.00518271799666,-3.0019214145189,
-2.99889180664146,-2.99495700769636,-2.98837587584108,-2.9392578410892,
-2.86310012201381,-2.84587672669976,-2.84235053198704,-2.8403910470402,
-2.83871343885712,-2.83659174209633,-2.83242930386336,-2.80548067831588,
-2.73162543526178,-2.70411439915233,-2.68730520105543,-2.68214889754865,
-2.67888904360795,-2.67585868075213,-2.67191991552082,-2.66532556577614,
-2.6155567639682,-2.53787653517198,-2.52261378549417,-2.51921207582781,
-2.51727975436108,-2.51559869340779,-2.51343775810565,-2.50893868465012,
-2.46818773048134,-2.41140556771671,-2.38205791036345,-2.36445764283756,
-2.35921571566852,-2.35593675978992,-2.35291249419321,-2.34901513433722,
-2.34256294487568,-2.29901685157658,-2.23632701948247,-2.21204345611577,
-2.19928316951178,-2.196069996818,-2.19417932781648,-2.19249011501072,-2.19029638201601,
-2.18662086812254,-2.16301729331119,-2.09488224879521,-2.04459631984225,
-2.03760506999759,-2.03394617682264,-2.03124240612375,-2.02788138381756,
-2.02226888935828,-2.00077383956864,-1.92029935513111,-1.87838752279567,
-1.87387849850888,-1.87171550128931,-1.87003410970749,-1.86810282970024,
-1.86470635798594,-1.84952270222907,-1.77181033003987,-1.72203224496142,
-1.71543728631934,-1.71149806854268,-1.70846732314914,-1.70520702538135,
-1.70004995332058,-1.68323782740404,-1.65571748444761,-1.58174623965975,
-1.55483552393685,-1.55067381081448,-1.54855207881564,-1.54687423417808,
-1.54491422198477,-1.54138646819637,-1.52414252396053,-1.44802798268863,
-1.39892782666286,-1.39234630777616,-1.38841099787858,-1.38538085059294,
-1.38211882409639,-1.37695396240566,-1.37009647383181),.UNSPECIFIED.);
#211=B_SPLINE_CURVE_WITH_KNOTS('',3,(#20169,#20170,#20171,#20172,#20173,
#20174,#20175,#20176,#20177,#20178,#20179,#20180,#20181,#20182,#20183,#20184,
#20185,#20186,#20187,#20188,#20189,#20190,#20191,#20192,#20193,#20194,#20195,
#20196,#20197,#20198,#20199,#20200,#20201,#20202,#20203,#20204,#20205,#20206,
#20207,#20208,#20209,#20210,#20211,#20212,#20213,#20214,#20215,#20216,#20217,
#20218,#20219,#20220,#20221,#20222,#20223,#20224,#20225,#20226,#20227,#20228,
#20229,#20230,#20231,#20232,#20233,#20234,#20235,#20236,#20237,#20238,#20239,
#20240,#20241,#20242,#20243,#20244),.UNSPECIFIED.,.F.,.F.,(4,2,2,2,2,2,
2,2,2,2,2,2,2,2,2,2,2,2,2,2,2,2,2,2,2,2,2,2,2,2,2,2,2,2,2,2,2,4),(-0.661728295761303,
-0.610815008485105,-0.561583971244939,-0.555001604028606,-0.5510668437837,
-0.548037746741959,-0.544777474721572,-0.53961673580376,-0.52390332568263,
-0.498367783465112,-0.416315153428545,-0.394074951591542,-0.390453257662493,
-0.388275633138542,-0.386588987397853,-0.384690169563046,-0.381503994986904,
-0.368922016892563,-0.345058087830577,-0.296520050215664,-0.238719470933928,
-0.232031714938196,-0.228066128117626,-0.225031917703408,-0.221784314022387,
-0.216681961847125,-0.200746292228467,-0.156926182370389,-0.122396956235019,
-0.0975934140122743,-0.0713673360125964,-0.0672317821819891,-0.0651161327737426,
-0.0634393244099186,-0.0614761928712398,-0.0593948705733298,-0.0561558460900975,
-0.000961981174542983),.UNSPECIFIED.);
#212=B_SPLINE_CURVE_WITH_KNOTS('',3,(#20245,#20246,#20247,#20248,#20249,
#20250,#20251,#20252,#20253,#20254,#20255,#20256,#20257,#20258,#20259,#20260,
#20261,#20262,#20263,#20264,#20265,#20266,#20267,#20268,#20269,#20270,#20271,
#20272,#20273,#20274,#20275,#20276,#20277,#20278,#20279,#20280,#20281,#20282,
#20283,#20284,#20285,#20286,#20287,#20288,#20289,#20290,#20291,#20292,#20293,
#20294,#20295,#20296,#20297,#20298,#20299,#20300,#20301,#20302,#20303,#20304,
#20305,#20306,#20307,#20308,#20309,#20310,#20311,#20312,#20313,#20314,#20315,
#20316,#20317,#20318,#20319,#20320,#20321,#20322,#20323,#20324,#20325,#20326,
#20327,#20328,#20329,#20330,#20331,#20332,#20333,#20334,#20335,#20336,#20337,
#20338,#20339,#20340,#20341,#20342,#20343,#20344,#20345,#20346,#20347,#20348,
#20349,#20350,#20351,#20352,#20353,#20354,#20355,#20356,#20357,#20358,#20359,
#20360,#20361,#20362,#20363,#20364,#20365,#20366,#20367,#20368,#20369,#20370,
#20371,#20372,#20373,#20374,#20375,#20376,#20377,#20378,#20379,#20380,#20381,
#20382,#20383,#20384,#20385,#20386,#20387,#20388,#20389,#20390),
 .UNSPECIFIED.,.F.,.F.,(4,2,2,2,2,2,2,2,2,2,2,2,2,2,2,2,2,2,2,2,2,2,2,2,
2,2,2,2,2,2,2,2,2,2,2,2,2,2,2,2,2,2,2,2,2,2,2,2,2,2,2,2,2,2,2,2,2,2,2,2,
2,2,2,2,2,2,2,2,2,2,2,2,4),(-4.0611470534665,-3.97946902488515,-3.96965145523291,
-3.9654577117724,-3.96239736646629,-3.95958437074479,-3.95505180491361,
-3.94396228855254,-3.87768596605957,-3.84543925377997,-3.82003258159493,
-3.80692915525169,-3.80376407204218,-3.80183408645674,-3.80015362614578,
-3.79799162283085,-3.79348395991318,-3.75143218553444,-3.67070044832043,
-3.64966864652559,-3.64407023781302,-3.64071349823518,-3.63771050538882,
-3.63390328725673,-3.62788754992851,-3.5955536658021,-3.52072655021728,
-3.49652584640034,-3.48379637841951,-3.48058685021556,-3.47869759037803,
-3.47700914039031,-3.47481578566657,-3.47113962057223,-3.44748897124155,
-3.44120042806564,-3.37026904772027,-3.34267010541243,-3.3258239005242,
-3.3206647980075,-3.31740516913945,-3.31437639905568,-3.31044167737777,
-3.30385847378207,-3.25456398580373,-3.17814277092822,-3.16131673389292,
-3.15781519833253,-3.15586149103941,-3.15418393456454,-3.1520560460983,
-3.14786264167539,-3.11997844918352,-3.04730888222496,-3.01966642328088,
-3.00280093887991,-2.9976395186792,-2.99437925161932,-2.99135045856442,
-2.98741651617018,-2.98083639886609,-2.93171316182019,-2.85564035127376,
-2.8383319726208,-2.83480144026594,-2.83284134603925,-2.8311643319978,-2.82904485085657,
-2.82489115787273,-2.79816557270861,-2.72401104340086,-2.69653098908436,
-2.69214420168212),.UNSPECIFIED.);
#213=B_SPLINE_CURVE_WITH_KNOTS('',3,(#20396,#20397,#20398,#20399,#20400,
#20401,#20402,#20403,#20404,#20405,#20406,#20407,#20408,#20409,#20410,#20411,
#20412,#20413,#20414,#20415,#20416,#20417,#20418,#20419,#20420,#20421,#20422,
#20423,#20424,#20425,#20426,#20427,#20428,#20429,#20430,#20431,#20432,#20433,
#20434,#20435,#20436,#20437,#20438,#20439,#20440,#20441,#20442,#20443,#20444,
#20445,#20446,#20447,#20448,#20449,#20450,#20451,#20452,#20453,#20454,#20455,
#20456,#20457,#20458,#20459,#20460,#20461,#20462,#20463,#20464,#20465,#20466,
#20467,#20468,#20469,#20470,#20471,#20472,#20473,#20474,#20475,#20476,#20477,
#20478,#20479,#20480,#20481,#20482,#20483,#20484,#20485,#20486,#20487,#20488,
#20489,#20490,#20491,#20492,#20493,#20494,#20495,#20496,#20497,#20498,#20499,
#20500,#20501,#20502,#20503,#20504,#20505,#20506,#20507,#20508,#20509,#20510,
#20511,#20512,#20513,#20514,#20515,#20516,#20517,#20518,#20519,#20520,#20521,
#20522,#20523,#20524,#20525,#20526,#20527,#20528,#20529,#20530,#20531,#20532,
#20533,#20534,#20535,#20536,#20537,#20538,#20539,#20540,#20541,#20542,#20543,
#20544,#20545,#20546,#20547,#20548,#20549,#20550,#20551,#20552,#20553),
 .UNSPECIFIED.,.F.,.F.,(4,2,2,2,2,2,2,2,2,2,2,2,2,2,2,2,2,2,2,2,2,2,2,2,
2,2,2,2,2,2,2,2,2,2,2,2,2,2,2,2,2,2,2,2,2,2,2,2,2,2,2,2,2,2,2,2,2,2,2,2,
2,2,2,2,2,2,2,2,2,2,2,2,2,2,2,2,2,2,4),(-1.36944548578019,-1.36685508335615,
-1.36473347674478,-1.36305571269168,-1.3610957732222,-1.35756809666554,
-1.34032346801666,-1.26421357917519,-1.21511627636007,-1.20853507721217,
-1.20459995510823,-1.20156995044009,-1.19830807552231,-1.19314344966717,
-1.17626142839677,-1.1485805305303,-1.07617139302344,-1.04802314847339,
-1.04381972674251,-1.04168915448406,-1.04001070961269,-1.03805733229479,
-1.03455976189052,-1.01781565328565,-0.941337050177608,-0.892059912697068,
-0.885475116329598,-0.881538947322674,-0.878508781914032,-0.875247369609173,
-0.870084831183972,-0.853221774374299,-0.82558434751641,-0.752702894258793,
-0.72493888615982,-0.720747988955342,-0.718620083668117,-0.716941846042953,
-0.714986534434993,-0.711480100500522,-0.69459050339053,-0.618220259872811,
-0.568994407109077,-0.562410631263075,-0.558474758183008,-0.5554446369634,
-0.552183091361504,-0.54701995644478,-0.530475386363742,-0.503428506327888,
-0.427122710844942,-0.422931781795328,-0.401430160587616,-0.397849174516712,
-0.395683167212009,-0.393997521194305,-0.392090769841944,-0.388871213100074,
-0.37589600991404,-0.350913011538589,-0.298584493958666,-0.246080525137938,
-0.239435449672719,-0.235481605811399,-0.232448502934618,-0.229194382385887,
-0.224065533934083,-0.207902223077646,-0.168168060512799,-0.135652290613352,
-0.0791226485939434,-0.0747236304802112,-0.072582301660274,-0.0709029524686051,
-0.0689571617927164,-0.0669006777669633,-0.0637222316588258,-0.0577186424769282,
-0.000962232141326606),.UNSPECIFIED.);
#214=B_SPLINE_CURVE_WITH_KNOTS('',3,(#20554,#20555,#20556,#20557,#20558,
#20559,#20560,#20561,#20562,#20563,#20564,#20565,#20566,#20567,#20568,#20569,
#20570,#20571,#20572,#20573,#20574,#20575,#20576,#20577,#20578,#20579,#20580,
#20581,#20582,#20583,#20584,#20585,#20586,#20587,#20588,#20589,#20590,#20591,
#20592,#20593,#20594,#20595,#20596,#20597,#20598,#20599,#20600,#20601,#20602,
#20603,#20604,#20605,#20606,#20607,#20608,#20609,#20610,#20611,#20612,#20613,
#20614,#20615,#20616,#20617,#20618,#20619,#20620,#20621,#20622,#20623,#20624,
#20625,#20626,#20627,#20628,#20629,#20630,#20631),.UNSPECIFIED.,.F.,.F.,
(4,2,2,2,2,2,2,2,2,2,2,2,2,2,2,2,2,2,2,2,2,2,2,2,2,2,2,2,2,2,2,2,2,2,2,
2,2,2,4),(-4.06105430689023,-3.99656812749712,-3.98512601458802,-3.97914984493825,
-3.97401873272135,-3.97076482823473,-3.96773307376906,-3.96378262465774,
-3.95714683680808,-3.89007832436105,-3.85768781871186,-3.82063014135095,
-3.81320996672058,-3.81117504882215,-3.80924463791343,-3.8075638189508,
-3.80540133333362,-3.80089256753859,-3.7587518252921,-3.6926845608974,-3.65864448390997,
-3.65243664936152,-3.64883446441842,-3.64587376855026,-3.64237746811502,
-3.63631231893072,-3.61173737201564,-3.60453958170595,-3.52710871464621,
-3.50369007507047,-3.4912772988814,-3.48809997677297,-3.48620305720783,
-3.48451584949507,-3.48233457089039,-3.47870065865522,-3.45607474347752,
-3.44128182274636,-3.39989171054498),.UNSPECIFIED.);
#215=B_SPLINE_CURVE_WITH_KNOTS('',3,(#20632,#20633,#20634,#20635,#20636,
#20637,#20638,#20639,#20640,#20641,#20642,#20643,#20644,#20645,#20646,#20647,
#20648,#20649,#20650,#20651,#20652,#20653,#20654,#20655,#20656,#20657,#20658,
#20659,#20660,#20661,#20662,#20663,#20664,#20665,#20666,#20667,#20668,#20669,
#20670,#20671,#20672,#20673,#20674,#20675,#20676,#20677,#20678,#20679,#20680,
#20681,#20682,#20683,#20684,#20685,#20686,#20687,#20688,#20689,#20690,#20691,
#20692,#20693,#20694,#20695,#20696,#20697,#20698,#20699,#20700,#20701,#20702,
#20703,#20704,#20705,#20706,#20707,#20708,#20709,#20710,#20711,#20712,#20713,
#20714,#20715,#20716,#20717,#20718,#20719,#20720,#20721,#20722,#20723,#20724,
#20725,#20726,#20727,#20728,#20729,#20730,#20731,#20732,#20733,#20734,#20735,
#20736,#20737,#20738,#20739,#20740,#20741,#20742,#20743,#20744,#20745,#20746,
#20747,#20748,#20749,#20750,#20751,#20752,#20753,#20754,#20755,#20756,#20757,
#20758,#20759,#20760,#20761,#20762,#20763,#20764,#20765,#20766,#20767,#20768,
#20769,#20770,#20771,#20772,#20773,#20774,#20775,#20776,#20777,#20778,#20779,
#20780,#20781,#20782,#20783,#20784,#20785,#20786,#20787,#20788,#20789,#20790,
#20791,#20792,#20793,#20794,#20795,#20796,#20797,#20798,#20799,#20800,#20801,
#20802,#20803,#20804,#20805,#20806,#20807,#20808,#20809,#20810,#20811,#20812,
#20813,#20814,#20815,#20816,#20817,#20818,#20819,#20820,#20821,#20822,#20823,
#20824,#20825,#20826,#20827,#20828,#20829,#20830,#20831,#20832,#20833,#20834,
#20835,#20836,#20837,#20838,#20839,#20840,#20841,#20842,#20843,#20844,#20845,
#20846,#20847,#20848,#20849,#20850,#20851,#20852,#20853,#20854,#20855,#20856,
#20857,#20858,#20859),.UNSPECIFIED.,.F.,.F.,(4,2,2,2,2,2,2,2,2,2,2,2,2,
2,2,2,2,2,2,2,2,2,2,2,2,2,2,2,2,2,2,2,2,2,2,2,2,2,2,2,2,2,2,2,2,2,2,2,2,
2,2,2,2,2,2,2,2,2,2,2,2,2,2,2,2,2,2,2,2,2,2,2,2,2,2,2,2,2,2,2,2,2,2,2,2,
2,2,2,2,2,2,2,2,2,2,2,2,2,2,2,2,2,2,2,2,2,2,2,2,2,2,2,2,4),(-2.69214420168212,
-2.67973619593171,-2.67458237891731,-2.67132367241898,-2.66829408939555,
-2.66435593831008,-2.65776176172773,-2.60794407083172,-2.53025102046682,
-2.51503192846507,-2.51163384492198,-2.50970265456142,-2.50802199066382,
-2.50586083304291,-2.50135877979141,-2.46015665689658,-2.38130797234107,
-2.3578388945831,-2.35206644839734,-2.34867078894003,-2.34567322123776,
-2.34192642209654,-2.33610951900337,-2.30713797266868,-2.23214079973542,
-2.20535490684935,-2.19173899336989,-2.18845774434828,-2.18655233387126,
-2.1848671016102,-2.18270068842031,-2.1791171198563,-2.15754520488519,-2.14989323317005,
-2.0761138376243,-2.03997334956528,-2.03102968730414,-2.02703378172422,
-2.0239946422948,-2.02075938775664,-2.01571307773361,-1.99986899625076,
-1.97451931270814,-1.9242454105774,-1.89328683005485,-1.87007736772437,
-1.86641892233116,-1.8642305854261,-1.86254260764619,-1.86065007199541,
-1.85742661802092,-1.84453263428126,-1.81986795164492,-1.75735563355225,
-1.71421223308437,-1.7077728497534,-1.70387992384522,-1.70085716260779,
-1.69757790696673,-1.69233131702317,-1.67467623005482,-1.64519178392337,
-1.58758527717084,-1.54777307596717,-1.54328317919534,-1.54112445325438,
-1.53944409350665,-1.53751144687149,-1.53410651735475,-1.51878504810215,
-1.44122176624357,-1.39145478805498,-1.38486193147988,-1.38092416016115,
-1.37789464827414,-1.37463580237969,-1.36948130772471,-1.35268040125277,
-1.32518230094414,-1.25101802340827,-1.22426124465494,-1.22010623719456,
-1.21798644952337,-1.2163093833264,-1.21434943739582,-1.21081971592342,
-1.19352525392567,-1.11748255282312,-1.06837193429881,-1.06179207486316,
-1.05785808011058,-1.0548291434526,-1.05156862154496,-1.04640658638491,
-1.0295373699114,-1.00188292407963,-0.929141443246179,-0.901267290284923,
-0.897073809129345,-0.894945805419274,-0.893268120518162,-0.891314209286817,
-0.887812192822024,-0.870980835262293,-0.794598309860886,-0.745320093665881,
-0.738736875909263,-0.734801900745541,-0.731772809806856,-0.728512713298485,
-0.723352612227376,-0.706501006252207,-0.678886930515555,-0.662304444938604),
 .UNSPECIFIED.);
#216=B_SPLINE_CURVE_WITH_KNOTS('',3,(#20864,#20865,#20866,#20867,#20868,
#20869,#20870,#20871,#20872,#20873,#20874,#20875,#20876,#20877,#20878,#20879,
#20880,#20881,#20882,#20883,#20884,#20885,#20886,#20887,#20888,#20889,#20890,
#20891,#20892,#20893,#20894,#20895,#20896,#20897,#20898,#20899,#20900,#20901,
#20902,#20903,#20904,#20905,#20906,#20907,#20908,#20909,#20910,#20911,#20912,
#20913,#20914,#20915,#20916,#20917,#20918,#20919,#20920,#20921,#20922,#20923,
#20924,#20925,#20926,#20927,#20928,#20929,#20930,#20931,#20932,#20933,#20934,
#20935,#20936,#20937,#20938,#20939,#20940,#20941,#20942,#20943,#20944,#20945,
#20946,#20947,#20948,#20949,#20950,#20951,#20952,#20953,#20954,#20955,#20956,
#20957,#20958,#20959,#20960,#20961,#20962,#20963,#20964,#20965,#20966,#20967,
#20968,#20969,#20970,#20971,#20972,#20973,#20974,#20975,#20976,#20977,#20978,
#20979,#20980,#20981,#20982,#20983,#20984,#20985,#20986,#20987,#20988,#20989,
#20990,#20991,#20992,#20993,#20994,#20995,#20996,#20997,#20998,#20999,#21000,
#21001,#21002,#21003,#21004,#21005,#21006,#21007,#21008,#21009,#21010,#21011,
#21012,#21013,#21014,#21015,#21016,#21017,#21018,#21019,#21020,#21021,#21022,
#21023,#21024,#21025,#21026,#21027,#21028,#21029,#21030,#21031,#21032,#21033,
#21034,#21035,#21036,#21037,#21038,#21039,#21040,#21041,#21042,#21043,#21044,
#21045,#21046,#21047,#21048,#21049,#21050,#21051,#21052,#21053,#21054,#21055,
#21056,#21057,#21058,#21059,#21060,#21061,#21062,#21063,#21064,#21065,#21066,
#21067,#21068,#21069,#21070,#21071,#21072,#21073),.UNSPECIFIED.,.F.,.F.,
(4,2,2,2,2,2,2,2,2,2,2,2,2,2,2,2,2,2,2,2,2,2,2,2,2,2,2,2,2,2,2,2,2,2,2,
2,2,2,2,2,2,2,2,2,2,2,2,2,2,2,2,2,2,2,2,2,2,2,2,2,2,2,2,2,2,2,2,2,2,2,2,
2,2,2,2,2,2,2,2,2,2,2,2,2,2,2,2,2,2,2,2,2,2,2,2,2,2,2,2,2,2,2,2,2,4),(-3.39921582738553,
-3.32481449484858,-3.30797204107994,-3.30446916420648,-3.30251498590862,
-3.30083718732464,-3.29870916466968,-3.29451599472769,-3.26664925628896,
-3.19397761073236,-3.1663465501906,-3.1494858161877,-3.14432445482504,-3.14106388128885,
-3.13803455985473,-3.13409957702268,-3.12751691295561,-3.0782858165178,
-3.00189575808859,-2.98500486145439,-2.98149889632078,-2.97954397315815,
-2.9778661408787,-2.97573885432162,-2.97154948562348,-2.94380391627405,
-2.87097584465458,-2.84335764833016,-2.8265022422895,-2.82134126972633,
-2.81808065552759,-2.81505109875404,-2.81111552974511,-2.80453126707731,
-2.75523674437102,-2.67871415564775,-2.66199391026287,-2.65849819775023,
-2.65654543973425,-2.65486726016679,-2.65273669366933,-2.64853227368191,
-2.62032987930118,-2.54805679372162,-2.52038554596727,-2.50350669964811,
-2.49834294745525,-2.49508158963164,-2.49205204038094,-2.48811747241642,
-2.48153706788515,-2.43245266483799,-2.3563606378107,-2.33904762085849,
-2.33551616421612,-2.33355554550493,-2.33187806631487,-2.32975794052694,
-2.32560279115239,-2.29885712373006,-2.22473481912716,-2.19725827844759,
-2.18046421850513,-2.17530961896144,-2.1720501625438,-2.16901969944224,
-2.1650801360264,-2.15848297600417,-2.10856767226204,-2.03044723688045,
-2.01597481920901,-2.01250315737895,-2.01053455404231,-2.00885767955125,
-2.00674778779779,-2.00250568674842,-1.96247756126698,-1.89318044936584,
-1.86030054312869,-1.85425101246816,-1.85043251301819,-1.84742698875623,
-1.8440740303073,-1.83849748626483,-1.81741498603992,-1.73660164759996,
-1.6945550508575,-1.69004526258722,-1.68788217634461,-1.68620084491157,
-1.68426977978387,-1.6808740325054,-1.66569931345358,-1.5879837647268,-1.53820564997236,
-1.53161095427254,-1.52767190776974,-1.52464130245084,-1.52138116353253,
-1.5162243601143,-1.49941326497488,-1.47189476671748,-1.39792253642723,
-1.37101648029654,-1.36944548578019),.UNSPECIFIED.);
#217=B_SPLINE_CURVE_WITH_KNOTS('',3,(#21075,#21076,#21077,#21078,#21079,
#21080,#21081,#21082,#21083,#21084,#21085,#21086,#21087,#21088,#21089,#21090,
#21091,#21092,#21093,#21094,#21095,#21096,#21097,#21098,#21099,#21100,#21101,
#21102,#21103,#21104,#21105,#21106,#21107,#21108,#21109,#21110,#21111,#21112,
#21113,#21114,#21115,#21116,#21117,#21118,#21119,#21120,#21121,#21122,#21123,
#21124,#21125,#21126,#21127,#21128,#21129,#21130,#21131,#21132,#21133,#21134,
#21135,#21136,#21137,#21138,#21139,#21140,#21141,#21142,#21143,#21144,#21145,
#21146,#21147,#21148,#21149,#21150),.UNSPECIFIED.,.F.,.F.,(4,2,2,2,2,2,
2,2,2,2,2,2,2,2,2,2,2,2,2,2,2,2,2,2,2,2,2,2,2,2,2,2,2,2,2,2,2,4),(-0.662304444938604,
-0.63510021468167,-0.578477873728376,-0.574082661913293,-0.571942617297102,
-0.570264008758051,-0.568318804463193,-0.565099959077751,-0.551433987379965,
-0.524294500285268,-0.446054304749311,-0.420452860529858,-0.414309608485123,
-0.4107957026584,-0.408106194423922,-0.404633303173324,-0.398985520822482,
-0.374703149293996,-0.291094634145217,-0.255474777269919,-0.251032176228322,
-0.248882730945909,-0.247203238869721,-0.245264380807548,-0.243217478816965,
-0.235647647195005,-0.196108431693412,-0.162561834215048,-0.142574300536187,
-0.0990487023498325,-0.0925986579080474,-0.0887025324900113,-0.0856792144300964,
-0.0824012833215487,-0.0790422999552084,-0.0741458825853799,-0.0566546994879453,
-0.00096234511667658),.UNSPECIFIED.);
#218=B_SPLINE_CURVE_WITH_KNOTS('',3,(#21151,#21152,#21153,#21154,#21155,
#21156,#21157,#21158,#21159,#21160,#21161,#21162,#21163,#21164,#21165,#21166,
#21167,#21168,#21169,#21170,#21171,#21172,#21173,#21174,#21175,#21176,#21177,
#21178,#21179,#21180,#21181,#21182,#21183,#21184,#21185,#21186,#21187,#21188,
#21189,#21190,#21191,#21192,#21193,#21194,#21195,#21196,#21197,#21198,#21199,
#21200,#21201,#21202,#21203,#21204,#21205,#21206,#21207,#21208,#21209,#21210,
#21211,#21212,#21213,#21214,#21215,#21216,#21217,#21218,#21219,#21220,#21221,
#21222,#21223,#21224,#21225,#21226,#21227,#21228,#21229,#21230,#21231,#21232,
#21233,#21234,#21235,#21236,#21237,#21238,#21239,#21240,#21241,#21242,#21243,
#21244,#21245,#21246,#21247,#21248,#21249,#21250,#21251,#21252,#21253,#21254,
#21255,#21256,#21257,#21258,#21259,#21260,#21261,#21262,#21263,#21264,#21265,
#21266,#21267,#21268,#21269,#21270,#21271,#21272,#21273,#21274,#21275,#21276,
#21277,#21278,#21279,#21280,#21281,#21282,#21283,#21284,#21285,#21286,#21287,
#21288,#21289,#21290,#21291,#21292,#21293,#21294,#21295,#21296,#21297,#21298,
#21299,#21300,#21301,#21302,#21303,#21304),.UNSPECIFIED.,.F.,.F.,(4,2,2,
2,2,2,2,2,2,2,2,2,2,2,2,2,2,2,2,2,2,2,2,2,2,2,2,2,2,2,2,2,2,2,2,2,2,2,2,
2,2,2,2,2,2,2,2,2,2,2,2,2,2,2,2,2,2,2,2,2,2,2,2,2,2,2,2,2,2,2,2,2,2,2,2,
2,4),(-4.06007593280828,-3.99508670064763,-3.99042194715341,-3.98776077535643,
-3.98538711376223,-3.98367662841544,-3.98207435650221,-3.97935938264497,
-3.9720265854057,-3.91556034035554,-3.8827315202545,-3.83998657274542,-3.82975634765789,
-3.82642509712098,-3.82316636481412,-3.82013759582651,-3.81620169374451,
-3.80961390953123,-3.76006666597922,-3.70094237722576,-3.67857286962766,
-3.66653741920305,-3.66339613799091,-3.66150782191981,-3.65981929132283,
-3.6576246250592,-3.65394369652287,-3.63017141919948,-3.62397508904615,
-3.54783538865922,-3.52360536853894,-3.50833632884403,-3.50347413144518,
-3.50021467130849,-3.49718620563316,-3.49325208901566,-3.48667035960177,
-3.43742539958884,-3.36110525559634,-3.34415337328646,-3.34064443200445,
-3.3386892137869,-3.33701198197228,-3.33488658932606,-3.33070438709033,
-3.30314862482051,-3.2300802790426,-3.20247969303012,-3.18563290730004,
-3.18047383514902,-3.17721427347346,-3.17418559895685,-3.17025104847686,
-3.16366823498459,-3.11438531399867,-3.03798766474525,-3.02113336432045,
-3.01763018167405,-3.0156761491635,-3.01399868145626,-3.01187137883828,
-3.00768055820981,-2.97987210006679,-2.90711205193522,-2.87947911680082,
-2.86261792626382,-2.85745707334647,-2.85419699258987,-2.85116825392184,
-2.84723421370144,-2.84065356166726,-2.79149557310213,-2.71535395356781,
-2.69814409994251,-2.69461945246054,-2.69266067310163,-2.69180502268216),
 .UNSPECIFIED.);
#219=B_SPLINE_CURVE_WITH_KNOTS('',3,(#21310,#21311,#21312,#21313,#21314,
#21315,#21316,#21317,#21318,#21319,#21320,#21321,#21322,#21323,#21324,#21325,
#21326,#21327,#21328,#21329,#21330,#21331,#21332,#21333,#21334,#21335,#21336,
#21337,#21338,#21339,#21340,#21341,#21342,#21343,#21344,#21345,#21346,#21347,
#21348,#21349,#21350,#21351,#21352,#21353,#21354,#21355,#21356,#21357,#21358,
#21359,#21360,#21361,#21362,#21363,#21364,#21365,#21366,#21367,#21368,#21369,
#21370,#21371,#21372,#21373,#21374,#21375,#21376,#21377,#21378,#21379,#21380,
#21381,#21382,#21383,#21384,#21385,#21386,#21387,#21388,#21389,#21390,#21391,
#21392,#21393,#21394,#21395,#21396,#21397,#21398,#21399,#21400,#21401,#21402,
#21403,#21404,#21405,#21406,#21407,#21408,#21409,#21410,#21411,#21412,#21413,
#21414,#21415,#21416,#21417,#21418,#21419,#21420,#21421,#21422,#21423,#21424,
#21425,#21426,#21427,#21428,#21429,#21430,#21431,#21432,#21433,#21434,#21435,
#21436,#21437,#21438,#21439,#21440,#21441,#21442,#21443,#21444,#21445,#21446,
#21447,#21448,#21449,#21450,#21451,#21452,#21453,#21454,#21455,#21456,#21457,
#21458,#21459,#21460,#21461,#21462,#21463,#21464,#21465,#21466,#21467,#21468,
#21469,#21470,#21471,#21472,#21473,#21474,#21475,#21476,#21477,#21478,#21479,
#21480,#21481,#21482,#21483,#21484,#21485,#21486,#21487,#21488,#21489,#21490,
#21491,#21492,#21493,#21494,#21495,#21496,#21497,#21498,#21499,#21500,#21501,
#21502,#21503,#21504,#21505,#21506,#21507,#21508,#21509,#21510,#21511,#21512,
#21513),.UNSPECIFIED.,.F.,.F.,(4,2,2,2,2,2,2,2,2,2,2,2,2,2,2,2,2,2,2,2,
2,2,2,2,2,2,2,2,2,2,2,2,2,2,2,2,2,2,2,2,2,2,2,2,2,2,2,2,2,2,2,2,2,2,2,2,
2,2,2,2,2,2,2,2,2,2,2,2,2,2,2,2,2,2,2,2,2,2,2,2,2,2,2,2,2,2,2,2,2,2,2,2,
2,2,2,2,2,2,2,2,2,4),(-1.37015241264804,-1.35570167221927,-1.34911020280277,
-1.34517184391813,-1.34214104368373,-1.33887998266,-1.33372020388906,-1.31688586729512,
-1.28931555875076,-1.21574475579553,-1.18851814157379,-1.18434507533776,
-1.18222082213135,-1.18054267426951,-1.17858425479071,-1.17506423658523,
-1.15795382549888,-1.08173522975928,-1.032581929931,-1.02599891416521,-1.02206301295249,
-1.01903258795034,-1.01577043744264,-1.01060575243728,-0.99372691981051,
-0.966054700086884,-0.893500726404919,-0.865460163196997,-0.861259800617952,
-0.859129726214254,-0.857451132930531,-0.855496962431575,-0.851996434210784,
-0.835208971356298,-0.758751733720428,-0.709504648386363,-0.702907312120488,
-0.698967235220946,-0.695936156354818,-0.69267582199739,-0.687519377516122,
-0.670715408820021,-0.643214620991501,-0.569065739521207,-0.542282788116421,
-0.538125382693541,-0.536004469917919,-0.534326558392875,-0.53236564356778,
-0.528834197182952,-0.511531168312921,-0.435452029791617,-0.386395765008376,
-0.379799368310777,-0.375859550998606,-0.37282849579225,-0.372756962554819,
-0.372695205486438,-0.37264188380147,-0.372595840334254,-0.372556076881171,
-0.372521732658634,-0.372492065480112,-0.372456341309402,-0.372421787924555,
-0.372388362413708,-0.372356024898909,-0.372324737004946,-0.37229446180026,
-0.372265163735355,-0.372236808603881,-0.372209363485444,-0.372182796719788,
-0.37215707782998,-0.37213217978693,-0.372108076696769,-0.372084737184498,
-0.372062135128295,-0.372040245393113,-0.368586703197645,-0.362467433708289,
-0.354934034015112,-0.339130344809145,-0.292302260847055,-0.223613311847423,
-0.216443223500477,-0.213751925897575,-0.212153567805215,-0.210438561239818,
-0.208044291725156,-0.202254565889217,-0.175127893333119,-0.104932832839247,
-0.0858200753755365,-0.0613244148699548,-0.0552638180302682,-0.0517678051873036,
-0.0488059839202267,-0.0459509476860365,-0.0424235859125755,-0.0371219143882906,
-0.000961528038556079),.UNSPECIFIED.);
#220=B_SPLINE_CURVE_WITH_KNOTS('',3,(#21514,#21515,#21516,#21517,#21518,
#21519,#21520,#21521,#21522,#21523,#21524,#21525,#21526,#21527,#21528,#21529,
#21530,#21531,#21532,#21533,#21534,#21535,#21536,#21537,#21538,#21539,#21540,
#21541,#21542,#21543,#21544,#21545,#21546,#21547,#21548,#21549,#21550,#21551,
#21552,#21553,#21554,#21555,#21556,#21557,#21558,#21559,#21560,#21561,#21562,
#21563,#21564,#21565,#21566,#21567,#21568,#21569,#21570,#21571,#21572,#21573,
#21574,#21575,#21576,#21577,#21578,#21579,#21580,#21581,#21582,#21583,#21584,
#21585,#21586,#21587),.UNSPECIFIED.,.F.,.F.,(4,2,2,2,2,2,2,2,2,2,2,2,2,
2,2,2,2,2,2,2,2,2,2,2,2,2,2,2,2,2,2,2,2,2,2,2,4),(-4.0598307301908,-4.03672959654851,
-3.95835106002174,-3.95188085665108,-3.94937832677973,-3.94764332351265,
-3.94607023270309,-3.9435082940285,-3.93713708709772,-3.86158186525947,
-3.82533930506727,-3.8068002885785,-3.79430707685316,-3.78976557777166,
-3.78696446288447,-3.78393493284727,-3.77999677157192,-3.77340237704567,
-3.72417508750641,-3.6477441627003,-3.63092268536297,-3.62742123393807,
-3.6254674383618,-3.62378971257453,-3.62166145320441,-3.61746682253874,
-3.58954942267503,-3.5169466966478,-3.48931127062046,-3.47244892089151,
-3.46728758094606,-3.46402713981489,-3.46099802341706,-3.45706342335037,
-3.45048165609643,-3.40123518122251,-3.39921582738553),.UNSPECIFIED.);
#221=B_SPLINE_CURVE_WITH_KNOTS('',3,(#21588,#21589,#21590,#21591,#21592,
#21593,#21594,#21595,#21596,#21597,#21598,#21599,#21600,#21601,#21602,#21603,
#21604,#21605,#21606,#21607,#21608,#21609,#21610,#21611,#21612,#21613,#21614,
#21615,#21616,#21617,#21618,#21619,#21620,#21621,#21622,#21623,#21624,#21625,
#21626,#21627,#21628,#21629,#21630,#21631,#21632,#21633,#21634,#21635,#21636,
#21637,#21638,#21639,#21640,#21641,#21642,#21643,#21644,#21645,#21646,#21647,
#21648,#21649,#21650,#21651,#21652,#21653,#21654,#21655,#21656,#21657,#21658,
#21659,#21660,#21661,#21662,#21663,#21664,#21665,#21666,#21667,#21668,#21669,
#21670,#21671,#21672,#21673,#21674,#21675,#21676,#21677,#21678,#21679,#21680,
#21681,#21682,#21683,#21684,#21685,#21686,#21687,#21688,#21689,#21690,#21691,
#21692,#21693,#21694,#21695,#21696,#21697,#21698,#21699,#21700,#21701,#21702,
#21703,#21704,#21705,#21706,#21707,#21708,#21709,#21710,#21711,#21712,#21713,
#21714,#21715,#21716,#21717,#21718,#21719,#21720,#21721,#21722,#21723,#21724,
#21725,#21726,#21727,#21728,#21729,#21730,#21731,#21732,#21733,#21734,#21735,
#21736,#21737,#21738,#21739,#21740,#21741,#21742,#21743,#21744,#21745,#21746,
#21747,#21748,#21749,#21750,#21751,#21752,#21753,#21754,#21755,#21756,#21757,
#21758,#21759,#21760,#21761,#21762,#21763,#21764,#21765,#21766,#21767,#21768,
#21769,#21770,#21771,#21772,#21773,#21774,#21775,#21776,#21777,#21778,#21779,
#21780,#21781,#21782,#21783,#21784,#21785,#21786,#21787,#21788,#21789,#21790,
#21791,#21792,#21793,#21794,#21795,#21796,#21797,#21798,#21799,#21800,#21801,
#21802,#21803,#21804,#21805),.UNSPECIFIED.,.F.,.F.,(4,2,2,2,2,2,2,2,2,2,
2,2,2,2,2,2,2,2,2,2,2,2,2,2,2,2,2,2,2,2,2,2,2,2,2,2,2,2,2,2,2,2,2,2,2,2,
2,2,2,2,2,2,2,2,2,2,2,2,2,2,2,2,2,2,2,2,2,2,2,2,2,2,2,2,2,2,2,2,2,2,2,2,
2,2,2,2,2,2,2,2,2,2,2,2,2,2,2,2,2,2,2,2,2,2,2,2,2,2,4),(-2.69180502268216,
-2.69098358363705,-2.68886246929761,-2.68470097689536,-2.6577549091569,
-2.58389478623317,-2.55637814733146,-2.5395674861602,-2.53441201103297,
-2.53115299800168,-2.52812364253832,-2.52418651570319,-2.51759566115706,
-2.46793923265734,-2.39068125422341,-2.37493000085803,-2.37149626078189,
-2.36955727521549,-2.3678777726856,-2.36572845901756,-2.36128660196571,
-2.32521766519254,-2.26256970565054,-2.23393241278596,-2.21663605089012,
-2.21142748729118,-2.20815658155172,-2.20513100478276,-2.2012197036306,
-2.19471781410534,-2.14917658715137,-2.08156441301318,-2.06214658048509,
-2.05485433177623,-2.04957085857689,-2.04726416463708,-2.04556448048204,
-2.04371115668083,-2.04066395643112,-2.03086934245073,-1.95121836060041,
-1.89744691537271,-1.89078577967483,-1.88682805874426,-1.88379528173221,
-1.88054473992063,-1.87542835743921,-1.85897088566994,-1.83225328723325,
-1.75640354428838,-1.73009268910162,-1.72595389450485,-1.72383752417177,
-1.72216063304425,-1.72019796947154,-1.71665599776122,-1.69915378515835,
-1.62325628349064,-1.57422088611227,-1.56764228836061,-1.56370857108618,
-1.56067956920271,-1.55741870232406,-1.55225553513478,-1.53537736598037,
-1.50770288505918,-1.43516336059359,-1.40712092096809,-1.40292181085711,
-1.40079255368937,-1.39911470404518,-1.39716154604376,-1.39366322321443,
-1.37689424866944,-1.30046125112015,-1.25115863798108,-1.2445746865456,
-1.24063940859038,-1.23761016390584,-1.2343499800531,-1.22918990720931,
-1.21233988340498,-1.18472991746882,-1.11151823182696,-1.08401810062982,
-1.07983694701505,-1.07771151444344,-1.07603395721322,-1.07407801063294,
-1.07056691228205,-1.05358735349408,-0.977310537189237,-0.928082510657953,
-0.921500035257714,-0.91756518284616,-0.914535998778254,-0.911275617259664,
-0.906114671276844,-0.889256780249801,-0.861628813866283,-0.78859483489283,
-0.760952521356919,-0.756766570732481,-0.754640112795603,-0.752962474562208,
-0.751007270713667,-0.747499589186207,-0.730576758887035,-0.661807984799128),
 .UNSPECIFIED.);
#222=B_SPLINE_CURVE_WITH_KNOTS('',3,(#21810,#21811,#21812,#21813,#21814,
#21815,#21816,#21817,#21818,#21819,#21820,#21821,#21822,#21823,#21824,#21825,
#21826,#21827,#21828,#21829,#21830,#21831,#21832,#21833,#21834,#21835,#21836,
#21837,#21838,#21839,#21840,#21841,#21842,#21843,#21844,#21845,#21846,#21847,
#21848,#21849,#21850,#21851,#21852,#21853,#21854,#21855,#21856,#21857,#21858,
#21859,#21860,#21861,#21862,#21863,#21864,#21865,#21866,#21867,#21868,#21869,
#21870,#21871,#21872,#21873,#21874,#21875,#21876,#21877,#21878,#21879,#21880,
#21881,#21882,#21883,#21884,#21885,#21886,#21887,#21888,#21889,#21890,#21891,
#21892,#21893,#21894,#21895,#21896,#21897,#21898,#21899,#21900,#21901,#21902,
#21903,#21904,#21905,#21906,#21907,#21908,#21909,#21910,#21911,#21912,#21913,
#21914,#21915,#21916,#21917,#21918,#21919,#21920,#21921,#21922,#21923,#21924,
#21925,#21926,#21927,#21928,#21929,#21930,#21931,#21932,#21933,#21934,#21935,
#21936,#21937,#21938,#21939,#21940,#21941,#21942,#21943,#21944,#21945,#21946,
#21947,#21948,#21949,#21950,#21951,#21952,#21953,#21954,#21955,#21956,#21957,
#21958,#21959,#21960,#21961,#21962,#21963,#21964,#21965,#21966,#21967,#21968,
#21969,#21970,#21971,#21972,#21973,#21974,#21975,#21976,#21977,#21978,#21979,
#21980,#21981,#21982,#21983,#21984,#21985,#21986,#21987,#21988,#21989,#21990,
#21991,#21992,#21993,#21994,#21995,#21996,#21997,#21998,#21999,#22000,#22001,
#22002,#22003,#22004,#22005,#22006,#22007,#22008,#22009,#22010,#22011,#22012,
#22013,#22014,#22015,#22016,#22017,#22018,#22019,#22020,#22021,#22022,#22023),
 .UNSPECIFIED.,.F.,.F.,(4,2,2,2,2,2,2,2,2,2,2,2,2,2,2,2,2,2,2,2,2,2,2,2,
2,2,2,2,2,2,2,2,2,2,2,2,2,2,2,2,2,2,2,2,2,2,2,2,2,2,2,2,2,2,2,2,2,2,2,2,
2,2,2,2,2,2,2,2,2,2,2,2,2,2,2,2,2,2,2,2,2,2,2,2,2,2,2,2,2,2,2,2,2,2,2,2,
2,2,2,2,2,2,2,2,2,2,4),(-3.40023537643569,-3.33482078185619,-3.30719486950161,
-3.29033523387914,-3.28517320247625,-3.28191197376044,-3.27888188358579,
-3.27494567499668,-3.26836045983183,-3.21906860335362,-3.1425569306785,
-3.12580076494813,-3.12230240871166,-3.12034886027345,-3.11867042783018,
-3.11654008924492,-3.1123377816331,-3.08421993346944,-3.01182460862819,
-2.98415801707282,-2.96728033953895,-2.96211612285055,-2.95885428238125,
-2.95582415422582,-2.95188864913119,-2.94530626920494,-2.89617337285961,
-2.81998983409003,-2.80278126440513,-2.79925552182887,-2.79729593292003,
-2.79561801718591,-2.7934956514125,-2.78933106242006,-2.76233708521128,
-2.68852255018912,-2.66100033844717,-2.64418544131733,-2.63902794809165,
-2.63576747103202,-2.63273661807035,-2.62879734251646,-2.62220241790063,
-2.57245296636962,-2.49483755632898,-2.47947731681429,-2.47606857340942,
-2.47413450500865,-2.47245336709749,-2.47029422017985,-2.46580539845458,
-2.4262386953559,-2.36847625742542,-2.33896598030259,-2.32129602970495,
-2.31604619892625,-2.3127651407173,-2.30974086132929,-2.30584617027375,
-2.29940420549618,-2.25626330165687,-2.19386345910526,-2.16905381699869,
-2.1561088099532,-2.15288002433365,-2.1509856900146,-2.14929700013531,-2.14710888804055,
-2.14345323594964,-2.12034146941491,-2.10962599753095,-2.03152314379028,
-2.02122744771306,-1.99944375006007,-1.99361917422242,-1.99017733836269,
-1.98718316977388,-1.9834975552179,-1.97637918050148,-1.9200651726639,-1.85963851291728,
-1.83458282172232,-1.83049138590502,-1.82838461643966,-1.8267076302322,
-1.82473587112967,-1.82115458829943,-1.80297942502917,-1.72618180678269,
-1.67871268495384,-1.67216469347124,-1.66823897361453,-1.66521007514229,
-1.66194332995739,-1.65675802400204,-1.6396911344249,-1.6115862890577,-1.54671124652989,
-1.51195632735406,-1.50752256950061,-1.50537423955513,-1.50369411251794,
-1.50175277797187,-1.49831093281251,-1.48245266118319,-1.40528043645708,
-1.37015241264804),.UNSPECIFIED.);
#223=B_SPLINE_CURVE_WITH_KNOTS('',3,(#22025,#22026,#22027,#22028,#22029,
#22030,#22031,#22032,#22033,#22034,#22035,#22036,#22037,#22038,#22039,#22040,
#22041,#22042,#22043,#22044,#22045,#22046,#22047,#22048,#22049,#22050,#22051,
#22052,#22053,#22054,#22055,#22056,#22057,#22058,#22059,#22060,#22061,#22062,
#22063,#22064,#22065,#22066,#22067,#22068,#22069,#22070,#22071,#22072,#22073,
#22074,#22075,#22076,#22077,#22078,#22079,#22080,#22081,#22082,#22083,#22084,
#22085,#22086,#22087,#22088,#22089,#22090,#22091,#22092,#22093,#22094,#22095,
#22096,#22097,#22098,#22099,#22100),.UNSPECIFIED.,.F.,.F.,(4,2,2,2,2,2,
2,2,2,2,2,2,2,2,2,2,2,2,2,2,2,2,2,2,2,2,2,2,2,2,2,2,2,2,2,2,2,4),(-0.661807984799128,
-0.654257869818397,-0.605014980974329,-0.598429031543051,-0.594493162276247,
-0.591463814719946,-0.58820386700501,-0.583044906843026,-0.566205126427913,
-0.538618671574585,-0.468140561817124,-0.462130454299904,-0.437689929728706,
-0.433625192760907,-0.431524767779201,-0.429848909425109,-0.42787393520875,
-0.424275166859475,-0.405758519692253,-0.325536566182482,-0.281740120617086,
-0.275267094480029,-0.271364303988575,-0.268340089133171,-0.265538401924824,
-0.261004058170068,-0.248366526641298,-0.22953730751555,-0.193035807796621,
-0.118118298295534,-0.111729377774037,-0.10916430395282,-0.107590514978991,
-0.105855895048481,-0.103355943930342,-0.096903514059749,-0.0634855304692036,
-0.000963188783679523),.UNSPECIFIED.);
#224=B_SPLINE_CURVE_WITH_KNOTS('',3,(#22101,#22102,#22103,#22104,#22105,
#22106,#22107,#22108,#22109,#22110,#22111,#22112,#22113,#22114,#22115,#22116,
#22117,#22118,#22119,#22120,#22121,#22122,#22123,#22124,#22125,#22126,#22127,
#22128,#22129,#22130,#22131,#22132,#22133,#22134,#22135,#22136,#22137,#22138,
#22139,#22140,#22141,#22142,#22143,#22144,#22145,#22146,#22147,#22148,#22149,
#22150,#22151,#22152,#22153,#22154,#22155,#22156,#22157,#22158,#22159,#22160,
#22161,#22162,#22163,#22164,#22165,#22166,#22167,#22168,#22169,#22170,#22171,
#22172,#22173,#22174,#22175,#22176,#22177,#22178,#22179,#22180,#22181,#22182,
#22183,#22184,#22185,#22186,#22187,#22188,#22189,#22190,#22191,#22192,#22193,
#22194,#22195,#22196,#22197,#22198,#22199,#22200,#22201,#22202,#22203,#22204,
#22205,#22206,#22207,#22208,#22209,#22210,#22211,#22212,#22213,#22214,#22215,
#22216,#22217,#22218,#22219,#22220,#22221,#22222,#22223,#22224,#22225,#22226,
#22227,#22228,#22229,#22230,#22231,#22232,#22233,#22234,#22235,#22236,#22237,
#22238,#22239,#22240,#22241,#22242,#22243,#22244,#22245,#22246,#22247,#22248,
#22249,#22250,#22251,#22252,#22253,#22254,#22255,#22256,#22257,#22258,#22259,
#22260,#22261,#22262,#22263,#22264),.UNSPECIFIED.,.F.,.F.,(4,2,2,2,2,2,
2,2,2,2,2,2,2,2,2,2,2,2,2,2,2,2,2,2,2,2,2,2,2,2,2,2,2,2,2,2,2,2,2,2,2,2,
2,2,2,2,2,2,2,2,2,2,2,2,2,2,2,2,2,2,2,2,2,2,2,2,2,2,2,2,2,2,2,2,2,2,2,2,
2,2,2,4),(-4.0614287578822,-4.03248871540076,-4.01846104360662,-4.01365489798641,
-4.01033316269565,-4.00752181880818,-4.00452327004274,-4.0007622030692,
-3.99489804196461,-3.96524899606189,-3.94584283611108,-3.88111634163756,
-3.85452293802728,-3.84879489543677,-3.84641168900244,-3.84469933804932,
-3.84309929440734,-3.84039647146944,-3.8331451375629,-3.77212380131558,
-3.72144008924457,-3.70353835756497,-3.69530252279819,-3.68872717556511,
-3.68517352177786,-3.68247422333838,-3.67909297441338,-3.67338468946435,
-3.65345836652772,-3.55643899838608,-3.53774678690756,-3.53064256320669,
-3.52546566485076,-3.52317800715839,-3.52148127783768,-3.5196194663786,
-3.51653417352629,-3.50641678134479,-3.50451420221678,-3.41361908352743,
-3.38615026898234,-3.36936041640254,-3.36420716022018,-3.36094858742808,
-3.35791897603315,-3.35398057099992,-3.34738549014509,-3.29815696099868,
-3.22183041738727,-3.20486364478017,-3.2013533191308,-3.1993975661187,-3.19772002182691,
-3.19559442110385,-3.19141237522778,-3.16388011103469,-3.09076122624934,
-3.06315893043958,-3.04631045962763,-3.04115055523152,-3.03789039483268,
-3.03486111368623,-3.03092570368943,-3.02434129471597,-2.97503329712059,
-2.89858817553595,-2.8817742661767,-2.87827305475125,-2.87631921920786,
-2.87464136090194,-2.87251284295468,-2.86831745264589,-2.84038932807227,
-2.76775598971946,-2.74010440623786,-2.72323413696449,-2.71807163743497,
-2.71481077727113,-2.71178149438938,-2.70784700259689,-2.70126615755269,
-2.69232820337898),.UNSPECIFIED.);
#225=B_SPLINE_CURVE_WITH_KNOTS('',3,(#22270,#22271,#22272,#22273,#22274,
#22275,#22276,#22277,#22278),.UNSPECIFIED.,.F.,.F.,(4,1,1,1,1,1,4),(160.22122533308,
160.306526627267,161.306472639618,162.306418651969,163.306364664321,164.306310676672,
164.458927396546),.UNSPECIFIED.);
#226=B_SPLINE_CURVE_WITH_KNOTS('',3,(#22279,#22280,#22281,#22282,#22283,
#22284,#22285,#22286,#22287,#22288,#22289,#22290,#22291,#22292,#22293,#22294,
#22295,#22296,#22297,#22298,#22299,#22300,#22301,#22302,#22303,#22304,#22305,
#22306,#22307,#22308,#22309,#22310,#22311,#22312,#22313,#22314,#22315,#22316,
#22317,#22318,#22319,#22320,#22321,#22322,#22323,#22324,#22325,#22326,#22327,
#22328,#22329,#22330,#22331,#22332,#22333,#22334,#22335,#22336,#22337,#22338,
#22339,#22340,#22341,#22342,#22343,#22344,#22345,#22346,#22347,#22348,#22349,
#22350,#22351,#22352,#22353,#22354),.UNSPECIFIED.,.F.,.F.,(4,2,2,2,2,2,
2,2,2,2,2,2,2,2,2,2,2,2,2,2,2,2,2,2,2,2,2,2,2,2,2,2,2,2,2,2,2,4),(-4.0614630673581,
-4.05235423870892,-3.96283840444798,-3.93777252469754,-3.93188013811726,
-3.92845778818342,-3.92546300471007,-3.92175396700727,-3.91606035920602,
-3.88902746696132,-3.8050304357142,-3.78310043186638,-3.77517962828362,
-3.77130702260846,-3.76816909778494,-3.76629336885218,-3.76469327318415,
-3.76255009404327,-3.75814060112062,-3.7020680575884,-3.65787276096341,
-3.6302390214585,-3.6133762570027,-3.60821407922187,-3.60495294503442,-3.60192307173183,
-3.59798732806223,-3.59140329432733,-3.54215389317604,-3.4657303365375,
-3.44886309154659,-3.44535811526621,-3.44340319417903,-3.44172502335401,
-3.43959686996878,-3.43540447334862,-3.40763336833459,-3.40023537643569),
 .UNSPECIFIED.);
#227=B_SPLINE_CURVE_WITH_KNOTS('',3,(#22355,#22356,#22357,#22358,#22359,
#22360,#22361,#22362,#22363,#22364,#22365,#22366,#22367,#22368,#22369,#22370,
#22371,#22372,#22373,#22374,#22375,#22376,#22377,#22378,#22379,#22380,#22381,
#22382,#22383,#22384,#22385,#22386,#22387,#22388,#22389,#22390,#22391,#22392,
#22393,#22394,#22395,#22396,#22397,#22398,#22399,#22400,#22401,#22402,#22403,
#22404,#22405,#22406,#22407,#22408,#22409,#22410,#22411,#22412,#22413,#22414,
#22415,#22416,#22417,#22418,#22419,#22420,#22421,#22422,#22423,#22424,#22425,
#22426,#22427,#22428,#22429,#22430,#22431,#22432,#22433,#22434,#22435,#22436,
#22437,#22438,#22439,#22440,#22441,#22442,#22443,#22444,#22445,#22446,#22447,
#22448,#22449,#22450,#22451,#22452,#22453,#22454,#22455,#22456,#22457,#22458,
#22459,#22460,#22461,#22462,#22463,#22464,#22465,#22466,#22467,#22468,#22469,
#22470,#22471,#22472,#22473,#22474,#22475,#22476,#22477,#22478,#22479,#22480,
#22481,#22482,#22483,#22484,#22485,#22486,#22487,#22488,#22489,#22490,#22491,
#22492,#22493,#22494,#22495,#22496,#22497,#22498,#22499,#22500,#22501,#22502,
#22503,#22504,#22505,#22506,#22507,#22508,#22509,#22510,#22511,#22512,#22513,
#22514,#22515,#22516,#22517,#22518,#22519,#22520,#22521,#22522,#22523,#22524,
#22525,#22526,#22527,#22528,#22529,#22530,#22531,#22532,#22533,#22534,#22535,
#22536,#22537,#22538,#22539,#22540,#22541,#22542,#22543,#22544,#22545,#22546,
#22547,#22548,#22549,#22550,#22551,#22552,#22553,#22554,#22555,#22556,#22557,
#22558,#22559,#22560,#22561,#22562,#22563,#22564,#22565,#22566),
 .UNSPECIFIED.,.F.,.F.,(4,2,2,2,2,2,2,2,2,2,2,2,2,2,2,2,2,2,2,2,2,2,2,2,
2,2,2,2,2,2,2,2,2,2,2,2,2,2,2,2,2,2,2,2,2,2,2,2,2,2,2,2,2,2,2,2,2,2,2,2,
2,2,2,2,2,2,2,2,2,2,2,2,2,2,2,2,2,2,2,2,2,2,2,2,2,2,2,2,2,2,2,2,2,2,2,2,
2,2,2,2,2,2,2,2,2,4),(-2.69232820337898,-2.65215331755146,-2.57610388787892,
-2.55874252190226,-2.55520845908299,-2.55324739746129,-2.55157016471346,
-2.54945118635699,-2.5453008033091,-2.51868116942949,-2.44436574494018,
-2.41690138391812,-2.40011266218735,-2.39495896467106,-2.391699930452,-2.38866976400286,
-2.38473045818825,-2.37813347333805,-2.32868997370835,-2.25191573891669,
-2.23552390746872,-2.23204851955261,-2.23010018678417,-2.22842149070606,
-2.22628472487605,-2.22287778578281,-2.20478565495202,-2.1045602781164,
-2.07843784358157,-2.07247131749459,-2.06903277073797,-2.06603972630721,
-2.06235328025359,-2.05673239951629,-2.03080471296937,-1.97580982653872,
-1.94588728187544,-1.93779308354745,-1.9134451694628,-1.90938428253259,
-1.90728467757254,-1.90560885148976,-1.90363318936277,-1.90003129527163,
-1.88145719932781,-1.80063827631087,-1.7574399740288,-1.75099908058603,
-1.74710571190354,-1.7440828863301,-1.74080384074389,-1.73555819605331,
-1.71791208240507,-1.68844885628179,-1.63096870377777,-1.59100057425755,
-1.58650919985396,-1.58435018577139,-1.5826697993837,-1.5807373452675,-1.57733328749,
-1.56202461388756,-1.48445088468712,-1.43468019637624,-1.42808727138658,
-1.42414948173725,-1.42111996890225,-1.41786113492771,-1.41270668666146,
-1.39590617689815,-1.36840897502444,-1.29423806712174,-1.26748633929008,
-1.26333151633647,-1.2612117690953,-1.25953470699639,-1.25757473367821,
-1.25404488214976,-1.23674817735237,-1.16070716478711,-1.11159742061136,
-1.10501758302102,-1.10108359618052,-1.09805466260356,-1.0947941410465,
-1.08963210011751,-1.07276280810492,-1.04510818063073,-0.972368929468456,
-0.944493035068862,-0.940299499291466,-0.938171484898872,-0.936493800339113,
-0.934539899570493,-0.931037926828355,-0.914207256388892,-0.837824288323109,
-0.788545872915298,-0.781962655556508,-0.778027682083294,-0.774998593294991,
-0.771738499937146,-0.766578405634705,-0.749726837719345,-0.7221128406229,
-0.662156536932336),.UNSPECIFIED.);
#228=B_SPLINE_CURVE_WITH_KNOTS('',3,(#22572,#22573,#22574,#22575,#22576,
#22577,#22578,#22579,#22580,#22581,#22582,#22583,#22584,#22585,#22586,#22587,
#22588,#22589,#22590,#22591,#22592,#22593,#22594,#22595,#22596,#22597,#22598,
#22599,#22600,#22601,#22602,#22603,#22604,#22605,#22606,#22607,#22608,#22609,
#22610,#22611,#22612,#22613,#22614,#22615,#22616,#22617,#22618,#22619,#22620,
#22621,#22622,#22623,#22624,#22625,#22626,#22627,#22628,#22629,#22630,#22631,
#22632,#22633,#22634,#22635,#22636,#22637,#22638,#22639,#22640,#22641,#22642,
#22643,#22644,#22645,#22646,#22647,#22648,#22649,#22650,#22651,#22652,#22653,
#22654,#22655,#22656,#22657,#22658,#22659,#22660,#22661,#22662,#22663,#22664,
#22665,#22666,#22667,#22668,#22669,#22670,#22671,#22672,#22673,#22674,#22675,
#22676,#22677,#22678,#22679,#22680,#22681,#22682,#22683,#22684,#22685,#22686,
#22687,#22688,#22689,#22690,#22691,#22692,#22693,#22694,#22695,#22696,#22697,
#22698,#22699,#22700,#22701,#22702,#22703,#22704,#22705,#22706,#22707,#22708,
#22709,#22710,#22711,#22712,#22713,#22714,#22715,#22716,#22717,#22718,#22719),
 .UNSPECIFIED.,.F.,.F.,(4,2,2,2,2,2,2,2,2,2,2,2,2,2,2,2,2,2,2,2,2,2,2,2,
2,2,2,2,2,2,2,2,2,2,2,2,2,2,2,2,2,2,2,2,2,2,2,2,2,2,2,2,2,2,2,2,2,2,2,2,
2,2,2,2,2,2,2,2,2,2,2,2,2,4),(-1.37008796384114,-1.36509452139955,-1.33756705120965,
-1.26368343230619,-1.23671424426907,-1.23255080247012,-1.2304288356845,
-1.22875114013694,-1.22679168817352,-1.22326591239097,-1.20605080402931,
-1.12992498236679,-1.08081976705881,-1.07423874891923,-1.070303803348,-1.06727397461942,
-1.06401232857066,-1.05884814934947,-1.0419683457706,-1.01429186311723,
-0.941855362331853,-0.913734708695746,-0.909532372698914,-0.907402106931502,
-0.905723776584494,-0.903770385711698,-0.900272435613842,-0.883519770475412,
-0.807052768490655,-0.757781920452373,-0.751197573840573,-0.747261652086498,
-0.744231664359939,-0.740970430796123,-0.735808148573984,-0.718945687248358,
-0.691308980812469,-0.620870374069518,-0.614969858323678,-0.590479109974328,
-0.586411585532371,-0.584310240216116,-0.582633918546744,-0.580658681749976,
-0.577060132417265,-0.558559337013442,-0.478501477509581,-0.468039787372866,
-0.433871639893346,-0.42776519906544,-0.423929513645285,-0.420922167846103,
-0.417579260091554,-0.412047651623141,-0.391792315100057,-0.310341290712693,
-0.26802602034066,-0.263514571034847,-0.261351215984343,-0.259669921488299,
-0.257739175796078,-0.254573477874679,-0.241479782206959,-0.216107046963393,
-0.183560071733502,-0.117597596727701,-0.106504907451117,-0.101970548454938,
-0.0991562778078226,-0.0960944020792617,-0.0918983056610401,-0.087252618025963,
-0.0792406479124629,-0.000962876874443607),.UNSPECIFIED.);
#229=B_SPLINE_CURVE_WITH_KNOTS('',3,(#22720,#22721,#22722,#22723,#22724,
#22725),.UNSPECIFIED.,.F.,.F.,(4,1,1,4),(164.458927396546,165.306256689024,
166.306202701375,166.504410640259),.UNSPECIFIED.);
#230=B_SPLINE_CURVE_WITH_KNOTS('',3,(#22727,#22728,#22729,#22730,#22731,
#22732,#22733,#22734,#22735,#22736,#22737,#22738,#22739,#22740,#22741,#22742,
#22743,#22744,#22745,#22746,#22747,#22748,#22749,#22750,#22751,#22752,#22753,
#22754,#22755,#22756,#22757,#22758,#22759,#22760,#22761,#22762,#22763,#22764,
#22765,#22766,#22767,#22768,#22769,#22770,#22771,#22772,#22773,#22774,#22775,
#22776,#22777,#22778,#22779,#22780,#22781,#22782,#22783,#22784,#22785,#22786,
#22787,#22788,#22789,#22790,#22791,#22792,#22793,#22794,#22795,#22796,#22797,
#22798,#22799,#22800,#22801,#22802,#22803,#22804,#22805,#22806,#22807,#22808,
#22809,#22810,#22811,#22812,#22813,#22814),.UNSPECIFIED.,.F.,.F.,(4,2,2,
2,2,2,2,2,2,2,2,2,2,2,2,2,2,2,2,2,2,2,2,2,2,2,2,2,2,2,2,2,2,2,2,2,2,2,2,
2,2,2,2,4),(-0.662156536932336,-0.648956013746852,-0.621418192193571,-0.617234499775957,
-0.615108581233505,-0.613431055280487,-0.611475622140756,-0.607966632969675,
-0.591020215921372,-0.514722936640716,-0.465485531341795,-0.458903121030178,
-0.454968378544555,-0.451939320614257,-0.448679115744897,-0.443518536519126,
-0.426662623721119,-0.399038694208074,-0.355194168524487,-0.298655849376382,
-0.294253481146245,-0.292112018854427,-0.290433286732513,-0.290426632483179,
-0.290420084506535,-0.290413640687297,-0.290407299018121,-0.290401057478961,
-0.2903949140909,-0.288474887817562,-0.285144057785002,-0.280975459144695,
-0.272195312542459,-0.246600417983609,-0.184345430883523,-0.142200987206802,
-0.135789521101596,-0.13190488755513,-0.128883447241603,-0.125600486147694,
-0.120336747935594,-0.102516454894325,-0.0726393233951299,-0.000963379534404715),
 .UNSPECIFIED.);
#231=B_SPLINE_CURVE_WITH_KNOTS('',3,(#22815,#22816,#22817,#22818,#22819,
#22820,#22821,#22822,#22823,#22824,#22825,#22826,#22827,#22828,#22829,#22830,
#22831,#22832,#22833,#22834,#22835,#22836,#22837,#22838,#22839,#22840,#22841,
#22842,#22843,#22844,#22845,#22846,#22847,#22848,#22849,#22850,#22851,#22852,
#22853,#22854,#22855,#22856,#22857,#22858,#22859,#22860,#22861,#22862,#22863,
#22864,#22865,#22866,#22867,#22868,#22869,#22870,#22871,#22872,#22873,#22874,
#22875,#22876,#22877,#22878,#22879,#22880,#22881,#22882,#22883,#22884,#22885,
#22886,#22887,#22888,#22889,#22890,#22891,#22892,#22893,#22894,#22895,#22896,
#22897,#22898,#22899,#22900,#22901,#22902,#22903,#22904,#22905,#22906,#22907,
#22908,#22909,#22910,#22911,#22912,#22913,#22914,#22915,#22916,#22917,#22918,
#22919,#22920,#22921,#22922,#22923,#22924,#22925,#22926,#22927,#22928,#22929,
#22930,#22931,#22932,#22933,#22934,#22935,#22936,#22937,#22938,#22939,#22940,
#22941,#22942,#22943,#22944,#22945,#22946,#22947,#22948,#22949,#22950,#22951,
#22952,#22953,#22954,#22955,#22956,#22957,#22958,#22959,#22960,#22961,#22962,
#22963,#22964,#22965,#22966,#22967,#22968,#22969,#22970,#22971,#22972,#22973,
#22974,#22975,#22976,#22977,#22978,#22979,#22980,#22981,#22982),
 .UNSPECIFIED.,.F.,.F.,(4,2,2,2,2,2,2,2,2,2,2,2,2,2,2,2,2,2,2,2,2,2,2,2,
2,2,2,2,2,2,2,2,2,2,2,2,2,2,2,2,2,2,2,2,2,2,2,2,2,2,2,2,2,2,2,2,2,2,2,2,
2,2,2,2,2,2,2,2,2,2,2,2,2,2,2,2,2,2,2,2,2,2,2,4),(-4.06137411129811,-4.03546814208168,
-4.03260936723115,-4.03068543622094,-4.02910207865154,-4.02742394594966,
-4.02528765473165,-4.02188101107949,-4.00378125912536,-3.99087511127817,
-3.92336215122477,-3.89390000861074,-3.87625324670922,-3.87100804923103,
-3.86772941140725,-3.86470704756532,-3.86081439142151,-3.85437488405435,
-3.81121148531092,-3.74866773042392,-3.72400495439522,-3.71543798804153,
-3.71134229651865,-3.70803197674221,-3.70613041934244,-3.70612544828196,
-3.70612044883366,-3.70611542078261,-3.70443560804051,-3.70228077409685,
-3.69780993954386,-3.64539408540266,-3.5975998397588,-3.5699879776209,-3.55313585729943,
-3.54797591462403,-3.5447159788346,-3.5416870780946,-3.53775240607612,-3.53116976900817,
-3.48191981090553,-3.40559298472915,-3.38863278312118,-3.38512298134602,
-3.38316740373971,-3.38148993761662,-3.37936434319125,-3.3751820310455,
-3.34763695028034,-3.27453969815414,-3.24693700621568,-3.23008860856498,
-3.22492888144925,-3.2216688687451,-3.21863974945762,-3.21470458469248,
-3.20812066303947,-3.15882272722111,-3.08239739921846,-3.06556304272006,
-3.06206071391739,-3.06010669570504,-3.05842895425275,-3.05630093644398,
-3.05210759438145,-3.02423685725316,-2.95153830415818,-2.92389457450066,
-2.90702798083542,-2.90186605690893,-2.89860543385016,-2.89557628398828,
-2.89164184114217,-2.88506080525283,-2.83592398160934,-2.75982708098895,
-2.74253790851482,-2.73900821643197,-2.73704816754924,-2.73537093391692,
-2.73325084441166,-2.72909497053658,-2.70231907556713,-2.69288841829231),
 .UNSPECIFIED.);
#232=B_SPLINE_CURVE_WITH_KNOTS('',3,(#22987,#22988,#22989,#22990,#22991,
#22992,#22993,#22994,#22995,#22996,#22997,#22998,#22999,#23000,#23001,#23002,
#23003,#23004,#23005,#23006,#23007,#23008,#23009,#23010,#23011,#23012,#23013,
#23014,#23015,#23016,#23017,#23018,#23019,#23020,#23021,#23022,#23023,#23024,
#23025,#23026,#23027,#23028,#23029,#23030,#23031,#23032,#23033,#23034,#23035,
#23036,#23037,#23038,#23039,#23040,#23041,#23042,#23043,#23044,#23045,#23046,
#23047,#23048,#23049,#23050,#23051,#23052,#23053,#23054,#23055,#23056,#23057,
#23058,#23059,#23060,#23061,#23062,#23063,#23064,#23065,#23066,#23067,#23068,
#23069,#23070,#23071,#23072,#23073,#23074,#23075,#23076,#23077,#23078,#23079,
#23080,#23081,#23082,#23083,#23084,#23085,#23086,#23087,#23088,#23089,#23090,
#23091,#23092,#23093,#23094,#23095,#23096,#23097,#23098,#23099,#23100,#23101,
#23102,#23103,#23104,#23105,#23106,#23107,#23108,#23109,#23110,#23111,#23112,
#23113,#23114,#23115,#23116,#23117,#23118,#23119,#23120,#23121,#23122,#23123,
#23124,#23125,#23126,#23127,#23128,#23129,#23130,#23131,#23132,#23133,#23134,
#23135,#23136,#23137,#23138,#23139,#23140,#23141,#23142,#23143,#23144,#23145,
#23146,#23147,#23148,#23149,#23150,#23151,#23152,#23153,#23154,#23155,#23156,
#23157,#23158,#23159,#23160,#23161,#23162,#23163,#23164,#23165,#23166,#23167,
#23168,#23169,#23170,#23171,#23172,#23173,#23174,#23175,#23176,#23177,#23178,
#23179,#23180,#23181,#23182,#23183,#23184,#23185,#23186,#23187,#23188,#23189,
#23190,#23191,#23192,#23193,#23194,#23195,#23196,#23197,#23198,#23199,#23200,
#23201,#23202,#23203,#23204,#23205,#23206,#23207,#23208,#23209,#23210),
 .UNSPECIFIED.,.F.,.F.,(4,2,2,2,2,2,2,2,2,2,2,2,2,2,2,2,2,2,2,2,2,2,2,2,
2,2,2,2,2,2,2,2,2,2,2,2,2,2,2,2,2,2,2,2,2,2,2,2,2,2,2,2,2,2,2,2,2,2,2,2,
2,2,2,2,2,2,2,2,2,2,2,2,2,2,2,2,2,2,2,2,2,2,2,2,2,2,2,2,2,2,2,2,2,2,2,2,
2,2,2,2,2,2,2,2,2,2,2,2,2,2,2,4),(-3.39966608106449,-3.38261128349882,-3.35497570774651,
-3.338113451604,-3.33295200935335,-3.32969146948553,-3.32666223742753,-3.32272745345153,
-3.31614531186498,-3.26694168136053,-3.1907099101825,-3.17363514114318,
-3.17011842316367,-3.16816131401051,-3.16648402352849,-3.16436051743969,
-3.16018776103442,-3.13291633050984,-3.05949811623182,-3.03194119663903,
-3.01511328560141,-3.00995596861619,-3.00669657453334,-3.00366740214253,
-2.99973127200117,-2.99314374523304,-2.94364090247096,-2.86670894548044,
-2.85055095601095,-2.84709090394187,-2.84514617557408,-2.84346726749296,
-2.84132600076709,-2.83790404593358,-2.81957711423026,-2.80891652745426,
-2.73669207491879,-2.70901751536791,-2.69213721490099,-2.68697328756015,
-2.68371187685395,-2.68068231677239,-2.67674778689009,-2.67016755184739,
-2.62108505627865,-2.54493668804139,-2.52769090989588,-2.52416333160112,
-2.52220351047619,-2.52052595489496,-2.51840471596455,-2.51424415045443,
-2.48734372264166,-2.41343298042621,-2.38593254279303,-2.36912835008891,
-2.36397282631354,-2.3607132905156,-2.35768310268818,-2.35374439357789,
-2.34714976139369,-2.29734863682004,-2.21959576937047,-2.20443222572976,
-2.20103751302584,-2.19910683116374,-2.19742569567641,-2.19526269934773,
-2.19075250656781,-2.14851804884808,-2.06719291631178,-2.04677288712501,
-2.0412558210861,-2.03791627694886,-2.03490847978163,-2.03106742517263,
-2.02317458368319,-1.95967605606827,-1.88628544679042,-1.87975250323861,
-1.877162868236,-1.87558422288974,-1.87385357929687,-1.87137531622725,-1.86506480397488,
-1.83306105454725,-1.77047461586855,-1.75729397090777,-1.7441860953638,
-1.72414060652952,-1.71841855108414,-1.71503336288645,-1.71233325925205,
-1.70870922850884,-1.70188403501992,-1.65762275671428,-1.60008308379339,
-1.56020166884823,-1.55571017087348,-1.55355071755667,-1.55186981265787,
-1.54993653655055,-1.54653042770158,-1.53120211913237,-1.45361840498715,
-1.40388867049861,-1.39729526300685,-1.39335671251092,-1.3903263291247,
-1.38706627187768,-1.38190926344052,-1.37008796384114),.UNSPECIFIED.);
#233=B_SPLINE_CURVE_WITH_KNOTS('',3,(#23211,#23212,#23213,#23214,#23215,
#23216,#23217,#23218,#23219,#23220,#23221,#23222,#23223,#23224,#23225,#23226,
#23227,#23228,#23229,#23230,#23231,#23232,#23233,#23234,#23235,#23236,#23237,
#23238,#23239,#23240,#23241,#23242,#23243,#23244,#23245,#23246,#23247,#23248,
#23249,#23250,#23251,#23252,#23253,#23254,#23255,#23256,#23257,#23258,#23259,
#23260,#23261,#23262,#23263,#23264,#23265,#23266,#23267,#23268,#23269,#23270,
#23271,#23272,#23273,#23274,#23275,#23276,#23277,#23278,#23279,#23280,#23281,
#23282,#23283,#23284,#23285,#23286,#23287,#23288,#23289,#23290,#23291,#23292,
#23293,#23294,#23295,#23296,#23297,#23298,#23299,#23300,#23301,#23302,#23303,
#23304,#23305,#23306,#23307,#23308,#23309,#23310,#23311,#23312,#23313,#23314,
#23315,#23316,#23317,#23318,#23319,#23320,#23321,#23322,#23323,#23324,#23325,
#23326,#23327,#23328,#23329,#23330,#23331,#23332,#23333,#23334,#23335,#23336,
#23337,#23338,#23339,#23340,#23341,#23342,#23343,#23344,#23345,#23346,#23347,
#23348,#23349,#23350,#23351,#23352,#23353,#23354,#23355,#23356,#23357,#23358,
#23359,#23360,#23361,#23362,#23363,#23364,#23365,#23366,#23367,#23368,#23369,
#23370,#23371,#23372,#23373,#23374,#23375,#23376,#23377,#23378,#23379,#23380,
#23381,#23382,#23383,#23384,#23385,#23386,#23387,#23388,#23389,#23390,#23391,
#23392,#23393,#23394,#23395,#23396,#23397,#23398,#23399,#23400,#23401,#23402,
#23403,#23404,#23405,#23406,#23407,#23408,#23409,#23410,#23411,#23412,#23413,
#23414,#23415,#23416,#23417,#23418,#23419,#23420),.UNSPECIFIED.,.F.,.F.,
(4,2,2,2,2,2,2,2,2,2,2,2,2,2,2,2,2,2,2,2,2,2,2,2,2,2,2,2,2,2,2,2,2,2,2,
2,2,2,2,2,2,2,2,2,2,2,2,2,2,2,2,2,2,2,2,2,2,2,2,2,2,2,2,2,2,2,2,2,2,2,2,
2,2,2,2,2,2,2,2,2,2,2,2,2,2,2,2,2,2,2,2,2,2,2,2,2,2,2,2,2,2,2,2,2,4),(-2.69288841829231,
-2.62821882857888,-2.6007272457602,-2.58392685535843,-2.57877203897195,
-2.5755128666472,-2.57248296531735,-2.5685445636208,-2.56195032742445,-2.5121627565062,
-2.43456185993032,-2.41921818360647,-2.41581133401556,-2.41387807961672,
-2.41219749054209,-2.41003887805007,-2.40555060755085,-2.36593727651975,
-2.30537801053633,-2.27772835275544,-2.26085845100696,-2.25569566369569,
-2.25243452943043,-2.24940492818091,-2.24546993238837,-2.23888804491525,
-2.18975083361885,-2.11365587102885,-2.09634556667394,-2.09281425284967,
-2.09085367158604,-2.08917621102593,-2.08705612618127,-2.08290112561271,
-2.05616258912101,-2.03199624470501,-1.94597896357116,-1.93591544299417,
-1.93199209624569,-1.92914836552149,-1.92610767860638,-1.92203409081843,
-1.91290505419737,-1.87535572106653,-1.80071489023966,-1.77429011247854,
-1.77014648718103,-1.76802884968564,-1.76635158185573,-1.76438920303215,
-1.76084957159198,-1.74339580996198,-1.66744737487523,-1.61838183785446,
-1.6118015624543,-1.60786697224214,-1.60483737445711,-1.60157594124946,
-1.5964120377444,-1.57953290048706,-1.55185828817305,-1.47924943754684,
-1.45124694014851,-1.44704848820846,-1.44491913173856,-1.44324097358994,
-1.44128718560547,-1.43778709672479,-1.42099750256704,-1.34456105711149,
-1.29525838411997,-1.28867332750679,-1.2847373215308,-1.28170747656142,
-1.27844660714296,-1.27328536447936,-1.25643075273483,-1.22881247853191,
-1.15561506517993,-1.12808709532021,-1.12390436286328,-1.12177835145588,
-1.1201004670003,-1.11814429827942,-1.1146331345721,-1.09765973572434,-1.02136300866315,
-0.97211996680353,-0.965536191401954,-0.961600609134019,-0.958570891342557,
-0.955309963443433,-0.950148213284202,-0.933288257111523,-0.905657539389735,
-0.832580728904072,-0.804956179165809,-0.800770253437381,-0.79864358802766,
-0.796965672120665,-0.795010015864425,-0.791501209614637,-0.774566977529387,
-0.698242856613169,-0.662479512201711),.UNSPECIFIED.);
#234=B_SPLINE_CURVE_WITH_KNOTS('',3,(#23426,#23427,#23428,#23429,#23430,
#23431,#23432,#23433,#23434,#23435,#23436,#23437,#23438,#23439,#23440,#23441,
#23442,#23443,#23444,#23445,#23446,#23447,#23448,#23449,#23450,#23451,#23452,
#23453,#23454,#23455,#23456,#23457,#23458,#23459,#23460,#23461,#23462,#23463,
#23464,#23465,#23466,#23467,#23468,#23469,#23470,#23471,#23472,#23473,#23474,
#23475,#23476,#23477,#23478,#23479,#23480,#23481,#23482,#23483,#23484,#23485,
#23486,#23487,#23488,#23489,#23490,#23491,#23492,#23493,#23494,#23495,#23496,
#23497,#23498,#23499,#23500,#23501,#23502,#23503,#23504,#23505,#23506,#23507,
#23508,#23509,#23510,#23511,#23512,#23513,#23514,#23515,#23516,#23517,#23518,
#23519,#23520,#23521,#23522,#23523,#23524,#23525,#23526,#23527,#23528,#23529,
#23530,#23531,#23532,#23533,#23534,#23535,#23536,#23537,#23538,#23539,#23540,
#23541,#23542,#23543,#23544,#23545,#23546,#23547,#23548,#23549,#23550,#23551,
#23552,#23553,#23554,#23555,#23556,#23557,#23558,#23559,#23560,#23561,#23562,
#23563,#23564,#23565,#23566,#23567),.UNSPECIFIED.,.F.,.F.,(4,3,3,3,3,3,
3,3,3,3,3,3,3,3,3,3,3,3,3,3,3,3,3,3,3,3,3,3,3,3,3,3,3,3,3,3,3,3,3,3,3,3,
3,3,3,3,3,4),(179.070781254915,179.194664687591,179.305500861943,179.39859273852,
179.491558370991,179.584425373595,179.677224205602,179.769987658213,179.862740536934,
179.955507631942,180.048373536086,180.141291001732,180.234363515655,180.305446874294,
180.398541048115,180.491509359221,180.584379412833,180.677181836596,180.769949210642,
180.862706333617,180.955477989103,181.048348910899,181.141271655451,181.234349817205,
181.305392886646,181.398334052106,181.491148767177,181.583864836116,181.676513311331,
181.76912680166,181.861730280687,181.954348707172,182.047067984862,182.139839721645,
182.232769500411,182.305338898997,182.398589636842,182.491713738259,182.584738616987,
182.677693796661,182.770612606954,182.863519673557,182.956439605844,183.04945531922,
183.142521141419,183.235738105157,183.305284911348,183.307775588641),
 .UNSPECIFIED.);
#235=B_SPLINE_CURVE_WITH_KNOTS('',3,(#23568,#23569,#23570,#23571,#23572,
#23573,#23574,#23575,#23576,#23577,#23578,#23579,#23580,#23581,#23582,#23583,
#23584,#23585,#23586,#23587,#23588,#23589,#23590,#23591,#23592,#23593,#23594,
#23595,#23596,#23597,#23598,#23599,#23600,#23601,#23602,#23603,#23604,#23605,
#23606,#23607,#23608,#23609,#23610,#23611,#23612,#23613,#23614,#23615,#23616,
#23617,#23618,#23619,#23620,#23621,#23622,#23623,#23624,#23625,#23626,#23627,
#23628,#23629,#23630,#23631,#23632,#23633,#23634,#23635,#23636,#23637,#23638,
#23639,#23640,#23641,#23642,#23643,#23644,#23645,#23646,#23647,#23648,#23649),
 .UNSPECIFIED.,.F.,.F.,(4,2,2,2,2,2,2,2,2,2,2,2,2,2,2,2,2,2,2,2,2,2,2,2,
2,2,2,2,2,2,2,2,2,2,2,2,2,2,2,2,4),(-4.06064997137112,-4.00430212489643,
-3.9868513581544,-3.9820030275949,-3.97866530730521,-3.97540299905737,-3.97237911174722,
-3.96846118072314,-3.96192906392512,-3.91487982033083,-3.89956282472104,
-3.89810813990657,-3.864651258576,-3.82517255520197,-3.81778930412554,-3.81575922412801,
-3.81383283440873,-3.81215259313831,-3.80998797932649,-3.80546786376064,
-3.75977925280789,-3.69886501358032,-3.67541231637473,-3.66050213306632,
-3.65574544601386,-3.65248155291347,-3.64945235973654,-3.64552208156608,
-3.63895720591681,-3.59061317511019,-3.51471753417946,-3.4966681963661,
-3.49309358890036,-3.49111519062416,-3.48943896207023,-3.48734102711929,
-3.48406109914624,-3.46794153634667,-3.45940315232818,-3.42919062260033,
-3.39966608106449),.UNSPECIFIED.);
#236=B_SPLINE_CURVE_WITH_KNOTS('',3,(#23651,#23652,#23653,#23654,#23655,
#23656,#23657,#23658,#23659,#23660,#23661,#23662,#23663,#23664,#23665,#23666,
#23667,#23668,#23669,#23670,#23671,#23672,#23673,#23674,#23675,#23676,#23677,
#23678,#23679,#23680,#23681,#23682,#23683,#23684,#23685,#23686,#23687,#23688,
#23689,#23690,#23691,#23692,#23693,#23694,#23695,#23696,#23697,#23698,#23699,
#23700,#23701,#23702,#23703,#23704,#23705,#23706,#23707,#23708,#23709,#23710,
#23711,#23712,#23713,#23714,#23715,#23716,#23717,#23718,#23719,#23720,#23721,
#23722,#23723,#23724,#23725,#23726,#23727,#23728,#23729,#23730,#23731,#23732,
#23733,#23734,#23735,#23736,#23737,#23738,#23739,#23740,#23741,#23742,#23743,
#23744,#23745,#23746,#23747,#23748,#23749,#23750,#23751,#23752,#23753,#23754,
#23755,#23756,#23757,#23758,#23759,#23760,#23761,#23762,#23763,#23764,#23765,
#23766),.UNSPECIFIED.,.F.,.F.,(4,2,2,2,2,2,2,2,2,2,2,2,2,2,2,2,2,2,2,2,
2,2,2,2,2,2,2,2,2,2,2,2,2,2,2,2,2,2,2,2,2,2,2,2,2,2,2,2,2,2,2,2,2,2,2,2,
2,4),(-0.662479512201711,-0.649009424411012,-0.642409141833841,-0.638468707869307,
-0.635438182478318,-0.632179264095796,-0.627026819422034,-0.610251866436487,
-0.582815677117585,-0.508156618053557,-0.481743925243419,-0.477600639337013,
-0.475483028236158,-0.473805651605458,-0.471842955267847,-0.468302491705472,
-0.450839150649112,-0.374882833553105,-0.325871973122078,-0.318694037867528,
-0.314917377826305,-0.311983489431598,-0.311920428982104,-0.31186191958805,
-0.311807486730928,-0.311756719226512,-0.311709262158357,-0.311664806402384,
-0.311623081297898,-0.311583848699337,-0.311546898111623,-0.311512042695099,
-0.311479115966062,-0.311447969026018,-0.311418468253126,-0.311390493337331,
-0.311363935643299,-0.311338696775966,-0.31131468739484,-0.31129182617357,
-0.311270038880336,-0.311234493337896,-0.307662220568363,-0.303815800756465,
-0.297749141659154,-0.26285874592463,-0.212549790608409,-0.18103199971563,
-0.158401309690868,-0.154766783500816,-0.152585227276661,-0.150897943913734,
-0.149001242898515,-0.145759233350475,-0.132638674924846,-0.107321035533903,
-0.0120020791574577,-0.00125822521736063),.UNSPECIFIED.);
#237=B_SPLINE_CURVE_WITH_KNOTS('',3,(#23767,#23768,#23769,#23770,#23771,
#23772,#23773,#23774,#23775,#23776,#23777,#23778,#23779,#23780,#23781,#23782,
#23783,#23784,#23785,#23786,#23787,#23788,#23789,#23790,#23791,#23792,#23793,
#23794,#23795,#23796,#23797,#23798,#23799,#23800,#23801,#23802,#23803,#23804,
#23805,#23806,#23807,#23808,#23809,#23810,#23811,#23812,#23813,#23814,#23815,
#23816,#23817,#23818,#23819,#23820,#23821,#23822,#23823,#23824,#23825,#23826,
#23827,#23828,#23829,#23830,#23831,#23832,#23833,#23834,#23835,#23836,#23837,
#23838,#23839,#23840,#23841,#23842,#23843,#23844,#23845,#23846,#23847,#23848,
#23849,#23850,#23851,#23852,#23853,#23854,#23855,#23856,#23857,#23858,#23859,
#23860,#23861,#23862,#23863,#23864,#23865,#23866,#23867,#23868,#23869,#23870,
#23871,#23872,#23873,#23874,#23875,#23876,#23877,#23878,#23879,#23880,#23881,
#23882,#23883,#23884,#23885,#23886,#23887,#23888,#23889,#23890,#23891,#23892,
#23893,#23894,#23895,#23896,#23897,#23898,#23899,#23900,#23901,#23902,#23903,
#23904,#23905,#23906,#23907,#23908,#23909,#23910,#23911,#23912,#23913,#23914,
#23915,#23916,#23917,#23918),.UNSPECIFIED.,.F.,.F.,(4,2,2,2,2,2,2,2,2,2,
2,2,2,2,2,2,2,2,2,2,2,2,2,2,2,2,2,2,2,2,2,2,2,2,2,2,2,2,2,2,2,2,2,2,2,2,
2,2,2,2,2,2,2,2,2,2,2,2,2,2,2,2,2,2,2,2,2,2,2,2,2,2,2,2,2,4),(1.36975430456593,
1.42172213103555,1.42835907822274,1.43231026028757,1.43534261990349,1.43859721798056,
1.44372951406029,1.46032157515104,1.48733375467083,1.56345959992786,1.58911797235801,
1.59323077093026,1.59534102870295,1.5970163230271,1.59898047451482,1.60253580486721,
1.62032079655486,1.69595908431547,1.74497514520024,1.75154764787522,1.75547693459096,
1.75850205496357,1.76175826077702,1.7669129693815,1.78375284916472,1.81134514278918,
1.88470936858748,1.91205219408331,1.91622378369688,1.9183453985704,1.92002128184319,
1.9219772152077,1.92548956202872,1.9424990451031,2.01876868011758,2.06797842187324,
2.07457334368562,2.07851187574343,2.08154172293333,2.0848006946761,2.08995491720612,
2.10675154389236,2.13423850540126,2.2080107693298,2.234962355599,2.23912474317568,
2.24124647941251,2.24292384677168,2.24488255613175,2.24840757550826,2.26562940368616,
2.3417535912804,2.39083775208834,2.39800956423947,2.40178339871772,2.40470300808647,
2.40798193156949,2.41142081405101,2.41651204772883,2.47970159142052,2.55460999112475,
2.56099596046146,2.56355977958516,2.56513277122848,2.56686638517147,2.56936480342705,
2.57581282132122,2.60920785722189,2.70538587515279,2.71843531316576,2.72327801529024,
2.72614870782649,2.72903657179424,2.73196675294122,2.73523955564581,2.73829514625514),
 .UNSPECIFIED.);
#238=B_SPLINE_CURVE_WITH_KNOTS('',3,(#23922,#23923,#23924,#23925,#23926,
#23927,#23928,#23929,#23930,#23931,#23932,#23933,#23934,#23935,#23936,#23937,
#23938,#23939,#23940,#23941,#23942,#23943,#23944,#23945,#23946,#23947,#23948,
#23949,#23950,#23951,#23952,#23953,#23954,#23955,#23956,#23957,#23958,#23959,
#23960,#23961,#23962,#23963,#23964,#23965,#23966,#23967,#23968,#23969,#23970,
#23971,#23972,#23973,#23974,#23975,#23976,#23977,#23978,#23979,#23980,#23981,
#23982,#23983,#23984,#23985,#23986,#23987,#23988,#23989,#23990,#23991,#23992,
#23993,#23994),.UNSPECIFIED.,.F.,.F.,(4,3,3,3,3,3,3,3,3,3,3,3,3,3,3,3,3,
3,3,3,3,3,3,3,4),(-4.09274904019422,-3.99978404940549,-3.91106269308813,
-3.8224565701686,-3.73394206808229,-3.64217906420377,-3.55376958798201,
-3.46537482046749,-3.37697356575947,-3.28854462858425,-3.20001846627961,
-3.11143447070011,-3.02272368784104,-2.99983803705412,-2.91202313233303,
-2.82432062379338,-2.73670592850525,-2.64915228090865,-2.56163015593267,
-2.47411747838494,-2.38659218514979,-2.29898035505946,-2.21132256779175,
-2.12353003259716,-2.06151489981891),.UNSPECIFIED.);
#239=B_SPLINE_CURVE_WITH_KNOTS('',3,(#23998,#23999,#24000,#24001,#24002),
 .UNSPECIFIED.,.F.,.F.,(4,1,4),(0.,0.99994601235136,1.11004521091143),
 .UNSPECIFIED.);
#240=B_SPLINE_CURVE_WITH_KNOTS('',3,(#24004,#24005,#24006,#24007,#24008,
#24009,#24010,#24011,#24012,#24013,#24014,#24015,#24016,#24017,#24018,#24019,
#24020,#24021,#24022,#24023,#24024,#24025,#24026,#24027,#24028,#24029,#24030,
#24031,#24032,#24033,#24034,#24035,#24036,#24037,#24038,#24039,#24040,#24041,
#24042,#24043,#24044,#24045,#24046,#24047,#24048,#24049,#24050,#24051,#24052,
#24053,#24054,#24055,#24056,#24057,#24058,#24059,#24060,#24061,#24062,#24063,
#24064,#24065,#24066,#24067,#24068,#24069,#24070,#24071,#24072,#24073,#24074,
#24075,#24076,#24077,#24078,#24079,#24080,#24081,#24082,#24083,#24084,#24085,
#24086,#24087,#24088,#24089,#24090,#24091,#24092,#24093,#24094,#24095,#24096,
#24097,#24098,#24099,#24100,#24101,#24102,#24103,#24104,#24105,#24106,#24107,
#24108,#24109,#24110,#24111,#24112,#24113,#24114,#24115,#24116,#24117,#24118,
#24119,#24120,#24121,#24122,#24123,#24124,#24125,#24126,#24127,#24128,#24129,
#24130,#24131,#24132,#24133,#24134,#24135,#24136,#24137,#24138,#24139,#24140,
#24141,#24142,#24143,#24144,#24145,#24146,#24147,#24148,#24149,#24150,#24151,
#24152,#24153,#24154,#24155,#24156,#24157,#24158,#24159,#24160,#24161,#24162,
#24163,#24164,#24165,#24166,#24167,#24168,#24169,#24170,#24171,#24172,#24173,
#24174,#24175,#24176,#24177,#24178,#24179,#24180,#24181,#24182,#24183,#24184,
#24185,#24186,#24187,#24188,#24189,#24190,#24191,#24192,#24193,#24194,#24195,
#24196,#24197,#24198,#24199,#24200,#24201,#24202,#24203,#24204,#24205,#24206,
#24207,#24208,#24209,#24210,#24211,#24212,#24213,#24214,#24215,#24216,#24217,
#24218,#24219,#24220,#24221,#24222,#24223,#24224,#24225,#24226,#24227,#24228,
#24229),.UNSPECIFIED.,.F.,.F.,(4,3,3,3,3,3,3,3,3,3,3,3,3,3,3,3,3,3,3,3,
3,3,3,3,3,3,3,3,3,3,3,3,3,3,3,3,3,3,3,3,3,3,3,3,3,3,3,3,3,3,3,3,3,3,3,3,
3,3,3,3,3,3,3,3,3,3,3,3,3,3,3,3,3,3,3,4),(1.11004521091143,1.19654798308244,
1.28294343992058,1.37256201301835,1.45882332647987,1.54506113767005,1.63129831945091,
1.71755774326959,1.80391109059945,1.89032034860343,1.97685772330168,1.99989202470273,
2.08856526631284,2.17712371506071,2.26559102252296,2.35737189933935,2.44573560240637,
2.53408518581266,2.62244188184438,2.71082692264793,2.79931035885651,2.88785225711593,
2.97652216123164,2.99983803705411,3.08854237714131,3.17713472538585,3.26563868098512,
3.35740685203767,3.44581388317613,3.53420920066809,3.62261399977723,3.7110494773624,
3.79958658197351,3.88818409875563,3.97691207014386,3.99978404940548,4.08821701236545,
4.1765337235679,4.26475813713124,4.35662962770944,4.4447491111496,4.53285440935254,
4.62096701909789,4.70910843742362,4.79735018389678,4.88565122025918,4.97408335872012,
4.99973006175686,5.08830339777262,5.17676200893295,5.26512967357959,5.35694797364567,
5.44521319848833,5.53346491396212,5.62172446584756,5.710013200411,5.79840208000763,
5.88685032811372,5.97542865050467,5.99967607410823,6.08824398278253,6.17669743939677,
6.26506022746791,6.35688045984187,6.44514154014848,6.53338938989229,6.62164536044511,
6.70993080388133,6.79831684303157,6.88676250976978,6.97533865408563,6.9996220864596,
7.09845393160949,7.19699737151629,7.29511382857198,7.39323028562766),
 .UNSPECIFIED.);
#241=B_SPLINE_CURVE_WITH_KNOTS('',3,(#24231,#24232,#24233,#24234,#24235,
#24236,#24237,#24238,#24239,#24240),.UNSPECIFIED.,.F.,.F.,(4,1,1,1,1,1,
1,4),(7.39323051809102,7.99956809881098,8.99951411116236,9.99946012351374,
10.9994061358651,11.9993521482165,12.9992981605679,13.6764158252706),
 .UNSPECIFIED.);
#242=B_SPLINE_CURVE_WITH_KNOTS('',3,(#24242,#24243,#24244,#24245,#24246,
#24247,#24248,#24249,#24250,#24251,#24252,#24253,#24254,#24255,#24256,#24257,
#24258,#24259,#24260,#24261,#24262,#24263,#24264,#24265,#24266,#24267,#24268,
#24269,#24270,#24271,#24272,#24273,#24274,#24275,#24276,#24277,#24278,#24279,
#24280,#24281,#24282,#24283,#24284,#24285,#24286,#24287,#24288,#24289,#24290,
#24291,#24292,#24293,#24294,#24295,#24296,#24297,#24298,#24299,#24300,#24301,
#24302,#24303,#24304,#24305,#24306,#24307,#24308,#24309,#24310,#24311,#24312,
#24313,#24314,#24315,#24316,#24317,#24318,#24319,#24320,#24321,#24322,#24323,
#24324,#24325,#24326,#24327,#24328,#24329,#24330,#24331,#24332,#24333,#24334,
#24335,#24336,#24337,#24338,#24339,#24340,#24341,#24342,#24343,#24344,#24345,
#24346,#24347,#24348,#24349,#24350,#24351,#24352,#24353,#24354,#24355,#24356,
#24357,#24358,#24359,#24360,#24361,#24362,#24363,#24364,#24365,#24366,#24367,
#24368,#24369,#24370,#24371,#24372,#24373,#24374,#24375,#24376,#24377,#24378,
#24379,#24380,#24381,#24382,#24383,#24384,#24385,#24386,#24387,#24388,#24389,
#24390,#24391,#24392,#24393,#24394,#24395,#24396,#24397,#24398,#24399,#24400,
#24401,#24402,#24403,#24404,#24405,#24406,#24407,#24408,#24409,#24410,#24411,
#24412,#24413,#24414,#24415,#24416,#24417,#24418,#24419,#24420,#24421,#24422,
#24423,#24424,#24425,#24426,#24427,#24428,#24429,#24430,#24431,#24432,#24433,
#24434,#24435,#24436,#24437,#24438,#24439,#24440,#24441,#24442,#24443,#24444,
#24445,#24446,#24447,#24448,#24449,#24450,#24451,#24452,#24453,#24454,#24455,
#24456,#24457,#24458,#24459,#24460,#24461,#24462,#24463,#24464),
 .UNSPECIFIED.,.F.,.F.,(4,3,3,3,3,3,3,3,3,3,3,3,3,3,3,3,3,3,3,3,3,3,3,3,
3,3,3,3,3,3,3,3,3,3,3,3,3,3,3,3,3,3,3,3,3,3,3,3,3,3,3,3,3,3,3,3,3,3,3,3,
3,3,3,3,3,3,3,3,3,3,3,3,3,3,4),(13.6764160462236,13.7802779401167,13.8897610565179,
13.9992441729192,14.0877938450277,14.1762287121119,14.2645725817854,14.3563997822211,
14.4446412388262,14.5328692371514,14.6211051488017,14.7093703459499,14.7977359613827,
14.886161075732,14.9747166370169,14.9991901852706,15.0877397450242,15.1761744991284,
15.2645182553368,15.3563454981224,15.4445868407756,15.5328147251651,15.6210505230179,
15.7093156066296,15.7976811094917,15.8861061116931,15.9746615623273,15.999136197622,
16.0876856965531,16.1761203885788,16.264464081533,16.356291347588,16.4445326244357,
16.5327604421866,16.6209961726353,16.7092611881441,16.7976266222034,16.8860515551089,
16.974606936256,16.9990822099733,17.0876317737306,17.1760665314604,17.264410290913,
17.3562375323395,17.4444788772557,17.5327067635402,17.6209425629163,17.7092076476754,
17.7975731511168,17.8859981535672,17.9745536039599,17.9990282223247,18.0875777660888,
18.1760125036722,18.2643562428505,18.3561834918287,18.4444248162795,18.5326526820631,
18.6208884609244,18.7091535251768,18.7975190082276,18.8859439903297,18.9744994205947,
18.9989742346761,19.0869698722266,19.1748511299411,19.2626424314125,19.3503698897695,
19.4380636509169,19.5257456458262,19.6134377916244,19.7012172493001,19.7890401091154,
19.8770064336621,19.9596011323108),.UNSPECIFIED.);
#243=B_SPLINE_CURVE_WITH_KNOTS('',3,(#24466,#24467,#24468,#24469,#24470,
#24471,#24472,#24473,#24474,#24475,#24476,#24477,#24478,#24479,#24480,#24481,
#24482,#24483,#24484,#24485,#24486,#24487,#24488,#24489,#24490,#24491,#24492,
#24493,#24494,#24495,#24496,#24497,#24498,#24499,#24500,#24501,#24502,#24503,
#24504,#24505,#24506,#24507,#24508,#24509,#24510,#24511,#24512,#24513,#24514,
#24515,#24516,#24517,#24518,#24519,#24520,#24521,#24522,#24523,#24524,#24525,
#24526,#24527,#24528,#24529,#24530,#24531,#24532,#24533,#24534,#24535,#24536,
#24537,#24538,#24539,#24540,#24541,#24542,#24543,#24544,#24545,#24546,#24547,
#24548,#24549,#24550,#24551,#24552,#24553,#24554,#24555,#24556,#24557,#24558,
#24559,#24560,#24561,#24562,#24563,#24564,#24565,#24566,#24567,#24568,#24569,
#24570,#24571,#24572,#24573,#24574,#24575,#24576,#24577,#24578,#24579,#24580,
#24581,#24582,#24583,#24584,#24585,#24586,#24587,#24588,#24589,#24590,#24591,
#24592,#24593,#24594,#24595,#24596,#24597,#24598,#24599,#24600,#24601,#24602,
#24603,#24604,#24605,#24606,#24607,#24608,#24609,#24610,#24611,#24612,#24613,
#24614,#24615,#24616,#24617,#24618,#24619,#24620,#24621,#24622,#24623,#24624,
#24625,#24626,#24627,#24628,#24629,#24630,#24631,#24632,#24633,#24634,#24635,
#24636,#24637,#24638,#24639,#24640,#24641,#24642,#24643,#24644,#24645,#24646,
#24647,#24648,#24649,#24650,#24651,#24652,#24653,#24654,#24655,#24656,#24657,
#24658,#24659,#24660,#24661,#24662,#24663,#24664,#24665,#24666,#24667,#24668,
#24669,#24670,#24671,#24672,#24673,#24674,#24675,#24676,#24677,#24678,#24679,
#24680,#24681,#24682,#24683,#24684,#24685,#24686,#24687,#24688,#24689,#24690,
#24691,#24692,#24693,#24694),.UNSPECIFIED.,.F.,.F.,(4,3,3,3,3,3,3,3,3,3,
3,3,3,3,3,3,3,3,3,3,3,3,3,3,3,3,3,3,3,3,3,3,3,3,3,3,3,3,3,3,3,3,3,3,3,3,
3,3,3,3,3,3,3,3,3,3,3,3,3,3,3,3,3,3,3,3,3,3,3,3,3,3,3,3,3,3,4),(19.9596011324502,
19.9989202470274,20.0874697934524,20.1759045336718,20.2642482754581,20.3560755234482,
20.4443168504197,20.532544718687,20.6207804999927,20.7090455666468,20.7974110520236,
20.8858360364104,20.9743914688815,20.9988662593788,21.0874158024492,21.1758505392836,
21.2641942776585,21.3560215269175,21.4442628504338,21.5324907152358,21.6207264930694,
21.7089915562485,21.7973570381634,21.8857820190918,21.9743374481363,21.9988122717302,
22.0873618142379,22.175796550492,22.26414028827,22.3559675377465,22.4442088606275,
22.532436724781,22.6206725019536,22.7089375644599,22.7973030456876,22.8857280259196,
22.9742834542594,22.9987582840816,23.0873078278185,23.17574256532,23.2640863043619,
23.3559135533708,23.4441548775493,23.5323827430104,23.6206185214995,23.7088835853299,
23.7972490678861,23.8856740494509,23.9742294791195,23.9987042964329,24.0872538396301,
24.1756885765864,24.2640323150784,24.3558595642917,24.4441008879117,24.5323287528123,
24.6205645307393,24.7088295940064,24.7971950760008,24.8856200570039,24.9741754861153,
24.9986503087843,25.0871998519514,25.1756345888759,25.263978327334,25.3558055765592,
25.4440469001412,25.5322747650021,25.6205105428879,25.7087756061121,25.7971410880619,
25.8855660690191,25.9741214980832,25.9985963211357,26.1206913455188,26.2351355066195,
26.2427863699019),.UNSPECIFIED.);
#244=B_SPLINE_CURVE_WITH_KNOTS('',3,(#24696,#24697,#24698,#24699,#24700,
#24701,#24702,#24703,#24704,#24705),.UNSPECIFIED.,.F.,.F.,(4,1,1,1,1,1,
1,4),(26.2427864396298,26.998542333487,27.9984883458384,28.9984343581898,
29.9983803705412,30.9983263828926,31.9982723952439,32.5259717468094),
 .UNSPECIFIED.);
#245=B_SPLINE_CURVE_WITH_KNOTS('',3,(#24707,#24708,#24709,#24710,#24711,
#24712,#24713,#24714,#24715,#24716),.UNSPECIFIED.,.F.,.F.,(4,1,1,1,1,1,
1,4),(32.5259717468094,32.9982184075953,33.9981644199467,34.998110432298,
35.9980564446494,36.9980024570008,37.9979484693521,38.8091526513998),
 .UNSPECIFIED.);
#246=B_SPLINE_CURVE_WITH_KNOTS('',3,(#24718,#24719,#24720,#24721,#24722,
#24723,#24724,#24725,#24726,#24727,#24728,#24729,#24730,#24731,#24732,#24733,
#24734,#24735,#24736,#24737,#24738,#24739,#24740,#24741,#24742,#24743,#24744,
#24745,#24746,#24747,#24748,#24749,#24750,#24751,#24752,#24753,#24754,#24755,
#24756,#24757,#24758,#24759,#24760,#24761,#24762,#24763,#24764,#24765,#24766,
#24767,#24768,#24769,#24770,#24771,#24772,#24773,#24774,#24775,#24776,#24777,
#24778,#24779,#24780,#24781,#24782,#24783,#24784,#24785,#24786,#24787,#24788,
#24789,#24790,#24791,#24792,#24793,#24794,#24795,#24796,#24797,#24798,#24799,
#24800,#24801,#24802,#24803,#24804,#24805,#24806,#24807,#24808,#24809,#24810,
#24811,#24812,#24813,#24814,#24815,#24816,#24817,#24818,#24819,#24820,#24821,
#24822,#24823,#24824,#24825,#24826,#24827,#24828,#24829,#24830,#24831,#24832,
#24833,#24834,#24835,#24836,#24837,#24838,#24839,#24840,#24841,#24842,#24843,
#24844,#24845,#24846,#24847,#24848,#24849,#24850,#24851,#24852,#24853,#24854,
#24855,#24856,#24857,#24858,#24859,#24860,#24861,#24862,#24863,#24864,#24865,
#24866,#24867,#24868,#24869,#24870,#24871,#24872,#24873,#24874,#24875,#24876,
#24877,#24878,#24879,#24880,#24881,#24882,#24883,#24884,#24885,#24886,#24887,
#24888,#24889,#24890,#24891,#24892,#24893,#24894,#24895,#24896,#24897,#24898,
#24899,#24900,#24901,#24902,#24903,#24904,#24905,#24906,#24907,#24908,#24909,
#24910,#24911,#24912,#24913,#24914,#24915,#24916,#24917,#24918,#24919,#24920,
#24921,#24922,#24923,#24924,#24925,#24926,#24927,#24928,#24929,#24930,#24931,
#24932,#24933,#24934,#24935,#24936,#24937,#24938,#24939,#24940,#24941,#24942,
#24943),.UNSPECIFIED.,.F.,.F.,(4,3,3,3,3,3,3,3,3,3,3,3,3,3,3,3,3,3,3,3,
3,3,3,3,3,3,3,3,3,3,3,3,3,3,3,3,3,3,3,3,3,3,3,3,3,3,3,3,3,3,3,3,3,3,3,3,
3,3,3,3,3,3,3,3,3,3,3,3,3,3,3,3,3,3,3,4),(38.809157053989,38.9402318305317,
38.9978944817035,39.0864440249643,39.174878761984,39.2632225005392,39.3550497497287,
39.4432910734108,39.5315189383729,39.6197547163609,39.7080197796883,39.7963852617418,
39.8848102428031,39.9733656719714,39.9978404940549,40.0863900373156,40.1748247743353,
40.2631685128904,40.3549957620799,40.4432370857619,40.5314649507239,40.6197007287117,
40.7079657920391,40.7963312740924,40.8847562551537,40.9733116843219,40.9977865064063,
41.086336049667,41.1747707866867,41.2631145252418,41.3549417744313,41.4431830981132,
41.5314109630753,41.619646741063,41.7079118043903,41.7962772864437,41.8847022675049,
41.9732576966731,41.9977325187576,42.0862820620183,42.174716799038,42.2630605375931,
42.3548877867826,42.4431291104647,42.5313569754267,42.6195927534145,42.7078578167418,
42.7962232987952,42.8846482798565,42.9732037090247,42.997678531109,43.0862280743697,
43.1746628113895,43.2630065499446,43.3548337991341,43.4430751228161,43.5313029877781,
43.619538765766,43.7078038290934,43.7961693111468,43.8845942922081,43.9731497213763,
43.9976245434604,44.0861740867211,44.1746088237409,44.2629525622959,44.3547798114854,
44.4430211351675,44.5312490001295,44.6194847781173,44.7077498414445,44.7961153234978,
44.8845403045592,44.9730957337274,44.9975705558118,45.0923423611685),
 .UNSPECIFIED.);
#247=B_SPLINE_CURVE_WITH_KNOTS('',3,(#24945,#24946,#24947,#24948,#24949,
#24950,#24951,#24952,#24953,#24954),.UNSPECIFIED.,.F.,.F.,(4,1,1,1,1,1,
1,4),(45.0923512995181,45.9975165681631,46.9974625805145,47.9974085928659,
48.9973546052172,49.9973006175686,50.99724662992,51.3755200907042),
 .UNSPECIFIED.);
#248=B_SPLINE_CURVE_WITH_KNOTS('',3,(#24956,#24957,#24958,#24959,#24960,
#24961,#24962,#24963,#24964,#24965,#24966,#24967,#24968,#24969,#24970,#24971,
#24972,#24973,#24974,#24975,#24976,#24977,#24978,#24979,#24980,#24981,#24982,
#24983,#24984,#24985,#24986,#24987,#24988,#24989,#24990,#24991,#24992,#24993,
#24994,#24995,#24996,#24997,#24998,#24999,#25000,#25001,#25002,#25003,#25004,
#25005,#25006,#25007,#25008,#25009,#25010,#25011,#25012,#25013,#25014,#25015,
#25016,#25017,#25018,#25019,#25020,#25021,#25022,#25023,#25024,#25025,#25026,
#25027,#25028,#25029,#25030,#25031,#25032,#25033,#25034,#25035,#25036,#25037,
#25038,#25039,#25040,#25041,#25042,#25043,#25044,#25045,#25046,#25047,#25048,
#25049,#25050,#25051,#25052,#25053,#25054,#25055,#25056,#25057,#25058,#25059,
#25060,#25061,#25062,#25063,#25064,#25065,#25066,#25067,#25068,#25069,#25070,
#25071,#25072,#25073,#25074,#25075,#25076,#25077,#25078,#25079,#25080,#25081,
#25082,#25083,#25084,#25085,#25086,#25087,#25088,#25089,#25090,#25091,#25092,
#25093,#25094,#25095,#25096,#25097,#25098,#25099,#25100,#25101,#25102,#25103,
#25104,#25105,#25106,#25107,#25108,#25109,#25110,#25111,#25112,#25113,#25114,
#25115,#25116,#25117,#25118,#25119,#25120,#25121,#25122,#25123,#25124,#25125,
#25126,#25127,#25128,#25129,#25130,#25131,#25132,#25133,#25134,#25135,#25136,
#25137,#25138,#25139,#25140,#25141,#25142,#25143,#25144,#25145,#25146,#25147,
#25148,#25149,#25150,#25151,#25152,#25153,#25154,#25155,#25156,#25157,#25158,
#25159,#25160,#25161,#25162,#25163,#25164,#25165,#25166,#25167,#25168,#25169,
#25170,#25171,#25172,#25173,#25174,#25175,#25176,#25177,#25178,#25179,#25180,
#25181),.UNSPECIFIED.,.F.,.F.,(4,3,3,3,3,3,3,3,3,3,3,3,3,3,3,3,3,3,3,3,
3,3,3,3,3,3,3,3,3,3,3,3,3,3,3,3,3,3,3,3,3,3,3,3,3,3,3,3,3,3,3,3,3,3,3,3,
3,3,3,3,3,3,3,3,3,3,3,3,3,3,3,3,3,3,3,4),(51.3755276683481,51.4644854095652,
51.5534539425206,51.642453477088,51.731568782179,51.8207424676004,51.9100816636312,
51.9971926422714,52.0857421855321,52.1741769225517,52.2625206611069,52.3543479102964,
52.4425892339784,52.5308170989404,52.6190528769282,52.7073179402553,52.7956834223086,
52.8841084033699,52.972663832538,52.9971386546227,53.0856881978835,53.1741229349033,
53.2624666734584,53.3542939226479,53.4425352463299,53.530763111292,53.6189988892798,
53.7072639526072,53.7956294346605,53.8840544157218,53.9726098448899,53.9970846669741,
54.0856342102349,54.1740689472545,54.2624126858097,54.3542399349992,54.4424812586813,
54.5307091236433,54.618944901631,54.7072099649584,54.7955754470118,54.8840004280729,
54.9725558572412,54.9970306793255,55.0855802225862,55.1740149596059,55.2623586981611,
55.3541859473506,55.4424272710327,55.5306551359947,55.6188909139824,55.7071559773094,
55.7955214593627,55.8839464404242,55.9725018695924,55.9969766916768,56.0855262349375,
56.1739609719573,56.2623047105123,56.3541319597018,56.442373283384,56.5306011483461,
56.6188369263337,56.7071019896608,56.7954674717142,56.8838924527754,56.9724478819438,
56.9969227040282,57.0854947724333,57.1739540959007,57.26232214872,57.3506203291089,
57.4388747032672,57.5271032295614,57.6153453697455,57.6587129755277),
 .UNSPECIFIED.);
#249=B_SPLINE_CURVE_WITH_KNOTS('',3,(#25183,#25184,#25185,#25186,#25187,
#25188,#25189,#25190,#25191,#25192,#25193,#25194,#25195,#25196,#25197,#25198,
#25199,#25200,#25201,#25202,#25203,#25204,#25205,#25206,#25207,#25208,#25209,
#25210,#25211,#25212,#25213,#25214,#25215,#25216,#25217,#25218,#25219,#25220,
#25221,#25222,#25223,#25224,#25225,#25226,#25227,#25228,#25229,#25230,#25231,
#25232,#25233,#25234,#25235,#25236,#25237,#25238,#25239,#25240,#25241,#25242,
#25243,#25244,#25245,#25246,#25247,#25248,#25249,#25250,#25251,#25252,#25253,
#25254,#25255,#25256,#25257,#25258,#25259,#25260,#25261,#25262,#25263,#25264,
#25265,#25266,#25267,#25268,#25269,#25270,#25271,#25272,#25273,#25274,#25275,
#25276,#25277,#25278,#25279,#25280,#25281,#25282,#25283,#25284,#25285,#25286,
#25287,#25288,#25289,#25290,#25291,#25292,#25293,#25294,#25295,#25296,#25297,
#25298,#25299,#25300,#25301,#25302,#25303,#25304,#25305,#25306,#25307,#25308,
#25309,#25310,#25311,#25312,#25313,#25314,#25315,#25316,#25317,#25318,#25319,
#25320,#25321,#25322,#25323,#25324,#25325,#25326,#25327,#25328,#25329,#25330,
#25331,#25332,#25333,#25334,#25335,#25336,#25337,#25338,#25339,#25340,#25341,
#25342,#25343,#25344,#25345,#25346,#25347,#25348,#25349,#25350,#25351,#25352,
#25353,#25354,#25355,#25356,#25357,#25358,#25359,#25360,#25361,#25362,#25363,
#25364,#25365,#25366,#25367,#25368,#25369,#25370,#25371,#25372,#25373,#25374,
#25375,#25376,#25377,#25378,#25379,#25380,#25381,#25382,#25383,#25384,#25385,
#25386,#25387,#25388,#25389,#25390,#25391,#25392,#25393,#25394,#25395,#25396,
#25397,#25398,#25399,#25400,#25401,#25402,#25403,#25404,#25405,#25406,#25407,
#25408),.UNSPECIFIED.,.F.,.F.,(4,3,3,3,3,3,3,3,3,3,3,3,3,3,3,3,3,3,3,3,
3,3,3,3,3,3,3,3,3,3,3,3,3,3,3,3,3,3,3,3,3,3,3,3,3,3,3,3,3,3,3,3,3,3,3,3,
3,3,3,3,3,3,3,3,3,3,3,3,3,3,3,3,3,3,3,4),(57.6587129757527,57.7611008096764,
57.8640988984394,57.9677937989378,57.9968687163796,58.0854182596404,58.17385299666,
58.2621967352151,58.3540239844046,58.4422653080866,58.5304931730487,58.6187289510364,
58.7069940143638,58.7953594964171,58.8837844774784,58.9723399066465,58.996814728731,
59.0853642719917,59.1737990090114,59.2621427475665,59.3539699967559,59.442211320438,
59.5304391854,59.6186749633878,59.7069400267152,59.7953055087685,59.8837304898298,
59.972285918998,59.9967607410823,60.085310284343,60.1737450213627,60.2620887599178,
60.3539160091073,60.4421573327893,60.5303851977514,60.6186209757392,60.7068860390665,
60.7952515211198,60.8836765021811,60.9722319313493,60.9967067534337,61.0852562966945,
61.1736910337142,61.2620347722692,61.3538620214587,61.4421033451408,61.5303312101028,
61.6185669880906,61.706832051418,61.7951975334714,61.8836225145326,61.9721779437008,
61.9966527657851,62.0852023090459,62.1736370460656,62.2619807846206,62.3538080338101,
62.4420493574922,62.5302772224542,62.618513000442,62.7067780637692,62.7951435458225,
62.8835685268838,62.972123956052,62.9965987781365,63.0844206635694,63.1721283405569,
63.2597464032859,63.3473010237067,63.4348225101216,63.5223329419007,63.6098543850565,
63.6974616170165,63.7851133634083,63.8729020343142,63.9418982827073),
 .UNSPECIFIED.);
#250=B_SPLINE_CURVE_WITH_KNOTS('',3,(#25410,#25411,#25412,#25413,#25414,
#25415,#25416,#25417,#25418,#25419,#25420),.UNSPECIFIED.,.F.,.F.,(4,1,1,
1,1,1,1,1,4),(63.9418982827073,63.9965447904879,64.9964908028392,65.9964368151906,
66.996382827542,67.9963288398934,68.9962748522447,69.9962208645961,70.2250835898869),
 .UNSPECIFIED.);
#251=B_SPLINE_CURVE_WITH_KNOTS('',3,(#25422,#25423,#25424,#25425,#25426,
#25427,#25428,#25429,#25430,#25431,#25432,#25433,#25434,#25435,#25436,#25437,
#25438,#25439,#25440,#25441,#25442,#25443,#25444,#25445,#25446,#25447,#25448,
#25449,#25450,#25451,#25452,#25453,#25454,#25455,#25456,#25457,#25458,#25459,
#25460,#25461,#25462,#25463,#25464,#25465,#25466,#25467,#25468,#25469,#25470,
#25471,#25472,#25473,#25474,#25475,#25476,#25477,#25478,#25479,#25480,#25481,
#25482,#25483,#25484,#25485,#25486,#25487,#25488,#25489,#25490,#25491,#25492,
#25493,#25494,#25495,#25496,#25497,#25498,#25499,#25500,#25501,#25502,#25503,
#25504,#25505,#25506,#25507,#25508,#25509,#25510,#25511,#25512,#25513,#25514,
#25515,#25516,#25517,#25518,#25519,#25520,#25521,#25522,#25523,#25524,#25525,
#25526,#25527,#25528,#25529,#25530,#25531,#25532,#25533,#25534,#25535,#25536,
#25537,#25538,#25539,#25540,#25541,#25542,#25543,#25544,#25545,#25546,#25547,
#25548,#25549,#25550,#25551,#25552,#25553,#25554,#25555,#25556,#25557,#25558,
#25559,#25560,#25561,#25562,#25563,#25564,#25565,#25566,#25567,#25568,#25569,
#25570,#25571,#25572,#25573,#25574,#25575,#25576,#25577,#25578,#25579,#25580,
#25581,#25582,#25583,#25584,#25585,#25586,#25587,#25588,#25589,#25590,#25591,
#25592,#25593,#25594,#25595,#25596,#25597,#25598,#25599,#25600,#25601,#25602,
#25603,#25604,#25605,#25606,#25607,#25608,#25609,#25610,#25611,#25612,#25613,
#25614,#25615,#25616,#25617,#25618,#25619,#25620,#25621,#25622,#25623,#25624,
#25625,#25626,#25627,#25628,#25629,#25630,#25631,#25632,#25633,#25634,#25635,
#25636,#25637,#25638,#25639,#25640,#25641,#25642,#25643,#25644,#25645,#25646,
#25647),.UNSPECIFIED.,.F.,.F.,(4,3,3,3,3,3,3,3,3,3,3,3,3,3,3,3,3,3,3,3,
3,3,3,3,3,3,3,3,3,3,3,3,3,3,3,3,3,3,3,3,3,3,3,3,3,3,3,3,3,3,3,3,3,3,3,3,
3,3,3,3,3,3,3,3,3,3,3,3,3,3,3,3,3,3,3,4),(70.2250835898869,70.31227753055,
70.3994065089422,70.4865013955672,70.5735846005634,70.6606785201825,70.7478600908778,
70.8350863988569,70.9224543524563,70.9961668769474,71.0847164202081,71.1731511572278,
71.2614948957828,71.3533221449723,71.4415634686544,71.5297913336164,71.6180271116043,
71.7062921749316,71.794657656985,71.8830826380461,71.9716380672144,71.9961128892988,
72.0846624325596,72.1730971695793,72.2614409081343,72.3532681573238,72.441509481006,
72.529737345968,72.6179731239558,72.7062381872829,72.7946036693362,72.8830286503972,
72.9715840795655,72.9960589016502,73.0846084449109,73.1730431819306,73.2613869204854,
73.3532141696749,73.4414554933569,73.5296833583189,73.6179191363067,73.7061841996341,
73.7945496816876,73.8829746627492,73.9715300919174,73.9960049140016,74.0845544572622,
74.1729891942819,74.2613329328369,74.3531601820264,74.4414015057085,74.5296293706705,
74.617865148658,74.7061302119854,74.7944956940387,74.8829206751001,74.9714761042681,
74.9959509263529,75.0845004696136,75.1729352066333,75.2612789451884,75.3531061943779,
75.44134751806,75.5295753830218,75.6178111610097,75.7060762243367,75.7944417063901,
75.8828666874513,75.9714221166195,75.9958969387043,76.0885121594138,76.1809656964412,
76.2732153511774,76.3653433520313,76.4573224600646,76.5082688970665),
 .UNSPECIFIED.);
#252=B_SPLINE_CURVE_WITH_KNOTS('',3,(#25649,#25650,#25651,#25652,#25653,
#25654,#25655,#25656,#25657,#25658,#25659,#25660,#25661,#25662,#25663,#25664,
#25665,#25666,#25667,#25668,#25669,#25670,#25671,#25672,#25673,#25674,#25675,
#25676,#25677,#25678,#25679,#25680,#25681,#25682,#25683,#25684,#25685,#25686,
#25687,#25688,#25689,#25690,#25691,#25692,#25693,#25694,#25695,#25696,#25697,
#25698,#25699,#25700,#25701,#25702,#25703,#25704,#25705,#25706,#25707,#25708,
#25709,#25710,#25711,#25712,#25713,#25714,#25715,#25716,#25717,#25718,#25719,
#25720,#25721,#25722,#25723,#25724,#25725,#25726,#25727,#25728,#25729,#25730,
#25731,#25732,#25733,#25734,#25735,#25736,#25737,#25738,#25739,#25740,#25741,
#25742,#25743,#25744,#25745,#25746,#25747,#25748,#25749,#25750,#25751,#25752,
#25753,#25754,#25755,#25756,#25757,#25758,#25759,#25760,#25761,#25762,#25763,
#25764,#25765,#25766,#25767,#25768,#25769,#25770,#25771,#25772,#25773,#25774,
#25775,#25776,#25777,#25778,#25779,#25780,#25781,#25782,#25783,#25784,#25785,
#25786,#25787,#25788,#25789,#25790,#25791,#25792,#25793,#25794,#25795,#25796,
#25797,#25798,#25799,#25800,#25801,#25802,#25803,#25804,#25805,#25806,#25807,
#25808,#25809,#25810,#25811,#25812,#25813,#25814,#25815,#25816,#25817,#25818,
#25819,#25820,#25821,#25822,#25823,#25824,#25825,#25826,#25827,#25828,#25829,
#25830,#25831,#25832,#25833,#25834,#25835,#25836,#25837,#25838,#25839,#25840,
#25841,#25842,#25843,#25844,#25845,#25846,#25847,#25848,#25849,#25850,#25851,
#25852,#25853,#25854,#25855,#25856,#25857,#25858,#25859,#25860,#25861,#25862,
#25863,#25864,#25865,#25866,#25867,#25868,#25869,#25870,#25871,#25872,#25873,
#25874),.UNSPECIFIED.,.F.,.F.,(4,3,3,3,3,3,3,3,3,3,3,3,3,3,3,3,3,3,3,3,
3,3,3,3,3,3,3,3,3,3,3,3,3,3,3,3,3,3,3,3,3,3,3,3,3,3,3,3,3,3,3,3,3,3,3,3,
3,3,3,3,3,3,3,3,3,3,3,3,3,3,3,3,3,3,3,4),(76.5082688972016,76.6011857099923,
76.6942510627784,76.7875594403697,76.8810035839464,76.9746605070459,76.9958429510557,
77.0843924943164,77.1728272313361,77.2611709698913,77.3529982190808,77.4412395427628,
77.5294674077249,77.6177031857127,77.70596824904,77.7943337310934,77.8827587121547,
77.9713141413228,77.9957889634071,78.0843385066678,78.1727732436875,78.2611169822426,
78.3529442314321,78.4411855551141,78.5294134200761,78.6176491980639,78.7059142613912,
78.7942797434445,78.8827047245058,78.9712601536739,78.9957349757584,79.0842845190191,
79.1727192560388,79.2610629945939,79.3528902437834,79.4411315674654,79.5293594324275,
79.6175952104153,79.7058602737426,79.794225755796,79.8826507368573,79.9712061660255,
79.9956809881098,80.0842305313706,80.1726652683903,80.2610090069454,80.3528362561349,
80.4410775798169,80.529305444779,80.6175412227668,80.7058062860941,80.7941717681475,
80.8825967492088,80.971152178377,80.9956270004612,81.0841765437219,81.1726112807416,
81.2609550192967,81.3527822684862,81.4410235921682,81.5292514571302,81.6174872351179,
81.7057522984453,81.7941177804986,81.8825427615599,81.9710981907281,81.9955730128125,
82.0828584263191,82.1714328985413,82.2585004412254,82.3455122336891,82.4324907952618,
82.5222316474705,82.6092419427961,82.7003480734463,82.7914542040965),
 .UNSPECIFIED.);
#253=B_SPLINE_CURVE_WITH_KNOTS('',3,(#25876,#25877,#25878,#25879,#25880,
#25881,#25882,#25883,#25884,#25885,#25886,#25887,#25888,#25889,#25890,#25891,
#25892,#25893,#25894,#25895,#25896,#25897,#25898,#25899,#25900,#25901,#25902,
#25903,#25904,#25905,#25906,#25907,#25908,#25909,#25910,#25911,#25912,#25913,
#25914,#25915,#25916,#25917,#25918,#25919,#25920,#25921,#25922,#25923,#25924,
#25925,#25926,#25927,#25928,#25929,#25930,#25931,#25932,#25933,#25934,#25935,
#25936,#25937,#25938,#25939,#25940,#25941,#25942,#25943,#25944,#25945,#25946,
#25947,#25948,#25949,#25950,#25951,#25952,#25953,#25954,#25955,#25956,#25957,
#25958,#25959,#25960,#25961,#25962,#25963,#25964,#25965,#25966,#25967,#25968,
#25969,#25970,#25971,#25972,#25973,#25974,#25975,#25976,#25977,#25978,#25979,
#25980,#25981,#25982,#25983,#25984,#25985,#25986,#25987,#25988,#25989,#25990,
#25991,#25992,#25993,#25994,#25995,#25996,#25997,#25998,#25999,#26000,#26001,
#26002,#26003,#26004,#26005,#26006,#26007,#26008,#26009,#26010,#26011,#26012,
#26013,#26014,#26015,#26016,#26017,#26018,#26019,#26020,#26021,#26022,#26023,
#26024,#26025,#26026,#26027,#26028,#26029,#26030,#26031,#26032,#26033,#26034,
#26035,#26036,#26037,#26038,#26039,#26040,#26041,#26042,#26043,#26044,#26045,
#26046,#26047,#26048,#26049,#26050,#26051,#26052,#26053,#26054,#26055,#26056,
#26057,#26058,#26059,#26060,#26061,#26062,#26063,#26064,#26065,#26066,#26067,
#26068,#26069,#26070,#26071,#26072,#26073,#26074,#26075,#26076,#26077,#26078,
#26079,#26080,#26081,#26082,#26083,#26084,#26085,#26086,#26087,#26088,#26089,
#26090,#26091,#26092,#26093,#26094,#26095,#26096,#26097,#26098,#26099,#26100,
#26101),.UNSPECIFIED.,.F.,.F.,(4,3,3,3,3,3,3,3,3,3,3,3,3,3,3,3,3,3,3,3,
3,3,3,3,3,3,3,3,3,3,3,3,3,3,3,3,3,3,3,3,3,3,3,3,3,3,3,3,3,3,3,3,3,3,3,3,
3,3,3,3,3,3,3,3,3,3,3,3,3,3,3,3,3,3,3,4),(82.7914542042461,82.9173221738109,
82.9955190251639,83.0840685684247,83.1725033054443,83.2608470439993,83.3526742931888,
83.4409156168709,83.529143481833,83.6173792598209,83.7056443231483,83.7940098052017,
83.882434786263,83.9709902154312,83.9954650375153,84.084014580776,84.1724493177957,
84.2607930563507,84.3526203055402,84.4408616292222,84.5290894941842,84.617325272172,
84.7055903354994,84.7939558175527,84.8823807986139,84.9709362277821,84.9954110498666,
85.0839605931273,85.172395330147,85.2607390687021,85.3525663178916,85.4408076415736,
85.5290355065357,85.6172712845235,85.7055363478508,85.7939018299042,85.8823268109655,
85.9708822401336,85.995357062218,86.0839066054788,86.1723413424985,86.2606850810536,
86.352512330243,86.4407536539251,86.5289815188871,86.617217296875,86.7054823602023,
86.7938478422556,86.8822728233169,86.9708282524851,86.9953030745694,87.0838526178302,
87.1722873548499,87.260631093405,87.3524583425945,87.4406996662765,87.5289275312386,
87.6171633092263,87.7054283725537,87.793793854607,87.8822188356683,87.9707742648366,
87.9952490869208,88.0837986301816,88.1722333672013,88.2605771057564,88.3524043549458,
88.4406456786279,88.5288735435899,88.6171093215776,88.7053743849048,88.7937398669581,
88.8821648480194,88.9707202771877,88.9951950992722,89.0746395114257),
 .UNSPECIFIED.);
#254=B_SPLINE_CURVE_WITH_KNOTS('',3,(#26103,#26104,#26105,#26106,#26107,
#26108,#26109,#26110,#26111,#26112),.UNSPECIFIED.,.F.,.F.,(4,1,1,1,1,1,
1,4),(89.0746480063059,89.9951411116235,90.9950871239749,91.9950331363263,
92.9949791486776,93.994925161029,94.9948711733804,95.3578171110057),
 .UNSPECIFIED.);
#255=B_SPLINE_CURVE_WITH_KNOTS('',3,(#26114,#26115,#26116,#26117,#26118,
#26119,#26120,#26121,#26122,#26123,#26124,#26125,#26126,#26127,#26128,#26129,
#26130,#26131,#26132,#26133,#26134,#26135,#26136,#26137,#26138,#26139,#26140,
#26141,#26142,#26143,#26144,#26145,#26146,#26147,#26148,#26149,#26150,#26151,
#26152,#26153,#26154,#26155,#26156,#26157,#26158,#26159,#26160,#26161,#26162,
#26163,#26164,#26165,#26166,#26167,#26168,#26169,#26170,#26171,#26172,#26173,
#26174,#26175,#26176,#26177,#26178,#26179,#26180,#26181,#26182,#26183,#26184,
#26185,#26186,#26187,#26188,#26189,#26190,#26191,#26192,#26193,#26194,#26195,
#26196,#26197,#26198,#26199,#26200,#26201,#26202,#26203,#26204,#26205,#26206,
#26207,#26208,#26209,#26210,#26211,#26212,#26213,#26214,#26215,#26216,#26217,
#26218,#26219,#26220,#26221,#26222,#26223,#26224,#26225,#26226,#26227,#26228,
#26229,#26230,#26231,#26232,#26233,#26234,#26235,#26236,#26237,#26238,#26239,
#26240,#26241,#26242,#26243,#26244,#26245,#26246,#26247,#26248,#26249,#26250,
#26251,#26252,#26253,#26254,#26255,#26256,#26257,#26258,#26259,#26260,#26261,
#26262,#26263,#26264,#26265,#26266,#26267,#26268,#26269,#26270,#26271,#26272,
#26273,#26274,#26275,#26276,#26277,#26278,#26279,#26280,#26281,#26282,#26283,
#26284,#26285,#26286,#26287,#26288,#26289,#26290,#26291,#26292,#26293,#26294,
#26295,#26296,#26297,#26298,#26299,#26300,#26301,#26302,#26303,#26304,#26305,
#26306,#26307,#26308,#26309,#26310,#26311,#26312,#26313,#26314,#26315,#26316,
#26317,#26318,#26319,#26320,#26321,#26322,#26323,#26324,#26325,#26326,#26327,
#26328,#26329,#26330,#26331,#26332,#26333,#26334,#26335,#26336,#26337,#26338,
#26339,#26340,#26341,#26342),.UNSPECIFIED.,.F.,.F.,(4,3,3,3,3,3,3,3,3,3,
3,3,3,3,3,3,3,3,3,3,3,3,3,3,3,3,3,3,3,3,3,3,3,3,3,3,3,3,3,3,3,3,3,3,3,3,
3,3,3,3,3,3,3,3,3,3,3,3,3,3,3,3,3,3,3,3,3,3,3,3,3,3,3,3,3,3,4),(95.3578248186053,
95.4464898257287,95.5351563461466,95.6238450600736,95.7165880914881,95.80543883478,
95.8943605288811,95.9834198358781,95.9948171857317,96.0833667289924,96.1718014660123,
96.2601452045674,96.3519724537569,96.4402137774389,96.528441642401,96.6166774203887,
96.7049424837157,96.793307965769,96.8817329468303,96.9702883759985,96.9947631980831,
97.0833127413439,97.1717474783636,97.2600912169187,97.3519184661082,97.4401597897902,
97.5283876547524,97.6166234327403,97.7048884960678,97.7932539781212,97.8816789591828,
97.970234388351,97.9947092104345,98.0832587536953,98.1716934907152,98.2600372292703,
98.3518644784597,98.4401058021418,98.5283336671038,98.6165694450914,98.7048345084186,
98.793199990472,98.8816249715333,98.9701804007016,98.9946552227859,99.0832047660465,
99.1716395030662,99.2599832416215,99.3518104908109,99.4400518144929,99.5282796794549,
99.6165154574425,99.7047805207696,99.793146002823,99.8815709838841,99.9701264130522,
99.9946012351372,100.083150778398,100.171585515418,100.259929253973,100.351756503162,
100.439997826844,100.528225691807,100.616461469795,100.704726533122,100.793092015175,
100.881516996236,100.970072425405,100.994547247489,101.083392821799,101.172123155493,
101.260759394379,101.349322607109,101.437835030598,101.526318499633,101.614805634129,
101.641010125785),.UNSPECIFIED.);
#256=B_SPLINE_CURVE_WITH_KNOTS('',3,(#26344,#26345,#26346,#26347,#26348,
#26349,#26350,#26351,#26352,#26353,#26354,#26355,#26356,#26357,#26358,#26359,
#26360,#26361,#26362,#26363,#26364,#26365,#26366,#26367,#26368,#26369,#26370,
#26371,#26372,#26373,#26374,#26375,#26376,#26377,#26378,#26379,#26380,#26381,
#26382,#26383,#26384,#26385,#26386,#26387,#26388,#26389,#26390,#26391,#26392,
#26393,#26394,#26395,#26396,#26397,#26398,#26399,#26400,#26401,#26402,#26403,
#26404,#26405,#26406,#26407,#26408,#26409,#26410,#26411,#26412,#26413,#26414,
#26415,#26416,#26417,#26418,#26419,#26420,#26421,#26422,#26423,#26424,#26425,
#26426,#26427,#26428,#26429,#26430,#26431,#26432,#26433,#26434,#26435,#26436,
#26437,#26438,#26439,#26440,#26441,#26442,#26443,#26444,#26445,#26446,#26447,
#26448,#26449,#26450,#26451,#26452,#26453,#26454,#26455,#26456,#26457,#26458,
#26459,#26460,#26461,#26462,#26463,#26464,#26465,#26466,#26467,#26468,#26469,
#26470,#26471,#26472,#26473,#26474,#26475,#26476,#26477,#26478,#26479,#26480,
#26481,#26482,#26483,#26484,#26485,#26486,#26487,#26488,#26489,#26490,#26491,
#26492,#26493,#26494,#26495,#26496,#26497,#26498,#26499,#26500,#26501,#26502,
#26503,#26504,#26505,#26506,#26507,#26508,#26509,#26510,#26511,#26512,#26513,
#26514,#26515,#26516,#26517,#26518,#26519,#26520,#26521,#26522,#26523,#26524,
#26525,#26526,#26527,#26528,#26529,#26530,#26531,#26532,#26533,#26534,#26535,
#26536,#26537,#26538,#26539,#26540,#26541,#26542,#26543,#26544,#26545,#26546,
#26547,#26548,#26549,#26550,#26551,#26552,#26553,#26554,#26555,#26556,#26557,
#26558,#26559,#26560,#26561,#26562,#26563,#26564,#26565,#26566,#26567,#26568,
#26569),.UNSPECIFIED.,.F.,.F.,(4,3,3,3,3,3,3,3,3,3,3,3,3,3,3,3,3,3,3,3,
3,3,3,3,3,3,3,3,3,3,3,3,3,3,3,3,3,3,3,3,3,3,3,3,3,3,3,3,3,3,3,3,3,3,3,3,
3,3,3,3,3,3,3,3,3,3,3,3,3,3,3,3,3,3,3,4),(101.641010126018,101.742054504281,
101.843610345288,101.945794784302,101.99449325984,102.083042803101,102.17147754012,
102.259821278675,102.351648527865,102.439889851546,102.528117716508,102.616353494496,
102.704618557823,102.792984039877,102.881409020938,102.969964450106,102.994439272191,
103.082988815452,103.171423552472,103.259767291027,103.351594540217,103.439835863899,
103.528063728861,103.616299506849,103.704564570177,103.79293005223,103.881355033292,
103.96991046246,103.994385284543,104.082934827804,104.171369564823,104.259713303379,
104.351540552568,104.43978187625,104.528009741212,104.6162455192,104.704510582527,
104.792876064581,104.881301045642,104.96985647481,104.994331296894,105.082880840154,
105.171315577174,105.259659315729,105.351486564918,105.4397278886,105.527955753562,
105.616191531549,105.704456594876,105.79282207693,105.881247057991,105.969802487158,
105.994277309245,106.082826852506,106.171261589526,106.259605328081,106.351432577271,
106.439673900953,106.527901765915,106.616137543904,106.704402607231,106.792768089285,
106.881193070346,106.969748499515,106.994223321597,107.081894309482,107.169451242158,
107.256918854214,107.344323253543,107.43169496891,107.519056200791,107.606429136683,
107.693885954662,107.781388212332,107.869020538835,107.924195432964),
 .UNSPECIFIED.);
#257=B_SPLINE_CURVE_WITH_KNOTS('',3,(#26571,#26572,#26573,#26574,#26575,
#26576,#26577,#26578,#26579,#26580,#26581),.UNSPECIFIED.,.F.,.F.,(4,1,1,
1,1,1,1,1,4),(107.924195432964,107.994169333948,108.9941153463,109.994061358651,
110.994007371002,111.993953383354,112.993899395705,113.993845408056,114.207380740144),
 .UNSPECIFIED.);
#258=B_SPLINE_CURVE_WITH_KNOTS('',3,(#26583,#26584,#26585,#26586,#26587,
#26588,#26589,#26590,#26591,#26592),.UNSPECIFIED.,.F.,.F.,(4,1,1,1,1,1,
1,4),(114.207380740144,114.993791420408,115.993737432759,116.993683445111,
117.993629457462,118.993575469813,119.993521482165,120.490566047324),
 .UNSPECIFIED.);
#259=B_SPLINE_CURVE_WITH_KNOTS('',3,(#26594,#26595,#26596,#26597,#26598,
#26599,#26600,#26601,#26602,#26603),.UNSPECIFIED.,.F.,.F.,(4,1,1,1,1,1,
1,4),(120.490566047324,120.993467494516,121.993413506867,122.993359519219,
123.99330553157,124.993251543922,125.993197556273,126.773751354503),
 .UNSPECIFIED.);
#260=B_SPLINE_CURVE_WITH_KNOTS('',3,(#26605,#26606,#26607,#26608,#26609,
#26610,#26611,#26612,#26613,#26614,#26615),.UNSPECIFIED.,.F.,.F.,(4,1,1,
1,1,1,1,1,4),(126.773751354503,126.993143568624,127.993089580976,128.993035593327,
129.992981605678,130.99292761803,131.992873630381,132.992819642733,133.056936661683),
 .UNSPECIFIED.);
#261=B_SPLINE_CURVE_WITH_KNOTS('',3,(#26617,#26618,#26619,#26620,#26621,
#26622,#26623,#26624,#26625,#26626,#26627,#26628,#26629,#26630,#26631,#26632,
#26633,#26634,#26635,#26636,#26637,#26638,#26639,#26640,#26641,#26642,#26643,
#26644,#26645,#26646,#26647,#26648,#26649,#26650,#26651,#26652,#26653,#26654,
#26655,#26656,#26657,#26658,#26659,#26660,#26661,#26662,#26663,#26664,#26665,
#26666,#26667,#26668,#26669,#26670,#26671,#26672,#26673,#26674,#26675,#26676,
#26677,#26678,#26679,#26680,#26681,#26682,#26683,#26684,#26685,#26686,#26687,
#26688,#26689,#26690,#26691,#26692,#26693,#26694,#26695,#26696,#26697,#26698,
#26699,#26700,#26701,#26702,#26703,#26704,#26705,#26706,#26707,#26708,#26709,
#26710,#26711,#26712,#26713,#26714,#26715,#26716,#26717,#26718,#26719,#26720,
#26721,#26722,#26723,#26724,#26725,#26726,#26727,#26728,#26729,#26730,#26731,
#26732,#26733,#26734,#26735,#26736,#26737,#26738,#26739,#26740,#26741,#26742,
#26743,#26744,#26745,#26746,#26747,#26748,#26749,#26750,#26751,#26752,#26753,
#26754,#26755,#26756,#26757,#26758,#26759,#26760,#26761,#26762,#26763,#26764,
#26765,#26766,#26767,#26768,#26769,#26770,#26771,#26772,#26773,#26774,#26775,
#26776,#26777,#26778,#26779,#26780,#26781,#26782,#26783,#26784,#26785,#26786,
#26787,#26788,#26789,#26790,#26791,#26792,#26793,#26794,#26795,#26796,#26797,
#26798,#26799,#26800,#26801,#26802,#26803,#26804,#26805,#26806,#26807,#26808,
#26809,#26810,#26811,#26812,#26813,#26814,#26815,#26816,#26817,#26818,#26819,
#26820,#26821,#26822,#26823,#26824,#26825,#26826,#26827,#26828,#26829,#26830,
#26831,#26832,#26833,#26834,#26835,#26836,#26837,#26838,#26839,#26840,#26841,
#26842),.UNSPECIFIED.,.F.,.F.,(4,3,3,3,3,3,3,3,3,3,3,3,3,3,3,3,3,3,3,3,
3,3,3,3,3,3,3,3,3,3,3,3,3,3,3,3,3,3,3,3,3,3,3,3,3,3,3,3,3,3,3,3,3,3,3,3,
3,3,3,3,3,3,3,3,3,3,3,3,3,3,3,3,3,3,3,4),(133.056936661683,133.144638878716,
133.232231781202,133.319740031263,133.407192196977,133.494615948175,133.58203343827,
133.669466811322,133.756991613018,133.844565328127,133.932277736142,133.992765655084,
134.081315198345,134.169749935364,134.258093673919,134.349920923109,134.438162246791,
134.526390111752,134.61462588974,134.702890953068,134.791256435121,134.879681416182,
134.96823684535,134.992711667435,135.081261210696,135.169695947716,135.258039686271,
135.34986693546,135.438108259143,135.526336124105,135.614571902093,135.70283696542,
135.791202447473,135.879627428534,135.968182857703,135.992657679787,136.081207223048,
136.169641960068,136.257985698623,136.349812947812,136.438054271494,136.526282136456,
136.614517914444,136.702782977771,136.791148459825,136.879573440886,136.968128870055,
136.992603692138,137.081153235398,137.169587972418,137.257931710973,137.349758960162,
137.438000283844,137.526228148806,137.614463926793,137.702728990121,137.791094472174,
137.879519453235,137.968074882403,137.992549704489,138.08109924775,138.16953398477,
138.257877723325,138.349704972515,138.437946296197,138.526174161159,138.614409939148,
138.702675002476,138.791040484529,138.879465465591,138.968020894759,138.992495716841,
139.095160517603,139.197384563926,139.29881023738,139.340121968631),
 .UNSPECIFIED.);
#262=B_SPLINE_CURVE_WITH_KNOTS('',3,(#26844,#26845,#26846,#26847,#26848,
#26849,#26850,#26851,#26852,#26853,#26854,#26855,#26856,#26857,#26858,#26859,
#26860,#26861,#26862,#26863,#26864,#26865,#26866,#26867,#26868,#26869,#26870,
#26871,#26872,#26873,#26874,#26875,#26876,#26877,#26878,#26879,#26880,#26881,
#26882,#26883,#26884,#26885,#26886,#26887,#26888,#26889,#26890,#26891,#26892,
#26893,#26894,#26895,#26896,#26897,#26898,#26899,#26900,#26901,#26902,#26903,
#26904,#26905,#26906,#26907,#26908,#26909,#26910,#26911,#26912,#26913,#26914,
#26915,#26916,#26917,#26918,#26919,#26920,#26921,#26922,#26923,#26924,#26925,
#26926,#26927,#26928,#26929,#26930,#26931,#26932,#26933,#26934,#26935,#26936,
#26937,#26938,#26939,#26940,#26941,#26942,#26943,#26944,#26945,#26946,#26947,
#26948,#26949,#26950,#26951,#26952,#26953,#26954,#26955,#26956,#26957,#26958,
#26959,#26960,#26961,#26962,#26963,#26964,#26965,#26966,#26967,#26968,#26969,
#26970,#26971,#26972,#26973,#26974,#26975,#26976,#26977,#26978,#26979,#26980,
#26981,#26982,#26983,#26984,#26985,#26986,#26987,#26988,#26989,#26990,#26991,
#26992,#26993,#26994,#26995,#26996,#26997,#26998,#26999,#27000,#27001,#27002,
#27003,#27004,#27005,#27006,#27007,#27008,#27009,#27010,#27011,#27012,#27013,
#27014,#27015,#27016,#27017,#27018,#27019,#27020,#27021,#27022,#27023,#27024,
#27025,#27026,#27027,#27028,#27029,#27030,#27031,#27032,#27033,#27034,#27035,
#27036,#27037,#27038,#27039,#27040,#27041,#27042,#27043,#27044,#27045,#27046,
#27047,#27048,#27049,#27050,#27051,#27052,#27053,#27054,#27055,#27056,#27057,
#27058,#27059,#27060,#27061,#27062,#27063,#27064,#27065,#27066,#27067,#27068,
#27069),.UNSPECIFIED.,.F.,.F.,(4,3,3,3,3,3,3,3,3,3,3,3,3,3,3,3,3,3,3,3,
3,3,3,3,3,3,3,3,3,3,3,3,3,3,3,3,3,3,3,3,3,3,3,3,3,3,3,3,3,3,3,3,3,3,3,3,
3,3,3,3,3,3,3,3,3,3,3,3,3,3,3,3,3,3,3,4),(139.340121968862,139.428521800617,
139.516914594785,139.605321416591,139.693763336218,139.782315552249,139.870931673301,
139.95968890979,139.992441729192,140.080991272453,140.169426009473,140.257769748028,
140.349596997217,140.4378383209,140.526066185862,140.61430196385,140.702567027178,
140.790932509231,140.879357490293,140.967912919461,140.992387741544,141.080937284805,
141.169372021824,141.257715760379,141.349543009569,141.437784333251,141.526012198212,
141.6142479762,141.702513039528,141.790878521581,141.879303502642,141.96785893181,
141.992333753895,142.080883297156,142.169318034175,142.257661772731,142.34948902192,
142.437730345602,142.525958210564,142.614193988552,142.702459051879,142.790824533932,
142.879249514994,142.967804944162,142.992279766246,143.080829309507,143.169264046527,
143.257607785082,143.349435034271,143.437676357953,143.525904222915,143.614140000903,
143.70240506423,143.790770546284,143.879195527345,143.967750956513,143.992225778598,
144.080775321858,144.169210058877,144.257553797432,144.349381046622,144.437622370303,
144.525850235265,144.614086013251,144.702351076578,144.79071655863,144.879141539691,
144.967696968859,144.992171790949,145.081319122906,145.170348342848,145.259280195558,
145.350286965679,145.439082830911,145.531195053476,145.623307276042),
 .UNSPECIFIED.);
#263=B_SPLINE_CURVE_WITH_KNOTS('',3,(#27071,#27072,#27073,#27074,#27075,
#27076,#27077,#27078,#27079,#27080),.UNSPECIFIED.,.F.,.F.,(4,1,1,1,1,1,
1,4),(145.623314962503,145.9921178033,146.992063815652,147.992009828003,
148.991955840354,149.991901852706,150.991847865057,151.906483871255),
 .UNSPECIFIED.);
#264=B_SPLINE_CURVE_WITH_KNOTS('',3,(#27082,#27083,#27084,#27085,#27086,
#27087,#27088,#27089,#27090,#27091,#27092,#27093,#27094,#27095,#27096,#27097,
#27098,#27099,#27100,#27101,#27102,#27103,#27104,#27105,#27106,#27107,#27108,
#27109,#27110,#27111,#27112,#27113,#27114,#27115,#27116,#27117,#27118,#27119,
#27120,#27121,#27122,#27123,#27124,#27125,#27126,#27127,#27128,#27129,#27130,
#27131,#27132,#27133,#27134,#27135,#27136,#27137,#27138,#27139,#27140,#27141,
#27142,#27143,#27144,#27145,#27146,#27147,#27148,#27149,#27150,#27151,#27152,
#27153,#27154,#27155,#27156,#27157,#27158,#27159,#27160,#27161,#27162,#27163,
#27164,#27165,#27166,#27167,#27168,#27169,#27170,#27171,#27172,#27173,#27174,
#27175,#27176,#27177,#27178,#27179,#27180,#27181,#27182,#27183,#27184,#27185,
#27186,#27187,#27188,#27189,#27190,#27191,#27192,#27193,#27194,#27195,#27196,
#27197,#27198,#27199,#27200,#27201,#27202,#27203,#27204,#27205,#27206,#27207,
#27208,#27209,#27210,#27211,#27212,#27213,#27214,#27215,#27216,#27217,#27218,
#27219,#27220,#27221,#27222,#27223,#27224,#27225,#27226,#27227,#27228,#27229,
#27230,#27231,#27232,#27233,#27234,#27235,#27236,#27237,#27238,#27239,#27240,
#27241,#27242,#27243,#27244,#27245,#27246,#27247,#27248,#27249,#27250,#27251,
#27252,#27253,#27254,#27255,#27256,#27257,#27258,#27259,#27260,#27261,#27262,
#27263,#27264,#27265,#27266,#27267,#27268,#27269,#27270,#27271,#27272,#27273,
#27274,#27275,#27276,#27277,#27278,#27279,#27280,#27281,#27282,#27283,#27284,
#27285,#27286,#27287,#27288,#27289,#27290,#27291,#27292,#27293,#27294,#27295,
#27296,#27297,#27298,#27299,#27300,#27301,#27302,#27303,#27304,#27305,#27306,
#27307),.UNSPECIFIED.,.F.,.F.,(4,3,3,3,3,3,3,3,3,3,3,3,3,3,3,3,3,3,3,3,
3,3,3,3,3,3,3,3,3,3,3,3,3,3,3,3,3,3,3,3,3,3,3,3,3,3,3,3,3,3,3,3,3,3,3,3,
3,3,3,3,3,3,3,3,3,3,3,3,3,3,3,3,3,3,3,4),(151.906492583222,151.991793877409,
152.080343420566,152.168778157483,152.257121895935,152.348949145163,152.437190468744,
152.525418333606,152.613654111494,152.701919174722,152.790284656678,152.878709637644,
152.967265066718,152.99173988976,153.080289432964,153.168724169926,153.257067908422,
153.348895157633,153.437136481254,153.525364346154,153.61360012408,153.701865187344,
153.790230669334,153.878655650331,153.967211079435,153.991685902111,154.08023544587,
154.16867018339,154.257013922446,154.348841171448,154.43708249563,154.52531036109,
154.613546139575,154.701811203397,154.790176685939,154.878601667486,154.967157097132,
154.991631914463,155.080181456899,155.168616193095,155.256959930829,155.348787180327,
155.437028503198,155.525256367354,155.613492144542,155.701757207076,155.79012268835,
155.878547668639,155.967103097051,155.991577926814,156.080127469951,156.168562206839,
156.256905945255,156.348733194494,156.43697451802,156.525202382819,156.613438160639,
156.701703223792,156.790068705663,156.878493686538,156.967049115515,156.991523939165,
157.080073485715,157.168508226035,157.256851967898,157.34867921585,157.436920542839,
157.525148411102,157.613384192381,157.701649258987,157.790014744282,157.87843972857,
157.966995160914,157.991469951517,158.119206215025,158.189677890401),
 .UNSPECIFIED.);
#265=B_SPLINE_CURVE_WITH_KNOTS('',3,(#27309,#27310,#27311,#27312,#27313,
#27314,#27315,#27316,#27317,#27318),.UNSPECIFIED.,.F.,.F.,(4,1,1,1,1,1,
1,4),(158.189681389038,158.991415963868,159.99136197622,160.991307988571,
161.991254000922,162.991200013274,163.991146025625,164.472861769939),
 .UNSPECIFIED.);
#266=B_SPLINE_CURVE_WITH_KNOTS('',3,(#27320,#27321,#27322,#27323,#27324,
#27325,#27326,#27327,#27328,#27329,#27330,#27331,#27332,#27333,#27334,#27335,
#27336,#27337,#27338,#27339,#27340,#27341,#27342,#27343,#27344,#27345,#27346,
#27347,#27348,#27349,#27350,#27351,#27352,#27353,#27354,#27355,#27356,#27357,
#27358,#27359,#27360,#27361,#27362,#27363,#27364,#27365,#27366,#27367,#27368,
#27369,#27370,#27371,#27372,#27373,#27374,#27375,#27376,#27377,#27378,#27379,
#27380,#27381,#27382,#27383,#27384,#27385,#27386,#27387,#27388,#27389,#27390,
#27391,#27392,#27393,#27394,#27395,#27396,#27397,#27398,#27399,#27400,#27401,
#27402,#27403,#27404,#27405,#27406,#27407,#27408,#27409,#27410,#27411,#27412,
#27413,#27414,#27415,#27416,#27417,#27418,#27419,#27420,#27421,#27422,#27423,
#27424,#27425,#27426,#27427,#27428,#27429,#27430,#27431,#27432,#27433,#27434,
#27435,#27436,#27437,#27438,#27439,#27440,#27441,#27442,#27443,#27444,#27445,
#27446,#27447,#27448,#27449,#27450,#27451,#27452,#27453,#27454,#27455,#27456,
#27457,#27458,#27459,#27460,#27461,#27462,#27463,#27464,#27465,#27466,#27467,
#27468,#27469,#27470,#27471,#27472,#27473,#27474,#27475,#27476,#27477,#27478,
#27479,#27480,#27481,#27482,#27483,#27484,#27485,#27486,#27487,#27488,#27489,
#27490,#27491,#27492,#27493,#27494,#27495,#27496,#27497,#27498,#27499,#27500,
#27501,#27502,#27503,#27504,#27505,#27506,#27507,#27508,#27509,#27510,#27511,
#27512,#27513,#27514,#27515,#27516,#27517,#27518,#27519,#27520,#27521,#27522,
#27523,#27524,#27525,#27526,#27527,#27528,#27529,#27530,#27531,#27532,#27533,
#27534,#27535,#27536,#27537,#27538,#27539,#27540,#27541,#27542,#27543,#27544,
#27545),.UNSPECIFIED.,.F.,.F.,(4,3,3,3,3,3,3,3,3,3,3,3,3,3,3,3,3,3,3,3,
3,3,3,3,3,3,3,3,3,3,3,3,3,3,3,3,3,3,3,3,3,3,3,3,3,3,3,3,3,3,3,3,3,3,3,3,
3,3,3,3,3,3,3,3,3,3,3,3,3,3,3,3,3,3,3,4),(164.472863197581,164.564620554491,
164.656481689159,164.748542726059,164.840710752793,164.933083630566,164.991092037976,
165.079641825262,165.168076804179,165.256420782257,165.348247940766,165.436489496637,
165.524717590711,165.612953594507,165.701218880108,165.78958457811,165.87800977171,
165.966565406784,165.991038050328,166.079588379573,166.168023907756,166.256368441678,
166.348195394303,166.436437518814,166.524666185258,166.612902764528,166.701168628086,
166.789534904754,166.877960678146,166.966516890119,166.990984062679,167.079531079788,
167.167963287752,167.256304497273,167.348132694493,167.436371504789,167.524596866325,
167.612830153446,167.701092741073,167.789455782318,167.877878339832,167.966431389575,
167.990930075031,168.079481963654,168.167919033012,168.256265088403,168.348091463276,
168.436335051259,168.524565157465,168.612803151383,168.701070403051,168.789438021748,
168.877865112049,168.966422594011,168.990876087382,169.079430061653,169.167869267384,
169.256217506719,169.348043080846,169.436288956627,169.524521384817,169.612761732272,
169.701031366421,169.789401398027,169.877830921893,169.966390848492,169.990822099733,
170.078237539823,170.165512518093,170.252707282048,170.339844321629,170.426946068895,
170.514063004851,170.601185227643,170.688382092216,170.75604850476),
 .UNSPECIFIED.);
#267=B_SPLINE_CURVE_WITH_KNOTS('',3,(#27547,#27548,#27549,#27550,#27551,
#27552,#27553,#27554,#27555,#27556,#27557,#27558,#27559,#27560,#27561,#27562,
#27563,#27564,#27565,#27566,#27567,#27568,#27569,#27570,#27571,#27572,#27573,
#27574,#27575,#27576,#27577,#27578,#27579,#27580,#27581,#27582,#27583,#27584,
#27585,#27586,#27587,#27588,#27589,#27590,#27591,#27592,#27593,#27594,#27595,
#27596,#27597,#27598,#27599,#27600,#27601,#27602,#27603,#27604,#27605,#27606,
#27607,#27608,#27609,#27610,#27611,#27612,#27613,#27614,#27615,#27616,#27617,
#27618,#27619,#27620,#27621,#27622,#27623,#27624,#27625,#27626,#27627,#27628,
#27629,#27630,#27631,#27632,#27633,#27634,#27635,#27636,#27637,#27638,#27639,
#27640,#27641,#27642,#27643,#27644,#27645,#27646,#27647,#27648,#27649,#27650,
#27651,#27652,#27653,#27654,#27655,#27656,#27657,#27658,#27659,#27660,#27661,
#27662,#27663,#27664,#27665,#27666,#27667,#27668,#27669,#27670,#27671,#27672,
#27673,#27674,#27675,#27676,#27677,#27678,#27679,#27680,#27681,#27682,#27683,
#27684,#27685,#27686,#27687,#27688,#27689,#27690,#27691,#27692,#27693,#27694,
#27695,#27696,#27697,#27698,#27699,#27700,#27701,#27702,#27703,#27704,#27705,
#27706,#27707,#27708,#27709,#27710,#27711,#27712,#27713,#27714,#27715,#27716,
#27717,#27718,#27719,#27720,#27721,#27722,#27723,#27724,#27725,#27726,#27727,
#27728,#27729,#27730),.UNSPECIFIED.,.F.,.F.,(4,3,3,3,3,3,3,3,3,3,3,3,3,
3,3,3,3,3,3,3,3,3,3,3,3,3,3,3,3,3,3,3,3,3,3,3,3,3,3,3,3,3,3,3,3,3,3,3,3,
3,3,3,3,3,3,3,3,3,3,3,3,4),(170.756048504935,170.873914600802,170.990768112085,
171.079338276875,171.16779355935,171.256157744839,171.347977292289,171.436238693458,
171.524486466626,171.612741963255,171.701026535212,171.789411117863,171.87785498588,
171.966428842985,171.990714124436,172.079286474888,172.167744288444,172.256111342656,
172.347929941922,172.436195026618,172.524446775571,172.612706534521,172.700995649825,
172.789385165724,172.877834199635,172.966413521211,172.990660136787,173.079086910887,
173.167398611765,173.255619188468,173.347492558552,173.435611157336,173.523716659296,
173.611830560963,173.699974359953,173.788220091732,173.876526050693,173.964964454657,
173.990606149139,174.079327458897,174.167933535642,174.256447991984,174.348211013172,
174.436620444989,174.525015168666,174.613416380147,174.701845274749,174.790371395654,
174.878955350467,174.967666093791,174.99055216149,175.078366871321,175.16606918391,
175.25368368237,175.34123713241,175.428759059388,175.51627153865,175.603796633468,
175.691408265889,175.779065855606,175.866858195123,175.92887515605),
 .UNSPECIFIED.);
#268=B_SPLINE_CURVE_WITH_KNOTS('',3,(#27734,#27735,#27736,#27737,#27738,
#27739,#27740,#27741),.UNSPECIFIED.,.F.,.F.,(4,1,1,1,1,4),(-177.990390198544,
-176.990444186193,-175.990498173842,-174.99055216149,-173.990606149139,
-173.73875440895),.UNSPECIFIED.);
#269=B_SPLINE_CURVE_WITH_KNOTS('',3,(#27743,#27744,#27745,#27746,#27747,
#27748,#27749,#27750,#27751,#27752,#27753,#27754,#27755,#27756,#27757,#27758,
#27759,#27760,#27761,#27762,#27763,#27764,#27765,#27766,#27767,#27768,#27769,
#27770,#27771,#27772,#27773,#27774,#27775,#27776,#27777,#27778,#27779,#27780,
#27781,#27782,#27783,#27784,#27785,#27786,#27787,#27788,#27789,#27790,#27791,
#27792,#27793,#27794,#27795,#27796,#27797,#27798,#27799,#27800,#27801,#27802,
#27803,#27804,#27805,#27806,#27807,#27808,#27809,#27810,#27811,#27812,#27813,
#27814,#27815,#27816,#27817,#27818,#27819,#27820,#27821,#27822,#27823,#27824,
#27825,#27826,#27827,#27828,#27829,#27830,#27831,#27832,#27833,#27834,#27835,
#27836,#27837,#27838,#27839,#27840,#27841,#27842,#27843,#27844,#27845,#27846,
#27847,#27848,#27849,#27850,#27851,#27852,#27853,#27854,#27855,#27856,#27857,
#27858,#27859,#27860,#27861,#27862,#27863,#27864,#27865,#27866,#27867,#27868,
#27869,#27870,#27871,#27872,#27873,#27874,#27875,#27876,#27877,#27878,#27879,
#27880,#27881,#27882,#27883,#27884,#27885,#27886,#27887,#27888,#27889,#27890,
#27891,#27892,#27893,#27894,#27895,#27896,#27897,#27898,#27899,#27900,#27901,
#27902,#27903,#27904,#27905,#27906,#27907,#27908,#27909,#27910,#27911,#27912,
#27913,#27914,#27915,#27916,#27917,#27918,#27919,#27920,#27921,#27922,#27923,
#27924,#27925,#27926,#27927,#27928,#27929,#27930,#27931,#27932,#27933,#27934,
#27935,#27936,#27937,#27938,#27939,#27940,#27941,#27942,#27943,#27944,#27945,
#27946,#27947,#27948,#27949,#27950,#27951,#27952,#27953,#27954,#27955,#27956,
#27957,#27958,#27959,#27960,#27961,#27962,#27963,#27964,#27965,#27966,#27967,
#27968),.UNSPECIFIED.,.F.,.F.,(4,3,3,3,3,3,3,3,3,3,3,3,3,3,3,3,3,3,3,3,
3,3,3,3,3,3,3,3,3,3,3,3,3,3,3,3,3,3,3,3,3,3,3,3,3,3,3,3,3,3,3,3,3,3,3,3,
3,3,3,3,3,3,3,3,3,3,3,3,3,3,3,3,3,3,3,4),(-173.738752334043,-173.651535863068,
-173.564373232163,-173.477237355581,-173.39010587623,-173.302956444482,
-173.215714308532,-173.128421050025,-173.040991470072,-172.990660136787,
-172.902086758176,-172.813628104058,-172.725260396143,-172.63344211218,
-172.545176843568,-172.456925084215,-172.368665488387,-172.280376709863,
-172.191987786504,-172.103539494695,-172.01496112903,-171.990714124436,
-171.90214620507,-171.81369273751,-171.725329938254,-171.633509709983,-171.545248617959,
-171.45700075632,-171.368744773707,-171.280459318054,-171.192073266518,
-171.103627587279,-171.015051430389,-170.990768112085,-170.902235390015,
-170.813817694881,-170.725491197375,-170.63365756017,-170.545433867796,
-170.457223748581,-170.369005812376,-170.280758668513,-170.192411131339,
-170.10400413231,-170.01546660041,-169.990822099733,-169.902268068231,-169.8138288144,
-169.72548053607,-169.633654979984,-169.545409088144,-169.457176652377,
-169.368936305834,-169.280666681103,-169.192296671475,-169.103867176925,
-169.015307290188,-168.990876087382,-168.902324496367,-168.813887667493,
-168.725541795705,-168.633715330621,-168.545471783305,-168.457241665011,
-168.369003606262,-168.280736236998,-168.192368423046,-168.103941092068,
-168.015383304581,-167.99093007503,-167.899167922216,-167.807554835821,
-167.716121750623,-167.624794219276,-167.533586961915,-167.455567026863),
 .UNSPECIFIED.);
#270=B_SPLINE_CURVE_WITH_KNOTS('',3,(#27970,#27971,#27972,#27973,#27974,
#27975,#27976,#27977,#27978,#27979,#27980,#27981,#27982,#27983,#27984,#27985,
#27986,#27987,#27988,#27989,#27990,#27991,#27992,#27993,#27994,#27995,#27996,
#27997,#27998,#27999,#28000,#28001,#28002,#28003,#28004,#28005,#28006,#28007,
#28008,#28009,#28010,#28011,#28012,#28013,#28014,#28015,#28016,#28017,#28018,
#28019,#28020,#28021,#28022,#28023,#28024,#28025,#28026,#28027,#28028,#28029,
#28030,#28031,#28032,#28033,#28034,#28035,#28036,#28037,#28038,#28039,#28040,
#28041,#28042,#28043,#28044,#28045,#28046,#28047,#28048,#28049,#28050,#28051,
#28052,#28053,#28054,#28055,#28056,#28057,#28058,#28059,#28060,#28061,#28062,
#28063,#28064,#28065,#28066,#28067,#28068,#28069,#28070,#28071,#28072,#28073,
#28074,#28075,#28076,#28077,#28078,#28079,#28080,#28081,#28082,#28083,#28084,
#28085,#28086,#28087,#28088,#28089,#28090,#28091,#28092,#28093,#28094,#28095,
#28096,#28097,#28098,#28099,#28100,#28101,#28102,#28103,#28104,#28105,#28106,
#28107,#28108,#28109,#28110,#28111,#28112,#28113,#28114,#28115,#28116,#28117,
#28118,#28119,#28120,#28121,#28122,#28123,#28124,#28125,#28126,#28127,#28128,
#28129,#28130,#28131,#28132,#28133,#28134,#28135,#28136,#28137,#28138,#28139,
#28140,#28141,#28142,#28143,#28144,#28145,#28146,#28147,#28148,#28149,#28150,
#28151,#28152,#28153,#28154,#28155,#28156,#28157,#28158,#28159,#28160,#28161,
#28162,#28163,#28164,#28165,#28166,#28167,#28168,#28169,#28170,#28171,#28172,
#28173,#28174,#28175,#28176,#28177,#28178,#28179,#28180,#28181,#28182,#28183,
#28184,#28185,#28186,#28187,#28188,#28189,#28190,#28191,#28192,#28193,#28194,
#28195),.UNSPECIFIED.,.F.,.F.,(4,3,3,3,3,3,3,3,3,3,3,3,3,3,3,3,3,3,3,3,
3,3,3,3,3,3,3,3,3,3,3,3,3,3,3,3,3,3,3,3,3,3,3,3,3,3,3,3,3,3,3,3,3,3,3,3,
3,3,3,3,3,3,3,3,3,3,3,3,3,3,3,3,3,3,3,4),(-167.455567026675,-167.36166117942,
-167.26743965224,-167.173059830492,-167.078395851896,-166.990984062679,
-166.902433737907,-166.813998212985,-166.72565368112,-166.633826727271,
-166.545584601802,-166.457355933291,-166.369119350847,-166.280853483008,
-166.19248720044,-166.1040614202,-166.015505200038,-165.991038050328,-165.902488301604,
-165.814053353852,-165.725709399573,-165.633882229373,-165.54564067879,
-165.457412583173,-165.369176571003,-165.280911270194,-165.192545546928,
-165.104120322181,-165.015564647562,-164.991092037976,-164.902542823081,
-164.814108419134,-164.725765017936,-164.633937643897,-164.545696666176,
-164.457469149771,-164.369233722574,-164.280969011912,-164.19260388354,
-164.104179257191,-164.015624181504,-163.991146025625,-163.902596353175,
-163.814161485746,-163.725817615724,-163.633990415418,-163.545748958459,
-163.457520959779,-163.369285047773,-163.281019850269,-163.19265423448,
-163.104229119776,-163.015673558138,-162.991200013274,-162.902650453511,
-162.814215699397,-162.725871943178,-162.634044700396,-162.545803357729,
-162.457575473325,-162.369339675457,-162.281074591829,-162.192709088949,
-162.10428408673,-162.015728636077,-161.991254000922,-161.904020167719,
-161.812565361731,-161.72554948886,-161.638587796198,-161.55165773383,-161.464736785871,
-161.377767495936,-161.290769922006,-161.203680569857,-161.172381719815),
 .UNSPECIFIED.);
#271=B_SPLINE_CURVE_WITH_KNOTS('',3,(#28197,#28198,#28199,#28200,#28201,
#28202,#28203,#28204,#28205,#28206,#28207,#28208,#28209,#28210,#28211,#28212,
#28213,#28214,#28215,#28216,#28217,#28218,#28219,#28220,#28221,#28222,#28223,
#28224,#28225,#28226,#28227,#28228,#28229,#28230,#28231,#28232,#28233,#28234,
#28235,#28236,#28237,#28238,#28239,#28240,#28241,#28242,#28243,#28244,#28245,
#28246,#28247,#28248,#28249,#28250,#28251,#28252,#28253,#28254,#28255,#28256,
#28257,#28258,#28259,#28260,#28261,#28262,#28263,#28264,#28265,#28266,#28267,
#28268,#28269,#28270,#28271,#28272,#28273,#28274,#28275,#28276,#28277,#28278,
#28279,#28280,#28281,#28282,#28283,#28284,#28285,#28286,#28287,#28288,#28289,
#28290,#28291,#28292,#28293,#28294,#28295,#28296,#28297,#28298,#28299,#28300,
#28301,#28302,#28303,#28304,#28305,#28306,#28307,#28308,#28309,#28310,#28311,
#28312,#28313,#28314,#28315,#28316,#28317,#28318,#28319,#28320,#28321,#28322,
#28323,#28324,#28325,#28326,#28327,#28328,#28329,#28330,#28331,#28332,#28333,
#28334,#28335,#28336,#28337,#28338,#28339,#28340,#28341,#28342,#28343,#28344,
#28345,#28346,#28347,#28348,#28349,#28350,#28351,#28352,#28353,#28354,#28355,
#28356,#28357,#28358,#28359,#28360,#28361,#28362,#28363,#28364,#28365,#28366,
#28367,#28368,#28369,#28370,#28371,#28372,#28373,#28374,#28375,#28376,#28377,
#28378,#28379,#28380,#28381,#28382,#28383,#28384,#28385,#28386,#28387,#28388,
#28389,#28390,#28391,#28392,#28393,#28394,#28395,#28396,#28397,#28398,#28399,
#28400,#28401,#28402,#28403,#28404,#28405,#28406,#28407,#28408,#28409,#28410,
#28411,#28412,#28413,#28414,#28415,#28416,#28417,#28418,#28419,#28420,#28421,
#28422),.UNSPECIFIED.,.F.,.F.,(4,3,3,3,3,3,3,3,3,3,3,3,3,3,3,3,3,3,3,3,
3,3,3,3,3,3,3,3,3,3,3,3,3,3,3,3,3,3,3,3,3,3,3,3,3,3,3,3,3,3,3,3,3,3,3,3,
3,3,3,3,3,3,3,3,3,3,3,3,3,3,3,3,3,3,3,4),(-161.172381719684,-161.038271783866,
-160.991307988571,-160.902758424752,-160.81432366696,-160.725979907444,
-160.634152666041,-160.545911321061,-160.457683434712,-160.369447635271,
-160.281182550447,-160.192817046941,-160.104392044426,-160.015836593969,
-159.99136197622,-159.902812432459,-159.814377694878,-159.726033955703,
-159.634206706723,-159.545965382275,-159.457737516494,-159.369501737634,
-159.281236673384,-159.192871190335,-159.104446208235,-159.015890777971,
-158.991415963868,-158.902866426481,-158.814431695428,-158.726087962924,
-158.634260711498,-158.546019394041,-158.457791535358,-158.369555763696,
-158.281290706736,-158.192925231079,-158.104500256439,-158.015944833679,
-157.991469951517,-157.902920405082,-157.814485664852,-157.726141923055,
-157.634314675069,-157.546073348086,-157.457845479808,-157.369609698492,
-157.281344631827,-157.192979146439,-157.104554162041,-157.015998729559,
-156.991523939165,-156.902974396096,-156.814539659262,-156.726195920889,
-156.634368671629,-156.546127348114,-156.457899483313,-156.369663705481,
-156.281398642303,-156.193033160389,-156.104608179461,-156.016052750418,
-155.991577926814,-155.903028384309,-155.814593648058,-155.726249910282,
-155.634422660805,-155.546181337927,-155.457953473776,-155.369717696606,
-155.281452634103,-155.193087152878,-155.104662172649,-155.016106744312,
-154.991631914463,-154.889196412504),.UNSPECIFIED.);
#272=B_SPLINE_CURVE_WITH_KNOTS('',3,(#28424,#28425,#28426,#28427,#28428,
#28429,#28430,#28431,#28432,#28433),.UNSPECIFIED.,.F.,.F.,(4,1,1,1,1,1,
1,4),(-154.889187401721,-153.991685902111,-152.99173988976,-151.991793877409,
-150.991847865057,-149.991901852706,-148.991955840354,-148.606018529037),
 .UNSPECIFIED.);
#273=B_SPLINE_CURVE_WITH_KNOTS('',3,(#28435,#28436,#28437,#28438,#28439,
#28440,#28441,#28442,#28443,#28444,#28445,#28446,#28447,#28448,#28449,#28450,
#28451,#28452,#28453,#28454,#28455,#28456,#28457,#28458,#28459,#28460,#28461,
#28462,#28463,#28464,#28465,#28466,#28467,#28468,#28469,#28470,#28471,#28472,
#28473,#28474,#28475,#28476,#28477,#28478,#28479,#28480,#28481,#28482,#28483,
#28484,#28485,#28486,#28487,#28488,#28489,#28490,#28491,#28492,#28493,#28494,
#28495,#28496,#28497,#28498,#28499,#28500,#28501,#28502,#28503,#28504,#28505,
#28506,#28507,#28508,#28509,#28510,#28511,#28512,#28513,#28514,#28515,#28516,
#28517,#28518,#28519,#28520,#28521,#28522,#28523,#28524,#28525,#28526,#28527,
#28528,#28529,#28530,#28531,#28532,#28533,#28534,#28535,#28536,#28537,#28538,
#28539,#28540,#28541,#28542,#28543,#28544,#28545,#28546,#28547,#28548,#28549,
#28550,#28551,#28552,#28553,#28554,#28555,#28556,#28557,#28558,#28559,#28560,
#28561,#28562,#28563,#28564,#28565,#28566,#28567,#28568,#28569,#28570,#28571,
#28572,#28573,#28574,#28575,#28576,#28577,#28578,#28579,#28580,#28581,#28582,
#28583,#28584,#28585,#28586,#28587,#28588,#28589,#28590,#28591,#28592,#28593,
#28594,#28595,#28596,#28597,#28598,#28599,#28600,#28601,#28602,#28603,#28604,
#28605,#28606,#28607,#28608,#28609,#28610,#28611,#28612,#28613,#28614,#28615,
#28616,#28617,#28618,#28619,#28620,#28621,#28622,#28623,#28624,#28625,#28626,
#28627,#28628,#28629,#28630,#28631,#28632,#28633,#28634,#28635,#28636,#28637,
#28638,#28639,#28640,#28641,#28642,#28643,#28644,#28645,#28646,#28647,#28648,
#28649,#28650,#28651,#28652,#28653,#28654,#28655,#28656,#28657,#28658,#28659,
#28660),.UNSPECIFIED.,.F.,.F.,(4,3,3,3,3,3,3,3,3,3,3,3,3,3,3,3,3,3,3,3,
3,3,3,3,3,3,3,3,3,3,3,3,3,3,3,3,3,3,3,3,3,3,3,3,3,3,3,3,3,3,3,3,3,3,3,3,
3,3,3,3,3,3,3,3,3,3,3,3,3,3,3,3,3,3,3,4),(-148.606011105325,-148.516896311246,
-148.427765779446,-148.338599573289,-148.249313397802,-148.159965224952,
-148.070452324036,-147.992009828003,-147.903460284745,-147.815025547728,
-147.726681809176,-147.634854559986,-147.546613236307,-147.458385371348,
-147.370149593363,-147.281884530039,-147.193519047988,-147.10509406693,
-147.016538637765,-146.992063815652,-146.903514272392,-146.815079535374,
-146.72673579682,-146.63490854763,-146.546667223949,-146.458439358988,-146.370203581002,
-146.281938517676,-146.193573035624,-146.105148054564,-146.016592625397,
-145.9921178033,-145.903568260038,-145.815133523017,-145.72678978446,-145.634962535271,
-145.546721211588,-145.458493346624,-145.370257568635,-145.281992505305,
-145.19362702325,-145.105202042187,-145.016646613017,-144.992171790949,
-144.903622247689,-144.81518751067,-144.726843772116,-144.635016522926,
-144.546775199245,-144.458547334283,-144.370311556296,-144.28204649297,
-144.193681010918,-144.105256029857,-144.016700600689,-143.992225778598,
-143.903676235337,-143.815241498317,-143.726897759762,-143.635070510573,
-143.54682918689,-143.458601321928,-143.37036554394,-143.282100480614,-143.193734998561,
-143.105310017499,-143.016754588331,-142.992279766246,-142.903834207347,
-142.815500271385,-142.727256342741,-142.639080881638,-142.55094590012,
-142.462835403558,-142.374706207577,-142.322825798145),.UNSPECIFIED.);
#274=B_SPLINE_CURVE_WITH_KNOTS('',3,(#28662,#28663,#28664,#28665,#28666,
#28667,#28668,#28669,#28670,#28671),.UNSPECIFIED.,.F.,.F.,(4,1,1,1,1,1,
1,4),(-142.322818623298,-141.992333753895,-140.992387741543,-139.992441729192,
-138.992495716841,-137.992549704489,-136.992603692138,-136.039640490966),
 .UNSPECIFIED.);
#275=B_SPLINE_CURVE_WITH_KNOTS('',3,(#28673,#28674,#28675,#28676,#28677,
#28678,#28679,#28680,#28681,#28682,#28683),.UNSPECIFIED.,.F.,.F.,(4,1,1,
1,1,1,1,1,4),(-136.039640490966,-135.992657679787,-134.992711667435,-133.992765655084,
-132.992819642732,-131.992873630381,-130.99292761803,-129.992981605678,
-129.756455515395),.UNSPECIFIED.);
#276=B_SPLINE_CURVE_WITH_KNOTS('',3,(#28685,#28686,#28687,#28688,#28689,
#28690,#28691,#28692,#28693,#28694,#28695,#28696,#28697,#28698,#28699,#28700,
#28701,#28702,#28703,#28704,#28705,#28706,#28707,#28708,#28709,#28710,#28711,
#28712,#28713,#28714,#28715,#28716,#28717,#28718,#28719,#28720,#28721,#28722,
#28723,#28724,#28725,#28726,#28727,#28728,#28729,#28730,#28731,#28732,#28733,
#28734,#28735,#28736,#28737,#28738,#28739,#28740,#28741,#28742,#28743,#28744,
#28745,#28746,#28747,#28748,#28749,#28750,#28751,#28752,#28753,#28754,#28755,
#28756,#28757,#28758,#28759,#28760,#28761,#28762,#28763,#28764,#28765,#28766,
#28767,#28768,#28769,#28770,#28771,#28772,#28773,#28774,#28775,#28776,#28777,
#28778,#28779,#28780,#28781,#28782,#28783,#28784,#28785,#28786,#28787,#28788,
#28789,#28790,#28791,#28792,#28793,#28794,#28795,#28796,#28797,#28798,#28799,
#28800,#28801,#28802,#28803,#28804,#28805,#28806,#28807,#28808,#28809,#28810,
#28811,#28812,#28813,#28814,#28815,#28816,#28817,#28818,#28819,#28820,#28821,
#28822,#28823,#28824,#28825,#28826,#28827,#28828,#28829,#28830,#28831,#28832,
#28833,#28834,#28835,#28836,#28837,#28838,#28839,#28840,#28841,#28842,#28843,
#28844,#28845,#28846,#28847,#28848,#28849,#28850,#28851,#28852,#28853,#28854,
#28855,#28856,#28857,#28858,#28859,#28860,#28861,#28862,#28863,#28864,#28865,
#28866,#28867,#28868,#28869,#28870,#28871,#28872,#28873,#28874,#28875,#28876,
#28877,#28878,#28879,#28880,#28881,#28882,#28883,#28884,#28885,#28886,#28887,
#28888,#28889,#28890,#28891,#28892,#28893,#28894,#28895,#28896,#28897,#28898,
#28899,#28900,#28901,#28902,#28903,#28904,#28905,#28906,#28907,#28908,#28909,
#28910),.UNSPECIFIED.,.F.,.F.,(4,3,3,3,3,3,3,3,3,3,3,3,3,3,3,3,3,3,3,3,
3,3,3,3,3,3,3,3,3,3,3,3,3,3,3,3,3,3,3,3,3,3,3,3,3,3,3,3,3,3,3,3,3,3,3,3,
3,3,3,3,3,3,3,3,3,3,3,3,3,3,3,3,3,3,3,4),(-129.756455183786,-129.669225879151,
-129.582057726946,-129.494921170303,-129.407793834464,-129.320653356375,
-129.233423612432,-129.146147015044,-129.058730806341,-128.993035593327,
-128.904486050066,-128.816051313047,-128.727707574492,-128.635880325302,
-128.54763900162,-128.459411136659,-128.371175358671,-128.282910295343,
-128.19454481329,-128.106119832229,-128.017564403061,-127.993089580976,
-127.904540037715,-127.816105300695,-127.72776156214,-127.635934312951,
-127.547692989268,-127.459465124306,-127.371229346318,-127.28296428299,
-127.194598800937,-127.106173819875,-127.017618390707,-126.993143568624,
-126.904594025363,-126.816159288344,-126.727815549789,-126.635988300599,
-126.547746976917,-126.459519111955,-126.371283333967,-126.28301827064,
-126.194652788587,-126.106227807525,-126.017672378357,-125.993197556273,
-125.904648013013,-125.816213275993,-125.727869537438,-125.636042288249,
-125.547800964567,-125.459573099605,-125.371337321617,-125.28307225829,
-125.194706776237,-125.106281795176,-125.017726366008,-124.993251543922,
-124.904702000661,-124.816267263641,-124.727923525086,-124.636096275897,
-124.547854952214,-124.459627087252,-124.371391309264,-124.283126245937,
-124.194760763884,-124.106335782822,-124.017780353654,-123.99330553157,
-123.900984823973,-123.808821255979,-123.71685311386,-123.625000764951,
-123.533287515117,-123.473269876606),.UNSPECIFIED.);
#277=B_SPLINE_CURVE_WITH_KNOTS('',3,(#28912,#28913,#28914,#28915,#28916,
#28917,#28918,#28919,#28920,#28921),.UNSPECIFIED.,.F.,.F.,(4,1,1,1,1,1,
1,4),(-123.473268309875,-122.993359519219,-121.993413506867,-120.993467494516,
-119.993521482165,-118.993575469813,-117.993629457462,-117.19008824286),
 .UNSPECIFIED.);
#278=B_SPLINE_CURVE_WITH_KNOTS('',3,(#28923,#28924,#28925,#28926,#28927,
#28928,#28929,#28930,#28931,#28932,#28933,#28934,#28935,#28936,#28937,#28938,
#28939,#28940,#28941,#28942,#28943,#28944,#28945,#28946,#28947,#28948,#28949,
#28950,#28951,#28952,#28953,#28954,#28955,#28956,#28957,#28958,#28959,#28960,
#28961,#28962,#28963,#28964,#28965,#28966,#28967,#28968,#28969,#28970,#28971,
#28972,#28973,#28974,#28975,#28976,#28977,#28978,#28979,#28980,#28981,#28982,
#28983,#28984,#28985,#28986,#28987,#28988,#28989,#28990,#28991,#28992,#28993,
#28994,#28995,#28996,#28997,#28998,#28999,#29000,#29001,#29002,#29003,#29004,
#29005,#29006,#29007,#29008,#29009,#29010,#29011,#29012,#29013,#29014,#29015,
#29016,#29017,#29018,#29019,#29020,#29021,#29022,#29023,#29024,#29025,#29026,
#29027,#29028,#29029,#29030,#29031,#29032,#29033,#29034,#29035,#29036,#29037,
#29038,#29039,#29040,#29041,#29042,#29043,#29044,#29045,#29046,#29047,#29048,
#29049,#29050,#29051,#29052,#29053,#29054,#29055,#29056,#29057,#29058,#29059,
#29060,#29061,#29062,#29063,#29064,#29065,#29066,#29067,#29068,#29069,#29070,
#29071,#29072,#29073,#29074,#29075,#29076,#29077,#29078,#29079,#29080,#29081,
#29082,#29083,#29084,#29085,#29086,#29087,#29088,#29089,#29090,#29091,#29092,
#29093,#29094,#29095,#29096,#29097,#29098,#29099,#29100,#29101,#29102,#29103,
#29104,#29105,#29106,#29107,#29108,#29109,#29110,#29111,#29112,#29113,#29114,
#29115,#29116,#29117,#29118,#29119,#29120,#29121,#29122,#29123,#29124,#29125,
#29126,#29127,#29128,#29129,#29130,#29131,#29132,#29133,#29134,#29135,#29136,
#29137,#29138,#29139,#29140,#29141,#29142,#29143,#29144,#29145,#29146,#29147,
#29148),.UNSPECIFIED.,.F.,.F.,(4,3,3,3,3,3,3,3,3,3,3,3,3,3,3,3,3,3,3,3,
3,3,3,3,3,3,3,3,3,3,3,3,3,3,3,3,3,3,3,3,3,3,3,3,3,3,3,3,3,3,3,3,3,3,3,3,
3,3,3,3,3,3,3,3,3,3,3,3,3,3,3,3,3,3,3,4),(-117.190084569427,-117.061743136065,
-116.993683445111,-116.905133901849,-116.816699164829,-116.728355426273,
-116.636528177084,-116.548286853401,-116.460058988438,-116.371823210449,
-116.283558147121,-116.195192665067,-116.106767684005,-116.018212254836,
-115.993737432759,-115.905187889498,-115.816753152479,-115.728409413924,
-115.636582164735,-115.548340841053,-115.460112976091,-115.371877198104,
-115.283612134777,-115.195246652723,-115.106821671662,-115.018266242494,
-114.993791420408,-114.905241877147,-114.816807140127,-114.728463401572,
-114.636636152383,-114.548394828701,-114.460166963739,-114.371931185751,
-114.283666122424,-114.19530064037,-114.106875659309,-114.018320230141,
-113.993845408056,-113.905295864795,-113.816861127775,-113.72851738922,
-113.636690140031,-113.548448816348,-113.460220951386,-113.371985173398,
-113.283720110071,-113.195354628017,-113.106929646956,-113.018374217788,
-112.993899395705,-112.905349852445,-112.816915115425,-112.72857137687,
-112.636744127681,-112.548502803999,-112.460274939037,-112.37203916105,
-112.283774097722,-112.195408615669,-112.106983634608,-112.018428205441,
-111.993953383354,-111.905403840093,-111.816969103073,-111.728625364518,
-111.636798115329,-111.548556791647,-111.460328926684,-111.372093148696,
-111.283828085369,-111.195462603316,-111.107037622254,-111.018482193086,
-110.994007371002,-110.906899262247),.UNSPECIFIED.);
#279=B_SPLINE_CURVE_WITH_KNOTS('',3,(#29150,#29151,#29152,#29153,#29154,
#29155,#29156,#29157,#29158,#29159),.UNSPECIFIED.,.F.,.F.,(4,1,1,1,1,1,
1,4),(-110.906890495548,-109.994061358651,-108.9941153463,-107.994169333948,
-106.994223321597,-105.994277309245,-104.994331296894,-104.623721628154),
 .UNSPECIFIED.);
#280=B_SPLINE_CURVE_WITH_KNOTS('',3,(#29161,#29162,#29163,#29164,#29165,
#29166,#29167,#29168,#29169,#29170,#29171,#29172,#29173,#29174,#29175,#29176,
#29177,#29178,#29179,#29180,#29181,#29182,#29183,#29184,#29185,#29186,#29187,
#29188,#29189,#29190,#29191,#29192,#29193,#29194,#29195,#29196,#29197,#29198,
#29199,#29200,#29201,#29202,#29203,#29204,#29205,#29206,#29207,#29208,#29209,
#29210,#29211,#29212,#29213,#29214,#29215,#29216,#29217,#29218,#29219,#29220,
#29221,#29222,#29223,#29224,#29225,#29226,#29227,#29228,#29229,#29230,#29231,
#29232,#29233,#29234,#29235,#29236,#29237,#29238,#29239,#29240,#29241,#29242,
#29243,#29244,#29245,#29246,#29247,#29248,#29249,#29250,#29251,#29252,#29253,
#29254,#29255,#29256,#29257,#29258,#29259,#29260,#29261,#29262,#29263,#29264,
#29265,#29266,#29267,#29268,#29269,#29270,#29271,#29272,#29273,#29274,#29275,
#29276,#29277,#29278,#29279,#29280,#29281,#29282,#29283,#29284,#29285,#29286,
#29287,#29288,#29289,#29290,#29291,#29292,#29293,#29294,#29295,#29296,#29297,
#29298,#29299,#29300,#29301,#29302,#29303,#29304,#29305,#29306,#29307,#29308,
#29309,#29310,#29311,#29312,#29313,#29314,#29315,#29316,#29317,#29318,#29319,
#29320,#29321,#29322,#29323,#29324,#29325,#29326,#29327,#29328,#29329,#29330,
#29331,#29332,#29333,#29334,#29335,#29336,#29337,#29338,#29339,#29340,#29341,
#29342,#29343,#29344,#29345,#29346,#29347,#29348,#29349,#29350,#29351,#29352,
#29353,#29354,#29355,#29356,#29357,#29358,#29359,#29360,#29361,#29362,#29363,
#29364,#29365,#29366,#29367,#29368,#29369,#29370,#29371,#29372,#29373,#29374,
#29375,#29376,#29377,#29378,#29379,#29380,#29381,#29382,#29383,#29384,#29385,
#29386),.UNSPECIFIED.,.F.,.F.,(4,3,3,3,3,3,3,3,3,3,3,3,3,3,3,3,3,3,3,3,
3,3,3,3,3,3,3,3,3,3,3,3,3,3,3,3,3,3,3,3,3,3,3,3,3,3,3,3,3,3,3,3,3,3,3,3,
3,3,3,3,3,3,3,3,3,3,3,3,3,3,3,3,3,3,3,4),(-104.623713955068,-104.534906093999,
-104.446092177846,-104.357251749749,-104.266535133448,-104.177526827267,
-104.085956055905,-103.994385284543,-103.905835741282,-103.817401004262,
-103.729057265707,-103.637230016517,-103.548988692835,-103.460760827873,
-103.372525049885,-103.284259986557,-103.195894504504,-103.107469523442,
-103.018914094274,-102.994439272191,-102.90588972893,-102.817454991911,
-102.729111253356,-102.637284004166,-102.549042680484,-102.460814815522,
-102.372579037534,-102.284313974207,-102.195948492154,-102.107523511093,
-102.018968081925,-101.99449325984,-101.905943716579,-101.81750897956,-101.729165241005,
-101.637337991815,-101.549096668134,-101.460868803172,-101.372633025184,
-101.284367961857,-101.196002479804,-101.107577498743,-101.019022069575,
-100.994547247489,-100.905997704228,-100.817562967208,-100.729219228653,
-100.637391979464,-100.549150655781,-100.460922790819,-100.372687012831,
-100.284421949504,-100.19605646745,-100.107631486389,-100.019076057221,
-99.9946012351372,-99.9060516918764,-99.8176169548564,-99.7292732163011,
-99.6374459671117,-99.5492046434295,-99.4609767784672,-99.3727410004794,
-99.2844759371525,-99.1961104550991,-99.107685474038,-99.0191300448696,
-98.9946552227858,-98.905949860575,-98.8173584473077,-98.7288596647749,
-98.6404322712687,-98.5520521175381,-98.4636992979816,-98.3753378753946,
-98.3405286478881),.UNSPECIFIED.);
#281=B_SPLINE_CURVE_WITH_KNOTS('',3,(#29388,#29389,#29390,#29391,#29392,
#29393,#29394,#29395,#29396,#29397,#29398,#29399,#29400,#29401,#29402,#29403,
#29404,#29405,#29406,#29407,#29408,#29409,#29410,#29411,#29412,#29413,#29414,
#29415,#29416,#29417,#29418,#29419,#29420,#29421,#29422,#29423,#29424,#29425,
#29426,#29427,#29428,#29429,#29430,#29431,#29432,#29433,#29434,#29435,#29436,
#29437,#29438,#29439,#29440,#29441,#29442,#29443,#29444,#29445,#29446,#29447,
#29448,#29449,#29450,#29451,#29452,#29453,#29454,#29455,#29456,#29457,#29458,
#29459,#29460,#29461,#29462,#29463,#29464,#29465,#29466,#29467,#29468,#29469,
#29470,#29471,#29472,#29473,#29474,#29475,#29476,#29477,#29478,#29479,#29480,
#29481,#29482,#29483,#29484,#29485,#29486,#29487,#29488,#29489,#29490,#29491,
#29492,#29493,#29494,#29495,#29496,#29497,#29498,#29499,#29500,#29501,#29502,
#29503,#29504,#29505,#29506,#29507,#29508,#29509,#29510,#29511,#29512,#29513,
#29514,#29515,#29516,#29517,#29518,#29519,#29520,#29521,#29522,#29523,#29524,
#29525,#29526,#29527,#29528,#29529,#29530,#29531,#29532,#29533,#29534,#29535,
#29536,#29537,#29538,#29539,#29540,#29541,#29542,#29543,#29544,#29545,#29546,
#29547,#29548,#29549,#29550,#29551,#29552,#29553,#29554,#29555,#29556,#29557,
#29558,#29559,#29560,#29561,#29562,#29563,#29564,#29565,#29566,#29567,#29568,
#29569,#29570,#29571,#29572,#29573,#29574,#29575,#29576,#29577,#29578,#29579,
#29580,#29581,#29582,#29583,#29584,#29585,#29586,#29587,#29588,#29589,#29590,
#29591,#29592,#29593,#29594,#29595,#29596,#29597,#29598,#29599,#29600,#29601,
#29602,#29603,#29604,#29605,#29606,#29607,#29608,#29609,#29610,#29611,#29612,
#29613),.UNSPECIFIED.,.F.,.F.,(4,3,3,3,3,3,3,3,3,3,3,3,3,3,3,3,3,3,3,3,
3,3,3,3,3,3,3,3,3,3,3,3,3,3,3,3,3,3,3,3,3,3,3,3,3,3,3,3,3,3,3,3,3,3,3,3,
3,3,3,3,3,3,3,3,3,3,3,3,3,3,3,3,3,3,3,4),(-98.3405286476581,-98.2388278601938,
-98.1365688139642,-98.0336484171347,-97.9947092104345,-97.9061596671738,
-97.8177249301541,-97.7293811915989,-97.6375539424094,-97.5493126187274,
-97.4610847537654,-97.3728489757775,-97.2845839124504,-97.1962184303971,
-97.1077934493357,-97.0192380201675,-96.9947631980831,-96.9062136548223,
-96.8177789178026,-96.7294351792475,-96.637607930058,-96.549366606376,-96.4611387414139,
-96.3729029634261,-96.2846379000986,-96.1962724180453,-96.107847436984,
-96.0192920078157,-95.9948171857317,-95.906267642471,-95.8178329054513,
-95.7294891668962,-95.6376619177068,-95.5494205940248,-95.4611927290627,
-95.372956951075,-95.2846918877477,-95.1963264056944,-95.1079014246331,
-95.0193459954649,-94.9948711733804,-94.9063216301196,-94.8178868930999,
-94.7295431545448,-94.6377159053554,-94.5494745816733,-94.4612467167113,
-94.3730109387235,-94.2847458753962,-94.1963803933429,-94.1079554122816,
-94.0193999831134,-93.994925161029,-93.9063756177682,-93.8179408807485,
-93.7295971421934,-93.6377698930039,-93.5495285693218,-93.4613007043598,
-93.3730649263719,-93.2847998630446,-93.1964343809913,-93.10800939993,-93.0194539707618,
-92.9949791486776,-92.9072355423437,-92.8196060648545,-92.732066048324,
-92.6445893384008,-92.5571455235984,-92.4697124608468,-92.3822680202302,
-92.2947386999218,-92.207164380361,-92.1194565324101,-92.0573433407085),
 .UNSPECIFIED.);
#282=B_SPLINE_CURVE_WITH_KNOTS('',3,(#29615,#29616,#29617,#29618,#29619,
#29620,#29621,#29622,#29623,#29624,#29625),.UNSPECIFIED.,.F.,.F.,(4,1,1,
1,1,1,1,1,4),(-92.0573433407085,-91.9950331363262,-90.9950871239749,-89.9951411116235,
-88.9951950992721,-87.9952490869208,-86.9953030745694,-85.995357062218,
-85.7741580335289),.UNSPECIFIED.);
#283=B_SPLINE_CURVE_WITH_KNOTS('',3,(#29627,#29628,#29629,#29630,#29631,
#29632,#29633,#29634,#29635,#29636,#29637,#29638,#29639,#29640,#29641,#29642,
#29643,#29644,#29645,#29646,#29647,#29648,#29649,#29650,#29651,#29652,#29653,
#29654,#29655,#29656,#29657,#29658,#29659,#29660,#29661,#29662,#29663,#29664,
#29665,#29666,#29667,#29668,#29669,#29670,#29671,#29672,#29673,#29674,#29675,
#29676,#29677,#29678,#29679,#29680,#29681,#29682,#29683,#29684,#29685,#29686,
#29687,#29688,#29689,#29690,#29691,#29692,#29693,#29694,#29695,#29696,#29697,
#29698,#29699,#29700,#29701,#29702,#29703,#29704,#29705,#29706,#29707,#29708,
#29709,#29710,#29711,#29712,#29713,#29714,#29715,#29716,#29717,#29718,#29719,
#29720,#29721,#29722,#29723,#29724,#29725,#29726,#29727,#29728,#29729,#29730,
#29731,#29732,#29733,#29734,#29735,#29736,#29737,#29738,#29739,#29740,#29741,
#29742,#29743,#29744,#29745,#29746,#29747,#29748,#29749,#29750,#29751,#29752,
#29753,#29754,#29755,#29756,#29757,#29758,#29759,#29760,#29761,#29762,#29763,
#29764,#29765,#29766,#29767,#29768,#29769,#29770,#29771,#29772,#29773,#29774,
#29775,#29776,#29777,#29778,#29779,#29780,#29781,#29782,#29783,#29784,#29785,
#29786,#29787,#29788,#29789,#29790,#29791,#29792,#29793,#29794,#29795,#29796,
#29797,#29798,#29799,#29800,#29801,#29802,#29803,#29804,#29805,#29806,#29807,
#29808,#29809,#29810,#29811,#29812,#29813,#29814,#29815,#29816,#29817,#29818,
#29819,#29820,#29821,#29822,#29823,#29824,#29825,#29826,#29827,#29828,#29829,
#29830,#29831,#29832,#29833,#29834,#29835,#29836,#29837,#29838,#29839,#29840,
#29841,#29842,#29843,#29844,#29845,#29846,#29847,#29848,#29849,#29850,#29851,
#29852),.UNSPECIFIED.,.F.,.F.,(4,3,3,3,3,3,3,3,3,3,3,3,3,3,3,3,3,3,3,3,
3,3,3,3,3,3,3,3,3,3,3,3,3,3,3,3,3,3,3,3,3,3,3,3,3,3,3,3,3,3,3,3,3,3,3,3,
3,3,3,3,3,3,3,3,3,3,3,3,3,3,3,3,3,3,3,4),(-85.7741580335289,-85.6869940390936,
-85.5998987318649,-85.5128399462755,-85.4257952412113,-85.3387421916226,
-85.2516030644243,-85.1644212737914,-85.0770957414917,-84.9954110498666,
-84.9068615066059,-84.8184267695863,-84.7300830310311,-84.6382557818416,
-84.5500144581596,-84.4617865931975,-84.3735508152097,-84.2852857518826,
-84.1969202698293,-84.1084952887679,-84.0199398595997,-83.9954650375153,
-83.9069154942545,-83.8184807572348,-83.7301370186797,-83.6383097694902,
-83.5500684458081,-83.4618405808461,-83.3736048028584,-83.2853397395314,
-83.196974257478,-83.1085492764167,-83.0199938472485,-82.9955190251639,
-82.9069694819031,-82.8185347448832,-82.7301910063281,-82.6383637571386,
-82.5501224334565,-82.4618945684944,-82.3736587905064,-82.2853937271789,
-82.1970282451255,-82.1086032640641,-82.0200478348961,-81.9955730128125,
-81.9070234695518,-81.8185887325322,-81.730244993977,-81.6384177447876,
-81.5501764211055,-81.4619485561435,-81.3737127781559,-81.2854477148285,
-81.1970822327752,-81.1086572517138,-81.0201018225456,-80.9956270004612,
-80.9070774572005,-80.8186427201807,-80.7302989816257,-80.6384717324362,
-80.5502304087541,-80.462002543792,-80.3737667658043,-80.2855017024774,
-80.197136220424,-80.1087112393627,-80.0201558101946,-79.9956809881098,
-79.9027596067704,-79.8100048180451,-79.717462914801,-79.6250490832349,
-79.5327942325015,-79.4909727263493),.UNSPECIFIED.);
#284=B_SPLINE_CURVE_WITH_KNOTS('',3,(#29854,#29855,#29856,#29857,#29858,
#29859,#29860,#29861,#29862,#29863,#29864,#29865,#29866,#29867,#29868,#29869,
#29870,#29871,#29872,#29873,#29874,#29875,#29876,#29877,#29878,#29879,#29880,
#29881,#29882,#29883,#29884,#29885,#29886,#29887,#29888,#29889,#29890,#29891,
#29892,#29893,#29894,#29895,#29896,#29897,#29898,#29899,#29900,#29901,#29902,
#29903,#29904,#29905,#29906,#29907,#29908,#29909,#29910,#29911,#29912,#29913,
#29914,#29915,#29916,#29917,#29918,#29919,#29920,#29921,#29922,#29923,#29924,
#29925,#29926,#29927,#29928,#29929,#29930,#29931,#29932,#29933,#29934,#29935,
#29936,#29937,#29938,#29939,#29940,#29941,#29942,#29943,#29944,#29945,#29946,
#29947,#29948,#29949,#29950,#29951,#29952,#29953,#29954,#29955,#29956,#29957,
#29958,#29959,#29960,#29961,#29962,#29963,#29964,#29965,#29966,#29967,#29968,
#29969,#29970,#29971,#29972,#29973,#29974,#29975,#29976,#29977,#29978,#29979,
#29980,#29981,#29982,#29983,#29984,#29985,#29986,#29987,#29988,#29989,#29990,
#29991,#29992,#29993,#29994,#29995,#29996,#29997,#29998,#29999,#30000,#30001,
#30002,#30003,#30004,#30005,#30006,#30007,#30008,#30009,#30010,#30011,#30012,
#30013,#30014,#30015,#30016,#30017,#30018,#30019,#30020,#30021,#30022,#30023,
#30024,#30025,#30026,#30027,#30028,#30029,#30030,#30031,#30032,#30033,#30034,
#30035,#30036,#30037,#30038,#30039,#30040,#30041,#30042,#30043,#30044,#30045,
#30046,#30047,#30048,#30049,#30050,#30051,#30052,#30053,#30054,#30055,#30056,
#30057,#30058,#30059,#30060,#30061,#30062,#30063,#30064,#30065,#30066,#30067,
#30068,#30069,#30070,#30071,#30072,#30073,#30074,#30075,#30076,#30077,#30078,
#30079),.UNSPECIFIED.,.F.,.F.,(4,3,3,3,3,3,3,3,3,3,3,3,3,3,3,3,3,3,3,3,
3,3,3,3,3,3,3,3,3,3,3,3,3,3,3,3,3,3,3,3,3,3,3,3,3,3,3,3,3,3,3,3,3,3,3,3,
3,3,3,3,3,3,3,3,3,3,3,3,3,3,3,3,3,3,3,4),(-79.4909727261433,-79.3983623352896,
-79.3056157212193,-79.2126378190239,-79.1195318864591,-79.0262153902688,
-78.9957349757584,-78.9071854324977,-78.8187506954779,-78.7304069569228,
-78.6385797077333,-78.5503383840513,-78.4621105190892,-78.3738747411014,
-78.285609677774,-78.1972441957207,-78.1088192146593,-78.0202637854911,
-77.995788963407,-77.9072394201463,-77.8188046831266,-77.7304609445716,
-77.6386336953821,-77.5503923717001,-77.462164506738,-77.3739287287503,
-77.285663665423,-77.1972981833697,-77.1088732023084,-77.0203177731402,
-76.9958429510557,-76.907293407795,-76.8188586707753,-76.7305149322202,
-76.6386876830307,-76.5504463593487,-76.4622184943866,-76.3739827163988,
-76.2857176530715,-76.1973521710181,-76.1089271899568,-76.0203717607886,
-75.9958969387043,-75.9073473954435,-75.8189126584238,-75.7305689198687,
-75.6387416706792,-75.5505003469971,-75.4622724820351,-75.3740367040473,
-75.28577164072,-75.1974061586667,-75.1089811776053,-75.0204257484371,-74.9959509263529,
-74.9074013830922,-74.8189666460725,-74.7306229075175,-74.638795658328,
-74.550554334646,-74.462326469684,-74.3740906916963,-74.285825628369,-74.1974601463157,
-74.1090351652543,-74.0204797360861,-73.9960049140016,-73.9086913845972,
-73.8210783889188,-73.7339828174008,-73.6469435929607,-73.5599382140351,
-73.4719005153187,-73.3848666078328,-73.2963270135013,-73.2077874191697),
 .UNSPECIFIED.);
#285=B_SPLINE_CURVE_WITH_KNOTS('',3,(#30081,#30082,#30083,#30084,#30085,
#30086,#30087,#30088,#30089,#30090,#30091),.UNSPECIFIED.,.F.,.F.,(4,1,1,
1,1,1,1,1,4),(-73.2077874191697,-72.9960589016502,-71.9961128892988,-70.9961668769474,
-69.9962208645961,-68.9962748522447,-67.9963288398933,-66.9963828275419,
-66.9246021119901),.UNSPECIFIED.);
#286=B_SPLINE_CURVE_WITH_KNOTS('',3,(#30093,#30094,#30095,#30096,#30097,
#30098,#30099,#30100,#30101,#30102,#30103,#30104,#30105,#30106,#30107,#30108,
#30109,#30110,#30111,#30112,#30113,#30114,#30115,#30116,#30117,#30118,#30119,
#30120,#30121,#30122,#30123,#30124,#30125,#30126,#30127,#30128,#30129,#30130,
#30131,#30132,#30133,#30134,#30135,#30136,#30137,#30138,#30139,#30140,#30141,
#30142,#30143,#30144,#30145,#30146,#30147,#30148,#30149,#30150,#30151,#30152,
#30153,#30154,#30155,#30156,#30157,#30158,#30159,#30160,#30161,#30162,#30163,
#30164,#30165,#30166,#30167,#30168,#30169,#30170,#30171,#30172,#30173,#30174,
#30175,#30176,#30177,#30178,#30179,#30180,#30181,#30182,#30183,#30184,#30185,
#30186,#30187,#30188,#30189,#30190,#30191,#30192,#30193,#30194,#30195,#30196,
#30197,#30198,#30199,#30200,#30201,#30202,#30203,#30204,#30205,#30206,#30207,
#30208,#30209,#30210,#30211,#30212,#30213,#30214,#30215,#30216,#30217,#30218,
#30219,#30220,#30221,#30222,#30223,#30224,#30225,#30226,#30227,#30228,#30229,
#30230,#30231,#30232,#30233,#30234,#30235,#30236,#30237,#30238,#30239,#30240,
#30241,#30242,#30243,#30244,#30245,#30246,#30247,#30248,#30249,#30250,#30251,
#30252,#30253,#30254,#30255,#30256,#30257,#30258,#30259,#30260,#30261,#30262,
#30263,#30264,#30265,#30266,#30267,#30268,#30269,#30270,#30271,#30272,#30273,
#30274,#30275,#30276,#30277,#30278,#30279,#30280,#30281,#30282,#30283,#30284,
#30285,#30286,#30287,#30288,#30289,#30290,#30291,#30292,#30293,#30294,#30295,
#30296,#30297,#30298,#30299,#30300,#30301,#30302,#30303,#30304,#30305,#30306,
#30307,#30308,#30309,#30310,#30311,#30312,#30313,#30314,#30315,#30316,#30317,
#30318),.UNSPECIFIED.,.F.,.F.,(4,3,3,3,3,3,3,3,3,3,3,3,3,3,3,3,3,3,3,3,
3,3,3,3,3,3,3,3,3,3,3,3,3,3,3,3,3,3,3,3,3,3,3,3,3,3,3,3,3,3,3,3,3,3,3,3,
3,3,3,3,3,3,3,3,3,3,3,3,3,3,3,3,3,3,3,4),(-66.9246021119901,-66.8369765253447,
-66.7494590597405,-66.6620249933431,-66.5746452757939,-66.4872927329728,
-66.3999451562261,-66.312580345127,-66.225123600006,-66.1376166205138,-66.0499731462281,
-65.9964368151906,-65.9078872719299,-65.8194525349102,-65.731108796355,
-65.6392815471655,-65.5510402234834,-65.4628123585214,-65.3745765805337,
-65.2863115172062,-65.1979460351529,-65.1095210540915,-65.0209656249233,
-64.9964908028392,-64.9079412595785,-64.8195065225587,-64.7311627840035,
-64.6393355348141,-64.5510942111319,-64.4628663461699,-64.3746305681822,
-64.2863655048552,-64.1980000228018,-64.1095750417404,-64.0210196125721,
-63.9965447904878,-63.907995247227,-63.8195605102072,-63.7312167716523,
-63.6393895224628,-63.5511481987807,-63.4629203338186,-63.3746845558308,
-63.2864194925035,-63.1980540104502,-63.1096290293892,-63.021073600221,
-62.9965987781364,-62.9080492348756,-62.819614497856,-62.7312707593011,
-62.6394435101116,-62.5512021864295,-62.4629743214675,-62.3747385434799,
-62.2864734801525,-62.1981079980991,-62.1096830170379,-62.0211275878698,
-61.9966527657851,-61.9081032225242,-61.8196684855045,-61.731324746949,
-61.6394974977596,-61.5512561740775,-61.4630283091153,-61.3747925311274,
-61.2865274678006,-61.1981619857472,-61.1097370046858,-61.0211815755178,
-60.9967067534337,-60.8947512781198,-60.7932032283243,-60.6923996642118,
-60.6414170517604),.UNSPECIFIED.);
#287=B_SPLINE_CURVE_WITH_KNOTS('',3,(#30320,#30321,#30322,#30323,#30324,
#30325,#30326,#30327,#30328,#30329),.UNSPECIFIED.,.F.,.F.,(4,1,1,1,1,1,
1,4),(-60.6414168048105,-59.9967607410823,-58.996814728731,-57.9968687163796,
-56.9969227040282,-55.9969766916768,-54.9970306793255,-54.3582314976309),
 .UNSPECIFIED.);
#288=B_SPLINE_CURVE_WITH_KNOTS('',3,(#30331,#30332,#30333,#30334,#30335,
#30336,#30337,#30338,#30339,#30340),.UNSPECIFIED.,.F.,.F.,(4,1,1,1,1,1,
1,4),(-54.3582314976309,-53.9970846669741,-52.9971386546227,-51.9971926422714,
-50.99724662992,-49.9973006175686,-48.9973546052172,-48.0750546059844),
 .UNSPECIFIED.);
#289=B_SPLINE_CURVE_WITH_KNOTS('',3,(#30342,#30343,#30344,#30345,#30346,
#30347,#30348,#30349,#30350,#30351,#30352,#30353,#30354,#30355,#30356,#30357,
#30358,#30359,#30360,#30361,#30362,#30363,#30364,#30365,#30366,#30367,#30368,
#30369,#30370,#30371,#30372,#30373,#30374,#30375,#30376,#30377,#30378,#30379,
#30380,#30381,#30382,#30383,#30384,#30385,#30386,#30387,#30388,#30389,#30390,
#30391,#30392,#30393,#30394,#30395,#30396,#30397,#30398,#30399,#30400,#30401,
#30402,#30403,#30404,#30405,#30406,#30407,#30408,#30409,#30410,#30411,#30412,
#30413,#30414,#30415,#30416,#30417,#30418,#30419,#30420,#30421,#30422,#30423,
#30424,#30425,#30426,#30427,#30428,#30429,#30430,#30431,#30432,#30433,#30434,
#30435,#30436,#30437,#30438,#30439,#30440,#30441,#30442,#30443,#30444,#30445,
#30446,#30447,#30448,#30449,#30450,#30451,#30452,#30453,#30454,#30455,#30456,
#30457,#30458,#30459,#30460,#30461,#30462,#30463,#30464,#30465,#30466,#30467,
#30468,#30469,#30470,#30471,#30472,#30473,#30474,#30475,#30476,#30477,#30478,
#30479,#30480,#30481,#30482,#30483,#30484,#30485,#30486,#30487,#30488,#30489,
#30490,#30491,#30492,#30493,#30494,#30495,#30496,#30497,#30498,#30499,#30500,
#30501,#30502,#30503,#30504,#30505,#30506,#30507,#30508,#30509,#30510,#30511,
#30512,#30513,#30514,#30515,#30516,#30517,#30518,#30519,#30520,#30521,#30522,
#30523,#30524,#30525,#30526,#30527,#30528,#30529,#30530,#30531,#30532,#30533,
#30534,#30535,#30536,#30537,#30538,#30539,#30540,#30541,#30542,#30543,#30544,
#30545,#30546,#30547,#30548,#30549,#30550,#30551,#30552,#30553,#30554,#30555,
#30556,#30557,#30558,#30559,#30560,#30561,#30562,#30563,#30564,#30565,#30566,
#30567),.UNSPECIFIED.,.F.,.F.,(4,3,3,3,3,3,3,3,3,3,3,3,3,3,3,3,3,3,3,3,
3,3,3,3,3,3,3,3,3,3,3,3,3,3,3,3,3,3,3,3,3,3,3,3,3,3,3,3,3,3,3,3,3,3,3,3,
3,3,3,3,3,3,3,3,3,3,3,3,3,3,3,3,3,3,3,4),(-48.0750461904513,-47.9974085928659,
-47.9088590496049,-47.820424312585,-47.7320805740297,-47.6402533248403,
-47.552012001158,-47.4637841361958,-47.3755483582077,-47.2872832948801,
-47.1989178128266,-47.1104928317649,-47.0219374025965,-46.9974625805145,
-46.9089130372538,-46.8204783002341,-46.732134561679,-46.6403073124895,
-46.5520659888075,-46.4638381238455,-46.3756023458578,-46.2873372825305,
-46.1989718004772,-46.1105468194159,-46.0219913902478,-45.9975165681631,
-45.9089670249024,-45.8205322878828,-45.7321885493277,-45.6403613001382,
-45.5521199764563,-45.4638921114943,-45.3756563335065,-45.2873912701792,
-45.1990257881259,-45.1106008070647,-45.0220453778966,-44.9975705558118,
-44.909021012551,-44.8205862755313,-44.7322425369762,-44.6404152877867,
-44.5521739641047,-44.4639460991426,-44.3757103211548,-44.2874452578275,
-44.1990797757741,-44.1106547947128,-44.0220993655446,-43.9976245434604,
-43.9090750001997,-43.82064026318,-43.7322965246249,-43.6404692754354,-43.5522279517533,
-43.4640000867913,-43.3757643088036,-43.2874992454762,-43.1991337634229,
-43.1107087823616,-43.0221533531934,-42.997678531109,-42.9091289878483,
-42.8206942508286,-42.7323505122735,-42.6405232630841,-42.552281939402,
-42.46405407444,-42.3758182964522,-42.287553233125,-42.1991877510717,-42.1107627700105,
-42.0222073408422,-41.9977325187576,-41.8724138615788,-41.7918608832717),
 .UNSPECIFIED.);
#290=B_SPLINE_CURVE_WITH_KNOTS('',3,(#30569,#30570,#30571,#30572,#30573,
#30574,#30575,#30576,#30577,#30578,#30579,#30580,#30581,#30582,#30583,#30584,
#30585,#30586,#30587,#30588,#30589,#30590,#30591,#30592,#30593,#30594,#30595,
#30596,#30597,#30598,#30599,#30600,#30601,#30602,#30603,#30604,#30605,#30606,
#30607,#30608,#30609,#30610,#30611,#30612,#30613,#30614,#30615,#30616,#30617,
#30618,#30619,#30620,#30621,#30622,#30623,#30624,#30625,#30626,#30627,#30628,
#30629,#30630,#30631,#30632,#30633,#30634,#30635,#30636,#30637,#30638,#30639,
#30640,#30641,#30642,#30643,#30644,#30645,#30646,#30647,#30648,#30649,#30650,
#30651,#30652,#30653,#30654,#30655,#30656,#30657,#30658,#30659,#30660,#30661,
#30662,#30663,#30664,#30665,#30666,#30667,#30668,#30669,#30670,#30671,#30672,
#30673,#30674,#30675,#30676,#30677,#30678,#30679,#30680,#30681,#30682,#30683,
#30684,#30685,#30686,#30687,#30688,#30689,#30690,#30691,#30692,#30693,#30694,
#30695,#30696,#30697,#30698,#30699,#30700,#30701,#30702,#30703,#30704,#30705,
#30706,#30707,#30708,#30709,#30710,#30711,#30712,#30713,#30714,#30715,#30716,
#30717,#30718,#30719,#30720,#30721,#30722,#30723,#30724,#30725,#30726,#30727,
#30728,#30729,#30730,#30731,#30732,#30733,#30734,#30735,#30736,#30737,#30738,
#30739,#30740,#30741,#30742,#30743,#30744,#30745,#30746,#30747,#30748,#30749,
#30750,#30751,#30752,#30753,#30754,#30755,#30756,#30757,#30758,#30759,#30760,
#30761,#30762,#30763,#30764,#30765,#30766,#30767,#30768,#30769,#30770,#30771,
#30772,#30773,#30774,#30775,#30776,#30777,#30778,#30779,#30780,#30781,#30782,
#30783,#30784,#30785,#30786,#30787,#30788,#30789,#30790,#30791,#30792,#30793,
#30794),.UNSPECIFIED.,.F.,.F.,(4,3,3,3,3,3,3,3,3,3,3,3,3,3,3,3,3,3,3,3,
3,3,3,3,3,3,3,3,3,3,3,3,3,3,3,3,3,3,3,3,3,3,3,3,3,3,3,3,3,3,3,3,3,3,3,3,
3,3,3,3,3,3,3,3,3,3,3,3,3,3,3,3,3,3,3,4),(-41.7918608831318,-41.7047406880879,
-41.6163714153777,-41.5293687538345,-41.442384448814,-41.3553960300837,
-41.2659936491644,-41.1788817051822,-41.0883341057943,-40.9977865064063,
-40.9092369631456,-40.8208022261259,-40.732458487571,-40.6406312383815,
-40.5523899146994,-40.4641620497374,-40.3759262717495,-40.2876612084222,
-40.1992957263689,-40.1108707453076,-40.0223153161394,-39.9978404940549,
-39.9092909507942,-39.8208562137744,-39.7325124752191,-39.6406852260297,
-39.5524439023476,-39.4642160373855,-39.3759802593978,-39.2877151960708,
-39.1993497140176,-39.1109247329563,-39.0223693037881,-38.9978944817035,
-38.9093449384427,-38.8209102014229,-38.7325664628676,-38.6407392136782,
-38.5524978899962,-38.4642700250342,-38.3760342470463,-38.2877691837193,
-38.1994037016659,-38.1109787206049,-38.0224232914369,-37.9979484693521,
-37.9093989260914,-37.8209641890717,-37.7326204505165,-37.6407932013271,
-37.552551877645,-37.4643240126829,-37.3760882346953,-37.2878231713679,
-37.1994576893146,-37.1110327082532,-37.022477279085,-36.9980024570008,
-36.9094529137401,-36.8210181767205,-36.7326744381654,-36.6408471889759,
-36.5526058652939,-36.464378000332,-36.3761422223444,-36.2878771590168,
-36.1995116769635,-36.1110866959022,-36.0225312667339,-35.9980564446494,
-35.9044859724487,-35.8110931478129,-35.717933086428,-35.6249158515222,
-35.5320788066918,-35.5086755763231),.UNSPECIFIED.);
#291=B_SPLINE_CURVE_WITH_KNOTS('',3,(#30796,#30797,#30798,#30799,#30800,
#30801,#30802,#30803,#30804,#30805,#30806,#30807,#30808,#30809,#30810,#30811,
#30812,#30813,#30814,#30815,#30816,#30817,#30818,#30819,#30820,#30821,#30822,
#30823,#30824,#30825,#30826,#30827,#30828,#30829,#30830,#30831,#30832,#30833,
#30834,#30835,#30836,#30837,#30838,#30839,#30840,#30841,#30842,#30843,#30844,
#30845,#30846,#30847,#30848,#30849,#30850,#30851,#30852,#30853,#30854,#30855,
#30856,#30857,#30858,#30859,#30860,#30861,#30862,#30863,#30864,#30865,#30866,
#30867,#30868,#30869,#30870,#30871,#30872,#30873,#30874,#30875,#30876,#30877,
#30878,#30879,#30880,#30881,#30882,#30883,#30884,#30885,#30886,#30887,#30888,
#30889,#30890,#30891,#30892,#30893,#30894,#30895,#30896,#30897,#30898,#30899,
#30900,#30901,#30902,#30903,#30904,#30905,#30906,#30907,#30908,#30909,#30910,
#30911,#30912,#30913,#30914,#30915,#30916,#30917,#30918,#30919,#30920,#30921,
#30922,#30923,#30924,#30925,#30926,#30927,#30928,#30929,#30930,#30931,#30932,
#30933,#30934,#30935,#30936,#30937,#30938,#30939,#30940,#30941,#30942,#30943,
#30944,#30945,#30946,#30947,#30948,#30949,#30950,#30951,#30952,#30953,#30954,
#30955,#30956,#30957,#30958,#30959,#30960,#30961,#30962,#30963,#30964,#30965,
#30966,#30967,#30968,#30969,#30970,#30971,#30972,#30973,#30974,#30975,#30976,
#30977,#30978,#30979,#30980,#30981,#30982,#30983,#30984,#30985,#30986,#30987,
#30988,#30989,#30990,#30991,#30992,#30993,#30994,#30995,#30996,#30997,#30998,
#30999,#31000,#31001,#31002,#31003,#31004,#31005,#31006,#31007,#31008,#31009,
#31010,#31011,#31012,#31013,#31014,#31015,#31016,#31017,#31018,#31019,#31020,
#31021),.UNSPECIFIED.,.F.,.F.,(4,3,3,3,3,3,3,3,3,3,3,3,3,3,3,3,3,3,3,3,
3,3,3,3,3,3,3,3,3,3,3,3,3,3,3,3,3,3,3,3,3,3,3,3,3,3,3,3,3,3,3,3,3,3,3,3,
3,3,3,3,3,3,3,3,3,3,3,3,3,3,3,3,3,3,3,4),(-35.5086755760921,-35.4166443511499,
-35.3244992203645,-35.2321443196328,-35.1396757545066,-35.0470006032941,
-34.998110432298,-34.9095608890373,-34.8211261520178,-34.7327824134629,
-34.6409551642734,-34.5527138405915,-34.4644859756297,-34.3762501976422,
-34.2879851343154,-34.1996196522622,-34.111194671201,-34.022639242033,-33.9981644199467,
-33.9096148766864,-33.8211801396674,-33.7328364011129,-33.6410091519232,
-33.5527678282416,-33.4645399632801,-33.3763041852927,-33.2880391219658,
-33.199673639913,-33.1112486588522,-33.0226932296844,-32.9982184075953,
-32.909668864333,-32.8212341273119,-32.7328903887551,-32.6410631395662,
-32.5528218158826,-32.4645939509191,-32.3763581729298,-32.2880931096009,
-32.1997276275461,-32.1113026464833,-32.0227472173137,-31.9982723952439,
-31.9097228519846,-31.8212881149664,-31.7329443764129,-31.6411171272228,
-31.5528758035421,-31.4646479385814,-31.3764121605949,-31.2881470972685,
-31.1997816152164,-31.1113566341565,-31.0228012049898,-30.9983263828925,
-30.9097768396345,-30.8213421026175,-30.7329983640648,-30.6411711148743,
-30.552929791195,-30.4647019262356,-30.3764661482503,-30.2882010849253,
-30.1998356028746,-30.1114106218163,-30.0228551926506,-29.9983803705412,
-29.9109940179612,-29.8237474432069,-29.7365806384812,-29.6494710931914,
-29.5623963544676,-29.4753042131104,-29.3882064147977,-29.3010292666083,
-29.2254902689126),.UNSPECIFIED.);
#292=B_SPLINE_CURVE_WITH_KNOTS('',3,(#31023,#31024,#31025,#31026,#31027,
#31028,#31029,#31030,#31031,#31032,#31033),.UNSPECIFIED.,.F.,.F.,(4,1,1,
1,1,1,1,1,4),(-29.2254902689126,-28.9984343581898,-27.9984883458384,-26.9985423334871,
-25.9985963211357,-24.9986503087843,-23.9987042964329,-22.9987582840816,
-22.942304961733),.UNSPECIFIED.);
#293=B_SPLINE_CURVE_WITH_KNOTS('',3,(#31035,#31036,#31037,#31038,#31039,
#31040,#31041,#31042,#31043,#31044,#31045,#31046,#31047,#31048,#31049,#31050,
#31051,#31052,#31053,#31054,#31055,#31056,#31057,#31058,#31059,#31060,#31061,
#31062,#31063,#31064,#31065,#31066,#31067,#31068,#31069,#31070,#31071,#31072,
#31073,#31074,#31075,#31076,#31077,#31078,#31079,#31080,#31081,#31082,#31083,
#31084,#31085,#31086,#31087,#31088,#31089,#31090,#31091,#31092,#31093,#31094,
#31095,#31096,#31097,#31098,#31099,#31100,#31101,#31102,#31103,#31104,#31105,
#31106,#31107,#31108,#31109,#31110,#31111,#31112,#31113,#31114,#31115,#31116,
#31117,#31118,#31119,#31120,#31121,#31122,#31123,#31124,#31125,#31126,#31127,
#31128,#31129,#31130,#31131,#31132,#31133,#31134,#31135,#31136,#31137,#31138,
#31139,#31140,#31141,#31142,#31143,#31144,#31145,#31146,#31147,#31148,#31149,
#31150,#31151,#31152,#31153,#31154,#31155,#31156,#31157,#31158,#31159,#31160,
#31161,#31162,#31163,#31164,#31165,#31166,#31167,#31168,#31169,#31170,#31171,
#31172,#31173,#31174,#31175,#31176,#31177,#31178,#31179,#31180,#31181,#31182,
#31183,#31184,#31185,#31186,#31187,#31188,#31189,#31190,#31191,#31192,#31193,
#31194,#31195,#31196,#31197,#31198,#31199,#31200,#31201,#31202,#31203,#31204,
#31205,#31206,#31207,#31208,#31209,#31210,#31211,#31212,#31213,#31214,#31215,
#31216,#31217,#31218,#31219,#31220,#31221,#31222,#31223,#31224,#31225,#31226,
#31227,#31228,#31229,#31230,#31231,#31232,#31233,#31234,#31235,#31236,#31237,
#31238,#31239,#31240,#31241,#31242,#31243,#31244,#31245,#31246,#31247,#31248,
#31249,#31250,#31251,#31252,#31253,#31254,#31255,#31256,#31257,#31258,#31259,
#31260),.UNSPECIFIED.,.F.,.F.,(4,3,3,3,3,3,3,3,3,3,3,3,3,3,3,3,3,3,3,3,
3,3,3,3,3,3,3,3,3,3,3,3,3,3,3,3,3,3,3,3,3,3,3,3,3,3,3,3,3,3,3,3,3,3,3,3,
3,3,3,3,3,3,3,3,3,3,3,3,3,3,3,3,3,3,3,4),(-22.942304961733,-22.8545209046868,
-22.766847257432,-22.6792594249928,-22.5917293086245,-22.5042287777375,
-22.4167357403712,-22.3292281149642,-22.2416295280414,-22.1539833092983,
-22.0661961744187,-21.9988122717302,-21.9102627285941,-21.8218279917067,
-21.7334842532916,-21.6416570040525,-21.5534156805278,-21.4651878157292,
-21.3769520379107,-21.2886869747587,-21.2003214928881,-21.1118965120143,
-21.0233410830385,-20.9988662593788,-20.9103167128181,-20.8218819724869,
-20.7335382306125,-20.6417109826644,-20.5534696556644,-20.4652417873905,
-20.3770060061005,-20.2887409394836,-20.2003754541768,-20.1119504698788,
-20.0233950375239,-19.9989202470274,-19.9103707101465,-19.8219359795026,
-19.733592247312,-19.6417649957325,-19.5535236783475,-19.4652958196472,
-19.3770600478799,-19.2887949907244,-19.2004295147407,-19.1120045396972,
-19.0234491164242,-18.9989742346761,-18.9104246903274,-18.8219899522712,
-18.7336462127319,-18.641818963931,-18.5535776393991,-18.465349773638,-18.3771139949023,
-18.2888489308791,-18.2004834482097,-18.1120584665778,-18.02350303691,-17.9990282223247,
-17.9104786578628,-17.8220438995504,-17.7337001396359,-17.6418728984281,
-17.5536315533559,-17.4654036670284,-17.377167867722,-17.2889027831457,
-17.2005372800539,-17.1121122780503,-17.0235568282441,-16.9990822099733,
-16.8956727885515,-16.7927418059338,-16.6906685903549,-16.6591196547798),
 .UNSPECIFIED.);
#294=B_SPLINE_CURVE_WITH_KNOTS('',3,(#31262,#31263,#31264,#31265,#31266,
#31267,#31268,#31269,#31270,#31271,#31272,#31273,#31274,#31275,#31276,#31277,
#31278,#31279,#31280,#31281,#31282,#31283,#31284,#31285,#31286,#31287,#31288,
#31289,#31290,#31291,#31292,#31293,#31294,#31295,#31296,#31297,#31298,#31299,
#31300,#31301,#31302,#31303,#31304,#31305,#31306,#31307,#31308,#31309,#31310,
#31311,#31312,#31313,#31314,#31315,#31316,#31317,#31318,#31319,#31320,#31321,
#31322,#31323,#31324,#31325,#31326,#31327,#31328,#31329,#31330,#31331,#31332,
#31333,#31334,#31335,#31336,#31337,#31338,#31339,#31340,#31341,#31342,#31343,
#31344,#31345,#31346,#31347,#31348,#31349,#31350,#31351,#31352,#31353,#31354,
#31355,#31356,#31357,#31358,#31359,#31360,#31361,#31362,#31363,#31364,#31365,
#31366,#31367,#31368,#31369,#31370,#31371,#31372,#31373,#31374,#31375,#31376,
#31377,#31378,#31379,#31380,#31381,#31382,#31383,#31384,#31385,#31386,#31387,
#31388,#31389,#31390,#31391,#31392,#31393,#31394,#31395,#31396,#31397,#31398,
#31399,#31400,#31401,#31402,#31403,#31404,#31405,#31406,#31407,#31408,#31409,
#31410,#31411,#31412,#31413,#31414,#31415,#31416,#31417,#31418,#31419,#31420,
#31421,#31422,#31423,#31424,#31425,#31426,#31427,#31428,#31429,#31430,#31431,
#31432,#31433,#31434,#31435,#31436,#31437,#31438,#31439,#31440,#31441,#31442,
#31443,#31444,#31445,#31446,#31447,#31448,#31449,#31450,#31451,#31452,#31453,
#31454,#31455,#31456,#31457,#31458,#31459,#31460,#31461,#31462,#31463,#31464,
#31465,#31466,#31467,#31468,#31469,#31470,#31471,#31472,#31473,#31474,#31475,
#31476,#31477,#31478,#31479,#31480,#31481,#31482,#31483,#31484,#31485,#31486,
#31487),.UNSPECIFIED.,.F.,.F.,(4,3,3,3,3,3,3,3,3,3,3,3,3,3,3,3,3,3,3,3,
3,3,3,3,3,3,3,3,3,3,3,3,3,3,3,3,3,3,3,3,3,3,3,3,3,3,3,3,3,3,3,3,3,3,3,3,
3,3,3,3,3,3,3,3,3,3,3,3,3,3,3,3,3,3,3,4),(-16.6591196545534,-16.5708424404528,
-16.4825762959745,-16.3942999901969,-16.3059922899729,-16.2175771928198,
-16.12910117663,-16.0404827781768,-15.999136197622,-15.9105866329858,-15.8221518749269,
-15.7338081156886,-15.6419808743863,-15.5537395310261,-15.4655116467871,
-15.3772758499421,-15.2890107681959,-15.200645268462,-15.112220270127,-15.0236648244138,
-14.9991901852706,-14.9106405100812,-14.8222056404348,-14.7338617687161,
-14.6420345692415,-14.553793111893,-14.4655651133053,-14.3773292018738,
-14.2890640054263,-14.2006983914055,-14.1122732788836,-14.0237177200223,
-13.9992441729192,-13.910694981617,-13.8222605967651,-13.7339172101825,
-13.6420898289807,-13.5538488546178,-13.4656213374149,-13.3773859052664,
-13.2891211854972,-13.2007560418992,-13.1123313967461,-13.0237762971454,
-12.9992981605678,-12.9107483730229,-12.8223133938516,-12.7339694155237,
-12.6421422571103,-12.5539007010024,-12.4656726066969,-12.3774366026758,
-12.2891713168544,-12.2008056186421,-12.1123804248366,-12.023824789566,
-11.9993521482165,-11.9108018171415,-11.8223662871184,-11.7340217513491,
-11.6421947994136,-11.5539526730479,-11.4657240047502,-11.3774874236279,
-11.2892215582218,-11.2008552797222,-11.1124295045045,-11.0238732907307,
-10.9994061358651,-10.9100993890415,-10.8209123500255,-10.7318245035481,
-10.6428246466122,-10.5538777775384,-10.4649060624561,-10.3759343473738),
 .UNSPECIFIED.);
#295=B_SPLINE_CURVE_WITH_KNOTS('',3,(#31488,#31489,#31490,#31491,#31492,
#31493,#31494,#31495,#31496,#31497),.UNSPECIFIED.,.F.,.F.,(4,1,1,1,1,1,
1,4),(-10.3759267393627,-9.99946012351372,-8.99951411116235,-7.99956809881098,
-6.99962208645961,-5.99967607410823,-4.99973006175686,-4.0927579581402),
 .UNSPECIFIED.);
#296=B_SPLINE_CURVE_WITH_KNOTS('',3,(#31500,#31501,#31502,#31503,#31504,
#31505,#31506,#31507,#31508,#31509,#31510,#31511,#31512,#31513,#31514,#31515,
#31516,#31517,#31518,#31519,#31520,#31521,#31522,#31523,#31524,#31525,#31526,
#31527,#31528,#31529,#31530,#31531,#31532,#31533,#31534,#31535,#31536,#31537,
#31538,#31539,#31540,#31541,#31542,#31543,#31544,#31545,#31546,#31547,#31548,
#31549,#31550,#31551,#31552,#31553,#31554,#31555,#31556,#31557,#31558,#31559,
#31560,#31561,#31562,#31563,#31564,#31565,#31566,#31567,#31568,#31569,#31570,
#31571,#31572,#31573,#31574,#31575,#31576,#31577,#31578,#31579,#31580,#31581,
#31582,#31583,#31584,#31585,#31586,#31587,#31588,#31589,#31590,#31591,#31592,
#31593,#31594,#31595,#31596,#31597,#31598,#31599,#31600,#31601,#31602,#31603,
#31604,#31605,#31606,#31607,#31608,#31609,#31610,#31611,#31612,#31613,#31614,
#31615,#31616,#31617,#31618,#31619,#31620,#31621,#31622,#31623,#31624,#31625,
#31626,#31627,#31628,#31629,#31630,#31631,#31632,#31633,#31634,#31635,#31636,
#31637,#31638,#31639,#31640,#31641,#31642,#31643),.UNSPECIFIED.,.F.,.F.,
(4,2,2,2,2,2,2,2,2,2,2,2,2,2,2,2,2,2,2,2,2,2,2,2,2,2,2,2,2,2,2,2,2,2,2,
2,2,2,2,2,2,2,2,2,2,2,2,2,2,2,2,2,2,2,2,2,2,2,2,2,2,2,2,2,2,2,2,2,2,2,2,
4),(0.00584549622467335,0.093405921375881,0.130454269801855,0.139587899175375,
0.143701679159035,0.14678824815488,0.149686852724838,0.153705523253871,
0.164128408972305,0.241981531619902,0.268158297474372,0.296705073611049,
0.300784772366485,0.302502481570271,0.304210123261048,0.306047999034772,
0.309016606254543,0.318500512927684,0.399678224516204,0.447309111008664,
0.457678111996666,0.461978384339338,0.465070615966961,0.467881648682991,
0.47234354095253,0.482917709960205,0.564585567652315,0.60372389239076,0.620985267235939,
0.624516669834605,0.626478597891468,0.628151253543898,0.630258357458671,
0.634388810107199,0.660936540551689,0.736613518874363,0.763293960149108,
0.779708437347709,0.784796539914734,0.788025127073784,0.791034488430205,
0.794957245692005,0.801548971967704,0.852690893089723,0.928853038104393,
0.944722661187104,0.948144328498009,0.950070510781237,0.951745318861767,
0.953888164862695,0.958296575900975,1.01437647864604,1.05723809872353,1.08588504932026,
1.10319606995781,1.10841393049374,1.11169193141533,1.11472499158421,1.11864735127438,
1.12517099269234,1.17139366649591,1.23724911591007,1.25690874508622,1.26426889979486,
1.26959469417094,1.2719145215793,1.27362093904285,1.27547544412718,1.27852147831721,
1.2882877783795,1.36961643020412,1.36975430456593),.UNSPECIFIED.);
#297=B_SPLINE_CURVE_WITH_KNOTS('',3,(#31647,#31648,#31649,#31650,#31651,
#31652,#31653,#31654,#31655,#31656,#31657,#31658,#31659,#31660,#31661,#31662,
#31663,#31664,#31665,#31666,#31667,#31668,#31669,#31670,#31671,#31672,#31673,
#31674,#31675,#31676,#31677),.UNSPECIFIED.,.F.,.F.,(4,3,3,3,3,3,3,3,3,3,
4),(185.353966561968,185.448794091205,185.543475335336,185.638681286969,
185.733128562177,185.827512446235,185.921855079479,186.01767204671,186.112024247931,
186.208573598167,186.305122948402),.UNSPECIFIED.);
#298=B_SPLINE_CURVE_WITH_KNOTS('',3,(#31678,#31679,#31680,#31681,#31682,
#31683,#31684,#31685,#31686,#31687,#31688,#31689,#31690,#31691,#31692,#31693,
#31694,#31695,#31696,#31697,#31698,#31699,#31700,#31701,#31702,#31703,#31704,
#31705,#31706,#31707,#31708,#31709,#31710,#31711,#31712,#31713,#31714,#31715,
#31716,#31717,#31718,#31719,#31720,#31721,#31722,#31723,#31724,#31725,#31726,
#31727,#31728,#31729,#31730,#31731,#31732,#31733,#31734,#31735,#31736,#31737,
#31738,#31739,#31740,#31741,#31742,#31743,#31744,#31745,#31746,#31747),
 .UNSPECIFIED.,.F.,.F.,(4,3,3,3,3,3,3,3,3,3,3,3,3,3,3,3,3,3,3,3,3,3,3,4),
(183.307775588641,183.400962019436,183.494025064816,183.58699217182,183.679894571268,
183.772763733289,183.865624323015,183.95850099185,184.051477988904,184.1445079511,
184.237692355435,184.3052309237,184.397302867067,184.489248064613,184.581095274411,
184.672879103481,184.764630581829,184.856375514756,184.948139696577,185.04001655256,
185.131950850016,185.224060472127,185.305176936051,185.353966561798),
 .UNSPECIFIED.);
#299=B_SPLINE_CURVE_WITH_KNOTS('',3,(#32472,#32473,#32474,#32475,#32476,
#32477,#32478,#32479,#32480,#32481,#32482,#32483,#32484,#32485,#32486,#32487,
#32488,#32489,#32490,#32491,#32492,#32493,#32494,#32495,#32496,#32497,#32498,
#32499,#32500,#32501,#32502,#32503,#32504,#32505,#32506,#32507,#32508,#32509,
#32510,#32511,#32512,#32513,#32514,#32515,#32516,#32517,#32518,#32519,#32520,
#32521,#32522,#32523,#32524,#32525,#32526,#32527,#32528,#32529,#32530,#32531,
#32532,#32533,#32534,#32535,#32536,#32537,#32538,#32539,#32540,#32541,#32542,
#32543,#32544,#32545,#32546,#32547,#32548,#32549,#32550,#32551,#32552,#32553,
#32554,#32555,#32556,#32557,#32558,#32559,#32560,#32561,#32562,#32563,#32564,
#32565),.UNSPECIFIED.,.F.,.F.,(4,3,3,3,3,3,3,3,3,3,3,3,3,3,3,3,3,3,3,3,
3,3,3,3,3,3,3,3,3,3,3,4),(0.,0.0241761716010457,0.0604875164315824,0.0972511013618045,
0.133975157825424,0.147571430754056,0.153998040615924,0.189892464907858,
0.225711369702852,0.260761601706721,0.288115324129052,0.295702130337378,
0.30066260492773,0.335153736964546,0.36871896999146,0.40139690760849,0.422834472706132,
0.435070491669721,0.43982788192227,0.473488311702583,0.507453202697751,
0.541171507612653,0.566357468494487,0.571944200141793,0.604905779750409,
0.637688130984217,0.651026858257536,0.658444655992648,0.664614706512331,
0.696427343348877,0.727373814705075,0.744397949170765),.UNSPECIFIED.);
#300=B_SPLINE_CURVE_WITH_KNOTS('',3,(#32566,#32567,#32568,#32569,#32570,
#32571,#32572,#32573,#32574,#32575,#32576,#32577,#32578,#32579,#32580,#32581,
#32582,#32583,#32584,#32585,#32586,#32587,#32588,#32589,#32590,#32591,#32592,
#32593,#32594,#32595,#32596,#32597,#32598,#32599,#32600,#32601,#32602,#32603,
#32604,#32605,#32606,#32607,#32608,#32609,#32610,#32611,#32612,#32613,#32614,
#32615,#32616,#32617,#32618,#32619,#32620,#32621,#32622,#32623,#32624,#32625,
#32626,#32627,#32628,#32629,#32630,#32631,#32632,#32633,#32634,#32635,#32636,
#32637,#32638,#32639,#32640,#32641,#32642,#32643,#32644,#32645,#32646,#32647,
#32648,#32649,#32650,#32651,#32652,#32653,#32654,#32655,#32656),
 .UNSPECIFIED.,.F.,.F.,(4,3,3,3,3,3,3,3,3,3,3,3,3,3,3,3,3,3,3,3,3,3,3,3,
3,3,3,3,3,3,4),(0.,0.0199602231747668,0.0508723816443174,0.0823900365368249,
0.106689326960221,0.118838972171919,0.126476351449351,0.130988617383617,
0.163718139381269,0.196968473281095,0.230459187891393,0.259483610402608,
0.263706435719309,0.298090982061561,0.332366604613236,0.364032629283523,
0.387610012978702,0.395474382928205,0.402776496513689,0.43735314616912,
0.471952684989827,0.507230106948907,0.541083095135413,0.546695484975304,
0.582678619508019,0.618902355831596,0.635230940109389,0.645245254509382,
0.682087619663568,0.718444888016225,0.741270768406373),.UNSPECIFIED.);
#301=B_SPLINE_CURVE_WITH_KNOTS('',3,(#33382,#33383,#33384,#33385,#33386,
#33387,#33388,#33389,#33390,#33391,#33392,#33393,#33394,#33395,#33396,#33397,
#33398,#33399,#33400,#33401,#33402,#33403,#33404,#33405,#33406,#33407,#33408,
#33409,#33410,#33411,#33412,#33413,#33414,#33415,#33416,#33417,#33418,#33419,
#33420,#33421,#33422,#33423,#33424,#33425,#33426,#33427,#33428,#33429,#33430,
#33431,#33432,#33433,#33434,#33435,#33436,#33437,#33438,#33439,#33440,#33441,
#33442,#33443,#33444,#33445,#33446,#33447,#33448,#33449,#33450,#33451,#33452,
#33453,#33454,#33455,#33456,#33457,#33458,#33459,#33460,#33461,#33462,#33463,
#33464,#33465,#33466,#33467,#33468,#33469,#33470,#33471,#33472),
 .UNSPECIFIED.,.F.,.F.,(4,3,3,3,3,3,3,3,3,3,3,3,3,3,3,3,3,3,3,3,3,3,3,3,
3,3,3,3,3,3,4),(0.,0.0199602231747703,0.0508325943020119,0.0823137401186949,
0.114499218705538,0.125197051716921,0.130988613640588,0.163718126795733,
0.19696845695766,0.230459172327224,0.259483613438486,0.263706438258355,
0.298090983919407,0.332366606139957,0.364032629283524,0.387610012978706,
0.395474380525451,0.401789396924481,0.435694450351821,0.470229671357451,
0.505471622292725,0.5345543541377,0.54108302961338,0.546695468865373,0.5826459540699,
0.618859895288609,0.635230906731221,0.644561776401932,0.681404605551153,
0.717768931114021,0.741270768406441),.UNSPECIFIED.);
#302=B_SPLINE_CURVE_WITH_KNOTS('',3,(#33473,#33474,#33475,#33476),
 .UNSPECIFIED.,.F.,.F.,(4,4),(0.,0.0151628972499269),.UNSPECIFIED.);
#303=B_SPLINE_CURVE_WITH_KNOTS('',3,(#33477,#33478,#33479,#33480,#33481,
#33482,#33483,#33484,#33485,#33486,#33487,#33488,#33489,#33490,#33491,#33492,
#33493,#33494,#33495,#33496,#33497,#33498,#33499,#33500,#33501,#33502,#33503,
#33504,#33505,#33506,#33507,#33508,#33509,#33510,#33511,#33512,#33513,#33514,
#33515,#33516,#33517,#33518,#33519,#33520,#33521,#33522,#33523,#33524,#33525,
#33526,#33527,#33528,#33529,#33530,#33531,#33532,#33533,#33534,#33535,#33536,
#33537,#33538,#33539,#33540,#33541,#33542,#33543,#33544,#33545,#33546,#33547,
#33548,#33549,#33550,#33551,#33552,#33553,#33554,#33555,#33556,#33557,#33558,
#33559,#33560,#33561,#33562,#33563,#33564,#33565,#33566,#33567),
 .UNSPECIFIED.,.F.,.F.,(4,3,3,3,3,3,3,3,3,3,3,3,3,3,3,3,3,3,3,3,3,3,3,3,
3,3,3,3,3,3,4),(0.,0.0241761716010214,0.0604875142823813,0.0972510993394287,
0.133975152747319,0.14757142866777,0.153998039183633,0.189892463368544,
0.225711365233482,0.260761585954893,0.28811529479708,0.295702013482264,
0.300662585464541,0.335153710250192,0.36871892746383,0.401396907608365,
0.422016977849024,0.432236392759498,0.440631052868171,0.474302686606213,
0.508270521577337,0.541982161358676,0.566357469533634,0.571944201298751,
0.605035401265075,0.637484032208542,0.658444729985083,0.664614717127708,
0.696427371609928,0.727373866046416,0.744397949170599),.UNSPECIFIED.);
#425=CYLINDRICAL_SURFACE('',#4265,3.22275);
#426=CYLINDRICAL_SURFACE('',#4267,3.22275);
#427=CYLINDRICAL_SURFACE('',#4268,3.22275);
#428=CYLINDRICAL_SURFACE('',#4269,3.22275);
#429=CYLINDRICAL_SURFACE('',#4270,3.22275);
#430=CYLINDRICAL_SURFACE('',#4271,3.22275);
#431=CYLINDRICAL_SURFACE('',#4272,3.22275);
#432=CYLINDRICAL_SURFACE('',#4273,3.22275);
#433=CYLINDRICAL_SURFACE('',#4274,3.22275);
#434=CYLINDRICAL_SURFACE('',#4275,3.22275);
#435=CYLINDRICAL_SURFACE('',#4276,3.22275);
#436=CYLINDRICAL_SURFACE('',#4277,3.22275);
#437=CYLINDRICAL_SURFACE('',#4278,3.22275);
#438=CYLINDRICAL_SURFACE('',#4279,3.22275);
#439=CYLINDRICAL_SURFACE('',#4280,3.22275);
#440=CYLINDRICAL_SURFACE('',#4281,3.22275);
#441=CYLINDRICAL_SURFACE('',#4282,3.22275);
#442=CYLINDRICAL_SURFACE('',#4283,3.22275);
#443=CYLINDRICAL_SURFACE('',#4284,3.22275);
#444=CYLINDRICAL_SURFACE('',#4285,3.22275);
#445=CYLINDRICAL_SURFACE('',#4286,3.22275);
#446=CYLINDRICAL_SURFACE('',#4287,3.22275);
#447=CYLINDRICAL_SURFACE('',#4288,3.22275);
#448=CYLINDRICAL_SURFACE('',#4289,3.22275);
#449=CYLINDRICAL_SURFACE('',#4290,3.22275);
#450=CYLINDRICAL_SURFACE('',#4291,3.22275);
#451=CYLINDRICAL_SURFACE('',#4292,3.22275);
#452=CYLINDRICAL_SURFACE('',#4293,3.22275);
#453=CYLINDRICAL_SURFACE('',#4294,3.933);
#454=CYLINDRICAL_SURFACE('',#4297,3.22275);
#566=CIRCLE('',#4266,3.22275);
#567=CIRCLE('',#4295,3.933);
#568=CIRCLE('',#4296,3.933);
#569=CIRCLE('',#4298,3.22275);
#712=FACE_OUTER_BOUND('',#921,.T.);
#713=FACE_OUTER_BOUND('',#922,.T.);
#714=FACE_OUTER_BOUND('',#923,.T.);
#715=FACE_OUTER_BOUND('',#924,.T.);
#716=FACE_OUTER_BOUND('',#925,.T.);
#717=FACE_OUTER_BOUND('',#926,.T.);
#718=FACE_OUTER_BOUND('',#927,.T.);
#719=FACE_OUTER_BOUND('',#928,.T.);
#720=FACE_OUTER_BOUND('',#929,.T.);
#721=FACE_OUTER_BOUND('',#930,.T.);
#722=FACE_OUTER_BOUND('',#931,.T.);
#723=FACE_OUTER_BOUND('',#932,.T.);
#724=FACE_OUTER_BOUND('',#933,.T.);
#725=FACE_OUTER_BOUND('',#934,.T.);
#726=FACE_OUTER_BOUND('',#935,.T.);
#727=FACE_OUTER_BOUND('',#936,.T.);
#728=FACE_OUTER_BOUND('',#937,.T.);
#729=FACE_OUTER_BOUND('',#938,.T.);
#730=FACE_OUTER_BOUND('',#939,.T.);
#731=FACE_OUTER_BOUND('',#940,.T.);
#732=FACE_OUTER_BOUND('',#941,.T.);
#733=FACE_OUTER_BOUND('',#942,.T.);
#734=FACE_OUTER_BOUND('',#943,.T.);
#735=FACE_OUTER_BOUND('',#944,.T.);
#736=FACE_OUTER_BOUND('',#945,.T.);
#737=FACE_OUTER_BOUND('',#946,.T.);
#738=FACE_OUTER_BOUND('',#947,.T.);
#739=FACE_OUTER_BOUND('',#948,.T.);
#740=FACE_OUTER_BOUND('',#949,.T.);
#741=FACE_OUTER_BOUND('',#950,.T.);
#742=FACE_OUTER_BOUND('',#951,.T.);
#743=FACE_OUTER_BOUND('',#952,.T.);
#744=FACE_OUTER_BOUND('',#953,.T.);
#745=FACE_OUTER_BOUND('',#954,.T.);
#921=EDGE_LOOP('',(#2920,#2921,#2922,#2923));
#922=EDGE_LOOP('',(#2924,#2925,#2926,#2927,#2928,#2929));
#923=EDGE_LOOP('',(#2930,#2931,#2932,#2933));
#924=EDGE_LOOP('',(#2934,#2935,#2936,#2937,#2938,#2939));
#925=EDGE_LOOP('',(#2940,#2941,#2942,#2943,#2944));
#926=EDGE_LOOP('',(#2945,#2946,#2947,#2948,#2949));
#927=EDGE_LOOP('',(#2950,#2951,#2952,#2953,#2954));
#928=EDGE_LOOP('',(#2955,#2956,#2957,#2958,#2959));
#929=EDGE_LOOP('',(#2960,#2961,#2962,#2963,#2964));
#930=EDGE_LOOP('',(#2965,#2966,#2967,#2968,#2969));
#931=EDGE_LOOP('',(#2970,#2971,#2972,#2973,#2974));
#932=EDGE_LOOP('',(#2975,#2976,#2977,#2978,#2979));
#933=EDGE_LOOP('',(#2980,#2981,#2982,#2983,#2984,#2985));
#934=EDGE_LOOP('',(#2986,#2987,#2988,#2989));
#935=EDGE_LOOP('',(#2990,#2991,#2992,#2993,#2994,#2995));
#936=EDGE_LOOP('',(#2996,#2997,#2998,#2999));
#937=EDGE_LOOP('',(#3000,#3001,#3002,#3003,#3004,#3005));
#938=EDGE_LOOP('',(#3006,#3007,#3008,#3009,#3010));
#939=EDGE_LOOP('',(#3011,#3012,#3013,#3014,#3015));
#940=EDGE_LOOP('',(#3016,#3017,#3018,#3019,#3020));
#941=EDGE_LOOP('',(#3021,#3022,#3023,#3024,#3025));
#942=EDGE_LOOP('',(#3026,#3027,#3028,#3029,#3030));
#943=EDGE_LOOP('',(#3031,#3032,#3033,#3034,#3035));
#944=EDGE_LOOP('',(#3036,#3037,#3038,#3039,#3040));
#945=EDGE_LOOP('',(#3041,#3042,#3043,#3044,#3045));
#946=EDGE_LOOP('',(#3046,#3047,#3048,#3049,#3050,#3051));
#947=EDGE_LOOP('',(#3052,#3053,#3054,#3055));
#948=EDGE_LOOP('',(#3056,#3057,#3058,#3059,#3060,#3061));
#949=EDGE_LOOP('',(#3062,#3063,#3064,#3065,#3066,#3067,#3068,#3069,#3070,
#3071,#3072,#3073,#3074,#3075,#3076,#3077,#3078,#3079,#3080,#3081,#3082,
#3083,#3084,#3085,#3086,#3087,#3088,#3089,#3090,#3091,#3092,#3093,#3094,
#3095,#3096,#3097,#3098,#3099,#3100,#3101,#3102,#3103,#3104,#3105,#3106,
#3107,#3108,#3109,#3110,#3111,#3112,#3113,#3114,#3115,#3116,#3117,#3118,
#3119,#3120,#3121));
#950=EDGE_LOOP('',(#3122,#3123,#3124,#3125,#3126));
#951=EDGE_LOOP('',(#3127,#3128,#3129,#3130,#3131,#3132,#3133,#3134,#3135,
#3136,#3137,#3138,#3139,#3140,#3141,#3142,#3143,#3144,#3145,#3146,#3147,
#3148,#3149,#3150,#3151,#3152,#3153,#3154,#3155,#3156,#3157,#3158,#3159,
#3160,#3161,#3162,#3163,#3164,#3165,#3166,#3167,#3168,#3169,#3170,#3171,
#3172,#3173,#3174,#3175,#3176,#3177,#3178,#3179,#3180,#3181,#3182,#3183,
#3184,#3185,#3186,#3187,#3188,#3189,#3190,#3191,#3192,#3193,#3194,#3195,
#3196,#3197,#3198,#3199,#3200,#3201,#3202));
#952=EDGE_LOOP('',(#3203,#3204,#3205,#3206,#3207,#3208,#3209,#3210,#3211,
#3212,#3213,#3214,#3215,#3216,#3217,#3218,#3219,#3220,#3221,#3222,#3223,
#3224,#3225,#3226,#3227,#3228,#3229,#3230,#3231,#3232,#3233,#3234,#3235,
#3236,#3237,#3238,#3239,#3240,#3241,#3242,#3243,#3244,#3245,#3246,#3247,
#3248,#3249,#3250,#3251,#3252,#3253,#3254,#3255,#3256,#3257,#3258,#3259,
#3260,#3261,#3262,#3263,#3264,#3265,#3266,#3267,#3268,#3269,#3270,#3271,
#3272,#3273,#3274,#3275,#3276,#3277,#3278));
#953=EDGE_LOOP('',(#3279,#3280,#3281,#3282,#3283));
#954=EDGE_LOOP('',(#3284,#3285,#3286,#3287));
#1138=LINE('',#11679,#1351);
#1139=LINE('',#11868,#1352);
#1140=LINE('',#12373,#1353);
#1141=LINE('',#12815,#1354);
#1142=LINE('',#13203,#1355);
#1143=LINE('',#13596,#1356);
#1144=LINE('',#14073,#1357);
#1145=LINE('',#14568,#1358);
#1146=LINE('',#15045,#1359);
#1147=LINE('',#15534,#1360);
#1148=LINE('',#15991,#1361);
#1149=LINE('',#16532,#1362);
#1150=LINE('',#16849,#1363);
#1151=LINE('',#17277,#1364);
#1152=LINE('',#17731,#1365);
#1153=LINE('',#18219,#1366);
#1154=LINE('',#18663,#1367);
#1155=LINE('',#19059,#1368);
#1156=LINE('',#19484,#1369);
#1157=LINE('',#19945,#1370);
#1158=LINE('',#20394,#1371);
#1159=LINE('',#20863,#1372);
#1160=LINE('',#21308,#1373);
#1161=LINE('',#21809,#1374);
#1162=LINE('',#22268,#1375);
#1163=LINE('',#22570,#1376);
#1164=LINE('',#22986,#1377);
#1165=LINE('',#23424,#1378);
#1351=VECTOR('',#4805,3.22275);
#1352=VECTOR('',#4810,3.22275);
#1353=VECTOR('',#4813,3.22275);
#1354=VECTOR('',#4816,3.22275);
#1355=VECTOR('',#4819,3.22275);
#1356=VECTOR('',#4822,3.22275);
#1357=VECTOR('',#4825,3.22275);
#1358=VECTOR('',#4828,3.22275);
#1359=VECTOR('',#4831,3.22275);
#1360=VECTOR('',#4834,3.22275);
#1361=VECTOR('',#4837,3.22275);
#1362=VECTOR('',#4840,3.22275);
#1363=VECTOR('',#4843,3.22275);
#1364=VECTOR('',#4846,3.22275);
#1365=VECTOR('',#4849,3.22275);
#1366=VECTOR('',#4852,3.22275);
#1367=VECTOR('',#4855,3.22275);
#1368=VECTOR('',#4858,3.22275);
#1369=VECTOR('',#4861,3.22275);
#1370=VECTOR('',#4864,3.22275);
#1371=VECTOR('',#4867,3.22275);
#1372=VECTOR('',#4870,3.22275);
#1373=VECTOR('',#4873,3.22275);
#1374=VECTOR('',#4876,3.22275);
#1375=VECTOR('',#4879,3.22275);
#1376=VECTOR('',#4882,3.22275);
#1377=VECTOR('',#4885,3.22275);
#1378=VECTOR('',#4888,3.22275);
#1608=VERTEX_POINT('',#11677);
#1609=VERTEX_POINT('',#11678);
#1610=VERTEX_POINT('',#11680);
#1611=VERTEX_POINT('',#11793);
#1612=VERTEX_POINT('',#11866);
#1613=VERTEX_POINT('',#11867);
#1614=VERTEX_POINT('',#11869);
#1615=VERTEX_POINT('',#12141);
#1616=VERTEX_POINT('',#12371);
#1617=VERTEX_POINT('',#12372);
#1618=VERTEX_POINT('',#12813);
#1619=VERTEX_POINT('',#12814);
#1620=VERTEX_POINT('',#12816);
#1621=VERTEX_POINT('',#13069);
#1622=VERTEX_POINT('',#13201);
#1623=VERTEX_POINT('',#13202);
#1624=VERTEX_POINT('',#13424);
#1625=VERTEX_POINT('',#13594);
#1626=VERTEX_POINT('',#13595);
#1627=VERTEX_POINT('',#13597);
#1628=VERTEX_POINT('',#14071);
#1629=VERTEX_POINT('',#14072);
#1630=VERTEX_POINT('',#14302);
#1631=VERTEX_POINT('',#14566);
#1632=VERTEX_POINT('',#14567);
#1633=VERTEX_POINT('',#14569);
#1634=VERTEX_POINT('',#15043);
#1635=VERTEX_POINT('',#15044);
#1636=VERTEX_POINT('',#15278);
#1637=VERTEX_POINT('',#15532);
#1638=VERTEX_POINT('',#15533);
#1639=VERTEX_POINT('',#15535);
#1640=VERTEX_POINT('',#15989);
#1641=VERTEX_POINT('',#15990);
#1642=VERTEX_POINT('',#16220);
#1643=VERTEX_POINT('',#16530);
#1644=VERTEX_POINT('',#16531);
#1645=VERTEX_POINT('',#16533);
#1646=VERTEX_POINT('',#16847);
#1647=VERTEX_POINT('',#16848);
#1648=VERTEX_POINT('',#16850);
#1649=VERTEX_POINT('',#17047);
#1650=VERTEX_POINT('',#17275);
#1651=VERTEX_POINT('',#17276);
#1652=VERTEX_POINT('',#17729);
#1653=VERTEX_POINT('',#17730);
#1654=VERTEX_POINT('',#17732);
#1655=VERTEX_POINT('',#17985);
#1656=VERTEX_POINT('',#18217);
#1657=VERTEX_POINT('',#18218);
#1658=VERTEX_POINT('',#18661);
#1659=VERTEX_POINT('',#18662);
#1660=VERTEX_POINT('',#18664);
#1661=VERTEX_POINT('',#18973);
#1662=VERTEX_POINT('',#19057);
#1663=VERTEX_POINT('',#19058);
#1664=VERTEX_POINT('',#19284);
#1665=VERTEX_POINT('',#19482);
#1666=VERTEX_POINT('',#19483);
#1667=VERTEX_POINT('',#19485);
#1668=VERTEX_POINT('',#19943);
#1669=VERTEX_POINT('',#19944);
#1670=VERTEX_POINT('',#20168);
#1671=VERTEX_POINT('',#20392);
#1672=VERTEX_POINT('',#20393);
#1673=VERTEX_POINT('',#20395);
#1674=VERTEX_POINT('',#20861);
#1675=VERTEX_POINT('',#20862);
#1676=VERTEX_POINT('',#21074);
#1677=VERTEX_POINT('',#21306);
#1678=VERTEX_POINT('',#21307);
#1679=VERTEX_POINT('',#21309);
#1680=VERTEX_POINT('',#21807);
#1681=VERTEX_POINT('',#21808);
#1682=VERTEX_POINT('',#22024);
#1683=VERTEX_POINT('',#22266);
#1684=VERTEX_POINT('',#22267);
#1685=VERTEX_POINT('',#22269);
#1686=VERTEX_POINT('',#22568);
#1687=VERTEX_POINT('',#22569);
#1688=VERTEX_POINT('',#22571);
#1689=VERTEX_POINT('',#22726);
#1690=VERTEX_POINT('',#22984);
#1691=VERTEX_POINT('',#22985);
#1692=VERTEX_POINT('',#23422);
#1693=VERTEX_POINT('',#23423);
#1694=VERTEX_POINT('',#23425);
#1695=VERTEX_POINT('',#23650);
#1696=VERTEX_POINT('',#23920);
#1697=VERTEX_POINT('',#23921);
#1698=VERTEX_POINT('',#23995);
#1699=VERTEX_POINT('',#23997);
#1700=VERTEX_POINT('',#24003);
#1701=VERTEX_POINT('',#24230);
#1702=VERTEX_POINT('',#24241);
#1703=VERTEX_POINT('',#24465);
#1704=VERTEX_POINT('',#24695);
#1705=VERTEX_POINT('',#24706);
#1706=VERTEX_POINT('',#24717);
#1707=VERTEX_POINT('',#24944);
#1708=VERTEX_POINT('',#24955);
#1709=VERTEX_POINT('',#25182);
#1710=VERTEX_POINT('',#25409);
#1711=VERTEX_POINT('',#25421);
#1712=VERTEX_POINT('',#25648);
#1713=VERTEX_POINT('',#25875);
#1714=VERTEX_POINT('',#26102);
#1715=VERTEX_POINT('',#26113);
#1716=VERTEX_POINT('',#26343);
#1717=VERTEX_POINT('',#26570);
#1718=VERTEX_POINT('',#26582);
#1719=VERTEX_POINT('',#26593);
#1720=VERTEX_POINT('',#26604);
#1721=VERTEX_POINT('',#26616);
#1722=VERTEX_POINT('',#26843);
#1723=VERTEX_POINT('',#27070);
#1724=VERTEX_POINT('',#27081);
#1725=VERTEX_POINT('',#27308);
#1726=VERTEX_POINT('',#27319);
#1727=VERTEX_POINT('',#27546);
#1728=VERTEX_POINT('',#27731);
#1729=VERTEX_POINT('',#27733);
#1730=VERTEX_POINT('',#27742);
#1731=VERTEX_POINT('',#27969);
#1732=VERTEX_POINT('',#28196);
#1733=VERTEX_POINT('',#28423);
#1734=VERTEX_POINT('',#28434);
#1735=VERTEX_POINT('',#28661);
#1736=VERTEX_POINT('',#28672);
#1737=VERTEX_POINT('',#28684);
#1738=VERTEX_POINT('',#28911);
#1739=VERTEX_POINT('',#28922);
#1740=VERTEX_POINT('',#29149);
#1741=VERTEX_POINT('',#29160);
#1742=VERTEX_POINT('',#29387);
#1743=VERTEX_POINT('',#29614);
#1744=VERTEX_POINT('',#29626);
#1745=VERTEX_POINT('',#29853);
#1746=VERTEX_POINT('',#30080);
#1747=VERTEX_POINT('',#30092);
#1748=VERTEX_POINT('',#30319);
#1749=VERTEX_POINT('',#30330);
#1750=VERTEX_POINT('',#30341);
#1751=VERTEX_POINT('',#30568);
#1752=VERTEX_POINT('',#30795);
#1753=VERTEX_POINT('',#31022);
#1754=VERTEX_POINT('',#31034);
#1755=VERTEX_POINT('',#31261);
#1756=VERTEX_POINT('',#31499);
#1757=VERTEX_POINT('',#31644);
#1758=VERTEX_POINT('',#31646);
#1759=VERTEX_POINT('',#33381);
#2111=EDGE_CURVE('',#1608,#1609,#1138,.T.);
#2112=EDGE_CURVE('',#1610,#1608,#152,.T.);
#2113=EDGE_CURVE('',#1611,#1610,#566,.T.);
#2114=EDGE_CURVE('',#1611,#1609,#153,.T.);
#2115=EDGE_CURVE('',#1612,#1613,#1139,.T.);
#2116=EDGE_CURVE('',#1614,#1612,#154,.F.);
#2117=EDGE_CURVE('',#1608,#1614,#155,.T.);
#2118=EDGE_CURVE('',#1609,#1615,#156,.T.);
#2119=EDGE_CURVE('',#1615,#1613,#157,.T.);
#2120=EDGE_CURVE('',#1616,#1617,#1140,.T.);
#2121=EDGE_CURVE('',#1612,#1616,#158,.F.);
#2122=EDGE_CURVE('',#1613,#1617,#159,.T.);
#2123=EDGE_CURVE('',#1618,#1619,#1141,.T.);
#2124=EDGE_CURVE('',#1620,#1618,#160,.F.);
#2125=EDGE_CURVE('',#1616,#1620,#161,.F.);
#2126=EDGE_CURVE('',#1617,#1621,#162,.T.);
#2127=EDGE_CURVE('',#1621,#1619,#163,.T.);
#2128=EDGE_CURVE('',#1622,#1623,#1142,.T.);
#2129=EDGE_CURVE('',#1618,#1622,#164,.F.);
#2130=EDGE_CURVE('',#1619,#1624,#165,.T.);
#2131=EDGE_CURVE('',#1624,#1623,#166,.T.);
#2132=EDGE_CURVE('',#1625,#1626,#1143,.T.);
#2133=EDGE_CURVE('',#1627,#1625,#167,.F.);
#2134=EDGE_CURVE('',#1622,#1627,#168,.F.);
#2135=EDGE_CURVE('',#1623,#1626,#169,.T.);
#2136=EDGE_CURVE('',#1628,#1629,#1144,.T.);
#2137=EDGE_CURVE('',#1625,#1628,#170,.F.);
#2138=EDGE_CURVE('',#1626,#1630,#171,.T.);
#2139=EDGE_CURVE('',#1630,#1629,#172,.T.);
#2140=EDGE_CURVE('',#1631,#1632,#1145,.T.);
#2141=EDGE_CURVE('',#1633,#1631,#173,.F.);
#2142=EDGE_CURVE('',#1628,#1633,#174,.F.);
#2143=EDGE_CURVE('',#1629,#1632,#175,.T.);
#2144=EDGE_CURVE('',#1634,#1635,#1146,.T.);
#2145=EDGE_CURVE('',#1631,#1634,#176,.F.);
#2146=EDGE_CURVE('',#1632,#1636,#177,.T.);
#2147=EDGE_CURVE('',#1636,#1635,#178,.T.);
#2148=EDGE_CURVE('',#1637,#1638,#1147,.T.);
#2149=EDGE_CURVE('',#1639,#1637,#179,.F.);
#2150=EDGE_CURVE('',#1634,#1639,#180,.F.);
#2151=EDGE_CURVE('',#1635,#1638,#181,.T.);
#2152=EDGE_CURVE('',#1640,#1641,#1148,.T.);
#2153=EDGE_CURVE('',#1637,#1640,#182,.F.);
#2154=EDGE_CURVE('',#1638,#1642,#183,.T.);
#2155=EDGE_CURVE('',#1642,#1641,#184,.T.);
#2156=EDGE_CURVE('',#1643,#1644,#1149,.T.);
#2157=EDGE_CURVE('',#1645,#1643,#185,.T.);
#2158=EDGE_CURVE('',#1640,#1645,#186,.F.);
#2159=EDGE_CURVE('',#1641,#1644,#187,.T.);
#2160=EDGE_CURVE('',#1646,#1647,#1150,.T.);
#2161=EDGE_CURVE('',#1648,#1646,#188,.F.);
#2162=EDGE_CURVE('',#1643,#1648,#189,.T.);
#2163=EDGE_CURVE('',#1644,#1649,#190,.T.);
#2164=EDGE_CURVE('',#1649,#1647,#191,.T.);
#2165=EDGE_CURVE('',#1650,#1651,#1151,.T.);
#2166=EDGE_CURVE('',#1646,#1650,#192,.F.);
#2167=EDGE_CURVE('',#1647,#1651,#193,.T.);
#2168=EDGE_CURVE('',#1652,#1653,#1152,.T.);
#2169=EDGE_CURVE('',#1654,#1652,#194,.F.);
#2170=EDGE_CURVE('',#1650,#1654,#195,.F.);
#2171=EDGE_CURVE('',#1651,#1655,#196,.T.);
#2172=EDGE_CURVE('',#1655,#1653,#197,.T.);
#2173=EDGE_CURVE('',#1656,#1657,#1153,.T.);
#2174=EDGE_CURVE('',#1652,#1656,#198,.F.);
#2175=EDGE_CURVE('',#1653,#1657,#199,.T.);
#2176=EDGE_CURVE('',#1658,#1659,#1154,.T.);
#2177=EDGE_CURVE('',#1660,#1658,#200,.F.);
#2178=EDGE_CURVE('',#1656,#1660,#201,.F.);
#2179=EDGE_CURVE('',#1657,#1661,#202,.T.);
#2180=EDGE_CURVE('',#1661,#1659,#203,.T.);
#2181=EDGE_CURVE('',#1662,#1663,#1155,.T.);
#2182=EDGE_CURVE('',#1658,#1662,#204,.F.);
#2183=EDGE_CURVE('',#1659,#1664,#205,.T.);
#2184=EDGE_CURVE('',#1664,#1663,#206,.T.);
#2185=EDGE_CURVE('',#1665,#1666,#1156,.T.);
#2186=EDGE_CURVE('',#1667,#1665,#207,.F.);
#2187=EDGE_CURVE('',#1662,#1667,#208,.F.);
#2188=EDGE_CURVE('',#1663,#1666,#209,.T.);
#2189=EDGE_CURVE('',#1668,#1669,#1157,.T.);
#2190=EDGE_CURVE('',#1665,#1668,#210,.F.);
#2191=EDGE_CURVE('',#1666,#1670,#211,.T.);
#2192=EDGE_CURVE('',#1670,#1669,#212,.T.);
#2193=EDGE_CURVE('',#1671,#1672,#1158,.T.);
#2194=EDGE_CURVE('',#1673,#1671,#213,.F.);
#2195=EDGE_CURVE('',#1668,#1673,#214,.F.);
#2196=EDGE_CURVE('',#1669,#1672,#215,.T.);
#2197=EDGE_CURVE('',#1674,#1675,#1159,.T.);
#2198=EDGE_CURVE('',#1671,#1674,#216,.F.);
#2199=EDGE_CURVE('',#1672,#1676,#217,.T.);
#2200=EDGE_CURVE('',#1676,#1675,#218,.T.);
#2201=EDGE_CURVE('',#1677,#1678,#1160,.T.);
#2202=EDGE_CURVE('',#1679,#1677,#219,.F.);
#2203=EDGE_CURVE('',#1674,#1679,#220,.F.);
#2204=EDGE_CURVE('',#1675,#1678,#221,.T.);
#2205=EDGE_CURVE('',#1680,#1681,#1161,.T.);
#2206=EDGE_CURVE('',#1677,#1680,#222,.F.);
#2207=EDGE_CURVE('',#1678,#1682,#223,.T.);
#2208=EDGE_CURVE('',#1682,#1681,#224,.T.);
#2209=EDGE_CURVE('',#1683,#1684,#1162,.T.);
#2210=EDGE_CURVE('',#1685,#1683,#225,.T.);
#2211=EDGE_CURVE('',#1680,#1685,#226,.F.);
#2212=EDGE_CURVE('',#1681,#1684,#227,.T.);
#2213=EDGE_CURVE('',#1686,#1687,#1163,.T.);
#2214=EDGE_CURVE('',#1688,#1686,#228,.F.);
#2215=EDGE_CURVE('',#1683,#1688,#229,.T.);
#2216=EDGE_CURVE('',#1684,#1689,#230,.T.);
#2217=EDGE_CURVE('',#1689,#1687,#231,.T.);
#2218=EDGE_CURVE('',#1690,#1691,#1164,.T.);
#2219=EDGE_CURVE('',#1686,#1690,#232,.F.);
#2220=EDGE_CURVE('',#1687,#1691,#233,.T.);
#2221=EDGE_CURVE('',#1692,#1693,#1165,.T.);
#2222=EDGE_CURVE('',#1694,#1692,#234,.T.);
#2223=EDGE_CURVE('',#1690,#1694,#235,.F.);
#2224=EDGE_CURVE('',#1691,#1695,#236,.T.);
#2225=EDGE_CURVE('',#1695,#1693,#237,.F.);
#2226=EDGE_CURVE('',#1696,#1697,#238,.T.);
#2227=EDGE_CURVE('',#1698,#1697,#567,.T.);
#2228=EDGE_CURVE('',#1698,#1699,#239,.T.);
#2229=EDGE_CURVE('',#1699,#1700,#240,.T.);
#2230=EDGE_CURVE('',#1700,#1701,#241,.T.);
#2231=EDGE_CURVE('',#1701,#1702,#242,.T.);
#2232=EDGE_CURVE('',#1702,#1703,#243,.T.);
#2233=EDGE_CURVE('',#1703,#1704,#244,.T.);
#2234=EDGE_CURVE('',#1704,#1705,#245,.T.);
#2235=EDGE_CURVE('',#1705,#1706,#246,.T.);
#2236=EDGE_CURVE('',#1706,#1707,#247,.T.);
#2237=EDGE_CURVE('',#1707,#1708,#248,.T.);
#2238=EDGE_CURVE('',#1708,#1709,#249,.T.);
#2239=EDGE_CURVE('',#1709,#1710,#250,.T.);
#2240=EDGE_CURVE('',#1710,#1711,#251,.T.);
#2241=EDGE_CURVE('',#1711,#1712,#252,.T.);
#2242=EDGE_CURVE('',#1712,#1713,#253,.T.);
#2243=EDGE_CURVE('',#1713,#1714,#254,.T.);
#2244=EDGE_CURVE('',#1714,#1715,#255,.T.);
#2245=EDGE_CURVE('',#1715,#1716,#256,.T.);
#2246=EDGE_CURVE('',#1716,#1717,#257,.T.);
#2247=EDGE_CURVE('',#1717,#1718,#258,.T.);
#2248=EDGE_CURVE('',#1718,#1719,#259,.T.);
#2249=EDGE_CURVE('',#1719,#1720,#260,.T.);
#2250=EDGE_CURVE('',#1720,#1721,#261,.T.);
#2251=EDGE_CURVE('',#1721,#1722,#262,.T.);
#2252=EDGE_CURVE('',#1722,#1723,#263,.T.);
#2253=EDGE_CURVE('',#1723,#1724,#264,.T.);
#2254=EDGE_CURVE('',#1724,#1725,#265,.T.);
#2255=EDGE_CURVE('',#1725,#1726,#266,.T.);
#2256=EDGE_CURVE('',#1726,#1727,#267,.T.);
#2257=EDGE_CURVE('',#1728,#1727,#568,.F.);
#2258=EDGE_CURVE('',#1728,#1729,#268,.T.);
#2259=EDGE_CURVE('',#1729,#1730,#269,.T.);
#2260=EDGE_CURVE('',#1730,#1731,#270,.T.);
#2261=EDGE_CURVE('',#1731,#1732,#271,.T.);
#2262=EDGE_CURVE('',#1732,#1733,#272,.T.);
#2263=EDGE_CURVE('',#1733,#1734,#273,.T.);
#2264=EDGE_CURVE('',#1734,#1735,#274,.T.);
#2265=EDGE_CURVE('',#1735,#1736,#275,.T.);
#2266=EDGE_CURVE('',#1736,#1737,#276,.T.);
#2267=EDGE_CURVE('',#1737,#1738,#277,.T.);
#2268=EDGE_CURVE('',#1738,#1739,#278,.T.);
#2269=EDGE_CURVE('',#1739,#1740,#279,.T.);
#2270=EDGE_CURVE('',#1740,#1741,#280,.T.);
#2271=EDGE_CURVE('',#1741,#1742,#281,.T.);
#2272=EDGE_CURVE('',#1742,#1743,#282,.T.);
#2273=EDGE_CURVE('',#1743,#1744,#283,.T.);
#2274=EDGE_CURVE('',#1744,#1745,#284,.T.);
#2275=EDGE_CURVE('',#1745,#1746,#285,.T.);
#2276=EDGE_CURVE('',#1746,#1747,#286,.T.);
#2277=EDGE_CURVE('',#1747,#1748,#287,.T.);
#2278=EDGE_CURVE('',#1748,#1749,#288,.T.);
#2279=EDGE_CURVE('',#1749,#1750,#289,.T.);
#2280=EDGE_CURVE('',#1750,#1751,#290,.T.);
#2281=EDGE_CURVE('',#1751,#1752,#291,.T.);
#2282=EDGE_CURVE('',#1752,#1753,#292,.T.);
#2283=EDGE_CURVE('',#1753,#1754,#293,.T.);
#2284=EDGE_CURVE('',#1754,#1755,#294,.T.);
#2285=EDGE_CURVE('',#1755,#1696,#295,.T.);
#2286=EDGE_CURVE('',#1693,#1756,#296,.F.);
#2287=EDGE_CURVE('',#1757,#1756,#569,.T.);
#2288=EDGE_CURVE('',#1758,#1757,#297,.T.);
#2289=EDGE_CURVE('',#1692,#1758,#298,.T.);
#2290=EDGE_CURVE('',#1727,#1757,#299,.T.);
#2291=EDGE_CURVE('',#1610,#1698,#300,.T.);
#2292=EDGE_CURVE('',#1759,#1728,#301,.T.);
#2293=EDGE_CURVE('',#1756,#1759,#302,.T.);
#2294=EDGE_CURVE('',#1697,#1611,#303,.T.);
#2920=ORIENTED_EDGE('',*,*,#2111,.F.);
#2921=ORIENTED_EDGE('',*,*,#2112,.F.);
#2922=ORIENTED_EDGE('',*,*,#2113,.F.);
#2923=ORIENTED_EDGE('',*,*,#2114,.T.);
#2924=ORIENTED_EDGE('',*,*,#2115,.F.);
#2925=ORIENTED_EDGE('',*,*,#2116,.F.);
#2926=ORIENTED_EDGE('',*,*,#2117,.F.);
#2927=ORIENTED_EDGE('',*,*,#2111,.T.);
#2928=ORIENTED_EDGE('',*,*,#2118,.T.);
#2929=ORIENTED_EDGE('',*,*,#2119,.T.);
#2930=ORIENTED_EDGE('',*,*,#2120,.F.);
#2931=ORIENTED_EDGE('',*,*,#2121,.F.);
#2932=ORIENTED_EDGE('',*,*,#2115,.T.);
#2933=ORIENTED_EDGE('',*,*,#2122,.T.);
#2934=ORIENTED_EDGE('',*,*,#2123,.F.);
#2935=ORIENTED_EDGE('',*,*,#2124,.F.);
#2936=ORIENTED_EDGE('',*,*,#2125,.F.);
#2937=ORIENTED_EDGE('',*,*,#2120,.T.);
#2938=ORIENTED_EDGE('',*,*,#2126,.T.);
#2939=ORIENTED_EDGE('',*,*,#2127,.T.);
#2940=ORIENTED_EDGE('',*,*,#2128,.F.);
#2941=ORIENTED_EDGE('',*,*,#2129,.F.);
#2942=ORIENTED_EDGE('',*,*,#2123,.T.);
#2943=ORIENTED_EDGE('',*,*,#2130,.T.);
#2944=ORIENTED_EDGE('',*,*,#2131,.T.);
#2945=ORIENTED_EDGE('',*,*,#2132,.F.);
#2946=ORIENTED_EDGE('',*,*,#2133,.F.);
#2947=ORIENTED_EDGE('',*,*,#2134,.F.);
#2948=ORIENTED_EDGE('',*,*,#2128,.T.);
#2949=ORIENTED_EDGE('',*,*,#2135,.T.);
#2950=ORIENTED_EDGE('',*,*,#2136,.F.);
#2951=ORIENTED_EDGE('',*,*,#2137,.F.);
#2952=ORIENTED_EDGE('',*,*,#2132,.T.);
#2953=ORIENTED_EDGE('',*,*,#2138,.T.);
#2954=ORIENTED_EDGE('',*,*,#2139,.T.);
#2955=ORIENTED_EDGE('',*,*,#2140,.F.);
#2956=ORIENTED_EDGE('',*,*,#2141,.F.);
#2957=ORIENTED_EDGE('',*,*,#2142,.F.);
#2958=ORIENTED_EDGE('',*,*,#2136,.T.);
#2959=ORIENTED_EDGE('',*,*,#2143,.T.);
#2960=ORIENTED_EDGE('',*,*,#2144,.F.);
#2961=ORIENTED_EDGE('',*,*,#2145,.F.);
#2962=ORIENTED_EDGE('',*,*,#2140,.T.);
#2963=ORIENTED_EDGE('',*,*,#2146,.T.);
#2964=ORIENTED_EDGE('',*,*,#2147,.T.);
#2965=ORIENTED_EDGE('',*,*,#2148,.F.);
#2966=ORIENTED_EDGE('',*,*,#2149,.F.);
#2967=ORIENTED_EDGE('',*,*,#2150,.F.);
#2968=ORIENTED_EDGE('',*,*,#2144,.T.);
#2969=ORIENTED_EDGE('',*,*,#2151,.T.);
#2970=ORIENTED_EDGE('',*,*,#2152,.F.);
#2971=ORIENTED_EDGE('',*,*,#2153,.F.);
#2972=ORIENTED_EDGE('',*,*,#2148,.T.);
#2973=ORIENTED_EDGE('',*,*,#2154,.T.);
#2974=ORIENTED_EDGE('',*,*,#2155,.T.);
#2975=ORIENTED_EDGE('',*,*,#2156,.F.);
#2976=ORIENTED_EDGE('',*,*,#2157,.F.);
#2977=ORIENTED_EDGE('',*,*,#2158,.F.);
#2978=ORIENTED_EDGE('',*,*,#2152,.T.);
#2979=ORIENTED_EDGE('',*,*,#2159,.T.);
#2980=ORIENTED_EDGE('',*,*,#2160,.F.);
#2981=ORIENTED_EDGE('',*,*,#2161,.F.);
#2982=ORIENTED_EDGE('',*,*,#2162,.F.);
#2983=ORIENTED_EDGE('',*,*,#2156,.T.);
#2984=ORIENTED_EDGE('',*,*,#2163,.T.);
#2985=ORIENTED_EDGE('',*,*,#2164,.T.);
#2986=ORIENTED_EDGE('',*,*,#2165,.F.);
#2987=ORIENTED_EDGE('',*,*,#2166,.F.);
#2988=ORIENTED_EDGE('',*,*,#2160,.T.);
#2989=ORIENTED_EDGE('',*,*,#2167,.T.);
#2990=ORIENTED_EDGE('',*,*,#2168,.F.);
#2991=ORIENTED_EDGE('',*,*,#2169,.F.);
#2992=ORIENTED_EDGE('',*,*,#2170,.F.);
#2993=ORIENTED_EDGE('',*,*,#2165,.T.);
#2994=ORIENTED_EDGE('',*,*,#2171,.T.);
#2995=ORIENTED_EDGE('',*,*,#2172,.T.);
#2996=ORIENTED_EDGE('',*,*,#2173,.F.);
#2997=ORIENTED_EDGE('',*,*,#2174,.F.);
#2998=ORIENTED_EDGE('',*,*,#2168,.T.);
#2999=ORIENTED_EDGE('',*,*,#2175,.T.);
#3000=ORIENTED_EDGE('',*,*,#2176,.F.);
#3001=ORIENTED_EDGE('',*,*,#2177,.F.);
#3002=ORIENTED_EDGE('',*,*,#2178,.F.);
#3003=ORIENTED_EDGE('',*,*,#2173,.T.);
#3004=ORIENTED_EDGE('',*,*,#2179,.T.);
#3005=ORIENTED_EDGE('',*,*,#2180,.T.);
#3006=ORIENTED_EDGE('',*,*,#2181,.F.);
#3007=ORIENTED_EDGE('',*,*,#2182,.F.);
#3008=ORIENTED_EDGE('',*,*,#2176,.T.);
#3009=ORIENTED_EDGE('',*,*,#2183,.T.);
#3010=ORIENTED_EDGE('',*,*,#2184,.T.);
#3011=ORIENTED_EDGE('',*,*,#2185,.F.);
#3012=ORIENTED_EDGE('',*,*,#2186,.F.);
#3013=ORIENTED_EDGE('',*,*,#2187,.F.);
#3014=ORIENTED_EDGE('',*,*,#2181,.T.);
#3015=ORIENTED_EDGE('',*,*,#2188,.T.);
#3016=ORIENTED_EDGE('',*,*,#2189,.F.);
#3017=ORIENTED_EDGE('',*,*,#2190,.F.);
#3018=ORIENTED_EDGE('',*,*,#2185,.T.);
#3019=ORIENTED_EDGE('',*,*,#2191,.T.);
#3020=ORIENTED_EDGE('',*,*,#2192,.T.);
#3021=ORIENTED_EDGE('',*,*,#2193,.F.);
#3022=ORIENTED_EDGE('',*,*,#2194,.F.);
#3023=ORIENTED_EDGE('',*,*,#2195,.F.);
#3024=ORIENTED_EDGE('',*,*,#2189,.T.);
#3025=ORIENTED_EDGE('',*,*,#2196,.T.);
#3026=ORIENTED_EDGE('',*,*,#2197,.F.);
#3027=ORIENTED_EDGE('',*,*,#2198,.F.);
#3028=ORIENTED_EDGE('',*,*,#2193,.T.);
#3029=ORIENTED_EDGE('',*,*,#2199,.T.);
#3030=ORIENTED_EDGE('',*,*,#2200,.T.);
#3031=ORIENTED_EDGE('',*,*,#2201,.F.);
#3032=ORIENTED_EDGE('',*,*,#2202,.F.);
#3033=ORIENTED_EDGE('',*,*,#2203,.F.);
#3034=ORIENTED_EDGE('',*,*,#2197,.T.);
#3035=ORIENTED_EDGE('',*,*,#2204,.T.);
#3036=ORIENTED_EDGE('',*,*,#2205,.F.);
#3037=ORIENTED_EDGE('',*,*,#2206,.F.);
#3038=ORIENTED_EDGE('',*,*,#2201,.T.);
#3039=ORIENTED_EDGE('',*,*,#2207,.T.);
#3040=ORIENTED_EDGE('',*,*,#2208,.T.);
#3041=ORIENTED_EDGE('',*,*,#2209,.F.);
#3042=ORIENTED_EDGE('',*,*,#2210,.F.);
#3043=ORIENTED_EDGE('',*,*,#2211,.F.);
#3044=ORIENTED_EDGE('',*,*,#2205,.T.);
#3045=ORIENTED_EDGE('',*,*,#2212,.T.);
#3046=ORIENTED_EDGE('',*,*,#2213,.F.);
#3047=ORIENTED_EDGE('',*,*,#2214,.F.);
#3048=ORIENTED_EDGE('',*,*,#2215,.F.);
#3049=ORIENTED_EDGE('',*,*,#2209,.T.);
#3050=ORIENTED_EDGE('',*,*,#2216,.T.);
#3051=ORIENTED_EDGE('',*,*,#2217,.T.);
#3052=ORIENTED_EDGE('',*,*,#2218,.F.);
#3053=ORIENTED_EDGE('',*,*,#2219,.F.);
#3054=ORIENTED_EDGE('',*,*,#2213,.T.);
#3055=ORIENTED_EDGE('',*,*,#2220,.T.);
#3056=ORIENTED_EDGE('',*,*,#2221,.F.);
#3057=ORIENTED_EDGE('',*,*,#2222,.F.);
#3058=ORIENTED_EDGE('',*,*,#2223,.F.);
#3059=ORIENTED_EDGE('',*,*,#2218,.T.);
#3060=ORIENTED_EDGE('',*,*,#2224,.T.);
#3061=ORIENTED_EDGE('',*,*,#2225,.T.);
#3062=ORIENTED_EDGE('',*,*,#2226,.T.);
#3063=ORIENTED_EDGE('',*,*,#2227,.F.);
#3064=ORIENTED_EDGE('',*,*,#2228,.T.);
#3065=ORIENTED_EDGE('',*,*,#2229,.T.);
#3066=ORIENTED_EDGE('',*,*,#2230,.T.);
#3067=ORIENTED_EDGE('',*,*,#2231,.T.);
#3068=ORIENTED_EDGE('',*,*,#2232,.T.);
#3069=ORIENTED_EDGE('',*,*,#2233,.T.);
#3070=ORIENTED_EDGE('',*,*,#2234,.T.);
#3071=ORIENTED_EDGE('',*,*,#2235,.T.);
#3072=ORIENTED_EDGE('',*,*,#2236,.T.);
#3073=ORIENTED_EDGE('',*,*,#2237,.T.);
#3074=ORIENTED_EDGE('',*,*,#2238,.T.);
#3075=ORIENTED_EDGE('',*,*,#2239,.T.);
#3076=ORIENTED_EDGE('',*,*,#2240,.T.);
#3077=ORIENTED_EDGE('',*,*,#2241,.T.);
#3078=ORIENTED_EDGE('',*,*,#2242,.T.);
#3079=ORIENTED_EDGE('',*,*,#2243,.T.);
#3080=ORIENTED_EDGE('',*,*,#2244,.T.);
#3081=ORIENTED_EDGE('',*,*,#2245,.T.);
#3082=ORIENTED_EDGE('',*,*,#2246,.T.);
#3083=ORIENTED_EDGE('',*,*,#2247,.T.);
#3084=ORIENTED_EDGE('',*,*,#2248,.T.);
#3085=ORIENTED_EDGE('',*,*,#2249,.T.);
#3086=ORIENTED_EDGE('',*,*,#2250,.T.);
#3087=ORIENTED_EDGE('',*,*,#2251,.T.);
#3088=ORIENTED_EDGE('',*,*,#2252,.T.);
#3089=ORIENTED_EDGE('',*,*,#2253,.T.);
#3090=ORIENTED_EDGE('',*,*,#2254,.T.);
#3091=ORIENTED_EDGE('',*,*,#2255,.T.);
#3092=ORIENTED_EDGE('',*,*,#2256,.T.);
#3093=ORIENTED_EDGE('',*,*,#2257,.F.);
#3094=ORIENTED_EDGE('',*,*,#2258,.T.);
#3095=ORIENTED_EDGE('',*,*,#2259,.T.);
#3096=ORIENTED_EDGE('',*,*,#2260,.T.);
#3097=ORIENTED_EDGE('',*,*,#2261,.T.);
#3098=ORIENTED_EDGE('',*,*,#2262,.T.);
#3099=ORIENTED_EDGE('',*,*,#2263,.T.);
#3100=ORIENTED_EDGE('',*,*,#2264,.T.);
#3101=ORIENTED_EDGE('',*,*,#2265,.T.);
#3102=ORIENTED_EDGE('',*,*,#2266,.T.);
#3103=ORIENTED_EDGE('',*,*,#2267,.T.);
#3104=ORIENTED_EDGE('',*,*,#2268,.T.);
#3105=ORIENTED_EDGE('',*,*,#2269,.T.);
#3106=ORIENTED_EDGE('',*,*,#2270,.T.);
#3107=ORIENTED_EDGE('',*,*,#2271,.T.);
#3108=ORIENTED_EDGE('',*,*,#2272,.T.);
#3109=ORIENTED_EDGE('',*,*,#2273,.T.);
#3110=ORIENTED_EDGE('',*,*,#2274,.T.);
#3111=ORIENTED_EDGE('',*,*,#2275,.T.);
#3112=ORIENTED_EDGE('',*,*,#2276,.T.);
#3113=ORIENTED_EDGE('',*,*,#2277,.T.);
#3114=ORIENTED_EDGE('',*,*,#2278,.T.);
#3115=ORIENTED_EDGE('',*,*,#2279,.T.);
#3116=ORIENTED_EDGE('',*,*,#2280,.T.);
#3117=ORIENTED_EDGE('',*,*,#2281,.T.);
#3118=ORIENTED_EDGE('',*,*,#2282,.T.);
#3119=ORIENTED_EDGE('',*,*,#2283,.T.);
#3120=ORIENTED_EDGE('',*,*,#2284,.T.);
#3121=ORIENTED_EDGE('',*,*,#2285,.T.);
#3122=ORIENTED_EDGE('',*,*,#2221,.T.);
#3123=ORIENTED_EDGE('',*,*,#2286,.T.);
#3124=ORIENTED_EDGE('',*,*,#2287,.F.);
#3125=ORIENTED_EDGE('',*,*,#2288,.F.);
#3126=ORIENTED_EDGE('',*,*,#2289,.F.);
#3127=ORIENTED_EDGE('',*,*,#2290,.F.);
#3128=ORIENTED_EDGE('',*,*,#2256,.F.);
#3129=ORIENTED_EDGE('',*,*,#2255,.F.);
#3130=ORIENTED_EDGE('',*,*,#2254,.F.);
#3131=ORIENTED_EDGE('',*,*,#2253,.F.);
#3132=ORIENTED_EDGE('',*,*,#2252,.F.);
#3133=ORIENTED_EDGE('',*,*,#2251,.F.);
#3134=ORIENTED_EDGE('',*,*,#2250,.F.);
#3135=ORIENTED_EDGE('',*,*,#2249,.F.);
#3136=ORIENTED_EDGE('',*,*,#2248,.F.);
#3137=ORIENTED_EDGE('',*,*,#2247,.F.);
#3138=ORIENTED_EDGE('',*,*,#2246,.F.);
#3139=ORIENTED_EDGE('',*,*,#2245,.F.);
#3140=ORIENTED_EDGE('',*,*,#2244,.F.);
#3141=ORIENTED_EDGE('',*,*,#2243,.F.);
#3142=ORIENTED_EDGE('',*,*,#2242,.F.);
#3143=ORIENTED_EDGE('',*,*,#2241,.F.);
#3144=ORIENTED_EDGE('',*,*,#2240,.F.);
#3145=ORIENTED_EDGE('',*,*,#2239,.F.);
#3146=ORIENTED_EDGE('',*,*,#2238,.F.);
#3147=ORIENTED_EDGE('',*,*,#2237,.F.);
#3148=ORIENTED_EDGE('',*,*,#2236,.F.);
#3149=ORIENTED_EDGE('',*,*,#2235,.F.);
#3150=ORIENTED_EDGE('',*,*,#2234,.F.);
#3151=ORIENTED_EDGE('',*,*,#2233,.F.);
#3152=ORIENTED_EDGE('',*,*,#2232,.F.);
#3153=ORIENTED_EDGE('',*,*,#2231,.F.);
#3154=ORIENTED_EDGE('',*,*,#2230,.F.);
#3155=ORIENTED_EDGE('',*,*,#2229,.F.);
#3156=ORIENTED_EDGE('',*,*,#2228,.F.);
#3157=ORIENTED_EDGE('',*,*,#2291,.F.);
#3158=ORIENTED_EDGE('',*,*,#2112,.T.);
#3159=ORIENTED_EDGE('',*,*,#2117,.T.);
#3160=ORIENTED_EDGE('',*,*,#2116,.T.);
#3161=ORIENTED_EDGE('',*,*,#2121,.T.);
#3162=ORIENTED_EDGE('',*,*,#2125,.T.);
#3163=ORIENTED_EDGE('',*,*,#2124,.T.);
#3164=ORIENTED_EDGE('',*,*,#2129,.T.);
#3165=ORIENTED_EDGE('',*,*,#2134,.T.);
#3166=ORIENTED_EDGE('',*,*,#2133,.T.);
#3167=ORIENTED_EDGE('',*,*,#2137,.T.);
#3168=ORIENTED_EDGE('',*,*,#2142,.T.);
#3169=ORIENTED_EDGE('',*,*,#2141,.T.);
#3170=ORIENTED_EDGE('',*,*,#2145,.T.);
#3171=ORIENTED_EDGE('',*,*,#2150,.T.);
#3172=ORIENTED_EDGE('',*,*,#2149,.T.);
#3173=ORIENTED_EDGE('',*,*,#2153,.T.);
#3174=ORIENTED_EDGE('',*,*,#2158,.T.);
#3175=ORIENTED_EDGE('',*,*,#2157,.T.);
#3176=ORIENTED_EDGE('',*,*,#2162,.T.);
#3177=ORIENTED_EDGE('',*,*,#2161,.T.);
#3178=ORIENTED_EDGE('',*,*,#2166,.T.);
#3179=ORIENTED_EDGE('',*,*,#2170,.T.);
#3180=ORIENTED_EDGE('',*,*,#2169,.T.);
#3181=ORIENTED_EDGE('',*,*,#2174,.T.);
#3182=ORIENTED_EDGE('',*,*,#2178,.T.);
#3183=ORIENTED_EDGE('',*,*,#2177,.T.);
#3184=ORIENTED_EDGE('',*,*,#2182,.T.);
#3185=ORIENTED_EDGE('',*,*,#2187,.T.);
#3186=ORIENTED_EDGE('',*,*,#2186,.T.);
#3187=ORIENTED_EDGE('',*,*,#2190,.T.);
#3188=ORIENTED_EDGE('',*,*,#2195,.T.);
#3189=ORIENTED_EDGE('',*,*,#2194,.T.);
#3190=ORIENTED_EDGE('',*,*,#2198,.T.);
#3191=ORIENTED_EDGE('',*,*,#2203,.T.);
#3192=ORIENTED_EDGE('',*,*,#2202,.T.);
#3193=ORIENTED_EDGE('',*,*,#2206,.T.);
#3194=ORIENTED_EDGE('',*,*,#2211,.T.);
#3195=ORIENTED_EDGE('',*,*,#2210,.T.);
#3196=ORIENTED_EDGE('',*,*,#2215,.T.);
#3197=ORIENTED_EDGE('',*,*,#2214,.T.);
#3198=ORIENTED_EDGE('',*,*,#2219,.T.);
#3199=ORIENTED_EDGE('',*,*,#2223,.T.);
#3200=ORIENTED_EDGE('',*,*,#2222,.T.);
#3201=ORIENTED_EDGE('',*,*,#2289,.T.);
#3202=ORIENTED_EDGE('',*,*,#2288,.T.);
#3203=ORIENTED_EDGE('',*,*,#2292,.F.);
#3204=ORIENTED_EDGE('',*,*,#2293,.F.);
#3205=ORIENTED_EDGE('',*,*,#2286,.F.);
#3206=ORIENTED_EDGE('',*,*,#2225,.F.);
#3207=ORIENTED_EDGE('',*,*,#2224,.F.);
#3208=ORIENTED_EDGE('',*,*,#2220,.F.);
#3209=ORIENTED_EDGE('',*,*,#2217,.F.);
#3210=ORIENTED_EDGE('',*,*,#2216,.F.);
#3211=ORIENTED_EDGE('',*,*,#2212,.F.);
#3212=ORIENTED_EDGE('',*,*,#2208,.F.);
#3213=ORIENTED_EDGE('',*,*,#2207,.F.);
#3214=ORIENTED_EDGE('',*,*,#2204,.F.);
#3215=ORIENTED_EDGE('',*,*,#2200,.F.);
#3216=ORIENTED_EDGE('',*,*,#2199,.F.);
#3217=ORIENTED_EDGE('',*,*,#2196,.F.);
#3218=ORIENTED_EDGE('',*,*,#2192,.F.);
#3219=ORIENTED_EDGE('',*,*,#2191,.F.);
#3220=ORIENTED_EDGE('',*,*,#2188,.F.);
#3221=ORIENTED_EDGE('',*,*,#2184,.F.);
#3222=ORIENTED_EDGE('',*,*,#2183,.F.);
#3223=ORIENTED_EDGE('',*,*,#2180,.F.);
#3224=ORIENTED_EDGE('',*,*,#2179,.F.);
#3225=ORIENTED_EDGE('',*,*,#2175,.F.);
#3226=ORIENTED_EDGE('',*,*,#2172,.F.);
#3227=ORIENTED_EDGE('',*,*,#2171,.F.);
#3228=ORIENTED_EDGE('',*,*,#2167,.F.);
#3229=ORIENTED_EDGE('',*,*,#2164,.F.);
#3230=ORIENTED_EDGE('',*,*,#2163,.F.);
#3231=ORIENTED_EDGE('',*,*,#2159,.F.);
#3232=ORIENTED_EDGE('',*,*,#2155,.F.);
#3233=ORIENTED_EDGE('',*,*,#2154,.F.);
#3234=ORIENTED_EDGE('',*,*,#2151,.F.);
#3235=ORIENTED_EDGE('',*,*,#2147,.F.);
#3236=ORIENTED_EDGE('',*,*,#2146,.F.);
#3237=ORIENTED_EDGE('',*,*,#2143,.F.);
#3238=ORIENTED_EDGE('',*,*,#2139,.F.);
#3239=ORIENTED_EDGE('',*,*,#2138,.F.);
#3240=ORIENTED_EDGE('',*,*,#2135,.F.);
#3241=ORIENTED_EDGE('',*,*,#2131,.F.);
#3242=ORIENTED_EDGE('',*,*,#2130,.F.);
#3243=ORIENTED_EDGE('',*,*,#2127,.F.);
#3244=ORIENTED_EDGE('',*,*,#2126,.F.);
#3245=ORIENTED_EDGE('',*,*,#2122,.F.);
#3246=ORIENTED_EDGE('',*,*,#2119,.F.);
#3247=ORIENTED_EDGE('',*,*,#2118,.F.);
#3248=ORIENTED_EDGE('',*,*,#2114,.F.);
#3249=ORIENTED_EDGE('',*,*,#2294,.F.);
#3250=ORIENTED_EDGE('',*,*,#2226,.F.);
#3251=ORIENTED_EDGE('',*,*,#2285,.F.);
#3252=ORIENTED_EDGE('',*,*,#2284,.F.);
#3253=ORIENTED_EDGE('',*,*,#2283,.F.);
#3254=ORIENTED_EDGE('',*,*,#2282,.F.);
#3255=ORIENTED_EDGE('',*,*,#2281,.F.);
#3256=ORIENTED_EDGE('',*,*,#2280,.F.);
#3257=ORIENTED_EDGE('',*,*,#2279,.F.);
#3258=ORIENTED_EDGE('',*,*,#2278,.F.);
#3259=ORIENTED_EDGE('',*,*,#2277,.F.);
#3260=ORIENTED_EDGE('',*,*,#2276,.F.);
#3261=ORIENTED_EDGE('',*,*,#2275,.F.);
#3262=ORIENTED_EDGE('',*,*,#2274,.F.);
#3263=ORIENTED_EDGE('',*,*,#2273,.F.);
#3264=ORIENTED_EDGE('',*,*,#2272,.F.);
#3265=ORIENTED_EDGE('',*,*,#2271,.F.);
#3266=ORIENTED_EDGE('',*,*,#2270,.F.);
#3267=ORIENTED_EDGE('',*,*,#2269,.F.);
#3268=ORIENTED_EDGE('',*,*,#2268,.F.);
#3269=ORIENTED_EDGE('',*,*,#2267,.F.);
#3270=ORIENTED_EDGE('',*,*,#2266,.F.);
#3271=ORIENTED_EDGE('',*,*,#2265,.F.);
#3272=ORIENTED_EDGE('',*,*,#2264,.F.);
#3273=ORIENTED_EDGE('',*,*,#2263,.F.);
#3274=ORIENTED_EDGE('',*,*,#2262,.F.);
#3275=ORIENTED_EDGE('',*,*,#2261,.F.);
#3276=ORIENTED_EDGE('',*,*,#2260,.F.);
#3277=ORIENTED_EDGE('',*,*,#2259,.F.);
#3278=ORIENTED_EDGE('',*,*,#2258,.F.);
#3279=ORIENTED_EDGE('',*,*,#2290,.T.);
#3280=ORIENTED_EDGE('',*,*,#2287,.T.);
#3281=ORIENTED_EDGE('',*,*,#2293,.T.);
#3282=ORIENTED_EDGE('',*,*,#2292,.T.);
#3283=ORIENTED_EDGE('',*,*,#2257,.T.);
#3284=ORIENTED_EDGE('',*,*,#2291,.T.);
#3285=ORIENTED_EDGE('',*,*,#2227,.T.);
#3286=ORIENTED_EDGE('',*,*,#2294,.T.);
#3287=ORIENTED_EDGE('',*,*,#2113,.T.);
#3806=PLANE('',#4299);
#3807=PLANE('',#4300);
#3908=ADVANCED_FACE('',(#712),#425,.T.);
#3909=ADVANCED_FACE('',(#713),#426,.T.);
#3910=ADVANCED_FACE('',(#714),#427,.T.);
#3911=ADVANCED_FACE('',(#715),#428,.T.);
#3912=ADVANCED_FACE('',(#716),#429,.T.);
#3913=ADVANCED_FACE('',(#717),#430,.T.);
#3914=ADVANCED_FACE('',(#718),#431,.T.);
#3915=ADVANCED_FACE('',(#719),#432,.T.);
#3916=ADVANCED_FACE('',(#720),#433,.T.);
#3917=ADVANCED_FACE('',(#721),#434,.T.);
#3918=ADVANCED_FACE('',(#722),#435,.T.);
#3919=ADVANCED_FACE('',(#723),#436,.T.);
#3920=ADVANCED_FACE('',(#724),#437,.T.);
#3921=ADVANCED_FACE('',(#725),#438,.T.);
#3922=ADVANCED_FACE('',(#726),#439,.T.);
#3923=ADVANCED_FACE('',(#727),#440,.T.);
#3924=ADVANCED_FACE('',(#728),#441,.T.);
#3925=ADVANCED_FACE('',(#729),#442,.T.);
#3926=ADVANCED_FACE('',(#730),#443,.T.);
#3927=ADVANCED_FACE('',(#731),#444,.T.);
#3928=ADVANCED_FACE('',(#732),#445,.T.);
#3929=ADVANCED_FACE('',(#733),#446,.T.);
#3930=ADVANCED_FACE('',(#734),#447,.T.);
#3931=ADVANCED_FACE('',(#735),#448,.T.);
#3932=ADVANCED_FACE('',(#736),#449,.T.);
#3933=ADVANCED_FACE('',(#737),#450,.T.);
#3934=ADVANCED_FACE('',(#738),#451,.T.);
#3935=ADVANCED_FACE('',(#739),#452,.T.);
#3936=ADVANCED_FACE('',(#740),#453,.T.);
#3937=ADVANCED_FACE('',(#741),#454,.T.);
#3938=ADVANCED_FACE('',(#742),#88,.F.);
#3939=ADVANCED_FACE('',(#743),#89,.F.);
#3940=ADVANCED_FACE('',(#744),#3806,.T.);
#3941=ADVANCED_FACE('',(#745),#3807,.F.);
#4036=CLOSED_SHELL('',(#3908,#3909,#3910,#3911,#3912,#3913,#3914,#3915,
#3916,#3917,#3918,#3919,#3920,#3921,#3922,#3923,#3924,#3925,#3926,#3927,
#3928,#3929,#3930,#3931,#3932,#3933,#3934,#3935,#3936,#3937,#3938,#3939,
#3940,#3941));
#4264=AXIS2_PLACEMENT_3D('',#11675,#4801,#4802);
#4265=AXIS2_PLACEMENT_3D('',#11676,#4803,#4804);
#4266=AXIS2_PLACEMENT_3D('',#11794,#4806,#4807);
#4267=AXIS2_PLACEMENT_3D('',#11865,#4808,#4809);
#4268=AXIS2_PLACEMENT_3D('',#12370,#4811,#4812);
#4269=AXIS2_PLACEMENT_3D('',#12812,#4814,#4815);
#4270=AXIS2_PLACEMENT_3D('',#13200,#4817,#4818);
#4271=AXIS2_PLACEMENT_3D('',#13593,#4820,#4821);
#4272=AXIS2_PLACEMENT_3D('',#14070,#4823,#4824);
#4273=AXIS2_PLACEMENT_3D('',#14565,#4826,#4827);
#4274=AXIS2_PLACEMENT_3D('',#15042,#4829,#4830);
#4275=AXIS2_PLACEMENT_3D('',#15531,#4832,#4833);
#4276=AXIS2_PLACEMENT_3D('',#15988,#4835,#4836);
#4277=AXIS2_PLACEMENT_3D('',#16529,#4838,#4839);
#4278=AXIS2_PLACEMENT_3D('',#16846,#4841,#4842);
#4279=AXIS2_PLACEMENT_3D('',#17274,#4844,#4845);
#4280=AXIS2_PLACEMENT_3D('',#17728,#4847,#4848);
#4281=AXIS2_PLACEMENT_3D('',#18216,#4850,#4851);
#4282=AXIS2_PLACEMENT_3D('',#18660,#4853,#4854);
#4283=AXIS2_PLACEMENT_3D('',#19056,#4856,#4857);
#4284=AXIS2_PLACEMENT_3D('',#19481,#4859,#4860);
#4285=AXIS2_PLACEMENT_3D('',#19942,#4862,#4863);
#4286=AXIS2_PLACEMENT_3D('',#20391,#4865,#4866);
#4287=AXIS2_PLACEMENT_3D('',#20860,#4868,#4869);
#4288=AXIS2_PLACEMENT_3D('',#21305,#4871,#4872);
#4289=AXIS2_PLACEMENT_3D('',#21806,#4874,#4875);
#4290=AXIS2_PLACEMENT_3D('',#22265,#4877,#4878);
#4291=AXIS2_PLACEMENT_3D('',#22567,#4880,#4881);
#4292=AXIS2_PLACEMENT_3D('',#22983,#4883,#4884);
#4293=AXIS2_PLACEMENT_3D('',#23421,#4886,#4887);
#4294=AXIS2_PLACEMENT_3D('',#23919,#4889,#4890);
#4295=AXIS2_PLACEMENT_3D('',#23996,#4891,#4892);
#4296=AXIS2_PLACEMENT_3D('',#27732,#4893,#4894);
#4297=AXIS2_PLACEMENT_3D('',#31498,#4895,#4896);
#4298=AXIS2_PLACEMENT_3D('',#31645,#4897,#4898);
#4299=AXIS2_PLACEMENT_3D('',#33568,#4899,#4900);
#4300=AXIS2_PLACEMENT_3D('',#33569,#4901,#4902);
#4801=DIRECTION('axis',(0.,0.,1.));
#4802=DIRECTION('refdir',(1.,0.,0.));
#4803=DIRECTION('center_axis',(0.,0.,1.));
#4804=DIRECTION('ref_axis',(0.457762905907022,0.889074306217179,0.));
#4805=DIRECTION('',(0.,0.,-1.));
#4806=DIRECTION('center_axis',(0.,0.,-1.));
#4807=DIRECTION('ref_axis',(-1.,1.34107269471161E-13,0.));
#4808=DIRECTION('center_axis',(0.,0.,1.));
#4809=DIRECTION('ref_axis',(0.457762905907022,0.889074306217179,0.));
#4810=DIRECTION('',(0.,0.,-1.));
#4811=DIRECTION('center_axis',(0.,0.,1.));
#4812=DIRECTION('ref_axis',(0.457762905907022,0.889074306217179,0.));
#4813=DIRECTION('',(0.,0.,-1.));
#4814=DIRECTION('center_axis',(0.,0.,1.));
#4815=DIRECTION('ref_axis',(0.457762905907022,0.889074306217179,0.));
#4816=DIRECTION('',(0.,0.,-1.));
#4817=DIRECTION('center_axis',(0.,0.,1.));
#4818=DIRECTION('ref_axis',(0.457762905907022,0.889074306217179,0.));
#4819=DIRECTION('',(0.,0.,-1.));
#4820=DIRECTION('center_axis',(0.,0.,1.));
#4821=DIRECTION('ref_axis',(0.457762905907022,0.889074306217179,0.));
#4822=DIRECTION('',(0.,0.,-1.));
#4823=DIRECTION('center_axis',(0.,0.,1.));
#4824=DIRECTION('ref_axis',(0.457762905907022,0.889074306217179,0.));
#4825=DIRECTION('',(0.,0.,-1.));
#4826=DIRECTION('center_axis',(0.,0.,1.));
#4827=DIRECTION('ref_axis',(0.457762905907022,0.889074306217179,0.));
#4828=DIRECTION('',(0.,0.,-1.));
#4829=DIRECTION('center_axis',(0.,0.,1.));
#4830=DIRECTION('ref_axis',(0.457762905907022,0.889074306217179,0.));
#4831=DIRECTION('',(0.,0.,-1.));
#4832=DIRECTION('center_axis',(0.,0.,1.));
#4833=DIRECTION('ref_axis',(0.457762905907022,0.889074306217179,0.));
#4834=DIRECTION('',(0.,0.,-1.));
#4835=DIRECTION('center_axis',(0.,0.,1.));
#4836=DIRECTION('ref_axis',(0.457762905907022,0.889074306217179,0.));
#4837=DIRECTION('',(0.,0.,-1.));
#4838=DIRECTION('center_axis',(0.,0.,1.));
#4839=DIRECTION('ref_axis',(0.457762905907022,0.889074306217179,0.));
#4840=DIRECTION('',(0.,0.,-1.));
#4841=DIRECTION('center_axis',(0.,0.,1.));
#4842=DIRECTION('ref_axis',(0.457762905907022,0.889074306217179,0.));
#4843=DIRECTION('',(0.,0.,-1.));
#4844=DIRECTION('center_axis',(0.,0.,1.));
#4845=DIRECTION('ref_axis',(0.457762905907022,0.889074306217179,0.));
#4846=DIRECTION('',(0.,0.,-1.));
#4847=DIRECTION('center_axis',(0.,0.,1.));
#4848=DIRECTION('ref_axis',(0.457762905907022,0.889074306217179,0.));
#4849=DIRECTION('',(0.,0.,-1.));
#4850=DIRECTION('center_axis',(0.,0.,1.));
#4851=DIRECTION('ref_axis',(0.457762905907022,0.889074306217179,0.));
#4852=DIRECTION('',(0.,0.,-1.));
#4853=DIRECTION('center_axis',(0.,0.,1.));
#4854=DIRECTION('ref_axis',(0.457762905907022,0.889074306217179,0.));
#4855=DIRECTION('',(0.,0.,-1.));
#4856=DIRECTION('center_axis',(0.,0.,1.));
#4857=DIRECTION('ref_axis',(0.457762905907022,0.889074306217179,0.));
#4858=DIRECTION('',(0.,0.,-1.));
#4859=DIRECTION('center_axis',(0.,0.,1.));
#4860=DIRECTION('ref_axis',(0.457762905907022,0.889074306217179,0.));
#4861=DIRECTION('',(0.,0.,-1.));
#4862=DIRECTION('center_axis',(0.,0.,1.));
#4863=DIRECTION('ref_axis',(0.457762905907022,0.889074306217179,0.));
#4864=DIRECTION('',(0.,0.,-1.));
#4865=DIRECTION('center_axis',(0.,0.,1.));
#4866=DIRECTION('ref_axis',(0.457762905907022,0.889074306217179,0.));
#4867=DIRECTION('',(0.,0.,-1.));
#4868=DIRECTION('center_axis',(0.,0.,1.));
#4869=DIRECTION('ref_axis',(0.457762905907022,0.889074306217179,0.));
#4870=DIRECTION('',(0.,0.,-1.));
#4871=DIRECTION('center_axis',(0.,0.,1.));
#4872=DIRECTION('ref_axis',(0.457762905907022,0.889074306217179,0.));
#4873=DIRECTION('',(0.,0.,-1.));
#4874=DIRECTION('center_axis',(0.,0.,1.));
#4875=DIRECTION('ref_axis',(0.457762905907022,0.889074306217179,0.));
#4876=DIRECTION('',(0.,0.,-1.));
#4877=DIRECTION('center_axis',(0.,0.,1.));
#4878=DIRECTION('ref_axis',(0.457762905907022,0.889074306217179,0.));
#4879=DIRECTION('',(0.,0.,-1.));
#4880=DIRECTION('center_axis',(0.,0.,1.));
#4881=DIRECTION('ref_axis',(0.457762905907022,0.889074306217179,0.));
#4882=DIRECTION('',(0.,0.,-1.));
#4883=DIRECTION('center_axis',(0.,0.,1.));
#4884=DIRECTION('ref_axis',(0.457762905907022,0.889074306217179,0.));
#4885=DIRECTION('',(0.,0.,-1.));
#4886=DIRECTION('center_axis',(0.,0.,1.));
#4887=DIRECTION('ref_axis',(0.457762905907022,0.889074306217179,0.));
#4888=DIRECTION('',(0.,0.,-1.));
#4889=DIRECTION('center_axis',(0.,0.,1.));
#4890=DIRECTION('ref_axis',(-1.,0.,0.));
#4891=DIRECTION('center_axis',(0.,0.,-1.));
#4892=DIRECTION('ref_axis',(-1.,0.,0.));
#4893=DIRECTION('center_axis',(0.,0.,-1.));
#4894=DIRECTION('ref_axis',(-1.,0.,0.));
#4895=DIRECTION('center_axis',(0.,0.,1.));
#4896=DIRECTION('ref_axis',(0.457762905907022,0.889074306217179,0.));
#4897=DIRECTION('center_axis',(0.,0.,1.));
#4898=DIRECTION('ref_axis',(-1.,1.34107269471161E-13,0.));
#4899=DIRECTION('center_axis',(0.,0.,1.));
#4900=DIRECTION('ref_axis',(-1.,0.,0.));
#4901=DIRECTION('center_axis',(0.,0.,1.));
#4902=DIRECTION('ref_axis',(-1.,0.,0.));
#11675=CARTESIAN_POINT('',(0.,0.,0.));
#11676=CARTESIAN_POINT('Origin',(0.,0.,4.68922655072688));
#11677=CARTESIAN_POINT('',(-1.47525540501185,-2.86526422036142,7.65376407014636));
#11678=CARTESIAN_POINT('',(-1.47525540501185,-2.86526422036142,7.40717138384282));
#11679=CARTESIAN_POINT('',(-1.47525540501186,-2.86526422036142,4.68922655072688));
#11680=CARTESIAN_POINT('',(1.87152456426716,2.62364505370765,7.00006724526264));
#11681=CARTESIAN_POINT('Ctrl Pts',(1.87152456426716,2.62364505370765,7.00006724526264));
#11682=CARTESIAN_POINT('Ctrl Pts',(1.79127682369291,2.68088816953973,7.00618730725958));
#11683=CARTESIAN_POINT('Ctrl Pts',(1.70825160021717,2.73455212168423,7.01230736925651));
#11684=CARTESIAN_POINT('Ctrl Pts',(1.62280488302109,2.78435304409174,7.01842743125345));
#11685=CARTESIAN_POINT('Ctrl Pts',(1.53747062668585,2.83408842091963,7.02453943831904));
#11686=CARTESIAN_POINT('Ctrl Pts',(1.44972158771444,2.87997064926674,7.03065144538463));
#11687=CARTESIAN_POINT('Ctrl Pts',(1.35994463582073,2.92175771582834,7.03676345245022));
#11688=CARTESIAN_POINT('Ctrl Pts',(1.26815769042948,2.96448034246742,7.04301229969806));
#11689=CARTESIAN_POINT('Ctrl Pts',(1.17425130695441,3.00292194634153,7.0492611469459));
#11690=CARTESIAN_POINT('Ctrl Pts',(1.07866802208888,3.03687221670963,7.05550999419374));
#11691=CARTESIAN_POINT('Ctrl Pts',(0.98533379127609,3.07002364454715,7.06161180741521));
#11692=CARTESIAN_POINT('Ctrl Pts',(0.890401144946329,3.09889261286461,7.06771362063667));
#11693=CARTESIAN_POINT('Ctrl Pts',(0.794303269988383,3.12333153504167,7.07381543385814));
#11694=CARTESIAN_POINT('Ctrl Pts',(0.698234643998841,3.14776301883091,7.07991538989242));
#11695=CARTESIAN_POINT('Ctrl Pts',(0.601001922285462,3.16776702607249,7.0860153459267));
#11696=CARTESIAN_POINT('Ctrl Pts',(0.503052557517713,3.18324609272907,7.09211530196098));
#11697=CARTESIAN_POINT('Ctrl Pts',(0.405105726564905,3.19872475896355,7.09821510019781));
#11698=CARTESIAN_POINT('Ctrl Pts',(0.30644272650644,3.20967864914956,7.10431489843464));
#11699=CARTESIAN_POINT('Ctrl Pts',(0.207519177167271,3.21606177701981,7.11041469667147));
#11700=CARTESIAN_POINT('Ctrl Pts',(0.104374329965198,3.22271728779804,7.11677478748205));
#11701=CARTESIAN_POINT('Ctrl Pts',(0.000946722460567373,3.22440320262582,
7.12313487829262));
#11702=CARTESIAN_POINT('Ctrl Pts',(-0.102245417469026,3.22112766544677,
7.1294949691032));
#11703=CARTESIAN_POINT('Ctrl Pts',(-0.201349360971802,3.21798189628495,
7.13560309013639));
#11704=CARTESIAN_POINT('Ctrl Pts',(-0.30023569264504,3.21026042906621,7.14171121116958));
#11705=CARTESIAN_POINT('Ctrl Pts',(-0.398450710501723,3.1980235449103,7.14781933220276));
#11706=CARTESIAN_POINT('Ctrl Pts',(-0.496732126942532,3.18577838796883,
7.15393158265116));
#11707=CARTESIAN_POINT('Ctrl Pts',(-0.594340891938124,3.16901181580139,
7.16004383309956));
#11708=CARTESIAN_POINT('Ctrl Pts',(-0.690834245690382,3.14783506675324,
7.16615608354795));
#11709=CARTESIAN_POINT('Ctrl Pts',(-0.787468407724652,3.12662741545602,
7.17227725332034));
#11710=CARTESIAN_POINT('Ctrl Pts',(-0.882983487642857,3.10099686775126,
7.17839842309272));
#11711=CARTESIAN_POINT('Ctrl Pts',(-0.976953019268458,3.07110409472591,
7.1845195928651));
#11712=CARTESIAN_POINT('Ctrl Pts',(-0.988293698477211,3.06749649613862,
7.18525832404286));
#11713=CARTESIAN_POINT('Ctrl Pts',(-0.99961189323101,3.0638268757802,7.18599705522062));
#11714=CARTESIAN_POINT('Ctrl Pts',(-1.01090687624163,3.06009556224432,7.18673578639837));
#11715=CARTESIAN_POINT('Ctrl Pts',(-1.10543852769614,3.02886689812778,7.19291848522568));
#11716=CARTESIAN_POINT('Ctrl Pts',(-1.19868177442532,2.99320091442327,7.19910118405298));
#11717=CARTESIAN_POINT('Ctrl Pts',(-1.29019080625755,2.95322285748104,7.20528388288029));
#11718=CARTESIAN_POINT('Ctrl Pts',(-1.3815790573384,2.9132975666938,7.21145842129987));
#11719=CARTESIAN_POINT('Ctrl Pts',(-1.47123725036822,2.86907168796002,7.21763295971945));
#11720=CARTESIAN_POINT('Ctrl Pts',(-1.55873551592881,2.82071997083761,7.22380749813904));
#11721=CARTESIAN_POINT('Ctrl Pts',(-1.64614388885164,2.77241792856721,7.22997569305522));
#11722=CARTESIAN_POINT('Ctrl Pts',(-1.73139636969943,2.71999868399673,7.23614388797139));
#11723=CARTESIAN_POINT('Ctrl Pts',(-1.81408470890849,2.66368433403893,7.24231208288757));
#11724=CARTESIAN_POINT('Ctrl Pts',(-1.89671587603632,2.60740892075128,7.24847601301207));
#11725=CARTESIAN_POINT('Ctrl Pts',(-1.97678606976541,2.54724399940528,7.25463994313658));
#11726=CARTESIAN_POINT('Ctrl Pts',(-2.05391399381773,2.48345623446432,7.26080387326108));
#11727=CARTESIAN_POINT('Ctrl Pts',(-2.13101448396032,2.41969115842374,7.26696561091502));
#11728=CARTESIAN_POINT('Ctrl Pts',(-2.20517445103947,2.35230607499375,7.27312734856897));
#11729=CARTESIAN_POINT('Ctrl Pts',(-2.2760445269573,2.28160883453052,7.27928908622291));
#11730=CARTESIAN_POINT('Ctrl Pts',(-2.34690816624739,2.21091801499761,7.28545026424981));
#11731=CARTESIAN_POINT('Ctrl Pts',(-2.41448220220194,2.13691594216141,7.29161144227671));
#11732=CARTESIAN_POINT('Ctrl Pts',(-2.47845380927167,2.05994763957892,7.2977726203036));
#11733=CARTESIAN_POINT('Ctrl Pts',(-2.54243655018751,1.98296594115918,7.30393487064384));
#11734=CARTESIAN_POINT('Ctrl Pts',(-2.60281534004262,1.90301732011431,7.31009712098408));
#11735=CARTESIAN_POINT('Ctrl Pts',(-2.65931799386684,1.82047943410412,7.31625937132433));
#11736=CARTESIAN_POINT('Ctrl Pts',(-2.71588198103346,1.73785195363984,7.32242831075587));
#11737=CARTESIAN_POINT('Ctrl Pts',(-2.76856118534086,1.65262995338251,7.32859725018741));
#11738=CARTESIAN_POINT('Ctrl Pts',(-2.81712715630606,1.56521952061139,7.33476618961895));
#11739=CARTESIAN_POINT('Ctrl Pts',(-2.86572077106075,1.47775933375208,7.34093864041574));
#11740=CARTESIAN_POINT('Ctrl Pts',(-2.9101962972974,1.38810862107274,7.34711109121254));
#11741=CARTESIAN_POINT('Ctrl Pts',(-2.9503725327185,1.296695600625,7.35328354200934));
#11742=CARTESIAN_POINT('Ctrl Pts',(-2.99061595500699,1.20512970984437,7.35946631501847));
#11743=CARTESIAN_POINT('Ctrl Pts',(-3.02654556955357,1.11179602839463,7.36564908802761));
#11744=CARTESIAN_POINT('Ctrl Pts',(-3.05802929386376,1.01714030515514,7.37183186103675));
#11745=CARTESIAN_POINT('Ctrl Pts',(-3.081515842817,0.946528065775037,7.37644414894511));
#11746=CARTESIAN_POINT('Ctrl Pts',(-3.10252928054058,0.875180462760919,
7.38105643685346));
#11747=CARTESIAN_POINT('Ctrl Pts',(-3.1210333525377,0.803285985715719,7.38566872476182));
#11748=CARTESIAN_POINT('Ctrl Pts',(-3.14576188247488,0.707207418349198,
7.39183250858402));
#11749=CARTESIAN_POINT('Ctrl Pts',(-3.16609437828951,0.609812275758225,
7.39799629240622));
#11750=CARTESIAN_POINT('Ctrl Pts',(-3.18189322309051,0.51153990983176,7.40416007622841));
#11751=CARTESIAN_POINT('Ctrl Pts',(-3.19767035311234,0.413402614712841,
7.41031538821572));
#11752=CARTESIAN_POINT('Ctrl Pts',(-3.20892614793691,0.314390918801613,
7.41647070020303));
#11753=CARTESIAN_POINT('Ctrl Pts',(-3.21557314781084,0.214957887917286,
7.42262601219034));
#11754=CARTESIAN_POINT('Ctrl Pts',(-3.22221299064851,0.115631919741172,
7.42877469655738));
#11755=CARTESIAN_POINT('Ctrl Pts',(-3.2242538746182,0.0158859507229964,
7.43492338092442));
#11756=CARTESIAN_POINT('Ctrl Pts',(-3.22165980543998,-0.0838192132654753,
7.44107206529145));
#11757=CARTESIAN_POINT('Ctrl Pts',(-3.21906768223833,-0.183449582057625,
7.44721613713858));
#11758=CARTESIAN_POINT('Ctrl Pts',(-3.21184752969372,-0.283038772450925,
7.4533602089857));
#11759=CARTESIAN_POINT('Ctrl Pts',(-3.20001540502417,-0.382124286205456,
7.45950428083282));
#11760=CARTESIAN_POINT('Ctrl Pts',(-3.18818790171217,-0.481171099422168,
7.46564595294586));
#11761=CARTESIAN_POINT('Ctrl Pts',(-3.17175205680164,-0.579714194694247,
7.47178762505889));
#11762=CARTESIAN_POINT('Ctrl Pts',(-3.15077585500389,-0.677295411194052,
7.47792929717193));
#11763=CARTESIAN_POINT('Ctrl Pts',(-3.1298021927133,-0.774864813915528,
7.48407022573661));
#11764=CARTESIAN_POINT('Ctrl Pts',(-3.10428935783583,-0.871472143348168,
7.49021115430129));
#11765=CARTESIAN_POINT('Ctrl Pts',(-3.07435640514299,-0.966669672978465,
7.49635208286598));
#11766=CARTESIAN_POINT('Ctrl Pts',(-3.04441900906306,-1.06188133417401,
7.50249392301873));
#11767=CARTESIAN_POINT('Ctrl Pts',(-3.010060322785,-1.15568236421211,7.50863576317149));
#11768=CARTESIAN_POINT('Ctrl Pts',(-2.97144888083816,-1.24764141926504,
7.51477760332424));
#11769=CARTESIAN_POINT('Ctrl Pts',(-2.93279616806333,-1.33969876710763,
7.52092600834005));
#11770=CARTESIAN_POINT('Ctrl Pts',(-2.8898817913854,-1.42990980580736,7.52707441335585));
#11771=CARTESIAN_POINT('Ctrl Pts',(-2.84292190183757,-1.51786449413386,
7.53322281837165));
#11772=CARTESIAN_POINT('Ctrl Pts',(-2.79593596524847,-1.60586796791149,
7.53937463369699));
#11773=CARTESIAN_POINT('Ctrl Pts',(-2.74490027030643,-1.69161222466882,
7.54552644902233));
#11774=CARTESIAN_POINT('Ctrl Pts',(-2.69007518096602,-1.77471493013685,
7.55167826434767));
#11775=CARTESIAN_POINT('Ctrl Pts',(-2.63515766627508,-1.85795773198731,
7.55784045053961));
#11776=CARTESIAN_POINT('Ctrl Pts',(-2.57643825363058,-1.93854973511658,
7.56400263673155));
#11777=CARTESIAN_POINT('Ctrl Pts',(-2.51421866168475,-2.01614039286359,
7.57016482292349));
#11778=CARTESIAN_POINT('Ctrl Pts',(-2.46562907143422,-2.07673381929555,
7.57497710299074));
#11779=CARTESIAN_POINT('Ctrl Pts',(-2.4149057024178,-2.13549746859355,7.579789383058));
#11780=CARTESIAN_POINT('Ctrl Pts',(-2.36220738045403,-2.19228051449364,
7.58460166312525));
#11781=CARTESIAN_POINT('Ctrl Pts',(-2.29461677109524,-2.26511017074482,
7.59077386994381));
#11782=CARTESIAN_POINT('Ctrl Pts',(-2.22353619037049,-2.33493893300441,
7.59694607676236));
#11783=CARTESIAN_POINT('Ctrl Pts',(-2.14926265549304,-2.40141366703094,
7.60311828358091));
#11784=CARTESIAN_POINT('Ctrl Pts',(-2.07507717426126,-2.46780959313907,
7.60928317305132));
#11785=CARTESIAN_POINT('Ctrl Pts',(-1.9977065768573,-2.53085910109103,7.61544806252174));
#11786=CARTESIAN_POINT('Ctrl Pts',(-1.91748654889088,-2.59024379109816,
7.62161295199215));
#11787=CARTESIAN_POINT('Ctrl Pts',(-1.83735475836048,-2.64956316134764,
7.62777106043725));
#11788=CARTESIAN_POINT('Ctrl Pts',(-1.75438011671107,-2.70522547284929,
7.63392916888235));
#11789=CARTESIAN_POINT('Ctrl Pts',(-1.66893246721288,-2.75695157418166,
7.64008727732745));
#11790=CARTESIAN_POINT('Ctrl Pts',(-1.60567441703572,-2.79524510633577,
7.64464620826709));
#11791=CARTESIAN_POINT('Ctrl Pts',(-1.54106175878119,-2.831382116787,7.64920513920673));
#11792=CARTESIAN_POINT('Ctrl Pts',(-1.47525540501185,-2.86526422036142,
7.65376407014636));
#11793=CARTESIAN_POINT('',(-1.87158653173903,2.62360084935058,7.));
#11794=CARTESIAN_POINT('Origin',(0.,0.,7.));
#11795=CARTESIAN_POINT('Ctrl Pts',(-1.87158653173896,2.62360084935063,7.));
#11796=CARTESIAN_POINT('Ctrl Pts',(-1.95488455526994,2.56417890679422,7.00631636296639));
#11797=CARTESIAN_POINT('Ctrl Pts',(-2.0354058791132,2.50074665614785,7.01263272593278));
#11798=CARTESIAN_POINT('Ctrl Pts',(-2.11275911458763,2.43359127345306,7.01894908889917));
#11799=CARTESIAN_POINT('Ctrl Pts',(-2.19006764871673,2.3664746989081,7.02526180172836));
#11800=CARTESIAN_POINT('Ctrl Pts',(-2.26421143417526,2.29563954104779,7.03157451455755));
#11801=CARTESIAN_POINT('Ctrl Pts',(-2.33483186844915,2.2214134483644,7.03788722738675));
#11802=CARTESIAN_POINT('Ctrl Pts',(-2.40542791175611,2.14721299197442,7.04419775992391));
#11803=CARTESIAN_POINT('Ctrl Pts',(-2.47250274843121,2.06962422637506,7.05050829246107));
#11804=CARTESIAN_POINT('Ctrl Pts',(-2.53573481925193,1.98901143509367,7.05681882499824));
#11805=CARTESIAN_POINT('Ctrl Pts',(-2.59897761335262,1.9083849730038,7.06313042771397));
#11806=CARTESIAN_POINT('Ctrl Pts',(-2.65837608332418,1.82473377464521,7.0694420304297));
#11807=CARTESIAN_POINT('Ctrl Pts',(-2.71364928332791,1.73845481091512,7.07575363314544));
#11808=CARTESIAN_POINT('Ctrl Pts',(-2.7689307737664,1.65216290619155,7.08206618253932));
#11809=CARTESIAN_POINT('Ctrl Pts',(-2.82008554331845,1.5632427926457,7.0883787319332));
#11810=CARTESIAN_POINT('Ctrl Pts',(-2.86687682085001,1.47211917200102,7.09469128132708));
#11811=CARTESIAN_POINT('Ctrl Pts',(-2.9136850090638,1.38096261866729,7.10100611211875));
#11812=CARTESIAN_POINT('Ctrl Pts',(-2.95612638052977,1.28760133341672,7.10732094291041));
#11813=CARTESIAN_POINT('Ctrl Pts',(-2.99401111992302,1.19248269433031,7.11363577370208));
#11814=CARTESIAN_POINT('Ctrl Pts',(-3.03191756464926,1.09730955884861,7.11995422245462));
#11815=CARTESIAN_POINT('Ctrl Pts',(-3.06526203005559,1.00037744137021,7.12627267120716));
#11816=CARTESIAN_POINT('Ctrl Pts',(-3.09390384883166,0.902151060900918,
7.13259111995971));
#11817=CARTESIAN_POINT('Ctrl Pts',(-3.12258819884177,0.803778820658934,
7.13891895119682));
#11818=CARTESIAN_POINT('Ctrl Pts',(-3.14655584252349,0.704108868842967,
7.14524678243393));
#11819=CARTESIAN_POINT('Ctrl Pts',(-3.16571666474431,0.603618721595178,
7.15157461367104));
#11820=CARTESIAN_POINT('Ctrl Pts',(-3.18489319973714,0.503046167718055,
7.15790763402626));
#11821=CARTESIAN_POINT('Ctrl Pts',(-3.19925499963053,0.401652478673659,
7.16424065438148));
#11822=CARTESIAN_POINT('Ctrl Pts',(-3.20876377075636,0.299921032909348,
7.17057367473671));
#11823=CARTESIAN_POINT('Ctrl Pts',(-3.21828938395578,0.198009398930137,
7.1769179122296));
#11824=CARTESIAN_POINT('Ctrl Pts',(-3.22294477780767,0.0957592177962029,
7.1832621497225));
#11825=CARTESIAN_POINT('Ctrl Pts',(-3.22274375398103,-0.00634497251973922,
7.18960638721539));
#11826=CARTESIAN_POINT('Ctrl Pts',(-3.22264524679225,-0.056378826311069,
7.19271523759807));
#11827=CARTESIAN_POINT('Ctrl Pts',(-3.22138137649325,-0.106377683652681,
7.19582408798075));
#11828=CARTESIAN_POINT('Ctrl Pts',(-3.21895829870692,-0.156285103851417,
7.19893293836343));
#11829=CARTESIAN_POINT('Ctrl Pts',(-3.2141962974436,-0.254366642701122,
7.20504266770573));
#11830=CARTESIAN_POINT('Ctrl Pts',(-3.20493703544895,-0.352439736616328,
7.21115239704804));
#11831=CARTESIAN_POINT('Ctrl Pts',(-3.19117079167538,-0.450051709093428,
7.21726212639034));
#11832=CARTESIAN_POINT('Ctrl Pts',(-3.17742529840946,-0.547516546446787,
7.22336264624983));
#11833=CARTESIAN_POINT('Ctrl Pts',(-3.15918637904269,-0.644521208194034,
7.22946316610932));
#11834=CARTESIAN_POINT('Ctrl Pts',(-3.13649628481895,-0.740613676498684,
7.2355636859688));
#11835=CARTESIAN_POINT('Ctrl Pts',(-3.11383333468033,-0.836591189699454,
7.24165690779644));
#11836=CARTESIAN_POINT('Ctrl Pts',(-3.08672989080458,-0.931658248347009,
7.24775012962408));
#11837=CARTESIAN_POINT('Ctrl Pts',(-3.05527977719574,-1.0253697116449,7.25384335145172));
#11838=CARTESIAN_POINT('Ctrl Pts',(-3.02385762985271,-1.11899784425202,
7.25993115502672));
#11839=CARTESIAN_POINT('Ctrl Pts',(-2.98809663559724,-1.21127235777711,
7.26601895860171));
#11840=CARTESIAN_POINT('Ctrl Pts',(-2.94814103357299,-1.30176111812543,
7.27210676217671));
#11841=CARTESIAN_POINT('Ctrl Pts',(-2.90820437617437,-1.39220697395969,
7.27819167926886));
#11842=CARTESIAN_POINT('Ctrl Pts',(-2.86407723941635,-1.48086835208181,
7.28427659636101));
#11843=CARTESIAN_POINT('Ctrl Pts',(-2.81595244431603,-1.56733193480212,
7.29036151345317));
#11844=CARTESIAN_POINT('Ctrl Pts',(-2.76783693766769,-1.65377882939245,
7.29644525610998));
#11845=CARTESIAN_POINT('Ctrl Pts',(-2.71572552160548,-1.73802838303165,
7.30252899876679));
#11846=CARTESIAN_POINT('Ctrl Pts',(-2.65985700406729,-1.81969180918478,
7.3086127414236));
#11847=CARTESIAN_POINT('Ctrl Pts',(-2.60398356273015,-1.90136243249132,
7.31469702025225));
#11848=CARTESIAN_POINT('Ctrl Pts',(-2.5443526141527,-1.98044610937609,7.32078129908089));
#11849=CARTESIAN_POINT('Ctrl Pts',(-2.48124567103609,-2.05658393518589,
7.32686557790954));
#11850=CARTESIAN_POINT('Ctrl Pts',(-2.41807320159362,-2.1328008177799,7.33295617427502));
#11851=CARTESIAN_POINT('Ctrl Pts',(-2.35141781427544,-2.2060653980937,7.33904677064049));
#11852=CARTESIAN_POINT('Ctrl Pts',(-2.28160046354572,-2.27605291837601,
7.34513736700596));
#11853=CARTESIAN_POINT('Ctrl Pts',(-2.21174675054973,-2.34607688955228,
7.35123113547528));
#11854=CARTESIAN_POINT('Ctrl Pts',(-2.13872812446055,-2.41282010374611,
7.35732490394461));
#11855=CARTESIAN_POINT('Ctrl Pts',(-2.06289978202659,-2.47599718332123,
7.36341867241393));
#11856=CARTESIAN_POINT('Ctrl Pts',(-1.9869397203935,-2.53928400595624,7.36952302619049));
#11857=CARTESIAN_POINT('Ctrl Pts',(-1.90816054833947,-2.59899205243666,
7.37562737996706));
#11858=CARTESIAN_POINT('Ctrl Pts',(-1.82694775631032,-2.65487842625848,
7.38173173374362));
#11859=CARTESIAN_POINT('Ctrl Pts',(-1.75539779668978,-2.70411534682703,
7.38710978140471));
#11860=CARTESIAN_POINT('Ctrl Pts',(-1.68195947092443,-2.75038647700699,
7.39248782906579));
#11861=CARTESIAN_POINT('Ctrl Pts',(-1.6069110018128,-2.79355590507027,7.39786587672688));
#11862=CARTESIAN_POINT('Ctrl Pts',(-1.56362614533898,-2.81845424769998,
7.40096771243219));
#11863=CARTESIAN_POINT('Ctrl Pts',(-1.51972485578459,-2.84236797325646,
7.4040695481375));
#11864=CARTESIAN_POINT('Ctrl Pts',(-1.47525540501185,-2.86526422036142,
7.40717138384282));
#11865=CARTESIAN_POINT('Origin',(0.,0.,4.68922655072688));
#11866=CARTESIAN_POINT('',(-1.47525556020637,-2.8652641404555,8.90579936292296));
#11867=CARTESIAN_POINT('',(-1.47525540497551,-2.86526422038013,8.65558740743848));
#11868=CARTESIAN_POINT('',(-1.47525540501186,-2.86526422036142,4.68922655072688));
#11869=CARTESIAN_POINT('',(3.22274949386856,-0.00180617550826221,8.06077344923593));
#11870=CARTESIAN_POINT('Ctrl Pts',(-1.47525556020637,-2.8652641404555,8.90579936292296));
#11871=CARTESIAN_POINT('Ctrl Pts',(-1.56191584290783,-2.82064484616451,
8.9001782983926));
#11872=CARTESIAN_POINT('Ctrl Pts',(-1.64653192564077,-2.77210432391562,
8.89445384481769));
#11873=CARTESIAN_POINT('Ctrl Pts',(-1.74732582984747,-2.70803429645877,
8.88727024250858));
#11874=CARTESIAN_POINT('Ctrl Pts',(-1.76568991081099,-2.69609651330088,
8.88594609824383));
#11875=CARTESIAN_POINT('Ctrl Pts',(-1.79483672095497,-2.67672378086745,
8.88381910504022));
#11876=CARTESIAN_POINT('Ctrl Pts',(-1.80569848880261,-2.66940855126029,
8.88302075531027));
#11877=CARTESIAN_POINT('Ctrl Pts',(-1.82484375429939,-2.65634419792067,
8.88160326897679));
#11878=CARTESIAN_POINT('Ctrl Pts',(-1.83314546940875,-2.65062198544963,
8.88098516116634));
#11879=CARTESIAN_POINT('Ctrl Pts',(-1.85032771157253,-2.63865926721531,
8.87969856997363));
#11880=CARTESIAN_POINT('Ctrl Pts',(-1.85920382696431,-2.63241267544839,
8.87902985821276));
#11881=CARTESIAN_POINT('Ctrl Pts',(-1.88205101427809,-2.61616070584337,
8.8772979262051));
#11882=CARTESIAN_POINT('Ctrl Pts',(-1.89597378050373,-2.60608830708994,
8.87623212468758));
#11883=CARTESIAN_POINT('Ctrl Pts',(-1.95505444363666,-2.56262248890407,
8.87166432267757));
#11884=CARTESIAN_POINT('Ctrl Pts',(-1.99941353186853,-2.52816470714099,
8.86812089055773));
#11885=CARTESIAN_POINT('Ctrl Pts',(-2.11406016631624,-2.43420311009594,
8.85865041136447));
#11886=CARTESIAN_POINT('Ctrl Pts',(-2.18273299514682,-2.37281885265166,
8.85265147681694));
#11887=CARTESIAN_POINT('Ctrl Pts',(-2.42137386943083,-2.14037036060827,
8.83061161306671));
#11888=CARTESIAN_POINT('Ctrl Pts',(-2.57463129709393,-1.95332937520388,
8.81403486023412));
#11889=CARTESIAN_POINT('Ctrl Pts',(-2.75636266549661,-1.67251703985024,
8.7917698958822));
#11890=CARTESIAN_POINT('Ctrl Pts',(-2.8036990385628,-1.59189310158585,8.78565022208224));
#11891=CARTESIAN_POINT('Ctrl Pts',(-2.85401455155441,-1.49696822750696,
8.77884472223392));
#11892=CARTESIAN_POINT('Ctrl Pts',(-2.86048042076661,-1.48457560053888,
8.77796386642576));
#11893=CARTESIAN_POINT('Ctrl Pts',(-2.87010281165793,-1.46583683795933,
8.77664381755683));
#11894=CARTESIAN_POINT('Ctrl Pts',(-2.87331926374573,-1.45952190660949,
8.77620098354383));
#11895=CARTESIAN_POINT('Ctrl Pts',(-2.87903262519064,-1.44821265074036,
8.77541159855454));
#11896=CARTESIAN_POINT('Ctrl Pts',(-2.88153740232486,-1.44322241504034,
8.77506455854859));
#11897=CARTESIAN_POINT('Ctrl Pts',(-2.88692943479051,-1.43240993911197,
8.77431538984498));
#11898=CARTESIAN_POINT('Ctrl Pts',(-2.88981204413429,-1.42658548515855,
8.77391355269614));
#11899=CARTESIAN_POINT('Ctrl Pts',(-2.89780797274013,-1.41030563167213,
8.77279507804597));
#11900=CARTESIAN_POINT('Ctrl Pts',(-2.9028823626142,-1.39983106840124,8.77208083164053));
#11901=CARTESIAN_POINT('Ctrl Pts',(-2.93194065425306,-1.33901134734256,
8.76796342033422));
#11902=CARTESIAN_POINT('Ctrl Pts',(-2.95467294484771,-1.28807455059822,
8.76463287007666));
#11903=CARTESIAN_POINT('Ctrl Pts',(-3.07368517942321,-1.00164584814562,
8.74641373676251));
#11904=CARTESIAN_POINT('Ctrl Pts',(-3.14314712502643,-0.755968689147023,
8.73260956516305));
#11905=CARTESIAN_POINT('Ctrl Pts',(-3.20868236742669,-0.342622672841557,
8.70897172935884));
#11906=CARTESIAN_POINT('Ctrl Pts',(-3.22195949021845,-0.178883766546193,
8.69951858710015));
#11907=CARTESIAN_POINT('Ctrl Pts',(-3.22281676813793,0.00705201471682277,
8.68833510825207));
#11908=CARTESIAN_POINT('Ctrl Pts',(-3.22269433460698,0.0289627566378994,
8.68701050324264));
#11909=CARTESIAN_POINT('Ctrl Pts',(-3.22214176634534,0.0639649697824238,
8.68488298994749));
#11910=CARTESIAN_POINT('Ctrl Pts',(-3.22185522579968,0.077058262542411,
8.68408458647804));
#11911=CARTESIAN_POINT('Ctrl Pts',(-3.22120688608411,0.100226709786385,
8.68266713820439));
#11912=CARTESIAN_POINT('Ctrl Pts',(-3.22087760048591,0.110302653321238,
8.68204912320675));
#11913=CARTESIAN_POINT('Ctrl Pts',(-3.22009577069156,0.131219339565238,
8.6807628592837));
#11914=CARTESIAN_POINT('Ctrl Pts',(-3.21963574586003,0.142059659550053,
8.68009438268703));
#11915=CARTESIAN_POINT('Ctrl Pts',(-3.21830622391815,0.170051591003138,
8.67836335015214));
#11916=CARTESIAN_POINT('Ctrl Pts',(-3.21735436256677,0.187198776119536,
8.67729821653906));
#11917=CARTESIAN_POINT('Ctrl Pts',(-3.21270939306384,0.260310524804873,
8.67273594273521));
#11918=CARTESIAN_POINT('Ctrl Pts',(-3.2076929140099,0.316178343891641,8.66919748290491));
#11919=CARTESIAN_POINT('Ctrl Pts',(-3.19061669986576,0.463172367564257,
8.65974328643643));
#11920=CARTESIAN_POINT('Ctrl Pts',(-3.17611271358921,0.553957650238664,
8.65375594827045));
#11921=CARTESIAN_POINT('Ctrl Pts',(-3.10920634554157,0.882025980317213,
8.6316064529134));
#11922=CARTESIAN_POINT('Ctrl Pts',(-3.03390974688837,1.11378210204861,8.61489679298693));
#11923=CARTESIAN_POINT('Ctrl Pts',(-2.89521884214251,1.41854780620448,8.59262025619512));
#11924=CARTESIAN_POINT('Ctrl Pts',(-2.85357089629121,1.50056874902238,8.58660221977168));
#11925=CARTESIAN_POINT('Ctrl Pts',(-2.8016373262799,1.59284017043318,8.57989545603576));
#11926=CARTESIAN_POINT('Ctrl Pts',(-2.79472775553292,1.60493249250087,8.57901783707648));
#11927=CARTESIAN_POINT('Ctrl Pts',(-2.7841899060956,1.62310017847586,8.57770171879629));
#11928=CARTESIAN_POINT('Ctrl Pts',(-2.78061975809547,1.62920882201503,8.57725960889085));
#11929=CARTESIAN_POINT('Ctrl Pts',(-2.7741968489609,1.64011602286669,8.57647102342865));
#11930=CARTESIAN_POINT('Ctrl Pts',(-2.77135172105746,1.64491895393319,8.57612406289979));
#11931=CARTESIAN_POINT('Ctrl Pts',(-2.76516336600325,1.65530403772327,8.57537448757764));
#11932=CARTESIAN_POINT('Ctrl Pts',(-2.76181571951796,1.66088344900567,8.57497216742491));
#11933=CARTESIAN_POINT('Ctrl Pts',(-2.75241477797755,1.67644466924457,8.5738510626584));
#11934=CARTESIAN_POINT('Ctrl Pts',(-2.74632403864026,1.68640390285786,8.5731346869855));
#11935=CARTESIAN_POINT('Ctrl Pts',(-2.71052735340222,1.74422834313809,8.56898062799087));
#11936=CARTESIAN_POINT('Ctrl Pts',(-2.67962257809606,1.79134440601588,8.56561707103738));
#11937=CARTESIAN_POINT('Ctrl Pts',(-2.50268463307353,2.04626120634536,8.5473967484244));
#11938=CARTESIAN_POINT('Ctrl Pts',(-2.33370664075608,2.23706410608582,8.53361490966403));
#11939=CARTESIAN_POINT('Ctrl Pts',(-2.02173041204856,2.51506888703168,8.5100121280717));
#11940=CARTESIAN_POINT('Ctrl Pts',(-1.89128091654333,2.6145767194305,8.500570419313));
#11941=CARTESIAN_POINT('Ctrl Pts',(-1.73542694140845,2.71567537702212,8.4893971628286));
#11942=CARTESIAN_POINT('Ctrl Pts',(-1.71688965944886,2.7274327275099,8.4880701397851));
#11943=CARTESIAN_POINT('Ctrl Pts',(-1.68709247569136,2.74590757242795,8.48593940595385));
#11944=CARTESIAN_POINT('Ctrl Pts',(-1.67590897860193,2.75274744670181,8.48514022015577));
#11945=CARTESIAN_POINT('Ctrl Pts',(-1.65604900630699,2.76472800709805,8.48372177974039));
#11946=CARTESIAN_POINT('Ctrl Pts',(-1.64738949897839,2.76989658642821,8.48310355871688));
#11947=CARTESIAN_POINT('Ctrl Pts',(-1.6293656110088,2.78054004333162,8.48181726080737));
#11948=CARTESIAN_POINT('Ctrl Pts',(-1.61999757476011,2.78600844939026,8.48114895817598));
#11949=CARTESIAN_POINT('Ctrl Pts',(-1.595742730712,2.80000303766307,8.47941922239956));
#11950=CARTESIAN_POINT('Ctrl Pts',(-1.58081527599739,2.80845774730057,8.47835522021374));
#11951=CARTESIAN_POINT('Ctrl Pts',(-1.51695785188169,2.84395532250318,8.47380537636145));
#11952=CARTESIAN_POINT('Ctrl Pts',(-1.46739859746591,2.8698403658216,8.47027850670192));
#11953=CARTESIAN_POINT('Ctrl Pts',(-1.33502721792961,2.93465325805991,8.46086327890989));
#11954=CARTESIAN_POINT('Ctrl Pts',(-1.25119176427262,2.97136401321875,8.45490407314585));
#11955=CARTESIAN_POINT('Ctrl Pts',(-0.936264577472805,3.09357516656347,
8.43256166640414));
#11956=CARTESIAN_POINT('Ctrl Pts',(-0.6971794875072,3.15606145360958,8.41560900263179));
#11957=CARTESIAN_POINT('Ctrl Pts',(-0.364938512903642,3.2032650890367,8.39330593887493));
#11958=CARTESIAN_POINT('Ctrl Pts',(-0.276059656320446,3.21214594500282,
8.38746816700556));
#11959=CARTESIAN_POINT('Ctrl Pts',(-0.173104642769638,3.21812737713856,
8.38093662225614));
#11960=CARTESIAN_POINT('Ctrl Pts',(-0.15928533661647,3.21884097627461,8.38006471914973));
#11961=CARTESIAN_POINT('Ctrl Pts',(-0.138411284595818,3.21978410562802,
8.37875539607126));
#11962=CARTESIAN_POINT('Ctrl Pts',(-0.131359887447836,3.22007949479204,
8.3783144214118));
#11963=CARTESIAN_POINT('Ctrl Pts',(-0.118728067577128,3.22056709057461,
8.37752690212941));
#11964=CARTESIAN_POINT('Ctrl Pts',(-0.113148088982313,3.22076795972613,
8.37717988007813));
#11965=CARTESIAN_POINT('Ctrl Pts',(-0.101044665211502,3.22117216750185,
8.3764290261362));
#11966=CARTESIAN_POINT('Ctrl Pts',(-0.0945211362517755,3.22137019195878,
8.37602549523407));
#11967=CARTESIAN_POINT('Ctrl Pts',(-0.0762496291795751,3.22186928037541,
8.37489841368772));
#11968=CARTESIAN_POINT('Ctrl Pts',(-0.0645003978578495,3.22212590914076,
8.37417730976002));
#11969=CARTESIAN_POINT('Ctrl Pts',(0.00478784292492184,3.2232601676578,
8.3699449147229));
#11970=CARTESIAN_POINT('Ctrl Pts',(0.0623445902081485,3.22266087779381,
8.36651097389545));
#11971=CARTESIAN_POINT('Ctrl Pts',(0.373118292862246,3.2110947857646,8.34826455816404));
#11972=CARTESIAN_POINT('Ctrl Pts',(0.624405016901019,3.17182785454008,8.33450906399677));
#11973=CARTESIAN_POINT('Ctrl Pts',(1.02520605030147,3.0596642465497,8.31099204798635));
#11974=CARTESIAN_POINT('Ctrl Pts',(1.17833211311284,3.00401663105659,8.30161245074197));
#11975=CARTESIAN_POINT('Ctrl Pts',(1.34658173339306,2.9280226026677,8.29050848005503));
#11976=CARTESIAN_POINT('Ctrl Pts',(1.36647949825128,2.91878955577153,8.28918239150363));
#11977=CARTESIAN_POINT('Ctrl Pts',(1.39811371285924,2.90371613764046,8.28705272567481));
#11978=CARTESIAN_POINT('Ctrl Pts',(1.40991169001187,2.89800593175453,8.28625366187736));
#11979=CARTESIAN_POINT('Ctrl Pts',(1.4307272707706,2.88777402099146,8.28483517354185));
#11980=CARTESIAN_POINT('Ctrl Pts',(1.43975914542981,2.88328162327544,8.28421678052989));
#11981=CARTESIAN_POINT('Ctrl Pts',(1.44894556310741,2.87865842996574,8.28358479724617));
#11982=CARTESIAN_POINT('Ctrl Pts',(1.44912141895466,2.87856990785151,8.28357269804586));
#11983=CARTESIAN_POINT('Ctrl Pts',(1.44949010197805,2.87838427826791,8.28354732962392));
#11984=CARTESIAN_POINT('Ctrl Pts',(1.44968292750618,2.87828716753724,8.28353406028741));
#11985=CARTESIAN_POINT('Ctrl Pts',(1.45004265414901,2.87810595680168,8.28350930307968));
#11986=CARTESIAN_POINT('Ctrl Pts',(1.45020955742023,2.87802186179936,8.2834978153999));
#11987=CARTESIAN_POINT('Ctrl Pts',(1.45052089772116,2.87786495755752,8.28347638445922));
#11988=CARTESIAN_POINT('Ctrl Pts',(1.45066533754033,2.87779215148027,8.28346644126128));
#11989=CARTESIAN_POINT('Ctrl Pts',(1.45093475823428,2.8776563223289,8.28344789299351));
#11990=CARTESIAN_POINT('Ctrl Pts',(1.45105974175618,2.87759330134494,8.28343928793259));
#11991=CARTESIAN_POINT('Ctrl Pts',(1.45129286049334,2.87747573582274,8.28342323674557));
#11992=CARTESIAN_POINT('Ctrl Pts',(1.45140099837991,2.87742119250351,8.28341579057875));
#11993=CARTESIAN_POINT('Ctrl Pts',(1.45160268999296,2.87731944766031,8.28340190168581));
#11994=CARTESIAN_POINT('Ctrl Pts',(1.45169624646475,2.87727224667359,8.2833954588779));
#11995=CARTESIAN_POINT('Ctrl Pts',(1.45189715079337,2.87717087439633,8.28338162282568));
#11996=CARTESIAN_POINT('Ctrl Pts',(1.45200450021031,2.87711670050562,8.28337422937272));
#11997=CARTESIAN_POINT('Ctrl Pts',(1.4522157160377,2.87701009559024,8.28335968152221));
#11998=CARTESIAN_POINT('Ctrl Pts',(1.45231957730882,2.87695766764132,8.28335252750566));
#11999=CARTESIAN_POINT('Ctrl Pts',(1.4525239278985,2.87685449997981,8.28333845095853));
#12000=CARTESIAN_POINT('Ctrl Pts',(1.45262441808936,2.87680376027666,8.28333152839296));
#12001=CARTESIAN_POINT('Ctrl Pts',(1.45282214130987,2.8767039124812,8.28331790691457));
#12002=CARTESIAN_POINT('Ctrl Pts',(1.45291937533058,2.87665480430889,8.28331120795692));
#12003=CARTESIAN_POINT('Ctrl Pts',(1.45311069710945,2.87655816481374,8.28329802612367));
#12004=CARTESIAN_POINT('Ctrl Pts',(1.45320478592302,2.87651063335084,8.28329154319727));
#12005=CARTESIAN_POINT('Ctrl Pts',(1.45338992424005,2.87641709441151,8.28327878612238));
#12006=CARTESIAN_POINT('Ctrl Pts',(1.45348097490983,2.87637108671325,8.28327251191403));
#12007=CARTESIAN_POINT('Ctrl Pts',(1.45366014024989,2.8762805441915,8.28326016521712));
#12008=CARTESIAN_POINT('Ctrl Pts',(1.45374825613992,2.87623600909513,8.28325409266368));
#12009=CARTESIAN_POINT('Ctrl Pts',(1.45392165144414,2.87614836249648,8.28324214247482));
#12010=CARTESIAN_POINT('Ctrl Pts',(1.45400693222277,2.87610525062572,8.28323626476329));
#12011=CARTESIAN_POINT('Ctrl Pts',(1.45417475348336,2.87602040281084,8.28322469768269));
#12012=CARTESIAN_POINT('Ctrl Pts',(1.45425729537493,2.8759786664544,8.28321900823322));
#12013=CARTESIAN_POINT('Ctrl Pts',(1.45441973144542,2.87589652374621,8.28320781134494));
#12014=CARTESIAN_POINT('Ctrl Pts',(1.45449962719732,2.8758561168799,8.28320230381336));
#12015=CARTESIAN_POINT('Ctrl Pts',(1.45465686045572,2.87577658873875,8.28319146464015));
#12016=CARTESIAN_POINT('Ctrl Pts',(1.45473419958992,2.87573746690334,8.28318613290095));
#12017=CARTESIAN_POINT('Ctrl Pts',(1.45488639914185,2.87566046937528,8.28317563987343));
#12018=CARTESIAN_POINT('Ctrl Pts',(1.45496126132407,2.87562259303767,8.28317047847757));
#12019=CARTESIAN_POINT('Ctrl Pts',(1.45510862278797,2.87554802863505,8.28316031819173));
#12020=CARTESIAN_POINT('Ctrl Pts',(1.45518110393332,2.87551134997834,8.28315532056545));
#12021=CARTESIAN_POINT('Ctrl Pts',(1.45532375933505,2.87543915327744,8.28314548399554));
#12022=CARTESIAN_POINT('Ctrl Pts',(1.45539393367991,2.87540363540385,8.28314064505787));
#12023=CARTESIAN_POINT('Ctrl Pts',(1.45553205290674,2.87533372172008,8.28313112056191));
#12024=CARTESIAN_POINT('Ctrl Pts',(1.4555999978773,2.87529932606662,8.28312643500879));
#12025=CARTESIAN_POINT('Ctrl Pts',(1.45573373307805,2.87523161959461,8.28311721216244));
#12026=CARTESIAN_POINT('Ctrl Pts',(1.45579952336763,2.87519830893463,8.28311267487567));
#12027=CARTESIAN_POINT('Ctrl Pts',(1.46613360586299,2.86996555454922,8.28239995060537));
#12028=CARTESIAN_POINT('Ctrl Pts',(1.47637386319367,2.86471119750456,8.28168983009041));
#12029=CARTESIAN_POINT('Ctrl Pts',(1.50475679532078,2.84995508509782,8.27971069068866));
#12030=CARTESIAN_POINT('Ctrl Pts',(1.52283712778484,2.84033520048992,8.27843749813012));
#12031=CARTESIAN_POINT('Ctrl Pts',(1.56296807023564,2.81848967122392,8.27558316607803));
#12032=CARTESIAN_POINT('Ctrl Pts',(1.58496918684809,2.80617637255745,8.2739989539887));
#12033=CARTESIAN_POINT('Ctrl Pts',(1.65276816168936,2.76717984313757,8.26905574579382));
#12034=CARTESIAN_POINT('Ctrl Pts',(1.69805201947264,2.73962510128927,8.26566605775303));
#12035=CARTESIAN_POINT('Ctrl Pts',(1.87539698758895,2.62562619239151,8.25203372394604));
#12036=CARTESIAN_POINT('Ctrl Pts',(2.0016968561666,2.53065724137172,8.24150173867995));
#12037=CARTESIAN_POINT('Ctrl Pts',(2.2905503527454,2.27826241015908,8.21559746268043));
#12038=CARTESIAN_POINT('Ctrl Pts',(2.44450735163029,2.11222615715828,8.20014330439292));
#12039=CARTESIAN_POINT('Ctrl Pts',(2.59410994337361,1.91240093692607,8.18417037034958));
#12040=CARTESIAN_POINT('Ctrl Pts',(2.6081595136398,1.89319512243291,8.18265991212846));
#12041=CARTESIAN_POINT('Ctrl Pts',(2.62719646252656,1.86655734461766,8.1806007276607));
#12042=CARTESIAN_POINT('Ctrl Pts',(2.63236712616528,1.85925815610738,8.18004012148366));
#12043=CARTESIAN_POINT('Ctrl Pts',(2.64056224724243,1.84758676151705,8.1791496302794));
#12044=CARTESIAN_POINT('Ctrl Pts',(2.64360634652024,1.84322850143718,8.17881841561658));
#12045=CARTESIAN_POINT('Ctrl Pts',(2.64989274381402,1.83418061082435,8.1781335415127));
#12046=CARTESIAN_POINT('Ctrl Pts',(2.65313338408978,1.82948990526959,8.17778000417152));
#12047=CARTESIAN_POINT('Ctrl Pts',(2.66087015350301,1.81822743106244,8.17693474076742));
#12048=CARTESIAN_POINT('Ctrl Pts',(2.66535444449386,1.81164749696855,8.17644381968037));
#12049=CARTESIAN_POINT('Ctrl Pts',(2.68061139660243,1.78908124735452,8.17476986499453));
#12050=CARTESIAN_POINT('Ctrl Pts',(2.69126523638913,1.77301456241518,8.17359459837548));
#12051=CARTESIAN_POINT('Ctrl Pts',(2.75108891190173,1.68101477443178,8.16695267436686));
#12052=CARTESIAN_POINT('Ctrl Pts',(2.79719305364331,1.60312662590675,8.16166675577809));
#12053=CARTESIAN_POINT('Ctrl Pts',(2.97390819186197,1.27368846713814,8.1402346970622));
#12054=CARTESIAN_POINT('Ctrl Pts',(3.07433847305442,1.00740787792131,8.12494432390821));
#12055=CARTESIAN_POINT('Ctrl Pts',(3.15317723981285,0.669093012184489,8.1048473039023));
#12056=CARTESIAN_POINT('Ctrl Pts',(3.16583972636272,0.606358172287019,8.10109998830986));
#12057=CARTESIAN_POINT('Ctrl Pts',(3.18349483106141,0.503128612881159,8.09487342480401));
#12058=CARTESIAN_POINT('Ctrl Pts',(3.18960114412124,0.462841284842914,8.09242860422071));
#12059=CARTESIAN_POINT('Ctrl Pts',(3.19700041338162,0.406881489302844,8.08900793060503));
#12060=CARTESIAN_POINT('Ctrl Pts',(3.19894514461284,0.391298016377325,8.08805271324975));
#12061=CARTESIAN_POINT('Ctrl Pts',(3.20188023352817,0.366292606015592,8.08651549693148));
#12062=CARTESIAN_POINT('Ctrl Pts',(3.20294309376386,0.356879304743489,8.08593579894911));
#12063=CARTESIAN_POINT('Ctrl Pts',(3.20499467234622,0.337961570921506,8.0847687015072));
#12064=CARTESIAN_POINT('Ctrl Pts',(3.20598265222462,0.328457156536636,8.08418128493849));
#12065=CARTESIAN_POINT('Ctrl Pts',(3.20789892967487,0.309189584762989,8.08298826345403));
#12066=CARTESIAN_POINT('Ctrl Pts',(3.20882496015555,0.299426308128521,8.08238259331582));
#12067=CARTESIAN_POINT('Ctrl Pts',(3.21085396987018,0.276942889645245,8.0809851358859));
#12068=CARTESIAN_POINT('Ctrl Pts',(3.21192594388193,0.264220179771188,8.08019237794668));
#12069=CARTESIAN_POINT('Ctrl Pts',(3.21541309354019,0.21967021619048,8.07740935626988));
#12070=CARTESIAN_POINT('Ctrl Pts',(3.21743095265524,0.187814569564738,8.07540666130566));
#12071=CARTESIAN_POINT('Ctrl Pts',(3.22152329183475,0.103336231139147,8.07006066720517));
#12072=CARTESIAN_POINT('Ctrl Pts',(3.22278156527427,0.0506859090623757,
8.06669274223213));
#12073=CARTESIAN_POINT('Ctrl Pts',(3.22274939864108,-0.00196877082894968,
8.06328801173323));
#12074=CARTESIAN_POINT('Ctrl Pts',(-1.47525540501185,-2.86526422036142,
7.65376407014636));
#12075=CARTESIAN_POINT('Ctrl Pts',(-1.38644963466766,-2.9109881685284,7.65991635409541));
#12076=CARTESIAN_POINT('Ctrl Pts',(-1.29546923767711,-2.95260373781076,
7.66606863804446));
#12077=CARTESIAN_POINT('Ctrl Pts',(-1.20273214142544,-2.98990852008589,
7.6722209219935));
#12078=CARTESIAN_POINT('Ctrl Pts',(-1.11001191723956,-3.02720651533871,
7.67837208663061));
#12079=CARTESIAN_POINT('Ctrl Pts',(-1.01553603176287,-3.06019512043509,
7.68452325126771));
#12080=CARTESIAN_POINT('Ctrl Pts',(-0.919742622604065,-3.08871997284723,
7.69067441590482));
#12081=CARTESIAN_POINT('Ctrl Pts',(-0.823941047833115,-3.11724725677197,
7.69682610487888));
#12082=CARTESIAN_POINT('Ctrl Pts',(-0.726822142574996,-3.14130990861831,
7.70297779385294));
#12083=CARTESIAN_POINT('Ctrl Pts',(-0.628838468977979,-3.16080365452102,
7.709129482827));
#12084=CARTESIAN_POINT('Ctrl Pts',(-0.530078506583397,-3.18045184224053,
7.71532990938214));
#12085=CARTESIAN_POINT('Ctrl Pts',(-0.430440450089063,-3.19545831082972,
7.72153033593728));
#12086=CARTESIAN_POINT('Ctrl Pts',(-0.330395857705662,-3.20576919626335,
7.72773076249242));
#12087=CARTESIAN_POINT('Ctrl Pts',(-0.230986158321603,-3.21601464778573,
7.73389184051988));
#12088=CARTESIAN_POINT('Ctrl Pts',(-0.131175508218247,-3.22162397899351,
7.74005291854734));
#12089=CARTESIAN_POINT('Ctrl Pts',(-0.0314279910081243,-3.2225967547742,
7.7462139965748));
#12090=CARTESIAN_POINT('Ctrl Pts',(0.0692751019773634,-3.22357884969382,
7.75243409739379));
#12091=CARTESIAN_POINT('Ctrl Pts',(0.169913393363746,-3.21983510293097,
7.75865419821277));
#12092=CARTESIAN_POINT('Ctrl Pts',(0.270014601907335,-3.21141863936436,
7.76487429903175));
#12093=CARTESIAN_POINT('Ctrl Pts',(0.370115810450923,-3.20300217579775,
7.77109439985074));
#12094=CARTESIAN_POINT('Ctrl Pts',(0.469679499641924,-3.18991311630918,
7.77731450066972));
#12095=CARTESIAN_POINT('Ctrl Pts',(0.568245329918624,-3.17225705256142,
7.7835346014887));
#12096=CARTESIAN_POINT('Ctrl Pts',(0.666067788263,-3.15473414877578,7.78970779103679));
#12097=CARTESIAN_POINT('Ctrl Pts',(0.763250526326483,-3.13265146741895,
7.79588098058488));
#12098=CARTESIAN_POINT('Ctrl Pts',(0.859335649326477,-3.10606822273701,
7.80205417013297));
#12099=CARTESIAN_POINT('Ctrl Pts',(0.95529095626567,-3.07952089341845,7.80821901937691));
#12100=CARTESIAN_POINT('Ctrl Pts',(1.0501511808306,-3.04848520131768,7.81438386862085));
#12101=CARTESIAN_POINT('Ctrl Pts',(1.14346700560903,-3.01307165025718,7.82054871786479));
#12102=CARTESIAN_POINT('Ctrl Pts',(1.23668430195901,-2.97769549094176,7.82670705789222));
#12103=CARTESIAN_POINT('Ctrl Pts',(1.32836003673228,-2.93795081575181,7.83286539791965));
#12104=CARTESIAN_POINT('Ctrl Pts',(1.41805942227855,-2.89399810597502,7.83902373794708));
#12105=CARTESIAN_POINT('Ctrl Pts',(1.50769365270407,-2.8500773222153,7.84517760472883));
#12106=CARTESIAN_POINT('Ctrl Pts',(1.59535399928417,-2.80195477138832,7.85133147151059));
#12107=CARTESIAN_POINT('Ctrl Pts',(1.68062591525096,-2.74983892173467,7.85748533829234));
#12108=CARTESIAN_POINT('Ctrl Pts',(1.76586572460008,-2.69774269476265,7.86363688801759));
#12109=CARTESIAN_POINT('Ctrl Pts',(1.84871852014072,-2.64165638274115,7.86978843774284));
#12110=CARTESIAN_POINT('Ctrl Pts',(1.92879541135377,-2.58183381022881,7.87593998746809));
#12111=CARTESIAN_POINT('Ctrl Pts',(2.00886355338595,-2.52201777391562,7.88209086507657));
#12112=CARTESIAN_POINT('Ctrl Pts',(2.08615604621886,-2.4584665486047,7.88824174268504));
#12113=CARTESIAN_POINT('Ctrl Pts',(2.16031481799547,-2.39147599813362,7.89439262029352));
#12114=CARTESIAN_POINT('Ctrl Pts',(2.23448530675665,-2.32447486324713,7.90054446973226));
#12115=CARTESIAN_POINT('Ctrl Pts',(2.30552076874257,-2.25403361492285,7.90669631917099));
#12116=CARTESIAN_POINT('Ctrl Pts',(2.37309867492827,-2.18048623970748,7.91284816860973));
#12117=CARTESIAN_POINT('Ctrl Pts',(2.44074905272957,-2.10685999112351,7.91900661538912));
#12118=CARTESIAN_POINT('Ctrl Pts',(2.50493417597123,-2.0301212842115,7.9251650621685));
#12119=CARTESIAN_POINT('Ctrl Pts',(2.56537073886303,-1.95063849410529,7.93132350894789));
#12120=CARTESIAN_POINT('Ctrl Pts',(2.62584110262679,-1.87111125098119,7.93748540001433));
#12121=CARTESIAN_POINT('Ctrl Pts',(2.6825584844241,-1.78883722581535,7.94364729108077));
#12122=CARTESIAN_POINT('Ctrl Pts',(2.73528318951348,-1.70421343606515,7.94980918214721));
#12123=CARTESIAN_POINT('Ctrl Pts',(2.78809621421564,-1.61944789226758,7.95598139505105));
#12124=CARTESIAN_POINT('Ctrl Pts',(2.83690299037388,-1.53232510057701,7.96215360795489));
#12125=CARTESIAN_POINT('Ctrl Pts',(2.88150994870523,-1.44326642655221,7.96832582085873));
#12126=CARTESIAN_POINT('Ctrl Pts',(2.91557763667492,-1.37524961412725,7.97303972718986));
#12127=CARTESIAN_POINT('Ctrl Pts',(2.94719659092646,-1.30610413706821,7.97775363352099));
#12128=CARTESIAN_POINT('Ctrl Pts',(2.97629999177014,-1.23602423984689,7.98246753985212));
#12129=CARTESIAN_POINT('Ctrl Pts',(3.0188297503367,-1.13361417700918,7.98935612648999));
#12130=CARTESIAN_POINT('Ctrl Pts',(3.05611340035765,-1.0289026103966,7.99624471312786));
#12131=CARTESIAN_POINT('Ctrl Pts',(3.08792381878256,-0.922412083558831,
8.00313329976573));
#12132=CARTESIAN_POINT('Ctrl Pts',(3.11963641267084,-0.816249040198438,
8.01000070237556));
#12133=CARTESIAN_POINT('Ctrl Pts',(3.14590924755755,-0.708318181077056,
8.01686810498539));
#12134=CARTESIAN_POINT('Ctrl Pts',(3.16656354493143,-0.599160144211315,
8.02373550759522));
#12135=CARTESIAN_POINT('Ctrl Pts',(3.18710346491378,-0.490606592276461,
8.03056488056004));
#12136=CARTESIAN_POINT('Ctrl Pts',(3.2020867924657,-0.380839652699022,8.03739425352486));
#12137=CARTESIAN_POINT('Ctrl Pts',(3.21138534471515,-0.270410299820069,
8.04422362648968));
#12138=CARTESIAN_POINT('Ctrl Pts',(3.21889649751144,-0.181208054092015,
8.04974023407176));
#12139=CARTESIAN_POINT('Ctrl Pts',(3.22269918389552,-0.0915739967349043,
8.05525684165385));
#12140=CARTESIAN_POINT('Ctrl Pts',(3.22274949386856,-0.00180617550826221,
8.06077344923593));
#12141=CARTESIAN_POINT('',(3.22274940930447,-0.00195123747957988,7.81422655072689));
#12142=CARTESIAN_POINT('Ctrl Pts',(-1.47525540501185,-2.86526422036142,
7.40717138384282));
#12143=CARTESIAN_POINT('Ctrl Pts',(-1.38671147020266,-2.91085335572981,
7.41334750551078));
#12144=CARTESIAN_POINT('Ctrl Pts',(-1.29591331447514,-2.9524058816945,7.41952362717875));
#12145=CARTESIAN_POINT('Ctrl Pts',(-1.20326442470719,-2.98969434670738,
7.42569974884672));
#12146=CARTESIAN_POINT('Ctrl Pts',(-1.11072730614301,-3.02693782708383,
7.43186841966929));
#12147=CARTESIAN_POINT('Ctrl Pts',(-1.01634429106289,-3.05992731241399,
7.43803709049186));
#12148=CARTESIAN_POINT('Ctrl Pts',(-0.920542606245815,-3.08848164517553,
7.44420576131444));
#12149=CARTESIAN_POINT('Ctrl Pts',(-0.821799889057217,-3.11791257230135,
7.45056380522177));
#12150=CARTESIAN_POINT('Ctrl Pts',(-0.721550396993546,-3.14263139571463,
7.4569218491291));
#12151=CARTESIAN_POINT('Ctrl Pts',(-0.620283454517043,-3.16249363612837,
7.46327989303642));
#12152=CARTESIAN_POINT('Ctrl Pts',(-0.522177050373216,-3.18173597659583,
7.46943950257812));
#12153=CARTESIAN_POINT('Ctrl Pts',(-0.423116222109622,-3.19642030312448,
7.47559911211981));
#12154=CARTESIAN_POINT('Ctrl Pts',(-0.323559181618689,-3.20646643807326,
7.48175872166151));
#12155=CARTESIAN_POINT('Ctrl Pts',(-0.224026376014791,-3.21651012752001,
7.48791683178698));
#12156=CARTESIAN_POINT('Ctrl Pts',(-0.123998028914641,-3.22191782599267,
7.49407494191246));
#12157=CARTESIAN_POINT('Ctrl Pts',(-0.0239386781153377,-3.22266109018465,
7.50023305203793));
#12158=CARTESIAN_POINT('Ctrl Pts',(0.0761228768800743,-3.22340437074991,
7.50639129781972));
#12159=CARTESIAN_POINT('Ctrl Pts',(0.176215003847994,-3.21948301033851,
7.5125495436015));
#12160=CARTESIAN_POINT('Ctrl Pts',(0.275872946911921,-3.21092069034134,
7.51870778938328));
#12161=CARTESIAN_POINT('Ctrl Pts',(0.375559539726755,-3.20235590884108,
7.52486780554285));
#12162=CARTESIAN_POINT('Ctrl Pts',(0.474811269307638,-3.1891475539048,7.53102782170241));
#12163=CARTESIAN_POINT('Ctrl Pts',(0.573169271697264,-3.17137108337735,
7.53718783786197));
#12164=CARTESIAN_POINT('Ctrl Pts',(0.671637472571346,-3.15357469642151,
7.54335475558956));
#12165=CARTESIAN_POINT('Ctrl Pts',(0.769209521553051,-3.13120005760236,
7.54952167331716));
#12166=CARTESIAN_POINT('Ctrl Pts',(0.865437712260869,-3.10437354851131,
7.55568859104475));
#12167=CARTESIAN_POINT('Ctrl Pts',(0.961730663784091,-3.07752898539065,
7.56185965905946));
#12168=CARTESIAN_POINT('Ctrl Pts',(1.05667754608014,-3.04622672280497,7.56803072707418));
#12169=CARTESIAN_POINT('Ctrl Pts',(1.14984864136705,-3.01064206847084,7.57420179508889));
#12170=CARTESIAN_POINT('Ctrl Pts',(1.24315849563187,-2.97500441819145,7.58038205362657));
#12171=CARTESIAN_POINT('Ctrl Pts',(1.33468689024469,-2.93507182280368,7.58656231216424));
#12172=CARTESIAN_POINT('Ctrl Pts',(1.42402700472962,-2.89106635210968,7.59274257070192));
#12173=CARTESIAN_POINT('Ctrl Pts',(1.44357232179737,-2.88143908800342,7.59409465216472));
#12174=CARTESIAN_POINT('Ctrl Pts',(1.4630130093848,-2.87161705432507,7.59544673362752));
#12175=CARTESIAN_POINT('Ctrl Pts',(1.48234499273142,-2.861602852428,7.59679881509032));
#12176=CARTESIAN_POINT('Ctrl Pts',(1.57074490588527,-2.81581062500192,7.6029815166655));
#12177=CARTESIAN_POINT('Ctrl Pts',(1.65717056177596,-2.76584082135359,7.60916421824068));
#12178=CARTESIAN_POINT('Ctrl Pts',(1.74120158228424,-2.71188764744243,7.61534691981586));
#12179=CARTESIAN_POINT('Ctrl Pts',(1.82512169312725,-2.65800568447722,7.62152146105503));
#12180=CARTESIAN_POINT('Ctrl Pts',(1.90665309024184,-2.60015103407787,7.6276960022942));
#12181=CARTESIAN_POINT('Ctrl Pts',(1.98539896798611,-2.53856425965933,7.63387054353338));
#12182=CARTESIAN_POINT('Ctrl Pts',(2.06406394588774,-2.47704075662084,7.64003874133682));
#12183=CARTESIAN_POINT('Ctrl Pts',(2.13994875533962,-2.41179301830379,7.64620693914026));
#12184=CARTESIAN_POINT('Ctrl Pts',(2.21268542963185,-2.34310493832328,7.65237513694371));
#12185=CARTESIAN_POINT('Ctrl Pts',(2.28537181367839,-2.27446434938426,7.65853907004594));
#12186=CARTESIAN_POINT('Ctrl Pts',(2.35491407642516,-2.20238844422196,7.66470300314817));
#12187=CARTESIAN_POINT('Ctrl Pts',(2.42097791650659,-2.1272008580027,7.6708669362504));
#12188=CARTESIAN_POINT('Ctrl Pts',(2.48701825869888,-2.05204001484838,7.67702867693668));
#12189=CARTESIAN_POINT('Ctrl Pts',(2.54958235152694,-1.97377001471056,7.68319041762297));
#12190=CARTESIAN_POINT('Ctrl Pts',(2.60837393614563,-1.89275010810624,7.68935215830925));
#12191=CARTESIAN_POINT('Ctrl Pts',(2.6671601816317,-1.81173755929009,7.69551333941969));
#12192=CARTESIAN_POINT('Ctrl Pts',(2.72217434603628,-1.72797595076776,7.70167452053012));
#12193=CARTESIAN_POINT('Ctrl Pts',(2.7731621343777,-1.64185545616956,7.70783570164056));
#12194=CARTESIAN_POINT('Ctrl Pts',(2.82415879720679,-1.55571997219266,7.7139979551122));
#12195=CARTESIAN_POINT('Ctrl Pts',(2.87112747127984,-1.46722515879271,7.72016020858384));
#12196=CARTESIAN_POINT('Ctrl Pts',(2.91385915369973,-1.37678698239789,7.72632246205547));
#12197=CARTESIAN_POINT('Ctrl Pts',(2.95663722150481,-1.28625063505799,7.73249140467401));
#12198=CARTESIAN_POINT('Ctrl Pts',(2.99516892824132,-1.19376710416503,7.73866034729254));
#12199=CARTESIAN_POINT('Ctrl Pts',(3.02929295278728,-1.09977350790666,7.74482928991108));
#12200=CARTESIAN_POINT('Ctrl Pts',(3.06343640094297,-1.00572640990121,7.75100174393061));
#12201=CARTESIAN_POINT('Ctrl Pts',(3.09316704163156,-0.910167947767144,
7.75717419795014));
#12202=CARTESIAN_POINT('Ctrl Pts',(3.11837370832897,-0.81354961600545,7.76334665196967));
#12203=CARTESIAN_POINT('Ctrl Pts',(3.14362252831195,-0.716769708729668,
7.76952942822737));
#12204=CARTESIAN_POINT('Ctrl Pts',(3.16433217268322,-0.618926814870015,
7.77571220448507));
#12205=CARTESIAN_POINT('Ctrl Pts',(3.18044274974578,-0.520481967112708,
7.78189498074276));
#12206=CARTESIAN_POINT('Ctrl Pts',(3.19246099655305,-0.447043599718565,
7.78650723831309));
#12207=CARTESIAN_POINT('Ctrl Pts',(3.20192096831247,-0.373270435471746,
7.79111949588342));
#12208=CARTESIAN_POINT('Ctrl Pts',(3.20881669037223,-0.299354321980865,
7.79573175345375));
#12209=CARTESIAN_POINT('Ctrl Pts',(3.21803379498261,-0.200555016479001,
7.80189668587813));
#12210=CARTESIAN_POINT('Ctrl Pts',(3.22268924659059,-0.101318614663308,
7.80806161830251));
#12211=CARTESIAN_POINT('Ctrl Pts',(3.22274940930447,-0.00195123747957988,
7.81422655072689));
#12212=CARTESIAN_POINT('Ctrl Pts',(3.22274932270398,-0.00208938053611371,
7.81661100490856));
#12213=CARTESIAN_POINT('Ctrl Pts',(3.22291239419932,0.249439023247388,7.8311833694689));
#12214=CARTESIAN_POINT('Ctrl Pts',(3.19362926120235,0.500148083184054,7.84481689517584));
#12215=CARTESIAN_POINT('Ctrl Pts',(3.11304789178756,0.839323643325621,7.86460739709412));
#12216=CARTESIAN_POINT('Ctrl Pts',(3.08637114396103,0.932653367675951,7.87019217685673));
#12217=CARTESIAN_POINT('Ctrl Pts',(3.03702325784947,1.07981222902295,7.87933101176798));
#12218=CARTESIAN_POINT('Ctrl Pts',(3.01702917710218,1.13447742086749,7.88280133181157));
#12219=CARTESIAN_POINT('Ctrl Pts',(2.98917878097904,1.20466916884041,7.88736914577782));
#12220=CARTESIAN_POINT('Ctrl Pts',(2.98266097621755,1.22071744217555,7.88842119815647));
#12221=CARTESIAN_POINT('Ctrl Pts',(2.97185811066363,1.2467133712967,7.89013824177165));
#12222=CARTESIAN_POINT('Ctrl Pts',(2.96765165744539,1.25669347718225,7.89080053785394));
#12223=CARTESIAN_POINT('Ctrl Pts',(2.95947034396081,1.27583406340428,7.89207680293235));
#12224=CARTESIAN_POINT('Ctrl Pts',(2.95550305182177,1.28499765804987,7.89269050555653));
#12225=CARTESIAN_POINT('Ctrl Pts',(2.94632807113943,1.30592262726926,7.89409812244582));
#12226=CARTESIAN_POINT('Ctrl Pts',(2.94109245362894,1.31767150027749,7.89489299590258));
#12227=CARTESIAN_POINT('Ctrl Pts',(2.92700875580443,1.34877356737663,7.89700942593846));
#12228=CARTESIAN_POINT('Ctrl Pts',(2.91803920197356,1.36807074854517,7.89833518695753));
#12229=CARTESIAN_POINT('Ctrl Pts',(2.84799321808213,1.51494500003797,7.90852440611709));
#12230=CARTESIAN_POINT('Ctrl Pts',(2.77877707849778,1.63844803163552,7.91767522228456));
#12231=CARTESIAN_POINT('Ctrl Pts',(2.58696198290358,1.93339715144885,7.94099802439458));
#12232=CARTESIAN_POINT('Ctrl Pts',(2.45524212287087,2.09813537452023,7.95541066578146));
#12233=CARTESIAN_POINT('Ctrl Pts',(2.25008038076588,2.30873267972408,7.97515359571141));
#12234=CARTESIAN_POINT('Ctrl Pts',(2.18942374043026,2.3663334451214,7.98070997231011));
#12235=CARTESIAN_POINT('Ctrl Pts',(2.1049415164223,2.44052637500369,7.98801075027205));
#12236=CARTESIAN_POINT('Ctrl Pts',(2.08303683116699,2.45924896257552,7.98986627708023));
#12237=CARTESIAN_POINT('Ctrl Pts',(2.05034708217619,2.48643966698099,7.99257708070185));
#12238=CARTESIAN_POINT('Ctrl Pts',(2.03975497069508,2.49513627876588,7.99344659340964));
#12239=CARTESIAN_POINT('Ctrl Pts',(2.02059230835463,2.51066613007455,7.99500333965673));
#12240=CARTESIAN_POINT('Ctrl Pts',(2.01204182646676,2.51752366226652,7.99569219562318));
#12241=CARTESIAN_POINT('Ctrl Pts',(1.99850021089175,2.52827105065238,7.9967738590614));
#12242=CARTESIAN_POINT('Ctrl Pts',(1.9935324166196,2.53218998182143,7.99716871555721));
#12243=CARTESIAN_POINT('Ctrl Pts',(1.98853853016755,2.53610569118877,7.99756366077424));
#12244=CARTESIAN_POINT('Ctrl Pts',(1.98852399843804,2.53611708532492,7.99756481001003));
#12245=CARTESIAN_POINT('Ctrl Pts',(1.9884948810692,2.53613991546308,7.99756711271136));
#12246=CARTESIAN_POINT('Ctrl Pts',(1.98848029540349,2.53615135148429,7.99756826617885));
#12247=CARTESIAN_POINT('Ctrl Pts',(1.98845019244889,2.53617495355482,7.99757064675373));
#12248=CARTESIAN_POINT('Ctrl Pts',(1.98843467506125,2.5361871196548,7.9975718738667));
#12249=CARTESIAN_POINT('Ctrl Pts',(1.98840338093371,2.53621165473099,7.99757434856349));
#12250=CARTESIAN_POINT('Ctrl Pts',(1.98838760423611,2.5362240236663,7.99757559614334));
#12251=CARTESIAN_POINT('Ctrl Pts',(1.98835578614724,2.53624896857747,7.99757811219431));
#12252=CARTESIAN_POINT('Ctrl Pts',(1.98833974475694,2.53626154454453,7.9975793806647));
#12253=CARTESIAN_POINT('Ctrl Pts',(1.98830739182855,2.53628690777079,7.99758193892604));
#12254=CARTESIAN_POINT('Ctrl Pts',(1.98829108029912,2.53629969501487,7.99758322871561));
#12255=CARTESIAN_POINT('Ctrl Pts',(1.98388901657916,2.53975057588469,7.99793130414242));
#12256=CARTESIAN_POINT('Ctrl Pts',(1.97949436027855,2.54317728359509,7.99827725613142));
#12257=CARTESIAN_POINT('Ctrl Pts',(1.96945807277163,2.55096124526612,7.99906387158608));
#12258=CARTESIAN_POINT('Ctrl Pts',(1.9638107963393,2.55531124009185,7.99950401834394));
#12259=CARTESIAN_POINT('Ctrl Pts',(1.94650630314225,2.56854932982754,8.00084535181694));
#12260=CARTESIAN_POINT('Ctrl Pts',(1.93480264630484,2.57737680339038,8.00174236965873));
#12261=CARTESIAN_POINT('Ctrl Pts',(1.77243199238497,2.69811542548282,8.01405368247367));
#12262=CARTESIAN_POINT('Ctrl Pts',(1.61230561832042,2.79675418420261,8.02462904823332));
#12263=CARTESIAN_POINT('Ctrl Pts',(1.31562301647539,2.94551054961165,8.04320218946657));
#12264=CARTESIAN_POINT('Ctrl Pts',(1.18257688858008,3.00140080208691,8.05120669365991));
#12265=CARTESIAN_POINT('Ctrl Pts',(0.957753331581384,3.07856762020385,8.06472954336099));
#12266=CARTESIAN_POINT('Ctrl Pts',(0.867991302652524,3.10506990587199,8.07012583530546));
#12267=CARTESIAN_POINT('Ctrl Pts',(0.722040652644978,3.14133829389882,8.07899083353608));
#12268=CARTESIAN_POINT('Ctrl Pts',(0.666522630973167,3.15358462152701,8.08238317238944));
#12269=CARTESIAN_POINT('Ctrl Pts',(0.593743553348956,3.16763078918094,8.08686829675858));
#12270=CARTESIAN_POINT('Ctrl Pts',(0.576749066642107,3.17076910540319,8.08791827103549));
#12271=CARTESIAN_POINT('Ctrl Pts',(0.54900534341609,3.1756620255081,8.08963702309177));
#12272=CARTESIAN_POINT('Ctrl Pts',(0.538270859982677,3.17749911786822,8.09030316726141));
#12273=CARTESIAN_POINT('Ctrl Pts',(0.517563639668784,3.18093499629054,8.09159044815188));
#12274=CARTESIAN_POINT('Ctrl Pts',(0.507592280179287,3.18254138152798,8.09221133503163));
#12275=CARTESIAN_POINT('Ctrl Pts',(0.484676630399889,3.18612265613375,8.09364061253893));
#12276=CARTESIAN_POINT('Ctrl Pts',(0.471727591307244,3.18806557138825,8.09445000717394));
#12277=CARTESIAN_POINT('Ctrl Pts',(0.437139984646929,3.19303986949242,8.09661676367176));
#12278=CARTESIAN_POINT('Ctrl Pts',(0.415482116672585,3.19593015368049,8.09797855773902));
#12279=CARTESIAN_POINT('Ctrl Pts',(0.234857759553856,3.21816779616052,8.10937943104561));
#12280=CARTESIAN_POINT('Ctrl Pts',(0.074705678239877,3.22585918932508,8.11978646975565));
#12281=CARTESIAN_POINT('Ctrl Pts',(-0.34142491355845,3.21483667004354,8.14751307528701));
#12282=CARTESIAN_POINT('Ctrl Pts',(-0.595778106288571,3.17754439942478,
8.16518974121458));
#12283=CARTESIAN_POINT('Ctrl Pts',(-0.89716771663642,3.09586081282522,8.18560963661507));
#12284=CARTESIAN_POINT('Ctrl Pts',(-0.950920069685817,3.07977531747029,
8.18922600764724));
#12285=CARTESIAN_POINT('Ctrl Pts',(-1.01533753221225,3.05865067224684,8.193506664754));
#12286=CARTESIAN_POINT('Ctrl Pts',(-1.02642663418538,3.05494723581705,8.19424162145674));
#12287=CARTESIAN_POINT('Ctrl Pts',(-1.04367455731185,3.04908241536222,8.19538147901506));
#12288=CARTESIAN_POINT('Ctrl Pts',(-1.04984724772803,3.04696257205005,8.19578875234949));
#12289=CARTESIAN_POINT('Ctrl Pts',(-1.06130146130086,3.04298999284143,8.19654321773187));
#12290=CARTESIAN_POINT('Ctrl Pts',(-1.06658456098769,3.04114226294447,8.19689069032292));
#12291=CARTESIAN_POINT('Ctrl Pts',(-1.07855473741985,3.03692074154765,8.19767682421497));
#12292=CARTESIAN_POINT('Ctrl Pts',(-1.08523878582975,3.03453862919129,8.19811498571747));
#12293=CARTESIAN_POINT('Ctrl Pts',(-1.10508609886458,3.0273913278311,8.1994137870648));
#12294=CARTESIAN_POINT('Ctrl Pts',(-1.11822644224297,3.02256235304654,8.20027072990811));
#12295=CARTESIAN_POINT('Ctrl Pts',(-1.21961463491292,2.98455128077434,8.20686285523089));
#12296=CARTESIAN_POINT('Ctrl Pts',(-1.30640852586918,2.94759335573578,8.21238969921858));
#12297=CARTESIAN_POINT('Ctrl Pts',(-1.60792321106036,2.80326428826997,8.23158968182284));
#12298=CARTESIAN_POINT('Ctrl Pts',(-1.81213767813902,2.67579461295379,8.24464748064823));
#12299=CARTESIAN_POINT('Ctrl Pts',(-2.07244815745649,2.46972468172623,8.26355017385069));
#12300=CARTESIAN_POINT('Ctrl Pts',(-2.14209781674233,2.40956352509111,8.26886059430073));
#12301=CARTESIAN_POINT('Ctrl Pts',(-2.24994121681319,2.30803644520514,8.27759481609647));
#12302=CARTESIAN_POINT('Ctrl Pts',(-2.28979308661072,2.26850496038625,8.28094505097589));
#12303=CARTESIAN_POINT('Ctrl Pts',(-2.34046849690914,2.21554055983848,8.28538093340298));
#12304=CARTESIAN_POINT('Ctrl Pts',(-2.35224659711994,2.20303170333044,8.28642486364947));
#12305=CARTESIAN_POINT('Ctrl Pts',(-2.37130114201489,2.18246792996896,8.28813532541151));
#12306=CARTESIAN_POINT('Ctrl Pts',(-2.37863800623781,2.17446926908372,8.28879925831892));
#12307=CARTESIAN_POINT('Ctrl Pts',(-2.39271324055299,2.1589679488566,8.29008338226154));
#12308=CARTESIAN_POINT('Ctrl Pts',(-2.39945708545186,2.15147041511032,8.29070333008597));
#12309=CARTESIAN_POINT('Ctrl Pts',(-2.41487995631976,2.13416118244532,8.2921320279114));
#12310=CARTESIAN_POINT('Ctrl Pts',(-2.42353452674198,2.12432802213781,8.29294179066548));
#12311=CARTESIAN_POINT('Ctrl Pts',(-2.44650636077899,2.09790476416592,8.29511296263071));
#12312=CARTESIAN_POINT('Ctrl Pts',(-2.46071456813859,2.08122116765404,8.29647885314647));
#12313=CARTESIAN_POINT('Ctrl Pts',(-2.57967483338234,1.93861417360511,8.30811418962841));
#12314=CARTESIAN_POINT('Ctrl Pts',(-2.6748402046713,1.80503805129905,8.31877045707719));
#12315=CARTESIAN_POINT('Ctrl Pts',(-2.88965063120983,1.44899217831922,8.34650564291163));
#12316=CARTESIAN_POINT('Ctrl Pts',(-2.99409050299239,1.21863699019569,8.36390197583305));
#12317=CARTESIAN_POINT('Ctrl Pts',(-3.08840438705934,0.922662848981157,
8.38424998917271));
#12318=CARTESIAN_POINT('Ctrl Pts',(-3.10466462765573,0.866375763504488,
8.38803103874007));
#12319=CARTESIAN_POINT('Ctrl Pts',(-3.12234782082464,0.798248676855255,
8.39247665849845));
#12320=CARTESIAN_POINT('Ctrl Pts',(-3.12525034542224,0.786808205928582,
8.39321881308502));
#12321=CARTESIAN_POINT('Ctrl Pts',(-3.129661747258,0.769010786393292,8.39436625942861));
#12322=CARTESIAN_POINT('Ctrl Pts',(-3.13121422022984,0.762664900640009,
8.39477399910329));
#12323=CARTESIAN_POINT('Ctrl Pts',(-3.13405570503181,0.750895118596302,
8.39552759582176));
#12324=CARTESIAN_POINT('Ctrl Pts',(-3.13534992942518,0.745472643521718,
8.39587374292877));
#12325=CARTESIAN_POINT('Ctrl Pts',(-3.1382438918827,0.733206809843047,8.3966544013219));
#12326=CARTESIAN_POINT('Ctrl Pts',(-3.13983531561365,0.72636157936522,8.39708842969506));
#12327=CARTESIAN_POINT('Ctrl Pts',(-3.14446866258261,0.706132265454387,
8.39836640889907));
#12328=CARTESIAN_POINT('Ctrl Pts',(-3.14744753597062,0.69273369354334,8.39920681870286));
#12329=CARTESIAN_POINT('Ctrl Pts',(-3.16859455172315,0.594664040890788,
8.40531676340006));
#12330=CARTESIAN_POINT('Ctrl Pts',(-3.18343069731096,0.509302113536559,
8.41041033933932));
#12331=CARTESIAN_POINT('Ctrl Pts',(-3.22766651600784,0.175546192818822,
8.42981776288062));
#12332=CARTESIAN_POINT('Ctrl Pts',(-3.23156117410327,-0.0753367921670371,
8.44338678472963));
#12333=CARTESIAN_POINT('Ctrl Pts',(-3.19725577395872,-0.414666429627105,
8.46281082990313));
#12334=CARTESIAN_POINT('Ctrl Pts',(-3.18427846140868,-0.504739071184974,
8.46806346755697));
#12335=CARTESIAN_POINT('Ctrl Pts',(-3.15724770205412,-0.648847428059623,
8.47671086724397));
#12336=CARTESIAN_POINT('Ctrl Pts',(-3.14557044659996,-0.703279488168077,
8.48003377933204));
#12337=CARTESIAN_POINT('Ctrl Pts',(-3.12846802410272,-0.774014392802717,
8.48443758235242));
#12338=CARTESIAN_POINT('Ctrl Pts',(-3.12431363039132,-0.790616708308909,
8.48547741725762));
#12339=CARTESIAN_POINT('Ctrl Pts',(-3.11731510549376,-0.817668240630555,
8.48718218056504));
#12340=CARTESIAN_POINT('Ctrl Pts',(-3.11455015952333,-0.828137740933525,
8.48784453210263));
#12341=CARTESIAN_POINT('Ctrl Pts',(-3.10911164481082,-0.848318213444777,
8.48912630314015));
#12342=CARTESIAN_POINT('Ctrl Pts',(-3.10644520768443,-0.858030989612591,
8.4897454836416));
#12343=CARTESIAN_POINT('Ctrl Pts',(-3.10020612835715,-0.880347165803772,
8.49117341926795));
#12344=CARTESIAN_POINT('Ctrl Pts',(-3.09660210155425,-0.892941536237934,
8.4919831923793));
#12345=CARTESIAN_POINT('Ctrl Pts',(-3.08675391408626,-0.926579546320306,
8.4941566184354));
#12346=CARTESIAN_POINT('Ctrl Pts',(-3.08037146114403,-0.947581661184512,
8.49552478190982));
#12347=CARTESIAN_POINT('Ctrl Pts',(-3.02362112304629,-1.12768986855556,
8.50735610465119));
#12348=CARTESIAN_POINT('Ctrl Pts',(-2.96118734985755,-1.28270149302478,
8.51822202388104));
#12349=CARTESIAN_POINT('Ctrl Pts',(-2.77168984861823,-1.6647023517483,8.54668743406963));
#12350=CARTESIAN_POINT('Ctrl Pts',(-2.62866977294471,-1.88244272121886,
8.56462354286451));
#12351=CARTESIAN_POINT('Ctrl Pts',(-2.4295901264145,-2.1179209401305,8.58470851864057));
#12352=CARTESIAN_POINT('Ctrl Pts',(-2.39725137917777,-2.15445671347857,
8.58784403981477));
#12353=CARTESIAN_POINT('Ctrl Pts',(-2.35650402086181,-2.19843832546854,
8.59162766756298));
#12354=CARTESIAN_POINT('Ctrl Pts',(-2.34887183217735,-2.20659089907569,
8.59232940588338));
#12355=CARTESIAN_POINT('Ctrl Pts',(-2.33680595919136,-2.21934591824998,
8.59342768532506));
#12356=CARTESIAN_POINT('Ctrl Pts',(-2.33240078661435,-2.22397503764171,
8.59382635875229));
#12357=CARTESIAN_POINT('Ctrl Pts',(-2.32411356840756,-2.23263184940374,
8.59457200576773));
#12358=CARTESIAN_POINT('Ctrl Pts',(-2.32023485212496,-2.23666248801878,
8.59491921444437));
#12359=CARTESIAN_POINT('Ctrl Pts',(-2.31131681927921,-2.24588166135363,
8.59571348561187));
#12360=CARTESIAN_POINT('Ctrl Pts',(-2.30627052284075,-2.25106333846185,
8.59615999462763));
#12361=CARTESIAN_POINT('Ctrl Pts',(-2.29298303880059,-2.26461571331645,
8.59732818088585));
#12362=CARTESIAN_POINT('Ctrl Pts',(-2.28471336820862,-2.27295850822992,
8.59804768331967));
#12363=CARTESIAN_POINT('Ctrl Pts',(-2.22814774798873,-2.32940367215067,
8.60291977523013));
#12364=CARTESIAN_POINT('Ctrl Pts',(-2.17837798877688,-2.3760123525556,8.60696345033467));
#12365=CARTESIAN_POINT('Ctrl Pts',(-2.1056051498441,-2.43995247055496,8.61260527242614));
#12366=CARTESIAN_POINT('Ctrl Pts',(-2.08379434720952,-2.4586057639987,8.61426335794122));
#12367=CARTESIAN_POINT('Ctrl Pts',(-1.88099374527501,-2.62740966316,8.62941227749103));
#12368=CARTESIAN_POINT('Ctrl Pts',(-1.68433187323717,-2.75761579212618,
8.6422176227668));
#12369=CARTESIAN_POINT('Ctrl Pts',(-1.47525540497551,-2.86526422038013,
8.65558740743848));
#12370=CARTESIAN_POINT('Origin',(0.,0.,4.68922655072688));
#12371=CARTESIAN_POINT('',(-1.47525540501219,-2.86526422036124,10.1510771966379));
#12372=CARTESIAN_POINT('',(-1.47525538675478,-2.86526422976154,9.90456889022841));
#12373=CARTESIAN_POINT('',(-1.47525540501186,-2.86526422036142,4.68922655072688));
#12374=CARTESIAN_POINT('Ctrl Pts',(-1.47525540501219,-2.86526422036124,
10.1510771966379));
#12375=CARTESIAN_POINT('Ctrl Pts',(-1.49798330242841,-2.85356217443139,
10.1495893801617));
#12376=CARTESIAN_POINT('Ctrl Pts',(-1.52057167187558,-2.8415898554236,10.1481119797034));
#12377=CARTESIAN_POINT('Ctrl Pts',(-1.75495113035089,-2.7137685504471,10.1327715715633));
#12378=CARTESIAN_POINT('Ctrl Pts',(-1.95323586278964,-2.5747379397887,10.119643525819));
#12379=CARTESIAN_POINT('Ctrl Pts',(-2.20310559319854,-2.35391451488999,
10.1006602024223));
#12380=CARTESIAN_POINT('Ctrl Pts',(-2.26942121423015,-2.29004655308268,
10.0953483063834));
#12381=CARTESIAN_POINT('Ctrl Pts',(-2.37164549888876,-2.18278892774195,
10.0866115088114));
#12382=CARTESIAN_POINT('Ctrl Pts',(-2.40931060051194,-2.14114262205184,
10.0832603040736));
#12383=CARTESIAN_POINT('Ctrl Pts',(-2.45705509425807,-2.08549587202644,
10.0788234103592));
#12384=CARTESIAN_POINT('Ctrl Pts',(-2.46813845933246,-2.07236707565026,
10.0777794983055));
#12385=CARTESIAN_POINT('Ctrl Pts',(-2.4860504739894,-2.05080188878633,10.0760691452295));
#12386=CARTESIAN_POINT('Ctrl Pts',(-2.49294251506406,-2.04241840921544,
10.0754053048263));
#12387=CARTESIAN_POINT('Ctrl Pts',(-2.50615532190427,-2.02617983340296,
10.074121416626));
#12388=CARTESIAN_POINT('Ctrl Pts',(-2.51248183782853,-2.01832956320141,
10.073501612386));
#12389=CARTESIAN_POINT('Ctrl Pts',(-2.52694066273657,-2.00021497316811,
10.0720733272728));
#12390=CARTESIAN_POINT('Ctrl Pts',(-2.5350474126451,-1.98993056647264,10.0712638341013));
#12391=CARTESIAN_POINT('Ctrl Pts',(-2.55654599720707,-1.96231239164215,
10.0690935583276));
#12392=CARTESIAN_POINT('Ctrl Pts',(-2.56982398582325,-1.94489125707648,
10.067728297218));
#12393=CARTESIAN_POINT('Ctrl Pts',(-2.68079255262662,-1.79617655180575,
10.0561031313478));
#12394=CARTESIAN_POINT('Ctrl Pts',(-2.7685143128291,-1.65777344139973,10.0454570177789));
#12395=CARTESIAN_POINT('Ctrl Pts',(-2.96450120822199,-1.28928133952013,
10.0176214483249));
#12396=CARTESIAN_POINT('Ctrl Pts',(-3.0567784004247,-1.05195754527471,10.0001055939133));
#12397=CARTESIAN_POINT('Ctrl Pts',(-3.13445565251752,-0.75134779497655,
9.97978918864016));
#12398=CARTESIAN_POINT('Ctrl Pts',(-3.14719656026249,-0.696053513058442,
9.97613019505615));
#12399=CARTESIAN_POINT('Ctrl Pts',(-3.16079652554137,-0.62898309348485,
9.97180841804277));
#12400=CARTESIAN_POINT('Ctrl Pts',(-3.16305885504856,-0.617505544239278,
9.97107293311871));
#12401=CARTESIAN_POINT('Ctrl Pts',(-3.16648324617846,-0.599619731555221,
9.96993343130642));
#12402=CARTESIAN_POINT('Ctrl Pts',(-3.16768843725006,-0.593219973612614,
9.96952702166769));
#12403=CARTESIAN_POINT('Ctrl Pts',(-3.16989072655983,-0.581327367698841,
9.9687742969665));
#12404=CARTESIAN_POINT('Ctrl Pts',(-3.17089294200678,-0.575835634378956,
9.96842770178606));
#12405=CARTESIAN_POINT('Ctrl Pts',(-3.17313199315836,-0.563383432580207,
9.96764404954695));
#12406=CARTESIAN_POINT('Ctrl Pts',(-3.17436019633908,-0.556421498738663,
9.96720748816599));
#12407=CARTESIAN_POINT('Ctrl Pts',(-3.17793470792605,-0.535762690840379,
9.96591654893985));
#12408=CARTESIAN_POINT('Ctrl Pts',(-3.18021538176781,-0.522054413292213,
9.9650658119158));
#12409=CARTESIAN_POINT('Ctrl Pts',(-3.19676145970589,-0.418467762870959,
9.95867858624681));
#12410=CARTESIAN_POINT('Ctrl Pts',(-3.20730426088762,-0.328027099196606,
9.95333638335265));
#12411=CARTESIAN_POINT('Ctrl Pts',(-3.23197408711659,0.00616865497466972,
9.93406079204967));
#12412=CARTESIAN_POINT('Ctrl Pts',(-3.22223238796559,0.25085153834473,9.92079543740196));
#12413=CARTESIAN_POINT('Ctrl Pts',(-3.17094490334434,0.582792774803053,
9.90167217074299));
#12414=CARTESIAN_POINT('Ctrl Pts',(-3.15306591000912,0.672839092153315,
9.89637495399306));
#12415=CARTESIAN_POINT('Ctrl Pts',(-3.11812266495177,0.816436108454772,
9.88766010022414));
#12416=CARTESIAN_POINT('Ctrl Pts',(-3.10345808221088,0.870519517592819,
9.88431567664817));
#12417=CARTESIAN_POINT('Ctrl Pts',(-3.08246840334816,0.940638544687956,
9.8798865154964));
#12418=CARTESIAN_POINT('Ctrl Pts',(-3.07741361852219,0.957046358428913,
9.87884337039329));
#12419=CARTESIAN_POINT('Ctrl Pts',(-3.06895087267763,0.983755978737971,
9.87713395989083));
#12420=CARTESIAN_POINT('Ctrl Pts',(-3.06562151871285,0.99408248353102,9.87647028961194));
#12421=CARTESIAN_POINT('Ctrl Pts',(-3.05909760074557,1.01397293037028,9.87518650978715));
#12422=CARTESIAN_POINT('Ctrl Pts',(-3.05591016870599,1.02353909135034,9.87456664261014));
#12423=CARTESIAN_POINT('Ctrl Pts',(-3.04847799372856,1.04550042615752,9.87313789604433));
#12424=CARTESIAN_POINT('Ctrl Pts',(-3.04420247311019,1.05788492469834,9.87232800219654));
#12425=CARTESIAN_POINT('Ctrl Pts',(-3.03257012165674,1.09092473599328,9.8701559479281));
#12426=CARTESIAN_POINT('Ctrl Pts',(-3.02507791253301,1.11153133428337,9.86878929741879));
#12427=CARTESIAN_POINT('Ctrl Pts',(-2.95950138301336,1.28631813786793,9.85709312066563));
#12428=CARTESIAN_POINT('Ctrl Pts',(-2.88989202018284,1.43588717610679,9.84637190550986));
#12429=CARTESIAN_POINT('Ctrl Pts',(-2.68360201039837,1.80278617387882,9.81829147750748));
#12430=CARTESIAN_POINT('Ctrl Pts',(-2.53186237251953,2.01032991578635,9.8006002660016));
#12431=CARTESIAN_POINT('Ctrl Pts',(-2.32066532674737,2.23684888889761,9.7803718934559));
#12432=CARTESIAN_POINT('Ctrl Pts',(-2.28320564784507,2.27507214719117,9.77692557209138));
#12433=CARTESIAN_POINT('Ctrl Pts',(-2.23655897998637,2.32035637326267,9.77282108197791));
#12434=CARTESIAN_POINT('Ctrl Pts',(-2.22826602203411,2.32832135118031,9.77209831424605));
#12435=CARTESIAN_POINT('Ctrl Pts',(-2.21524132570283,2.34069760383624,9.7709741995424));
#12436=CARTESIAN_POINT('Ctrl Pts',(-2.21053873152024,2.3451392116252,9.77057056103418));
#12437=CARTESIAN_POINT('Ctrl Pts',(-2.20174917953522,2.35339102839649,9.76982031748659));
#12438=CARTESIAN_POINT('Ctrl Pts',(-2.19766572851964,2.35720472773749,9.76947344889975));
#12439=CARTESIAN_POINT('Ctrl Pts',(-2.18834841325355,2.36586128694528,9.768685778058));
#12440=CARTESIAN_POINT('Ctrl Pts',(-2.18310839275273,2.37069739837347,9.76824549273941));
#12441=CARTESIAN_POINT('Ctrl Pts',(-2.16703974483438,2.38542899350795,9.76690340960159));
#12442=CARTESIAN_POINT('Ctrl Pts',(-2.15615939265464,2.39526813345481,9.7660057886217));
#12443=CARTESIAN_POINT('Ctrl Pts',(-2.0062073826821,2.52902050638279,9.75378009747099));
#12444=CARTESIAN_POINT('Ctrl Pts',(-1.85669279309748,2.64074338310637,9.7432785203068));
#12445=CARTESIAN_POINT('Ctrl Pts',(-1.57744951807622,2.81389496316148,9.72488799190989));
#12446=CARTESIAN_POINT('Ctrl Pts',(-1.45172804239822,2.88077007724106,9.71698961155022));
#12447=CARTESIAN_POINT('Ctrl Pts',(-1.23501970008563,2.97824460780462,9.70348309559244));
#12448=CARTESIAN_POINT('Ctrl Pts',(-1.14634737152156,3.01348638555492,9.69798655318822));
#12449=CARTESIAN_POINT('Ctrl Pts',(-1.00183698375023,3.06361828910557,9.68897431149231));
#12450=CARTESIAN_POINT('Ctrl Pts',(-0.946932956252721,3.08103095048887,
9.68553854747924));
#12451=CARTESIAN_POINT('Ctrl Pts',(-0.874932642321345,3.10175934835942,
9.68100534546626));
#12452=CARTESIAN_POINT('Ctrl Pts',(-0.85823276882279,3.10642152322956,9.67995202291908));
#12453=CARTESIAN_POINT('Ctrl Pts',(-0.830986645732835,3.11379146578005,
9.67823012256292));
#12454=CARTESIAN_POINT('Ctrl Pts',(-0.820462719058099,3.11658098238875,
9.67756421344988));
#12455=CARTESIAN_POINT('Ctrl Pts',(-0.800177928237605,3.12184789111245,
9.67627902135131));
#12456=CARTESIAN_POINT('Ctrl Pts',(-0.790419176992457,3.12433296769904,
9.67565999646816));
#12457=CARTESIAN_POINT('Ctrl Pts',(-0.768019186020709,3.12992548604776,
9.67423734605707));
#12458=CARTESIAN_POINT('Ctrl Pts',(-0.755370508290407,3.13300213940569,
9.67343273435095));
#12459=CARTESIAN_POINT('Ctrl Pts',(-0.721648157117469,3.14098865030842,
9.67128401858587));
#12460=CARTESIAN_POINT('Ctrl Pts',(-0.700543369886417,3.14576297804875,
9.66993557479394));
#12461=CARTESIAN_POINT('Ctrl Pts',(-0.531255537784271,3.18227124631683,
9.65908807285468));
#12462=CARTESIAN_POINT('Ctrl Pts',(-0.381071663922611,3.203725234389,9.64925995083529));
#12463=CARTESIAN_POINT('Ctrl Pts',(-0.00567248030310788,3.2305796653726,
9.62424507274492));
#12464=CARTESIAN_POINT('Ctrl Pts',(0.21965468893966,3.22310717750737,9.60880529587015));
#12465=CARTESIAN_POINT('Ctrl Pts',(0.528483400541867,3.1803116765297,9.58804768226647));
#12466=CARTESIAN_POINT('Ctrl Pts',(0.614095951465856,3.16489589395617,9.58234507767179));
#12467=CARTESIAN_POINT('Ctrl Pts',(0.717425223241102,3.14193815157551,9.57560578178687));
#12468=CARTESIAN_POINT('Ctrl Pts',(0.735827251549994,3.13767949212627,9.57441121379952));
#12469=CARTESIAN_POINT('Ctrl Pts',(0.761874204345368,3.13140985922785,9.57272942361945));
#12470=CARTESIAN_POINT('Ctrl Pts',(0.769550392055552,3.12953226648004,9.57223490938894));
#12471=CARTESIAN_POINT('Ctrl Pts',(0.782745762778267,3.12625319777419,9.57138685912824));
#12472=CARTESIAN_POINT('Ctrl Pts',(0.788268254516875,3.12486530056206,9.57103254646471));
#12473=CARTESIAN_POINT('Ctrl Pts',(0.798956579270361,3.12214900284774,9.57034802112019));
#12474=CARTESIAN_POINT('Ctrl Pts',(0.804122795027835,3.12082241453158,9.57001770216024));
#12475=CARTESIAN_POINT('Ctrl Pts',(0.818033471925459,3.11721357536209,9.56912969396428));
#12476=CARTESIAN_POINT('Ctrl Pts',(0.826771744301351,3.11490733779355,9.56857338400094));
#12477=CARTESIAN_POINT('Ctrl Pts',(0.859071640603072,3.10623713187091,9.56652225761763));
#12478=CARTESIAN_POINT('Ctrl Pts',(0.882571143337986,3.09964215073174,9.56504024065413));
#12479=CARTESIAN_POINT('Ctrl Pts',(1.07885081183562,3.04214429508616,9.55273041844396));
#12480=CARTESIAN_POINT('Ctrl Pts',(1.24718223920008,2.97709836740406,9.54261115321278));
#12481=CARTESIAN_POINT('Ctrl Pts',(1.5341898329561,2.8375501387894,9.52476288014499));
#12482=CARTESIAN_POINT('Ctrl Pts',(1.65510324437602,2.76876523350859,9.51703614433546));
#12483=CARTESIAN_POINT('Ctrl Pts',(1.84816236532744,2.64176095669568,9.50388135650029));
#12484=CARTESIAN_POINT('Ctrl Pts',(1.92291734367836,2.58785471581919,9.49856426891199));
#12485=CARTESIAN_POINT('Ctrl Pts',(2.03938008311484,2.49603753048567,9.48981971212175));
#12486=CARTESIAN_POINT('Ctrl Pts',(2.08258380002192,2.4601054070721,9.48646611008544));
#12487=CARTESIAN_POINT('Ctrl Pts',(2.13774599011124,2.41173278118607,9.482026478794));
#12488=CARTESIAN_POINT('Ctrl Pts',(2.15057655728285,2.40029860216433,9.48098229133988));
#12489=CARTESIAN_POINT('Ctrl Pts',(2.17135997399603,2.3814766916414,9.47927159667604));
#12490=CARTESIAN_POINT('Ctrl Pts',(2.17936814535857,2.37415034316318,9.4786076920225));
#12491=CARTESIAN_POINT('Ctrl Pts',(2.19474329466983,2.35994090603032,9.47732375648716));
#12492=CARTESIAN_POINT('Ctrl Pts',(2.20211529227447,2.35306341718573,9.47670396957851));
#12493=CARTESIAN_POINT('Ctrl Pts',(2.21898668487585,2.33717502306297,9.47527583458854));
#12494=CARTESIAN_POINT('Ctrl Pts',(2.22846363137538,2.3281406382756,9.47446647495386));
#12495=CARTESIAN_POINT('Ctrl Pts',(2.25364176254992,2.30384370911539,9.47229680213002));
#12496=CARTESIAN_POINT('Ctrl Pts',(2.26924267586403,2.28847868020525,9.47093201442676));
#12497=CARTESIAN_POINT('Ctrl Pts',(2.39983737529585,2.157210061642,9.45933120051799));
#12498=CARTESIAN_POINT('Ctrl Pts',(2.50600903112001,2.03289913147211,9.44871083796801));
#12499=CARTESIAN_POINT('Ctrl Pts',(2.75154839361424,1.69679550900973,9.4209534828316));
#12500=CARTESIAN_POINT('Ctrl Pts',(2.87621582036658,1.47563918253337,9.40349158095591));
#12501=CARTESIAN_POINT('Ctrl Pts',(2.99599847901292,1.18888487028301,9.38314505362866));
#12502=CARTESIAN_POINT('Ctrl Pts',(3.01682746053736,1.13499214879745,9.3794177231507));
#12503=CARTESIAN_POINT('Ctrl Pts',(3.04014064956671,1.06948617394439,9.37502640799508));
#12504=CARTESIAN_POINT('Ctrl Pts',(3.04402288902337,1.05838580232535,9.37428702442598));
#12505=CARTESIAN_POINT('Ctrl Pts',(3.04996488561941,1.04109285919292,9.37314280810061));
#12506=CARTESIAN_POINT('Ctrl Pts',(3.05206669242826,1.0349149973481,9.37273555120382));
#12507=CARTESIAN_POINT('Ctrl Pts',(3.05593128977814,1.02344157805368,9.37198205876087));
#12508=CARTESIAN_POINT('Ctrl Pts',(3.05769907260211,1.01814787417535,9.37163553803965));
#12509=CARTESIAN_POINT('Ctrl Pts',(3.06166920903117,1.00615552323239,9.37085306867315));
#12510=CARTESIAN_POINT('Ctrl Pts',(3.06386332985656,0.999454241400612,9.37041760942009));
#12511=CARTESIAN_POINT('Ctrl Pts',(3.07029010964349,0.979605518807584,9.36913292678391));
#12512=CARTESIAN_POINT('Ctrl Pts',(3.07446032692231,0.966437811699707,9.36828729213164));
#12513=CARTESIAN_POINT('Ctrl Pts',(3.10475795287041,0.868590160540404,9.36204972150661));
#12514=CARTESIAN_POINT('Ctrl Pts',(3.12746986524456,0.782883215436703,9.35684192756291));
#12515=CARTESIAN_POINT('Ctrl Pts',(3.15375064262285,0.66412581295219,9.34983739866215));
#12516=CARTESIAN_POINT('Ctrl Pts',(3.16038482555225,0.631802233210747,9.34795208838726));
#12517=CARTESIAN_POINT('Ctrl Pts',(3.20376790413385,0.402610327376689,9.33469908676473));
#12518=CARTESIAN_POINT('Ctrl Pts',(3.22259253227262,0.202793807467092,9.32371333098121));
#12519=CARTESIAN_POINT('Ctrl Pts',(3.22286530194858,-0.146309910456225,
9.30391398381168));
#12520=CARTESIAN_POINT('Ctrl Pts',(3.21267240414683,-0.294949237190834,
9.29529762126277));
#12521=CARTESIAN_POINT('Ctrl Pts',(3.18928614388277,-0.463721191285525,
9.28504670735152));
#12522=CARTESIAN_POINT('Ctrl Pts',(3.18610889489276,-0.48507064016707,9.28374156663271));
#12523=CARTESIAN_POINT('Ctrl Pts',(3.18067454520792,-0.519226390681428,
9.28163937885324));
#12524=CARTESIAN_POINT('Ctrl Pts',(3.17855394234404,-0.532053977661528,
9.28084666557937));
#12525=CARTESIAN_POINT('Ctrl Pts',(3.17465366011762,-0.554791005188704,
9.2794357270943));
#12526=CARTESIAN_POINT('Ctrl Pts',(3.17290504781711,-0.56470565343308,9.27881849944492));
#12527=CARTESIAN_POINT('Ctrl Pts',(3.16916758408359,-0.585331591729099,
9.277530260138));
#12528=CARTESIAN_POINT('Ctrl Pts',(3.16717082125311,-0.596041301100955,
9.27685900277794));
#12529=CARTESIAN_POINT('Ctrl Pts',(3.1618495464183,-0.623800236435388,9.27511292105727));
#12530=CARTESIAN_POINT('Ctrl Pts',(3.15844146081401,-0.64083290234613,9.27403543436173));
#12531=CARTESIAN_POINT('Ctrl Pts',(3.14307892566315,-0.714509519888538,
9.26934759894313));
#12532=CARTESIAN_POINT('Ctrl Pts',(3.12973772570854,-0.770850215272871,
9.26569305806917));
#12533=CARTESIAN_POINT('Ctrl Pts',(3.0902376559278,-0.919663130509084,9.25584722265343));
#12534=CARTESIAN_POINT('Ctrl Pts',(3.0614497149314,-1.01137126634294,9.24957674504851));
#12535=CARTESIAN_POINT('Ctrl Pts',(2.98022535374917,-1.23466994676335,9.23382728287994));
#12536=CARTESIAN_POINT('Ctrl Pts',(2.92313126069588,-1.3643504593328,9.22424625302479));
#12537=CARTESIAN_POINT('Ctrl Pts',(2.77176098731157,-1.65469599580339,9.20208353823569));
#12538=CARTESIAN_POINT('Ctrl Pts',(2.67170607793641,-1.81181697256035,9.18953678143932));
#12539=CARTESIAN_POINT('Ctrl Pts',(2.54972666132089,-1.97109788310698,9.17682059420688));
#12540=CARTESIAN_POINT('Ctrl Pts',(2.54072464006728,-1.98268788134281,9.17589544650774));
#12541=CARTESIAN_POINT('Ctrl Pts',(2.52723056380333,-1.99981851675774,9.17452874573523));
#12542=CARTESIAN_POINT('Ctrl Pts',(2.5227989268441,-2.00540619317524,9.17408306943009));
#12543=CARTESIAN_POINT('Ctrl Pts',(2.51486221130881,-2.01534534008821,9.17329059302083));
#12544=CARTESIAN_POINT('Ctrl Pts',(2.51136433889133,-2.0197024386445,9.172943288152));
#12545=CARTESIAN_POINT('Ctrl Pts',(2.50379313025655,-2.02908337737495,9.17219575804493));
#12546=CARTESIAN_POINT('Ctrl Pts',(2.49971600939352,-2.03410404492456,9.17179581252982));
#12547=CARTESIAN_POINT('Ctrl Pts',(2.48835116928453,-2.04801321648941,9.1706880687874));
#12548=CARTESIAN_POINT('Ctrl Pts',(2.48103088544622,-2.05687516182828,9.16998258709342));
#12549=CARTESIAN_POINT('Ctrl Pts',(2.43940627810851,-2.10672042705616,9.1660149409455));
#12550=CARTESIAN_POINT('Ctrl Pts',(2.40413183363912,-2.14688724595349,9.16281934083323));
#12551=CARTESIAN_POINT('Ctrl Pts',(2.19407341603368,-2.37440551977974,9.14460141689181));
#12552=CARTESIAN_POINT('Ctrl Pts',(1.9984304037041,-2.54127222198343,9.13070291672181));
#12553=CARTESIAN_POINT('Ctrl Pts',(1.64786297988882,-2.77449501317888,9.10692510198949));
#12554=CARTESIAN_POINT('Ctrl Pts',(1.50387583268631,-2.85510453037785,9.09743162937913));
#12555=CARTESIAN_POINT('Ctrl Pts',(1.33447161178886,-2.93356163941016,9.08620296970295));
#12556=CARTESIAN_POINT('Ctrl Pts',(1.31448135868329,-2.94257320999233,9.08487737416152));
#12557=CARTESIAN_POINT('Ctrl Pts',(1.28240218132652,-2.95664233112758,9.08274851622357));
#12558=CARTESIAN_POINT('Ctrl Pts',(1.27037145130872,-2.96183145986221,9.08194976638928));
#12559=CARTESIAN_POINT('Ctrl Pts',(1.24902658658154,-2.97088401352726,9.08053184996504));
#12560=CARTESIAN_POINT('Ctrl Pts',(1.23972528149492,-2.9747773796658,9.07991371464923));
#12561=CARTESIAN_POINT('Ctrl Pts',(1.22037796719648,-2.98276933384184,9.078627346075));
#12562=CARTESIAN_POINT('Ctrl Pts',(1.21032923814628,-2.98686096301863,9.07795888584223));
#12563=CARTESIAN_POINT('Ctrl Pts',(1.18432710459764,-2.9972957172052,9.0762282075589));
#12564=CARTESIAN_POINT('Ctrl Pts',(1.16834348907939,-3.00356218184378,9.07516341484057));
#12565=CARTESIAN_POINT('Ctrl Pts',(1.09999073722591,-3.02973209939585,9.07060538648529));
#12566=CARTESIAN_POINT('Ctrl Pts',(1.04716008443043,-3.04839487894896,9.06707093559214));
#12567=CARTESIAN_POINT('Ctrl Pts',(0.90658853443234,-3.09396735397512,9.05763037682584));
#12568=CARTESIAN_POINT('Ctrl Pts',(0.818143193577447,-3.11852143886941,
9.05165293920046));
#12569=CARTESIAN_POINT('Ctrl Pts',(0.490857110636059,-3.19450050766365,
9.02942785652711));
#12570=CARTESIAN_POINT('Ctrl Pts',(0.247454931007985,-3.22250291739819,
9.01262439416313));
#12571=CARTESIAN_POINT('Ctrl Pts',(-0.0876520562247414,-3.22283972451628,
8.99033885097901));
#12572=CARTESIAN_POINT('Ctrl Pts',(-0.178515946018587,-3.21908591656147,
8.98439165540514));
#12573=CARTESIAN_POINT('Ctrl Pts',(-0.282951967910212,-3.2103346790872,
8.97775364388958));
#12574=CARTESIAN_POINT('Ctrl Pts',(-0.296788736266056,-3.20908507682182,
8.97687820494529));
#12575=CARTESIAN_POINT('Ctrl Pts',(-0.317653036887747,-3.20706471351594,
8.97556466914158));
#12576=CARTESIAN_POINT('Ctrl Pts',(-0.324686611909918,-3.20636026279526,
8.97512298320988));
#12577=CARTESIAN_POINT('Ctrl Pts',(-0.337270918242436,-3.20505804261154,
8.97433480502017));
#12578=CARTESIAN_POINT('Ctrl Pts',(-0.342822445514734,-3.20446898896062,
8.97398783047988));
#12579=CARTESIAN_POINT('Ctrl Pts',(-0.354847837520738,-3.20316140707925,
8.97323782077653));
#12580=CARTESIAN_POINT('Ctrl Pts',(-0.361321043459785,-3.2024376797873,
8.97283508248482));
#12581=CARTESIAN_POINT('Ctrl Pts',(-0.379417873678807,-3.20035882087031,
8.97171181922907));
#12582=CARTESIAN_POINT('Ctrl Pts',(-0.391036516503718,-3.1989599806402,
8.97099371736013));
#12583=CARTESIAN_POINT('Ctrl Pts',(-0.458988538091207,-3.19040306768619,
8.9668104601808));
#12584=CARTESIAN_POINT('Ctrl Pts',(-0.515136280018205,-3.18181987875896,
8.96342063625298));
#12585=CARTESIAN_POINT('Ctrl Pts',(-0.820749016689553,-3.12679845796169,
8.94519273797376));
#12586=CARTESIAN_POINT('Ctrl Pts',(-1.06430605591794,-3.052503420149,8.93142271107741));
#12587=CARTESIAN_POINT('Ctrl Pts',(-1.35706233084856,-2.92384247699667,
8.9133583200562));
#12588=CARTESIAN_POINT('Ctrl Pts',(-1.41662675287091,-2.8954507025908,8.90960221584586));
#12589=CARTESIAN_POINT('Ctrl Pts',(-1.47525556020637,-2.8652641404555,8.90579936292296));
#12590=CARTESIAN_POINT('Ctrl Pts',(-1.47525540497551,-2.86526422038013,
8.65558740743848));
#12591=CARTESIAN_POINT('Ctrl Pts',(-1.4716703386366,-2.86711008452629,8.65581666119134));
#12592=CARTESIAN_POINT('Ctrl Pts',(-1.46808162110067,-2.86894931632668,
8.65604606387195));
#12593=CARTESIAN_POINT('Ctrl Pts',(-1.38229776875123,-2.91271074979506,
8.66152776812017));
#12594=CARTESIAN_POINT('Ctrl Pts',(-1.29834902590854,-2.9510877474239,8.66685272648349));
#12595=CARTESIAN_POINT('Ctrl Pts',(-1.16075934891695,-3.00697844890102,
8.67560917369799));
#12596=CARTESIAN_POINT('Ctrl Pts',(-1.10810194889063,-3.02677900553692,
8.67896655367161));
#12597=CARTESIAN_POINT('Ctrl Pts',(-1.03870922200339,-3.05081896214508,
8.683410516769));
#12598=CARTESIAN_POINT('Ctrl Pts',(-1.02241823841246,-3.05631708361633,
8.68445516869137));
#12599=CARTESIAN_POINT('Ctrl Pts',(-0.995770867771936,-3.06507353801751,
8.6861664584646));
#12600=CARTESIAN_POINT('Ctrl Pts',(-0.985440497902606,-3.06841040851662,
8.68683049147229));
#12601=CARTESIAN_POINT('Ctrl Pts',(-0.965484058273281,-3.07474547626349,
8.68811455985541));
#12602=CARTESIAN_POINT('Ctrl Pts',(-0.955860378730679,-3.07775082540322,
8.68873435070027));
#12603=CARTESIAN_POINT('Ctrl Pts',(-0.933709097689958,-3.08455446537566,
8.69016233101586));
#12604=CARTESIAN_POINT('Ctrl Pts',(-0.921172202562161,-3.08832166298787,
8.69097153064602));
#12605=CARTESIAN_POINT('Ctrl Pts',(-0.88761396206841,-3.09818302358101,
8.69314041771855));
#12606=CARTESIAN_POINT('Ctrl Pts',(-0.866553189475032,-3.10413951440997,
8.6945045724049));
#12607=CARTESIAN_POINT('Ctrl Pts',(-0.688300452419962,-3.15259824695472,
8.70607743356053));
#12608=CARTESIAN_POINT('Ctrl Pts',(-0.528180312545542,-3.18333855606427,
8.71666816677794));
#12609=CARTESIAN_POINT('Ctrl Pts',(-0.114852080147411,-3.23064300032144,
8.74440659358943));
#12610=CARTESIAN_POINT('Ctrl Pts',(0.139242916007588,-3.22968286062258,
8.7618825022252));
#12611=CARTESIAN_POINT('Ctrl Pts',(0.44790830719467,-3.19199450129588,8.78224033719575));
#12612=CARTESIAN_POINT('Ctrl Pts',(0.505022415411805,-3.1834578824089,8.78596562762726));
#12613=CARTESIAN_POINT('Ctrl Pts',(0.573460161699617,-3.17134030070757,
8.79035506889609));
#12614=CARTESIAN_POINT('Ctrl Pts',(0.585028942337611,-3.16922656284242,
8.7910944822084));
#12615=CARTESIAN_POINT('Ctrl Pts',(0.603000158094171,-3.16584127394099,
8.79223881040948));
#12616=CARTESIAN_POINT('Ctrl Pts',(0.60941059694925,-3.16461354490051,8.79264614763672));
#12617=CARTESIAN_POINT('Ctrl Pts',(0.621295875164245,-3.16229981974072,
8.79339973455768));
#12618=CARTESIAN_POINT('Ctrl Pts',(0.626771575046279,-3.1612190857196,8.79374626978552));
#12619=CARTESIAN_POINT('Ctrl Pts',(0.639158763553322,-3.1587407866198,8.79452874988903));
#12620=CARTESIAN_POINT('Ctrl Pts',(0.646068471747284,-3.157334764343,8.79496420565854));
#12621=CARTESIAN_POINT('Ctrl Pts',(0.666501705666531,-3.1531070206157,8.79624905433342));
#12622=CARTESIAN_POINT('Ctrl Pts',(0.680011967978001,-3.15022096786465,
8.79709485737361));
#12623=CARTESIAN_POINT('Ctrl Pts',(0.780161081353696,-3.12815287457219,
8.80333975732255));
#12624=CARTESIAN_POINT('Ctrl Pts',(0.866001731128185,-3.10548479398337,
8.80855425541047));
#12625=CARTESIAN_POINT('Ctrl Pts',(1.1868328461683,-3.00642077449665,8.82789033869272));
#12626=CARTESIAN_POINT('Ctrl Pts',(1.41370747229911,-2.90664476623202,8.84130638490641));
#12627=CARTESIAN_POINT('Ctrl Pts',(1.70586383023312,-2.73578141405782,8.86057975248932));
#12628=CARTESIAN_POINT('Ctrl Pts',(1.78275697294445,-2.68630732155295,8.86585662164684));
#12629=CARTESIAN_POINT('Ctrl Pts',(1.90309176305783,-2.60143807419683,8.87454077949634));
#12630=CARTESIAN_POINT('Ctrl Pts',(1.94789647938893,-2.56806095112801,8.87787552514703));
#12631=CARTESIAN_POINT('Ctrl Pts',(2.00528932027912,-2.52294001700273,8.88229345042803));
#12632=CARTESIAN_POINT('Ctrl Pts',(2.01868440865049,-2.51223502642831,8.8833353019335));
#12633=CARTESIAN_POINT('Ctrl Pts',(2.0404093254302,-2.49458712376726,8.88504299161517));
#12634=CARTESIAN_POINT('Ctrl Pts',(2.04879077891802,-2.48770807633137,8.8857062434288));
#12635=CARTESIAN_POINT('Ctrl Pts',(2.06489764993535,-2.47435181247372,8.88698949385681));
#12636=CARTESIAN_POINT('Ctrl Pts',(2.07262771297458,-2.46788037723152,8.88760925177809));
#12637=CARTESIAN_POINT('Ctrl Pts',(2.09033681141244,-2.45291282786906,8.88903814732017));
#12638=CARTESIAN_POINT('Ctrl Pts',(2.10029458749696,-2.44439194153583,8.88984830148738));
#12639=CARTESIAN_POINT('Ctrl Pts',(2.12678817129933,-2.42143992745245,8.89202194047289));
#12640=CARTESIAN_POINT('Ctrl Pts',(2.14322877241587,-2.40690042138002,8.8933899271966));
#12641=CARTESIAN_POINT('Ctrl Pts',(2.2827557645539,-2.28094442635079,8.90516694677602));
#12642=CARTESIAN_POINT('Ctrl Pts',(2.39719183393805,-2.1603558549026,8.91597398164589));
#12643=CARTESIAN_POINT('Ctrl Pts',(2.66492841174709,-1.83063607487209,8.94431876069702));
#12644=CARTESIAN_POINT('Ctrl Pts',(2.8032466602291,-1.61086202739786,8.96219378389989));
#12645=CARTESIAN_POINT('Ctrl Pts',(2.93522607940133,-1.33157090491372,8.98233057654168));
#12646=CARTESIAN_POINT('Ctrl Pts',(2.95559521241621,-1.28572579333039,8.98555632963982));
#12647=CARTESIAN_POINT('Ctrl Pts',(2.97922195121041,-1.2290163445903,8.98943376617703));
#12648=CARTESIAN_POINT('Ctrl Pts',(2.98350227188833,-1.21858886108651,8.9901421264491));
#12649=CARTESIAN_POINT('Ctrl Pts',(2.99013349329532,-1.20218984925436,8.99124868803198));
#12650=CARTESIAN_POINT('Ctrl Pts',(2.99252136704051,-1.19623351018502,8.99164906915882));
#12651=CARTESIAN_POINT('Ctrl Pts',(2.99695663195689,-1.18507374238135,8.99239629464451));
#12652=CARTESIAN_POINT('Ctrl Pts',(2.99900824882141,-1.17987217646759,8.99274338379594));
#12653=CARTESIAN_POINT('Ctrl Pts',(3.00367049331907,-1.16796102746749,8.99353549271096));
#12654=CARTESIAN_POINT('Ctrl Pts',(3.00627217808673,-1.16124803024697,8.9939799709226));
#12655=CARTESIAN_POINT('Ctrl Pts',(3.01423580993555,-1.14049373062079,8.99534831122658));
#12656=CARTESIAN_POINT('Ctrl Pts',(3.01952213308221,-1.12642335541242,8.99626775216012));
#12657=CARTESIAN_POINT('Ctrl Pts',(3.07921875309348,-0.964090953341672,
9.00678673019368));
#12658=CARTESIAN_POINT('Ctrl Pts',(3.12276612550697,-0.812037597486608,
9.01579504065694));
#12659=CARTESIAN_POINT('Ctrl Pts',(3.19991700970102,-0.441767162907315,
9.0370583626955));
#12660=CARTESIAN_POINT('Ctrl Pts',(3.22262092942917,-0.2221226451123,9.04916950956993));
#12661=CARTESIAN_POINT('Ctrl Pts',(3.22280503408505,0.0933690777550868,
9.06741248524487));
#12662=CARTESIAN_POINT('Ctrl Pts',(3.2186379330999,0.188566570256866,9.07302010788799));
#12663=CARTESIAN_POINT('Ctrl Pts',(3.20856656757026,0.302638112184638,9.07992375128113));
#12664=CARTESIAN_POINT('Ctrl Pts',(3.20669875230241,0.321826556668248,9.08109126048284));
#12665=CARTESIAN_POINT('Ctrl Pts',(3.20334236530984,0.353369598652563,9.08302119681374));
#12666=CARTESIAN_POINT('Ctrl Pts',(3.20195418596328,0.36573455784507,9.08378045261212));
#12667=CARTESIAN_POINT('Ctrl Pts',(3.19932471440276,0.387992713683405,9.08515220645007));
#12668=CARTESIAN_POINT('Ctrl Pts',(3.19810904369534,0.397888822587316,9.08576388625864));
#12669=CARTESIAN_POINT('Ctrl Pts',(3.19541617396367,0.418999995317155,9.08707266108792));
#12670=CARTESIAN_POINT('Ctrl Pts',(3.19392581370026,0.430213217199748,9.08777016578625));
#12671=CARTESIAN_POINT('Ctrl Pts',(3.18973678696645,0.460508635314292,9.08966111865225));
#12672=CARTESIAN_POINT('Ctrl Pts',(3.18692596923275,0.479574617682628,9.09085810916952));
#12673=CARTESIAN_POINT('Ctrl Pts',(3.17172843103085,0.576619875930451,9.09698707409035));
#12674=CARTESIAN_POINT('Ctrl Pts',(3.15665091278065,0.654144462051568,9.10200395413512));
#12675=CARTESIAN_POINT('Ctrl Pts',(3.07883713311036,0.988243965040913,9.12416981602641));
#12676=CARTESIAN_POINT('Ctrl Pts',(2.9875461356485,1.23709004365705,9.14220635502869));
#12677=CARTESIAN_POINT('Ctrl Pts',(2.80552433449375,1.59161619042313,9.16903199702341));
#12678=CARTESIAN_POINT('Ctrl Pts',(2.73665244334882,1.70732273639555,9.17796761178809));
#12679=CARTESIAN_POINT('Ctrl Pts',(2.65230421274883,1.83074399138336,9.18744590603594));
#12680=CARTESIAN_POINT('Ctrl Pts',(2.64378030160727,1.84303199541076,9.18838890461649));
#12681=CARTESIAN_POINT('Ctrl Pts',(2.6310349591373,1.86113519794421,9.18977663021936));
#12682=CARTESIAN_POINT('Ctrl Pts',(2.62687926452469,1.86699612029948,9.19022566594569));
#12683=CARTESIAN_POINT('Ctrl Pts',(2.61945526623255,1.87739258599433,9.19102169111578));
#12684=CARTESIAN_POINT('Ctrl Pts',(2.61619473339349,1.88193356216186,9.19136920460908));
#12685=CARTESIAN_POINT('Ctrl Pts',(2.60916000045344,1.89167728899086,9.19211448556203));
#12686=CARTESIAN_POINT('Ctrl Pts',(2.60538205787526,1.896877225299,9.19251198783122));
#12687=CARTESIAN_POINT('Ctrl Pts',(2.59490949045635,1.91120128828204,9.19360643583568));
#12688=CARTESIAN_POINT('Ctrl Pts',(2.58818224824883,1.92030161347566,9.19430115432792));
#12689=CARTESIAN_POINT('Ctrl Pts',(2.55099350602217,1.97005850746889,9.19809741611763));
#12690=CARTESIAN_POINT('Ctrl Pts',(2.51961999814508,2.01002838935398,9.20113895943597));
#12691=CARTESIAN_POINT('Ctrl Pts',(2.32310159242365,2.24855689683973,9.21935474595476));
#12692=CARTESIAN_POINT('Ctrl Pts',(2.13551256692765,2.42743190190348,9.23335936385393));
#12693=CARTESIAN_POINT('Ctrl Pts',(1.79581040655307,2.68116346683125,9.25729820196802));
#12694=CARTESIAN_POINT('Ctrl Pts',(1.65562654777068,2.76992104126593,9.26684091373934));
#12695=CARTESIAN_POINT('Ctrl Pts',(1.48986637585403,2.85777836006941,9.27812442829722));
#12696=CARTESIAN_POINT('Ctrl Pts',(1.47037600372026,2.86785518190884,9.27945083938159));
#12697=CARTESIAN_POINT('Ctrl Pts',(1.43908328106106,2.88363114730782,9.2815806449037));
#12698=CARTESIAN_POINT('Ctrl Pts',(1.4273462104678,2.88945878514584,9.28237951914445));
#12699=CARTESIAN_POINT('Ctrl Pts',(1.40651728978323,2.89964279004675,9.28379743890598));
#12700=CARTESIAN_POINT('Ctrl Pts',(1.39743987537588,2.90402840677751,9.28441545184472));
#12701=CARTESIAN_POINT('Ctrl Pts',(1.37855574517857,2.91304294802772,9.28570134856046));
#12702=CARTESIAN_POINT('Ctrl Pts',(1.36874595671442,2.91766510432482,9.28636945809643));
#12703=CARTESIAN_POINT('Ctrl Pts',(1.34336077950514,2.92946984265458,9.28809876061871));
#12704=CARTESIAN_POINT('Ctrl Pts',(1.32775119802434,2.93657768171548,9.28916252167605));
#12705=CARTESIAN_POINT('Ctrl Pts',(1.26102660271578,2.96632002912187,9.29371188402403));
#12706=CARTESIAN_POINT('Ctrl Pts',(1.209386592148,2.98774598102589,9.29723850925931));
#12707=CARTESIAN_POINT('Ctrl Pts',(1.07183342575039,3.04066774856621,9.30665339166827));
#12708=CARTESIAN_POINT('Ctrl Pts',(0.985095799150493,3.06986498538147,9.31261250319956));
#12709=CARTESIAN_POINT('Ctrl Pts',(0.660406553527635,3.16398225574356,9.3349711211711));
#12710=CARTESIAN_POINT('Ctrl Pts',(0.416502584125903,3.20521926836399,9.35194162961529));
#12711=CARTESIAN_POINT('Ctrl Pts',(0.0813536956044349,3.22295392914406,
9.37424571010358));
#12712=CARTESIAN_POINT('Ctrl Pts',(-0.00775475380571619,3.22397168958091,
9.38006951616286));
#12713=CARTESIAN_POINT('Ctrl Pts',(-0.11061850414362,3.2208806655178,9.38658716508006));
#12714=CARTESIAN_POINT('Ctrl Pts',(-0.124435534088911,3.22037645764459,
9.38745833889117));
#12715=CARTESIAN_POINT('Ctrl Pts',(-0.145295944476533,3.21948076550597,
9.38876667457754));
#12716=CARTESIAN_POINT('Ctrl Pts',(-0.152341776959527,3.21915505935725,
9.38920738501686));
#12717=CARTESIAN_POINT('Ctrl Pts',(-0.164959541589484,3.21853026184113,
9.38999440652327));
#12718=CARTESIAN_POINT('Ctrl Pts',(-0.170531796884725,3.21823983017888,
9.39034119501025));
#12719=CARTESIAN_POINT('Ctrl Pts',(-0.182614166329064,3.21757861531134,
9.39109144824682));
#12720=CARTESIAN_POINT('Ctrl Pts',(-0.189123898343437,3.21720254760361,
9.39149461285096));
#12721=CARTESIAN_POINT('Ctrl Pts',(-0.207353222164459,3.21609391761046,
9.39262075468844));
#12722=CARTESIAN_POINT('Ctrl Pts',(-0.219070159062452,3.215317048275,9.3933412872343));
#12723=CARTESIAN_POINT('Ctrl Pts',(-0.288154387947364,3.2103571571785,9.39757153764361));
#12724=CARTESIAN_POINT('Ctrl Pts',(-0.345409595099409,3.20470266771449,
9.40100391604283));
#12725=CARTESIAN_POINT('Ctrl Pts',(-0.653570588365002,3.16591298818201,
9.41922684568966));
#12726=CARTESIAN_POINT('Ctrl Pts',(-0.900080585264105,3.1048415486136,9.43296222679318));
#12727=CARTESIAN_POINT('Ctrl Pts',(-1.28986509138494,2.95788461482416,9.45649447512827));
#12728=CARTESIAN_POINT('Ctrl Pts',(-1.43817805786563,2.88867908232728,9.46591447254841));
#12729=CARTESIAN_POINT('Ctrl Pts',(-1.59967309308622,2.79779251669632,9.47706061546423));
#12730=CARTESIAN_POINT('Ctrl Pts',(-1.61864398385091,2.78685998724867,9.47838430205226));
#12731=CARTESIAN_POINT('Ctrl Pts',(-1.6487763986443,2.76908383952427,9.48051053128794));
#12732=CARTESIAN_POINT('Ctrl Pts',(-1.66001038279993,2.76236392318277,9.48130857737277));
#12733=CARTESIAN_POINT('Ctrl Pts',(-1.67982063588193,2.75034939113107,9.48272550560085));
#12734=CARTESIAN_POINT('Ctrl Pts',(-1.6884136421585,2.74508260555808,9.48334335958267));
#12735=CARTESIAN_POINT('Ctrl Pts',(-1.70620492816868,2.73406291229642,9.4846294023192));
#12736=CARTESIAN_POINT('Ctrl Pts',(-1.71539913390263,2.72830369865587,9.48529781918662));
#12737=CARTESIAN_POINT('Ctrl Pts',(-1.73907379116622,2.71330700880579,9.48702894104857));
#12738=CARTESIAN_POINT('Ctrl Pts',(-1.75350964528765,2.7040000888737,9.48809422487012));
#12739=CARTESIAN_POINT('Ctrl Pts',(-1.81480001518858,2.66378844776997,9.4926593151154));
#12740=CARTESIAN_POINT('Ctrl Pts',(-1.86091488820877,2.63177946059573,9.49620050363308));
#12741=CARTESIAN_POINT('Ctrl Pts',(-1.98035413162681,2.54416587160632,9.50566416782904));
#12742=CARTESIAN_POINT('Ctrl Pts',(-2.05216952081148,2.48660012856006,9.51165842230677));
#12743=CARTESIAN_POINT('Ctrl Pts',(-2.30359672599659,2.26674337127322,9.53375417034777));
#12744=CARTESIAN_POINT('Ctrl Pts',(-2.46723286329789,2.08744593288653,9.55039719987753));
#12745=CARTESIAN_POINT('Ctrl Pts',(-2.663655123612,1.81649378285743,9.57266761024716));
#12746=CARTESIAN_POINT('Ctrl Pts',(-2.71479873660925,1.73913184686213,9.57873629335791));
#12747=CARTESIAN_POINT('Ctrl Pts',(-2.76972400385542,1.64770782914626,9.58549209160489));
#12748=CARTESIAN_POINT('Ctrl Pts',(-2.77683015815761,1.63570365196964,9.58637115117821));
#12749=CARTESIAN_POINT('Ctrl Pts',(-2.78742485295167,1.61753836627179,9.58768894027755));
#12750=CARTESIAN_POINT('Ctrl Pts',(-2.79097129348321,1.6114114677634,9.5881312942419));
#12751=CARTESIAN_POINT('Ctrl Pts',(-2.7972776527689,1.60043320605524,9.58892006004445));
#12752=CARTESIAN_POINT('Ctrl Pts',(-2.80004517463904,1.59558632962392,9.58926695862875));
#12753=CARTESIAN_POINT('Ctrl Pts',(-2.80600878783743,1.58507870531524,9.59001610059725));
#12754=CARTESIAN_POINT('Ctrl Pts',(-2.8092003384224,1.57941548676574,9.59041805113255));
#12755=CARTESIAN_POINT('Ctrl Pts',(-2.81806444010061,1.5635747920973,9.59153742176606));
#12756=CARTESIAN_POINT('Ctrl Pts',(-2.82369903394965,1.55337603122321,9.59225244416452));
#12757=CARTESIAN_POINT('Ctrl Pts',(-2.85609538871937,1.49397902119982,9.59638521905967));
#12758=CARTESIAN_POINT('Ctrl Pts',(-2.88162816616604,1.44411709294727,9.59972972498443));
#12759=CARTESIAN_POINT('Ctrl Pts',(-3.01575700741424,1.16444211187001,9.61794643979218));
#12760=CARTESIAN_POINT('Ctrl Pts',(-3.09817900032483,0.923054716826732,
9.63173881364856));
#12761=CARTESIAN_POINT('Ctrl Pts',(-3.18570859213243,0.514082174206023,
9.65536176966456));
#12762=CARTESIAN_POINT('Ctrl Pts',(-3.20773697381939,0.351329983190187,
9.66481285743821));
#12763=CARTESIAN_POINT('Ctrl Pts',(-3.21855927477537,0.165751795175915,
9.6759937772376));
#12764=CARTESIAN_POINT('Ctrl Pts',(-3.21961158512325,0.143870314831026,
9.67731813157889));
#12765=CARTESIAN_POINT('Ctrl Pts',(-3.22093630437289,0.108895955216128,
9.67944522388613));
#12766=CARTESIAN_POINT('Ctrl Pts',(-3.2213521450291,0.0958089539899059,
9.6802434592628));
#12767=CARTESIAN_POINT('Ctrl Pts',(-3.22194692165271,0.0726442245217949,
9.68166059782442));
#12768=CARTESIAN_POINT('Ctrl Pts',(-3.2221583542197,0.0625674513636109,
9.68227847172605));
#12769=CARTESIAN_POINT('Ctrl Pts',(-3.22249918715289,0.0416439451329804,
9.68356443044205));
#12770=CARTESIAN_POINT('Ctrl Pts',(-3.2226211001604,0.0307972330203178,
9.68423274274175));
#12771=CARTESIAN_POINT('Ctrl Pts',(-3.22279453240761,0.00278159494860291,
9.6859633239097));
#12772=CARTESIAN_POINT('Ctrl Pts',(-3.22276361556241,-0.0143873279685257,
9.68702816867261));
#12773=CARTESIAN_POINT('Ctrl Pts',(-3.22204654739059,-0.0876190338672722,
9.69158893827817));
#12774=CARTESIAN_POINT('Ctrl Pts',(-3.22003467467528,-0.143656205561677,
9.69512614878719));
#12775=CARTESIAN_POINT('Ctrl Pts',(-3.21087253438286,-0.29129731510064,
9.70457654195249));
#12776=CARTESIAN_POINT('Ctrl Pts',(-3.20126549255612,-0.382692157390562,
9.71056125480832));
#12777=CARTESIAN_POINT('Ctrl Pts',(-3.152003315448,-0.714310667014597,9.73273901207245));
#12778=CARTESIAN_POINT('Ctrl Pts',(-3.08908152802351,-0.950223591043525,
9.74948244496187));
#12779=CARTESIAN_POINT('Ctrl Pts',(-2.96678166476351,-1.26202453511395,
9.77176154231382));
#12780=CARTESIAN_POINT('Ctrl Pts',(-2.92973094659563,-1.34580062619013,
9.77775345703828));
#12781=CARTESIAN_POINT('Ctrl Pts',(-2.88299531550636,-1.4403642263741,9.78443470487312));
#12782=CARTESIAN_POINT('Ctrl Pts',(-2.87675075076475,-1.45279600366016,
9.78531135087426));
#12783=CARTESIAN_POINT('Ctrl Pts',(-2.86721094744229,-1.47148528569103,
9.78662623839569));
#12784=CARTESIAN_POINT('Ctrl Pts',(-2.86397538915655,-1.47777282953404,
9.78706808122251));
#12785=CARTESIAN_POINT('Ctrl Pts',(-2.85814923070862,-1.48900358710928,
9.78785629887589));
#12786=CARTESIAN_POINT('Ctrl Pts',(-2.85556647007918,-1.49395075017566,
9.78820315755586));
#12787=CARTESIAN_POINT('Ctrl Pts',(-2.84994461869872,-1.50465131123633,
9.78895262920103));
#12788=CARTESIAN_POINT('Ctrl Pts',(-2.84690096056134,-1.51040220490367,
9.78935494707622));
#12789=CARTESIAN_POINT('Ctrl Pts',(-2.83834560884316,-1.52644952754833,
9.79047635235176));
#12790=CARTESIAN_POINT('Ctrl Pts',(-2.83279526655956,-1.53672539605512,
9.79119302804344));
#12791=CARTESIAN_POINT('Ctrl Pts',(-2.80009072036655,-1.59649505770504,
9.79535464469759));
#12792=CARTESIAN_POINT('Ctrl Pts',(-2.77169381693364,-1.64530203835713,
9.79872514163799));
#12793=CARTESIAN_POINT('Ctrl Pts',(-2.60865283788858,-1.90931430755236,
9.81694364049441));
#12794=CARTESIAN_POINT('Ctrl Pts',(-2.45021759577852,-2.10879387516649,
9.83071915178048));
#12795=CARTESIAN_POINT('Ctrl Pts',(-2.15374024844893,-2.40298652498989,
9.85431126676552));
#12796=CARTESIAN_POINT('Ctrl Pts',(-2.02887418081197,-2.50930277753416,
9.86374898835794));
#12797=CARTESIAN_POINT('Ctrl Pts',(-1.87873857697021,-2.61857603550263,
9.87491742070084));
#12798=CARTESIAN_POINT('Ctrl Pts',(-1.86086543534739,-2.63130744865655,
9.87624399463155));
#12799=CARTESIAN_POINT('Ctrl Pts',(-1.83211329116219,-2.65134874795622,
9.87837398979661));
#12800=CARTESIAN_POINT('Ctrl Pts',(-1.82131709964672,-2.65877665656885,
9.87917288903861));
#12801=CARTESIAN_POINT('Ctrl Pts',(-1.80213616556458,-2.67180171971412,
9.88059080996733));
#12802=CARTESIAN_POINT('Ctrl Pts',(-1.79376985189442,-2.67742579793915,
9.8812087987458));
#12803=CARTESIAN_POINT('Ctrl Pts',(-1.77635023594889,-2.68901747386498,
9.88249460191662));
#12804=CARTESIAN_POINT('Ctrl Pts',(-1.76729293966667,-2.69497881184812,
9.88316264184022));
#12805=CARTESIAN_POINT('Ctrl Pts',(-1.74383422122608,-2.71024977440604,
9.88489167062717));
#12806=CARTESIAN_POINT('Ctrl Pts',(-1.72938840997827,-2.71949027207282,
9.88595522642143));
#12807=CARTESIAN_POINT('Ctrl Pts',(-1.66755962161982,-2.75834819943891,
9.89050285297789));
#12808=CARTESIAN_POINT('Ctrl Pts',(-1.61948677151221,-2.78684442464143,
9.89402791235606));
#12809=CARTESIAN_POINT('Ctrl Pts',(-1.53916957404902,-2.83167414442461,
9.89990366609363));
#12810=CARTESIAN_POINT('Ctrl Pts',(-1.50735021788572,-2.84873937595535,
9.90222798148366));
#12811=CARTESIAN_POINT('Ctrl Pts',(-1.47525538675478,-2.86526422976154,
9.90456889022841));
#12812=CARTESIAN_POINT('Origin',(0.,0.,4.68922655072688));
#12813=CARTESIAN_POINT('',(-1.47525557920441,-2.86526413067387,11.4032056183244));
#12814=CARTESIAN_POINT('',(-1.47708659324034,-2.8687591534968,11.1570143151468));
#12815=CARTESIAN_POINT('',(-1.47525540501186,-2.86526422036142,4.68922655072688));
#12816=CARTESIAN_POINT('',(3.22274985762459,0.000957956508987824,10.5578331123621));
#12817=CARTESIAN_POINT('Ctrl Pts',(-1.47525557920443,-2.86526413067385,
11.4032056183244));
#12818=CARTESIAN_POINT('Ctrl Pts',(-1.55962558463346,-2.8218240443327,11.3967822218367));
#12819=CARTESIAN_POINT('Ctrl Pts',(-1.64209689519603,-2.77464724284609,
11.3903638243335));
#12820=CARTESIAN_POINT('Ctrl Pts',(-1.8010868080994,-2.67411042193256,11.3778439993238));
#12821=CARTESIAN_POINT('Ctrl Pts',(-1.87756866665631,-2.62097685199999,
11.3717490710442));
#12822=CARTESIAN_POINT('Ctrl Pts',(-1.96276323435873,-2.55614418275809,
11.364967581164));
#12823=CARTESIAN_POINT('Ctrl Pts',(-1.97382183989785,-2.54761456232175,
11.3640874949074));
#12824=CARTESIAN_POINT('Ctrl Pts',(-1.99040603044308,-2.53465018909514,
11.36276837734));
#12825=CARTESIAN_POINT('Ctrl Pts',(-1.99597284166916,-2.53026879297454,
11.3623257123631));
#12826=CARTESIAN_POINT('Ctrl Pts',(-2.00590142234858,-2.52240128106146,
11.361536495505));
#12827=CARTESIAN_POINT('Ctrl Pts',(-2.01026860632467,-2.5189221645156,11.361189455717));
#12828=CARTESIAN_POINT('Ctrl Pts',(-2.01970132753046,-2.51136743195457,
11.3604401186348));
#12829=CARTESIAN_POINT('Ctrl Pts',(-2.02476356552014,-2.5072878447072,11.3600381138118));
#12830=CARTESIAN_POINT('Ctrl Pts',(-2.03886134501968,-2.49585609985865,
11.358918856345));
#12831=CARTESIAN_POINT('Ctrl Pts',(-2.04786952959166,-2.48847014345071,
11.3582039994555));
#12832=CARTESIAN_POINT('Ctrl Pts',(-2.09988183790694,-2.44535069664492,
11.35407706346));
#12833=CARTESIAN_POINT('Ctrl Pts',(-2.1419931595153,-2.40854934434578,11.3507379774741));
#12834=CARTESIAN_POINT('Ctrl Pts',(-2.37021804312523,-2.19837898327467,
11.3325154773323));
#12835=CARTESIAN_POINT('Ctrl Pts',(-2.53627271948698,-2.00453282905629,
11.3187142659827));
#12836=CARTESIAN_POINT('Ctrl Pts',(-2.76903105961657,-1.65694280405326,
11.2950857487114));
#12837=CARTESIAN_POINT('Ctrl Pts',(-2.84970803114943,-1.5139835367721,11.2856392318007));
#12838=CARTESIAN_POINT('Ctrl Pts',(-2.9284397823553,-1.34567383179771,11.2744631234362));
#12839=CARTESIAN_POINT('Ctrl Pts',(-2.93752060996286,-1.32573385345459,
11.2731385544043));
#12840=CARTESIAN_POINT('Ctrl Pts',(-2.95170357167115,-1.29372915342543,
11.2710110338555));
#12841=CARTESIAN_POINT('Ctrl Pts',(-2.95693679529346,-1.28172301146974,
11.2702125858214));
#12842=CARTESIAN_POINT('Ctrl Pts',(-2.96606890513097,-1.26041837104777,
11.268795018528));
#12843=CARTESIAN_POINT('Ctrl Pts',(-2.9699976336371,-1.25113279574154,11.2681769288483));
#12844=CARTESIAN_POINT('Ctrl Pts',(-2.97806432867333,-1.23181499568147,
11.2668904690997));
#12845=CARTESIAN_POINT('Ctrl Pts',(-2.98219531959709,-1.22178001312148,
11.2662218711312));
#12846=CARTESIAN_POINT('Ctrl Pts',(-2.9927343004414,-1.1958068636574,11.2644904360779));
#12847=CARTESIAN_POINT('Ctrl Pts',(-2.99906561952948,-1.17983814124989,
11.2634250200485));
#12848=CARTESIAN_POINT('Ctrl Pts',(-3.02553309288648,-1.11149261804459,
11.2588607112183));
#12849=CARTESIAN_POINT('Ctrl Pts',(-3.04442608431466,-1.05864796535023,
11.2553204616164));
#12850=CARTESIAN_POINT('Ctrl Pts',(-3.09061690034974,-0.917966149474457,
11.2458605009044));
#12851=CARTESIAN_POINT('Ctrl Pts',(-3.11554936373178,-0.829412029341887,
11.2398690944451));
#12852=CARTESIAN_POINT('Ctrl Pts',(-3.19227882083046,-0.504141170004751,
11.2177603009327));
#12853=CARTESIAN_POINT('Ctrl Pts',(-3.22113139770626,-0.262868800148311,
11.2010997713144));
#12854=CARTESIAN_POINT('Ctrl Pts',(-3.22327656267709,0.0718289220936422,
11.1788279631784));
#12855=CARTESIAN_POINT('Ctrl Pts',(-3.21988794949052,0.164305346742109,
11.1727728340378));
#12856=CARTESIAN_POINT('Ctrl Pts',(-3.21141494718138,0.270418373152363,
11.1660299561688));
#12857=CARTESIAN_POINT('Ctrl Pts',(-3.21021463914389,0.284313289683923,
11.1651510987502));
#12858=CARTESIAN_POINT('Ctrl Pts',(-3.20826903287116,0.305249900405214,
11.1638334582812));
#12859=CARTESIAN_POINT('Ctrl Pts',(-3.20759068519768,0.312297434322119,
11.1633910533549));
#12860=CARTESIAN_POINT('Ctrl Pts',(-3.2063358642608,0.324898539356072,11.1626021172376));
#12861=CARTESIAN_POINT('Ctrl Pts',(-3.20576818094243,0.330452881595464,
11.162255099594));
#12862=CARTESIAN_POINT('Ctrl Pts',(-3.20450790150722,0.342474785370255,
11.1615056024776));
#12863=CARTESIAN_POINT('Ctrl Pts',(-3.20381016152499,0.348941714491311,
11.1611034165942));
#12864=CARTESIAN_POINT('Ctrl Pts',(-3.20180670670892,0.366997801809824,
11.1599831434204));
#12865=CARTESIAN_POINT('Ctrl Pts',(-3.20045764061975,0.378582189160632,
11.1592674589385));
#12866=CARTESIAN_POINT('Ctrl Pts',(-3.19224953043448,0.445883227602772,
11.1551260554791));
#12867=CARTESIAN_POINT('Ctrl Pts',(-3.18399805864601,0.501424138252252,
11.1517739292324));
#12868=CARTESIAN_POINT('Ctrl Pts',(-3.13039205258962,0.807071513004934,
11.1335507822168));
#12869=CARTESIAN_POINT('Ctrl Pts',(-3.05701996011788,1.0513682098473,11.1197582529772));
#12870=CARTESIAN_POINT('Ctrl Pts',(-2.89038256268382,1.43480140705761,11.0961431925978));
#12871=CARTESIAN_POINT('Ctrl Pts',(-2.81371579365257,1.57986057230784,11.0867010159045));
#12872=CARTESIAN_POINT('Ctrl Pts',(-2.71467825288291,1.73698576107125,11.0755297628835));
#12873=CARTESIAN_POINT('Ctrl Pts',(-2.70280755151247,1.75539991284622,11.0742052885981));
#12874=CARTESIAN_POINT('Ctrl Pts',(-2.68354228510609,1.78462598023583,11.0720778915194));
#12875=CARTESIAN_POINT('Ctrl Pts',(-2.67626782295579,1.79551653212933,11.0712794713738));
#12876=CARTESIAN_POINT('Ctrl Pts',(-2.66327600920426,1.81471213071937,11.0698619363849));
#12877=CARTESIAN_POINT('Ctrl Pts',(-2.65758565277239,1.8230353022067,11.0692438509651));
#12878=CARTESIAN_POINT('Ctrl Pts',(-2.64568958411317,1.84026138311309,11.0679573829183));
#12879=CARTESIAN_POINT('Ctrl Pts',(-2.63947777987166,1.84915991158509,11.0672887723064));
#12880=CARTESIAN_POINT('Ctrl Pts',(-2.62331693753186,1.8720632801465,11.0655572676057));
#12881=CARTESIAN_POINT('Ctrl Pts',(-2.61330074964344,1.88602010941229,11.0644917941784));
#12882=CARTESIAN_POINT('Ctrl Pts',(-2.57008805902577,1.94522868562821,11.0599269059579));
#12883=CARTESIAN_POINT('Ctrl Pts',(-2.5358258108675,1.98968693227618,11.056386121302));
#12884=CARTESIAN_POINT('Ctrl Pts',(-2.44239097178528,2.10459129706378,11.0469243676953));
#12885=CARTESIAN_POINT('Ctrl Pts',(-2.38133609116377,2.17343370779137,11.0409316695951));
#12886=CARTESIAN_POINT('Ctrl Pts',(-2.14922051437845,2.41361884040175,11.0188347530876));
#12887=CARTESIAN_POINT('Ctrl Pts',(-1.96196151834427,2.56815047343785,11.0021886538032));
#12888=CARTESIAN_POINT('Ctrl Pts',(-1.6815540356189,2.75083210892615,10.9799181384292));
#12889=CARTESIAN_POINT('Ctrl Pts',(-1.60177343369292,2.79803977986581,10.973852007448));
#12890=CARTESIAN_POINT('Ctrl Pts',(-1.50775919103358,2.84832835933724,10.9670984243568));
#12891=CARTESIAN_POINT('Ctrl Pts',(-1.49541376865095,2.85482922393731,10.9662191982724));
#12892=CARTESIAN_POINT('Ctrl Pts',(-1.47673933272304,2.86450844816374,10.9649011146534));
#12893=CARTESIAN_POINT('Ctrl Pts',(-1.47044161332789,2.86774635741748,10.9644586317073));
#12894=CARTESIAN_POINT('Ctrl Pts',(-1.4591593082244,2.87350010433309,10.9636696114092));
#12895=CARTESIAN_POINT('Ctrl Pts',(-1.45417882665911,2.87602376173337,10.963322587168));
#12896=CARTESIAN_POINT('Ctrl Pts',(-1.44338283151585,2.88145898104969,10.9625731382502));
#12897=CARTESIAN_POINT('Ctrl Pts',(-1.43756507323795,2.88436587827525,10.9621710068267));
#12898=CARTESIAN_POINT('Ctrl Pts',(-1.42129386777355,2.89243447970038,10.9610510390756));
#12899=CARTESIAN_POINT('Ctrl Pts',(-1.41082102751761,2.89755716353035,10.9603356034348));
#12900=CARTESIAN_POINT('Ctrl Pts',(-1.34982066994689,2.92698573463201,10.9561985562239));
#12901=CARTESIAN_POINT('Ctrl Pts',(-1.29869011552112,2.95002816923724,10.9528503565753));
#12902=CARTESIAN_POINT('Ctrl Pts',(-1.01256423107627,3.07009087819637,10.9346274126638));
#12903=CARTESIAN_POINT('Ctrl Pts',(-0.767310856162866,3.14038305454524,
10.920832275842));
#12904=CARTESIAN_POINT('Ctrl Pts',(-0.354560208746654,3.20737609084034,
10.8972131620794));
#12905=CARTESIAN_POINT('Ctrl Pts',(-0.191050714919731,3.22125185441022,
10.8877696689721));
#12906=CARTESIAN_POINT('Ctrl Pts',(-0.00529974196128598,3.22282011361123,
10.8765969432883));
#12907=CARTESIAN_POINT('Ctrl Pts',(0.0166094839844362,3.22278166506746,
10.8752724402596));
#12908=CARTESIAN_POINT('Ctrl Pts',(0.0516120848206564,3.22236330690173,
10.8731450057374));
#12909=CARTESIAN_POINT('Ctrl Pts',(0.0647067302673271,3.22212695592169,
10.8723465771452));
#12910=CARTESIAN_POINT('Ctrl Pts',(0.0878789691468688,3.22156739892338,
10.8709290323899));
#12911=CARTESIAN_POINT('Ctrl Pts',(0.0979572267871528,3.22127670296654,
10.8703109456978));
#12912=CARTESIAN_POINT('Ctrl Pts',(0.118879945858261,3.22057493171657,10.8690244802196));
#12913=CARTESIAN_POINT('Ctrl Pts',(0.129724012814446,3.22015636393875,10.8683558734746));
#12914=CARTESIAN_POINT('Ctrl Pts',(0.15772800000834,3.21893375950179,10.8666243900052));
#12915=CARTESIAN_POINT('Ctrl Pts',(0.174883806375793,3.2180472814885,10.8655589340622));
#12916=CARTESIAN_POINT('Ctrl Pts',(0.24805145342529,3.21367973866508,10.8609942221247));
#12917=CARTESIAN_POINT('Ctrl Pts',(0.303971492726745,3.20887327249658,10.8574536002401));
#12918=CARTESIAN_POINT('Ctrl Pts',(0.451135896167595,3.19234295185569,10.8479923919375));
#12919=CARTESIAN_POINT('Ctrl Pts',(0.542047982303594,3.17816906078065,10.8420000866492));
#12920=CARTESIAN_POINT('Ctrl Pts',(0.866412014270041,3.11327598257188,10.8201165218221));
#12921=CARTESIAN_POINT('Ctrl Pts',(1.09464275278692,3.04054268406527,10.803701380165));
#12922=CARTESIAN_POINT('Ctrl Pts',(1.40014810886269,2.90428378293928,10.7814167287697));
#12923=CARTESIAN_POINT('Ctrl Pts',(1.48579228432837,2.86141644763472,10.7751427147965));
#12924=CARTESIAN_POINT('Ctrl Pts',(1.58167602929379,2.80795579861786,10.7681881096508));
#12925=CARTESIAN_POINT('Ctrl Pts',(1.59389867997548,2.80103585187668,10.7673029413118));
#12926=CARTESIAN_POINT('Ctrl Pts',(1.61223237717275,2.79049722261895,10.7659777169445));
#12927=CARTESIAN_POINT('Ctrl Pts',(1.61837715256677,2.78693799389069,10.7655339783068));
#12928=CARTESIAN_POINT('Ctrl Pts',(1.62908010294893,2.78069120525911,10.7647618914686));
#12929=CARTESIAN_POINT('Ctrl Pts',(1.6336434630515,2.77801270657873,10.7644329638803));
#12930=CARTESIAN_POINT('Ctrl Pts',(1.64357017502513,2.77215322893339,10.7637180317112));
#12931=CARTESIAN_POINT('Ctrl Pts',(1.64893088528951,2.76896792722784,10.763332314453));
#12932=CARTESIAN_POINT('Ctrl Pts',(1.65999103911105,2.76235254092839,10.7625371941743));
#12933=CARTESIAN_POINT('Ctrl Pts',(1.66568918150305,2.75892032555409,10.7621279306267));
#12934=CARTESIAN_POINT('Ctrl Pts',(1.68002616244875,2.7502239898496,10.7610990408874));
#12935=CARTESIAN_POINT('Ctrl Pts',(1.6886509886705,2.74493674707836,10.7604808637656));
#12936=CARTESIAN_POINT('Ctrl Pts',(1.71320090751304,2.72972750609882,10.7587230800798));
#12937=CARTESIAN_POINT('Ctrl Pts',(1.72906472159331,2.71970675471726,10.7575894131268));
#12938=CARTESIAN_POINT('Ctrl Pts',(1.78238551226821,2.68537029574562,10.7537832048515));
#12939=CARTESIAN_POINT('Ctrl Pts',(1.8194258288144,2.66041383834934,10.7511462510898));
#12940=CARTESIAN_POINT('Ctrl Pts',(2.13152175171637,2.44056653566909,10.7288809610057));
#12941=CARTESIAN_POINT('Ctrl Pts',(2.3749574296183,2.2043987770684,10.7109741473272));
#12942=CARTESIAN_POINT('Ctrl Pts',(2.6235119611293,1.87328845512069,10.6868328791834));
#12943=CARTESIAN_POINT('Ctrl Pts',(2.6674361742777,1.81019542813909,10.6822810029715));
#12944=CARTESIAN_POINT('Ctrl Pts',(2.71977023657144,1.72897609662921,10.6764492564413));
#12945=CARTESIAN_POINT('Ctrl Pts',(2.73032617229488,1.71225799703041,10.6752503437857));
#12946=CARTESIAN_POINT('Ctrl Pts',(2.74679918297442,1.68562896691339,10.6733425395163));
#12947=CARTESIAN_POINT('Ctrl Pts',(2.75281810458146,1.67578138291038,10.6726374192599));
#12948=CARTESIAN_POINT('Ctrl Pts',(2.76392950169765,1.65738057185449,10.6713204978176));
#12949=CARTESIAN_POINT('Ctrl Pts',(2.76903551055157,1.648835646169,10.6707092032985));
#12950=CARTESIAN_POINT('Ctrl Pts',(2.78028303274159,1.62981327583443,10.6693488582996));
#12951=CARTESIAN_POINT('Ctrl Pts',(2.78640504995678,1.61932453428315,10.6685991082391));
#12952=CARTESIAN_POINT('Ctrl Pts',(2.8040093057205,1.58876805378918,10.6664156985395));
#12953=CARTESIAN_POINT('Ctrl Pts',(2.81533487337062,1.56861136713751,10.6649764079393));
#12954=CARTESIAN_POINT('Ctrl Pts',(2.90409803173457,1.40657669581037,10.6534120647824));
#12955=CARTESIAN_POINT('Ctrl Pts',(2.97096711974397,1.25919957825345,10.6429110463986));
#12956=CARTESIAN_POINT('Ctrl Pts',(3.12180178625786,0.846990579493617,10.6136678208884));
#12957=CARTESIAN_POINT('Ctrl Pts',(3.18308411018918,0.575334432107627,10.5944506372698));
#12958=CARTESIAN_POINT('Ctrl Pts',(3.21229553976881,0.262043956539741,10.5740783550387));
#12959=CARTESIAN_POINT('Ctrl Pts',(3.21511418750193,0.224834859504792,10.5716890219465));
#12960=CARTESIAN_POINT('Ctrl Pts',(3.21795671821606,0.17608195426987,10.5686051514979));
#12961=CARTESIAN_POINT('Ctrl Pts',(3.21856563976836,0.16457681152917,10.5678807943407));
#12962=CARTESIAN_POINT('Ctrl Pts',(3.21942362377048,0.146532940447777,10.5667503557756));
#12963=CARTESIAN_POINT('Ctrl Pts',(3.21971448617815,0.139996432912698,10.5663419973613));
#12964=CARTESIAN_POINT('Ctrl Pts',(3.22021643665896,0.127885799354535,10.5655875912027));
#12965=CARTESIAN_POINT('Ctrl Pts',(3.22043295805322,0.122312060161479,10.5652412512962));
#12966=CARTESIAN_POINT('Ctrl Pts',(3.22083082272986,0.11133550795636,10.5645608762737));
#12967=CARTESIAN_POINT('Ctrl Pts',(3.22101304241447,0.105932835257869,10.5642267938024));
#12968=CARTESIAN_POINT('Ctrl Pts',(3.22139714672244,0.0936253284672779,
10.5634675083963));
#12969=CARTESIAN_POINT('Ctrl Pts',(3.22159042766405,0.0867202252337855,
10.5630427800223));
#12970=CARTESIAN_POINT('Ctrl Pts',(3.2220561204257,0.0679222451187732,10.5618898486576));
#12971=CARTESIAN_POINT('Ctrl Pts',(3.22228489092747,0.0560282619952359,
10.5611639749329));
#12972=CARTESIAN_POINT('Ctrl Pts',(3.22264488862159,0.029742450308617,10.559567243009));
#12973=CARTESIAN_POINT('Ctrl Pts',(3.22274557949115,0.0153504198564817,
10.5586979364159));
#12974=CARTESIAN_POINT('Ctrl Pts',(3.22274985762459,0.000957956508987824,
10.5578331123621));
#12975=CARTESIAN_POINT('Ctrl Pts',(3.22274985678079,0.000960791019879378,
10.5578332826841));
#12976=CARTESIAN_POINT('Ctrl Pts',(3.22284502429836,-0.318256496901387,
10.5386519256575));
#12977=CARTESIAN_POINT('Ctrl Pts',(3.17551406438504,-0.635789600383076,
10.5216430859734));
#12978=CARTESIAN_POINT('Ctrl Pts',(3.05570701839362,-1.02811652446106,10.4982774444553));
#12979=CARTESIAN_POINT('Ctrl Pts',(3.02551755449615,-1.11382701694309,10.4930317249368));
#12980=CARTESIAN_POINT('Ctrl Pts',(2.97107126515853,-1.24977873948251,10.4843939002583));
#12981=CARTESIAN_POINT('Ctrl Pts',(2.9490600558191,-1.30086724348337,10.4810733252899));
#12982=CARTESIAN_POINT('Ctrl Pts',(2.91855856288254,-1.36690405717254,10.4766713579713));
#12983=CARTESIAN_POINT('Ctrl Pts',(2.91125456898652,-1.3823919861739,10.4756309119887));
#12984=CARTESIAN_POINT('Ctrl Pts',(2.89912586957821,-1.40758810111851,10.4739248117993));
#12985=CARTESIAN_POINT('Ctrl Pts',(2.89437493416836,-1.41733157940731,10.4732617333196));
#12986=CARTESIAN_POINT('Ctrl Pts',(2.88510844896831,-1.43609489433333,10.4719783143048));
#12987=CARTESIAN_POINT('Ctrl Pts',(2.88059952588633,-1.44511787602599,10.4713582119254));
#12988=CARTESIAN_POINT('Ctrl Pts',(2.87012639595589,-1.46583228702481,10.469927796404));
#12989=CARTESIAN_POINT('Ctrl Pts',(2.86413300943782,-1.47750868643941,10.4691164610791));
#12990=CARTESIAN_POINT('Ctrl Pts',(2.84790056561683,-1.50866303546962,10.4669380262231));
#12991=CARTESIAN_POINT('Ctrl Pts',(2.83753319786989,-1.52807300166756,10.4655663950886));
#12992=CARTESIAN_POINT('Ctrl Pts',(2.71837612220439,-1.74576636720364,10.450016847512));
#12993=CARTESIAN_POINT('Ctrl Pts',(2.58922376708028,-1.93213677343821,10.4350730546845));
#12994=CARTESIAN_POINT('Ctrl Pts',(2.2967124191642,-2.2716845654297,10.404820104905));
#12995=CARTESIAN_POINT('Ctrl Pts',(2.13475092148466,-2.42451849944251,10.3896152615607));
#12996=CARTESIAN_POINT('Ctrl Pts',(1.94241045328373,-2.57168466886247,10.3740445904836));
#12997=CARTESIAN_POINT('Ctrl Pts',(1.92635619951598,-2.58373223118786,10.3727624020859));
#12998=CARTESIAN_POINT('Ctrl Pts',(1.90164392252171,-2.60191862765083,10.3708165530086));
#12999=CARTESIAN_POINT('Ctrl Pts',(1.89306669790262,-2.60816576111351,10.370146232016));
#13000=CARTESIAN_POINT('Ctrl Pts',(1.87889627222094,-2.61837991436293,10.3690472933864));
#13001=CARTESIAN_POINT('Ctrl Pts',(1.87332106323312,-2.62237159338074,10.3686170750685));
#13002=CARTESIAN_POINT('Ctrl Pts',(1.86252550120425,-2.63004888815279,10.3677882293625));
#13003=CARTESIAN_POINT('Ctrl Pts',(1.85730684770323,-2.63373682661498,10.36738944668));
#13004=CARTESIAN_POINT('Ctrl Pts',(1.85206003720534,-2.63742131285979,10.3669904307397));
#13005=CARTESIAN_POINT('Ctrl Pts',(1.85204286822498,-2.63743336924312,10.3669891250724));
#13006=CARTESIAN_POINT('Ctrl Pts',(1.85200827980509,-2.63745765738266,10.3669864947322));
#13007=CARTESIAN_POINT('Ctrl Pts',(1.85199086037716,-2.63746988912339,10.3669851700609));
#13008=CARTESIAN_POINT('Ctrl Pts',(1.85195576586537,-2.63749453160466,10.3669825013194));
#13009=CARTESIAN_POINT('Ctrl Pts',(1.85193809086189,-2.63750694228114,10.366981157256));
#13010=CARTESIAN_POINT('Ctrl Pts',(1.85190247998262,-2.63753194627374,10.3669784493354));
#13011=CARTESIAN_POINT('Ctrl Pts',(1.85188454410604,-2.6375445395825,10.3669770854789));
#13012=CARTESIAN_POINT('Ctrl Pts',(1.85184840617116,-2.63756991254374,10.3669743375705));
#13013=CARTESIAN_POINT('Ctrl Pts',(1.85183020402882,-2.63758269224706,10.3669729535129));
#13014=CARTESIAN_POINT('Ctrl Pts',(1.85179352799323,-2.63760844188289,10.3669701647807));
#13015=CARTESIAN_POINT('Ctrl Pts',(1.8517750540992,-2.63762141180751,10.3669687601068));
#13016=CARTESIAN_POINT('Ctrl Pts',(1.85173782884695,-2.63764754587153,10.3669659297099));
#13017=CARTESIAN_POINT('Ctrl Pts',(1.85171907747196,-2.63766071001395,10.3669645039863));
#13018=CARTESIAN_POINT('Ctrl Pts',(1.85168129136368,-2.63768723662504,10.366961631044));
#13019=CARTESIAN_POINT('Ctrl Pts',(1.85166225667835,-2.63770059905095,10.3669601838296));
#13020=CARTESIAN_POINT('Ctrl Pts',(1.8516238979749,-2.63772752639571,10.3669572674537));
#13021=CARTESIAN_POINT('Ctrl Pts',(1.85160457390084,-2.63774109134443,10.3669557982888));
#13022=CARTESIAN_POINT('Ctrl Pts',(1.8515656301836,-2.63776842808412,10.3669528375399));
#13023=CARTESIAN_POINT('Ctrl Pts',(1.85154601060022,-2.63778219982337,10.3669513459613));
#13024=CARTESIAN_POINT('Ctrl Pts',(1.84708169753427,-2.64091579830804,10.3666119527316));
#13025=CARTESIAN_POINT('Ctrl Pts',(1.84262918598116,-2.6440243445692,10.3662748410378));
#13026=CARTESIAN_POINT('Ctrl Pts',(1.83234061762384,-2.651168755314,10.3654990284983));
#13027=CARTESIAN_POINT('Ctrl Pts',(1.82649908532334,-2.65519660321681,10.3650608770086));
#13028=CARTESIAN_POINT('Ctrl Pts',(1.80907676353054,-2.66712492301295,10.3637608614477));
#13029=CARTESIAN_POINT('Ctrl Pts',(1.79745749822692,-2.6749692801828,10.36290271458));
#13030=CARTESIAN_POINT('Ctrl Pts',(1.70709950446866,-2.73511684668989,10.3562944840935));
#13031=CARTESIAN_POINT('Ctrl Pts',(1.62613711227536,-2.78401412150131,10.350754166926));
#13032=CARTESIAN_POINT('Ctrl Pts',(1.33166788885473,-2.94462200004839,10.3314930094696));
#13033=CARTESIAN_POINT('Ctrl Pts',(1.10793218277272,-3.03589138369954,10.3183916060861));
#13034=CARTESIAN_POINT('Ctrl Pts',(0.788119084471142,-3.12623497886247,
10.2994675069156));
#13035=CARTESIAN_POINT('Ctrl Pts',(0.699121278738718,-3.14733289752156,
10.2941890526453));
#13036=CARTESIAN_POINT('Ctrl Pts',(0.554478384177032,-3.17518408874531,
10.2855022530201));
#13037=CARTESIAN_POINT('Ctrl Pts',(0.499342319239361,-3.18432048547578,
10.2821665051944));
#13038=CARTESIAN_POINT('Ctrl Pts',(0.427010102499228,-3.19438165247303,
10.2777472344394));
#13039=CARTESIAN_POINT('Ctrl Pts',(0.410002874366996,-3.19660904625651,
10.276705068272));
#13040=CARTESIAN_POINT('Ctrl Pts',(0.38221346511501,-3.20002313648449,10.2749968578659));
#13041=CARTESIAN_POINT('Ctrl Pts',(0.371441500054232,-3.20129136668941,
10.2743334017013));
#13042=CARTESIAN_POINT('Ctrl Pts',(0.350642214861469,-3.2036337647008,10.2730497517792));
#13043=CARTESIAN_POINT('Ctrl Pts',(0.340615838712425,-3.20471529279946,
10.2724297988624));
#13044=CARTESIAN_POINT('Ctrl Pts',(0.317543671443908,-3.20709455031482,
10.2710004465885));
#13045=CARTESIAN_POINT('Ctrl Pts',(0.304494774535512,-3.20835976194212,
10.2701900299765));
#13046=CARTESIAN_POINT('Ctrl Pts',(0.269573840309987,-3.21153071290395,
10.26801566431));
#13047=CARTESIAN_POINT('Ctrl Pts',(0.247689740222265,-3.21329259940096,
10.2666472101627));
#13048=CARTESIAN_POINT('Ctrl Pts',(0.059988465600142,-3.22647557303819,
10.254858011993));
#13049=CARTESIAN_POINT('Ctrl Pts',(-0.106438700738981,-3.22527498780651,
10.2440383384694));
#13050=CARTESIAN_POINT('Ctrl Pts',(-0.531338313986339,-3.18928379415443,
10.2155797395566));
#13051=CARTESIAN_POINT('Ctrl Pts',(-0.787039498767731,-3.1359874064069,
10.1975971022901));
#13052=CARTESIAN_POINT('Ctrl Pts',(-1.07954729539195,-3.03694815678367,
10.1774853033915));
#13053=CARTESIAN_POINT('Ctrl Pts',(-1.1251955315476,-3.02033310938187,10.1743639042678));
#13054=CARTESIAN_POINT('Ctrl Pts',(-1.18085402766399,-2.99863734623587,
10.1705941498794));
#13055=CARTESIAN_POINT('Ctrl Pts',(-1.19123357578031,-2.99452913585048,
10.1698927107355));
#13056=CARTESIAN_POINT('Ctrl Pts',(-1.20752540810535,-2.98798273829578,
10.1687944355655));
#13057=CARTESIAN_POINT('Ctrl Pts',(-1.21345202120171,-2.98558078931128,
10.1683954736367));
#13058=CARTESIAN_POINT('Ctrl Pts',(-1.22455360523872,-2.98104300057448,
10.1676492657864));
#13059=CARTESIAN_POINT('Ctrl Pts',(-1.22973009961706,-2.97891134242453,
10.1673017846651));
#13060=CARTESIAN_POINT('Ctrl Pts',(-1.24159083835303,-2.9739909560196,10.1665066461189));
#13061=CARTESIAN_POINT('Ctrl Pts',(-1.24827124460703,-2.97119318097447,
10.1660595444378));
#13062=CARTESIAN_POINT('Ctrl Pts',(-1.2657887305887,-2.96378729431802,10.1648889738636));
#13063=CARTESIAN_POINT('Ctrl Pts',(-1.27661019941558,-2.95914221440038,
10.1641676937968));
#13064=CARTESIAN_POINT('Ctrl Pts',(-1.35040293112984,-2.92698678512689,
10.1592602260017));
#13065=CARTESIAN_POINT('Ctrl Pts',(-1.41251083056509,-2.89752556693551,
10.1551847600551));
#13066=CARTESIAN_POINT('Ctrl Pts',(-1.47417450518162,-2.86582055618364,
10.1511479553663));
#13067=CARTESIAN_POINT('Ctrl Pts',(-1.47471499453864,-2.86554246467336,
10.1511125730562));
#13068=CARTESIAN_POINT('Ctrl Pts',(-1.47525540501219,-2.86526422036124,
10.1510771966379));
#13069=CARTESIAN_POINT('',(3.219554665156,0.0024747518059529,10.314228031951));
#13070=CARTESIAN_POINT('Ctrl Pts',(-1.47525538675478,-2.86526422976154,
9.90456889022841));
#13071=CARTESIAN_POINT('Ctrl Pts',(-1.42608413530922,-2.89058132017682,
9.9081553061229));
#13072=CARTESIAN_POINT('Ctrl Pts',(-1.3762662959304,-2.91463002933362,9.91178081147647));
#13073=CARTESIAN_POINT('Ctrl Pts',(-1.10064096532606,-3.03903929931898,
9.93178094839435));
#13074=CARTESIAN_POINT('Ctrl Pts',(-0.864512675695613,-3.11444578920707,
9.9487879064623));
#13075=CARTESIAN_POINT('Ctrl Pts',(-0.535068846551581,-3.17925885939,9.97109842536471));
#13076=CARTESIAN_POINT('Ctrl Pts',(-0.447356568786386,-3.19278260631622,
9.97689759602164));
#13077=CARTESIAN_POINT('Ctrl Pts',(-0.345464231859352,-3.20421016714256,
9.98339114517325));
#13078=CARTESIAN_POINT('Ctrl Pts',(-0.331728354010996,-3.20566134299046,
9.98426143367154));
#13079=CARTESIAN_POINT('Ctrl Pts',(-0.310967743538574,-3.20771980176948,
9.9855686826844));
#13080=CARTESIAN_POINT('Ctrl Pts',(-0.303949859257804,-3.20839239331602,
9.98600918378697));
#13081=CARTESIAN_POINT('Ctrl Pts',(-0.291374193910605,-3.20955600823922,
9.98679596302675));
#13082=CARTESIAN_POINT('Ctrl Pts',(-0.285817315268795,-3.21005563109679,
9.9871427174924));
#13083=CARTESIAN_POINT('Ctrl Pts',(-0.273761364423272,-3.21110803605871,
9.98789305152055));
#13084=CARTESIAN_POINT('Ctrl Pts',(-0.267261922870133,-3.21165551861589,
9.9882963301175));
#13085=CARTESIAN_POINT('Ctrl Pts',(-0.249048001287875,-3.21313410071747,
9.98942313393491));
#13086=CARTESIAN_POINT('Ctrl Pts',(-0.237329883312136,-3.21402087618217,
9.99014420971895));
#13087=CARTESIAN_POINT('Ctrl Pts',(-0.168074167435059,-3.2188810106791,
9.99438442331592));
#13088=CARTESIAN_POINT('Ctrl Pts',(-0.110439159877188,-3.22137362544372,
9.99782579394302));
#13089=CARTESIAN_POINT('Ctrl Pts',(0.200148389134544,-3.22645938590669,
10.0160489870111));
#13090=CARTESIAN_POINT('Ctrl Pts',(0.452691870845346,-3.20081178328196,
10.029778169041));
#13091=CARTESIAN_POINT('Ctrl Pts',(0.859077090697755,-3.11043021258567,
10.0532963674504));
#13092=CARTESIAN_POINT('Ctrl Pts',(1.0155513856581,-3.06291276088429,10.0627086543546));
#13093=CARTESIAN_POINT('Ctrl Pts',(1.18819183158754,-2.99579693215432,10.0738491812351));
#13094=CARTESIAN_POINT('Ctrl Pts',(1.20856218172659,-2.98763727781313,10.0751757454327));
#13095=CARTESIAN_POINT('Ctrl Pts',(1.24096173859374,-2.97427356764129,10.077305723501));
#13096=CARTESIAN_POINT('Ctrl Pts',(1.25304550623379,-2.96920296429354,10.0781046153966));
#13097=CARTESIAN_POINT('Ctrl Pts',(1.27436955453815,-2.96010159032109,10.0795225223718));
#13098=CARTESIAN_POINT('Ctrl Pts',(1.28362253157654,-2.95610087434726,10.0801405045478));
#13099=CARTESIAN_POINT('Ctrl Pts',(1.29307358353671,-2.95196177587413,10.0807745401857));
#13100=CARTESIAN_POINT('Ctrl Pts',(1.29329065361507,-2.95186668126035,10.0807891041314));
#13101=CARTESIAN_POINT('Ctrl Pts',(1.29369497105309,-2.95168950368619,10.0808162339662));
#13102=CARTESIAN_POINT('Ctrl Pts',(1.29388222044804,-2.95160742713306,10.0808287996007));
#13103=CARTESIAN_POINT('Ctrl Pts',(1.29423101296137,-2.95145450222513,10.0808522079338));
#13104=CARTESIAN_POINT('Ctrl Pts',(1.29439255882738,-2.95138365809453,10.080863050526));
#13105=CARTESIAN_POINT('Ctrl Pts',(1.29469349286324,-2.95125165738314,10.0808832501146));
#13106=CARTESIAN_POINT('Ctrl Pts',(1.2948328836109,-2.95119050371,10.0808926070677));
#13107=CARTESIAN_POINT('Ctrl Pts',(1.295092563856,-2.95107655454774,10.0809100399306));
#13108=CARTESIAN_POINT('Ctrl Pts',(1.29521285590914,-2.95102376094181,10.0809181158509));
#13109=CARTESIAN_POINT('Ctrl Pts',(1.29543697084459,-2.95092538535371,10.0809331628941));
#13110=CARTESIAN_POINT('Ctrl Pts',(1.295540796335,-2.95087980446283,10.0809401340724));
#13111=CARTESIAN_POINT('Ctrl Pts',(1.29573424476606,-2.95079486562865,10.0809531234767));
#13112=CARTESIAN_POINT('Ctrl Pts',(1.29582387043132,-2.95075550815367,10.0809591417965));
#13113=CARTESIAN_POINT('Ctrl Pts',(1.2960220916993,-2.95066845212975,10.0809724528357));
#13114=CARTESIAN_POINT('Ctrl Pts',(1.29613068892749,-2.95062075058619,10.0809797457865));
#13115=CARTESIAN_POINT('Ctrl Pts',(1.29634431710112,-2.95052689992457,10.0809940929456));
#13116=CARTESIAN_POINT('Ctrl Pts',(1.2964493422163,-2.95048075383071,10.0810011467376));
#13117=CARTESIAN_POINT('Ctrl Pts',(1.29665594485246,-2.95038996329112,10.0810150234768));
#13118=CARTESIAN_POINT('Ctrl Pts',(1.29675752329404,-2.95034531887204,10.0810218464629));
#13119=CARTESIAN_POINT('Ctrl Pts',(1.29695735535531,-2.95025747900218,10.0810352697684));
#13120=CARTESIAN_POINT('Ctrl Pts',(1.29705560995379,-2.9502142835234,10.081041870132));
#13121=CARTESIAN_POINT('Ctrl Pts',(1.29724891233806,-2.9501292908477,10.0810548560562));
#13122=CARTESIAN_POINT('Ctrl Pts',(1.29734396121599,-2.95008749354587,10.08106124167));
#13123=CARTESIAN_POINT('Ctrl Pts',(1.29753096570892,-2.95000524840497,10.0810738056633));
#13124=CARTESIAN_POINT('Ctrl Pts',(1.29762292249541,-2.94996480040091,10.0810799841027));
#13125=CARTESIAN_POINT('Ctrl Pts',(1.29780385200112,-2.94988520686447,10.0810921410283));
#13126=CARTESIAN_POINT('Ctrl Pts',(1.29789282598168,-2.94984606110413,10.0810981195817));
#13127=CARTESIAN_POINT('Ctrl Pts',(1.29806789489787,-2.9497690268191,10.08110988374));
#13128=CARTESIAN_POINT('Ctrl Pts',(1.29815399118848,-2.94973113800339,10.0811156694197));
#13129=CARTESIAN_POINT('Ctrl Pts',(1.29832340568559,-2.94965657408345,10.0811270545666));
#13130=CARTESIAN_POINT('Ctrl Pts',(1.29840672536958,-2.94961989861393,10.0811326541179));
#13131=CARTESIAN_POINT('Ctrl Pts',(1.29857068377375,-2.94954771948243,10.0811436734897));
#13132=CARTESIAN_POINT('Ctrl Pts',(1.2986513240798,-2.94951221538847,10.0811490934026));
#13133=CARTESIAN_POINT('Ctrl Pts',(1.29881001711054,-2.94944233868442,10.0811597597315));
#13134=CARTESIAN_POINT('Ctrl Pts',(1.29888807154065,-2.94940796557202,10.0811650062488));
#13135=CARTESIAN_POINT('Ctrl Pts',(1.29904167570169,-2.94934031507084,10.0811753313181));
#13136=CARTESIAN_POINT('Ctrl Pts',(1.29911722722685,-2.94930703712607,10.0811804099778));
#13137=CARTESIAN_POINT('Ctrl Pts',(1.29926594634109,-2.94924152445466,10.0811904074134));
#13138=CARTESIAN_POINT('Ctrl Pts',(1.29933909480496,-2.94920929837146,10.0811953248916));
#13139=CARTESIAN_POINT('Ctrl Pts',(1.29948306548533,-2.94914586465413,10.0812050038071));
#13140=CARTESIAN_POINT('Ctrl Pts',(1.29955388775872,-2.94911465719814,10.0812097652373));
#13141=CARTESIAN_POINT('Ctrl Pts',(1.29969328609028,-2.9490532260724,10.0812191374052));
#13142=CARTESIAN_POINT('Ctrl Pts',(1.29976186223343,-2.94902300255519,10.0812237481384));
#13143=CARTESIAN_POINT('Ctrl Pts',(1.29989684539823,-2.94896350589331,10.0812328240652));
#13144=CARTESIAN_POINT('Ctrl Pts',(1.29996325247529,-2.94893423290189,10.0812372892531));
#13145=CARTESIAN_POINT('Ctrl Pts',(1.31053599315781,-2.94427322257542,10.0819482194315));
#13146=CARTESIAN_POINT('Ctrl Pts',(1.32101738898217,-2.93958542163187,10.0826566095034));
#13147=CARTESIAN_POINT('Ctrl Pts',(1.34997829329839,-2.92644649388387,10.0846240648758));
#13148=CARTESIAN_POINT('Ctrl Pts',(1.36840301698019,-2.91787656122391,10.085887219836));
#13149=CARTESIAN_POINT('Ctrl Pts',(1.40932447906762,-2.89836984359615,10.0887188398179));
#13150=CARTESIAN_POINT('Ctrl Pts',(1.43177722100558,-2.88734431097182,10.0902903304164));
#13151=CARTESIAN_POINT('Ctrl Pts',(1.50089422166295,-2.85239963193541,10.0951842238588));
#13152=CARTESIAN_POINT('Ctrl Pts',(1.5471028852963,-2.82760309787463,10.0985366401983));
#13153=CARTESIAN_POINT('Ctrl Pts',(1.72753088496866,-2.72503477481736,10.1119515561755));
#13154=CARTESIAN_POINT('Ctrl Pts',(1.85665243310276,-2.63875145970691,10.1222935253476));
#13155=CARTESIAN_POINT('Ctrl Pts',(2.16011968383358,-2.4026312121583,10.1482487848494));
#13156=CARTESIAN_POINT('Ctrl Pts',(2.3256406485633,-2.24280275427979,10.1639655827974));
#13157=CARTESIAN_POINT('Ctrl Pts',(2.48806062547722,-2.04847230483622,10.1801720922222));
#13158=CARTESIAN_POINT('Ctrl Pts',(2.50312727316403,-2.0300340865497,10.18168352622));
#13159=CARTESIAN_POINT('Ctrl Pts',(2.52357143491082,-2.00444126482277,10.1837436631921));
#13160=CARTESIAN_POINT('Ctrl Pts',(2.52912512833821,-1.99742926306286,10.1843042646309));
#13161=CARTESIAN_POINT('Ctrl Pts',(2.53793182538466,-1.98621445334932,10.1851946475874));
#13162=CARTESIAN_POINT('Ctrl Pts',(2.54120370230815,-1.98202662680045,10.1855257592558));
#13163=CARTESIAN_POINT('Ctrl Pts',(2.54796579259157,-1.97332724534269,10.1862106997462));
#13164=CARTESIAN_POINT('Ctrl Pts',(2.55145439373001,-1.96881450995197,10.1865644059782));
#13165=CARTESIAN_POINT('Ctrl Pts',(2.55978618690903,-1.95797744943358,10.1874100381803));
#13166=CARTESIAN_POINT('Ctrl Pts',(2.5646179885906,-1.95164433003633,10.1879011594503));
#13167=CARTESIAN_POINT('Ctrl Pts',(2.58106097379721,-1.92992573399434,10.1895752034502));
#13168=CARTESIAN_POINT('Ctrl Pts',(2.59255785367073,-1.9144536835358,10.190750371415));
#13169=CARTESIAN_POINT('Ctrl Pts',(2.65717830536732,-1.82584024347576,10.1973884656028));
#13170=CARTESIAN_POINT('Ctrl Pts',(2.70734958682327,-1.75058573944091,10.2026711360758));
#13171=CARTESIAN_POINT('Ctrl Pts',(2.87096015946836,-1.4812809114951,10.2207385517243));
#13172=CARTESIAN_POINT('Ctrl Pts',(2.967227057881,-1.27756751748756,10.2330013144909));
#13173=CARTESIAN_POINT('Ctrl Pts',(3.0626547173377,-1.0051614243851,10.2493761674999));
#13174=CARTESIAN_POINT('Ctrl Pts',(3.08198754169092,-0.944222232435921,
10.2530344534341));
#13175=CARTESIAN_POINT('Ctrl Pts',(3.12384792697356,-0.79724294937789,10.2618960329593));
#13176=CARTESIAN_POINT('Ctrl Pts',(3.14465021461784,-0.710770771948116,
10.2671409765452));
#13177=CARTESIAN_POINT('Ctrl Pts',(3.16550237738691,-0.605035981498551,
10.2736405024501));
#13178=CARTESIAN_POINT('Ctrl Pts',(3.1689916486619,-0.58648593119685,10.2747838858624));
#13179=CARTESIAN_POINT('Ctrl Pts',(3.17448854200507,-0.555780367741568,
10.2766820884816));
#13180=CARTESIAN_POINT('Ctrl Pts',(3.17658980230377,-0.54364192420868,10.2774339163744));
#13181=CARTESIAN_POINT('Ctrl Pts',(3.18026428772516,-0.521666426952067,
10.2787977427621));
#13182=CARTESIAN_POINT('Ctrl Pts',(3.18186160126185,-0.511833515568684,
10.2794089653726));
#13183=CARTESIAN_POINT('Ctrl Pts',(3.18487368151964,-0.492732277424092,
10.2805982778261));
#13184=CARTESIAN_POINT('Ctrl Pts',(3.18629364442625,-0.483464862181792,
10.2811761955267));
#13185=CARTESIAN_POINT('Ctrl Pts',(3.18931846284915,-0.463131023994156,
10.2824462302536));
#13186=CARTESIAN_POINT('Ctrl Pts',(3.19090619623556,-0.452062213202765,
10.2831388841888));
#13187=CARTESIAN_POINT('Ctrl Pts',(3.19466754877879,-0.424832567341122,
10.2848461302208));
#13188=CARTESIAN_POINT('Ctrl Pts',(3.19677616163418,-0.408663203765155,
10.2858627665606));
#13189=CARTESIAN_POINT('Ctrl Pts',(3.21484596686634,-0.26139153043618,10.2951490927864));
#13190=CARTESIAN_POINT('Ctrl Pts',(3.22285444874402,-0.129459657241155,
10.303668699674));
#13191=CARTESIAN_POINT('Ctrl Pts',(3.22274897165249,0.002574531576424,10.3123883511433));
#13192=CARTESIAN_POINT('Ctrl Pts',(3.219554665156,0.0024747518059529,10.314228031951));
#13193=CARTESIAN_POINT('Ctrl Pts',(3.22212746863257,0.36848297700967,10.3367720053601));
#13194=CARTESIAN_POINT('Ctrl Pts',(2.99522905709534,1.80797061601092,10.4256269582238));
#13195=CARTESIAN_POINT('Ctrl Pts',(0.872388983325508,3.71103042484282,10.5807928905419));
#13196=CARTESIAN_POINT('Ctrl Pts',(-2.65122281047819,2.7393115444244,10.7797258289053));
#13197=CARTESIAN_POINT('Ctrl Pts',(-3.70009722952212,-0.630335825586912,
10.9717996371069));
#13198=CARTESIAN_POINT('Ctrl Pts',(-2.32704138798567,-2.42295171699722,
11.0975624658541));
#13199=CARTESIAN_POINT('Ctrl Pts',(-1.47708659324034,-2.8687591534968,11.1570143151468));
#13200=CARTESIAN_POINT('Origin',(0.,0.,4.68922655072688));
#13201=CARTESIAN_POINT('',(-1.47525540501257,-2.86526422036105,12.6567692800014));
#13202=CARTESIAN_POINT('',(-1.47525514217501,-2.86526435568975,12.4082778759135));
#13203=CARTESIAN_POINT('',(-1.47525540501186,-2.86526422036142,4.68922655072688));
#13204=CARTESIAN_POINT('Ctrl Pts',(-1.47525540501245,-2.86526422036111,
12.6567692800014));
#13205=CARTESIAN_POINT('Ctrl Pts',(-1.47619473560958,-2.86478058170375,
12.6567037974063));
#13206=CARTESIAN_POINT('Ctrl Pts',(-1.47713382808388,-2.86429648128078,
12.6566382984126));
#13207=CARTESIAN_POINT('Ctrl Pts',(-1.4975799459372,-2.85374381612472,12.6552115211502));
#13208=CARTESIAN_POINT('Ctrl Pts',(-1.51698342780398,-2.84347686886961,
12.6538432292352));
#13209=CARTESIAN_POINT('Ctrl Pts',(-1.68039354959082,-2.75486317396149,
12.6421964820092));
#13210=CARTESIAN_POINT('Ctrl Pts',(-1.81831116618325,-2.66584384159589,
12.6315304384339));
#13211=CARTESIAN_POINT('Ctrl Pts',(-2.1515527384478,-2.41282365798401,12.6036225825653));
#13212=CARTESIAN_POINT('Ctrl Pts',(-2.33530593020492,-2.23545044242906,
12.5860524973474));
#13213=CARTESIAN_POINT('Ctrl Pts',(-2.53151275203996,-1.99516025806213,
12.5657648530545));
#13214=CARTESIAN_POINT('Ctrl Pts',(-2.56562630930633,-1.951098100943,12.5621731041873));
#13215=CARTESIAN_POINT('Ctrl Pts',(-2.6054651856129,-1.89678784670337,12.5579198844388));
#13216=CARTESIAN_POINT('Ctrl Pts',(-2.61229707577267,-1.88736773483683,
12.5571883220117));
#13217=CARTESIAN_POINT('Ctrl Pts',(-2.62286474518232,-1.87262925435896,
12.5560535643887));
#13218=CARTESIAN_POINT('Ctrl Pts',(-2.62663563143923,-1.86733635353298,
12.5556480078588));
#13219=CARTESIAN_POINT('Ctrl Pts',(-2.63361678649892,-1.85747445866487,
12.5548960529092));
#13220=CARTESIAN_POINT('Ctrl Pts',(-2.63683115968704,-1.85290857268435,
12.5545493794605));
#13221=CARTESIAN_POINT('Ctrl Pts',(-2.64409878612255,-1.842527994079,12.5537645176564));
#13222=CARTESIAN_POINT('Ctrl Pts',(-2.64814472457018,-1.83670828378848,
12.5533268314023));
#13223=CARTESIAN_POINT('Ctrl Pts',(-2.66011531209191,-1.8193679152882,12.5520294757472));
#13224=CARTESIAN_POINT('Ctrl Pts',(-2.66798433904022,-1.80780880290746,
12.5511735010759));
#13225=CARTESIAN_POINT('Ctrl Pts',(-2.72795358574787,-1.71847325060117,
12.5446227544761));
#13226=CARTESIAN_POINT('Ctrl Pts',(-2.77672318446368,-1.63850327925736,
12.5391336918004));
#13227=CARTESIAN_POINT('Ctrl Pts',(-2.9382653934292,-1.34562900287555,12.5199186546022));
#13228=CARTESIAN_POINT('Ctrl Pts',(-3.03058341738554,-1.12236245184774,
12.5068195674281));
#13229=CARTESIAN_POINT('Ctrl Pts',(-3.12262260647631,-0.802387216530855,
12.4878659580322));
#13230=CARTESIAN_POINT('Ctrl Pts',(-3.1442718616317,-0.712846203559643,
12.4825512437766));
#13231=CARTESIAN_POINT('Ctrl Pts',(-3.17290627152424,-0.567395950289029,
12.4738102345405));
#13232=CARTESIAN_POINT('Ctrl Pts',(-3.18231250173899,-0.512014584879206,
12.4704577296295));
#13233=CARTESIAN_POINT('Ctrl Pts',(-3.19270011637933,-0.439407349369612,
12.46601935475));
#13234=CARTESIAN_POINT('Ctrl Pts',(-3.19499764675104,-0.422377640592802,
12.4649752972422));
#13235=CARTESIAN_POINT('Ctrl Pts',(-3.19852388336614,-0.394563461531825,
12.4632647663584));
#13236=CARTESIAN_POINT('Ctrl Pts',(-3.19983451341419,-0.383789577562793,
12.4626008946562));
#13237=CARTESIAN_POINT('Ctrl Pts',(-3.20225760785037,-0.36299507371952,
12.4613169884182));
#13238=CARTESIAN_POINT('Ctrl Pts',(-3.20337752189715,-0.352975436960663,
12.4606971976679));
#13239=CARTESIAN_POINT('Ctrl Pts',(-3.20584381149837,-0.329931015790019,
12.4592690045522));
#13240=CARTESIAN_POINT('Ctrl Pts',(-3.20715785209024,-0.316903017568776,
12.4584595903064));
#13241=CARTESIAN_POINT('Ctrl Pts',(-3.21045735552717,-0.28206513262069,
12.4562896616383));
#13242=CARTESIAN_POINT('Ctrl Pts',(-3.21229993402519,-0.260242706565,12.4549246709453));
#13243=CARTESIAN_POINT('Ctrl Pts',(-3.22601025526251,-0.0754138263689908,
12.4433131278362));
#13244=CARTESIAN_POINT('Ctrl Pts',(-3.22568281614904,0.0882338028203065,
12.432681411931));
#13245=CARTESIAN_POINT('Ctrl Pts',(-3.19320935247579,0.503698484376278,
12.4048899543915));
#13246=CARTESIAN_POINT('Ctrl Pts',(-3.14375836722508,0.753044771747766,
12.3874046746089));
#13247=CARTESIAN_POINT('Ctrl Pts',(-3.04794466935143,1.04853968504443,12.3670714471105));
#13248=CARTESIAN_POINT('Ctrl Pts',(-3.02881508240208,1.10257985535222,12.3633739565753));
#13249=CARTESIAN_POINT('Ctrl Pts',(-3.00404406329149,1.16703662579351,12.3590129911835));
#13250=CARTESIAN_POINT('Ctrl Pts',(-2.99977536298582,1.1779656199368,12.3582753006768));
#13251=CARTESIAN_POINT('Ctrl Pts',(-2.99304187570814,1.19493112747953,12.3571331322803));
#13252=CARTESIAN_POINT('Ctrl Pts',(-2.99061834716971,1.20098375198059,12.3567262438932));
#13253=CARTESIAN_POINT('Ctrl Pts',(-2.98608589129861,1.21220450754753,12.355973084361));
#13254=CARTESIAN_POINT('Ctrl Pts',(-2.98398192495134,1.21737446606616,12.3556265302511));
#13255=CARTESIAN_POINT('Ctrl Pts',(-2.9791866317673,1.22907054591091,12.3548435446411));
#13256=CARTESIAN_POINT('Ctrl Pts',(-2.97648729489427,1.23559329040738,12.354407605262));
#13257=CARTESIAN_POINT('Ctrl Pts',(-2.96842909111313,1.25488568068073,12.35312021111));
#13258=CARTESIAN_POINT('Ctrl Pts',(-2.96300924376663,1.26762990571747,12.3522723675196));
#13259=CARTESIAN_POINT('Ctrl Pts',(-2.92189854131814,1.36259319028294,12.3459712062301));
#13260=CARTESIAN_POINT('Ctrl Pts',(-2.88287017405998,1.44333433988521,12.3407063022715));
#13261=CARTESIAN_POINT('Ctrl Pts',(-2.72438795711605,1.73904303105259,12.3213950129442));
#13262=CARTESIAN_POINT('Ctrl Pts',(-2.5838362598838,1.94174269989726,12.3080392414193));
#13263=CARTESIAN_POINT('Ctrl Pts',(-2.36117702484197,2.1953005865531,12.2888250595191));
#13264=CARTESIAN_POINT('Ctrl Pts',(-2.2978584671852,2.26149202112921,12.2835391186751));
#13265=CARTESIAN_POINT('Ctrl Pts',(-2.19145583701924,2.36363453417611,12.2748411232642));
#13266=CARTESIAN_POINT('Ctrl Pts',(-2.1501005301157,2.40131506376535,12.2715019115213));
#13267=CARTESIAN_POINT('Ctrl Pts',(-2.09480720218862,2.44912122587711,12.2670786910635));
#13268=CARTESIAN_POINT('Ctrl Pts',(-2.08173780063864,2.4602397657669,12.2660361330823));
#13269=CARTESIAN_POINT('Ctrl Pts',(-2.06026213679578,2.47821612573831,12.2643274419006));
#13270=CARTESIAN_POINT('Ctrl Pts',(-2.05190882681644,2.48513689765095,12.2636638995881));
#13271=CARTESIAN_POINT('Ctrl Pts',(-2.03572324384206,2.49840951910628,12.262380196543));
#13272=CARTESIAN_POINT('Ctrl Pts',(-2.02789577634355,2.50476704850547,12.2617602772615));
#13273=CARTESIAN_POINT('Ctrl Pts',(-2.00982616691826,2.51930310397465,12.2603311655412));
#13274=CARTESIAN_POINT('Ctrl Pts',(-1.99956376451013,2.52745605192764,12.2595209569638));
#13275=CARTESIAN_POINT('Ctrl Pts',(-1.97198773956722,2.54909070658342,12.2573475126865));
#13276=CARTESIAN_POINT('Ctrl Pts',(-1.95458591469057,2.56245837800697,12.2559797778881));
#13277=CARTESIAN_POINT('Ctrl Pts',(-1.80467832633018,2.67519835414471,12.2442278728856));
#13278=CARTESIAN_POINT('Ctrl Pts',(-1.6648512892947,2.76438151077136,12.2334476854209));
#13279=CARTESIAN_POINT('Ctrl Pts',(-1.29083593980754,2.96423203106929,12.2051509434149));
#13280=CARTESIAN_POINT('Ctrl Pts',(-1.04904592999842,3.05817394012085,12.187296163694));
#13281=CARTESIAN_POINT('Ctrl Pts',(-0.749541532113809,3.13478437267555,
12.1671374364729));
#13282=CARTESIAN_POINT('Ctrl Pts',(-0.700153944727436,3.14618351464393,
12.163877541682));
#13283=CARTESIAN_POINT('Ctrl Pts',(-0.639437277930541,3.15869679714524,
12.159964678851));
#13284=CARTESIAN_POINT('Ctrl Pts',(-0.628347505382622,3.16092152862965,
12.1592538474349));
#13285=CARTESIAN_POINT('Ctrl Pts',(-0.610937743852355,3.16431887549834,
12.158144188094));
#13286=CARTESIAN_POINT('Ctrl Pts',(-0.604625696057268,3.16553102055254,
12.15774316197));
#13287=CARTESIAN_POINT('Ctrl Pts',(-0.592814117609411,3.16776265957437,
12.1569951968635));
#13288=CARTESIAN_POINT('Ctrl Pts',(-0.58731562099644,3.16878670903568,12.1566480101098));
#13289=CARTESIAN_POINT('Ctrl Pts',(-0.574740844954814,3.17109480209489,
12.1558562773945));
#13290=CARTESIAN_POINT('Ctrl Pts',(-0.567662927653378,3.17236947496112,
12.1554122695709));
#13291=CARTESIAN_POINT('Ctrl Pts',(-0.549150758582309,3.17563942019839,
12.1542550977663));
#13292=CARTESIAN_POINT('Ctrl Pts',(-0.537709771102787,3.17759665380526,
12.1535440422503));
#13293=CARTESIAN_POINT('Ctrl Pts',(-0.461739817088373,3.19017093136881,
12.1488482415702));
#13294=CARTESIAN_POINT('Ctrl Pts',(-0.396906115463345,3.19888435396724,
12.1449636675359));
#13295=CARTESIAN_POINT('Ctrl Pts',(-0.300698357953886,3.20884382804193,
12.1393211295345));
#13296=CARTESIAN_POINT('Ctrl Pts',(-0.269503260280589,3.21161428437234,
12.1375103865045));
#13297=CARTESIAN_POINT('Ctrl Pts',(0.000726964663289101,3.23164841284286,
12.1219505056869));
#13298=CARTESIAN_POINT('Ctrl Pts',(0.240963267835843,3.22265429209174,12.1089121721284));
#13299=CARTESIAN_POINT('Ctrl Pts',(0.569158991719774,3.17343251751868,12.0900211238264));
#13300=CARTESIAN_POINT('Ctrl Pts',(0.659691103190586,3.15585513074762,12.084700796398));
#13301=CARTESIAN_POINT('Ctrl Pts',(0.804012032936248,3.12135259113154,12.0759513989263));
#13302=CARTESIAN_POINT('Ctrl Pts',(0.858329324728526,3.10685492706569,12.072596304542));
#13303=CARTESIAN_POINT('Ctrl Pts',(0.928723213883803,3.08607942392808,12.0681549780869));
#13304=CARTESIAN_POINT('Ctrl Pts',(0.945169616767288,3.08108217945138,12.0671106291311));
#13305=CARTESIAN_POINT('Ctrl Pts',(0.971935010736505,3.07271503979346,12.0653997406673));
#13306=CARTESIAN_POINT('Ctrl Pts',(0.982278478991355,3.06942410983237,12.0647358049315));
#13307=CARTESIAN_POINT('Ctrl Pts',(1.00219660347124,3.06297586846961,12.0634518590359));
#13308=CARTESIAN_POINT('Ctrl Pts',(1.01177346955445,3.05982575410037,12.0628320931146));
#13309=CARTESIAN_POINT('Ctrl Pts',(1.03375217201273,3.05248184294397,12.0614040778255));
#13310=CARTESIAN_POINT('Ctrl Pts',(1.04614348650381,3.04825733037083,12.0605948174016));
#13311=CARTESIAN_POINT('Ctrl Pts',(1.07918561683694,3.03676722961454,12.0584255693009));
#13312=CARTESIAN_POINT('Ctrl Pts',(1.09978843666799,3.02936662667686,12.0570611097661));
#13313=CARTESIAN_POINT('Ctrl Pts',(1.27316639549322,2.96508689136535,12.0454763652371));
#13314=CARTESIAN_POINT('Ctrl Pts',(1.42147478806425,2.89691006061307,12.0348729697757));
#13315=CARTESIAN_POINT('Ctrl Pts',(1.78477905815851,2.69526553319872,12.0071659596091));
#13316=CARTESIAN_POINT('Ctrl Pts',(1.99040382436097,2.54719059929882,11.9897383267371));
#13317=CARTESIAN_POINT('Ctrl Pts',(2.21971949049879,2.33717282794068,11.9693720511778));
#13318=CARTESIAN_POINT('Ctrl Pts',(2.26173002654632,2.29654299902525,11.9656007074992));
#13319=CARTESIAN_POINT('Ctrl Pts',(2.31086992280861,2.24636082509433,11.9611646799951));
#13320=CARTESIAN_POINT('Ctrl Pts',(2.31907820923738,2.23788583852116,11.9604228354107));
#13321=CARTESIAN_POINT('Ctrl Pts',(2.33175981210671,2.22464748515599,11.9592756456731));
#13322=CARTESIAN_POINT('Ctrl Pts',(2.33626539486858,2.21991537250976,11.9588678564516));
#13323=CARTESIAN_POINT('Ctrl Pts',(2.34459230272368,2.21111637803907,11.9581138745836));
#13324=CARTESIAN_POINT('Ctrl Pts',(2.34841742212452,2.20705331051225,11.9577673936231));
#13325=CARTESIAN_POINT('Ctrl Pts',(2.35704450910685,2.19784173868495,11.9569856426085));
#13326=CARTESIAN_POINT('Ctrl Pts',(2.36184015894349,2.19268743601107,11.9565508580707));
#13327=CARTESIAN_POINT('Ctrl Pts',(2.37595871242727,2.17741293535599,11.9552700294249));
#13328=CARTESIAN_POINT('Ctrl Pts',(2.3852338759679,2.16724854754257,11.9544275419528));
#13329=CARTESIAN_POINT('Ctrl Pts',(2.45281227276223,2.09223194503135,11.9482787120151));
#13330=CARTESIAN_POINT('Ctrl Pts',(2.50853253827676,2.02509012289934,11.9431506280972));
#13331=CARTESIAN_POINT('Ctrl Pts',(2.71463763954851,1.75515419583803,11.9235782660041));
#13332=CARTESIAN_POINT('Ctrl Pts',(2.84371913698329,1.53723809334595,11.9098871789854));
#13333=CARTESIAN_POINT('Ctrl Pts',(2.98212971547954,1.22512832159454,11.8904224790711));
#13334=CARTESIAN_POINT('Ctrl Pts',(3.01481884032023,1.14232334457073,11.8852789515334));
#13335=CARTESIAN_POINT('Ctrl Pts',(3.0620359497016,1.00650748598984,11.8767942322024));
#13336=CARTESIAN_POINT('Ctrl Pts',(3.07870920263555,0.954290617893719,11.8735212953733));
#13337=CARTESIAN_POINT('Ctrl Pts',(3.09880782422475,0.885323530008186,11.8691736898158));
#13338=CARTESIAN_POINT('Ctrl Pts',(3.10344359717685,0.868933545257085,11.8681386927785));
#13339=CARTESIAN_POINT('Ctrl Pts',(3.11081138333749,0.842073140956572,11.8664392755297));
#13340=CARTESIAN_POINT('Ctrl Pts',(3.11362101128111,0.831624212619681,11.8657773920793));
#13341=CARTESIAN_POINT('Ctrl Pts',(3.11895001043523,0.81140020460836,11.864494691062));
#13342=CARTESIAN_POINT('Ctrl Pts',(3.12147618158367,0.801627035308575,11.8638741031005));
#13343=CARTESIAN_POINT('Ctrl Pts',(3.12719276372811,0.779074117363573,11.8624402634746));
#13344=CARTESIAN_POINT('Ctrl Pts',(3.13035080679509,0.766286421630827,11.8616259737636));
#13345=CARTESIAN_POINT('Ctrl Pts',(3.138613002571,0.731927156483886,11.859434436022));
#13346=CARTESIAN_POINT('Ctrl Pts',(3.14357305888789,0.710321987610526,11.8580525705126));
#13347=CARTESIAN_POINT('Ctrl Pts',(3.19391146281884,0.480195229483713,11.8432906800071));
#13348=CARTESIAN_POINT('Ctrl Pts',(3.21868566259682,0.267748686197534,11.8292345209011));
#13349=CARTESIAN_POINT('Ctrl Pts',(3.22261353595994,0.0353028390036726,
11.8135680300132));
#13350=CARTESIAN_POINT('Ctrl Pts',(3.2227664150345,0.0161529798790844,11.8122756787049));
#13351=CARTESIAN_POINT('Ctrl Pts',(3.22254099906837,-0.226242497291643,
11.7959007038741));
#13352=CARTESIAN_POINT('Ctrl Pts',(3.1991374061631,-0.448877816708697,11.7806320218433));
#13353=CARTESIAN_POINT('Ctrl Pts',(3.1480726137505,-0.690145486886651,11.764858078822));
#13354=CARTESIAN_POINT('Ctrl Pts',(3.14299331856508,-0.712920085269498,
11.7633773627682));
#13355=CARTESIAN_POINT('Ctrl Pts',(3.13564137771531,-0.744277809341747,
11.7613519358791));
#13356=CARTESIAN_POINT('Ctrl Pts',(3.13358010042799,-0.752909068696944,
11.7607958347463));
#13357=CARTESIAN_POINT('Ctrl Pts',(3.13023035094593,-0.766683521448196,
11.7599107255696));
#13358=CARTESIAN_POINT('Ctrl Pts',(3.12896481019171,-0.771832164136228,
11.759580415868));
#13359=CARTESIAN_POINT('Ctrl Pts',(3.12630836422833,-0.782525560207517,
11.7588955164548));
#13360=CARTESIAN_POINT('Ctrl Pts',(3.12491540876568,-0.788069748923611,
11.7585410562112));
#13361=CARTESIAN_POINT('Ctrl Pts',(3.12153118564186,-0.801389444844727,
11.7576909561421));
#13362=CARTESIAN_POINT('Ctrl Pts',(3.11952559033726,-0.809161343447773,
11.7571961423366));
#13363=CARTESIAN_POINT('Ctrl Pts',(3.11251466974097,-0.835915893804152,
11.7554966773848));
#13364=CARTESIAN_POINT('Ctrl Pts',(3.10736482867215,-0.85486070006757,11.7543001003763));
#13365=CARTESIAN_POINT('Ctrl Pts',(3.07666862674289,-0.963839308073972,
11.7474499560186));
#13366=CARTESIAN_POINT('Ctrl Pts',(3.04738083677664,-1.0527817682856,11.7419894428558));
#13367=CARTESIAN_POINT('Ctrl Pts',(2.9845001477277,-1.21899556925063,11.7318161141954));
#13368=CARTESIAN_POINT('Ctrl Pts',(2.95167120000717,-1.29646808977821,11.7270875533678));
#13369=CARTESIAN_POINT('Ctrl Pts',(2.80218367048182,-1.61403504874381,11.7074393911293));
#13370=CARTESIAN_POINT('Ctrl Pts',(2.65898297315646,-1.84041729271843,11.6926777492949));
#13371=CARTESIAN_POINT('Ctrl Pts',(2.46713354274841,-2.0737919083236,11.6746529493628));
#13372=CARTESIAN_POINT('Ctrl Pts',(2.44429777212406,-2.10065919405715,11.6725322964045));
#13373=CARTESIAN_POINT('Ctrl Pts',(2.4112476918558,-2.13827538603683,11.6694948567551));
#13374=CARTESIAN_POINT('Ctrl Pts',(2.4013924394172,-2.14933743243355,11.6685929998813));
#13375=CARTESIAN_POINT('Ctrl Pts',(2.38521729708612,-2.16724312769131,11.6671188837575));
#13376=CARTESIAN_POINT('Ctrl Pts',(2.37894331894642,-2.17412810367687,11.6665485705697));
#13377=CARTESIAN_POINT('Ctrl Pts',(2.36571586682559,-2.18851791684877,11.665349176972));
#13378=CARTESIAN_POINT('Ctrl Pts',(2.35875633798489,-2.19601702385896,11.6647198411901));
#13379=CARTESIAN_POINT('Ctrl Pts',(2.34205336716119,-2.213843984046,11.6632134260617));
#13380=CARTESIAN_POINT('Ctrl Pts',(2.33227721300811,-2.22414076704486,11.6623349393322));
#13381=CARTESIAN_POINT('Ctrl Pts',(2.29879923042876,-2.25893818223412,11.6593371834228));
#13382=CARTESIAN_POINT('Ctrl Pts',(2.27477749051116,-2.28312654872859,11.6572039594849));
#13383=CARTESIAN_POINT('Ctrl Pts',(2.13926184564403,-2.41532020771901,11.6452626633037));
#13384=CARTESIAN_POINT('Ctrl Pts',(2.02047668968535,-2.51552672605947,11.6351228598179));
#13385=CARTESIAN_POINT('Ctrl Pts',(1.75035522967044,-2.71188684810519,11.6128154184088));
#13386=CARTESIAN_POINT('Ctrl Pts',(1.59726605259747,-2.80478357669678,11.6006070194257));
#13387=CARTESIAN_POINT('Ctrl Pts',(1.41021681310188,-2.89798551556075,11.5865839363803));
#13388=CARTESIAN_POINT('Ctrl Pts',(1.38296933931043,-2.91108697683825,11.5845627609746));
#13389=CARTESIAN_POINT('Ctrl Pts',(1.2729104100378,-2.96211277361997,11.5764946069882));
#13390=CARTESIAN_POINT('Ctrl Pts',(1.18868419553505,-2.99690610548107,11.5705346805874));
#13391=CARTESIAN_POINT('Ctrl Pts',(1.09002983869993,-3.03284448870427,11.5638843011003));
#13392=CARTESIAN_POINT('Ctrl Pts',(1.07693955213573,-3.03751740066594,11.5630084620682));
#13393=CARTESIAN_POINT('Ctrl Pts',(1.05714554495973,-3.04443933146092,11.5616944506215));
#13394=CARTESIAN_POINT('Ctrl Pts',(1.05046418339184,-3.04675114636058,11.5612526852176));
#13395=CARTESIAN_POINT('Ctrl Pts',(1.03849360151569,-3.05084902385153,11.5604644386424));
#13396=CARTESIAN_POINT('Ctrl Pts',(1.03320731760689,-3.0526433409642,11.5601174745965));
#13397=CARTESIAN_POINT('Ctrl Pts',(1.02174463003235,-3.05650092039963,11.5593675799754));
#13398=CARTESIAN_POINT('Ctrl Pts',(1.01556664603151,-3.05855919587052,11.5589649457553));
#13399=CARTESIAN_POINT('Ctrl Pts',(0.998274687096857,-3.06426206659673,
11.5578421564981));
#13400=CARTESIAN_POINT('Ctrl Pts',(0.987146913883587,-3.06786494876582,
11.5571244217848));
#13401=CARTESIAN_POINT('Ctrl Pts',(0.921964360582787,-3.08857797685089,
11.5529468920375));
#13402=CARTESIAN_POINT('Ctrl Pts',(0.867481545450114,-3.10432100163293,
11.5495621983289));
#13403=CARTESIAN_POINT('Ctrl Pts',(0.567053143084973,-3.182602603636,11.5313372259335));
#13404=CARTESIAN_POINT('Ctrl Pts',(0.314778572355372,-3.2173669450883,11.5175662244789));
#13405=CARTESIAN_POINT('Ctrl Pts',(-0.102609078521045,-3.22527084468108,
11.4939847295924));
#13406=CARTESIAN_POINT('Ctrl Pts',(-0.266212305677577,-3.21590131087481,
11.4845535338796));
#13407=CARTESIAN_POINT('Ctrl Pts',(-0.450094124506783,-3.19123998684728,
11.4733945641864));
#13408=CARTESIAN_POINT('Ctrl Pts',(-0.471773684566638,-3.18810710749064,
11.4720703297883));
#13409=CARTESIAN_POINT('Ctrl Pts',(-0.506360322041596,-3.18274854156049,
11.4699432452501));
#13410=CARTESIAN_POINT('Ctrl Pts',(-0.519288928402661,-3.18066471911724,
11.4691448956423));
#13411=CARTESIAN_POINT('Ctrl Pts',(-0.542148179714665,-3.17683719540533,
11.4677274422646));
#13412=CARTESIAN_POINT('Ctrl Pts',(-0.552084072998699,-3.17512557035948,
11.4671093675229));
#13413=CARTESIAN_POINT('Ctrl Pts',(-0.572698137509648,-3.1714747654765,
11.4658228781847));
#13414=CARTESIAN_POINT('Ctrl Pts',(-0.583374858295766,-3.16952821644742,
11.4651542353869));
#13415=CARTESIAN_POINT('Ctrl Pts',(-0.610928330344991,-3.16436080979207,
11.4634225537547));
#13416=CARTESIAN_POINT('Ctrl Pts',(-0.627789354657151,-3.16105888384223,
11.4623569345819));
#13417=CARTESIAN_POINT('Ctrl Pts',(-0.699631712380283,-3.14639239597509,
11.4577905759502));
#13418=CARTESIAN_POINT('Ctrl Pts',(-0.754334652233257,-3.13372753045579,
11.4542484334825));
#13419=CARTESIAN_POINT('Ctrl Pts',(-0.89776193465971,-3.0965481762599,11.4447821297314));
#13420=CARTESIAN_POINT('Ctrl Pts',(-0.985810180822148,-3.06965191144472,
11.4387861534985));
#13421=CARTESIAN_POINT('Ctrl Pts',(-1.21070675631613,-2.9902779126194,11.423008239846));
#13422=CARTESIAN_POINT('Ctrl Pts',(-1.34523599042925,-2.93220808941505,
11.4131044842263));
#13423=CARTESIAN_POINT('Ctrl Pts',(-1.47525557920443,-2.86526413067386,
11.4032056183244));
#13424=CARTESIAN_POINT('',(3.22749356206024,0.00107973417029931,11.5643095400564));
#13425=CARTESIAN_POINT('Ctrl Pts',(-1.47708659324034,-2.8687591534968,11.1570143151468));
#13426=CARTESIAN_POINT('Ctrl Pts',(-1.37902487374519,-2.92019323452928,
11.1638734453086));
#13427=CARTESIAN_POINT('Ctrl Pts',(-0.304424137651661,-3.4118415492434,
11.2370435549249));
#13428=CARTESIAN_POINT('Ctrl Pts',(2.16938213632706,-3.09513680703482,11.3727804995698));
#13429=CARTESIAN_POINT('Ctrl Pts',(3.22315092886655,-1.00817079531109,11.5016583140529));
#13430=CARTESIAN_POINT('Ctrl Pts',(3.22764049557943,0.00108461746384235,
11.5642251490816));
#13431=CARTESIAN_POINT('Ctrl Pts',(3.22274986808945,0.000922078856079595,
11.5670340712653));
#13432=CARTESIAN_POINT('Ctrl Pts',(3.22274249037896,0.0267078512451821,
11.5687062102123));
#13433=CARTESIAN_POINT('Ctrl Pts',(3.22242563788659,0.052493591020987,11.5703659999436));
#13434=CARTESIAN_POINT('Ctrl Pts',(3.22138428404907,0.0953564309527305,
11.5731015027928));
#13435=CARTESIAN_POINT('Ctrl Pts',(3.2208333897793,0.112436021340087,11.5741853081487));
#13436=CARTESIAN_POINT('Ctrl Pts',(3.21984681431238,0.136966150523044,11.5757321982439));
#13437=CARTESIAN_POINT('Ctrl Pts',(3.21952107635683,0.144420481582638,11.5762009870684));
#13438=CARTESIAN_POINT('Ctrl Pts',(3.21890592421196,0.157459467209442,11.5770186525729));
#13439=CARTESIAN_POINT('Ctrl Pts',(3.21862785916603,0.163044589177729,11.5773681428694));
#13440=CARTESIAN_POINT('Ctrl Pts',(3.21805643252585,0.173950438145847,11.5780490791059));
#13441=CARTESIAN_POINT('Ctrl Pts',(3.21776440807274,0.179271229269288,11.5783805987438));
#13442=CARTESIAN_POINT('Ctrl Pts',(3.21715365382935,0.189916780604091,11.579042460404));
#13443=CARTESIAN_POINT('Ctrl Pts',(3.2168349014236,0.195241475791694,11.5793728015094));
#13444=CARTESIAN_POINT('Ctrl Pts',(3.21603427612127,0.208081245841575,11.5801677160106));
#13445=CARTESIAN_POINT('Ctrl Pts',(3.21553927782859,0.215595513574288,11.5806315568701));
#13446=CARTESIAN_POINT('Ctrl Pts',(3.21361722643613,0.243292538737717,11.5823364140497));
#13447=CARTESIAN_POINT('Ctrl Pts',(3.21202642019436,0.263463966103473,11.5835685920823));
#13448=CARTESIAN_POINT('Ctrl Pts',(3.20668281311921,0.323947402387177,11.5872384421211));
#13449=CARTESIAN_POINT('Ctrl Pts',(3.20236015899617,0.36420641922359,11.5896480693079));
#13450=CARTESIAN_POINT('Ctrl Pts',(3.16096800382506,0.691482425800945,11.6090436302363));
#13451=CARTESIAN_POINT('Ctrl Pts',(3.08614843790116,0.972415922668809,11.6245891255178));
#13452=CARTESIAN_POINT('Ctrl Pts',(2.94058238012473,1.32174546642264,11.6461645806989));
#13453=CARTESIAN_POINT('Ctrl Pts',(2.90297014836683,1.40242588019415,11.6513077463558));
#13454=CARTESIAN_POINT('Ctrl Pts',(2.83687897755517,1.53011057963693,11.6597917030701));
#13455=CARTESIAN_POINT('Ctrl Pts',(2.81045184794963,1.57812565752283,11.6630642441681));
#13456=CARTESIAN_POINT('Ctrl Pts',(2.77422603063957,1.64014556145109,11.6674111758868));
#13457=CARTESIAN_POINT('Ctrl Pts',(2.76552118869172,1.65478097324236,11.6684459035223));
#13458=CARTESIAN_POINT('Ctrl Pts',(2.75109799803448,1.67859892997589,11.6701448387876));
#13459=CARTESIAN_POINT('Ctrl Pts',(2.74544860766733,1.68782300631652,11.670806510797));
#13460=CARTESIAN_POINT('Ctrl Pts',(2.73443942089812,1.70559679840141,11.6720887731784));
#13461=CARTESIAN_POINT('Ctrl Pts',(2.7290856884291,1.71415013542971,11.6727091339611));
#13462=CARTESIAN_POINT('Ctrl Pts',(2.71665398157593,1.73380565860496,11.6741424056968));
#13463=CARTESIAN_POINT('Ctrl Pts',(2.70954800068266,1.74488983639341,11.6749563536819));
#13464=CARTESIAN_POINT('Ctrl Pts',(2.69030244115566,1.77450873132731,11.677146869809));
#13465=CARTESIAN_POINT('Ctrl Pts',(2.67803948175904,1.79296206233852,11.6785280505755));
#13466=CARTESIAN_POINT('Ctrl Pts',(2.54205176089383,1.99308890073625,11.6936901921808));
#13467=CARTESIAN_POINT('Ctrl Pts',(2.4002655229634,2.16174052258144,11.7081913687182));
#13468=CARTESIAN_POINT('Ctrl Pts',(2.11062723143564,2.44234738538761,11.7353924766799));
#13469=CARTESIAN_POINT('Ctrl Pts',(1.96812630188285,2.55857203759592,11.7479303185372));
#13470=CARTESIAN_POINT('Ctrl Pts',(1.77834919370969,2.68807091224547,11.7630607501357));
#13471=CARTESIAN_POINT('Ctrl Pts',(1.7396381930857,2.71328407830959,11.7660711726151));
#13472=CARTESIAN_POINT('Ctrl Pts',(1.68407525005283,2.74779498292184,11.7702719988765));
#13473=CARTESIAN_POINT('Ctrl Pts',(1.66766313108956,2.75778651037123,11.7714983486244));
#13474=CARTESIAN_POINT('Ctrl Pts',(1.64232839598178,2.77290115470138,11.7733681375891));
#13475=CARTESIAN_POINT('Ctrl Pts',(1.63346926812361,2.77812914218243,11.7740176488681));
#13476=CARTESIAN_POINT('Ctrl Pts',(1.61878011121123,2.78670301483388,11.7750872704197));
#13477=CARTESIAN_POINT('Ctrl Pts',(1.61296445047471,2.79007319343898,11.7755088646787));
#13478=CARTESIAN_POINT('Ctrl Pts',(1.6016956348499,2.79655646868358,11.7763220703072));
#13479=CARTESIAN_POINT('Ctrl Pts',(1.59624384727609,2.79967186842773,11.7767138264377));
#13480=CARTESIAN_POINT('Ctrl Pts',(1.58612074454396,2.8054174884159,11.7774381179487));
#13481=CARTESIAN_POINT('Ctrl Pts',(1.5814520211789,2.80805195925302,11.777770920269));
#13482=CARTESIAN_POINT('Ctrl Pts',(1.57061901960535,2.81412922711128,11.7785402938721));
#13483=CARTESIAN_POINT('Ctrl Pts',(1.56444999683427,2.8175634192107,11.7789763090534));
#13484=CARTESIAN_POINT('Ctrl Pts',(1.54573176673379,2.82790311592356,11.7802930334057));
#13485=CARTESIAN_POINT('Ctrl Pts',(1.53314756161647,2.83474536770029,11.7811697914067));
#13486=CARTESIAN_POINT('Ctrl Pts',(1.43376245344371,2.88792736356153,11.788030988222));
#13487=CARTESIAN_POINT('Ctrl Pts',(1.34491702221414,2.93035859548682,11.7937881091403));
#13488=CARTESIAN_POINT('Ctrl Pts',(1.03680590172559,3.06053564091246,11.8129610100627));
#13489=CARTESIAN_POINT('Ctrl Pts',(0.809910356764825,3.12824243046199,11.8258154074241));
#13490=CARTESIAN_POINT('Ctrl Pts',(0.487227554761787,3.1870320886624,11.8444885765798));
#13491=CARTESIAN_POINT('Ctrl Pts',(0.396152940850973,3.1996289070675,11.8497934096994));
#13492=CARTESIAN_POINT('Ctrl Pts',(0.248834866693381,3.213618578218,11.8585194256859));
#13493=CARTESIAN_POINT('Ctrl Pts',(0.192874340959847,3.2174620541282,11.8618671377285));
#13494=CARTESIAN_POINT('Ctrl Pts',(0.119688718202076,3.22057246839202,11.8662998246035));
#13495=CARTESIAN_POINT('Ctrl Pts',(0.102527692945166,3.22116445836857,11.8673431157513));
#13496=CARTESIAN_POINT('Ctrl Pts',(0.0745187561960433,3.22190660911981,
11.869052554973));
#13497=CARTESIAN_POINT('Ctrl Pts',(0.0636732267531638,3.22213918981772,
11.8697161061062));
#13498=CARTESIAN_POINT('Ctrl Pts',(0.0427491398346177,3.22248222039309,
11.870999506736));
#13499=CARTESIAN_POINT('Ctrl Pts',(0.0326708192485477,3.2226001557116,11.8716191132431));
#13500=CARTESIAN_POINT('Ctrl Pts',(0.0094996513050964,3.22276259479761,
11.8730470445237));
#13501=CARTESIAN_POINT('Ctrl Pts',(-0.00359317861399371,3.22277459136332,
11.8738563815905));
#13502=CARTESIAN_POINT('Ctrl Pts',(-0.0385888829571881,3.22259340110126,
11.8760264602931));
#13503=CARTESIAN_POINT('Ctrl Pts',(-0.0604900250462614,3.22225670133831,
11.8773916810165));
#13504=CARTESIAN_POINT('Ctrl Pts',(-0.246202783867658,3.21750763303492,
11.8890306188454));
#13505=CARTESIAN_POINT('Ctrl Pts',(-0.409435950707107,3.20083093786686,
11.8996916386932));
#13506=CARTESIAN_POINT('Ctrl Pts',(-0.820554761215995,3.12686258942418,
11.9275521612582));
#13507=CARTESIAN_POINT('Ctrl Pts',(-1.06423534226815,3.05253633609439,11.9450773907194));
#13508=CARTESIAN_POINT('Ctrl Pts',(-1.34831418354115,2.9276867165127,11.9653784695869));
#13509=CARTESIAN_POINT('Ctrl Pts',(-1.39936376652582,2.90363265888656,11.9690169591603));
#13510=CARTESIAN_POINT('Ctrl Pts',(-1.46018735612178,2.87299613494754,11.9733176645033));
#13511=CARTESIAN_POINT('Ctrl Pts',(-1.47058736667286,2.86768664836898,11.9740517852065));
#13512=CARTESIAN_POINT('Ctrl Pts',(-1.48673694128351,2.85933089363235,11.9751895504171));
#13513=CARTESIAN_POINT('Ctrl Pts',(-1.49250640045858,2.85632360530528,11.9755955771843));
#13514=CARTESIAN_POINT('Ctrl Pts',(-1.50320789439459,2.85070425250725,11.9763478192089));
#13515=CARTESIAN_POINT('Ctrl Pts',(-1.50814220391267,2.84809687379613,11.9766943129702));
#13516=CARTESIAN_POINT('Ctrl Pts',(-1.51931380963264,2.84215642098321,11.9774780160625));
#13517=CARTESIAN_POINT('Ctrl Pts',(-1.52554690824573,2.83881563446275,11.9779147283269));
#13518=CARTESIAN_POINT('Ctrl Pts',(-1.54401149050716,2.82884069850565,11.9792069425469));
#13519=CARTESIAN_POINT('Ctrl Pts',(-1.55621124626149,2.82214772000768,11.9800587917559));
#13520=CARTESIAN_POINT('Ctrl Pts',(-1.64842050612833,2.77078050687666,11.9864855571273));
#13521=CARTESIAN_POINT('Ctrl Pts',(-1.72654327477322,2.72278652588155,11.9918634389635));
#13522=CARTESIAN_POINT('Ctrl Pts',(-2.00418739588655,2.53545540677384,12.0111231880685));
#13523=CARTESIAN_POINT('Ctrl Pts',(-2.18980515551159,2.37698713604192,12.0243472221739));
#13524=CARTESIAN_POINT('Ctrl Pts',(-2.41851899609109,2.13197634680636,12.0434293555514));
#13525=CARTESIAN_POINT('Ctrl Pts',(-2.47830328780289,2.0621755901511,12.0487320989932));
#13526=CARTESIAN_POINT('Ctrl Pts',(-2.5696420606219,1.9458162778558,12.0574549913814));
#13527=CARTESIAN_POINT('Ctrl Pts',(-2.60310391669494,1.90081843695513,12.0608017383624));
#13528=CARTESIAN_POINT('Ctrl Pts',(-2.64525609121311,1.8409325253953,12.0652333251167));
#13529=CARTESIAN_POINT('Ctrl Pts',(-2.65502606899793,1.8268138674625,12.0662765074791));
#13530=CARTESIAN_POINT('Ctrl Pts',(-2.67078382627517,1.80364879828592,12.0679858132374));
#13531=CARTESIAN_POINT('Ctrl Pts',(-2.67683964968382,1.79464891262382,12.0686493404749));
#13532=CARTESIAN_POINT('Ctrl Pts',(-2.68843440750514,1.77722806334803,12.069932726349));
#13533=CARTESIAN_POINT('Ctrl Pts',(-2.6939795079997,1.76881134081716,12.0705523421653));
#13534=CARTESIAN_POINT('Ctrl Pts',(-2.70663723012357,1.74940101587895,12.0719803400093));
#13535=CARTESIAN_POINT('Ctrl Pts',(-2.7137224811148,1.73838985765786,12.0727897346387));
#13536=CARTESIAN_POINT('Ctrl Pts',(-2.73248197900168,1.70884162608429,12.0749600680681));
#13537=CARTESIAN_POINT('Ctrl Pts',(-2.74403448692855,1.69022843570866,12.0763254876082));
#13538=CARTESIAN_POINT('Ctrl Pts',(-2.84047054421035,1.53125765982343,12.0879745419554));
#13539=CARTESIAN_POINT('Ctrl Pts',(-2.91470085818788,1.38474803167294,12.0986462585612));
#13540=CARTESIAN_POINT('Ctrl Pts',(-3.07473557039341,0.99837275599216,12.1265404312895));
#13541=CARTESIAN_POINT('Ctrl Pts',(-3.14388207541768,0.752826505316417,
12.1440893178192));
#13542=CARTESIAN_POINT('Ctrl Pts',(-3.19217173853121,0.446419487259036,
12.1643778785104));
#13543=CARTESIAN_POINT('Ctrl Pts',(-3.1994444548833,0.390905165253747,12.1679870563966));
#13544=CARTESIAN_POINT('Ctrl Pts',(-3.20647952486802,0.323639206522639,
12.1722578775545));
#13545=CARTESIAN_POINT('Ctrl Pts',(-3.20762850341694,0.312045947333867,
12.1729902884519));
#13546=CARTESIAN_POINT('Ctrl Pts',(-3.20932060802965,0.293974574578464,
12.1741259857712));
#13547=CARTESIAN_POINT('Ctrl Pts',(-3.20990702858604,0.287500756917704,
12.1745316407617));
#13548=CARTESIAN_POINT('Ctrl Pts',(-3.21096057573848,0.275464874375558,
12.1752835472067));
#13549=CARTESIAN_POINT('Ctrl Pts',(-3.2114328356937,0.269903424390084,12.175630074949));
#13550=CARTESIAN_POINT('Ctrl Pts',(-3.21247137274394,0.257284602528006,
12.1764143048046));
#13551=CARTESIAN_POINT('Ctrl Pts',(-3.21302884250843,0.250226591043907,
12.1768515070534));
#13552=CARTESIAN_POINT('Ctrl Pts',(-3.2146158099064,0.229254067373092,12.1781465171027));
#13553=CARTESIAN_POINT('Ctrl Pts',(-3.21557822656471,0.215334432624636,
12.1790006486707));
#13554=CARTESIAN_POINT('Ctrl Pts',(-3.22224828259434,0.108815182573246,
12.1854987241927));
#13555=CARTESIAN_POINT('Ctrl Pts',(-3.22404591461609,0.0160048392417297,
12.1909406570997));
#13556=CARTESIAN_POINT('Ctrl Pts',(-3.21607478716334,-0.318555463778213,
12.2101739790226));
#13557=CARTESIAN_POINT('Ctrl Pts',(-3.18311398985177,-0.558938893050106,
12.2233255010249));
#13558=CARTESIAN_POINT('Ctrl Pts',(-3.10091533984071,-0.882556932284656,
12.2423336450347));
#13559=CARTESIAN_POINT('Ctrl Pts',(-3.07445830211507,-0.970714632711053,
12.2476440267163));
#13560=CARTESIAN_POINT('Ctrl Pts',(-3.02584787840065,-1.1106361636464,12.2563783359346));
#13561=CARTESIAN_POINT('Ctrl Pts',(-3.00604670539333,-1.16316408942087,
12.2597286096372));
#13562=CARTESIAN_POINT('Ctrl Pts',(-2.97840865036355,-1.23105421900172,
12.2641642165881));
#13563=CARTESIAN_POINT('Ctrl Pts',(-2.97180540927946,-1.2469102494939,12.2652077963702));
#13564=CARTESIAN_POINT('Ctrl Pts',(-2.96082501647664,-1.27269418467854,
12.2669175897189));
#13565=CARTESIAN_POINT('Ctrl Pts',(-2.95652386484686,-1.28265423943773,
12.2675812042683));
#13566=CARTESIAN_POINT('Ctrl Pts',(-2.94813015614229,-1.30182476718858,
12.2688646441174));
#13567=CARTESIAN_POINT('Ctrl Pts',(-2.94404451753865,-1.31103814478786,
12.2694842259787));
#13568=CARTESIAN_POINT('Ctrl Pts',(-2.93455313430845,-1.33217372140194,
12.2709119808665));
#13569=CARTESIAN_POINT('Ctrl Pts',(-2.92911786045172,-1.34408239090049,
12.2717211653687));
#13570=CARTESIAN_POINT('Ctrl Pts',(-2.91439791287889,-1.37582039915591,
12.2738905689524));
#13571=CARTESIAN_POINT('Ctrl Pts',(-2.90498358407239,-1.3955885150647,12.2752552627428));
#13572=CARTESIAN_POINT('Ctrl Pts',(-2.82358863429697,-1.56210816238581,
12.2868674713166));
#13573=CARTESIAN_POINT('Ctrl Pts',(-2.74075219450701,-1.70326084694038,
12.2975002346816));
#13574=CARTESIAN_POINT('Ctrl Pts',(-2.5032958898301,-2.04540118072834,12.3252741370639));
#13575=CARTESIAN_POINT('Ctrl Pts',(-2.3350347729996,-2.23556790716262,12.3427393135935));
#13576=CARTESIAN_POINT('Ctrl Pts',(-2.10332622493173,-2.44242703613689,
12.3630734111069));
#13577=CARTESIAN_POINT('Ctrl Pts',(-2.05936318504076,-2.47960788865712,
12.3667874966365));
#13578=CARTESIAN_POINT('Ctrl Pts',(-2.00525695221621,-2.52293481037836,
12.3711651592417));
#13579=CARTESIAN_POINT('Ctrl Pts',(-1.99604907480359,-2.5302259983696,12.3719036131642));
#13580=CARTESIAN_POINT('Ctrl Pts',(-1.98166704757851,-2.54148692651986,
12.373046617751));
#13581=CARTESIAN_POINT('Ctrl Pts',(-1.97652047338424,-2.54549148598286,
12.373453585523));
#13582=CARTESIAN_POINT('Ctrl Pts',(-1.96694791562539,-2.5528933760697,12.3742066816674));
#13583=CARTESIAN_POINT('Ctrl Pts',(-1.9625253055307,-2.55629480268904,12.3745530941412));
#13584=CARTESIAN_POINT('Ctrl Pts',(-1.95249289569975,-2.56396934104302,
12.3753354854073));
#13585=CARTESIAN_POINT('Ctrl Pts',(-1.94687790502244,-2.56823552555741,
12.3757709741234));
#13586=CARTESIAN_POINT('Ctrl Pts',(-1.93021695415085,-2.58080822234851,
12.3770562193339));
#13587=CARTESIAN_POINT('Ctrl Pts',(-1.91913134787049,-2.58906227351373,
12.3779023812981));
#13588=CARTESIAN_POINT('Ctrl Pts',(-1.83631109790268,-2.64990383507711,
12.3841602991194));
#13589=CARTESIAN_POINT('Ctrl Pts',(-1.76247290626276,-2.69957795642286,
12.389386535945));
#13590=CARTESIAN_POINT('Ctrl Pts',(-1.61766785356306,-2.78851665839571,
12.3991714145107));
#13591=CARTESIAN_POINT('Ctrl Pts',(-1.54714526428157,-2.82824987494954,
12.4037409095));
#13592=CARTESIAN_POINT('Ctrl Pts',(-1.47525514217493,-2.86526435568979,
12.4082778759135));
#13593=CARTESIAN_POINT('Origin',(0.,0.,4.68922655072688));
#13594=CARTESIAN_POINT('',(-1.47525547426955,-2.8652641847023,13.9035519756546));
#13595=CARTESIAN_POINT('',(-1.4752554049854,-2.86526422037504,13.6541509617524));
#13596=CARTESIAN_POINT('',(-1.47525540501186,-2.86526422036142,4.68922655072688));
#13597=CARTESIAN_POINT('',(3.22274998502511,0.000310677704944338,13.0638091501483));
#13598=CARTESIAN_POINT('Ctrl Pts',(-1.47525547426939,-2.86526418470238,
13.9035519756546));
#13599=CARTESIAN_POINT('Ctrl Pts',(-1.54303258806227,-2.83036738227594,
13.8992923598215));
#13600=CARTESIAN_POINT('Ctrl Pts',(-1.60960295797985,-2.79304953613835,
13.8950259309918));
#13601=CARTESIAN_POINT('Ctrl Pts',(-1.81607017557258,-2.6674584409174,13.8813804824954));
#13602=CARTESIAN_POINT('Ctrl Pts',(-1.95046699540141,-2.57081957006326,
13.8718588107835));
#13603=CARTESIAN_POINT('Ctrl Pts',(-2.09362411535334,-2.45017078621481,
13.8605985964914));
#13604=CARTESIAN_POINT('Ctrl Pts',(-2.11025375650396,-2.43586285835686,
13.859272399019));
#13605=CARTESIAN_POINT('Ctrl Pts',(-2.13658212788618,-2.41273830262775,
13.8571427568952));
#13606=CARTESIAN_POINT('Ctrl Pts',(-2.14637557782703,-2.40403019471789,
13.8563438300992));
#13607=CARTESIAN_POINT('Ctrl Pts',(-2.163610160559,-2.388516342501,13.8549257086795));
#13608=CARTESIAN_POINT('Ctrl Pts',(-2.17107301754225,-2.38173491264197,
13.8543075463185));
#13609=CARTESIAN_POINT('Ctrl Pts',(-2.18649842783968,-2.36758524224134,
13.8530212301857));
#13610=CARTESIAN_POINT('Ctrl Pts',(-2.19445583780695,-2.36021160609201,
13.8523528499798));
#13611=CARTESIAN_POINT('Ctrl Pts',(-2.2149053182932,-2.34106952902646,13.8506226123593));
#13612=CARTESIAN_POINT('Ctrl Pts',(-2.22734076000807,-2.32924134197813,
13.8495581827643));
#13613=CARTESIAN_POINT('Ctrl Pts',(-2.27992692897469,-2.27841689123593,
13.8450038129448));
#13614=CARTESIAN_POINT('Ctrl Pts',(-2.31915055819439,-2.23847948086697,
13.8414727395624));
#13615=CARTESIAN_POINT('Ctrl Pts',(-2.41979742033047,-2.13051521614022,
13.8320435057938));
#13616=CARTESIAN_POINT('Ctrl Pts',(-2.47938994046956,-2.06085847778673,
13.8260742277801));
#13617=CARTESIAN_POINT('Ctrl Pts',(-2.68733680650509,-1.79569929280763,
13.8037853191059));
#13618=CARTESIAN_POINT('Ctrl Pts',(-2.81618655403238,-1.58599904794723,
13.7869027223514));
#13619=CARTESIAN_POINT('Ctrl Pts',(-2.95809217792732,-1.28215198604447,
13.7646080669701));
#13620=CARTESIAN_POINT('Ctrl Pts',(-2.9927580909071,-1.19901012732734,13.7587190744549));
#13621=CARTESIAN_POINT('Ctrl Pts',(-3.028693413358,-1.10151075320558,13.7521377382162));
#13622=CARTESIAN_POINT('Ctrl Pts',(-3.03340358651978,-1.08847252105512,
13.7512642206489));
#13623=CARTESIAN_POINT('Ctrl Pts',(-3.04038615681228,-1.06874667428207,
13.7499530010915));
#13624=CARTESIAN_POINT('Ctrl Pts',(-3.04272087001189,-1.06208151559836,
13.7495117282581));
#13625=CARTESIAN_POINT('Ctrl Pts',(-3.04686168534694,-1.0501345583423,13.748724011933));
#13626=CARTESIAN_POINT('Ctrl Pts',(-3.04867598500958,-1.04485571264213,
13.7483770883238));
#13627=CARTESIAN_POINT('Ctrl Pts',(-3.05257896700212,-1.03340296605372,
13.7476268836894));
#13628=CARTESIAN_POINT('Ctrl Pts',(-3.05466263278768,-1.02722745371197,
13.7472239011641));
#13629=CARTESIAN_POINT('Ctrl Pts',(-3.06044154448486,-1.00992699352833,
13.7460991560499));
#13630=CARTESIAN_POINT('Ctrl Pts',(-3.0640948913819,-0.998788008494019,
13.7453798274397));
#13631=CARTESIAN_POINT('Ctrl Pts',(-3.08519785149469,-0.93323983538195,
13.7411739263593));
#13632=CARTESIAN_POINT('Ctrl Pts',(-3.10125996544684,-0.878390534686486,
13.7377636513281));
#13633=CARTESIAN_POINT('Ctrl Pts',(-3.18058642451351,-0.578113508837934,
13.7195370382248));
#13634=CARTESIAN_POINT('Ctrl Pts',(-3.21619491058329,-0.326285608225221,
13.7057827935169));
#13635=CARTESIAN_POINT('Ctrl Pts',(-3.22562274707539,0.0905874172435899,
13.6822276235085));
#13636=CARTESIAN_POINT('Ctrl Pts',(-3.21687571246231,0.254063868117312,
13.6728051940844));
#13637=CARTESIAN_POINT('Ctrl Pts',(-3.19293929805797,0.437876549399655,
13.6616560295008));
#13638=CARTESIAN_POINT('Ctrl Pts',(-3.18988987774838,0.459564756225506,
13.6603319869841));
#13639=CARTESIAN_POINT('Ctrl Pts',(-3.18466441909867,0.494167550209274,
13.6582051524482));
#13640=CARTESIAN_POINT('Ctrl Pts',(-3.18263027271072,0.507103114992514,
13.6574068592696));
#13641=CARTESIAN_POINT('Ctrl Pts',(-3.17889051030178,0.529975787586873,
13.6559894711812));
#13642=CARTESIAN_POINT('Ctrl Pts',(-3.17721698043603,0.539918019216727,
13.6553714049834));
#13643=CARTESIAN_POINT('Ctrl Pts',(-3.17364511867495,0.560546175040645,
13.6540848986102));
#13644=CARTESIAN_POINT('Ctrl Pts',(-3.17173940665668,0.571230676075219,
13.6534162300606));
#13645=CARTESIAN_POINT('Ctrl Pts',(-3.16667716027091,0.598805966746297,
13.6516844068493));
#13646=CARTESIAN_POINT('Ctrl Pts',(-3.16343947281233,0.615681335279812,
13.6506186710489));
#13647=CARTESIAN_POINT('Ctrl Pts',(-3.14904444515144,0.687597719786117,
13.646051135372));
#13648=CARTESIAN_POINT('Ctrl Pts',(-3.13658490945476,0.742365144170672,
13.6425079059423));
#13649=CARTESIAN_POINT('Ctrl Pts',(-3.09993888730017,0.885987095718178,
13.633037959115));
#13650=CARTESIAN_POINT('Ctrl Pts',(-3.07336571726649,0.974173944725516,
13.6270393580275));
#13651=CARTESIAN_POINT('Ctrl Pts',(-2.96367548140917,1.28874820706117,13.6049988003053));
#13652=CARTESIAN_POINT('Ctrl Pts',(-2.85900920374412,1.50675012446826,13.5884208857116));
#13653=CARTESIAN_POINT('Ctrl Pts',(-2.68142134092985,1.79020258254658,13.5661559125677));
#13654=CARTESIAN_POINT('Ctrl Pts',(-2.62839566569023,1.86718651204528,13.5600372081405));
#13655=CARTESIAN_POINT('Ctrl Pts',(-2.56367300761934,1.95291925709105,13.5532326671665));
#13656=CARTESIAN_POINT('Ctrl Pts',(-2.5551790499884,1.96401959100875,13.5523518560313));
#13657=CARTESIAN_POINT('Ctrl Pts',(-2.54226998144362,1.98066431351743,13.551031867226));
#13658=CARTESIAN_POINT('Ctrl Pts',(-2.53790848971449,1.98624980339979,13.5505890489268));
#13659=CARTESIAN_POINT('Ctrl Pts',(-2.53007751054666,1.99621054290907,13.549799666462));
#13660=CARTESIAN_POINT('Ctrl Pts',(-2.52661505469898,2.00059118961085,13.549452613532));
#13661=CARTESIAN_POINT('Ctrl Pts',(-2.51909753232944,2.0100515989803,13.5487033704109));
#13662=CARTESIAN_POINT('Ctrl Pts',(-2.51503849099403,2.01512808489499,13.5483014720329));
#13663=CARTESIAN_POINT('Ctrl Pts',(-2.50366705809702,2.02926201629485,13.5471828114905));
#13664=CARTESIAN_POINT('Ctrl Pts',(-2.49632082252718,2.03829228258205,13.5464684409392));
#13665=CARTESIAN_POINT('Ctrl Pts',(-2.45349026034932,2.09036231968875,13.5423499755261));
#13666=CARTESIAN_POINT('Ctrl Pts',(-2.41693982384847,2.13251772423204,13.5390185239296));
#13667=CARTESIAN_POINT('Ctrl Pts',(-2.20769910009121,2.36154997597489,13.520796381851));
#13668=CARTESIAN_POINT('Ctrl Pts',(-2.01443066061862,2.52842841246223,13.5069900726337));
#13669=CARTESIAN_POINT('Ctrl Pts',(-1.66770050215146,2.76256278142866,13.483358762301));
#13670=CARTESIAN_POINT('Ctrl Pts',(-1.52509496310787,2.84377442822509,13.4739150247416));
#13671=CARTESIAN_POINT('Ctrl Pts',(-1.35708863378552,2.92316785186097,13.4627389780137));
#13672=CARTESIAN_POINT('Ctrl Pts',(-1.33713799125516,2.93234749064328,13.4614113787347));
#13673=CARTESIAN_POINT('Ctrl Pts',(-1.30512850881835,2.94668102470496,13.4592799104338));
#13674=CARTESIAN_POINT('Ctrl Pts',(-1.29312910837099,2.95196656264869,13.4584805716562));
#13675=CARTESIAN_POINT('Ctrl Pts',(-1.27184410397463,2.96118757295278,13.4570619732111));
#13676=CARTESIAN_POINT('Ctrl Pts',(-1.26257160148976,2.96515298331546,13.4564437481153));
#13677=CARTESIAN_POINT('Ctrl Pts',(-1.2432888067475,2.97329247348944,13.455157554643));
#13678=CARTESIAN_POINT('Ctrl Pts',(-1.23327576332165,2.97745966839048,13.4544893610906));
#13679=CARTESIAN_POINT('Ctrl Pts',(-1.2073764243642,2.98808530944424,13.4527601500264));
#13680=CARTESIAN_POINT('Ctrl Pts',(-1.19145942776883,2.99446757542719,13.4516965661283));
#13681=CARTESIAN_POINT('Ctrl Pts',(-1.12349114483691,3.02109323277472,13.4471507001349));
#13682=CARTESIAN_POINT('Ctrl Pts',(-1.07097188995434,3.04010777025807,13.443627475715));
#13683=CARTESIAN_POINT('Ctrl Pts',(-0.931308748587889,3.08660453434112,
13.4342244952542));
#13684=CARTESIAN_POINT('Ctrl Pts',(-0.843449136185809,3.11176069340846,
13.428274113069));
#13685=CARTESIAN_POINT('Ctrl Pts',(-0.514007625866643,3.19110950358245,
13.4058632639788));
#13686=CARTESIAN_POINT('Ctrl Pts',(-0.267519530766325,3.22114906003356,
13.3888254172375));
#13687=CARTESIAN_POINT('Ctrl Pts',(0.0683554982004519,3.22323726544437,
13.366509294822));
#13688=CARTESIAN_POINT('Ctrl Pts',(0.156741438929809,3.22015001854749,13.3607309370937));
#13689=CARTESIAN_POINT('Ctrl Pts',(0.258660421649681,3.21238274392139,13.3542574994357));
#13690=CARTESIAN_POINT('Ctrl Pts',(0.272417711615473,3.21124535244927,13.3533877267107));
#13691=CARTESIAN_POINT('Ctrl Pts',(0.293189288914914,3.20939360315166,13.3520810122999));
#13692=CARTESIAN_POINT('Ctrl Pts',(0.300209029068424,3.20874458319702,13.3516405353656));
#13693=CARTESIAN_POINT('Ctrl Pts',(0.312782247797374,3.20754048697188,13.3508536742618));
#13694=CARTESIAN_POINT('Ctrl Pts',(0.318336443286197,3.20699401628944,13.3505068144321));
#13695=CARTESIAN_POINT('Ctrl Pts',(0.330383106417583,3.20577715459673,13.3497561017607));
#13696=CARTESIAN_POINT('Ctrl Pts',(0.336874945860679,3.20510147024643,13.3493525509116));
#13697=CARTESIAN_POINT('Ctrl Pts',(0.355063226827502,3.20315252416093,13.3482246121953));
#13698=CARTESIAN_POINT('Ctrl Pts',(0.366754955893441,3.20183491147731,13.3475026806788));
#13699=CARTESIAN_POINT('Ctrl Pts',(0.435906375976321,3.19365806251771,13.3432498990653));
#13700=CARTESIAN_POINT('Ctrl Pts',(0.493184089225305,3.18531577838369,13.3397973447783));
#13701=CARTESIAN_POINT('Ctrl Pts',(0.799402117971898,3.13225714526095,13.3215676277044));
#13702=CARTESIAN_POINT('Ctrl Pts',(1.04266783510849,3.05989358148588,13.3078407872682));
#13703=CARTESIAN_POINT('Ctrl Pts',(1.42481624202104,2.89527727577188,13.2843339292745));
#13704=CARTESIAN_POINT('Ctrl Pts',(1.56950911323301,2.8194614094535,13.2749313441962));
#13705=CARTESIAN_POINT('Ctrl Pts',(1.72808506189678,2.72036946197471,13.2636847783017));
#13706=CARTESIAN_POINT('Ctrl Pts',(1.74819762755504,2.70748831921958,13.2622402899411));
#13707=CARTESIAN_POINT('Ctrl Pts',(1.77867118788821,2.68749033309294,13.2600230577577));
#13708=CARTESIAN_POINT('Ctrl Pts',(1.7891370811748,2.68053427189861,13.2592563403086));
#13709=CARTESIAN_POINT('Ctrl Pts',(1.80766180439341,2.66806515982784,13.2578897934385));
#13710=CARTESIAN_POINT('Ctrl Pts',(1.81573681032634,2.66257633288509,13.2572908867698));
#13711=CARTESIAN_POINT('Ctrl Pts',(1.82396708114496,2.65692711553739,13.2566771284976));
#13712=CARTESIAN_POINT('Ctrl Pts',(1.82414747100889,2.65680326979342,13.2566636745902));
#13713=CARTESIAN_POINT('Ctrl Pts',(1.82449631202256,2.6565637224954,13.2566376540142));
#13714=CARTESIAN_POINT('Ctrl Pts',(1.82466476963494,2.65644801995459,13.2566250870734));
#13715=CARTESIAN_POINT('Ctrl Pts',(1.82499103828847,2.65622388162727,13.2566007446468));
#13716=CARTESIAN_POINT('Ctrl Pts',(1.82514884549013,2.65611545136244,13.2565889696231));
#13717=CARTESIAN_POINT('Ctrl Pts',(1.82545489885312,2.65590512012645,13.2565661305442));
#13718=CARTESIAN_POINT('Ctrl Pts',(1.82560314615233,2.65580322080147,13.2565550665517));
#13719=CARTESIAN_POINT('Ctrl Pts',(1.82589102085572,2.65560531163277,13.2565335797267));
#13720=CARTESIAN_POINT('Ctrl Pts',(1.82603064921561,2.65550930319193,13.2565231569483));
#13721=CARTESIAN_POINT('Ctrl Pts',(1.82630210199719,2.65532262076383,13.2565028920095));
#13722=CARTESIAN_POINT('Ctrl Pts',(1.82643392724926,2.65523194796468,13.2564930498941));
#13723=CARTESIAN_POINT('Ctrl Pts',(1.8266904854685,2.65505545247603,13.2564738934623));
#13724=CARTESIAN_POINT('Ctrl Pts',(1.82681521913522,2.65496963081685,13.2564645791856));
#13725=CARTESIAN_POINT('Ctrl Pts',(1.82705821814233,2.6548024127288,13.2564464321075));
#13726=CARTESIAN_POINT('Ctrl Pts',(1.82717648409353,2.65472101718573,13.25643759934));
#13727=CARTESIAN_POINT('Ctrl Pts',(1.82740709745644,2.65456227677371,13.256420374452));
#13728=CARTESIAN_POINT('Ctrl Pts',(1.82751944541041,2.65448493266603,13.2564119823601));
#13729=CARTESIAN_POINT('Ctrl Pts',(1.82773870948594,2.65433396338863,13.2563956026701));
#13730=CARTESIAN_POINT('Ctrl Pts',(1.82784562606501,2.6542603388942,13.2563876150982));
#13731=CARTESIAN_POINT('Ctrl Pts',(1.82805446002122,2.65411651383503,13.2563720123042));
#13732=CARTESIAN_POINT('Ctrl Pts',(1.82815637780279,2.65404631386008,13.2563643971047));
#13733=CARTESIAN_POINT('Ctrl Pts',(1.82835560025163,2.65390907445809,13.2563495103625));
#13734=CARTESIAN_POINT('Ctrl Pts',(1.82845290528395,2.65384203554416,13.2563422388392));
#13735=CARTESIAN_POINT('Ctrl Pts',(1.82864324808455,2.6537108822367,13.2563280137412));
#13736=CARTESIAN_POINT('Ctrl Pts',(1.82873628616771,2.65364676830211,13.2563210601842));
#13737=CARTESIAN_POINT('Ctrl Pts',(1.82891840595857,2.65352125270398,13.2563074479043));
#13738=CARTESIAN_POINT('Ctrl Pts',(1.82900748792792,2.65345985145985,13.2563007891985));
#13739=CARTESIAN_POINT('Ctrl Pts',(1.82918197571369,2.65333956986007,13.2562877457825));
#13740=CARTESIAN_POINT('Ctrl Pts',(1.82926738180885,2.6532806898463,13.2562813610841));
#13741=CARTESIAN_POINT('Ctrl Pts',(1.82943477139101,2.65316527748324,13.2562688468243));
#13742=CARTESIAN_POINT('Ctrl Pts',(1.82951675510313,2.65310874545581,13.2562627172752));
#13743=CARTESIAN_POINT('Ctrl Pts',(1.82967752985226,2.65299787192051,13.2562506962088));
#13744=CARTESIAN_POINT('Ctrl Pts',(1.82975632108939,2.65294353070216,13.2562448047025));
#13745=CARTESIAN_POINT('Ctrl Pts',(1.82991092003765,2.65283689579824,13.2562332441597));
#13746=CARTESIAN_POINT('Ctrl Pts',(1.82998672791179,2.65278460238447,13.2562275751343));
#13747=CARTESIAN_POINT('Ctrl Pts',(1.83986503517043,2.64596977226778,13.2554888225628));
#13748=CARTESIAN_POINT('Ctrl Pts',(1.84962987022553,2.63915303089014,13.254753667877));
#13749=CARTESIAN_POINT('Ctrl Pts',(1.86983555667426,2.62488040710172,13.2532221729703));
#13750=CARTESIAN_POINT('Ctrl Pts',(1.88027010020347,2.61741599735144,13.2524255117581));
#13751=CARTESIAN_POINT('Ctrl Pts',(1.93725188108929,2.57613717978342,13.2480429712109));
#13752=CARTESIAN_POINT('Ctrl Pts',(1.98292928738133,2.54114509091567,13.244411482129));
#13753=CARTESIAN_POINT('Ctrl Pts',(2.10167304200838,2.44502744336957,13.2346439710303));
#13754=CARTESIAN_POINT('Ctrl Pts',(2.17300355299145,2.38185674476608,13.2284303222268));
#13755=CARTESIAN_POINT('Ctrl Pts',(2.34373830785972,2.21659271736009,13.212686524404));
#13756=CARTESIAN_POINT('Ctrl Pts',(2.43936775474247,2.11089385302071,13.2030493433906));
#13757=CARTESIAN_POINT('Ctrl Pts',(2.64328784588221,1.85307079718243,13.1807994533654));
#13758=CARTESIAN_POINT('Ctrl Pts',(2.74600647518844,1.69714666823927,13.1682213424386));
#13759=CARTESIAN_POINT('Ctrl Pts',(2.84165769087714,1.52030071515126,13.1554777750602));
#13760=CARTESIAN_POINT('Ctrl Pts',(2.84854763418732,1.50735168145237,13.1545530969659));
#13761=CARTESIAN_POINT('Ctrl Pts',(2.85865530732638,1.48803838556439,13.1531869481878));
#13762=CARTESIAN_POINT('Ctrl Pts',(2.86194059524063,1.48170996981639,13.1527413591609));
#13763=CARTESIAN_POINT('Ctrl Pts',(2.86776278822654,1.47040313242541,13.1519489721851));
#13764=CARTESIAN_POINT('Ctrl Pts',(2.87030776870668,1.46542898016969,13.1516016699928));
#13765=CARTESIAN_POINT('Ctrl Pts',(2.87577127136868,1.45468175260473,13.1508540711102));
#13766=CARTESIAN_POINT('Ctrl Pts',(2.87868534392187,1.44890651838495,13.1504540545464));
#13767=CARTESIAN_POINT('Ctrl Pts',(2.8867312543569,1.43284069503262,13.1493459325319));
#13768=CARTESIAN_POINT('Ctrl Pts',(2.89182549434616,1.4225312340237,13.1486401461141));
#13769=CARTESIAN_POINT('Ctrl Pts',(2.92031736028403,1.36408526697886,13.1446675649681));
#13770=CARTESIAN_POINT('Ctrl Pts',(2.94256970216377,1.31539591920006,13.1414675274994));
#13771=CARTESIAN_POINT('Ctrl Pts',(3.06424136383938,1.03061133214331,13.1232489150708));
#13772=CARTESIAN_POINT('Ctrl Pts',(3.13644897315352,0.783869572471844,13.1093529120562));
#13773=CARTESIAN_POINT('Ctrl Pts',(3.20070073527963,0.399359848305915,13.0873376944129));
#13774=CARTESIAN_POINT('Ctrl Pts',(3.21450392718355,0.266331696759462,13.0796706962223));
#13775=CARTESIAN_POINT('Ctrl Pts',(3.22119157718624,0.104223928745983,13.0700514696201));
#13776=CARTESIAN_POINT('Ctrl Pts',(3.22199056138468,0.0755946409071718,
13.068342574647));
#13777=CARTESIAN_POINT('Ctrl Pts',(3.22263444413199,0.0314104431670769,
13.0656878356073));
#13778=CARTESIAN_POINT('Ctrl Pts',(3.22274848599569,0.0158605448984554,
13.0647502303399));
#13779=CARTESIAN_POINT('Ctrl Pts',(3.22274998502511,0.000310677704944338,
13.0638091501483));
#13780=CARTESIAN_POINT('Ctrl Pts',(3.22274998514752,0.000309405382385037,
13.0638090731471));
#13781=CARTESIAN_POINT('Ctrl Pts',(3.22275119902617,-0.0123342900247772,
13.0630438747345));
#13782=CARTESIAN_POINT('Ctrl Pts',(3.22267800609396,-0.0249777782407157,
13.062276390535));
#13783=CARTESIAN_POINT('Ctrl Pts',(3.22241626611493,-0.0473981902040759,
13.0609112122533));
#13784=CARTESIAN_POINT('Ctrl Pts',(3.22225761857131,-0.0571753163518782,
13.0603144614021));
#13785=CARTESIAN_POINT('Ctrl Pts',(3.22185504357169,-0.0765493239484438,
13.0591290771725));
#13786=CARTESIAN_POINT('Ctrl Pts',(3.22161272659472,-0.0861461401344853,
13.0585405004048));
#13787=CARTESIAN_POINT('Ctrl Pts',(3.22104429950888,-0.105271461766646,
13.0573646830768));
#13788=CARTESIAN_POINT('Ctrl Pts',(3.22071877733159,-0.114799887972164,
13.0567774669285));
#13789=CARTESIAN_POINT('Ctrl Pts',(3.21973418090167,-0.140303238418092,
13.0552019017124));
#13790=CARTESIAN_POINT('Ctrl Pts',(3.21899850461072,-0.156274779957418,
13.0542111539936));
#13791=CARTESIAN_POINT('Ctrl Pts',(3.21587088744193,-0.21471140892968,13.0505710168166));
#13792=CARTESIAN_POINT('Ctrl Pts',(3.212757294087,-0.257131957836759,13.0478990935361));
#13793=CARTESIAN_POINT('Ctrl Pts',(3.17882940242412,-0.620659162934107,
13.0247379994649));
#13794=CARTESIAN_POINT('Ctrl Pts',(3.10080090528168,-0.935477557963266,
13.0026390784345));
#13795=CARTESIAN_POINT('Ctrl Pts',(2.93529802703581,-1.33500792121011,12.9736255945994));
#13796=CARTESIAN_POINT('Ctrl Pts',(2.88801347589584,-1.43443500080322,12.9663447777142));
#13797=CARTESIAN_POINT('Ctrl Pts',(2.82558525661003,-1.55004562884681,12.9579594462058));
#13798=CARTESIAN_POINT('Ctrl Pts',(2.81525300971195,-1.56873326049306,12.9566067059801));
#13799=CARTESIAN_POINT('Ctrl Pts',(2.80064694735087,-1.59454167238341,12.9547437232736));
#13800=CARTESIAN_POINT('Ctrl Pts',(2.79653047593873,-1.6017502206779,12.954223943739));
#13801=CARTESIAN_POINT('Ctrl Pts',(2.78950604055004,-1.61394141548422,12.9533459600165));
#13802=CARTESIAN_POINT('Ctrl Pts',(2.78661248375302,-1.61893227469542,12.9529868361295));
#13803=CARTESIAN_POINT('Ctrl Pts',(2.78106454856922,-1.62844251003251,12.9523031403497));
#13804=CARTESIAN_POINT('Ctrl Pts',(2.77841253452232,-1.63296320250473,12.9519784139127));
#13805=CARTESIAN_POINT('Ctrl Pts',(2.77140214404592,-1.64484677855304,12.9511254565011));
#13806=CARTESIAN_POINT('Ctrl Pts',(2.76702541836773,-1.65219887028441,12.9505984138741));
#13807=CARTESIAN_POINT('Ctrl Pts',(2.75161026250186,-1.67786042375699,12.9487608444603));
#13808=CARTESIAN_POINT('Ctrl Pts',(2.74041868421446,-1.69607786667844,12.9474599212906));
#13809=CARTESIAN_POINT('Ctrl Pts',(2.59724133330157,-1.92402178358547,12.9312099961186));
#13810=CARTESIAN_POINT('Ctrl Pts',(2.44165315088042,-2.11799220538469,12.9176357934344));
#13811=CARTESIAN_POINT('Ctrl Pts',(2.11481365107245,-2.44099822242077,12.8919025499043));
#13812=CARTESIAN_POINT('Ctrl Pts',(1.95001647775332,-2.57455377885432,12.8798856179341));
#13813=CARTESIAN_POINT('Ctrl Pts',(1.75916989388126,-2.70031970899399,12.8661353192103));
#13814=CARTESIAN_POINT('Ctrl Pts',(1.74493405863099,-2.70954061799208,12.8651108740881));
#13815=CARTESIAN_POINT('Ctrl Pts',(1.72096373665046,-2.7247995484285,12.8633876186979));
#13816=CARTESIAN_POINT('Ctrl Pts',(1.71126854484763,-2.73089888573605,12.8626910825326));
#13817=CARTESIAN_POINT('Ctrl Pts',(1.69226589332731,-2.7427127064052,12.8613266560411));
#13818=CARTESIAN_POINT('Ctrl Pts',(1.68296148561487,-2.74843182140175,12.860658948299));
#13819=CARTESIAN_POINT('Ctrl Pts',(1.66531738539575,-2.75915388224619,12.8593933689835));
#13820=CARTESIAN_POINT('Ctrl Pts',(1.65698375018078,-2.76416659923867,12.8587958658004));
#13821=CARTESIAN_POINT('Ctrl Pts',(1.63783130545497,-2.77556914033468,12.8574231914112));
#13822=CARTESIAN_POINT('Ctrl Pts',(1.62699761212112,-2.78193353638748,12.8566471027428));
#13823=CARTESIAN_POINT('Ctrl Pts',(1.59547096301335,-2.80020713382859,12.8543895599933));
#13824=CARTESIAN_POINT('Ctrl Pts',(1.57468288148178,-2.81194974339738,12.8529021118477));
#13825=CARTESIAN_POINT('Ctrl Pts',(1.41072778233451,-2.90217519996156,12.8411771459762));
#13826=CARTESIAN_POINT('Ctrl Pts',(1.2619367389219,-2.96989476271101,12.8305566484586));
#13827=CARTESIAN_POINT('Ctrl Pts',(0.870986988370921,-3.11313012284401,
12.8027905526368));
#13828=CARTESIAN_POINT('Ctrl Pts',(0.623878354689254,-3.17190293184503,
12.7853195598051));
#13829=CARTESIAN_POINT('Ctrl Pts',(0.31524401270032,-3.20781154981545,12.7649783010641));
#13830=CARTESIAN_POINT('Ctrl Pts',(0.257871271765716,-3.21293278936775,
12.7612626594714));
#13831=CARTESIAN_POINT('Ctrl Pts',(0.188661883698338,-3.21724451885631,
12.7568832315541));
#13832=CARTESIAN_POINT('Ctrl Pts',(0.176931540294084,-3.2179109435394,12.7561445106756));
#13833=CARTESIAN_POINT('Ctrl Pts',(0.158682940705784,-3.21884759494317,
12.755001096622));
#13834=CARTESIAN_POINT('Ctrl Pts',(0.152167208892545,-3.21916219806809,
12.7545939846412));
#13835=CARTESIAN_POINT('Ctrl Pts',(0.140074805848101,-3.21970926688188,
12.7538406215615));
#13836=CARTESIAN_POINT('Ctrl Pts',(0.134498537636614,-3.21994702729603,
12.7534940861688));
#13837=CARTESIAN_POINT('Ctrl Pts',(0.12187280824391,-3.22045250631243,12.7527114095447));
#13838=CARTESIAN_POINT('Ctrl Pts',(0.114823086455957,-3.220711565455,12.7522757587842));
#13839=CARTESIAN_POINT('Ctrl Pts',(0.0939539996455488,-3.22140984243835,
12.7509900069638));
#13840=CARTESIAN_POINT('Ctrl Pts',(0.0801323876580535,-3.22178328621796,
12.7501435034033));
#13841=CARTESIAN_POINT('Ctrl Pts',(-0.0226838977505775,-3.22389919302676,
12.7438812564736));
#13842=CARTESIAN_POINT('Ctrl Pts',(-0.111722977459457,-3.22204308678329,
12.7386513038527));
#13843=CARTESIAN_POINT('Ctrl Pts',(-0.446771128824899,-3.20114968864684,
12.7193226341891));
#13844=CARTESIAN_POINT('Ctrl Pts',(-0.690395170900753,-3.15758336300304,
12.7059249965003));
#13845=CARTESIAN_POINT('Ctrl Pts',(-1.01427312948718,-3.06034841874645,
12.6866691705564));
#13846=CARTESIAN_POINT('Ctrl Pts',(-1.10070523818209,-3.03033471719388,
12.6813890255472));
#13847=CARTESIAN_POINT('Ctrl Pts',(-1.23771352645921,-2.97612281282823,
12.6726996975242));
#13848=CARTESIAN_POINT('Ctrl Pts',(-1.28914098489699,-2.95420999953359,
12.6693631673588));
#13849=CARTESIAN_POINT('Ctrl Pts',(-1.35557130146388,-2.9238396444789,12.6649430044264));
#13850=CARTESIAN_POINT('Ctrl Pts',(-1.37111473608007,-2.91658296346666,
12.6639007496217));
#13851=CARTESIAN_POINT('Ctrl Pts',(-1.39639069799493,-2.90453580329068,
12.6621924303761));
#13852=CARTESIAN_POINT('Ctrl Pts',(-1.40615840992103,-2.89981960399327,
12.6615289546448));
#13853=CARTESIAN_POINT('Ctrl Pts',(-1.42496108559957,-2.89062366339293,
12.6602452925046));
#13854=CARTESIAN_POINT('Ctrl Pts',(-1.4339992083745,-2.88615064151755,12.6596253470745));
#13855=CARTESIAN_POINT('Ctrl Pts',(-1.45379319400704,-2.87623854752048,
12.6582611583369));
#13856=CARTESIAN_POINT('Ctrl Pts',(-1.46453979368046,-2.87078143005618,
12.6575162864758));
#13857=CARTESIAN_POINT('Ctrl Pts',(-1.47525540501245,-2.86526422036111,
12.6567692800014));
#13858=CARTESIAN_POINT('Ctrl Pts',(-1.47525514217493,-2.86526435568979,
12.4082778759135));
#13859=CARTESIAN_POINT('Ctrl Pts',(-1.32807964289666,-2.94104145167791,
12.4175660823812));
#13860=CARTESIAN_POINT('Ctrl Pts',(-1.17517331519269,-3.00542385950792,
12.4267296437769));
#13861=CARTESIAN_POINT('Ctrl Pts',(-0.931083016729306,-3.08667586857259,
12.441378750016));
#13862=CARTESIAN_POINT('Ctrl Pts',(-0.843114619318536,-3.11185464542109,
12.4466592428265));
#13863=CARTESIAN_POINT('Ctrl Pts',(-0.69985798827533,-3.14633761954119,
12.4553488670451));
#13864=CARTESIAN_POINT('Ctrl Pts',(-0.645188435910395,-3.1580014141481,
12.4586853274482));
#13865=CARTESIAN_POINT('Ctrl Pts',(-0.573385657482078,-3.17137833986141,
12.463105186689));
#13866=CARTESIAN_POINT('Ctrl Pts',(-0.556501154831585,-3.17438468584578,
12.4641472076288));
#13867=CARTESIAN_POINT('Ctrl Pts',(-0.528903383519519,-3.17907161804855,
12.4658550885166));
#13868=CARTESIAN_POINT('Ctrl Pts',(-0.518204066352105,-3.18083317431952,
12.466518360654));
#13869=CARTESIAN_POINT('Ctrl Pts',(-0.497541203884748,-3.18412812778795,
12.4678015894037));
#13870=CARTESIAN_POINT('Ctrl Pts',(-0.487578940676515,-3.18566883976614,
12.4684213050038));
#13871=CARTESIAN_POINT('Ctrl Pts',(-0.46465077986819,-3.18910472078019,
12.4698500154164));
#13872=CARTESIAN_POINT('Ctrl Pts',(-0.451680290949744,-3.19096759211842,
12.4706600261323));
#13873=CARTESIAN_POINT('Ctrl Pts',(-0.416962725831033,-3.19573794787928,
12.4728330865919));
#13874=CARTESIAN_POINT('Ctrl Pts',(-0.395197012861291,-3.19850249786062,
12.4742006347867));
#13875=CARTESIAN_POINT('Ctrl Pts',(-0.208787010211332,-3.2202474197314,
12.4859590069656));
#13876=CARTESIAN_POINT('Ctrl Pts',(-0.0429591055232302,-3.22672044094313,
12.4967463871683));
#13877=CARTESIAN_POINT('Ctrl Pts',(0.380799355072473,-3.21058686226732,
12.5250441529312));
#13878=CARTESIAN_POINT('Ctrl Pts',(0.636857764156288,-3.16974519918415,
12.5428915885471));
#13879=CARTESIAN_POINT('Ctrl Pts',(0.934019170458942,-3.0848491542892,12.563044025325));
#13880=CARTESIAN_POINT('Ctrl Pts',(0.982418519562595,-3.06977859962972,
12.5663042640375));
#13881=CARTESIAN_POINT('Ctrl Pts',(1.04115982971537,-3.04995600718061,12.5702173096445));
#13882=CARTESIAN_POINT('Ctrl Pts',(1.05185544222868,-3.04628389589195,12.5709279952417));
#13883=CARTESIAN_POINT('Ctrl Pts',(1.06859784199426,-3.04043705749284,12.5720373917615));
#13884=CARTESIAN_POINT('Ctrl Pts',(1.07465770741686,-3.03830045619146,12.5724383001979));
#13885=CARTESIAN_POINT('Ctrl Pts',(1.0859785386791,-3.03427082444546,12.5731860211055));
#13886=CARTESIAN_POINT('Ctrl Pts',(1.09124090944121,-3.03238224844945,12.5735330813293));
#13887=CARTESIAN_POINT('Ctrl Pts',(1.10325799770103,-3.02803418508311,12.574324485739));
#13888=CARTESIAN_POINT('Ctrl Pts',(1.11000940665089,-3.02556579089449,12.5747682924215));
#13889=CARTESIAN_POINT('Ctrl Pts',(1.13079581765924,-3.01788709301247,12.5761323358988));
#13890=CARTESIAN_POINT('Ctrl Pts',(1.14480305434446,-3.01260147949301,12.5770481927608));
#13891=CARTESIAN_POINT('Ctrl Pts',(1.31169888091134,-2.94829140951464,12.5879265564671));
#13892=CARTESIAN_POINT('Ctrl Pts',(1.4599297277231,-2.87777632466277,12.5972517623185));
#13893=CARTESIAN_POINT('Ctrl Pts',(1.74402251538407,-2.7150012027269,12.6156379056276));
#13894=CARTESIAN_POINT('Ctrl Pts',(1.87948320605962,-2.62304942145194,12.6246777734408));
#13895=CARTESIAN_POINT('Ctrl Pts',(2.08234395733136,-2.46153261112885,12.6394140712876));
#13896=CARTESIAN_POINT('Ctrl Pts',(2.15460196470166,-2.39853859479889,12.644935017842));
#13897=CARTESIAN_POINT('Ctrl Pts',(2.2657581053933,-2.29255227765536,12.6539833537267));
#13898=CARTESIAN_POINT('Ctrl Pts',(2.30649151818237,-2.25156656282776,12.6574299549641));
#13899=CARTESIAN_POINT('Ctrl Pts',(2.35799772013009,-2.19687630329258,12.6619752616268));
#13900=CARTESIAN_POINT('Ctrl Pts',(2.36979347626904,-2.18414688187869,12.6630295453128));
#13901=CARTESIAN_POINT('Ctrl Pts',(2.38882175317119,-2.16327685529851,12.6647524745948));
#13902=CARTESIAN_POINT('Ctrl Pts',(2.39611694107342,-2.15519366210888,12.6654184437282));
#13903=CARTESIAN_POINT('Ctrl Pts',(2.4100765445244,-2.13956769408213,12.6667033742869));
#13904=CARTESIAN_POINT('Ctrl Pts',(2.41674687133113,-2.13203035256774,12.6673220757543));
#13905=CARTESIAN_POINT('Ctrl Pts',(2.43195284746966,-2.11468483855536,12.6687434465091));
#13906=CARTESIAN_POINT('Ctrl Pts',(2.4404646246128,-2.10485605844719,12.6695470976707));
#13907=CARTESIAN_POINT('Ctrl Pts',(2.46295361190521,-2.07856761883061,12.6716920644322));
#13908=CARTESIAN_POINT('Ctrl Pts',(2.47682507865841,-2.06201875198085,12.6730376976517));
#13909=CARTESIAN_POINT('Ctrl Pts',(2.58558647651959,-1.92958382203471,12.68377150118));
#13910=CARTESIAN_POINT('Ctrl Pts',(2.67244554100373,-1.80736676720248,12.6934808220081));
#13911=CARTESIAN_POINT('Ctrl Pts',(2.86744260258071,-1.48803707138875,12.7183364730947));
#13912=CARTESIAN_POINT('Ctrl Pts',(2.96406624210033,-1.2848280678903,12.7337429744435));
#13913=CARTESIAN_POINT('Ctrl Pts',(3.06840533998564,-0.989399829864131,
12.7546184921491));
#13914=CARTESIAN_POINT('Ctrl Pts',(3.09453617955183,-0.904362837698054,
12.7604549186173));
#13915=CARTESIAN_POINT('Ctrl Pts',(3.12197045948239,-0.799864454496833,
12.7673351950641));
#13916=CARTESIAN_POINT('Ctrl Pts',(3.12665829718623,-0.781338997897061,
12.7685439255011));
#13917=CARTESIAN_POINT('Ctrl Pts',(3.13305998437349,-0.755060068471666,
12.7702419412962));
#13918=CARTESIAN_POINT('Ctrl Pts',(3.1349102780138,-0.747340701864984,12.7707387089341));
#13919=CARTESIAN_POINT('Ctrl Pts',(3.13803994037495,-0.734067689367205,
12.7715893114564));
#13920=CARTESIAN_POINT('Ctrl Pts',(3.13933312778204,-0.728517367503911,
12.7719439360743));
#13921=CARTESIAN_POINT('Ctrl Pts',(3.1418054056881,-0.717777594063654,12.7726280297301));
#13922=CARTESIAN_POINT('Ctrl Pts',(3.14298636664496,-0.712588648388276,
12.7729576099082));
#13923=CARTESIAN_POINT('Ctrl Pts',(3.14612596954831,-0.698634108110556,
12.7738414740361));
#13924=CARTESIAN_POINT('Ctrl Pts',(3.14806084676547,-0.6898631334293,12.7743944009279));
#13925=CARTESIAN_POINT('Ctrl Pts',(3.15504216740492,-0.657575086454122,
12.7764206266544));
#13926=CARTESIAN_POINT('Ctrl Pts',(3.15986211185853,-0.634009136853062,
12.7778815211945));
#13927=CARTESIAN_POINT('Ctrl Pts',(3.20302355340606,-0.410249413958796,
12.7916018108761));
#13928=CARTESIAN_POINT('Ctrl Pts',(3.22256012396323,-0.206867382593006,
12.8029491858007));
#13929=CARTESIAN_POINT('Ctrl Pts',(3.22296310569356,0.229014011018249,12.8273020880819));
#13930=CARTESIAN_POINT('Ctrl Pts',(3.19812848998415,0.460322081304765,12.8402815110925));
#13931=CARTESIAN_POINT('Ctrl Pts',(3.14083707101853,0.722921592924151,12.8563016916263));
#13932=CARTESIAN_POINT('Ctrl Pts',(3.13237345173311,0.758755248147586,12.8585146150015));
#13933=CARTESIAN_POINT('Ctrl Pts',(3.11958335295439,0.809039150874073,12.8616610990742));
#13934=CARTESIAN_POINT('Ctrl Pts',(3.11576633017217,0.823616905721149,12.8625782028728));
#13935=CARTESIAN_POINT('Ctrl Pts',(3.10941331294041,0.847203631754731,12.8640702519149));
#13936=CARTESIAN_POINT('Ctrl Pts',(3.10694003691891,0.856229378387173,12.8646431522876));
#13937=CARTESIAN_POINT('Ctrl Pts',(3.10169264103197,0.875056619371128,12.8658423268489));
#13938=CARTESIAN_POINT('Ctrl Pts',(3.09891129657857,0.884855976229839,12.866468831192));
#13939=CARTESIAN_POINT('Ctrl Pts',(3.09220597764269,0.908061046235031,12.8679580572882));
#13940=CARTESIAN_POINT('Ctrl Pts',(3.08824123810762,0.921454674538707,12.8688221050648));
#13941=CARTESIAN_POINT('Ctrl Pts',(3.07469214710865,0.966156198854201,12.8717211619859));
#13942=CARTESIAN_POINT('Ctrl Pts',(3.06471802291581,0.997342926156683,12.8737689147052));
#13943=CARTESIAN_POINT('Ctrl Pts',(3.00837016330244,1.16469649555872,12.884897572402));
#13944=CARTESIAN_POINT('Ctrl Pts',(2.95340038800004,1.29777704968047,12.8942617343917));
#13945=CARTESIAN_POINT('Ctrl Pts',(2.77953975058517,1.64991933857387,12.9204046279798));
#13946=CARTESIAN_POINT('Ctrl Pts',(2.64386722339222,1.85957879987468,12.9375692406869));
#13947=CARTESIAN_POINT('Ctrl Pts',(2.44311534142933,2.10278921598091,12.9583219593562));
#13948=CARTESIAN_POINT('Ctrl Pts',(2.39922654963696,2.15273046579338,12.9626294675551));
#13949=CARTESIAN_POINT('Ctrl Pts',(2.34585707858172,2.20979819804294,12.9675716736054));
#13950=CARTESIAN_POINT('Ctrl Pts',(2.33784673901691,2.21827098069142,12.9683059694807));
#13951=CARTESIAN_POINT('Ctrl Pts',(2.3248114187996,2.23190980097087,12.9694885686297));
#13952=CARTESIAN_POINT('Ctrl Pts',(2.31981486976677,2.23710269434689,12.9699389749901));
#13953=CARTESIAN_POINT('Ctrl Pts',(2.31090963060719,2.24629595573078,12.9707365294205));
#13954=CARTESIAN_POINT('Ctrl Pts',(2.30700790909753,2.25030294641519,12.9710842091079));
#13955=CARTESIAN_POINT('Ctrl Pts',(2.29860925613849,2.25888339383814,12.9718288259189));
#13956=CARTESIAN_POINT('Ctrl Pts',(2.2941091094302,2.26345357696786,12.9722255032189));
#13957=CARTESIAN_POINT('Ctrl Pts',(2.28167434553954,2.27600668418538,12.9733153815941));
#13958=CARTESIAN_POINT('Ctrl Pts',(2.27371141559396,2.28396161370644,12.9740063858905));
#13959=CARTESIAN_POINT('Ctrl Pts',(2.2302088974021,2.32696743274951,12.9777450912158));
#13960=CARTESIAN_POINT('Ctrl Pts',(2.19389814724152,2.36123288067854,12.980734915097));
#13961=CARTESIAN_POINT('Ctrl Pts',(1.96437123842322,2.56796285424501,12.998952949677));
#13962=CARTESIAN_POINT('Ctrl Pts',(1.75172921718002,2.7174737027081,13.0129954683047));
#13963=CARTESIAN_POINT('Ctrl Pts',(1.37722761058508,2.9183727880272,13.0369882672184));
#13964=CARTESIAN_POINT('Ctrl Pts',(1.22517275157435,2.98539722672146,13.0465446220541));
#13965=CARTESIAN_POINT('Ctrl Pts',(1.0479428742098,3.04769008871387,13.0578433748978));
#13966=CARTESIAN_POINT('Ctrl Pts',(1.02716612049091,3.05475512420929,13.0591700166121));
#13967=CARTESIAN_POINT('Ctrl Pts',(0.993869548144303,3.06569936934389,13.0613000960157));
#13968=CARTESIAN_POINT('Ctrl Pts',(0.98139518034783,3.06971542556511,13.0620990110482));
#13969=CARTESIAN_POINT('Ctrl Pts',(0.95928224087124,3.07668600449792,13.0635169452393));
#13970=CARTESIAN_POINT('Ctrl Pts',(0.94965359443676,3.07967161152451,13.0641349313674));
#13971=CARTESIAN_POINT('Ctrl Pts',(0.929639846959014,3.08577460037859,13.0654207142771));
#13972=CARTESIAN_POINT('Ctrl Pts',(0.919252717725339,3.08888484177537,13.0660887365144));
#13973=CARTESIAN_POINT('Ctrl Pts',(0.892398724783401,3.09677834432983,13.0678176877604));
#13974=CARTESIAN_POINT('Ctrl Pts',(0.875909188204659,3.10148265731174,13.0688811833354));
#13975=CARTESIAN_POINT('Ctrl Pts',(0.80553621599143,3.12095344735486,13.073428263993));
#13976=CARTESIAN_POINT('Ctrl Pts',(0.751313908730492,3.13444824425033,13.0769528260938));
#13977=CARTESIAN_POINT('Ctrl Pts',(0.607519783942016,3.16629020183804,13.0863608591637));
#13978=CARTESIAN_POINT('Ctrl Pts',(0.517475562756523,3.1822461390512,13.092315063787));
#13979=CARTESIAN_POINT('Ctrl Pts',(0.181828556465332,3.22710074705305,13.1147111154533));
#13980=CARTESIAN_POINT('Ctrl Pts',(-0.0661520216945494,3.23153973885737,
13.1317283138849));
#13981=CARTESIAN_POINT('Ctrl Pts',(-0.400370352298577,3.19901090298698,
13.1540405549022));
#13982=CARTESIAN_POINT('Ctrl Pts',(-0.488169418444432,3.18679476766393,
13.1598327232073));
#13983=CARTESIAN_POINT('Ctrl Pts',(-0.588947421548988,3.16850898024592,
13.1663194270417));
#13984=CARTESIAN_POINT('Ctrl Pts',(-0.60251788651561,3.16595648039392,13.1671894676034));
#13985=CARTESIAN_POINT('Ctrl Pts',(-0.6229908642707,3.161969265294,13.168496414642));
#13986=CARTESIAN_POINT('Ctrl Pts',(-0.629905557544051,3.16059903221658,
13.1689368594266));
#13987=CARTESIAN_POINT('Ctrl Pts',(-0.642284943777616,3.15810366211542,
13.169723575349));
#13988=CARTESIAN_POINT('Ctrl Pts',(-0.647751239821438,3.15698701652705,
13.1700703225124));
#13989=CARTESIAN_POINT('Ctrl Pts',(-0.65960229246785,3.15453402693439,13.1708206840841));
#13990=CARTESIAN_POINT('Ctrl Pts',(-0.665985880647245,3.15319249648276,
13.1712239972947));
#13991=CARTESIAN_POINT('Ctrl Pts',(-0.68386075064628,3.14937933447135,13.1723509983891));
#13992=CARTESIAN_POINT('Ctrl Pts',(-0.695342787437986,3.14686417510242,
13.1730722354391));
#13993=CARTESIAN_POINT('Ctrl Pts',(-0.763125691563052,3.13162710701117,
13.1773153860123));
#13994=CARTESIAN_POINT('Ctrl Pts',(-0.819094224153468,3.11745645817755,
13.1807594064041));
#13995=CARTESIAN_POINT('Ctrl Pts',(-1.11807584950103,3.03314833711307,13.1989827462395));
#13996=CARTESIAN_POINT('Ctrl Pts',(-1.35259168286045,2.93608661492708,13.212710164885));
#13997=CARTESIAN_POINT('Ctrl Pts',(-1.7159561714079,2.73282052353992,13.2362306927792));
#13998=CARTESIAN_POINT('Ctrl Pts',(-1.85225995471956,2.64233538428435,13.2456473779133));
#13999=CARTESIAN_POINT('Ctrl Pts',(-1.99837559765314,2.5284564246973,13.2567898231132));
#14000=CARTESIAN_POINT('Ctrl Pts',(-2.01550655745929,2.51482210136046,13.2581134405736));
#14001=CARTESIAN_POINT('Ctrl Pts',(-2.04265555215683,2.49275895538259,13.2602395799217));
#14002=CARTESIAN_POINT('Ctrl Pts',(-2.05276364388935,2.48444165332742,13.2610376058395));
#14003=CARTESIAN_POINT('Ctrl Pts',(-2.07056414831487,2.46961196320611,13.2624545108718));
#14004=CARTESIAN_POINT('Ctrl Pts',(-2.07827725280712,2.46312460056263,13.2630723619367));
#14005=CARTESIAN_POINT('Ctrl Pts',(-2.0942297717035,2.44957892952702,13.2643584111904));
#14006=CARTESIAN_POINT('Ctrl Pts',(-2.10246421739755,2.44251499046088,13.2650268375547));
#14007=CARTESIAN_POINT('Ctrl Pts',(-2.12364300702489,2.42416026231451,13.2667580111607));
#14008=CARTESIAN_POINT('Ctrl Pts',(-2.1365329057906,2.41280743589956,13.2678233375172));
#14009=CARTESIAN_POINT('Ctrl Pts',(-2.19115875263822,2.36391455179486,13.2723888584959));
#14010=CARTESIAN_POINT('Ctrl Pts',(-2.23199868794235,2.32539241957981,13.2759304447597));
#14011=CARTESIAN_POINT('Ctrl Pts',(-2.33707735928795,2.22095803410522,13.2853954695223));
#14012=CARTESIAN_POINT('Ctrl Pts',(-2.39953127467968,2.15333051479323,13.2913907120885));
#14013=CARTESIAN_POINT('Ctrl Pts',(-2.61529386198287,1.89863637644144,13.3134736964007));
#14014=CARTESIAN_POINT('Ctrl Pts',(-2.75031097836682,1.69716138434015,13.3301016764129));
#14015=CARTESIAN_POINT('Ctrl Pts',(-2.90423618238228,1.40005384004871,13.3523702712656));
#14016=CARTESIAN_POINT('Ctrl Pts',(-2.94336952550922,1.31579553520197,13.3584499966489));
#14017=CARTESIAN_POINT('Ctrl Pts',(-2.9841383347074,1.2170582155401,13.3652165204361));
#14018=CARTESIAN_POINT('Ctrl Pts',(-2.98938046256159,1.20412489689205,13.3660959289163));
#14019=CARTESIAN_POINT('Ctrl Pts',(-2.99715551093824,1.18457863310282,13.3674141418255));
#14020=CARTESIAN_POINT('Ctrl Pts',(-2.99975083732108,1.17799092144918,13.3678565739394));
#14021=CARTESIAN_POINT('Ctrl Pts',(-3.00435321270779,1.16619487613558,13.3686454296903));
#14022=CARTESIAN_POINT('Ctrl Pts',(-3.00636845474568,1.16098984996485,13.3689923404721));
#14023=CARTESIAN_POINT('Ctrl Pts',(-3.0107012684395,1.14971199999952,13.3697414534169));
#14024=CARTESIAN_POINT('Ctrl Pts',(-3.01301398687422,1.14363741080339,13.3701433630243));
#14025=CARTESIAN_POINT('Ctrl Pts',(-3.01941982053713,1.12665752850819,13.371262483001));
#14026=CARTESIAN_POINT('Ctrl Pts',(-3.02347226392441,1.11573684985899,13.3719772975185));
#14027=CARTESIAN_POINT('Ctrl Pts',(-3.04664464720478,1.05223761393905,13.3761062909239));
#14028=CARTESIAN_POINT('Ctrl Pts',(-3.06445335346116,0.999186731959985,
13.379447381951));
#14029=CARTESIAN_POINT('Ctrl Pts',(-3.15546951366754,0.702675608467921,
13.397664270947));
#14030=CARTESIAN_POINT('Ctrl Pts',(-3.20105776246953,0.451660785888588,
13.411459238772));
#14031=CARTESIAN_POINT('Ctrl Pts',(-3.226741044131,0.0341526453691606,13.4350857161843));
#14032=CARTESIAN_POINT('Ctrl Pts',(-3.22429731215423,-0.13007899355528,
13.4445375580286));
#14033=CARTESIAN_POINT('Ctrl Pts',(-3.20737233354436,-0.315214528777687,
13.4557193283967));
#14034=CARTESIAN_POINT('Ctrl Pts',(-3.20515555615476,-0.337009361427066,
13.4570437139644));
#14035=CARTESIAN_POINT('Ctrl Pts',(-3.20125908316678,-0.371792005362685,
13.4591708540761));
#14036=CARTESIAN_POINT('Ctrl Pts',(-3.19972210333762,-0.384795356365263,
13.4599691058792));
#14037=CARTESIAN_POINT('Ctrl Pts',(-3.19686184889068,-0.407790966154418,
13.4613862723029));
#14038=CARTESIAN_POINT('Ctrl Pts',(-3.19557085247388,-0.41778711818746,
13.4620041576086));
#14039=CARTESIAN_POINT('Ctrl Pts',(-3.1927931209413,-0.438528585214108,
13.4632901388356));
#14040=CARTESIAN_POINT('Ctrl Pts',(-3.19129898494474,-0.449272764881063,
13.4639584622399));
#14041=CARTESIAN_POINT('Ctrl Pts',(-3.18729995129729,-0.477002478016162,
13.4656890697067));
#14042=CARTESIAN_POINT('Ctrl Pts',(-3.18471353451077,-0.493975736538595,
13.466753929685));
#14043=CARTESIAN_POINT('Ctrl Pts',(-3.17310287998171,-0.566285454392075,
13.4713147460004));
#14044=CARTESIAN_POINT('Ctrl Pts',(-3.16277148365997,-0.621399233831103,
13.4748519879831));
#14045=CARTESIAN_POINT('Ctrl Pts',(-3.13173288046499,-0.766032537866834,
13.4843024573245));
#14046=CARTESIAN_POINT('Ctrl Pts',(-3.10862736737544,-0.854979565707767,
13.4902872144924));
#14047=CARTESIAN_POINT('Ctrl Pts',(-3.01055241267302,-1.17555576173496,
13.512463997259));
#14048=CARTESIAN_POINT('Ctrl Pts',(-2.91322060300083,-1.39945983489746,
13.5292063073026));
#14049=CARTESIAN_POINT('Ctrl Pts',(-2.74587375349919,-1.68957946321284,
13.5514852062674));
#14050=CARTESIAN_POINT('Ctrl Pts',(-2.69675930457981,-1.76691653965921,
13.5574778785254));
#14051=CARTESIAN_POINT('Ctrl Pts',(-2.63646091979439,-1.85347914125896,
13.5641598756857));
#14052=CARTESIAN_POINT('Ctrl Pts',(-2.62843502575435,-1.86484327505048,
13.5650365556203));
#14053=CARTESIAN_POINT('Ctrl Pts',(-2.61621900121881,-1.88190480720376,
13.5663514883278));
#14054=CARTESIAN_POINT('Ctrl Pts',(-2.61208341909765,-1.8876407973064,13.5667933426496));
#14055=CARTESIAN_POINT('Ctrl Pts',(-2.60465021961238,-1.89787932742662,
13.5675815750426));
#14056=CARTESIAN_POINT('Ctrl Pts',(-2.60135976719143,-1.9023869404529,13.5679284370278));
#14057=CARTESIAN_POINT('Ctrl Pts',(-2.59420767441188,-1.91213138646455,
13.5686779073967));
#14058=CARTESIAN_POINT('Ctrl Pts',(-2.59034189091565,-1.91736506357444,
13.5690802207338));
#14059=CARTESIAN_POINT('Ctrl Pts',(-2.57949324415851,-1.93195976996552,
13.5702016059116));
#14060=CARTESIAN_POINT('Ctrl Pts',(-2.5724752253207,-1.94129471597344,13.5709182661558));
#14061=CARTESIAN_POINT('Ctrl Pts',(-2.53124006064151,-1.99552696332442,
13.5750796493784));
#14062=CARTESIAN_POINT('Ctrl Pts',(-2.49589644752285,-2.0395602294932,13.5784499375394));
#14063=CARTESIAN_POINT('Ctrl Pts',(-2.29537316687291,-2.2763597204278,13.596668358589));
#14064=CARTESIAN_POINT('Ctrl Pts',(-2.10900786186528,-2.45003357393953,
13.6104439451503));
#14065=CARTESIAN_POINT('Ctrl Pts',(-1.77204017750306,-2.69681563626451,
13.6340360711576));
#14066=CARTESIAN_POINT('Ctrl Pts',(-1.63274012608523,-2.78335952069482,
13.643473722262));
#14067=CARTESIAN_POINT('Ctrl Pts',(-1.48340867397894,-2.86105528026574,
13.6535982023777));
#14068=CARTESIAN_POINT('Ctrl Pts',(-1.47933426699413,-2.86316411275432,
13.6538744332376));
#14069=CARTESIAN_POINT('Ctrl Pts',(-1.4752554049854,-2.86526422037504,13.6541509617524));
#14070=CARTESIAN_POINT('Origin',(0.,0.,4.68922655072688));
#14071=CARTESIAN_POINT('',(-1.47525540626678,-2.86526421971528,15.1508554073139));
#14072=CARTESIAN_POINT('',(-1.47525516809587,-2.86526434234373,14.9065719799118));
#14073=CARTESIAN_POINT('',(-1.47525540501186,-2.86526422036142,4.68922655072688));
#14074=CARTESIAN_POINT('Ctrl Pts',(-1.47525540626678,-2.86526421971528,
15.1508554073139));
#14075=CARTESIAN_POINT('Ctrl Pts',(-1.50339105412724,-2.85077785356121,
15.1488133657421));
#14076=CARTESIAN_POINT('Ctrl Pts',(-1.53131412858722,-2.83587665466912,
15.1467909671531));
#14077=CARTESIAN_POINT('Ctrl Pts',(-1.56922412136404,-2.81492260591201,
15.1440556586238));
#14078=CARTESIAN_POINT('Ctrl Pts',(-1.57940231774181,-2.80922443903595,
15.1433223176556));
#14079=CARTESIAN_POINT('Ctrl Pts',(-1.59520807439074,-2.80026267955658,
15.1421854088157));
#14080=CARTESIAN_POINT('Ctrl Pts',(-1.60085694755529,-2.79703716642421,
15.1417794653858));
#14081=CARTESIAN_POINT('Ctrl Pts',(-1.61133619693371,-2.79101135716602,
15.1410271619145));
#14082=CARTESIAN_POINT('Ctrl Pts',(-1.61616901541381,-2.78821563902556,
15.1406805245355));
#14083=CARTESIAN_POINT('Ctrl Pts',(-1.6271133574999,-2.78184647353503,15.1398962141376));
#14084=CARTESIAN_POINT('Ctrl Pts',(-1.63322037227713,-2.77826544777702,
15.1394590402937));
#14085=CARTESIAN_POINT('Ctrl Pts',(-1.65132034225001,-2.76757169884925,
15.1381646104348));
#14086=CARTESIAN_POINT('Ctrl Pts',(-1.66327917396285,-2.7604011278715,15.1373110245124));
#14087=CARTESIAN_POINT('Ctrl Pts',(-1.75411951229551,-2.70512815644969,
15.1308368158665));
#14088=CARTESIAN_POINT('Ctrl Pts',(-1.8309541822147,-2.6537264037884,15.1254165093946));
#14089=CARTESIAN_POINT('Ctrl Pts',(-2.10092552907359,-2.45580118795912,
15.1061741392801));
#14090=CARTESIAN_POINT('Ctrl Pts',(-2.27959126223985,-2.29092211366912,
15.0929979577751));
#14091=CARTESIAN_POINT('Ctrl Pts',(-2.49822154229909,-2.03800410913888,
15.0739653603523));
#14092=CARTESIAN_POINT('Ctrl Pts',(-2.55534259492575,-1.96590791113413,
15.0686583249957));
#14093=CARTESIAN_POINT('Ctrl Pts',(-2.64223063083345,-1.84604519517854,
15.0599287925599));
#14094=CARTESIAN_POINT('Ctrl Pts',(-2.67396703037729,-1.79976812756134,
15.0565798320844));
#14095=CARTESIAN_POINT('Ctrl Pts',(-2.71381987443033,-1.73827337098048,
15.0521454975276));
#14096=CARTESIAN_POINT('Ctrl Pts',(-2.7230462002902,-1.72378420819638,15.0511018392976));
#14097=CARTESIAN_POINT('Ctrl Pts',(-2.73791153667383,-1.70002227725716,
15.0493917982837));
#14098=CARTESIAN_POINT('Ctrl Pts',(-2.74362039425488,-1.6907934390385,15.0487280143001));
#14099=CARTESIAN_POINT('Ctrl Pts',(-2.75454327758538,-1.67293471275003,
15.0474441623079));
#14100=CARTESIAN_POINT('Ctrl Pts',(-2.75976363640794,-1.66430883212461,
15.0468243374637));
#14101=CARTESIAN_POINT('Ctrl Pts',(-2.77167210792768,-1.64442173216434,
15.0453959003581));
#14102=CARTESIAN_POINT('Ctrl Pts',(-2.77833218598325,-1.63314401179675,
15.0445862750852));
#14103=CARTESIAN_POINT('Ctrl Pts',(-2.79595006120658,-1.60289142846693,
15.0424154126279));
#14104=CARTESIAN_POINT('Ctrl Pts',(-2.80678324777666,-1.58384514328681,
15.0410496931151));
#14105=CARTESIAN_POINT('Ctrl Pts',(-2.89705248471956,-1.42130405278582,
15.0294011727022));
#14106=CARTESIAN_POINT('Ctrl Pts',(-2.96560938703671,-1.27207096805266,
15.0187303653674));
#14107=CARTESIAN_POINT('Ctrl Pts',(-3.11082541207775,-0.879581921124254,
14.9908172214239));
#14108=CARTESIAN_POINT('Ctrl Pts',(-3.17055178420517,-0.631265207656641,
14.973246866533));
#14109=CARTESIAN_POINT('Ctrl Pts',(-3.20698716349528,-0.323193508378476,
14.9529593616129));
#14110=CARTESIAN_POINT('Ctrl Pts',(-3.21209489830478,-0.267708730078014,
14.9493679436506));
#14111=CARTESIAN_POINT('Ctrl Pts',(-3.21652775534488,-0.200504765022391,
14.9451150615929));
#14112=CARTESIAN_POINT('Ctrl Pts',(-3.21723074828495,-0.188889607286423,
14.9443835186858));
#14113=CARTESIAN_POINT('Ctrl Pts',(-3.21822829277222,-0.170781879985132,
14.9432487846746));
#14114=CARTESIAN_POINT('Ctrl Pts',(-3.21856613362683,-0.164291935809402,
14.9428432323927));
#14115=CARTESIAN_POINT('Ctrl Pts',(-3.21915776009772,-0.152223711706366,
14.9420912812633));
#14116=CARTESIAN_POINT('Ctrl Pts',(-3.21941667674598,-0.146645848885181,
14.9417446074122));
#14117=CARTESIAN_POINT('Ctrl Pts',(-3.21997135556272,-0.13398608289893,
14.9409597395251));
#14118=CARTESIAN_POINT('Ctrl Pts',(-3.22025825199285,-0.126903876196469,
14.9405220476225));
#14119=CARTESIAN_POINT('Ctrl Pts',(-3.221041680693,-0.105847003915736,14.9392246596969));
#14120=CARTESIAN_POINT('Ctrl Pts',(-3.22147063581203,-0.0918697775634275,
14.9383686586757));
#14121=CARTESIAN_POINT('Ctrl Pts',(-3.22407146658485,0.0157099974861362,
14.9318170610924));
#14122=CARTESIAN_POINT('Ctrl Pts',(-3.22225457462109,0.109373870880423,
14.9263272341586));
#14123=CARTESIAN_POINT('Ctrl Pts',(-3.20120368336465,0.44317932895907,14.9071124929251));
#14124=CARTESIAN_POINT('Ctrl Pts',(-3.15915526917128,0.681075111207615,
14.894014257169));
#14125=CARTESIAN_POINT('Ctrl Pts',(-3.06493090883859,1.00039791195416,14.8750615227365));
#14126=CARTESIAN_POINT('Ctrl Pts',(-3.03509761190753,1.08755597849624,14.869746727306));
#14127=CARTESIAN_POINT('Ctrl Pts',(-2.98112607902476,1.2256262665161,14.8610055967566));
#14128=CARTESIAN_POINT('Ctrl Pts',(-2.95931365455275,1.27739365887942,14.8576530543894));
#14129=CARTESIAN_POINT('Ctrl Pts',(-2.92907662560662,1.34421835114289,14.8532146368152));
#14130=CARTESIAN_POINT('Ctrl Pts',(-2.9218675900796,1.3598171283211,14.8521705750905));
#14131=CARTESIAN_POINT('Ctrl Pts',(-2.90990241961235,1.38517264855677,14.8504600390333));
#14132=CARTESIAN_POINT('Ctrl Pts',(-2.90522107490098,1.39496446527128,14.8497961664049));
#14133=CARTESIAN_POINT('Ctrl Pts',(-2.89609583320821,1.41380625806437,14.8485122595942));
#14134=CARTESIAN_POINT('Ctrl Pts',(-2.8916587482981,1.42285940632668,14.8478924692038));
#14135=CARTESIAN_POINT('Ctrl Pts',(-2.88136149032117,1.44362217358492,14.846464278664));
#14136=CARTESIAN_POINT('Ctrl Pts',(-2.87547231665418,1.45531713588244,14.8456548666459));
#14137=CARTESIAN_POINT('Ctrl Pts',(-2.85954343532276,1.4864751955103,14.8434849478338));
#14138=CARTESIAN_POINT('Ctrl Pts',(-2.84937647052493,1.50587212483134,14.842119964833));
#14139=CARTESIAN_POINT('Ctrl Pts',(-2.76166897843788,1.66913507012453,14.8305088107152));
#14140=CARTESIAN_POINT('Ctrl Pts',(-2.67349814897883,1.80699211393752,14.8198775059535));
#14141=CARTESIAN_POINT('Ctrl Pts',(-2.42296518032278,2.13998406775255,14.7920872954272));
#14142=CARTESIAN_POINT('Ctrl Pts',(-2.24733465651383,2.32374137579747,14.7746028751454));
#14143=CARTESIAN_POINT('Ctrl Pts',(-2.00779899942243,2.52153668333864,14.7542691674285));
#14144=CARTESIAN_POINT('Ctrl Pts',(-1.96262438345589,2.55685560014849,14.7505705877408));
#14145=CARTESIAN_POINT('Ctrl Pts',(-1.90709491950525,2.59793075562248,14.7462085142417));
#14146=CARTESIAN_POINT('Ctrl Pts',(-1.89762328979931,2.60485721355607,14.7454707617328));
#14147=CARTESIAN_POINT('Ctrl Pts',(-1.88283009242172,2.61555174198484,14.7443285183764));
#14148=CARTESIAN_POINT('Ctrl Pts',(-1.87753467845655,2.61935557053818,14.743921616532));
#14149=CARTESIAN_POINT('Ctrl Pts',(-1.86768448521687,2.62638599253376,14.7431684447596));
#14150=CARTESIAN_POINT('Ctrl Pts',(-1.86313290980243,2.62961679323124,14.7428218917869));
#14151=CARTESIAN_POINT('Ctrl Pts',(-1.85280611240399,2.63690669147152,14.7420389248222));
#14152=CARTESIAN_POINT('Ctrl Pts',(-1.84702594869169,2.64095863973448,14.7416030028516));
#14153=CARTESIAN_POINT('Ctrl Pts',(-1.82986782707738,2.65290275715568,14.7403157077876));
#14154=CARTESIAN_POINT('Ctrl Pts',(-1.81845209451341,2.66074074261734,14.7394679450505));
#14155=CARTESIAN_POINT('Ctrl Pts',(-1.7328007421428,2.71873980476605,14.7331691478427));
#14156=CARTESIAN_POINT('Ctrl Pts',(-1.65654543491967,2.76586422762953,14.7279063671988));
#14157=CARTESIAN_POINT('Ctrl Pts',(-1.36402972012538,2.93018900306362,14.7085940471418));
#14158=CARTESIAN_POINT('Ctrl Pts',(-1.13655495339117,3.02569688703108,14.6952357524548));
#14159=CARTESIAN_POINT('Ctrl Pts',(-0.812507264135596,3.11998917228078,
14.6760190515784));
#14160=CARTESIAN_POINT('Ctrl Pts',(-0.723550771799499,3.14181044292119,
14.6707334484948));
#14161=CARTESIAN_POINT('Ctrl Pts',(-0.578945280369275,3.17081518860871,
14.6620359581591));
#14162=CARTESIAN_POINT('Ctrl Pts',(-0.523825492131568,3.18038564959663,
14.6586969026522));
#14163=CARTESIAN_POINT('Ctrl Pts',(-0.451510534592544,3.19101084617937,
14.6542738603294));
#14164=CARTESIAN_POINT('Ctrl Pts',(-0.434514719841401,3.1933695250957,14.6532313200056));
#14165=CARTESIAN_POINT('Ctrl Pts',(-0.406744766683932,3.19699764334492,
14.6515226504859));
#14166=CARTESIAN_POINT('Ctrl Pts',(-0.395981480669193,3.19834862064699,
14.6508591120512));
#14167=CARTESIAN_POINT('Ctrl Pts',(-0.375199898331274,3.20085055687497,
14.6495754113896));
#14168=CARTESIAN_POINT('Ctrl Pts',(-0.365182604606776,3.20200888705172,
14.6489554905865));
#14169=CARTESIAN_POINT('Ctrl Pts',(-0.34213300609411,3.20456461332747,14.6475263680116));
#14170=CARTESIAN_POINT('Ctrl Pts',(-0.329097349809334,3.20592955023028,
14.646716150051));
#14171=CARTESIAN_POINT('Ctrl Pts',(-0.294215746842355,3.20936694571269,
14.6445426642336));
#14172=CARTESIAN_POINT('Ctrl Pts',(-0.272356650780918,3.21129583100458,
14.6431748970083));
#14173=CARTESIAN_POINT('Ctrl Pts',(-0.0853272305184408,3.2258763190808,
14.6314213156921));
#14174=CARTESIAN_POINT('Ctrl Pts',(0.0805460206602419,3.22599689259224,
14.6206393536959));
#14175=CARTESIAN_POINT('Ctrl Pts',(0.503473688447166,3.1936627652405,14.5923356825053));
#14176=CARTESIAN_POINT('Ctrl Pts',(0.757954184321514,3.14300323557174,14.5744755283569));
#14177=CARTESIAN_POINT('Ctrl Pts',(1.05171302553985,3.0467320410251,14.554318903552));
#14178=CARTESIAN_POINT('Ctrl Pts',(1.09940831273505,3.02984792670845,14.5510649552143));
#14179=CARTESIAN_POINT('Ctrl Pts',(1.15725380517517,3.00782462571468,14.5471582234709));
#14180=CARTESIAN_POINT('Ctrl Pts',(1.16779723625433,3.00374682232084,14.5464477858425));
#14181=CARTESIAN_POINT('Ctrl Pts',(1.18430019639621,2.99726406911535,14.5453386036452));
#14182=CARTESIAN_POINT('Ctrl Pts',(1.1902742387872,2.99489667491003,14.5449376639284));
#14183=CARTESIAN_POINT('Ctrl Pts',(1.2014349441305,2.99043523968144,14.5441897731953));
#14184=CARTESIAN_POINT('Ctrl Pts',(1.2066231782339,2.98834558812232,14.5438425749318));
#14185=CARTESIAN_POINT('Ctrl Pts',(1.21847190045648,2.9835374206574,14.5430507033294));
#14186=CARTESIAN_POINT('Ctrl Pts',(1.22512873213765,2.98081010879967,14.5426065688496));
#14187=CARTESIAN_POINT('Ctrl Pts',(1.24562891452724,2.97233088484343,14.5412409873636));
#14188=CARTESIAN_POINT('Ctrl Pts',(1.25944154235226,2.96650455978889,14.5403239331994));
#14189=CARTESIAN_POINT('Ctrl Pts',(1.40021749197162,2.90596314659321,14.5310037639977));
#14190=CARTESIAN_POINT('Ctrl Pts',(1.52359270871539,2.84322105364998,14.5230524076603));
#14191=CARTESIAN_POINT('Ctrl Pts',(1.81102563186235,2.67294592726262,14.5041794323046));
#14192=CARTESIAN_POINT('Ctrl Pts',(1.9700354429281,2.55801005983356,14.4934182845393));
#14193=CARTESIAN_POINT('Ctrl Pts',(2.18656143945151,2.3692674185386,14.4770617588059));
#14194=CARTESIAN_POINT('Ctrl Pts',(2.25289793568172,2.30628012515123,14.4717826406863));
#14195=CARTESIAN_POINT('Ctrl Pts',(2.3553176227157,2.20039081953556,14.4630948484355));
#14196=CARTESIAN_POINT('Ctrl Pts',(2.39311833593905,2.1592185907574,14.4597587935222));
#14197=CARTESIAN_POINT('Ctrl Pts',(2.44109605235173,2.104153476444,14.4553391724874));
#14198=CARTESIAN_POINT('Ctrl Pts',(2.45226060736853,2.09113119748398,14.4542969714381));
#14199=CARTESIAN_POINT('Ctrl Pts',(2.47031432354651,2.06973001926472,14.4525887181388));
#14200=CARTESIAN_POINT('Ctrl Pts',(2.4772661710729,2.06140425993392,14.4519252542121));
#14201=CARTESIAN_POINT('Ctrl Pts',(2.49060011213333,2.0452702368466,14.4506415993182));
#14202=CARTESIAN_POINT('Ctrl Pts',(2.49698785343683,2.03746678902714,14.4500216492459));
#14203=CARTESIAN_POINT('Ctrl Pts',(2.51159516002398,2.01945021786906,14.4485923179534));
#14204=CARTESIAN_POINT('Ctrl Pts',(2.5197891995872,2.00921671598342,14.447781919577));
#14205=CARTESIAN_POINT('Ctrl Pts',(2.54153746830639,1.98171310447695,14.4456076349857));
#14206=CARTESIAN_POINT('Ctrl Pts',(2.55497786207329,1.96435424937896,14.4442392442077));
#14207=CARTESIAN_POINT('Ctrl Pts',(2.66861553936937,1.81444680034196,14.4324533520043));
#14208=CARTESIAN_POINT('Ctrl Pts',(2.75858503908641,1.67449078483124,14.4216371797868));
#14209=CARTESIAN_POINT('Ctrl Pts',(2.96069130823641,1.29925766384464,14.3931936983065));
#14210=CARTESIAN_POINT('Ctrl Pts',(3.05584877054075,1.05619525443937,14.375223223154));
#14211=CARTESIAN_POINT('Ctrl Pts',(3.13293175692409,0.75712231556495,14.3551072395965));
#14212=CARTESIAN_POINT('Ctrl Pts',(3.1440301257356,0.709627208834215,14.3519729341825));
#14213=CARTESIAN_POINT('Ctrl Pts',(3.15634241069869,0.650957041462287,14.3481898157189));
#14214=CARTESIAN_POINT('Ctrl Pts',(3.15858104788213,0.640006449990388,14.347487481503));
#14215=CARTESIAN_POINT('Ctrl Pts',(3.16201150077367,0.622769431052952,14.3463881211525));
#14216=CARTESIAN_POINT('Ctrl Pts',(3.16324161783913,0.616490846762013,14.3459889622682));
#14217=CARTESIAN_POINT('Ctrl Pts',(3.16551294518215,0.604712073078155,14.345242588961));
#14218=CARTESIAN_POINT('Ctrl Pts',(3.16655851047992,0.599212898481066,14.344895138132));
#14219=CARTESIAN_POINT('Ctrl Pts',(3.16892310176718,0.586597237913914,14.3441003339719));
#14220=CARTESIAN_POINT('Ctrl Pts',(3.17023248466124,0.57947902468446,14.343653534667));
#14221=CARTESIAN_POINT('Ctrl Pts',(3.17360635588108,0.560783866688975,14.3424842743218));
#14222=CARTESIAN_POINT('Ctrl Pts',(3.17563150121193,0.549199804760954,14.3417639941961));
#14223=CARTESIAN_POINT('Ctrl Pts',(3.18900098468622,0.470177468897702,14.3368776879659));
#14224=CARTESIAN_POINT('Ctrl Pts',(3.19826062185061,0.402398617924862,14.3328213043519));
#14225=CARTESIAN_POINT('Ctrl Pts',(3.21684428002505,0.224251511214762,14.3223912062999));
#14226=CARTESIAN_POINT('Ctrl Pts',(3.2226499711397,0.113605529013144,14.3161424827816));
#14227=CARTESIAN_POINT('Ctrl Pts',(3.22299534989345,-0.273689037745909,
14.2944381621487));
#14228=CARTESIAN_POINT('Ctrl Pts',(3.18764473413559,-0.549099614211858,
14.2791890572757));
#14229=CARTESIAN_POINT('Ctrl Pts',(3.10884493051252,-0.849933776056677,
14.2606250515512));
#14230=CARTESIAN_POINT('Ctrl Pts',(3.09958271938353,-0.883114405255533,
14.2585524761388));
#14231=CARTESIAN_POINT('Ctrl Pts',(3.08603519401101,-0.928805076754244,
14.2556611436774));
#14232=CARTESIAN_POINT('Ctrl Pts',(3.08220190956416,-0.941447539609258,
14.2548571375493));
#14233=CARTESIAN_POINT('Ctrl Pts',(3.07547746808638,-0.963143931143572,
14.253470330583));
#14234=CARTESIAN_POINT('Ctrl Pts',(3.07262377140076,-0.972209362825783,
14.2528887652637));
#14235=CARTESIAN_POINT('Ctrl Pts',(3.0666559576345,-0.990878768031159,14.2516866607862));
#14236=CARTESIAN_POINT('Ctrl Pts',(3.06353672878398,-1.00048098588582,14.251065958442));
#14237=CARTESIAN_POINT('Ctrl Pts',(3.05616870473473,-1.02280511766972,14.249617163114));
#14238=CARTESIAN_POINT('Ctrl Pts',(3.0518855303556,-1.03551540857386,14.2487879392545));
#14239=CARTESIAN_POINT('Ctrl Pts',(3.03789943316742,-1.07617846807766,14.2461208861781));
#14240=CARTESIAN_POINT('Ctrl Pts',(3.02789106684941,-1.10402384674811,14.2442729442098));
#14241=CARTESIAN_POINT('Ctrl Pts',(2.97572489536693,-1.24311349402467,14.2349308282727));
#14242=CARTESIAN_POINT('Ctrl Pts',(2.92781828379777,-1.35208881722406,14.2272454491624));
#14243=CARTESIAN_POINT('Ctrl Pts',(2.76831963433682,-1.66645801582727,14.2039853799899));
#14244=CARTESIAN_POINT('Ctrl Pts',(2.64030524265051,-1.86264539643857,14.1879612020676));
#14245=CARTESIAN_POINT('Ctrl Pts',(2.47296104969265,-2.06676210755497,14.1703051787076));
#14246=CARTESIAN_POINT('Ctrl Pts',(2.45335248969851,-2.09000086301943,14.1682801521482));
#14247=CARTESIAN_POINT('Ctrl Pts',(2.41701406412699,-2.13185049537101,14.1646106264563));
#14248=CARTESIAN_POINT('Ctrl Pts',(2.40039070634963,-2.15055063593615,14.1629623828965));
#14249=CARTESIAN_POINT('Ctrl Pts',(2.34532669873475,-2.21105985284406,14.1576058036567));
#14250=CARTESIAN_POINT('Ctrl Pts',(2.3059960170692,-2.25204935512446,14.1539400791037));
#14251=CARTESIAN_POINT('Ctrl Pts',(2.2576932531644,-2.29979615008754,14.1496473403914));
#14252=CARTESIAN_POINT('Ctrl Pts',(2.24974622524655,-2.3075708196659,14.1489476063431));
#14253=CARTESIAN_POINT('Ctrl Pts',(2.23669897287542,-2.32020362770557,14.1478096559964));
#14254=CARTESIAN_POINT('Ctrl Pts',(2.23162285122013,-2.32508636859612,14.1473695828788));
#14255=CARTESIAN_POINT('Ctrl Pts',(2.22249613133527,-2.33380797223854,14.1465831549406));
#14256=CARTESIAN_POINT('Ctrl Pts',(2.21845154903182,-2.33765297493322,14.1462363267225));
#14257=CARTESIAN_POINT('Ctrl Pts',(2.20965136206051,-2.34597550766676,14.145485352874));
#14258=CARTESIAN_POINT('Ctrl Pts',(2.20489214134958,-2.35044907862963,14.1450815110214));
#14259=CARTESIAN_POINT('Ctrl Pts',(2.19150605257617,-2.36295529536825,14.143951935974));
#14260=CARTESIAN_POINT('Ctrl Pts',(2.18284856247672,-2.37095522304369,14.1432286706289));
#14261=CARTESIAN_POINT('Ctrl Pts',(2.13115289384639,-2.41820127563144,14.1389515972645));
#14262=CARTESIAN_POINT('Ctrl Pts',(2.08709807058008,-2.45632503810693,14.1354771312879));
#14263=CARTESIAN_POINT('Ctrl Pts',(1.84658336666752,-2.65331337390348,14.1172456147136));
#14264=CARTESIAN_POINT('Ctrl Pts',(1.63297405866927,-2.78986807681687,14.1035328353902));
#14265=CARTESIAN_POINT('Ctrl Pts',(1.2588326929012,-2.97120411423322,14.0800435652225));
#14266=CARTESIAN_POINT('Ctrl Pts',(1.10690998547183,-3.03108125812217,14.0706436644758));
#14267=CARTESIAN_POINT('Ctrl Pts',(0.930203326758145,-3.0856634037397,14.0595196947244));
#14268=CARTESIAN_POINT('Ctrl Pts',(0.909220502564736,-3.09191120696827,
14.0581961468508));
#14269=CARTESIAN_POINT('Ctrl Pts',(0.875590912336023,-3.1015527596343,14.0560699568057));
#14270=CARTESIAN_POINT('Ctrl Pts',(0.862984064630332,-3.10508413135876,
14.0552718091158));
#14271=CARTESIAN_POINT('Ctrl Pts',(0.840631727694044,-3.11119872439373,
14.0538545893563));
#14272=CARTESIAN_POINT('Ctrl Pts',(0.830894921563278,-3.11381322977578,
14.0532365451839));
#14273=CARTESIAN_POINT('Ctrl Pts',(0.810650124066179,-3.11914760037152,
14.0519499948551));
#14274=CARTESIAN_POINT('Ctrl Pts',(0.800140352792831,-3.12186014865646,
14.051281259878));
#14275=CARTESIAN_POINT('Ctrl Pts',(0.772953131985983,-3.12873080395834,
14.0495490714257));
#14276=CARTESIAN_POINT('Ctrl Pts',(0.756255926453349,-3.13280863493769,
14.0484830347467));
#14277=CARTESIAN_POINT('Ctrl Pts',(0.684822972502983,-3.14964981285136,
14.0439124609492));
#14278=CARTESIAN_POINT('Ctrl Pts',(0.629793767883843,-3.16111303426801,
14.0403664257195));
#14279=CARTESIAN_POINT('Ctrl Pts',(0.483802916525641,-3.18756136045126,
14.0308870724698));
#14280=CARTESIAN_POINT('Ctrl Pts',(0.392454608034174,-3.20009211266829,
14.0248816930956));
#14281=CARTESIAN_POINT('Ctrl Pts',(0.061812681645723,-3.23107811296798,
14.0029101681072));
#14282=CARTESIAN_POINT('Ctrl Pts',(-0.17880385919135,-3.22671678130447,
13.9864151868103));
#14283=CARTESIAN_POINT('Ctrl Pts',(-0.449124598487464,-3.19146897361022,
13.9682630291823));
#14284=CARTESIAN_POINT('Ctrl Pts',(-0.481488776943131,-3.18674689824832,
13.9660974044244));
#14285=CARTESIAN_POINT('Ctrl Pts',(-0.576888542331726,-3.17134107187992,
13.9597462659715));
#14286=CARTESIAN_POINT('Ctrl Pts',(-0.639688666443664,-3.15927274637982,
13.9556073485603));
#14287=CARTESIAN_POINT('Ctrl Pts',(-0.713345063924788,-3.14283141511242,
13.9508346094893));
#14288=CARTESIAN_POINT('Ctrl Pts',(-0.724583947499703,-3.14025931993832,
13.9501086301054));
#14289=CARTESIAN_POINT('Ctrl Pts',(-0.742787878807237,-3.13599029225939,
13.9489366974488));
#14290=CARTESIAN_POINT('Ctrl Pts',(-0.749761375311988,-3.13433036364961,
13.9484887018967));
#14291=CARTESIAN_POINT('Ctrl Pts',(-0.762163854812354,-3.13133439256682,
13.9476936880605));
#14292=CARTESIAN_POINT('Ctrl Pts',(-0.767594945071087,-3.13000747948518,
13.94734615211));
#14293=CARTESIAN_POINT('Ctrl Pts',(-0.779277423167552,-3.12712100345797,
13.9465999023303));
#14294=CARTESIAN_POINT('Ctrl Pts',(-0.785527577890505,-3.12555683016938,
13.9462014587759));
#14295=CARTESIAN_POINT('Ctrl Pts',(-0.802805350278876,-3.12117776837382,
13.9451021249343));
#14296=CARTESIAN_POINT('Ctrl Pts',(-0.813822939122415,-3.11832315916913,
13.9444034939246));
#14297=CARTESIAN_POINT('Ctrl Pts',(-0.874823074406389,-3.10217297163409,
13.9405475117798));
#14298=CARTESIAN_POINT('Ctrl Pts',(-0.924498214031703,-3.08773320005452,
13.937452402517));
#14299=CARTESIAN_POINT('Ctrl Pts',(-1.14658871042072,-3.0173340724577,13.9237293053963));
#14300=CARTESIAN_POINT('Ctrl Pts',(-1.31432418387146,-2.94812382759616,
13.9136660899074));
#14301=CARTESIAN_POINT('Ctrl Pts',(-1.47525547426939,-2.86526418470238,
13.9035519756546));
#14302=CARTESIAN_POINT('',(3.22274997771073,0.000379032282113146,14.0611576755349));
#14303=CARTESIAN_POINT('Ctrl Pts',(-1.4752554049854,-2.86526422037504,13.6541509617524));
#14304=CARTESIAN_POINT('Ctrl Pts',(-1.45982376353312,-2.87320960017575,
13.6551971576971));
#14305=CARTESIAN_POINT('Ctrl Pts',(-1.44432835518962,-2.88103009647269,
13.6562476163241));
#14306=CARTESIAN_POINT('Ctrl Pts',(-1.4170239894115,-2.89453490501609,13.6580988942635));
#14307=CARTESIAN_POINT('Ctrl Pts',(-1.40524210014484,-2.90027307937424,
13.6588978115895));
#14308=CARTESIAN_POINT('Ctrl Pts',(-1.38433572830802,-2.91029788498968,
13.6603157484364));
#14309=CARTESIAN_POINT('Ctrl Pts',(-1.37522546321132,-2.91461388690045,
13.6609337349139));
#14310=CARTESIAN_POINT('Ctrl Pts',(-1.35627470346765,-2.92348320634336,
13.6622195171418));
#14311=CARTESIAN_POINT('Ctrl Pts',(-1.34643119226503,-2.92802974181157,
13.6628875383409));
#14312=CARTESIAN_POINT('Ctrl Pts',(-1.32096183568928,-2.93963797498741,
13.6646164838761));
#14313=CARTESIAN_POINT('Ctrl Pts',(-1.30530239145358,-2.9466247205715,13.6656799747465));
#14314=CARTESIAN_POINT('Ctrl Pts',(-1.2383868216666,-2.97584223705724,13.6702270081124));
#14315=CARTESIAN_POINT('Ctrl Pts',(-1.18661557317988,-2.99686199064071,
13.6737515265658));
#14316=CARTESIAN_POINT('Ctrl Pts',(-1.04876452882735,-3.04869916675506,
13.6831594136804));
#14317=CARTESIAN_POINT('Ctrl Pts',(-0.961879264632453,-3.07721618416813,
13.6891135132665));
#14318=CARTESIAN_POINT('Ctrl Pts',(-0.635926831564798,-3.16904457231667,
13.7115101920212));
#14319=CARTESIAN_POINT('Ctrl Pts',(-0.391049363940187,-3.20847489434767,
13.728528198626));
#14320=CARTESIAN_POINT('Ctrl Pts',(-0.055584648732851,-3.2234881789726,
13.7508405620566));
#14321=CARTESIAN_POINT('Ctrl Pts',(0.0330512780081772,-3.22379844303205,
13.756632164867));
#14322=CARTESIAN_POINT('Ctrl Pts',(0.135393188527221,-3.21993430046902,
13.7631183166994));
#14323=CARTESIAN_POINT('Ctrl Pts',(0.14918785022229,-3.21932465219847,13.7639883378338));
#14324=CARTESIAN_POINT('Ctrl Pts',(0.170018421978332,-3.21826987477703,
13.7652952614974));
#14325=CARTESIAN_POINT('Ctrl Pts',(0.177057280142272,-3.21789029839468,
13.7657357021501));
#14326=CARTESIAN_POINT('Ctrl Pts',(0.189664973434262,-3.21716892429825,
13.7665224136363));
#14327=CARTESIAN_POINT('Ctrl Pts',(0.195234195864137,-3.2168357589289,13.7668691604721));
#14328=CARTESIAN_POINT('Ctrl Pts',(0.207312981135927,-3.21608169047428,
13.7676195246972));
#14329=CARTESIAN_POINT('Ctrl Pts',(0.213822119996184,-3.215655487569,13.7680228408706));
#14330=CARTESIAN_POINT('Ctrl Pts',(0.23205669507289,-3.21440591932724,13.7691498586185));
#14331=CARTESIAN_POINT('Ctrl Pts',(0.243779128463169,-3.21353815449199,
13.7698711092424));
#14332=CARTESIAN_POINT('Ctrl Pts',(0.313038872103603,-3.20802996619662,
13.7741145054594));
#14333=CARTESIAN_POINT('Ctrl Pts',(0.370451841367153,-3.20190817967215,
13.7775587474066));
#14334=CARTESIAN_POINT('Ctrl Pts',(0.678346550880745,-3.16068457878031,
13.7957821042646));
#14335=CARTESIAN_POINT('Ctrl Pts',(0.924220157790897,-3.09772893879346,
13.8095093798324));
#14336=CARTESIAN_POINT('Ctrl Pts',(1.31258679528047,-2.94786460392411,13.8330256491715));
#14337=CARTESIAN_POINT('Ctrl Pts',(1.46024347612413,-2.87758031166909,13.8424380530076));
#14338=CARTESIAN_POINT('Ctrl Pts',(1.62264206521815,-2.78455026812397,13.8536947430961));
#14339=CARTESIAN_POINT('Ctrl Pts',(1.64322372968842,-2.7724543629574,13.8551385783413));
#14340=CARTESIAN_POINT('Ctrl Pts',(1.67421290905569,-2.75377563913955,13.857339627389));
#14341=CARTESIAN_POINT('Ctrl Pts',(1.68472049829767,-2.74735981836555,13.8580907309451));
#14342=CARTESIAN_POINT('Ctrl Pts',(1.70348624584461,-2.73575351715161,13.8594408738137));
#14343=CARTESIAN_POINT('Ctrl Pts',(1.71175813015563,-2.73058543116863,13.8600390805903));
#14344=CARTESIAN_POINT('Ctrl Pts',(1.72918327505788,-2.71958830018016,13.861305796142));
#14345=CARTESIAN_POINT('Ctrl Pts',(1.73833079324856,-2.71375042512134,13.861974628567));
#14346=CARTESIAN_POINT('Ctrl Pts',(1.75698799115922,-2.70171050606463,13.8633467652585));
#14347=CARTESIAN_POINT('Ctrl Pts',(1.7664947218345,-2.69550419255371,13.8640502234756));
#14348=CARTESIAN_POINT('Ctrl Pts',(1.80788925330062,-2.66816741189918,13.8671322131751));
#14349=CARTESIAN_POINT('Ctrl Pts',(1.83943111113826,-2.64652108889642,13.8695301401313));
#14350=CARTESIAN_POINT('Ctrl Pts',(2.02866635102685,-2.51163677532622,13.8842267992039));
#14351=CARTESIAN_POINT('Ctrl Pts',(2.17622227767912,-2.38491938456082,13.8970548275079));
#14352=CARTESIAN_POINT('Ctrl Pts',(2.48139659603935,-2.07081125580598,13.926570628857));
#14353=CARTESIAN_POINT('Ctrl Pts',(2.63093736718886,-1.87717116696135,13.9433275916306));
#14354=CARTESIAN_POINT('Ctrl Pts',(2.76847376049459,-1.64989211498185,13.9602949064087));
#14355=CARTESIAN_POINT('Ctrl Pts',(2.77954981427248,-1.63116334069773,13.961674257012));
#14356=CARTESIAN_POINT('Ctrl Pts',(2.79474728215645,-1.60486119752892,13.9635836997103));
#14357=CARTESIAN_POINT('Ctrl Pts',(2.79902898643129,-1.59738178642921,13.9641235866283));
#14358=CARTESIAN_POINT('Ctrl Pts',(2.80587143709609,-1.58531719837751,13.9649893685728));
#14359=CARTESIAN_POINT('Ctrl Pts',(2.80845103302877,-1.58074284341465,13.9653164658657));
#14360=CARTESIAN_POINT('Ctrl Pts',(2.81383409731772,-1.57114237285293,13.9660004849408));
#14361=CARTESIAN_POINT('Ctrl Pts',(2.81663529691228,-1.56611503021123,13.966357253297));
#14362=CARTESIAN_POINT('Ctrl Pts',(2.82341324021639,-1.55387357734788,13.9672225866999));
#14363=CARTESIAN_POINT('Ctrl Pts',(2.82737585531618,-1.54665160773086,13.9677302485261));
#14364=CARTESIAN_POINT('Ctrl Pts',(2.84132103826209,-1.52100344819781,13.9695233672761));
#14365=CARTESIAN_POINT('Ctrl Pts',(2.85115177575193,-1.50249470443291,13.9707995040502));
#14366=CARTESIAN_POINT('Ctrl Pts',(2.90966592200513,-1.38968494900232,13.9784778413112));
#14367=CARTESIAN_POINT('Ctrl Pts',(2.9538524016105,-1.29311278492101,13.9846326068678));
#14368=CARTESIAN_POINT('Ctrl Pts',(3.10422249771436,-0.916321586715868,
14.0077257341535));
#14369=CARTESIAN_POINT('Ctrl Pts',(3.1759194378451,-0.624008555973554,14.0239106002063));
#14370=CARTESIAN_POINT('Ctrl Pts',(3.2095745976177,-0.292998520352483,14.0434338250568));
#14371=CARTESIAN_POINT('Ctrl Pts',(3.21241945013261,-0.259958446686835,
14.0453934257377));
#14372=CARTESIAN_POINT('Ctrl Pts',(3.21744224503166,-0.188788817954243,
14.0496422973067));
#14373=CARTESIAN_POINT('Ctrl Pts',(3.21945326264819,-0.150652978737051,
14.0519361699742));
#14374=CARTESIAN_POINT('Ctrl Pts',(3.22130937779569,-0.0975098971026946,
14.0551601209091));
#14375=CARTESIAN_POINT('Ctrl Pts',(3.22172809385986,-0.0825249349214185,
14.0560722133335));
#14376=CARTESIAN_POINT('Ctrl Pts',(3.22224020211305,-0.05809365901413,14.0575644079765));
#14377=CARTESIAN_POINT('Ctrl Pts',(3.22239663702435,-0.0486487822809514,
14.0581425244156));
#14378=CARTESIAN_POINT('Ctrl Pts',(3.22261096818201,-0.0310308194195748,
14.0592232949781));
#14379=CARTESIAN_POINT('Ctrl Pts',(3.22267930108349,-0.0228579177843625,
14.0597256166059));
#14380=CARTESIAN_POINT('Ctrl Pts',(3.22273942344462,-0.00966359763668823,
14.0605381352299));
#14381=CARTESIAN_POINT('Ctrl Pts',(3.22275056827357,-0.00464227186255321,
14.0608477205496));
#14382=CARTESIAN_POINT('Ctrl Pts',(3.22274997771073,0.000379032282113146,
14.0611576755349));
#14383=CARTESIAN_POINT('Ctrl Pts',(3.22274997776876,0.000378538572947885,
14.0611576450592));
#14384=CARTESIAN_POINT('Ctrl Pts',(3.22274967767412,0.00293344333988479,
14.0613153541692));
#14385=CARTESIAN_POINT('Ctrl Pts',(3.2227463393961,0.00548834244600403,
14.0614731589751));
#14386=CARTESIAN_POINT('Ctrl Pts',(3.22272011115962,0.0159974016700903,
14.0621226539904));
#14387=CARTESIAN_POINT('Ctrl Pts',(3.22267081155901,0.0239514139831863,
14.0626151740574));
#14388=CARTESIAN_POINT('Ctrl Pts',(3.22236074946736,0.0552693998518561,
14.0645581486519));
#14389=CARTESIAN_POINT('Ctrl Pts',(3.22187535249879,0.0786299738390946,
14.0660156360751));
#14390=CARTESIAN_POINT('Ctrl Pts',(3.21596486344505,0.265313456636337,14.0777306166039));
#14391=CARTESIAN_POINT('Ctrl Pts',(3.19837964774811,0.427988739170791,14.0883715564805));
#14392=CARTESIAN_POINT('Ctrl Pts',(3.12133389613864,0.842733806174139,14.1165211074734));
#14393=CARTESIAN_POINT('Ctrl Pts',(3.04372936911141,1.09024465136447,14.134375414665));
#14394=CARTESIAN_POINT('Ctrl Pts',(2.91659558013825,1.3719127657331,14.1545251651779));
#14395=CARTESIAN_POINT('Ctrl Pts',(2.89471000241654,1.41750805826156,14.1577778018182));
#14396=CARTESIAN_POINT('Ctrl Pts',(2.86663067066838,1.47264179479184,14.1616830093862));
#14397=CARTESIAN_POINT('Ctrl Pts',(2.86144929842948,1.48268445032994,14.1623931916541));
#14398=CARTESIAN_POINT('Ctrl Pts',(2.85323982849152,1.49839290816322,14.1635019783022));
#14399=CARTESIAN_POINT('Ctrl Pts',(2.85024749107995,1.50407714809727,14.1639027762969));
#14400=CARTESIAN_POINT('Ctrl Pts',(2.84461879340147,1.5146922940599,14.1646504021283));
#14401=CARTESIAN_POINT('Ctrl Pts',(2.84198662628928,1.51962523078707,14.1649974770479));
#14402=CARTESIAN_POINT('Ctrl Pts',(2.83593977804495,1.53088694848938,14.1657890589076));
#14403=CARTESIAN_POINT('Ctrl Pts',(2.83251674978123,1.53721115606326,14.1662330274233));
#14404=CARTESIAN_POINT('Ctrl Pts',(2.82189581728083,1.55667790226928,14.1675980636627));
#14405=CARTESIAN_POINT('Ctrl Pts',(2.81462727726891,1.56978196103171,14.1685147422189));
#14406=CARTESIAN_POINT('Ctrl Pts',(2.73953452960236,1.70296413552254,14.17781378473));
#14407=CARTESIAN_POINT('Ctrl Pts',(2.66415133460978,1.81863788532363,14.1857466282412));
#14408=CARTESIAN_POINT('Ctrl Pts',(2.46668193772717,2.08289206122173,14.2043843394804));
#14409=CARTESIAN_POINT('Ctrl Pts',(2.33828081305552,2.22607353727253,14.2149384095779));
#14410=CARTESIAN_POINT('Ctrl Pts',(2.10380002167754,2.4447285822077,14.2331719308684));
#14411=CARTESIAN_POINT('Ctrl Pts',(2.00453894653988,2.52675493511236,14.2406292615811));
#14412=CARTESIAN_POINT('Ctrl Pts',(1.87573095370823,2.62082104910029,14.2501777467641));
#14413=CARTESIAN_POINT('Ctrl Pts',(1.8505539091607,2.63865869543472,14.2520380388337));
#14414=CARTESIAN_POINT('Ctrl Pts',(1.81412882041287,2.66368770722529,14.2547226532618));
#14415=CARTESIAN_POINT('Ctrl Pts',(1.80308567992886,2.67117532204798,14.2555356789102));
#14416=CARTESIAN_POINT('Ctrl Pts',(1.79171128914603,2.67878486194621,14.2563722827108));
#14417=CARTESIAN_POINT('Ctrl Pts',(1.79142605682764,2.67897561824745,14.2563932614628));
#14418=CARTESIAN_POINT('Ctrl Pts',(1.79086399036416,2.67935138445536,14.2564346002612));
#14419=CARTESIAN_POINT('Ctrl Pts',(1.79058715799431,2.67953639702685,14.2564549602074));
#14420=CARTESIAN_POINT('Ctrl Pts',(1.79004070155057,2.679901482222,14.256495148996));
#14421=CARTESIAN_POINT('Ctrl Pts',(1.78977107896822,2.68008155706354,14.2565149777539));
#14422=CARTESIAN_POINT('Ctrl Pts',(1.78923786019216,2.68043756550878,14.2565541911621));
#14423=CARTESIAN_POINT('Ctrl Pts',(1.78897426520726,2.68061350092879,14.2565735757441));
#14424=CARTESIAN_POINT('Ctrl Pts',(1.78845191054901,2.68096203309556,14.2566119884529));
#14425=CARTESIAN_POINT('Ctrl Pts',(1.78819315182996,2.68113463126986,14.2566310165257));
#14426=CARTESIAN_POINT('Ctrl Pts',(1.78767924896271,2.68147730912529,14.2566688060328));
#14427=CARTESIAN_POINT('Ctrl Pts',(1.78742410552117,2.6816473898571,14.256687567427));
#14428=CARTESIAN_POINT('Ctrl Pts',(1.78691615751997,2.68198588750361,14.2567249174172));
#14429=CARTESIAN_POINT('Ctrl Pts',(1.78666335340878,2.68215430509888,14.2567435059877));
#14430=CARTESIAN_POINT('Ctrl Pts',(1.78615872123296,2.68249038704563,14.2567806105619));
#14431=CARTESIAN_POINT('Ctrl Pts',(1.78590689336921,2.68265805168027,14.2567991265538));
#14432=CARTESIAN_POINT('Ctrl Pts',(1.78540272170402,2.68299362200167,14.2568361956802));
#14433=CARTESIAN_POINT('Ctrl Pts',(1.78515037781527,2.68316152755582,14.2568547488195));
#14434=CARTESIAN_POINT('Ctrl Pts',(1.78464349618142,2.68349869526269,14.2568920156013));
#14435=CARTESIAN_POINT('Ctrl Pts',(1.78438895802694,2.68366795681035,14.2569107292671));
#14436=CARTESIAN_POINT('Ctrl Pts',(1.78387574486745,2.68400912551326,14.2569484599295));
#14437=CARTESIAN_POINT('Ctrl Pts',(1.7836170690936,2.68418103148851,14.2569674769696));
#14438=CARTESIAN_POINT('Ctrl Pts',(1.78309325856536,2.68452902667538,14.2570059850556));
#14439=CARTESIAN_POINT('Ctrl Pts',(1.78282812257556,2.68470511400368,14.2570254761715));
#14440=CARTESIAN_POINT('Ctrl Pts',(1.78228851931199,2.68506337075063,14.2570651434974));
#14441=CARTESIAN_POINT('Ctrl Pts',(1.78201405018803,2.68524553736718,14.2570853198126));
#14442=CARTESIAN_POINT('Ctrl Pts',(1.78145209037566,2.68561838897635,14.2571266287138));
#14443=CARTESIAN_POINT('Ctrl Pts',(1.78116459699617,2.68580906989292,14.2571477614529));
#14444=CARTESIAN_POINT('Ctrl Pts',(1.78057163875083,2.68620221429373,14.257191346914));
#14445=CARTESIAN_POINT('Ctrl Pts',(1.78026616996209,2.68640467184091,14.2572137998592));
#14446=CARTESIAN_POINT('Ctrl Pts',(1.77963027441382,2.68682597240014,14.2572605390548));
#14447=CARTESIAN_POINT('Ctrl Pts',(1.77929984182474,2.68704480655914,14.2572848256371));
#14448=CARTESIAN_POINT('Ctrl Pts',(1.77860351060529,2.68750577805424,14.2573360041327));
#14449=CARTESIAN_POINT('Ctrl Pts',(1.77823760290523,2.68774790161316,14.2573628965627));
#14450=CARTESIAN_POINT('Ctrl Pts',(1.77753738876963,2.68821103238402,14.2574143573316));
#14451=CARTESIAN_POINT('Ctrl Pts',(1.7772030905083,2.68843205199474,14.2574389252041));
#14452=CARTESIAN_POINT('Ctrl Pts',(1.76889133356015,2.6939251004238,14.2580497467428));
#14453=CARTESIAN_POINT('Ctrl Pts',(1.76089056103802,2.69916161530606,14.2586373305727));
#14454=CARTESIAN_POINT('Ctrl Pts',(1.7425349770877,2.71105901903736,14.2599845675654));
#14455=CARTESIAN_POINT('Ctrl Pts',(1.73216511028682,2.71769629926261,14.2607450927187));
#14456=CARTESIAN_POINT('Ctrl Pts',(1.70157491656341,2.73702948652854,14.262987005587));
#14457=CARTESIAN_POINT('Ctrl Pts',(1.68125158263003,2.74956008720793,14.2644744802464));
#14458=CARTESIAN_POINT('Ctrl Pts',(1.52087563804502,2.84599895277093,14.2761992751412));
#14459=CARTESIAN_POINT('Ctrl Pts',(1.37479103207176,2.91936771099399,14.2868195595402));
#14460=CARTESIAN_POINT('Ctrl Pts',(0.989893130140116,3.07736235920731,14.3145656525276));
#14461=CARTESIAN_POINT('Ctrl Pts',(0.745515525725842,3.14551251764869,14.3320153658719));
#14462=CARTESIAN_POINT('Ctrl Pts',(0.438517603884532,3.19330045863065,14.352358259319));
#14463=CARTESIAN_POINT('Ctrl Pts',(0.38111102855807,3.20065944456107,14.3560920916717));
#14464=CARTESIAN_POINT('Ctrl Pts',(0.311830560277556,3.20764985856982,14.3604898297074));
#14465=CARTESIAN_POINT('Ctrl Pts',(0.3001211205991,3.20876662232385,14.3612293977294));
#14466=CARTESIAN_POINT('Ctrl Pts',(0.281907049715131,3.21040317563946,14.3623737490723));
#14467=CARTESIAN_POINT('Ctrl Pts',(0.275406654434022,3.21096734821765,14.3627809584953));
#14468=CARTESIAN_POINT('Ctrl Pts',(0.263344929312413,3.21197729389303,14.3635342750501));
#14469=CARTESIAN_POINT('Ctrl Pts',(0.257784206398508,3.21242836370809,14.363880667718));
#14470=CARTESIAN_POINT('Ctrl Pts',(0.245197175918996,3.21341649379329,14.364662726967));
#14471=CARTESIAN_POINT('Ctrl Pts',(0.238170279239326,3.2139449494316,14.3650979052464));
#14472=CARTESIAN_POINT('Ctrl Pts',(0.21738041540565,3.21543988710894,14.3663813851237));
#14473=CARTESIAN_POINT('Ctrl Pts',(0.203612705605847,3.21634105693527,14.3672261068646));
#14474=CARTESIAN_POINT('Ctrl Pts',(0.101702784767804,3.22235460624036,14.3734428661398));
#14475=CARTESIAN_POINT('Ctrl Pts',(0.0133808674177226,3.22393186355365,
14.378632135278));
#14476=CARTESIAN_POINT('Ctrl Pts',(-0.322468548617493,3.21612402209149,
14.3979816956495));
#14477=CARTESIAN_POINT('Ctrl Pts',(-0.568555215608009,3.18185471359297,
14.4114285204181));
#14478=CARTESIAN_POINT('Ctrl Pts',(-0.896724692867139,3.09682835423077,
14.430733669533));
#14479=CARTESIAN_POINT('Ctrl Pts',(-0.984127790872031,3.07017126912715,
14.4360073642664));
#14480=CARTESIAN_POINT('Ctrl Pts',(-1.12294659424284,3.02129550969271,14.444686821237));
#14481=CARTESIAN_POINT('Ctrl Pts',(-1.17512338168107,3.00138635958863,14.4480201349785));
#14482=CARTESIAN_POINT('Ctrl Pts',(-1.24260787253953,2.97360675920239,14.452436406297));
#14483=CARTESIAN_POINT('Ctrl Pts',(-1.25840876374391,2.96695447368759,14.4534780712834));
#14484=CARTESIAN_POINT('Ctrl Pts',(-1.28411432411955,2.95588997021927,14.4551855154937));
#14485=CARTESIAN_POINT('Ctrl Pts',(-1.29405126398141,2.95155322416806,14.4558487094634));
#14486=CARTESIAN_POINT('Ctrl Pts',(-1.31318518372179,2.94308747178516,14.4571318902334));
#14487=CARTESIAN_POINT('Ctrl Pts',(-1.32238505641324,2.9389652859832,14.4577516365763));
#14488=CARTESIAN_POINT('Ctrl Pts',(-1.34350092750508,2.92938468015524,14.4591805661273));
#14489=CARTESIAN_POINT('Ctrl Pts',(-1.35540321002592,2.92389662550317,14.4599907662541));
#14490=CARTESIAN_POINT('Ctrl Pts',(-1.38714894233019,2.9090234122377,14.4621646653525));
#14491=CARTESIAN_POINT('Ctrl Pts',(-1.40693026423603,2.89950799175033,14.4635328682284));
#14492=CARTESIAN_POINT('Ctrl Pts',(-1.57359812406625,2.8172285434943,14.475178387118));
#14493=CARTESIAN_POINT('Ctrl Pts',(-1.71481027312923,2.73356886690281,14.4858432045254));
#14494=CARTESIAN_POINT('Ctrl Pts',(-2.05720231681463,2.49371949561247,14.5137262555303));
#14495=CARTESIAN_POINT('Ctrl Pts',(-2.24738180071733,2.32378755176123,14.531271085042));
#14496=CARTESIAN_POINT('Ctrl Pts',(-2.45272261528797,2.09127019667595,14.5515617733742));
#14497=CARTESIAN_POINT('Ctrl Pts',(-2.48872559651583,2.04829320970447,14.5551759596538));
#14498=CARTESIAN_POINT('Ctrl Pts',(-2.53084003124578,1.99526993740475,14.5594518888165));
#14499=CARTESIAN_POINT('Ctrl Pts',(-2.53803906593545,1.9861045029021,14.5601845930571));
#14500=CARTESIAN_POINT('Ctrl Pts',(-2.54917634667188,1.97176565095079,14.5613206451771));
#14501=CARTESIAN_POINT('Ctrl Pts',(-2.55314883893586,1.96661913870326,14.5617263639716));
#14502=CARTESIAN_POINT('Ctrl Pts',(-2.56050278894569,1.95703198301917,14.5624783279329));
#14503=CARTESIAN_POINT('Ctrl Pts',(-2.5638882517552,1.95259461946905,14.5628248497679));
#14504=CARTESIAN_POINT('Ctrl Pts',(-2.57154120141764,1.94250959255976,14.5636089888774));
#14505=CARTESIAN_POINT('Ctrl Pts',(-2.57580160959158,1.93685666430392,14.5640461067692));
#14506=CARTESIAN_POINT('Ctrl Pts',(-2.58840031243995,1.92002496697108,14.5653406352771));
#14507=CARTESIAN_POINT('Ctrl Pts',(-2.59668483577818,1.90880589143384,14.5661943737113));
#14508=CARTESIAN_POINT('Ctrl Pts',(-2.6594050999744,1.82270473820819,14.5726800545787));
#14509=CARTESIAN_POINT('Ctrl Pts',(-2.71066981118429,1.74555454775614,14.5781108556848));
#14510=CARTESIAN_POINT('Ctrl Pts',(-2.88372455055585,1.45906327039345,14.5973486673834));
#14511=CARTESIAN_POINT('Ctrl Pts',(-2.98515738935376,1.23837841286995,14.610512716537));
#14512=CARTESIAN_POINT('Ctrl Pts',(-3.08970278440933,0.921040255274114,
14.6295336777268));
#14513=CARTESIAN_POINT('Ctrl Pts',(-3.11472910001279,0.832489728804896,
14.6348427867794));
#14514=CARTESIAN_POINT('Ctrl Pts',(-3.14887122121812,0.688387228352557,
14.6435751939299));
#14515=CARTESIAN_POINT('Ctrl Pts',(-3.16038015163296,0.633453758486885,
14.6469248801916));
#14516=CARTESIAN_POINT('Ctrl Pts',(-3.17353024451126,0.561354013047729,
14.6513598175218));
#14517=CARTESIAN_POINT('Ctrl Pts',(-3.17647673730421,0.544433706151925,
14.6524033311317));
#14518=CARTESIAN_POINT('Ctrl Pts',(-3.18106351312561,0.516788337810951,
14.6541130432923));
#14519=CARTESIAN_POINT('Ctrl Pts',(-3.18278515616924,0.506076976114933,
14.654776643302));
#14520=CARTESIAN_POINT('Ctrl Pts',(-3.18600183430004,0.485398244349972,
14.6560600741534));
#14521=CARTESIAN_POINT('Ctrl Pts',(-3.18750426204822,0.475432139766166,
14.6566796616597));
#14522=CARTESIAN_POINT('Ctrl Pts',(-3.19085062436683,0.452505502345633,
14.6581074569641));
#14523=CARTESIAN_POINT('Ctrl Pts',(-3.19266237796002,0.439540520208768,
14.6589166764253));
#14524=CARTESIAN_POINT('Ctrl Pts',(-3.19729339174301,0.404860489739731,
14.6610862347029));
#14525=CARTESIAN_POINT('Ctrl Pts',(-3.19997037114034,0.38312743915562,14.6624510492313));
#14526=CARTESIAN_POINT('Ctrl Pts',(-3.22076449645263,0.198851535730365,
14.6740693715794));
#14527=CARTESIAN_POINT('Ctrl Pts',(-3.22670300391755,0.0351993286825831,
14.6847085972871));
#14528=CARTESIAN_POINT('Ctrl Pts',(-3.21012794740424,-0.38122106731115,
14.7125020350797));
#14529=CARTESIAN_POINT('Ctrl Pts',(-3.17026651407814,-0.632183657607774,
14.7299806505244));
#14530=CARTESIAN_POINT('Ctrl Pts',(-3.08586703458046,-0.93103492043124,
14.7503072021715));
#14531=CARTESIAN_POINT('Ctrl Pts',(-3.06882334321127,-0.985761445944426,
14.754004220341));
#14532=CARTESIAN_POINT('Ctrl Pts',(-3.04654275455866,-1.0511100746245,14.7583645226158));
#14533=CARTESIAN_POINT('Ctrl Pts',(-3.04269688772852,-1.0621915099075,14.7591020077218));
#14534=CARTESIAN_POINT('Ctrl Pts',(-3.03662001351166,-1.07939748723584,
14.7602438410658));
#14535=CARTESIAN_POINT('Ctrl Pts',(-3.03443083007812,-1.08553654068747,
14.7606505986015));
#14536=CARTESIAN_POINT('Ctrl Pts',(-3.03033294353346,-1.09691884263039,
14.7614035033416));
#14537=CARTESIAN_POINT('Ctrl Pts',(-3.02842926557617,-1.10216372654799,
14.7617499333983));
#14538=CARTESIAN_POINT('Ctrl Pts',(-3.02408727241414,-1.11403030536733,
14.7625326151189));
#14539=CARTESIAN_POINT('Ctrl Pts',(-3.02164083193596,-1.12064893587091,
14.762968375156));
#14540=CARTESIAN_POINT('Ctrl Pts',(-3.01433117168504,-1.14022661541805,
14.7642551641995));
#14541=CARTESIAN_POINT('Ctrl Pts',(-3.00940610863046,-1.15316262356423,
14.765102585819));
#14542=CARTESIAN_POINT('Ctrl Pts',(-2.97200491269003,-1.24952766217803,
14.7713970211322));
#14543=CARTESIAN_POINT('Ctrl Pts',(-2.93614507618829,-1.331610990725,14.7766560568186));
#14544=CARTESIAN_POINT('Ctrl Pts',(-2.78913018677072,-1.63321026300772,
14.7959697020759));
#14545=CARTESIAN_POINT('Ctrl Pts',(-2.65638802951668,-1.8412603762879,14.8093319711001));
#14546=CARTESIAN_POINT('Ctrl Pts',(-2.44352295430689,-2.10325870578603,
14.8285534639843));
#14547=CARTESIAN_POINT('Ctrl Pts',(-2.38278591884533,-2.17182664258112,
14.833839428391));
#14548=CARTESIAN_POINT('Ctrl Pts',(-2.28037603687493,-2.2779665469539,14.8425372349247));
#14549=CARTESIAN_POINT('Ctrl Pts',(-2.24049707040061,-2.31720063105109,
14.8458762266778));
#14550=CARTESIAN_POINT('Ctrl Pts',(-2.18708133822446,-2.36708408603244,
14.8502989720815));
#14551=CARTESIAN_POINT('Ctrl Pts',(-2.17445049053268,-2.3786922661156,14.851341279142));
#14552=CARTESIAN_POINT('Ctrl Pts',(-2.15368481318203,-2.39747302175114,
14.8530495110448));
#14553=CARTESIAN_POINT('Ctrl Pts',(-2.14560528662977,-2.40470645069119,
14.853712846021));
#14554=CARTESIAN_POINT('Ctrl Pts',(-2.12994536816959,-2.41858469040365,
14.8549961134002));
#14555=CARTESIAN_POINT('Ctrl Pts',(-2.12236999604031,-2.42523499320478,
14.8556158043454));
#14556=CARTESIAN_POINT('Ctrl Pts',(-2.10487760822538,-2.44044656941355,
14.857044338872));
#14557=CARTESIAN_POINT('Ctrl Pts',(-2.09493938888231,-2.44898308539132,
14.8578541975418));
#14558=CARTESIAN_POINT('Ctrl Pts',(-2.0682254935597,-2.47164760616838,14.8600265848763));
#14559=CARTESIAN_POINT('Ctrl Pts',(-2.05135741377376,-2.48566516325797,
14.8613936076172));
#14560=CARTESIAN_POINT('Ctrl Pts',(-1.90613576389792,-2.60386091174171,
14.8731248309722));
#14561=CARTESIAN_POINT('Ctrl Pts',(-1.7701052656151,-2.69817669660086,14.88388347364));
#14562=CARTESIAN_POINT('Ctrl Pts',(-1.57745449062304,-2.8108915892576,14.8987759855522));
#14563=CARTESIAN_POINT('Ctrl Pts',(-1.52669994797171,-2.83877667198752,
14.9026674496955));
#14564=CARTESIAN_POINT('Ctrl Pts',(-1.47525516809595,-2.86526434234368,
14.9065719799118));
#14565=CARTESIAN_POINT('Origin',(0.,0.,4.68922655072688));
#14566=CARTESIAN_POINT('',(-1.47525540582449,-2.86526421994301,16.4055744628637));
#14567=CARTESIAN_POINT('',(-1.47525540483048,-2.8652642204548,16.1601692104994));
#14568=CARTESIAN_POINT('',(-1.47525540501186,-2.86526422036142,4.68922655072688));
#14569=CARTESIAN_POINT('',(3.22274959861812,-0.00160844855869799,15.5583907367487));
#14570=CARTESIAN_POINT('Ctrl Pts',(-1.47525540582449,-2.86526421994301,
16.4055744628637));
#14571=CARTESIAN_POINT('Ctrl Pts',(-1.68834631514222,-2.75554885278246,
16.3897071016039));
#14572=CARTESIAN_POINT('Ctrl Pts',(-1.88851797500529,-2.62241399723029,
16.3732267052815));
#14573=CARTESIAN_POINT('Ctrl Pts',(-2.1430559897236,-2.40873765580771,16.3511110036867));
#14574=CARTESIAN_POINT('Ctrl Pts',(-2.2114400298354,-2.34611221874768,16.3450431196542));
#14575=CARTESIAN_POINT('Ctrl Pts',(-2.28690899564965,-2.27076187177162,
16.3382878637327));
#14576=CARTESIAN_POINT('Ctrl Pts',(-2.29671869530835,-2.2608395528794,16.3374086103913));
#14577=CARTESIAN_POINT('Ctrl Pts',(-2.31140963825781,-2.24578565136435,
16.3360904939948));
#14578=CARTESIAN_POINT('Ctrl Pts',(-2.31633876358725,-2.24070132821915,
16.335648005267));
#14579=CARTESIAN_POINT('Ctrl Pts',(-2.32512429014357,-2.23157921030102,
16.3348589787052));
#14580=CARTESIAN_POINT('Ctrl Pts',(-2.32898698045568,-2.22754761630584,
16.3345119539501));
#14581=CARTESIAN_POINT('Ctrl Pts',(-2.33732623917017,-2.21879830282613,
16.3337625085123));
#14582=CARTESIAN_POINT('Ctrl Pts',(-2.34179899734263,-2.21407707967633,
16.3333603810583));
#14583=CARTESIAN_POINT('Ctrl Pts',(-2.35424955504378,-2.20085494830625,
16.3322404356902));
#14584=CARTESIAN_POINT('Ctrl Pts',(-2.36219566037684,-2.19232414179238,
16.3315250183069));
#14585=CARTESIAN_POINT('Ctrl Pts',(-2.40808490567337,-2.14251904577547,
16.3273882913274));
#14586=CARTESIAN_POINT('Ctrl Pts',(-2.44499469297349,-2.10030059973463,
16.3240403803592));
#14587=CARTESIAN_POINT('Ctrl Pts',(-2.64306072726742,-1.86144465891646,
16.3058174478728));
#14588=CARTESIAN_POINT('Ctrl Pts',(-2.78162516580758,-1.64722039289585,
16.292022116168));
#14589=CARTESIAN_POINT('Ctrl Pts',(-2.96573209890492,-1.27177356115637,
16.2684027065213));
#14590=CARTESIAN_POINT('Ctrl Pts',(-3.02654866310058,-1.11936036130739,
16.2589591227187));
#14591=CARTESIAN_POINT('Ctrl Pts',(-3.0820557571412,-0.942088044346691,
16.2477862955936));
#14592=CARTESIAN_POINT('Ctrl Pts',(-3.08838896622197,-0.921114070263639,
16.2464617905686));
#14593=CARTESIAN_POINT('Ctrl Pts',(-3.09816550623526,-0.887501878986326,
16.2443343534264));
#14594=CARTESIAN_POINT('Ctrl Pts',(-3.10174656412547,-0.874904185164823,
16.2435359242277));
#14595=CARTESIAN_POINT('Ctrl Pts',(-3.10794838331993,-0.852570270231802,
16.2421183787465));
#14596=CARTESIAN_POINT('Ctrl Pts',(-3.11060044349003,-0.842842865755071,
16.2415002919381));
#14597=CARTESIAN_POINT('Ctrl Pts',(-3.11601215284392,-0.822619958170176,
16.2402138265674));
#14598=CARTESIAN_POINT('Ctrl Pts',(-3.11876451857431,-0.81212265411104,
16.2395452200479));
#14599=CARTESIAN_POINT('Ctrl Pts',(-3.12573672914095,-0.784972973761023,
16.2378137379133));
#14600=CARTESIAN_POINT('Ctrl Pts',(-3.12987649818459,-0.768300564316399,
16.2367482830876));
#14601=CARTESIAN_POINT('Ctrl Pts',(-3.14697067769129,-0.697024046431928,
16.2321835827143));
#14602=CARTESIAN_POINT('Ctrl Pts',(-3.15863026063162,-0.642122422332045,
16.2286429715399));
#14603=CARTESIAN_POINT('Ctrl Pts',(-3.18560120036819,-0.496509859543548,
16.2191817992671));
#14604=CARTESIAN_POINT('Ctrl Pts',(-3.19847177631633,-0.40540451341519,
16.2131895199814));
#14605=CARTESIAN_POINT('Ctrl Pts',(-3.2310090566347,-0.0729175667754314,
16.1910887371651));
#14606=CARTESIAN_POINT('Ctrl Pts',(-3.22735998951859,0.169909127581393,
16.1744379425507));
#14607=CARTESIAN_POINT('Ctrl Pts',(-3.18477945000895,0.501867914894173,
16.1521669799668));
#14608=CARTESIAN_POINT('Ctrl Pts',(-3.16904459237215,0.593170626451046,
16.1461044033647));
#14609=CARTESIAN_POINT('Ctrl Pts',(-3.14643791796135,0.697309536097229,
16.1393542976587));
#14610=CARTESIAN_POINT('Ctrl Pts',(-3.14339003982371,0.710922805101249,
16.1384752088278));
#14611=CARTESIAN_POINT('Ctrl Pts',(-3.13866194822679,0.731415664773641,
16.1371572901847));
#14612=CARTESIAN_POINT('Ctrl Pts',(-3.13704734464756,0.738310002395416,
16.1367148362775));
#14613=CARTESIAN_POINT('Ctrl Pts',(-3.13411897744876,0.750631048640793,
16.1359258472998));
#14614=CARTESIAN_POINT('Ctrl Pts',(-3.13281382641785,0.756059697756088,
16.1355788255027));
#14615=CARTESIAN_POINT('Ctrl Pts',(-3.12995779253087,0.767804714171637,
16.1348293586037));
#14616=CARTESIAN_POINT('Ctrl Pts',(-3.12840190013486,0.774119767947654,
16.1344272068802));
#14617=CARTESIAN_POINT('Ctrl Pts',(-3.12400331372911,0.791742893487019,
16.1333071253659));
#14618=CARTESIAN_POINT('Ctrl Pts',(-3.12111831924455,0.803040447635769,
16.1325915970517));
#14619=CARTESIAN_POINT('Ctrl Pts',(-3.10399810666504,0.868596515740998,
16.1284529287458));
#14620=CARTESIAN_POINT('Ctrl Pts',(-3.08840856759553,0.922495288734444,
16.1251032679254));
#14621=CARTESIAN_POINT('Ctrl Pts',(-2.99443819224608,1.21822607160023,16.1068802469312));
#14622=CARTESIAN_POINT('Ctrl Pts',(-2.88905845907002,1.4505527951818,16.09308607898));
#14623=CARTESIAN_POINT('Ctrl Pts',(-2.67263700545135,1.80830937920154,16.0694684747699));
#14624=CARTESIAN_POINT('Ctrl Pts',(-2.57725778054361,1.94182987495263,16.0600254745735));
#14625=CARTESIAN_POINT('Ctrl Pts',(-2.45809350713611,2.08431616465558,16.0488533003112));
#14626=CARTESIAN_POINT('Ctrl Pts',(-2.44386739788618,2.10097826483533,16.0475288080214));
#14627=CARTESIAN_POINT('Ctrl Pts',(-2.42086760298079,2.12736671414123,16.0454013874718));
#14628=CARTESIAN_POINT('Ctrl Pts',(-2.41220243310124,2.13718705343997,16.0446029620182));
#14629=CARTESIAN_POINT('Ctrl Pts',(-2.39676092841285,2.15447354843376,16.0431854208708));
#14630=CARTESIAN_POINT('Ctrl Pts',(-2.39000892405974,2.16196127581243,16.0425673346301));
#14631=CARTESIAN_POINT('Ctrl Pts',(-2.37591671578696,2.17744232816478,16.0412808681316));
#14632=CARTESIAN_POINT('Ctrl Pts',(-2.36857106060516,2.18543049742853,16.0406122599051));
#14633=CARTESIAN_POINT('Ctrl Pts',(-2.34949349781975,2.20596758302776,16.0388807683847));
#14634=CARTESIAN_POINT('Ctrl Pts',(-2.33770146348104,2.21845994394444,16.0378153058269));
#14635=CARTESIAN_POINT('Ctrl Pts',(-2.28696234881986,2.27135869215398,16.0332505274538));
#14636=CARTESIAN_POINT('Ctrl Pts',(-2.24706522913268,2.31083627944824,16.0297098442537));
#14637=CARTESIAN_POINT('Ctrl Pts',(-2.13911159763896,2.41221456214176,16.0202484306416));
#14638=CARTESIAN_POINT('Ctrl Pts',(-2.06940423957531,2.47227447686804,16.0142559774932));
#14639=CARTESIAN_POINT('Ctrl Pts',(-1.80723586196336,2.67929502855329,15.9921567990691));
#14640=CARTESIAN_POINT('Ctrl Pts',(-1.60096405729656,2.80742275405419,15.9755079529812));
#14641=CARTESIAN_POINT('Ctrl Pts',(-1.29863867972593,2.95097160053913,15.9532370945625));
#14642=CARTESIAN_POINT('Ctrl Pts',(-1.21328965092433,2.98707674896513,15.9471729641674));
#14643=CARTESIAN_POINT('Ctrl Pts',(-1.11342568548895,3.02433387828785,15.9404213920042));
#14644=CARTESIAN_POINT('Ctrl Pts',(-1.10032387213833,3.02912521323038,15.9395422946014));
#14645=CARTESIAN_POINT('Ctrl Pts',(-1.08052535662699,3.03622012608023,15.9382243656541));
#14646=CARTESIAN_POINT('Ctrl Pts',(-1.0738516984519,3.03858688082716,15.9377819099325));
#14647=CARTESIAN_POINT('Ctrl Pts',(-1.06190188947173,3.04278049046413,15.9369929189964));
#14648=CARTESIAN_POINT('Ctrl Pts',(-1.05662875970516,3.04461564105465,15.9366458970453));
#14649=CARTESIAN_POINT('Ctrl Pts',(-1.04520277810696,3.04855884222297,15.935896431265));
#14650=CARTESIAN_POINT('Ctrl Pts',(-1.03904832468023,3.05066196793472,15.9354942808065));
#14651=CARTESIAN_POINT('Ctrl Pts',(-1.02184283421211,3.05648339330068,15.9343742063884));
#14652=CARTESIAN_POINT('Ctrl Pts',(-1.01077779045486,3.06016041725948,15.9336586838561));
#14653=CARTESIAN_POINT('Ctrl Pts',(-0.946366892727751,3.08117732067997,
15.9295201167653));
#14654=CARTESIAN_POINT('Ctrl Pts',(-0.892591959911847,3.09718330987246,
15.9261705471776));
#14655=CARTESIAN_POINT('Ctrl Pts',(-0.592975555588708,3.17791054502726,
15.9079475308191));
#14656=CARTESIAN_POINT('Ctrl Pts',(-0.340543308574817,3.21477729250494,
15.8941533022085));
#14657=CARTESIAN_POINT('Ctrl Pts',(0.0774326007228325,3.22598446194281,
15.870535603872));
#14658=CARTESIAN_POINT('Ctrl Pts',(0.241320837740447,3.21787590909853,15.8610925732337));
#14659=CARTESIAN_POINT('Ctrl Pts',(0.425605468836167,3.19459818278516,15.8499203649169));
#14660=CARTESIAN_POINT('Ctrl Pts',(0.447312713613298,3.19163106647518,15.8485958719627));
#14661=CARTESIAN_POINT('Ctrl Pts',(0.481944959607074,3.18653701431389,15.8464684505476));
#14662=CARTESIAN_POINT('Ctrl Pts',(0.494890411856844,3.18455217573653,15.8456700248987));
#14663=CARTESIAN_POINT('Ctrl Pts',(0.517779777362965,3.18089976595167,15.8442524835251));
#14664=CARTESIAN_POINT('Ctrl Pts',(0.527728695034615,3.17926432365178,15.8436343972548));
#14665=CARTESIAN_POINT('Ctrl Pts',(0.548369791740922,3.17577170217175,15.8423479308152));
#14666=CARTESIAN_POINT('Ctrl Pts',(0.559060578125948,3.17390715021434,15.8416793226778));
#14667=CARTESIAN_POINT('Ctrl Pts',(0.586649850824553,3.1689516604034,15.839947831647));
#14668=CARTESIAN_POINT('Ctrl Pts',(0.603533238405973,3.1657795698952,15.8388823694926));
#14669=CARTESIAN_POINT('Ctrl Pts',(0.675461159189337,3.15166928931439,15.8343175951885));
#14670=CARTESIAN_POINT('Ctrl Pts',(0.730237513473711,3.13942982430677,15.8307769157458));
#14671=CARTESIAN_POINT('Ctrl Pts',(0.873873755451342,3.10337270656353,15.8213155147237));
#14672=CARTESIAN_POINT('Ctrl Pts',(0.96207676678163,3.07717130916081,15.8153230706453));
#14673=CARTESIAN_POINT('Ctrl Pts',(1.18657921008579,2.99988476433525,15.7996156278636));
#14674=CARTESIAN_POINT('Ctrl Pts',(1.32075392492261,2.9432775479278,15.789774303263));
#14675=CARTESIAN_POINT('Ctrl Pts',(1.61878358001441,2.79304754868328,15.7671825403333));
#14676=CARTESIAN_POINT('Ctrl Pts',(1.7791985632143,2.69370450917543,15.7544651746456));
#14677=CARTESIAN_POINT('Ctrl Pts',(1.94175790024126,2.57214077514126,15.7415997014587));
#14678=CARTESIAN_POINT('Ctrl Pts',(1.95342308186026,2.56329284176574,15.7406767354938));
#14679=CARTESIAN_POINT('Ctrl Pts',(1.97067508270864,2.55002118535784,15.7393126175928));
#14680=CARTESIAN_POINT('Ctrl Pts',(1.97630798928483,2.54565808018037,15.7388673647797));
#14681=CARTESIAN_POINT('Ctrl Pts',(1.98633197584778,2.53784043194077,15.7380753435445));
#14682=CARTESIAN_POINT('Ctrl Pts',(1.99072857456762,2.53439312662783,15.7377280727559));
#14683=CARTESIAN_POINT('Ctrl Pts',(1.9951335648479,2.53092070626502,15.7373802610597));
#14684=CARTESIAN_POINT('Ctrl Pts',(1.99515083707017,2.53090709041678,15.7373788972716));
#14685=CARTESIAN_POINT('Ctrl Pts',(1.99518510569134,2.53088007558554,15.7373761914777));
#14686=CARTESIAN_POINT('Ctrl Pts',(1.99520210208371,2.53086667661676,15.7373748494722));
#14687=CARTESIAN_POINT('Ctrl Pts',(1.9952358245205,2.53084009125501,15.7373721868109));
#14688=CARTESIAN_POINT('Ctrl Pts',(1.99525255057485,2.53082690486295,15.7373708661543));
#14689=CARTESIAN_POINT('Ctrl Pts',(1.99528573758302,2.53080074054383,15.7373682457761));
#14690=CARTESIAN_POINT('Ctrl Pts',(1.99530219859447,2.53078776257976,15.7373669460499));
#14691=CARTESIAN_POINT('Ctrl Pts',(1.9953348608891,2.53076201090627,15.7373643671084));
#14692=CARTESIAN_POINT('Ctrl Pts',(1.99535106212959,2.53074923723864,15.7373630878964));
#14693=CARTESIAN_POINT('Ctrl Pts',(1.99538320984656,2.53072389026832,15.737360549591));
#14694=CARTESIAN_POINT('Ctrl Pts',(1.99539915636008,2.53071131694428,15.7373592904947));
#14695=CARTESIAN_POINT('Ctrl Pts',(2.0004341331456,2.52674131903528,15.7369617419573));
#14696=CARTESIAN_POINT('Ctrl Pts',(2.00544143099379,2.52276893173033,15.7365665288906));
#14697=CARTESIAN_POINT('Ctrl Pts',(2.01911267217375,2.51185684321436,15.7354878017362));
#14698=CARTESIAN_POINT('Ctrl Pts',(2.02775272687349,2.50488715729205,15.7348064004234));
#14699=CARTESIAN_POINT('Ctrl Pts',(2.04712329807086,2.48909556354318,15.7332790593965));
#14700=CARTESIAN_POINT('Ctrl Pts',(2.05783320464941,2.48024858413226,15.7324348271544));
#14701=CARTESIAN_POINT('Ctrl Pts',(2.09093348659294,2.45254390910229,15.7298251367465));
#14702=CARTESIAN_POINT('Ctrl Pts',(2.11312498442638,2.43344969074064,15.7280748141098));
#14703=CARTESIAN_POINT('Ctrl Pts',(2.19903686834224,2.35746695244925,15.721281771039));
#14704=CARTESIAN_POINT('Ctrl Pts',(2.26074943910409,2.29835324778644,15.7163646434504));
#14705=CARTESIAN_POINT('Ctrl Pts',(2.46445226745962,2.08707449693093,15.6997039356266));
#14706=CARTESIAN_POINT('Ctrl Pts',(2.5940175084814,1.92366368301244,15.6883031830026));
#14707=CARTESIAN_POINT('Ctrl Pts',(2.78241709293188,1.63206084422852,15.6685552412657));
#14708=CARTESIAN_POINT('Ctrl Pts',(2.85025277870055,1.51046997480914,15.6604775115245));
#14709=CARTESIAN_POINT('Ctrl Pts',(2.9191744353878,1.36564717326451,15.6508258111849));
#14710=CARTESIAN_POINT('Ctrl Pts',(2.92813966916638,1.34631706164547,15.6495371693472));
#14711=CARTESIAN_POINT('Ctrl Pts',(2.94223215709115,1.3151252550413,15.6474565014156));
#14712=CARTESIAN_POINT('Ctrl Pts',(2.94748099658353,1.30331894400933,15.6466686671447));
#14713=CARTESIAN_POINT('Ctrl Pts',(2.95668837845431,1.28226850298116,15.64526332467));
#14714=CARTESIAN_POINT('Ctrl Pts',(2.96067493846058,1.27303675758182,15.6446467867505));
#14715=CARTESIAN_POINT('Ctrl Pts',(2.96890532592276,1.25372973484051,15.6433568487929));
#14716=CARTESIAN_POINT('Ctrl Pts',(2.97314121574874,1.24365123278802,15.6426831873608));
#14717=CARTESIAN_POINT('Ctrl Pts',(2.98404041537881,1.21734469598425,15.6409239470946));
#14718=CARTESIAN_POINT('Ctrl Pts',(2.99062257811499,1.20108362952207,15.6398356304403));
#14719=CARTESIAN_POINT('Ctrl Pts',(3.01895604927355,1.1294094242253,15.635034270957));
#14720=CARTESIAN_POINT('Ctrl Pts',(3.03930119437825,1.0734564562034,15.631274343199));
#14721=CARTESIAN_POINT('Ctrl Pts',(3.08962533327696,0.922129779437808,15.6210674946168));
#14722=CARTESIAN_POINT('Ctrl Pts',(3.1167342229732,0.825876891313651,15.6145339986356));
#14723=CARTESIAN_POINT('Ctrl Pts',(3.19488793012977,0.489101728728742,15.5915790097839));
#14724=CARTESIAN_POINT('Ctrl Pts',(3.22287224785179,0.244136288781952,15.574647590367));
#14725=CARTESIAN_POINT('Ctrl Pts',(3.22274959861812,-0.00160844855869799,
15.5583907367487));
#14726=CARTESIAN_POINT('Ctrl Pts',(3.22274959627015,-0.00161314617362317,
15.5583904259856));
#14727=CARTESIAN_POINT('Ctrl Pts',(3.2227108806265,-0.0789594071645176,
15.5532737099094));
#14728=CARTESIAN_POINT('Ctrl Pts',(3.21988768448667,-0.156287636072416,
15.5482375533698));
#14729=CARTESIAN_POINT('Ctrl Pts',(3.21357695463654,-0.243178797591008,
15.5427212586633));
#14730=CARTESIAN_POINT('Ctrl Pts',(3.21282594566517,-0.252907531430216,
15.542105655882));
#14731=CARTESIAN_POINT('Ctrl Pts',(3.21150074981319,-0.269114833295441,
15.5410836570118));
#14732=CARTESIAN_POINT('Ctrl Pts',(3.21095112233921,-0.275595267067559,
15.5406759600701));
#14733=CARTESIAN_POINT('Ctrl Pts',(3.20991860236183,-0.287346732048848,
15.5399384224973));
#14734=CARTESIAN_POINT('Ctrl Pts',(3.209442336118,-0.292618301374302,15.5396082184293));
#14735=CARTESIAN_POINT('Ctrl Pts',(3.20843766540564,-0.303440937409622,
15.538931664499));
#14736=CARTESIAN_POINT('Ctrl Pts',(3.20790784723639,-0.308991747094943,
15.5385854096936));
#14737=CARTESIAN_POINT('Ctrl Pts',(3.20668325815074,-0.321478827744767,
15.5378081289579));
#14738=CARTESIAN_POINT('Ctrl Pts',(3.20598038983315,-0.328414215522219,
15.5373775643518));
#14739=CARTESIAN_POINT('Ctrl Pts',(3.20412279489459,-0.346169136152987,
15.5362780967607));
#14740=CARTESIAN_POINT('Ctrl Pts',(3.20293575601009,-0.356985302614786,
15.5356109721792));
#14741=CARTESIAN_POINT('Ctrl Pts',(3.19562998028578,-0.420582770401667,
15.5317029614291));
#14742=CARTESIAN_POINT('Ctrl Pts',(3.18826105332776,-0.473215647350341,
15.5285278329405));
#14743=CARTESIAN_POINT('Ctrl Pts',(3.17271221829946,-0.567269456737749,
15.5229217967447));
#14744=CARTESIAN_POINT('Ctrl Pts',(3.16501408194424,-0.608755771289282,
15.5204729487845));
#14745=CARTESIAN_POINT('Ctrl Pts',(3.1094337632759,-0.878629214621431,15.5046311665702));
#14746=CARTESIAN_POINT('Ctrl Pts',(3.03768038320479,-1.10139801172867,15.4919202563381));
#14747=CARTESIAN_POINT('Ctrl Pts',(2.90246880253642,-1.40407349179623,15.4731002291654));
#14748=CARTESIAN_POINT('Ctrl Pts',(2.85837451762567,-1.49179099612132,15.4674519833554));
#14749=CARTESIAN_POINT('Ctrl Pts',(2.78158821541533,-1.62859993871312,15.4582142128571));
#14750=CARTESIAN_POINT('Ctrl Pts',(2.75143186929814,-1.67904519594636,15.4547099616558));
#14751=CARTESIAN_POINT('Ctrl Pts',(2.71054796602091,-1.74337380881597,15.4500988674831));
#14752=CARTESIAN_POINT('Ctrl Pts',(2.70106166564937,-1.75803537309816,15.4490380825559));
#14753=CARTESIAN_POINT('Ctrl Pts',(2.68545328500086,-1.78173436594796,15.4473070207924));
#14754=CARTESIAN_POINT('Ctrl Pts',(2.67940353976657,-1.79081918773906,15.4466394670953));
#14755=CARTESIAN_POINT('Ctrl Pts',(2.66768869893312,-1.80821895724985,15.4453531998768));
#14756=CARTESIAN_POINT('Ctrl Pts',(2.66203057786545,-1.81653846384249,15.4447347558582));
#14757=CARTESIAN_POINT('Ctrl Pts',(2.64899643833406,-1.8355117377106,15.4433164037156));
#14758=CARTESIAN_POINT('Ctrl Pts',(2.64159497334884,-1.84614773473744,15.4425155293757));
#14759=CARTESIAN_POINT('Ctrl Pts',(2.62178031364328,-1.87425852015152,15.4403832752994));
#14760=CARTESIAN_POINT('Ctrl Pts',(2.6092567417693,-1.89165436405438,15.4390476603869));
#14761=CARTESIAN_POINT('Ctrl Pts',(2.5114539465005,-2.02468792196624,15.4287070273024));
#14762=CARTESIAN_POINT('Ctrl Pts',(2.41871275476403,-2.13461486975569,15.4194074157961));
#14763=CARTESIAN_POINT('Ctrl Pts',(2.17454436311254,-2.38761862145462,15.3960933350424));
#14764=CARTESIAN_POINT('Ctrl Pts',(2.0159867692261,-2.52292555332484,15.3818635396957));
#14765=CARTESIAN_POINT('Ctrl Pts',(1.7782498882188,-2.6889920233804,15.3624143870174));
#14766=CARTESIAN_POINT('Ctrl Pts',(1.70920548017092,-2.73339884891466,15.3569677881199));
#14767=CARTESIAN_POINT('Ctrl Pts',(1.61398892275687,-2.78961825197405,15.3497924053245));
#14768=CARTESIAN_POINT('Ctrl Pts',(1.58924891428097,-2.80378641186404,15.3479574960491));
#14769=CARTESIAN_POINT('Ctrl Pts',(1.55240655941075,-2.82424099841315,15.3452717844471));
#14770=CARTESIAN_POINT('Ctrl Pts',(1.54044775669879,-2.8307815292763,15.3444072036568));
#14771=CARTESIAN_POINT('Ctrl Pts',(1.51874519240997,-2.8424728773377,15.3428516232039));
#14772=CARTESIAN_POINT('Ctrl Pts',(1.5090158884109,-2.84764992137354,15.3421590950795));
#14773=CARTESIAN_POINT('Ctrl Pts',(1.49365846007077,-2.85572092674836,15.3410737897865));
#14774=CARTESIAN_POINT('Ctrl Pts',(1.4880481502379,-2.85864833636796,15.3406789462423));
#14775=CARTESIAN_POINT('Ctrl Pts',(1.48241445003584,-2.86156687168075,15.3402841217297));
#14776=CARTESIAN_POINT('Ctrl Pts',(1.48239970282712,-2.86157451131959,15.340283088218));
#14777=CARTESIAN_POINT('Ctrl Pts',(1.48237012412448,-2.8615898339703,15.3402810153106));
#14778=CARTESIAN_POINT('Ctrl Pts',(1.48235529270574,-2.86159751694159,15.3402799759204));
#14779=CARTESIAN_POINT('Ctrl Pts',(1.48232554508341,-2.86161292651109,15.3402778912213));
#14780=CARTESIAN_POINT('Ctrl Pts',(1.48231062880247,-2.86162065314769,15.3402768459072));
#14781=CARTESIAN_POINT('Ctrl Pts',(1.48228071093834,-2.86163615031079,15.3402747493245));
#14782=CARTESIAN_POINT('Ctrl Pts',(1.48226570923642,-2.86164392089709,15.3402736980477));
#14783=CARTESIAN_POINT('Ctrl Pts',(1.48223561981647,-2.86165950632426,15.3402715894902));
#14784=CARTESIAN_POINT('Ctrl Pts',(1.48222053217063,-2.86166732112601,15.3402705322146));
#14785=CARTESIAN_POINT('Ctrl Pts',(1.47723877439722,-2.86424762397113,15.3399214365737));
#14786=CARTESIAN_POINT('Ctrl Pts',(1.47226548688608,-2.86680714118089,15.3395742367904));
#14787=CARTESIAN_POINT('Ctrl Pts',(1.46088028386158,-2.87262912900951,15.3387823468855));
#14788=CARTESIAN_POINT('Ctrl Pts',(1.45446410261801,-2.87588308058095,15.338338195718));
#14789=CARTESIAN_POINT('Ctrl Pts',(1.43464353227989,-2.8858517389273,15.3369725118349));
#14790=CARTESIAN_POINT('Ctrl Pts',(1.42120291669234,-2.8924945312867,15.3360553729145));
#14791=CARTESIAN_POINT('Ctrl Pts',(1.28251169207302,-2.95984015026915,15.3266783291994));
#14792=CARTESIAN_POINT('Ctrl Pts',(1.15348307675403,-3.0124702134183,15.3186763870398));
#14793=CARTESIAN_POINT('Ctrl Pts',(0.837420529166947,-3.11809063574651,
15.2998557413592));
#14794=CARTESIAN_POINT('Ctrl Pts',(0.648225825811683,-3.1628415811601,15.2891887790513));
#14795=CARTESIAN_POINT('Ctrl Pts',(0.365094209550788,-3.20332406525421,
15.2729064436606));
#14796=CARTESIAN_POINT('Ctrl Pts',(0.273525426161436,-3.21243844413027,
15.2675972366621));
#14797=CARTESIAN_POINT('Ctrl Pts',(0.125662006465762,-3.22078818815127,
15.2588644583289));
#14798=CARTESIAN_POINT('Ctrl Pts',(0.0695567355263464,-3.22248797921902,
15.2555144952301));
#14799=CARTESIAN_POINT('Ctrl Pts',(-0.00374093713873998,-3.2227936162913,
15.2510790177485));
#14800=CARTESIAN_POINT('Ctrl Pts',(-0.0209200323831022,-3.22272788523748,
15.2500352465334));
#14801=CARTESIAN_POINT('Ctrl Pts',(-0.0489490639656499,-3.222396518736,
15.2483250669003));
#14802=CARTESIAN_POINT('Ctrl Pts',(-0.0597997776225279,-3.22221341888856,
15.2476612580956));
#14803=CARTESIAN_POINT('Ctrl Pts',(-0.080729277895057,-3.22175449125052,
15.2463773907639));
#14804=CARTESIAN_POINT('Ctrl Pts',(-0.0908081146579377,-3.22148616337669,
15.245757575577));
#14805=CARTESIAN_POINT('Ctrl Pts',(-0.113975566794437,-3.2207605704684,
15.2443292075589));
#14806=CARTESIAN_POINT('Ctrl Pts',(-0.127062918792827,-3.22027080982937,
15.2435196420365));
#14807=CARTESIAN_POINT('Ctrl Pts',(-0.162034273671959,-3.21874858092409,
15.2413490439872));
#14808=CARTESIAN_POINT('Ctrl Pts',(-0.183911044277697,-3.21757272218581,
15.2399835308476));
#14809=CARTESIAN_POINT('Ctrl Pts',(-0.369290110272627,-3.20571200294866,
15.2283455044269));
#14810=CARTESIAN_POINT('Ctrl Pts',(-0.531744731673002,-3.18279711704283,
15.21768579272));
#14811=CARTESIAN_POINT('Ctrl Pts',(-0.93998526669209,-3.09308113977407,
15.1898078442972));
#14812=CARTESIAN_POINT('Ctrl Pts',(-1.1808989702315,-3.00935143336284,15.1722623424249));
#14813=CARTESIAN_POINT('Ctrl Pts',(-1.4315227045649,-2.88746631098736,15.1540319917307));
#14814=CARTESIAN_POINT('Ctrl Pts',(-1.45345287857575,-2.87648981511593,
15.1524378008715));
#14815=CARTESIAN_POINT('Ctrl Pts',(-1.47525540626678,-2.86526421971528,
15.1508554073139));
#14816=CARTESIAN_POINT('Ctrl Pts',(-1.47525516809596,-2.86526434234368,
14.9065719799118));
#14817=CARTESIAN_POINT('Ctrl Pts',(-1.29829935559395,-2.95637460154743,
14.9200024838139));
#14818=CARTESIAN_POINT('Ctrl Pts',(-1.11317899372009,-3.0309507378844,14.933618121696));
#14819=CARTESIAN_POINT('Ctrl Pts',(-0.872313497822718,-3.1028859111795,
14.9500235892702));
#14820=CARTESIAN_POINT('Ctrl Pts',(-0.822036044264079,-3.11658295187011,
14.9533771319594));
#14821=CARTESIAN_POINT('Ctrl Pts',(-0.760373262704522,-3.131785450141,14.9573862220262));
#14822=CARTESIAN_POINT('Ctrl Pts',(-0.74928660001373,-3.13445644483712,
14.9581029764629));
#14823=CARTESIAN_POINT('Ctrl Pts',(-0.731910804305216,-3.13854515546142,
14.9592197245901));
#14824=CARTESIAN_POINT('Ctrl Pts',(-0.725631327811673,-3.14000291339942,
14.9596219630351));
#14825=CARTESIAN_POINT('Ctrl Pts',(-0.713900357826821,-3.14268914597708,
14.9603708374818));
#14826=CARTESIAN_POINT('Ctrl Pts',(-0.70845010232837,-3.14392227039492,
14.9607177292793));
#14827=CARTESIAN_POINT('Ctrl Pts',(-0.69601200923213,-3.14670241147349,
14.961507035731));
#14828=CARTESIAN_POINT('Ctrl Pts',(-0.689022221665945,-3.14824032814369,
14.9619489238048));
#14829=CARTESIAN_POINT('Ctrl Pts',(-0.670791855128358,-3.15218781219111,
14.9630972052505));
#14830=CARTESIAN_POINT('Ctrl Pts',(-0.659543288671677,-3.15456056777864,
14.9638015417738));
#14831=CARTESIAN_POINT('Ctrl Pts',(-0.586215240507551,-3.16961890466432,
14.9683672618144));
#14832=CARTESIAN_POINT('Ctrl Pts',(-0.523781173969791,-3.18053247477559,
14.9721346739348));
#14833=CARTESIAN_POINT('Ctrl Pts',(-0.428153420034432,-3.19435561081672,
14.9777785230944));
#14834=CARTESIAN_POINT('Ctrl Pts',(-0.395172938464891,-3.19860306908241,
14.9797022413641));
#14835=CARTESIAN_POINT('Ctrl Pts',(-0.123656983611868,-3.22930704116125,
14.9953948875432));
#14836=CARTESIAN_POINT('Ctrl Pts',(0.117090623299411,-3.22955367009755,
15.0084506593329));
#14837=CARTESIAN_POINT('Ctrl Pts',(0.44725348127025,-3.19289485256166,15.0273604278498));
#14838=CARTESIAN_POINT('Ctrl Pts',(0.538377760853058,-3.1787986189893,15.0326799729067));
#14839=CARTESIAN_POINT('Ctrl Pts',(0.683889636977428,-3.1498525607941,15.0414279761806));
#14840=CARTESIAN_POINT('Ctrl Pts',(0.738712252789463,-3.13744797860229,
15.0447824777654));
#14841=CARTESIAN_POINT('Ctrl Pts',(0.809835523821491,-3.11938764433208,
15.0492229038057));
#14842=CARTESIAN_POINT('Ctrl Pts',(0.826456555975406,-3.11502526387012,
15.0502669594897));
#14843=CARTESIAN_POINT('Ctrl Pts',(0.853514687341974,-3.10769174506031,
15.0519773367249));
#14844=CARTESIAN_POINT('Ctrl Pts',(0.863973210121691,-3.10480041088996,
15.0526410558339));
#14845=CARTESIAN_POINT('Ctrl Pts',(0.884116817806534,-3.0991219049677,15.0539245604343));
#14846=CARTESIAN_POINT('Ctrl Pts',(0.893803834905607,-3.09634200798374,
15.0545441017475));
#14847=CARTESIAN_POINT('Ctrl Pts',(0.916039227573804,-3.08984804654203,
15.0559715662417));
#14848=CARTESIAN_POINT('Ctrl Pts',(0.928578274402576,-3.08610291425306,
15.0567804995527));
#14849=CARTESIAN_POINT('Ctrl Pts',(0.962021814020893,-3.07589180458655,
15.0589487917748));
#14850=CARTESIAN_POINT('Ctrl Pts',(0.982883561545557,-3.06928920606619,
15.0603126181913));
#14851=CARTESIAN_POINT('Ctrl Pts',(1.15835274523631,-3.01178204994397,15.0718811047408));
#14852=CARTESIAN_POINT('Ctrl Pts',(1.30894244894143,-2.94945206014198,15.0824676666502));
#14853=CARTESIAN_POINT('Ctrl Pts',(1.67886041512723,-2.76241591858958,15.1101061793388));
#14854=CARTESIAN_POINT('Ctrl Pts',(1.88945805837219,-2.62287187205253,15.1274798689264));
#14855=CARTESIAN_POINT('Ctrl Pts',(2.12697498939373,-2.42190379463283,15.1478678258756));
#14856=CARTESIAN_POINT('Ctrl Pts',(2.17122233063687,-2.3823172012437,15.1517004821305));
#14857=CARTESIAN_POINT('Ctrl Pts',(2.22296249058293,-2.33338717496466,15.1561985241871));
#14858=CARTESIAN_POINT('Ctrl Pts',(2.23152615756828,-2.32519869284261,15.1569435603175));
#14859=CARTESIAN_POINT('Ctrl Pts',(2.24474895184221,-2.31241486807031,15.1580945197551));
#14860=CARTESIAN_POINT('Ctrl Pts',(2.24943946488151,-2.30785235110682,15.158502913516));
#14861=CARTESIAN_POINT('Ctrl Pts',(2.25810219319246,-2.2993745137522,15.1592573165035));
#14862=CARTESIAN_POINT('Ctrl Pts',(2.26207810609292,-2.29546320208016,15.1596036182839));
#14863=CARTESIAN_POINT('Ctrl Pts',(2.2710369494876,-2.28660404204402,15.160384078404));
#14864=CARTESIAN_POINT('Ctrl Pts',(2.27601386131793,-2.28165023093473,15.1608177570211));
#14865=CARTESIAN_POINT('Ctrl Pts',(2.29064004655196,-2.26699645659335,15.1620927248841));
#14866=CARTESIAN_POINT('Ctrl Pts',(2.30024392973773,-2.25725112386673,15.1629305046071));
#14867=CARTESIAN_POINT('Ctrl Pts',(2.36923969762895,-2.18634151118276,15.1689563304573));
#14868=CARTESIAN_POINT('Ctrl Pts',(2.42625149953874,-2.12289716652257,15.1739740825614));
#14869=CARTESIAN_POINT('Ctrl Pts',(2.64222566154837,-1.8624713134061,15.1934912494333));
#14870=CARTESIAN_POINT('Ctrl Pts',(2.78026869082285,-1.64932662340076,15.2072150144334));
#14871=CARTESIAN_POINT('Ctrl Pts',(2.93164122561744,-1.3415226797346,15.2267615279927));
#14872=CARTESIAN_POINT('Ctrl Pts',(2.96792671304666,-1.25921109209833,15.2319565669585));
#14873=CARTESIAN_POINT('Ctrl Pts',(3.02086127032029,-1.12408338171395,15.2405182810778));
#14874=CARTESIAN_POINT('Ctrl Pts',(3.03967535737743,-1.07216576834807,15.2438150545095));
#14875=CARTESIAN_POINT('Ctrl Pts',(3.06254886754779,-1.00359530998725,15.2481896447958));
#14876=CARTESIAN_POINT('Ctrl Pts',(3.06782305692954,-0.987355450817952,
15.2492271529717));
#14877=CARTESIAN_POINT('Ctrl Pts',(3.07623019802983,-0.960751035278142,
15.2509294982839));
#14878=CARTESIAN_POINT('Ctrl Pts',(3.07944045195426,-0.950411111783789,
15.2515917799493));
#14879=CARTESIAN_POINT('Ctrl Pts',(3.08554078223212,-0.930407108938799,
15.2528744065484));
#14880=CARTESIAN_POINT('Ctrl Pts',(3.08843771305024,-0.920745239519761,
15.2534945175237));
#14881=CARTESIAN_POINT('Ctrl Pts',(3.09500452235835,-0.898463849059415,
15.2549260324065));
#14882=CARTESIAN_POINT('Ctrl Pts',(3.09864264230274,-0.885835226531199,
15.2557384652094));
#14883=CARTESIAN_POINT('Ctrl Pts',(3.10818395560056,-0.851937370650033,
15.2579222581628));
#14884=CARTESIAN_POINT('Ctrl Pts',(3.11394596423509,-0.830629446884494,
15.2592981867979));
#14885=CARTESIAN_POINT('Ctrl Pts',(3.16288271534347,-0.641991930012578,
15.2715095081236));
#14886=CARTESIAN_POINT('Ctrl Pts',(3.19274570335591,-0.471527825870998,
15.2827776785713));
#14887=CARTESIAN_POINT('Ctrl Pts',(3.21818505364414,-0.198988189110471,
15.3010763308054));
#14888=CARTESIAN_POINT('Ctrl Pts',(3.22283890548999,-0.0980786939093705,
15.3079064951729));
#14889=CARTESIAN_POINT('Ctrl Pts',(3.22258736202469,0.183491806723148,15.3269679301503));
#14890=CARTESIAN_POINT('Ctrl Pts',(3.20724313318432,0.363789740046964,15.3391893359958));
#14891=CARTESIAN_POINT('Ctrl Pts',(3.1727669624573,0.565917522094113,15.3523170495701));
#14892=CARTESIAN_POINT('Ctrl Pts',(3.16839154439129,0.589921982582755,15.3538664215946));
#14893=CARTESIAN_POINT('Ctrl Pts',(3.16202291668154,0.622744132860431,15.3559695345655));
#14894=CARTESIAN_POINT('Ctrl Pts',(3.16026474166081,0.631605848524153,15.3565358138219));
#14895=CARTESIAN_POINT('Ctrl Pts',(3.15740969311579,0.64568569841765,15.3574329553973));
#14896=CARTESIAN_POINT('Ctrl Pts',(3.15633711019876,0.650908625761379,15.357765183688));
#14897=CARTESIAN_POINT('Ctrl Pts',(3.15409268895684,0.661701799929635,15.35845052617));
#14898=CARTESIAN_POINT('Ctrl Pts',(3.15291905402558,0.667271610174321,15.3588035257909));
#14899=CARTESIAN_POINT('Ctrl Pts',(3.15008150469355,0.680563349111567,15.3596443734835));
#14900=CARTESIAN_POINT('Ctrl Pts',(3.14840393111076,0.688282389750243,15.3601314406247));
#14901=CARTESIAN_POINT('Ctrl Pts',(3.1426210158562,0.714427808008232,15.3617772136713));
#14902=CARTESIAN_POINT('Ctrl Pts',(3.13838206541777,0.732824667304999,15.3629285142256));
#14903=CARTESIAN_POINT('Ctrl Pts',(3.11372949269161,0.835676615343761,15.3693328080026));
#14904=CARTESIAN_POINT('Ctrl Pts',(3.09006683023854,0.919323945272005,15.3744191545012));
#14905=CARTESIAN_POINT('Ctrl Pts',(2.99287163818115,1.21646724982702,15.3923770665024));
#14906=CARTESIAN_POINT('Ctrl Pts',(2.90034430817645,1.42305548734032,15.4046934005287));
#14907=CARTESIAN_POINT('Ctrl Pts',(2.71127995477215,1.74865833806095,15.426035671086));
#14908=CARTESIAN_POINT('Ctrl Pts',(2.62653350528946,1.87354160518883,15.4347585829232));
#14909=CARTESIAN_POINT('Ctrl Pts',(2.5200063902329,2.00901780520061,15.4451270220551));
#14910=CARTESIAN_POINT('Ctrl Pts',(2.50647583767706,2.02587353718917,15.4464339558098));
#14911=CARTESIAN_POINT('Ctrl Pts',(2.48453227643423,2.05265344040299,15.4485383481939));
#14912=CARTESIAN_POINT('Ctrl Pts',(2.47622680021474,2.06266517039267,15.4493314567514));
#14913=CARTESIAN_POINT('Ctrl Pts',(2.46138735199161,2.08033439386671,15.4507426841233));
#14914=CARTESIAN_POINT('Ctrl Pts',(2.45487765215542,2.08801211589994,15.4513598023895));
#14915=CARTESIAN_POINT('Ctrl Pts',(2.44125352746493,2.10392900893504,15.4526473947996));
#14916=CARTESIAN_POINT('Ctrl Pts',(2.43413312286338,2.11216287144763,15.4533181123987));
#14917=CARTESIAN_POINT('Ctrl Pts',(2.41556145657357,2.13342005910516,15.4550618759026));
#14918=CARTESIAN_POINT('Ctrl Pts',(2.40404666331769,2.14638717866029,15.456137572424));
#14919=CARTESIAN_POINT('Ctrl Pts',(2.35379660027261,2.20206348717016,15.4608089817069));
#14920=CARTESIAN_POINT('Ctrl Pts',(2.31402570509347,2.24381959628616,15.4644485105213));
#14921=CARTESIAN_POINT('Ctrl Pts',(2.20543048901519,2.3518764086763,15.4742439138608));
#14922=CARTESIAN_POINT('Ctrl Pts',(2.13474513109526,2.41621743724114,15.4804779808176));
#14923=CARTESIAN_POINT('Ctrl Pts',(1.95208527064258,2.56820385871222,15.4962241804197));
#14924=CARTESIAN_POINT('Ctrl Pts',(1.83697361706025,2.65176004065423,15.5058415686161));
#14925=CARTESIAN_POINT('Ctrl Pts',(1.5591531104243,2.82662841058469,15.5280611769739));
#14926=CARTESIAN_POINT('Ctrl Pts',(1.3932548539505,2.91198280314926,15.5406286829045));
#14927=CARTESIAN_POINT('Ctrl Pts',(1.20732307380647,2.98809365086722,15.5533627456282));
#14928=CARTESIAN_POINT('Ctrl Pts',(1.19371161897893,2.99355729205417,15.5542873673402));
#14929=CARTESIAN_POINT('Ctrl Pts',(1.17342952121593,3.00153819536411,15.5556533565314));
#14930=CARTESIAN_POINT('Ctrl Pts',(1.16678728527009,3.00412646417263,15.5560988423265));
#14931=CARTESIAN_POINT('Ctrl Pts',(1.15492540928409,3.00870338504555,15.5568910086825));
#14932=CARTESIAN_POINT('Ctrl Pts',(1.1497091489723,3.01070052223715,15.5572381934432));
#14933=CARTESIAN_POINT('Ctrl Pts',(1.13844333497434,3.01498028865391,15.557985490875));
#14934=CARTESIAN_POINT('Ctrl Pts',(1.13239211397071,3.01725827032956,15.5583853238786));
#14935=CARTESIAN_POINT('Ctrl Pts',(1.11556693076002,3.02353436335561,15.5594928136228));
#14936=CARTESIAN_POINT('Ctrl Pts',(1.10477825144893,3.02749312927487,15.560198154615));
#14937=CARTESIAN_POINT('Ctrl Pts',(1.04369248128592,3.04953774004932,15.5641659427037));
#14938=CARTESIAN_POINT('Ctrl Pts',(0.992969491682906,3.06642899561575,15.5673618124813));
#14939=CARTESIAN_POINT('Ctrl Pts',(0.696910994248216,3.15690173020031,15.5855746910391));
#14940=CARTESIAN_POINT('Ctrl Pts',(0.443902654072817,3.20229491667954,15.5994687165154));
#14941=CARTESIAN_POINT('Ctrl Pts',(0.0235701095507269,3.22687877549539,
15.6232457044706));
#14942=CARTESIAN_POINT('Ctrl Pts',(-0.141500873429374,3.22385934761599,
15.6327437279834));
#14943=CARTESIAN_POINT('Ctrl Pts',(-0.32742865069139,3.20614857736987,15.6439771753053));
#14944=CARTESIAN_POINT('Ctrl Pts',(-0.349231582890425,3.20384698239396,
15.645302562535));
#14945=CARTESIAN_POINT('Ctrl Pts',(-0.384020645301622,3.19981519546685,
15.6474310076476));
#14946=CARTESIAN_POINT('Ctrl Pts',(-0.39702289179336,3.19822794006303,15.6482295539525));
#14947=CARTESIAN_POINT('Ctrl Pts',(-0.420013019274603,3.19527905387204,
15.6496470612445));
#14948=CARTESIAN_POINT('Ctrl Pts',(-0.430004923536417,3.19394973826159,
15.6502649912669));
#14949=CARTESIAN_POINT('Ctrl Pts',(-0.450734269057387,3.19109288578607,
15.6515508841718));
#14950=CARTESIAN_POINT('Ctrl Pts',(-0.461470550694857,3.18955798085794,
15.6522190736363));
#14951=CARTESIAN_POINT('Ctrl Pts',(-0.489173110943545,3.18545470527882,
15.6539489445611));
#14952=CARTESIAN_POINT('Ctrl Pts',(-0.506126823327988,3.18280499437272,
15.6550131977779));
#14953=CARTESIAN_POINT('Ctrl Pts',(-0.578295537855609,3.17093448886617,
15.6595679005907));
#14954=CARTESIAN_POINT('Ctrl Pts',(-0.633283649195949,3.16041175280476,
15.6630994983137));
#14955=CARTESIAN_POINT('Ctrl Pts',(-0.777517851192644,3.12889529467526,
15.672531069072));
#14956=CARTESIAN_POINT('Ctrl Pts',(-0.866185523354872,3.10551765598511,
15.6785022167234));
#14957=CARTESIAN_POINT('Ctrl Pts',(-1.18798919520071,3.00581833787166,15.7007860758781));
#14958=CARTESIAN_POINT('Ctrl Pts',(-1.4131737711651,2.90674848371405,15.7176609816698));
#14959=CARTESIAN_POINT('Ctrl Pts',(-1.70275000060226,2.73767771385391,15.7399541547865));
#14960=CARTESIAN_POINT('Ctrl Pts',(-1.77863327340503,2.68899679121665,15.7458483020379));
#14961=CARTESIAN_POINT('Ctrl Pts',(-1.86372628726903,2.62922689040783,15.7524344408872));
#14962=CARTESIAN_POINT('Ctrl Pts',(-1.87501828518518,2.6211860219332,15.7533079203244));
#14963=CARTESIAN_POINT('Ctrl Pts',(-1.89198315206013,2.60893985493122,15.7546190042539));
#14964=CARTESIAN_POINT('Ctrl Pts',(-1.8976944874296,2.60478848449593,15.7550601797469));
#14965=CARTESIAN_POINT('Ctrl Pts',(-1.90789502347874,2.59732271356847,15.7558476810571));
#14966=CARTESIAN_POINT('Ctrl Pts',(-1.91238928470421,2.59401540557045,15.7561944869903));
#14967=CARTESIAN_POINT('Ctrl Pts',(-1.92211180495464,2.58682164226112,15.7569443831182));
#14968=CARTESIAN_POINT('Ctrl Pts',(-1.92733686119527,2.58293101434563,15.757347175317));
#14969=CARTESIAN_POINT('Ctrl Pts',(-1.94192483542134,2.57199975281724,15.7584712490166));
#14970=CARTESIAN_POINT('Ctrl Pts',(-1.95126132753185,2.56492378764273,15.7591901001729));
#14971=CARTESIAN_POINT('Ctrl Pts',(-2.00584067779629,2.52308854842995,15.7633903640214));
#14972=CARTESIAN_POINT('Ctrl Pts',(-2.05019576566972,2.48718131586969,15.766795707816));
#14973=CARTESIAN_POINT('Ctrl Pts',(-2.2862224661448,2.28550076884227,15.7850162812929));
#14974=CARTESIAN_POINT('Ctrl Pts',(-2.45879921188954,2.09872822355117,15.7987688288909));
#14975=CARTESIAN_POINT('Ctrl Pts',(-2.70387232571146,1.76124059799048,15.8223291000407));
#14976=CARTESIAN_POINT('Ctrl Pts',(-2.78978619625217,1.62172024955394,15.8317592270355));
#14977=CARTESIAN_POINT('Ctrl Pts',(-2.8747619970212,1.45682552061323,15.8429167063826));
#14978=CARTESIAN_POINT('Ctrl Pts',(-2.8845948042191,1.43725777654506,15.8442406181248));
#14979=CARTESIAN_POINT('Ctrl Pts',(-2.8999858395167,1.40583465695759,15.846367140896));
#14980=CARTESIAN_POINT('Ctrl Pts',(-2.9056726763958,1.39404276900303,15.8471652533616));
#14981=CARTESIAN_POINT('Ctrl Pts',(-2.91561019502526,1.37311191689143,15.8485822585399));
#14982=CARTESIAN_POINT('Ctrl Pts',(-2.91989017239619,1.36398699521775,15.8492001227182));
#14983=CARTESIAN_POINT('Ctrl Pts',(-2.92868799083181,1.34499885034228,15.8504861458784));
#14984=CARTESIAN_POINT('Ctrl Pts',(-2.93319896703917,1.33513260398243,15.8511545327703));
#14985=CARTESIAN_POINT('Ctrl Pts',(-2.94472211309302,1.30958931635942,15.8528854893365));
#14986=CARTESIAN_POINT('Ctrl Pts',(-2.95165887018737,1.2938788183222,15.853950636899));
#14987=CARTESIAN_POINT('Ctrl Pts',(-2.98072193289662,1.22660610482275,15.8585143536885));
#14988=CARTESIAN_POINT('Ctrl Pts',(-3.00162409149051,1.17452882147131,15.8620542738914));
#14989=CARTESIAN_POINT('Ctrl Pts',(-3.05316937879825,1.03572727249111,15.8715137155713));
#14990=CARTESIAN_POINT('Ctrl Pts',(-3.08147630686023,0.948195910633212,
15.8775049358458));
#14991=CARTESIAN_POINT('Ctrl Pts',(-3.17066090111398,0.625937041287872,
15.8996251215533));
#14992=CARTESIAN_POINT('Ctrl Pts',(-3.20874665667649,0.385768970806537,
15.9162982716766));
#14993=CARTESIAN_POINT('Ctrl Pts',(-3.22366332413373,0.0513683403728577,
15.9385707444958));
#14994=CARTESIAN_POINT('Ctrl Pts',(-3.22381211465226,-0.0410223082529205,
15.9446158687836));
#14995=CARTESIAN_POINT('Ctrl Pts',(-3.21941550923888,-0.147226390992114,
15.9513488147855));
#14996=CARTESIAN_POINT('Ctrl Pts',(-3.21874865074398,-0.16114890996879,
15.9522271498805));
#14997=CARTESIAN_POINT('Ctrl Pts',(-3.21760704438148,-0.182133335606764,
15.9535440725008));
#14998=CARTESIAN_POINT('Ctrl Pts',(-3.21719933644135,-0.189198509149784,
15.9539862774193));
#14999=CARTESIAN_POINT('Ctrl Pts',(-3.21642846261519,-0.201833242083144,
15.9547748879391));
#15000=CARTESIAN_POINT('Ctrl Pts',(-3.2160740993547,-0.207403234703026,
15.955121779415));
#15001=CARTESIAN_POINT('Ctrl Pts',(-3.21527554960807,-0.219460667715434,
15.955871032363));
#15002=CARTESIAN_POINT('Ctrl Pts',(-3.21482619985199,-0.225947673348353,
15.9562731003021));
#15003=CARTESIAN_POINT('Ctrl Pts',(-3.21351626641155,-0.244062948751036,
15.9573931084661));
#15004=CARTESIAN_POINT('Ctrl Pts',(-3.21261219507871,-0.255688113063449,
15.9581086466714));
#15005=CARTESIAN_POINT('Ctrl Pts',(-3.20698828117226,-0.32325808286155,
15.9622503003687));
#15006=CARTESIAN_POINT('Ctrl Pts',(-3.20086994652675,-0.379080593150567,
15.9656028030611));
#15007=CARTESIAN_POINT('Ctrl Pts',(-3.1590247127134,-0.686461573874854,
15.9838202624834));
#15008=CARTESIAN_POINT('Ctrl Pts',(-3.09510251850728,-0.933292194484601,
15.9976076342173));
#15009=CARTESIAN_POINT('Ctrl Pts',(-2.94331132836656,-1.3228453379133,16.0212223361923));
#15010=CARTESIAN_POINT('Ctrl Pts',(-2.8722180485136,-1.4708345890606,16.0306703779535));
#15011=CARTESIAN_POINT('Ctrl Pts',(-2.77921972874936,-1.63172764995896,
16.0418478970592));
#15012=CARTESIAN_POINT('Ctrl Pts',(-2.76806455602381,-1.65058050445976,
16.0431721998444));
#15013=CARTESIAN_POINT('Ctrl Pts',(-2.74993609937473,-1.6805179117041,16.045299232101));
#15014=CARTESIAN_POINT('Ctrl Pts',(-2.74308582498165,-1.69167643213656,
16.0460974595615));
#15015=CARTESIAN_POINT('Ctrl Pts',(-2.73084233864018,-1.7113501316738,16.0475145978139));
#15016=CARTESIAN_POINT('Ctrl Pts',(-2.72547678991981,-1.71988238424385,
16.0481324794272));
#15017=CARTESIAN_POINT('Ctrl Pts',(-2.71425358809905,-1.73754501999016,
16.0494184679731));
#15018=CARTESIAN_POINT('Ctrl Pts',(-2.70838969121832,-1.74667126640836,
16.0500868024634));
#15019=CARTESIAN_POINT('Ctrl Pts',(-2.69312560497364,-1.77016576818989,
16.0518174708897));
#15020=CARTESIAN_POINT('Ctrl Pts',(-2.68365655786252,-1.78448867524749,
16.0528823810858));
#15021=CARTESIAN_POINT('Ctrl Pts',(-2.64277638724699,-1.84526282291843,
16.0574437037481));
#15022=CARTESIAN_POINT('Ctrl Pts',(-2.61027182183478,-1.89096332523365,
16.0609814132607));
#15023=CARTESIAN_POINT('Ctrl Pts',(-2.5214034177145,-2.00924974839013,16.0704334486528));
#15024=CARTESIAN_POINT('Ctrl Pts',(-2.46310191021845,-2.08030916168714,
16.0764193338204));
#15025=CARTESIAN_POINT('Ctrl Pts',(-2.23967647796577,-2.33004858550497,
16.098586514666));
#15026=CARTESIAN_POINT('Ctrl Pts',(-2.05752235845153,-2.49236109717652,
16.1153170513016));
#15027=CARTESIAN_POINT('Ctrl Pts',(-1.78395280315852,-2.68552376252843,
16.1375948117975));
#15028=CARTESIAN_POINT('Ctrl Pts',(-1.70681720881273,-2.73519722936382,
16.1435963659005));
#15029=CARTESIAN_POINT('Ctrl Pts',(-1.61564947927401,-2.78854585619781,
16.1502869944425));
#15030=CARTESIAN_POINT('Ctrl Pts',(-1.60359263998892,-2.79549671675951,
16.1511639570257));
#15031=CARTESIAN_POINT('Ctrl Pts',(-1.58534117400641,-2.80586188916755,
16.1524792295715));
#15032=CARTESIAN_POINT('Ctrl Pts',(-1.57917989842218,-2.80933416128601,
16.1529211437864));
#15033=CARTESIAN_POINT('Ctrl Pts',(-1.56813622670317,-2.8155101639498,16.1537094407496));
#15034=CARTESIAN_POINT('Ctrl Pts',(-1.56325820898956,-2.81822151052739,
16.1540563077467));
#15035=CARTESIAN_POINT('Ctrl Pts',(-1.55267842112873,-2.82406614806578,
16.1548057408546));
#15036=CARTESIAN_POINT('Ctrl Pts',(-1.54697421625504,-2.82719484013737,
16.1552080121776));
#15037=CARTESIAN_POINT('Ctrl Pts',(-1.53100694205595,-2.83588991654829,
16.1563291615641));
#15038=CARTESIAN_POINT('Ctrl Pts',(-1.52072291767915,-2.84141790181805,
16.1570456296722));
#15039=CARTESIAN_POINT('Ctrl Pts',(-1.4987287032758,-2.85308686598192,16.1585664433318));
#15040=CARTESIAN_POINT('Ctrl Pts',(-1.48701064947239,-2.85921172865691,
16.1593698163877));
#15041=CARTESIAN_POINT('Ctrl Pts',(-1.47525540483048,-2.8652642204548,16.1601692104994));
#15042=CARTESIAN_POINT('Origin',(0.,0.,4.68922655072688));
#15043=CARTESIAN_POINT('',(-1.47525542042047,-2.86526421242789,17.6559915606006));
#15044=CARTESIAN_POINT('',(-1.47525540448703,-2.86526422063163,17.4058265726261));
#15045=CARTESIAN_POINT('',(-1.47525540501186,-2.86526422036142,4.68922655072688));
#15046=CARTESIAN_POINT('Ctrl Pts',(-1.47525542042047,-2.86526421242789,
17.6559915606006));
#15047=CARTESIAN_POINT('Ctrl Pts',(-1.50921165810786,-2.84778096481389,
17.6537750309423));
#15048=CARTESIAN_POINT('Ctrl Pts',(-1.54285734213704,-2.82969397413309,
17.6515415727465));
#15049=CARTESIAN_POINT('Ctrl Pts',(-1.62480603952861,-2.78374410403791,
17.646000501543));
#15050=CARTESIAN_POINT('Ctrl Pts',(-1.67271742503822,-2.75522081740872,
17.6426722865387));
#15051=CARTESIAN_POINT('Ctrl Pts',(-1.73435661497109,-2.71632443089516,
17.6382616055638));
#15052=CARTESIAN_POINT('Ctrl Pts',(-1.74877696519889,-2.70706305617555,
17.6372202923261));
#15053=CARTESIAN_POINT('Ctrl Pts',(-1.77219919325204,-2.69175503315924,
17.6355131281553));
#15054=CARTESIAN_POINT('Ctrl Pts',(-1.7812457537505,-2.68577711273711,17.6348498591701));
#15055=CARTESIAN_POINT('Ctrl Pts',(-1.79864828132301,-2.6741510137598,17.6335663236865));
#15056=CARTESIAN_POINT('Ctrl Pts',(-1.80700825145836,-2.66850903310619,
17.6329462966981));
#15057=CARTESIAN_POINT('Ctrl Pts',(-1.82617989108537,-2.65543906609416,
17.6315164177203));
#15058=CARTESIAN_POINT('Ctrl Pts',(-1.83697291319907,-2.64798416466915,
17.6307055460363));
#15059=CARTESIAN_POINT('Ctrl Pts',(-1.86572839785879,-2.6278619093799,17.6285291654409));
#15060=CARTESIAN_POINT('Ctrl Pts',(-1.88360703757233,-2.61507651105942,
17.6271591383215));
#15061=CARTESIAN_POINT('Ctrl Pts',(-2.03494700546774,-2.50449287652071,
17.6154152396306));
#15062=CARTESIAN_POINT('Ctrl Pts',(-2.16080388928503,-2.39674891031488,
17.6046462416823));
#15063=CARTESIAN_POINT('Ctrl Pts',(-2.46047210908902,-2.09734577721614,
17.5763805141774));
#15064=CARTESIAN_POINT('Ctrl Pts',(-2.62052426332478,-1.89357626754913,
17.5585461374716));
#15065=CARTESIAN_POINT('Ctrl Pts',(-2.78103111943354,-1.62929019396027,
17.5383793224932));
#15066=CARTESIAN_POINT('Ctrl Pts',(-2.80647773859535,-1.58505647276577,
17.5350967508596));
#15067=CARTESIAN_POINT('Ctrl Pts',(-2.83628163111878,-1.53027857913858,
17.5311605179076));
#15068=CARTESIAN_POINT('Ctrl Pts',(-2.8416459504201,-1.52029415649738,17.5304481923698));
#15069=CARTESIAN_POINT('Ctrl Pts',(-2.84997203293764,-1.50459906639595,
17.529336722765));
#15070=CARTESIAN_POINT('Ctrl Pts',(-2.85296949990192,-1.49890759337402,
17.5289353689053));
#15071=CARTESIAN_POINT('Ctrl Pts',(-2.85854106015948,-1.48825127055043,
17.5281871210898));
#15072=CARTESIAN_POINT('Ctrl Pts',(-2.8611192425356,-1.4832887505504,17.5278399773761));
#15073=CARTESIAN_POINT('Ctrl Pts',(-2.86697987309817,-1.47193599624572,
17.527048768643));
#15074=CARTESIAN_POINT('Ctrl Pts',(-2.87025387466152,-1.46554149280782,
17.5266052390386));
#15075=CARTESIAN_POINT('Ctrl Pts',(-2.88027067095304,-1.44581521036791,
17.5252433661779));
#15076=CARTESIAN_POINT('Ctrl Pts',(-2.88694227941604,-1.43244722616778,
17.5243293813019));
#15077=CARTESIAN_POINT('Ctrl Pts',(-2.94984664937029,-1.30418022979127,
17.515640029013));
#15078=CARTESIAN_POINT('Ctrl Pts',(-2.99929145139667,-1.186060789108,17.5082507005718));
#15079=CARTESIAN_POINT('Ctrl Pts',(-3.10606658832164,-0.881202469696688,
17.4899458601504));
#15080=CARTESIAN_POINT('Ctrl Pts',(-3.15369916777444,-0.691629844502033,
17.4792325375991));
#15081=CARTESIAN_POINT('Ctrl Pts',(-3.19918615115247,-0.401345476656031,
17.4625559673734));
#15082=CARTESIAN_POINT('Ctrl Pts',(-3.20998075155483,-0.303136109167712,
17.4568734339982));
#15083=CARTESIAN_POINT('Ctrl Pts',(-3.21999659180236,-0.145683515958993,
17.4475847842714));
#15084=CARTESIAN_POINT('Ctrl Pts',(-3.22212452373348,-0.0866869307072219,
17.4440651748651));
#15085=CARTESIAN_POINT('Ctrl Pts',(-3.22278138940034,-0.0101780825974663,
17.4394366268578));
#15086=CARTESIAN_POINT('Ctrl Pts',(-3.22278916282771,0.00731234864302059,
17.4383741879552));
#15087=CARTESIAN_POINT('Ctrl Pts',(-3.2225705180606,0.0357223442217228,
17.4366410953533));
#15088=CARTESIAN_POINT('Ctrl Pts',(-3.22243096348964,0.0466423697049451,
17.4359731769186));
#15089=CARTESIAN_POINT('Ctrl Pts',(-3.22205623909723,0.067619118490116,
17.4346866672659));
#15090=CARTESIAN_POINT('Ctrl Pts',(-3.22182948141615,0.0776758785427716,
17.4340683480629));
#15091=CARTESIAN_POINT('Ctrl Pts',(-3.22120325256674,0.100671440888486,
17.4326509300296));
#15092=CARTESIAN_POINT('Ctrl Pts',(-3.22077290153226,0.113609164482866,
17.4318508693236));
#15093=CARTESIAN_POINT('Ctrl Pts',(-3.21942469995066,0.147917965458351,
17.4297221931728));
#15094=CARTESIAN_POINT('Ctrl Pts',(-3.21837201330022,0.169282815227498,
17.4283893651131));
#15095=CARTESIAN_POINT('Ctrl Pts',(-3.20870195811495,0.332471987942826,
17.4181518634995));
#15096=CARTESIAN_POINT('Ctrl Pts',(-3.19092777737306,0.473577916294351,
17.4089593489613));
#15097=CARTESIAN_POINT('Ctrl Pts',(-3.12470239215704,0.815370413700592,
17.3858862865471));
#15098=CARTESIAN_POINT('Ctrl Pts',(-3.06617979775527,1.01347193703297,17.3717912585527));
#15099=CARTESIAN_POINT('Ctrl Pts',(-2.9575366076154,1.28306250278939,17.3522809492271));
#15100=CARTESIAN_POINT('Ctrl Pts',(-2.92284145821654,1.36024703184216,17.3466605664948));
#15101=CARTESIAN_POINT('Ctrl Pts',(-2.86564318331968,1.47516871159003,17.3383257400908));
#15102=CARTESIAN_POINT('Ctrl Pts',(-2.84534172006683,1.51395658115092,17.3355188041328));
#15103=CARTESIAN_POINT('Ctrl Pts',(-2.81905402971866,1.56178376732926,17.3320765641349));
#15104=CARTESIAN_POINT('Ctrl Pts',(-2.81380530123187,1.57122051060876,17.331398310369));
#15105=CARTESIAN_POINT('Ctrl Pts',(-2.80541236291031,1.58613331841402,17.3303281693956));
#15106=CARTESIAN_POINT('Ctrl Pts',(-2.80229937544328,1.59162672815316,17.3299343304625));
#15107=CARTESIAN_POINT('Ctrl Pts',(-2.79638800600752,1.60198726618452,17.3291922998867));
#15108=CARTESIAN_POINT('Ctrl Pts',(-2.79359308624969,1.60685616969134,17.3288439047019));
#15109=CARTESIAN_POINT('Ctrl Pts',(-2.78715679745384,1.61800098682562,17.3280471329418));
#15110=CARTESIAN_POINT('Ctrl Pts',(-2.78350695036536,1.62427191893873,17.3275993121445));
#15111=CARTESIAN_POINT('Ctrl Pts',(-2.77372284889367,1.64095249985227,17.3264093159857));
#15112=CARTESIAN_POINT('Ctrl Pts',(-2.76755111091637,1.65134018552999,17.325669507383));
#15113=CARTESIAN_POINT('Ctrl Pts',(-2.72262064223818,1.72600345866916,17.3203592256973));
#15114=CARTESIAN_POINT('Ctrl Pts',(-2.68168200504866,1.78894792710155,17.3159210424777));
#15115=CARTESIAN_POINT('Ctrl Pts',(-2.62555670430001,1.8689793856393,17.3102510468129));
#15116=CARTESIAN_POINT('Ctrl Pts',(-2.6123385216607,1.8874107759113,17.3089433107318));
#15117=CARTESIAN_POINT('Ctrl Pts',(-2.4584914079385,2.0972219026021,17.2940161264704));
#15118=CARTESIAN_POINT('Ctrl Pts',(-2.29731330288381,2.27263780219091,17.281088912887));
#15119=CARTESIAN_POINT('Ctrl Pts',(-2.01352783553751,2.52015006664786,17.2596555093744));
#15120=CARTESIAN_POINT('Ctrl Pts',(-1.90294799208682,2.60465593818988,17.2515737842408));
#15121=CARTESIAN_POINT('Ctrl Pts',(-1.76859530644773,2.69419592124285,17.2418482914132));
#15122=CARTESIAN_POINT('Ctrl Pts',(-1.74979498380323,2.70644388367541,17.2404896232876));
#15123=CARTESIAN_POINT('Ctrl Pts',(-1.72074526909365,2.72493987269632,17.2383929657998));
#15124=CARTESIAN_POINT('Ctrl Pts',(-1.71058606534811,2.7313287787849,17.2376602317155));
#15125=CARTESIAN_POINT('Ctrl Pts',(-1.69202028194145,2.74286019332181,17.2363219761966));
#15126=CARTESIAN_POINT('Ctrl Pts',(-1.6836253143024,2.74802119209754,17.235717148532));
#15127=CARTESIAN_POINT('Ctrl Pts',(-1.66527474077098,2.75918697636374,17.2343956337175));
#15128=CARTESIAN_POINT('Ctrl Pts',(-1.65531007612173,2.76517653667787,17.2336783978784));
#15129=CARTESIAN_POINT('Ctrl Pts',(-1.6279948535519,2.78139461082274,17.2317131866269));
#15130=CARTESIAN_POINT('Ctrl Pts',(-1.61058069675148,2.79151446599061,17.2304612762955));
#15131=CARTESIAN_POINT('Ctrl Pts',(-1.52252644242169,2.84158705472261,17.2241348761914));
#15132=CARTESIAN_POINT('Ctrl Pts',(-1.45049526646545,2.87902159332317,17.2189709655042));
#15133=CARTESIAN_POINT('Ctrl Pts',(-1.34046502149274,2.93102644078837,17.2110937631221));
#15134=CARTESIAN_POINT('Ctrl Pts',(-1.30347428291919,2.94766298141163,17.2084475437418));
#15135=CARTESIAN_POINT('Ctrl Pts',(-1.06322567157239,3.05030790325585,17.1912788387716));
#15136=CARTESIAN_POINT('Ctrl Pts',(-0.851911904511612,3.11593582546824,
17.1762035513759));
#15137=CARTESIAN_POINT('Ctrl Pts',(-0.544461007892324,3.177785214158,17.1551002312699));
#15138=CARTESIAN_POINT('Ctrl Pts',(-0.452582595593248,3.19216667970799,
17.1489036808425));
#15139=CARTESIAN_POINT('Ctrl Pts',(-0.313933301531223,3.2077611523098,17.1398285019107));
#15140=CARTESIAN_POINT('Ctrl Pts',(-0.267551193009791,3.21196242587454,
17.1368386985903));
#15141=CARTESIAN_POINT('Ctrl Pts',(-0.210102238954865,3.215912926075,17.1332055500954));
#15142=CARTESIAN_POINT('Ctrl Pts',(-0.199108918942868,3.21661227778708,
17.132513483837));
#15143=CARTESIAN_POINT('Ctrl Pts',(-0.181760687197741,3.21762662419329,
17.1314265770773));
#15144=CARTESIAN_POINT('Ctrl Pts',(-0.17540818032777,3.21797918142222,17.1310296818193));
#15145=CARTESIAN_POINT('Ctrl Pts',(-0.163458183963159,3.21860690221043,
17.1302851928531));
#15146=CARTESIAN_POINT('Ctrl Pts',(-0.157861088935017,3.21888627415952,
17.12993737663));
#15147=CARTESIAN_POINT('Ctrl Pts',(-0.14509619672751,3.21949004293042,17.1291461212268));
#15148=CARTESIAN_POINT('Ctrl Pts',(-0.137928035903201,3.21980510312202,
17.1287032104826));
#15149=CARTESIAN_POINT('Ctrl Pts',(-0.118959966937395,3.22057534158232,
17.1275348179507));
#15150=CARTESIAN_POINT('Ctrl Pts',(-0.107158378421279,3.22098961445206,
17.1268115687951));
#15151=CARTESIAN_POINT('Ctrl Pts',(-0.026006712394669,3.22339177771076,
17.1218620924443));
#15152=CARTESIAN_POINT('Ctrl Pts',(0.0433951599804932,3.22320482494652,
17.1177487467012));
#15153=CARTESIAN_POINT('Ctrl Pts',(0.355820978909821,3.21226845548931,17.099555329279));
#15154=CARTESIAN_POINT('Ctrl Pts',(0.597171840884709,3.17626872740986,17.0863307876468));
#15155=CARTESIAN_POINT('Ctrl Pts',(0.987807694218107,3.07185619275385,17.0634639638808));
#15156=CARTESIAN_POINT('Ctrl Pts',(1.14006782402883,3.0186585980268,17.0541658570101));
#15157=CARTESIAN_POINT('Ctrl Pts',(1.30888366047899,2.94507640245219,17.0430789357183));
#15158=CARTESIAN_POINT('Ctrl Pts',(1.32996475254857,2.9356166587567,17.0416803375862));
#15159=CARTESIAN_POINT('Ctrl Pts',(1.36196532970585,2.92084156095532,17.0395349133715));
#15160=CARTESIAN_POINT('Ctrl Pts',(1.37295979951491,2.91568968960838,17.0387937367698));
#15161=CARTESIAN_POINT('Ctrl Pts',(1.39204620469512,2.90661414655783,17.0374998388999));
#15162=CARTESIAN_POINT('Ctrl Pts',(1.40015136684782,2.90271848105921,17.0369480971851));
#15163=CARTESIAN_POINT('Ctrl Pts',(1.41831904797964,2.89389256911169,17.035706187806));
#15164=CARTESIAN_POINT('Ctrl Pts',(1.42837233382647,2.88894368139962,17.0350153732124));
#15165=CARTESIAN_POINT('Ctrl Pts',(1.45520064148423,2.87556275432808,17.0331621189701));
#15166=CARTESIAN_POINT('Ctrl Pts',(1.47192793466289,2.86703648252909,17.0319963778376));
#15167=CARTESIAN_POINT('Ctrl Pts',(1.54550256256333,2.82872027923607,17.0268227116797));
#15168=CARTESIAN_POINT('Ctrl Pts',(1.60152381998685,2.7973839728918,17.0227602685077));
#15169=CARTESIAN_POINT('Ctrl Pts',(1.90310394336902,2.61666167352433,17.0001901289475));
#15170=CARTESIAN_POINT('Ctrl Pts',(2.12873870261501,2.43662435203665,16.9805290442317));
#15171=CARTESIAN_POINT('Ctrl Pts',(2.38876069951904,2.16513093684089,16.9552634206903));
#15172=CARTESIAN_POINT('Ctrl Pts',(2.44739132564443,2.0986299279193,16.9493658372258));
#15173=CARTESIAN_POINT('Ctrl Pts',(2.53163781628203,1.99473425611013,16.9406733700638));
#15174=CARTESIAN_POINT('Ctrl Pts',(2.55932780593585,1.95908051387269,16.9377771682714));
#15175=CARTESIAN_POINT('Ctrl Pts',(2.59276825906274,1.91410272883475,16.9342415753543));
#15176=CARTESIAN_POINT('Ctrl Pts',(2.59923092654805,1.90531758514843,16.9335564597362));
#15177=CARTESIAN_POINT('Ctrl Pts',(2.60937871736071,1.89137527795711,16.9324779879709));
#15178=CARTESIAN_POINT('Ctrl Pts',(2.61309336649433,1.88623985545633,16.9320826291837));
#15179=CARTESIAN_POINT('Ctrl Pts',(2.62006678447413,1.87653911971586,16.9313393889866));
#15180=CARTESIAN_POINT('Ctrl Pts',(2.6233287445076,1.87197631439385,16.9309912945672));
#15181=CARTESIAN_POINT('Ctrl Pts',(2.63075943273545,1.86152475757216,16.9301973231937));
#15182=CARTESIAN_POINT('Ctrl Pts',(2.6349203050381,1.85563051399314,16.9297519881763));
#15183=CARTESIAN_POINT('Ctrl Pts',(2.64591648616228,1.83994189012584,16.9285729450347));
#15184=CARTESIAN_POINT('Ctrl Pts',(2.65271727762095,1.83012329258641,16.9278415351989));
#15185=CARTESIAN_POINT('Ctrl Pts',(2.70021824940439,1.76072297793753,16.9227155046396));
#15186=CARTESIAN_POINT('Ctrl Pts',(2.73896533401916,1.69982194942384,16.9184430712695));
#15187=CARTESIAN_POINT('Ctrl Pts',(2.80298315968369,1.59131980829472,16.9111233753168));
#15188=CARTESIAN_POINT('Ctrl Pts',(2.82916429582719,1.54429374231854,16.9080420985591));
#15189=CARTESIAN_POINT('Ctrl Pts',(2.98126386827609,1.2542318805005,16.8894538170206));
#15190=CARTESIAN_POINT('Ctrl Pts',(3.07697113863817,0.996636710725971,16.8745896734974));
#15191=CARTESIAN_POINT('Ctrl Pts',(3.15717528132441,0.651780297650595,16.8539645961918));
#15192=CARTESIAN_POINT('Ctrl Pts',(3.17244190741893,0.572873499747483,16.8492078053616));
#15193=CARTESIAN_POINT('Ctrl Pts',(3.18771176427329,0.474327952594113,16.8431855916211));
#15194=CARTESIAN_POINT('Ctrl Pts',(3.19050699188346,0.455146578607034,16.8420096573013));
#15195=CARTESIAN_POINT('Ctrl Pts',(3.19466292338349,0.424705737273957,16.840137071327));
#15196=CARTESIAN_POINT('Ctrl Pts',(3.19613755120719,0.413462097282861,16.8394440375476));
#15197=CARTESIAN_POINT('Ctrl Pts',(3.19879740286055,0.392316440802751,16.8381379880616));
#15198=CARTESIAN_POINT('Ctrl Pts',(3.1999960687612,0.382416226932203,16.8375254062753));
#15199=CARTESIAN_POINT('Ctrl Pts',(3.20258382452611,0.360178500039765,16.8361468942325));
#15200=CARTESIAN_POINT('Ctrl Pts',(3.20394760362646,0.347838254504404,16.8353801726675));
#15201=CARTESIAN_POINT('Ctrl Pts',(3.20723671537485,0.316414442758496,16.8334231636811));
#15202=CARTESIAN_POINT('Ctrl Pts',(3.20906302850927,0.297321209146729,16.8322297717533));
#15203=CARTESIAN_POINT('Ctrl Pts',(3.21879813030046,0.184973265233389,16.825181414043));
#15204=CARTESIAN_POINT('Ctrl Pts',(3.2228114076694,0.0914343725930345,16.8192049733415));
#15205=CARTESIAN_POINT('Ctrl Pts',(3.22260812845615,-0.214784973016233,
16.7992750104845));
#15206=CARTESIAN_POINT('Ctrl Pts',(3.20142070169844,-0.426873293043364,
16.7848545867541));
#15207=CARTESIAN_POINT('Ctrl Pts',(3.14466363018619,-0.709141254119123,
16.7653867776616));
#15208=CARTESIAN_POINT('Ctrl Pts',(3.12723119551926,-0.782442633742294,
16.7603109160857));
#15209=CARTESIAN_POINT('Ctrl Pts',(3.08246402247786,-0.945122803139734,
16.7490798027811));
#15210=CARTESIAN_POINT('Ctrl Pts',(3.05377633826291,-1.0340673037172,16.7429625965153));
#15211=CARTESIAN_POINT('Ctrl Pts',(3.01639764875923,-1.13475024536133,16.7361595076663));
#15212=CARTESIAN_POINT('Ctrl Pts',(3.01144810236233,-1.14782108284193,16.7352787420029));
#15213=CARTESIAN_POINT('Ctrl Pts',(3.00386100814568,-1.16747026642313,16.7339588078486));
#15214=CARTESIAN_POINT('Ctrl Pts',(3.00128661400922,-1.17407258808337,16.7335159991656));
#15215=CARTESIAN_POINT('Ctrl Pts',(2.99664480372383,-1.18586199078019,16.7327266270898));
#15216=CARTESIAN_POINT('Ctrl Pts',(2.994585671692,-1.19105222276095,16.7323795749864));
#15217=CARTESIAN_POINT('Ctrl Pts',(2.99010039539854,-1.20227261251952,16.7316303259829));
#15218=CARTESIAN_POINT('Ctrl Pts',(2.98766950228245,-1.20830077227111,16.731228420937));
#15219=CARTESIAN_POINT('Ctrl Pts',(2.98083399334295,-1.22510480547928,16.7301097230026));
#15220=CARTESIAN_POINT('Ctrl Pts',(2.97638915115945,-1.23586435775854,16.7293953219864));
#15221=CARTESIAN_POINT('Ctrl Pts',(2.95030605206727,-1.29804630177713,16.7252763266109));
#15222=CARTESIAN_POINT('Ctrl Pts',(2.92739229284414,-1.3489274397247,16.7219443973797));
#15223=CARTESIAN_POINT('Ctrl Pts',(2.79270535319926,-1.62838794226926,16.7037222334393));
#15224=CARTESIAN_POINT('Ctrl Pts',(2.65548091987462,-1.84371881742028,16.6899162435718));
#15225=CARTESIAN_POINT('Ctrl Pts',(2.39050750452443,-2.16759787712622,16.6662803365066));
#15226=CARTESIAN_POINT('Ctrl Pts',(2.27715285048547,-2.28638822658571,16.6568314493054));
#15227=CARTESIAN_POINT('Ctrl Pts',(2.13897211640319,-2.41068370876049,16.6456526892656));
#15228=CARTESIAN_POINT('Ctrl Pts',(2.12253309517528,-2.42517027897028,16.6443280685748));
#15229=CARTESIAN_POINT('Ctrl Pts',(2.09603375881475,-2.44804648361993,16.6422004807328));
#15230=CARTESIAN_POINT('Ctrl Pts',(2.08606761600122,-2.4565445238338,16.6414020175203));
#15231=CARTESIAN_POINT('Ctrl Pts',(2.06833821282144,-2.47147653402482,16.6399844326777));
#15232=CARTESIAN_POINT('Ctrl Pts',(2.0605959955818,-2.47793530185423,16.6393663407125));
#15233=CARTESIAN_POINT('Ctrl Pts',(2.04445811625709,-2.49127002506281,16.6380798855811));
#15234=CARTESIAN_POINT('Ctrl Pts',(2.03605778832255,-2.49814010914216,16.637411294562));
#15235=CARTESIAN_POINT('Ctrl Pts',(2.01427129230644,-2.51577498835048,16.6356798976594));
#15236=CARTESIAN_POINT('Ctrl Pts',(2.00083360134933,-2.52647531401277,16.6346145130469));
#15237=CARTESIAN_POINT('Ctrl Pts',(1.94313984177235,-2.57166743200128,16.6300505209162));
#15238=CARTESIAN_POINT('Ctrl Pts',(1.89807482783409,-2.6051059738277,16.6265105637313));
#15239=CARTESIAN_POINT('Ctrl Pts',(1.77691277894382,-2.69019585431608,16.6170515827017));
#15240=CARTESIAN_POINT('Ctrl Pts',(1.69944239467667,-2.73979301818201,16.6110608819657));
#15241=CARTESIAN_POINT('Ctrl Pts',(1.41044876229291,-2.90783245691427,16.5889456641452));
#15242=CARTESIAN_POINT('Ctrl Pts',(1.18788350038471,-3.00562359257762,16.5722773199921));
#15243=CARTESIAN_POINT('Ctrl Pts',(0.868239499374581,-3.10496619403906,
16.5500048248778));
#15244=CARTESIAN_POINT('Ctrl Pts',(0.778857058608428,-3.12858434900363,
16.5439556650797));
#15245=CARTESIAN_POINT('Ctrl Pts',(0.674953456053866,-3.15130922163454,
16.5372185813917));
#15246=CARTESIAN_POINT('Ctrl Pts',(0.661312650448159,-3.15419998939371,
16.5363399099712));
#15247=CARTESIAN_POINT('Ctrl Pts',(0.640718269620989,-3.15842488895197,
16.5350224931006));
#15248=CARTESIAN_POINT('Ctrl Pts',(0.633778565353956,-3.15982474396101,
16.5345801275577));
#15249=CARTESIAN_POINT('Ctrl Pts',(0.621357640402885,-3.16228768733928,
16.5337912339403));
#15250=CARTESIAN_POINT('Ctrl Pts',(0.615878236837986,-3.16335940635113,
16.5334442196338));
#15251=CARTESIAN_POINT('Ctrl Pts',(0.604008851983841,-3.16564893537518,
16.532694698199));
#15252=CARTESIAN_POINT('Ctrl Pts',(0.597617979686703,-3.16686163692679,
16.53229248483));
#15253=CARTESIAN_POINT('Ctrl Pts',(0.579756922009294,-3.17019487309247,
16.5311720574755));
#15254=CARTESIAN_POINT('Ctrl Pts',(0.568278693667798,-3.17227252265931,
16.5304562473701));
#15255=CARTESIAN_POINT('Ctrl Pts',(0.50146281119351,-3.18399243146146,16.5263126422797));
#15256=CARTESIAN_POINT('Ctrl Pts',(0.445888178102348,-3.19224957912384,
16.5229585314978));
#15257=CARTESIAN_POINT('Ctrl Pts',(0.137848799652848,-3.22981480221689,
16.5047352815579));
#15258=CARTESIAN_POINT('Ctrl Pts',(-0.117201385939855,-3.23063416120516,
16.4909440702368));
#15259=CARTESIAN_POINT('Ctrl Pts',(-0.532481629441486,-3.18267588268512,
16.467331056565));
#15260=CARTESIAN_POINT('Ctrl Pts',(-0.69355263211336,-3.1514975435824,16.4578895431112));
#15261=CARTESIAN_POINT('Ctrl Pts',(-0.872672789207635,-3.10242481668773,
16.4467190320074));
#15262=CARTESIAN_POINT('Ctrl Pts',(-0.893742568843931,-3.09642079255297,
16.4453945721666));
#15263=CARTESIAN_POINT('Ctrl Pts',(-0.927307059073515,-3.08648516951426,
16.4432671938948));
#15264=CARTESIAN_POINT('Ctrl Pts',(-0.939842088555001,-3.08269134427579,
16.4424687779838));
#15265=CARTESIAN_POINT('Ctrl Pts',(-0.961985670613258,-3.07584180150738,
16.4410512478789));
#15266=CARTESIAN_POINT('Ctrl Pts',(-0.971603716089313,-3.07281718193215,
16.4404331630847));
#15267=CARTESIAN_POINT('Ctrl Pts',(-0.991544377574944,-3.06644339286394,
16.4391466937124));
#15268=CARTESIAN_POINT('Ctrl Pts',(-1.00186457298129,-3.06308712039533,
16.4384780811364));
#15269=CARTESIAN_POINT('Ctrl Pts',(-1.0284773699044,-3.05428338306084,16.4367465656993));
#15270=CARTESIAN_POINT('Ctrl Pts',(-1.04474355742657,-3.04875770851709,
16.4356810834392));
#15271=CARTESIAN_POINT('Ctrl Pts',(-1.11395954859859,-3.02462585090819,
16.4311161063053));
#15272=CARTESIAN_POINT('Ctrl Pts',(-1.16645996777307,-3.00476919553406,
16.4275752395669));
#15273=CARTESIAN_POINT('Ctrl Pts',(-1.30357001872479,-2.94877668389805,
16.4181132109558));
#15274=CARTESIAN_POINT('Ctrl Pts',(-1.38719240977922,-2.91037341551829,
16.4121203147534));
#15275=CARTESIAN_POINT('Ctrl Pts',(-1.4711211693975,-2.86739001021449,16.4058821692644));
#15276=CARTESIAN_POINT('Ctrl Pts',(-1.47318889494024,-2.86632821653081,
16.4057283412007));
#15277=CARTESIAN_POINT('Ctrl Pts',(-1.47525540582449,-2.86526421994301,
16.4055744628637));
#15278=CARTESIAN_POINT('',(3.22275033525038,-0.00163969519989214,16.5668203720521));
#15279=CARTESIAN_POINT('Ctrl Pts',(-1.47525540483048,-2.8652642204548,16.1601692104994));
#15280=CARTESIAN_POINT('Ctrl Pts',(-1.43687104683692,-2.88502740012483,
16.1627794692134));
#15281=CARTESIAN_POINT('Ctrl Pts',(-1.3980901546135,-2.90401894906659,16.1653473167563));
#15282=CARTESIAN_POINT('Ctrl Pts',(-1.12873292759281,-3.02927932580612,
16.1827891100192));
#15283=CARTESIAN_POINT('Ctrl Pts',(-0.886665609477366,-3.10876543091489,
16.1965667153266));
#15284=CARTESIAN_POINT('Ctrl Pts',(-0.477124986012638,-3.19144535740846,
16.2201662265951));
#15285=CARTESIAN_POINT('Ctrl Pts',(-0.314274748655967,-3.21157168066685,
16.2296093263575));
#15286=CARTESIAN_POINT('Ctrl Pts',(-0.128733243122897,-3.22025233440821,
16.2407813169308));
#15287=CARTESIAN_POINT('Ctrl Pts',(-0.106843794828839,-3.221052888788,16.2421055119719));
#15288=CARTESIAN_POINT('Ctrl Pts',(-0.0718598700768303,-3.22197534867514,
16.2442324038511));
#15289=CARTESIAN_POINT('Ctrl Pts',(-0.058769620933428,-3.2222406974205,
16.2450305996282));
#15290=CARTESIAN_POINT('Ctrl Pts',(-0.0356002168597041,-3.22256912642433,
16.2464477012146));
#15291=CARTESIAN_POINT('Ctrl Pts',(-0.0255216432503605,-3.22266470363948,
16.247065578023));
#15292=CARTESIAN_POINT('Ctrl Pts',(-0.00459498457945542,-3.22276498182738,
16.2483515760995));
#15293=CARTESIAN_POINT('Ctrl Pts',(0.00625299345351246,-3.22276219064357,
16.2490199250224));
#15294=CARTESIAN_POINT('Ctrl Pts',(0.0342714343567632,-3.22261351632145,
16.2507506728098));
#15295=CARTESIAN_POINT('Ctrl Pts',(0.0514409461521228,-3.22238517521654,
16.2518156483829));
#15296=CARTESIAN_POINT('Ctrl Pts',(0.124678870817259,-3.22082569541067,
16.2563776303249));
#15297=CARTESIAN_POINT('Ctrl Pts',(0.180706401248717,-3.21816835169966,
16.2599159485872));
#15298=CARTESIAN_POINT('Ctrl Pts',(0.328288357972361,-3.20730268125544,
16.2693700232073));
#15299=CARTESIAN_POINT('Ctrl Pts',(0.419605168472895,-3.19663772081945,
16.2753573772499));
#15300=CARTESIAN_POINT('Ctrl Pts',(0.732533005896538,-3.14645113731676,
16.2963229025158));
#15301=CARTESIAN_POINT('Ctrl Pts',(0.950381880099279,-3.08763995407859,
16.3117528192285));
#15302=CARTESIAN_POINT('Ctrl Pts',(1.26200287906145,-2.96738100942387,16.3340991567899));
#15303=CARTESIAN_POINT('Ctrl Pts',(1.36165997201076,-2.92299310424172,16.3412789833713));
#15304=CARTESIAN_POINT('Ctrl Pts',(1.47188941530423,-2.86703188287969,16.3491137187671));
#15305=CARTESIAN_POINT('Ctrl Pts',(1.48484926595644,-2.86034140350533,16.3500330990949));
#15306=CARTESIAN_POINT('Ctrl Pts',(1.50406111575195,-2.85025758626339,16.3513928700871));
#15307=CARTESIAN_POINT('Ctrl Pts',(1.51034780889227,-2.84693126830408,16.3518373257058));
#15308=CARTESIAN_POINT('Ctrl Pts',(1.52131197242031,-2.8410835397242,16.3526115206454));
#15309=CARTESIAN_POINT('Ctrl Pts',(1.52599426051185,-2.83857135113489,16.3529418373027));
#15310=CARTESIAN_POINT('Ctrl Pts',(1.53068607837468,-2.83603908511265,16.3532725124688));
#15311=CARTESIAN_POINT('Ctrl Pts',(1.53070173753393,-2.83603063339014,16.353273616109));
#15312=CARTESIAN_POINT('Ctrl Pts',(1.5307329656665,-2.8360137782872,16.3532758170264));
#15313=CARTESIAN_POINT('Ctrl Pts',(1.53074853461697,-2.83600537492104,16.3532769143019));
#15314=CARTESIAN_POINT('Ctrl Pts',(1.53077958267836,-2.83598861634959,16.3532791025145));
#15315=CARTESIAN_POINT('Ctrl Pts',(1.53079506192688,-2.83598026107194,16.3532801934613));
#15316=CARTESIAN_POINT('Ctrl Pts',(1.53082593144913,-2.83596359821645,16.3532823690773));
#15317=CARTESIAN_POINT('Ctrl Pts',(1.53084132168351,-2.83595529066171,16.3532834537439));
#15318=CARTESIAN_POINT('Ctrl Pts',(1.53087201368719,-2.83593872298251,16.3532856168355));
#15319=CARTESIAN_POINT('Ctrl Pts',(1.53088731545902,-2.83593046285854,16.3532866952608));
#15320=CARTESIAN_POINT('Ctrl Pts',(1.53091783138174,-2.83591398959072,16.3532888459296));
#15321=CARTESIAN_POINT('Ctrl Pts',(1.53093304540083,-2.83590577651985,16.3532899181639));
#15322=CARTESIAN_POINT('Ctrl Pts',(1.53096338620605,-2.83588939715427,16.353292056478));
#15323=CARTESIAN_POINT('Ctrl Pts',(1.53097851303759,-2.83588123083685,16.3532931225611));
#15324=CARTESIAN_POINT('Ctrl Pts',(1.53100867997104,-2.83586494471184,16.3532952486084));
#15325=CARTESIAN_POINT('Ctrl Pts',(1.53102372018676,-2.83585682484459,16.3532963085808));
#15326=CARTESIAN_POINT('Ctrl Pts',(1.53105371439077,-2.83584063135414,16.3532984224422));
#15327=CARTESIAN_POINT('Ctrl Pts',(1.53106866848527,-2.83583255767536,16.3532994763388));
#15328=CARTESIAN_POINT('Ctrl Pts',(1.53109849149694,-2.83581645600016,16.3533015781228));
#15329=CARTESIAN_POINT('Ctrl Pts',(1.53111336021842,-2.83580842811114,16.3533026259965));
#15330=CARTESIAN_POINT('Ctrl Pts',(1.53114301285289,-2.83579241782153,16.3533047157608));
#15331=CARTESIAN_POINT('Ctrl Pts',(1.53115779674775,-2.83578443543244,16.3533057576501));
#15332=CARTESIAN_POINT('Ctrl Pts',(1.53118728021493,-2.83576851588544,16.3533078354801));
#15333=CARTESIAN_POINT('Ctrl Pts',(1.53120197983383,-2.83576057870407,16.3533088714241));
#15334=CARTESIAN_POINT('Ctrl Pts',(1.53123129531061,-2.83574474927439,16.353310937403));
#15335=CARTESIAN_POINT('Ctrl Pts',(1.53124591119265,-2.83573685701472,16.3533119674396));
#15336=CARTESIAN_POINT('Ctrl Pts',(1.53682950105994,-2.83272178368782,16.3537054630562));
#15337=CARTESIAN_POINT('Ctrl Pts',(1.54238966099265,-2.82969817372801,16.3540968724826));
#15338=CARTESIAN_POINT('Ctrl Pts',(1.55762976570956,-2.82135235315607,16.3551686091725));
#15339=CARTESIAN_POINT('Ctrl Pts',(1.56729141753032,-2.81599666343596,16.3558468319111));
#15340=CARTESIAN_POINT('Ctrl Pts',(1.58883856721532,-2.80390730354497,16.3573570883197));
#15341=CARTESIAN_POINT('Ctrl Pts',(1.60070924679475,-2.79714749009512,16.3581875384262));
#15342=CARTESIAN_POINT('Ctrl Pts',(1.63729797896763,-2.7760026604277,16.3607434618559));
#15343=CARTESIAN_POINT('Ctrl Pts',(1.66186846708456,-2.761363568712,16.3624545084569));
#15344=CARTESIAN_POINT('Ctrl Pts',(1.75651595199861,-2.70325163888702,16.3690377287852));
#15345=CARTESIAN_POINT('Ctrl Pts',(1.82511340845321,-2.65741993017932,16.3737924216299));
#15346=CARTESIAN_POINT('Ctrl Pts',(2.05998852297692,-2.48710364194464,16.3902861241016));
#15347=CARTESIAN_POINT('Ctrl Pts',(2.21592198644761,-2.34924063633112,16.4016626171965));
#15348=CARTESIAN_POINT('Ctrl Pts',(2.45530598079615,-2.09240603702729,16.4216072249065));
#15349=CARTESIAN_POINT('Ctrl Pts',(2.54597600075533,-1.98108280903499,16.4299252482917));
#15350=CARTESIAN_POINT('Ctrl Pts',(2.64131637295379,-1.84662511776808,16.4398433183095));
#15351=CARTESIAN_POINT('Ctrl Pts',(2.6535330550398,-1.82902673557182,16.4411388312144));
#15352=CARTESIAN_POINT('Ctrl Pts',(2.67285273508388,-1.80059533942263,16.4432283258975));
#15353=CARTESIAN_POINT('Ctrl Pts',(2.68006758409419,-1.78983883542452,16.4440180561888));
#15354=CARTESIAN_POINT('Ctrl Pts',(2.69276934051706,-1.77065298569718,16.4454253974699));
#15355=CARTESIAN_POINT('Ctrl Pts',(2.69828202754467,-1.76224084993321,16.4460420267629));
#15356=CARTESIAN_POINT('Ctrl Pts',(2.70969322140597,-1.7446487528916,16.4473307506324));
#15357=CARTESIAN_POINT('Ctrl Pts',(2.71558465479897,-1.73546437676793,16.4480030994042));
#15358=CARTESIAN_POINT('Ctrl Pts',(2.73078119955417,-1.71150706268432,16.4497558170423));
#15359=CARTESIAN_POINT('Ctrl Pts',(2.74001301052073,-1.6966882649136,16.4508388878112));
#15360=CARTESIAN_POINT('Ctrl Pts',(2.77979075792723,-1.63166611568644,16.4555871164191));
#15361=CARTESIAN_POINT('Ctrl Pts',(2.80907907613,-1.58071027775321,16.4592978957305));
#15362=CARTESIAN_POINT('Ctrl Pts',(2.88352119985531,-1.44258655895846,16.4693363625426));
#15363=CARTESIAN_POINT('Ctrl Pts',(2.92611063056265,-1.35411375008128,16.4757471439615));
#15364=CARTESIAN_POINT('Ctrl Pts',(3.06391328047553,-1.03087016547231,16.4990597496202));
#15365=CARTESIAN_POINT('Ctrl Pts',(3.13541675305209,-0.787024284961098,
16.5165261265935));
#15366=CARTESIAN_POINT('Ctrl Pts',(3.18445545964444,-0.497023538812584,
16.5359450691231));
#15367=CARTESIAN_POINT('Ctrl Pts',(3.19050456194766,-0.456585047758886,
16.5386209337383));
#15368=CARTESIAN_POINT('Ctrl Pts',(3.1960840269909,-0.413726841812239,16.5414159981397));
#15369=CARTESIAN_POINT('Ctrl Pts',(3.19638274399409,-0.411412641009479,
16.5415667964687));
#15370=CARTESIAN_POINT('Ctrl Pts',(3.20115105907343,-0.374153186569202,
16.5439926559566));
#15371=CARTESIAN_POINT('Ctrl Pts',(3.20505008346649,-0.339135540654309,
16.5462435908722));
#15372=CARTESIAN_POINT('Ctrl Pts',(3.20935959247385,-0.293662450607269,
16.5491230990537));
#15373=CARTESIAN_POINT('Ctrl Pts',(3.21029438425512,-0.283260661268862,
16.5497788305413));
#15374=CARTESIAN_POINT('Ctrl Pts',(3.21170639950285,-0.266642882345015,
16.5508215212418));
#15375=CARTESIAN_POINT('Ctrl Pts',(3.21221617008981,-0.260429839870924,
16.5512102692218));
#15376=CARTESIAN_POINT('Ctrl Pts',(3.21313455567376,-0.248823517618891,
16.5519343835033));
#15377=CARTESIAN_POINT('Ctrl Pts',(3.21354761655315,-0.24343075461257,16.5522699883894));
#15378=CARTESIAN_POINT('Ctrl Pts',(3.21435419241754,-0.232540457540709,
16.5529460392689));
#15379=CARTESIAN_POINT('Ctrl Pts',(3.21474717991929,-0.227042967240717,
16.5532864527513));
#15380=CARTESIAN_POINT('Ctrl Pts',(3.21562329551595,-0.214328488851954,
16.5540718183898));
#15381=CARTESIAN_POINT('Ctrl Pts',(3.21609623615602,-0.207110796221044,
16.5545162096624));
#15382=CARTESIAN_POINT('Ctrl Pts',(3.21725953382586,-0.188391644555414,
16.555665147561));
#15383=CARTESIAN_POINT('Ctrl Pts',(3.21791252461293,-0.176887853196649,
16.5563677062927));
#15384=CARTESIAN_POINT('Ctrl Pts',(3.22130600496964,-0.110846681959428,
16.560382052572));
#15385=CARTESIAN_POINT('Ctrl Pts',(3.2227218728278,-0.0562472651967042,
16.5636269405585));
#15386=CARTESIAN_POINT('Ctrl Pts',(3.22274958507906,-0.00163535095755876,
16.566821929544));
#15387=CARTESIAN_POINT('Ctrl Pts',(3.22274958283323,-0.00163977079054786,
16.5668216709681));
#15388=CARTESIAN_POINT('Ctrl Pts',(3.22288814644766,0.270688430919775,16.5827538418433));
#15389=CARTESIAN_POINT('Ctrl Pts',(3.18850939682181,0.541974969374395,16.5974513663888));
#15390=CARTESIAN_POINT('Ctrl Pts',(3.08809762302721,0.930840433051183,16.6202876628461));
#15391=CARTESIAN_POINT('Ctrl Pts',(3.04830463274175,1.05387104005822,16.6277746802112));
#15392=CARTESIAN_POINT('Ctrl Pts',(2.98997229446664,1.20297111761028,16.6373589726579));
#15393=CARTESIAN_POINT('Ctrl Pts',(2.97829202777991,1.23160477738666,16.6392233522321));
#15394=CARTESIAN_POINT('Ctrl Pts',(2.96086451649715,1.27262925477499,16.6419308410272));
#15395=CARTESIAN_POINT('Ctrl Pts',(2.95544749745275,1.28515912865734,16.6427627112954));
#15396=CARTESIAN_POINT('Ctrl Pts',(2.94587150754634,1.30692818317578,16.6442167661536));
#15397=CARTESIAN_POINT('Ctrl Pts',(2.94174823916291,1.31618293128753,16.6448377190982));
#15398=CARTESIAN_POINT('Ctrl Pts',(2.93370147243649,1.33401732961844,16.6460397857353));
#15399=CARTESIAN_POINT('Ctrl Pts',(2.92978380167953,1.34259950748036,16.6466206933161));
#15400=CARTESIAN_POINT('Ctrl Pts',(2.9203987414935,1.36292203759306,16.6480021741428));
#15401=CARTESIAN_POINT('Ctrl Pts',(2.91489818520797,1.37464680986191,16.6488038912345));
#15402=CARTESIAN_POINT('Ctrl Pts',(2.89518579790013,1.41601463294798,16.6516493938714));
#15403=CARTESIAN_POINT('Ctrl Pts',(2.88059162063208,1.44547225188051,16.6537064492311));
#15404=CARTESIAN_POINT('Ctrl Pts',(2.73215068373254,1.73391377962631,16.6741613660526));
#15405=CARTESIAN_POINT('Ctrl Pts',(2.5642196789729,1.97378066319265,16.693868316739));
#15406=CARTESIAN_POINT('Ctrl Pts',(2.32448742503514,2.2330893803528,16.7177379500803));
#15407=CARTESIAN_POINT('Ctrl Pts',(2.28127683380092,2.27721461059814,16.721898405702));
#15408=CARTESIAN_POINT('Ctrl Pts',(2.18591679230329,2.36915297582539,16.7307428112625));
#15409=CARTESIAN_POINT('Ctrl Pts',(2.13340425776605,2.41654829093347,16.7354128732634));
#15410=CARTESIAN_POINT('Ctrl Pts',(2.05965937535194,2.47882765166308,16.7416591764931));
#15411=CARTESIAN_POINT('Ctrl Pts',(2.03974730264462,2.4952383256033,16.7433161442429));
#15412=CARTESIAN_POINT('Ctrl Pts',(2.00975030533848,2.51936149037709,16.7457658830477));
#15413=CARTESIAN_POINT('Ctrl Pts',(1.99981391127771,2.52725601024126,16.7465698926828));
#15414=CARTESIAN_POINT('Ctrl Pts',(1.9817218795823,2.54145671300817,16.7480199704008));
#15415=CARTESIAN_POINT('Ctrl Pts',(1.97358217538157,2.54778280784465,16.7486673490659));
#15416=CARTESIAN_POINT('Ctrl Pts',(1.96048994660291,2.55785756180521,16.7497004143879));
#15417=CARTESIAN_POINT('Ctrl Pts',(1.95555677755493,2.56163108751508,16.7500878232504));
#15418=CARTESIAN_POINT('Ctrl Pts',(1.94635097190083,2.56863078685379,16.7508072795294));
#15419=CARTESIAN_POINT('Ctrl Pts',(1.94208125593679,2.57186053680696,16.7511395734207));
#15420=CARTESIAN_POINT('Ctrl Pts',(1.93205945300254,2.57940216122241,16.751916295475));
#15421=CARTESIAN_POINT('Ctrl Pts',(1.92630097741154,2.58370543716582,16.752360117959));
#15422=CARTESIAN_POINT('Ctrl Pts',(1.90850490193338,2.59691177487318,16.7537242583509));
#15423=CARTESIAN_POINT('Ctrl Pts',(1.89641941853812,2.60575039791774,16.7546401954249));
#15424=CARTESIAN_POINT('Ctrl Pts',(1.77361459680134,2.69425578553216,16.7638469879843));
#15425=CARTESIAN_POINT('Ctrl Pts',(1.65799018864464,2.7669118244583,16.7716981789034));
#15426=CARTESIAN_POINT('Ctrl Pts',(1.36500026586766,2.92603679283878,16.7905433398609));
#15427=CARTESIAN_POINT('Ctrl Pts',(1.18365312646038,3.00397801547755,16.8013658001541));
#15428=CARTESIAN_POINT('Ctrl Pts',(0.90892086360891,3.0932873767104,16.8178123676372));
#15429=CARTESIAN_POINT('Ctrl Pts',(0.820349363080166,3.11794626717646,16.8231171126153));
#15430=CARTESIAN_POINT('Ctrl Pts',(0.676226197475743,3.15150459447015,16.8318429968615));
#15431=CARTESIAN_POINT('Ctrl Pts',(0.621282522493068,3.16279473415359,16.835190668211));
#15432=CARTESIAN_POINT('Ctrl Pts',(0.549170454448684,3.17566122607053,16.8396233087036));
#15433=CARTESIAN_POINT('Ctrl Pts',(0.532242696753985,3.17854213513168,16.8406665952706));
#15434=CARTESIAN_POINT('Ctrl Pts',(0.504584497803225,3.1830221059754,16.8423760288762));
#15435=CARTESIAN_POINT('Ctrl Pts',(0.493867435710701,3.18470252832905,16.8430395790069));
#15436=CARTESIAN_POINT('Ctrl Pts',(0.4731770484024,3.18783980631016,16.8443229790252));
#15437=CARTESIAN_POINT('Ctrl Pts',(0.463204958640022,3.18930404828989,16.8449425859305));
#15438=CARTESIAN_POINT('Ctrl Pts',(0.44026346349064,3.19256277456438,16.8463705200317));
#15439=CARTESIAN_POINT('Ctrl Pts',(0.427289729461621,3.19432504072199,16.8471798595339));
#15440=CARTESIAN_POINT('Ctrl Pts',(0.392583777819613,3.1988240517302,16.8493499490017));
#15441=CARTESIAN_POINT('Ctrl Pts',(0.37083409056914,3.20141833810365,16.8507151781246));
#15442=CARTESIAN_POINT('Ctrl Pts',(0.186146766808726,3.22154043016926,16.8623545427983));
#15443=CARTESIAN_POINT('Ctrl Pts',(0.0221427005186359,3.22683565931571,
16.8730160139398));
#15444=CARTESIAN_POINT('Ctrl Pts',(-0.395194689870823,3.20848997520268,
16.900877948811));
#15445=CARTESIAN_POINT('Ctrl Pts',(-0.646637665879886,3.1674029857535,16.9184041684116));
#15446=CARTESIAN_POINT('Ctrl Pts',(-0.944851169216543,3.08164806758982,
16.9387047186415));
#15447=CARTESIAN_POINT('Ctrl Pts',(-0.998640302895386,3.06463978474988,
16.9423419768065));
#15448=CARTESIAN_POINT('Ctrl Pts',(-1.06299494740521,3.04241608297576,16.9466414272059));
#15449=CARTESIAN_POINT('Ctrl Pts',(-1.0740103568379,3.03854498788661,16.947375476424));
#15450=CARTESIAN_POINT('Ctrl Pts',(-1.09113074361928,3.03242371528115,16.9485131551884));
#15451=CARTESIAN_POINT('Ctrl Pts',(-1.09725022277467,3.03021481731377,16.9489191664214));
#15452=CARTESIAN_POINT('Ctrl Pts',(-1.10860669212745,3.02607665327396,16.949671394407));
#15453=CARTESIAN_POINT('Ctrl Pts',(-1.11384530965598,3.02415233349664,16.9500178895709));
#15454=CARTESIAN_POINT('Ctrl Pts',(-1.12571114265484,3.01975859987549,16.9508016145926));
#15455=CARTESIAN_POINT('Ctrl Pts',(-1.13233522857189,3.01728097972435,16.951238347267));
#15456=CARTESIAN_POINT('Ctrl Pts',(-1.1519693805056,3.00986341392209,16.9525306778812));
#15457=CARTESIAN_POINT('Ctrl Pts',(-1.16495586179563,3.00486090865413,16.953382622098));
#15458=CARTESIAN_POINT('Ctrl Pts',(-1.26320784837846,2.96628068057538,16.9598095905856));
#15459=CARTESIAN_POINT('Ctrl Pts',(-1.3470473050248,2.92916064175367,16.9651875753164));
#15460=CARTESIAN_POINT('Ctrl Pts',(-1.64723960812469,2.78062947794585,16.9844470886907));
#15461=CARTESIAN_POINT('Ctrl Pts',(-1.85237187114893,2.64840146045662,16.9976708473158));
#15462=CARTESIAN_POINT('Ctrl Pts',(-2.11178439176846,2.43616995736128,17.0167527005432));
#15463=CARTESIAN_POINT('Ctrl Pts',(-2.1803640826349,2.374987982864,17.0220554742781));
#15464=CARTESIAN_POINT('Ctrl Pts',(-2.28643953713941,2.27188370668758,17.0307784119491));
#15465=CARTESIAN_POINT('Ctrl Pts',(-2.32561692550568,2.23176313124768,17.0341251729222));
#15466=CARTESIAN_POINT('Ctrl Pts',(-2.37539700916889,2.17804990780606,17.0385567756291));
#15467=CARTESIAN_POINT('Ctrl Pts',(-2.38696681836457,2.16536411310951,17.0395999595713));
#15468=CARTESIAN_POINT('Ctrl Pts',(-2.40568006991776,2.14451361282182,17.0413092672694));
#15469=CARTESIAN_POINT('Ctrl Pts',(-2.41288472566808,2.13640411216259,17.0419727948554));
#15470=CARTESIAN_POINT('Ctrl Pts',(-2.42670438707492,2.1206897392875,17.0432561809479));
#15471=CARTESIAN_POINT('Ctrl Pts',(-2.43332493653283,2.11308989447489,17.0438757966316));
#15472=CARTESIAN_POINT('Ctrl Pts',(-2.44846397978494,2.09554602650425,17.0453037935163));
#15473=CARTESIAN_POINT('Ctrl Pts',(-2.45695769577548,2.08558094605268,17.0461131873146));
#15474=CARTESIAN_POINT('Ctrl Pts',(-2.47949904464798,2.05880595350854,17.048283517061));
#15475=CARTESIAN_POINT('Ctrl Pts',(-2.49343620801465,2.04190433294468,17.0496489337253));
#15476=CARTESIAN_POINT('Ctrl Pts',(-2.61025784551694,1.8972549018431,17.0612978414188));
#15477=CARTESIAN_POINT('Ctrl Pts',(-2.70340745699684,1.76198625855598,17.0719694029455));
#15478=CARTESIAN_POINT('Ctrl Pts',(-2.91365709843681,1.40048093370004,17.0998630840193));
#15479=CARTESIAN_POINT('Ctrl Pts',(-3.01500893817588,1.16638797056696,17.1174116234875));
#15480=CARTESIAN_POINT('Ctrl Pts',(-3.10383096287479,0.869186312944634,
17.1377003658454));
#15481=CARTESIAN_POINT('Ctrl Pts',(-3.1184619663617,0.815136404891894,17.141309971854));
#15482=CARTESIAN_POINT('Ctrl Pts',(-3.13442829984756,0.749408114249852,
17.1455812296786));
#15483=CARTESIAN_POINT('Ctrl Pts',(-3.13711695707819,0.738072148225407,
17.1463136656712));
#15484=CARTESIAN_POINT('Ctrl Pts',(-3.1412099373363,0.720388746664569,17.1474493933438));
#15485=CARTESIAN_POINT('Ctrl Pts',(-3.14265659555009,0.714051357367769,
17.1478550537932));
#15486=CARTESIAN_POINT('Ctrl Pts',(-3.14530977503582,0.702264291362181,
17.1486069651574));
#15487=CARTESIAN_POINT('Ctrl Pts',(-3.14652130193718,0.696815910425137,
17.1489534923926));
#15488=CARTESIAN_POINT('Ctrl Pts',(-3.14923749481479,0.684449331192447,
17.1497377144771));
#15489=CARTESIAN_POINT('Ctrl Pts',(-3.15073351874669,0.677529321743561,
17.1501749095033));
#15490=CARTESIAN_POINT('Ctrl Pts',(-3.15510991149637,0.656957885669661,
17.1514698783234));
#15491=CARTESIAN_POINT('Ctrl Pts',(-3.15792449265331,0.64329241577073,17.1523239762318));
#15492=CARTESIAN_POINT('Ctrl Pts',(-3.1787718334036,0.538638299834818,17.1588209881452));
#15493=CARTESIAN_POINT('Ctrl Pts',(-3.19295929309754,0.446918352276326,
17.1642619658142));
#15494=CARTESIAN_POINT('Ctrl Pts',(-3.22979287532408,0.114292330514911,
17.1834956713751));
#15495=CARTESIAN_POINT('Ctrl Pts',(-3.22926632173964,-0.128360909863536,
17.1966482671688));
#15496=CARTESIAN_POINT('Ctrl Pts',(-3.19106676167714,-0.460081781200723,
17.2156575103638));
#15497=CARTESIAN_POINT('Ctrl Pts',(-3.17663311220484,-0.550983175277661,
17.2209677836826));
#15498=CARTESIAN_POINT('Ctrl Pts',(-3.14716550179649,-0.696144582347413,
17.2297019309418));
#15499=CARTESIAN_POINT('Ctrl Pts',(-3.13456466839963,-0.750847346388877,
17.2330521546242));
#15500=CARTESIAN_POINT('Ctrl Pts',(-3.11625113098277,-0.82182203919301,
17.2374877045553));
#15501=CARTESIAN_POINT('Ctrl Pts',(-3.11182697131488,-0.838418426733112,
17.2385312787006));
#15502=CARTESIAN_POINT('Ctrl Pts',(-3.10439221451665,-0.865438758033863,
17.2402410651317));
#15503=CARTESIAN_POINT('Ctrl Pts',(-3.10146123211895,-0.875884402515627,
17.2409046784409));
#15504=CARTESIAN_POINT('Ctrl Pts',(-3.09570577093514,-0.896004978763492,
17.2421881175188));
#15505=CARTESIAN_POINT('Ctrl Pts',(-3.09288853656246,-0.905681864060256,
17.2428076998579));
#15506=CARTESIAN_POINT('Ctrl Pts',(-3.08630794113903,-0.92789666222965,
17.2442354581794));
#15507=CARTESIAN_POINT('Ctrl Pts',(-3.08251350669414,-0.940425114634566,
17.2450446456535));
#15508=CARTESIAN_POINT('Ctrl Pts',(-3.07216866666618,-0.973846320525354,
17.2472140623935));
#15509=CARTESIAN_POINT('Ctrl Pts',(-3.06548158241934,-0.994695733416725,
17.2485787664536));
#15510=CARTESIAN_POINT('Ctrl Pts',(-3.00707655740649,-1.17061006154054,
17.2601914949498));
#15511=CARTESIAN_POINT('Ctrl Pts',(-2.94385058567796,-1.32157727095709,
17.2708248078673));
#15512=CARTESIAN_POINT('Ctrl Pts',(-2.75425263541487,-1.69241150957489,
17.2986003649391));
#15513=CARTESIAN_POINT('Ctrl Pts',(-2.61291315845547,-1.90337702111653,
17.3160666772289));
#15514=CARTESIAN_POINT('Ctrl Pts',(-2.41093811945269,-2.13934707375403,
17.3364001332943));
#15515=CARTESIAN_POINT('Ctrl Pts',(-2.37235455828529,-2.18205484363251,
17.3401127728689));
#15516=CARTESIAN_POINT('Ctrl Pts',(-2.32454225219463,-2.23220939639732,
17.3444889650181));
#15517=CARTESIAN_POINT('Ctrl Pts',(-2.31639266660409,-2.24066519045606,
17.3452273370719));
#15518=CARTESIAN_POINT('Ctrl Pts',(-2.30364629185895,-2.25374662362072,
17.3463702426869));
#15519=CARTESIAN_POINT('Ctrl Pts',(-2.29908147682017,-2.25840307434431,
17.3467771926954));
#15520=CARTESIAN_POINT('Ctrl Pts',(-2.29058457586657,-2.26701808406307,
17.3475302726539));
#15521=CARTESIAN_POINT('Ctrl Pts',(-2.28665637943411,-2.27098024998006,
17.3478766865998));
#15522=CARTESIAN_POINT('Ctrl Pts',(-2.2777397420623,-2.27992740285685,17.348659102346));
#15523=CARTESIAN_POINT('Ctrl Pts',(-2.27274522903054,-2.28490621711702,
17.3490946139394));
#15524=CARTESIAN_POINT('Ctrl Pts',(-2.25791314556384,-2.29959493091296,
17.3503799892889));
#15525=CARTESIAN_POINT('Ctrl Pts',(-2.24802925731558,-2.30925812617988,
17.3512262574319));
#15526=CARTESIAN_POINT('Ctrl Pts',(-2.17404983510609,-2.38066057328217,
17.3574872343597));
#15527=CARTESIAN_POINT('Ctrl Pts',(-2.10747740693861,-2.43979088021718,
17.3627162187903));
#15528=CARTESIAN_POINT('Ctrl Pts',(-1.8641464998645,-2.63851686807412,17.3808054355103));
#15529=CARTESIAN_POINT('Ctrl Pts',(-1.67535224198654,-2.76223918761152,
17.3930890918511));
#15530=CARTESIAN_POINT('Ctrl Pts',(-1.47525540448705,-2.86526422063162,
17.4058265726261));
#15531=CARTESIAN_POINT('Origin',(0.,0.,4.68922655072688));
#15532=CARTESIAN_POINT('',(-1.47525548819425,-2.8652641775328,18.9012640026169));
#15533=CARTESIAN_POINT('',(-1.47525539597219,-2.86526422501572,18.654425498672));
#15534=CARTESIAN_POINT('',(-1.47525540501186,-2.86526422036142,4.68922655072688));
#15535=CARTESIAN_POINT('',(3.22274859936717,0.00236444057009463,18.0625860991293));
#15536=CARTESIAN_POINT('Ctrl Pts',(-1.4752554881943,-2.86526417753278,18.9012640026169));
#15537=CARTESIAN_POINT('Ctrl Pts',(-1.67171863009127,-2.76411003943129,
18.8885120716065));
#15538=CARTESIAN_POINT('Ctrl Pts',(-1.85735696437909,-2.64296677365553,
18.8764349148439));
#15539=CARTESIAN_POINT('Ctrl Pts',(-2.15721040708762,-2.39993951516703,
18.8546383190739));
#15540=CARTESIAN_POINT('Ctrl Pts',(-2.27705492008618,-2.28654252812363,
18.8451462635796));
#15541=CARTESIAN_POINT('Ctrl Pts',(-2.4024236645032,-2.14824553622978,18.8339192001379));
#15542=CARTESIAN_POINT('Ctrl Pts',(-2.41698387361396,-2.13185066690676,
18.8325936419603));
#15543=CARTESIAN_POINT('Ctrl Pts',(-2.43997509192983,-2.10542413185119,
18.83046483271));
#15544=CARTESIAN_POINT('Ctrl Pts',(-2.44851434335956,-2.09548722893398,
18.8296660938478));
#15545=CARTESIAN_POINT('Ctrl Pts',(-2.46351774606513,-2.07781124026806,
18.8282481899785));
#15546=CARTESIAN_POINT('Ctrl Pts',(-2.4700066516743,-2.07009332455724,18.8276300561806));
#15547=CARTESIAN_POINT('Ctrl Pts',(-2.48340240946966,-2.0540077303389,18.8263436838233));
#15548=CARTESIAN_POINT('Ctrl Pts',(-2.49030342901978,-2.04563538062245,
18.8256752182548));
#15549=CARTESIAN_POINT('Ctrl Pts',(-2.50801486865001,-2.02392532935546,
18.823944511199));
#15550=CARTESIAN_POINT('Ctrl Pts',(-2.51876111458003,-2.01053593588118,
18.8228796948802));
#15551=CARTESIAN_POINT('Ctrl Pts',(-2.56411835111969,-1.95308824128143,
18.818321431071));
#15552=CARTESIAN_POINT('Ctrl Pts',(-2.59768250219901,-1.90821947866712,
18.814786762879));
#15553=CARTESIAN_POINT('Ctrl Pts',(-2.68309084624673,-1.78761339058424,
18.8053454961269));
#15554=CARTESIAN_POINT('Ctrl Pts',(-2.73289610856644,-1.71050123479499,
18.7993675540166));
#15555=CARTESIAN_POINT('Ctrl Pts',(-2.90296300293422,-1.4207617055756,18.77714407621));
#15556=CARTESIAN_POINT('Ctrl Pts',(-3.00223360097899,-1.19680250230503,
18.7603429412645));
#15557=CARTESIAN_POINT('Ctrl Pts',(-3.10244883864784,-0.877037562064718,
18.7380575437401));
#15558=CARTESIAN_POINT('Ctrl Pts',(-3.12595815834096,-0.78915941668079,
18.7321085138865));
#15559=CARTESIAN_POINT('Ctrl Pts',(-3.14874069313296,-0.686835231848619,
18.7254687335981));
#15560=CARTESIAN_POINT('Ctrl Pts',(-3.15167246180206,-0.673254259683618,
18.7245932471418));
#15561=CARTESIAN_POINT('Ctrl Pts',(-3.15596324926836,-0.652735397201517,
18.7232796596718));
#15562=CARTESIAN_POINT('Ctrl Pts',(-3.15738737410719,-0.645811506233739,
18.7228379690362));
#15563=CARTESIAN_POINT('Ctrl Pts',(-3.15989538676375,-0.633411296429543,
18.7220498029931));
#15564=CARTESIAN_POINT('Ctrl Pts',(-3.16098783340588,-0.627936815578269,
18.7217028451295));
#15565=CARTESIAN_POINT('Ctrl Pts',(-3.16332395852555,-0.616069403648415,
18.7209529036556));
#15566=CARTESIAN_POINT('Ctrl Pts',(-3.16456248151383,-0.609675552290934,
18.7205502167251));
#15567=CARTESIAN_POINT('Ctrl Pts',(-3.16797182510812,-0.591784565590774,
18.7194271315627));
#15568=CARTESIAN_POINT('Ctrl Pts',(-3.17009945632821,-0.580279159992346,
18.718709155718));
#15569=CARTESIAN_POINT('Ctrl Pts',(-3.18218236287185,-0.512889018677115,
18.7145273501294));
#15570=CARTESIAN_POINT('Ctrl Pts',(-3.19072308545401,-0.456756874700976,
18.7111388013356));
#15571=CARTESIAN_POINT('Ctrl Pts',(-3.22929970137806,-0.148685318902755,
18.6929135928336));
#15572=CARTESIAN_POINT('Ctrl Pts',(-3.23098934338144,0.105918464265947,
18.6791451247785));
#15573=CARTESIAN_POINT('Ctrl Pts',(-3.18460986234148,0.520723345587924,
18.6555675995775));
#15574=CARTESIAN_POINT('Ctrl Pts',(-3.15407168514966,0.681699475468597,
18.6461377178382));
#15575=CARTESIAN_POINT('Ctrl Pts',(-3.10574092968199,0.860796509723744,
18.6349802178779));
#15576=CARTESIAN_POINT('Ctrl Pts',(-3.09981872906552,0.881885006168486,
18.6336560122168));
#15577=CARTESIAN_POINT('Ctrl Pts',(-3.09001322816324,0.915482004540831,
18.631528965117));
#15578=CARTESIAN_POINT('Ctrl Pts',(-3.08626778594734,0.928030277707106,
18.630730623957));
#15579=CARTESIAN_POINT('Ctrl Pts',(-3.07950351887017,0.950198553830946,
18.6293131803501));
#15580=CARTESIAN_POINT('Ctrl Pts',(-3.0765158153351,0.959827926640993,18.6286951068839));
#15581=CARTESIAN_POINT('Ctrl Pts',(-3.07021834120105,0.979793184016866,
18.6274086149846));
#15582=CARTESIAN_POINT('Ctrl Pts',(-3.06690145145268,0.990126672985495,
18.6267399683244));
#15583=CARTESIAN_POINT('Ctrl Pts',(-3.05819876055078,1.01677584053529,18.625008265472));
#15584=CARTESIAN_POINT('Ctrl Pts',(-3.05273461702311,1.03306539412136,18.6239426288216));
#15585=CARTESIAN_POINT('Ctrl Pts',(-3.02885975066243,1.10239672428763,18.6193760938647));
#15586=CARTESIAN_POINT('Ctrl Pts',(-3.00919578062714,1.15499352420319,18.6158337885739));
#15587=CARTESIAN_POINT('Ctrl Pts',(-2.95369796359921,1.29238404052255,18.6063669391563));
#15588=CARTESIAN_POINT('Ctrl Pts',(-2.91559000495747,1.37619786431467,18.6003705697869));
#15589=CARTESIAN_POINT('Ctrl Pts',(-2.76469229400977,1.67358824095776,18.5783083036408));
#15590=CARTESIAN_POINT('Ctrl Pts',(-2.63159300282053,1.87593298399687,18.5617041796305));
#15591=CARTESIAN_POINT('Ctrl Pts',(-2.4175863798237,2.13308837216077,18.5394371195426));
#15592=CARTESIAN_POINT('Ctrl Pts',(-2.35493550960416,2.20206089283585,18.5333386739722));
#15593=CARTESIAN_POINT('Ctrl Pts',(-2.27954852365089,2.27815082307226,18.5265537733142));
#15594=CARTESIAN_POINT('Ctrl Pts',(-2.26965357179802,2.28800903079234,18.525673579389));
#15595=CARTESIAN_POINT('Ctrl Pts',(-2.2546434462941,2.30277021916648,18.5243543324097));
#15596=CARTESIAN_POINT('Ctrl Pts',(-2.24957583622986,2.30772102116472,18.5239116446557));
#15597=CARTESIAN_POINT('Ctrl Pts',(-2.2404850698265,2.31654384613753,18.5231224032046));
#15598=CARTESIAN_POINT('Ctrl Pts',(-2.23646815166869,2.32042214852105,18.5227753614731));
#15599=CARTESIAN_POINT('Ctrl Pts',(-2.22775236774547,2.32879351066753,18.5220260383882));
#15600=CARTESIAN_POINT('Ctrl Pts',(-2.22304999412004,2.33328278456114,18.5216240494078));
#15601=CARTESIAN_POINT('Ctrl Pts',(-2.20988498633244,2.34577526093082,18.5205048807529));
#15602=CARTESIAN_POINT('Ctrl Pts',(-2.20139240091943,2.35374695633205,18.5197900962164));
#15603=CARTESIAN_POINT('Ctrl Pts',(-2.15189762402353,2.39970377141098,18.5156644215757));
#15604=CARTESIAN_POINT('Ctrl Pts',(-2.10995326087426,2.43666569058571,18.5123264724417));
#15605=CARTESIAN_POINT('Ctrl Pts',(-1.87192689628223,2.63565946837268,18.494104027447));
#15606=CARTESIAN_POINT('Ctrl Pts',(-1.65814347509957,2.77513942162934,18.4803020584553));
#15607=CARTESIAN_POINT('Ctrl Pts',(-1.28324315551436,2.96079095849586,18.4566721327093));
#15608=CARTESIAN_POINT('Ctrl Pts',(-1.13100556626155,3.02221972243942,18.4472249929358));
#15609=CARTESIAN_POINT('Ctrl Pts',(-0.953886489040685,3.07842461201488,
18.4360483281191));
#15610=CARTESIAN_POINT('Ctrl Pts',(-0.932937966991596,3.08483779788748,
18.4347238878604));
#15611=CARTESIAN_POINT('Ctrl Pts',(-0.899364822254162,3.0947426383176,18.432596535102));
#15612=CARTESIAN_POINT('Ctrl Pts',(-0.886781245041957,3.09837184605472,
18.4317981249496));
#15613=CARTESIAN_POINT('Ctrl Pts',(-0.86447160800387,3.10465908869522,18.4303806015085));
#15614=CARTESIAN_POINT('Ctrl Pts',(-0.854754483739298,3.10734838518644,
18.4297625175872));
#15615=CARTESIAN_POINT('Ctrl Pts',(-0.834552373647748,3.11283755934735,
18.4284760464805));
#15616=CARTESIAN_POINT('Ctrl Pts',(-0.824065558495295,3.1156301587213,18.4278074312794));
#15617=CARTESIAN_POINT('Ctrl Pts',(-0.796942050168053,3.12270652793809,
18.4260759014084));
#15618=CARTESIAN_POINT('Ctrl Pts',(-0.780285015068942,3.12691029097273,
18.4250104072577));
#15619=CARTESIAN_POINT('Ctrl Pts',(-0.709068355799243,3.14427887983443,
18.4204453101652));
#15620=CARTESIAN_POINT('Ctrl Pts',(-0.654206193393191,3.15614974688904,
18.4169043326551));
#15621=CARTESIAN_POINT('Ctrl Pts',(-0.508679431302738,3.18368099662322,
18.4074419328634));
#15622=CARTESIAN_POINT('Ctrl Pts',(-0.417610959557511,3.19690131416866,
18.4014487692547));
#15623=CARTESIAN_POINT('Ctrl Pts',(-0.0853757478731432,3.23069345661436,
18.3793561770081));
#15624=CARTESIAN_POINT('Ctrl Pts',(0.157323036334906,3.22798758196651,18.3627153256153));
#15625=CARTESIAN_POINT('Ctrl Pts',(0.489420883052464,3.18671925295795,18.3404452152041));
#15626=CARTESIAN_POINT('Ctrl Pts',(0.580895232767638,3.17132095643393,18.3343750193888));
#15627=CARTESIAN_POINT('Ctrl Pts',(0.685233822317667,3.14908984830965,18.3276175203486));
#15628=CARTESIAN_POINT('Ctrl Pts',(0.69886229639906,3.14609341425497,18.3267381954584));
#15629=CARTESIAN_POINT('Ctrl Pts',(0.719377511074815,3.14144293401129,18.3254199930564));
#15630=CARTESIAN_POINT('Ctrl Pts',(0.726278756195095,3.13985459562453,18.3249774891853));
#15631=CARTESIAN_POINT('Ctrl Pts',(0.738611764379593,3.13697328617736,18.3241884462775));
#15632=CARTESIAN_POINT('Ctrl Pts',(0.744045436093191,3.13568893981498,18.3238414202348));
#15633=CARTESIAN_POINT('Ctrl Pts',(0.755800816501357,3.13287806664361,18.3230919841252));
#15634=CARTESIAN_POINT('Ctrl Pts',(0.762121231774153,3.13134652897522,18.3226898672218));
#15635=CARTESIAN_POINT('Ctrl Pts',(0.779757984915972,3.12701629949713,18.3215699810386));
#15636=CARTESIAN_POINT('Ctrl Pts',(0.791063973366917,3.12417529150988,18.3208546118785));
#15637=CARTESIAN_POINT('Ctrl Pts',(0.856640836781233,3.10731810145019,18.3167187284499));
#15638=CARTESIAN_POINT('Ctrl Pts',(0.910557739454847,3.09194838133759,18.313371577826));
#15639=CARTESIAN_POINT('Ctrl Pts',(1.2066399540449,2.99912840565029,18.2951486835302));
#15640=CARTESIAN_POINT('Ctrl Pts',(1.43940148490777,2.89463329359777,18.2813528459546));
#15641=CARTESIAN_POINT('Ctrl Pts',(1.79797315437103,2.67959842873945,18.2577363040664));
#15642=CARTESIAN_POINT('Ctrl Pts',(1.93182129658792,2.58476522123123,18.248296275197));
#15643=CARTESIAN_POINT('Ctrl Pts',(2.07476017224962,2.46616491235887,18.2371252383939));
#15644=CARTESIAN_POINT('Ctrl Pts',(2.09150483055766,2.45198014971012,18.2357985935032));
#15645=CARTESIAN_POINT('Ctrl Pts',(2.11801710570682,2.42905185277313,18.2336683684992));
#15646=CARTESIAN_POINT('Ctrl Pts',(2.1278786896597,2.42041765768914,18.2328693101938));
#15647=CARTESIAN_POINT('Ctrl Pts',(2.14523360841067,2.40503472273328,18.2314510365198));
#15648=CARTESIAN_POINT('Ctrl Pts',(2.1527484958853,2.39831048073426,18.2308328541509));
#15649=CARTESIAN_POINT('Ctrl Pts',(2.16715096315845,2.38530107236995,18.2296401953241));
#15650=CARTESIAN_POINT('Ctrl Pts',(2.17404307714045,2.37902105891924,18.2290659409453));
#15651=CARTESIAN_POINT('Ctrl Pts',(2.19203346855889,2.3624849615626,18.2275576411727));
#15652=CARTESIAN_POINT('Ctrl Pts',(2.2030869330567,2.35218066350339,18.2266215368172));
#15653=CARTESIAN_POINT('Ctrl Pts',(2.24425796657028,2.31325527488551,18.2230990424902));
#15654=CARTESIAN_POINT('Ctrl Pts',(2.27389255058914,2.28413138744896,18.2204909112857));
#15655=CARTESIAN_POINT('Ctrl Pts',(2.3460843729106,2.21038614700822,18.2139505196783));
#15656=CARTESIAN_POINT('Ctrl Pts',(2.38793831318083,2.1651024463524,18.2099895603055));
#15657=CARTESIAN_POINT('Ctrl Pts',(2.5083266400144,2.02710933064286,18.1980787943525));
#15658=CARTESIAN_POINT('Ctrl Pts',(2.58294102879452,1.93113585737514,18.1899939342971));
#15659=CARTESIAN_POINT('Ctrl Pts',(2.7944592501101,1.62481187872696,18.1649296645631));
#15660=CARTESIAN_POINT('Ctrl Pts',(2.91239209062325,1.40249866989612,18.1476699394747));
#15661=CARTESIAN_POINT('Ctrl Pts',(3.01105641066714,1.14895945769275,18.1303019676058));
#15662=CARTESIAN_POINT('Ctrl Pts',(3.0185623306977,1.12909258064088,18.1289561275231));
#15663=CARTESIAN_POINT('Ctrl Pts',(3.02880797202738,1.10114151098179,18.1270851492334));
#15664=CARTESIAN_POINT('Ctrl Pts',(3.03171261142713,1.09311893418051,18.1265507193513));
#15665=CARTESIAN_POINT('Ctrl Pts',(3.03634854228329,1.0801539309388,18.1256913169539));
#15666=CARTESIAN_POINT('Ctrl Pts',(3.03809968381862,1.07521872047775,18.1253651754808));
#15667=CARTESIAN_POINT('Ctrl Pts',(3.04175618536977,1.06483341627488,18.1246809910771));
#15668=CARTESIAN_POINT('Ctrl Pts',(3.0436589396225,1.05938244069887,18.1243231105734));
#15669=CARTESIAN_POINT('Ctrl Pts',(3.04826915198432,1.04606023969208,18.1234513841908));
#15670=CARTESIAN_POINT('Ctrl Pts',(3.0509608069407,1.03818351274536,18.122938472925));
#15671=CARTESIAN_POINT('Ctrl Pts',(3.0604955236225,1.00992424507303,18.121106936953));
#15672=CARTESIAN_POINT('Ctrl Pts',(3.06716527260713,0.989483238282234,18.1197981678248));
#15673=CARTESIAN_POINT('Ctrl Pts',(3.10715374040053,0.862638288651236,18.111766819375));
#15674=CARTESIAN_POINT('Ctrl Pts',(3.13513996336408,0.754620344036068,18.1053169123422));
#15675=CARTESIAN_POINT('Ctrl Pts',(3.20072247970803,0.433752192019144,18.0867149640922));
#15676=CARTESIAN_POINT('Ctrl Pts',(3.2225904146029,0.218342495289665,18.0748961830584));
#15677=CARTESIAN_POINT('Ctrl Pts',(3.22274912977859,0.00236833514711092,
18.0625872459229));
#15678=CARTESIAN_POINT('Ctrl Pts',(3.22274913267655,0.00236438840992122,
18.0625870209879));
#15679=CARTESIAN_POINT('Ctrl Pts',(3.22284445157515,-0.127558807163035,
18.0551823522885));
#15680=CARTESIAN_POINT('Ctrl Pts',(3.21508323492089,-0.257358662884279,
18.0476275395715));
#15681=CARTESIAN_POINT('Ctrl Pts',(3.19737230323124,-0.404037165608398,
18.0387486267077));
#15682=CARTESIAN_POINT('Ctrl Pts',(3.19508730105094,-0.421725972463517,
18.0376722990145));
#15683=CARTESIAN_POINT('Ctrl Pts',(3.1910443671095,-0.451102061197792,18.0358751522722));
#15684=CARTESIAN_POINT('Ctrl Pts',(3.1893687454429,-0.46280041300465,18.0351569235573));
#15685=CARTESIAN_POINT('Ctrl Pts',(3.18622713333614,-0.48390583353325,18.0338564078719));
#15686=CARTESIAN_POINT('Ctrl Pts',(3.18478372254885,-0.493316164802716,
18.0332748407883));
#15687=CARTESIAN_POINT('Ctrl Pts',(3.1818967594068,-0.51159685385526,18.0321417069418));
#15688=CARTESIAN_POINT('Ctrl Pts',(3.18045775695675,-0.520467849159643,
18.0315902896153));
#15689=CARTESIAN_POINT('Ctrl Pts',(3.17713467290383,-0.540425098259222,
18.0303462202271));
#15690=CARTESIAN_POINT('Ctrl Pts',(3.17522964020086,-0.551507700262921,
18.0296529066549));
#15691=CARTESIAN_POINT('Ctrl Pts',(3.16995782196972,-0.581243711561549,
18.0277859357877));
#15692=CARTESIAN_POINT('Ctrl Pts',(3.1664844469219,-0.599877544118552,18.0266088912479));
#15693=CARTESIAN_POINT('Ctrl Pts',(3.15020371932445,-0.683135701098123,
18.0213170605459));
#15694=CARTESIAN_POINT('Ctrl Pts',(3.13558168493726,-0.747384993437679,
18.0171446573807));
#15695=CARTESIAN_POINT('Ctrl Pts',(3.10890837852777,-0.849949719402033,
18.0103355714641));
#15696=CARTESIAN_POINT('Ctrl Pts',(3.09809153218779,-0.888568778876834,
18.0077373744094));
#15697=CARTESIAN_POINT('Ctrl Pts',(3.06668922412087,-0.993129369458341,
18.0006099834175));
#15698=CARTESIAN_POINT('Ctrl Pts',(3.04470054740792,-1.05862476740318,17.9960433794611));
#15699=CARTESIAN_POINT('Ctrl Pts',(2.93043316240378,-1.36588065604806,17.9741683430614));
#15700=CARTESIAN_POINT('Ctrl Pts',(2.81136758919853,-1.5966455715593,17.9562941713203));
#15701=CARTESIAN_POINT('Ctrl Pts',(2.63770576812585,-1.85233932593556,17.936142975609));
#15702=CARTESIAN_POINT('Ctrl Pts',(2.60844262724126,-1.89332523048227,17.9329044844578));
#15703=CARTESIAN_POINT('Ctrl Pts',(2.57145644568551,-1.94264168891284,17.9290136953903));
#15704=CARTESIAN_POINT('Ctrl Pts',(2.56463620711472,-1.95163677912571,17.9283042852724));
#15705=CARTESIAN_POINT('Ctrl Pts',(2.55386159912693,-1.96569319631275,17.9271963481542));
#15706=CARTESIAN_POINT('Ctrl Pts',(2.54993920092933,-1.97077875034213,17.9267956339594));
#15707=CARTESIAN_POINT('Ctrl Pts',(2.54257202072558,-1.98027179274162,17.9260479370216));
#15708=CARTESIAN_POINT('Ctrl Pts',(2.53913100501961,-1.98468198803807,17.9257007084002));
#15709=CARTESIAN_POINT('Ctrl Pts',(2.53123508652209,-1.99474768526131,17.9249084728523));
#15710=CARTESIAN_POINT('Ctrl Pts',(2.52677271227889,-2.00039722404085,17.9244640066733));
#15711=CARTESIAN_POINT('Ctrl Pts',(2.51294295271654,-2.01778612238745,17.9230963890181));
#15712=CARTESIAN_POINT('Ctrl Pts',(2.50351225086715,-2.02947519061583,17.9221776493631));
#15713=CARTESIAN_POINT('Ctrl Pts',(2.40385725380719,-2.15124275853471,17.9126080672153));
#15714=CARTESIAN_POINT('Ctrl Pts',(2.30650440420755,-2.25530999285498,17.9044362802824));
#15715=CARTESIAN_POINT('Ctrl Pts',(2.06874167982989,-2.47790988873588,17.886057446617));
#15716=CARTESIAN_POINT('Ctrl Pts',(1.92445993656287,-2.59156023889675,17.8759620028464));
#15717=CARTESIAN_POINT('Ctrl Pts',(1.69034847326822,-2.74558344339987,17.8600440427088));
#15718=CARTESIAN_POINT('Ctrl Pts',(1.60704521374213,-2.79515829487832,17.85446386194));
#15719=CARTESIAN_POINT('Ctrl Pts',(1.48763613898095,-2.85911599057899,17.8464854752443));
#15720=CARTESIAN_POINT('Ctrl Pts',(1.45330927213291,-2.87671644517935,17.8441944455177));
#15721=CARTESIAN_POINT('Ctrl Pts',(1.39279862748717,-2.90638265272207,17.8401549113695));
#15722=CARTESIAN_POINT('Ctrl Pts',(1.36675312433593,-2.91872128779356,17.8384158914591));
#15723=CARTESIAN_POINT('Ctrl Pts',(1.32852772020526,-2.93620611107292,17.8358617185614));
#15724=CARTESIAN_POINT('Ctrl Pts',(1.31647560821576,-2.9416295135291,17.8350561397581));
#15725=CARTESIAN_POINT('Ctrl Pts',(1.29570867212515,-2.95082136747671,17.8336674404825));
#15726=CARTESIAN_POINT('Ctrl Pts',(1.28700986264378,-2.95462574891855,17.833085562513));
#15727=CARTESIAN_POINT('Ctrl Pts',(1.26968929143621,-2.96210981217899,17.8319265424967));
#15728=CARTESIAN_POINT('Ctrl Pts',(1.26106803239097,-2.96579042599213,17.8313494393696));
#15729=CARTESIAN_POINT('Ctrl Pts',(1.23847960553727,-2.97531764574597,17.829836782171));
#15730=CARTESIAN_POINT('Ctrl Pts',(1.22448720081539,-2.98110347167969,17.8288991698032));
#15731=CARTESIAN_POINT('Ctrl Pts',(1.17594884652967,-3.00077458105909,17.8256443111062));
#15732=CARTESIAN_POINT('Ctrl Pts',(1.1412044476014,-3.01415925211369,17.8233102688906));
#15733=CARTESIAN_POINT('Ctrl Pts',(1.09834236381055,-3.02982380113073,17.8204247154964));
#15734=CARTESIAN_POINT('Ctrl Pts',(1.09043642725761,-3.03267812502592,17.8198922203783));
#15735=CARTESIAN_POINT('Ctrl Pts',(0.747518494774859,-3.15496939851098,
17.7967841741866));
#15736=CARTESIAN_POINT('Ctrl Pts',(0.395077617771009,-3.21813806377519,
17.772171066051));
#15737=CARTESIAN_POINT('Ctrl Pts',(-0.0198095310532809,-3.22323680718099,
17.7446208297601));
#15738=CARTESIAN_POINT('Ctrl Pts',(-0.0792345535247083,-3.22232380114667,
17.7407189117324));
#15739=CARTESIAN_POINT('Ctrl Pts',(-0.161489729741018,-3.21878290181611,
17.7354079084667));
#15740=CARTESIAN_POINT('Ctrl Pts',(-0.184365289463808,-3.21755369916916,
17.7339405753569));
#15741=CARTESIAN_POINT('Ctrl Pts',(-0.2240003027912,-3.21499983758994,17.7314172197131));
#15742=CARTESIAN_POINT('Ctrl Pts',(-0.240765828266566,-3.2137877863793,
17.7303557495571));
#15743=CARTESIAN_POINT('Ctrl Pts',(-0.265034554699858,-3.21184231488938,
17.7288285314157));
#15744=CARTESIAN_POINT('Ctrl Pts',(-0.272545542442723,-3.21121368035888,
17.7283571606919));
#15745=CARTESIAN_POINT('Ctrl Pts',(-0.285668371530446,-3.2100689869704,
17.7275359450257));
#15746=CARTESIAN_POINT('Ctrl Pts',(-0.291281156137776,-3.20956455140521,
17.7271854525156));
#15747=CARTESIAN_POINT('Ctrl Pts',(-0.303098228047417,-3.20847126599808,
17.7264491389383));
#15748=CARTESIAN_POINT('Ctrl Pts',(-0.309302131199087,-3.20787914263887,
17.7260635042434));
#15749=CARTESIAN_POINT('Ctrl Pts',(-0.325883394367428,-3.20624801645108,
17.7250351964634));
#15750=CARTESIAN_POINT('Ctrl Pts',(-0.336257598355172,-3.20517661982347,
17.7243943248581));
#15751=CARTESIAN_POINT('Ctrl Pts',(-0.381505380560336,-3.20028154627505,
17.7216093122399));
#15752=CARTESIAN_POINT('Ctrl Pts',(-0.416321903141804,-3.19593877249969,
17.7194927826255));
#15753=CARTESIAN_POINT('Ctrl Pts',(-0.458313192895171,-3.19000316728307,
17.716964608063));
#15754=CARTESIAN_POINT('Ctrl Pts',(-0.46556074339324,-3.18895349388033,
17.7165291396256));
#15755=CARTESIAN_POINT('Ctrl Pts',(-0.769694187039384,-3.14384647410949,
17.6982901573871));
#15756=CARTESIAN_POINT('Ctrl Pts',(-1.05901076618924,-3.05855278755339,
17.6822134873302));
#15757=CARTESIAN_POINT('Ctrl Pts',(-1.38056708267961,-2.91255108091743,
17.6621009447274));
#15758=CARTESIAN_POINT('Ctrl Pts',(-1.42820932113431,-2.88948711399505,
17.6590625449461));
#15759=CARTESIAN_POINT('Ctrl Pts',(-1.47525542042047,-2.86526421242789,
17.6559915606006));
#15760=CARTESIAN_POINT('Ctrl Pts',(-1.47525540448706,-2.86526422063162,
17.4058265726261));
#15761=CARTESIAN_POINT('Ctrl Pts',(-1.45612575153564,-2.87511361731181,
17.4070443009508));
#15762=CARTESIAN_POINT('Ctrl Pts',(-1.43689277196508,-2.88477385269499,
17.4082657479273));
#15763=CARTESIAN_POINT('Ctrl Pts',(-1.33540932568462,-2.93447900172206,
17.4147004189395));
#15764=CARTESIAN_POINT('Ctrl Pts',(-1.25158913212826,-2.97119636113742,
17.4199813884629));
#15765=CARTESIAN_POINT('Ctrl Pts',(-1.11421716555984,-3.02452676453268,
17.4286717256038));
#15766=CARTESIAN_POINT('Ctrl Pts',(-1.06159419017941,-3.04339600551254,
17.432008406599));
#15767=CARTESIAN_POINT('Ctrl Pts',(-0.992220361865946,-3.06625348829933,
17.4364285173583));
#15768=CARTESIAN_POINT('Ctrl Pts',(-0.975888950667632,-3.07149026358307,
17.4374705632408));
#15769=CARTESIAN_POINT('Ctrl Pts',(-0.94916502936419,-3.07982481495259,
17.4391784747289));
#15770=CARTESIAN_POINT('Ctrl Pts',(-0.938797172099172,-3.08300097451808,
17.4398417523448));
#15771=CARTESIAN_POINT('Ctrl Pts',(-0.918760241051056,-3.08902877981518,
17.4411249844615));
#15772=CARTESIAN_POINT('Ctrl Pts',(-0.909093416116999,-3.09188750444613,
17.4417446979114));
#15773=CARTESIAN_POINT('Ctrl Pts',(-0.886830653444291,-3.0983577349787,
17.443173392985));
#15774=CARTESIAN_POINT('Ctrl Pts',(-0.874225848352245,-3.10193784910527,
17.443983390441));
#15775=CARTESIAN_POINT('Ctrl Pts',(-0.84045858751936,-3.11130652252011,
17.4461563921927));
#15776=CARTESIAN_POINT('Ctrl Pts',(-0.819258556591595,-3.11695593382606,
17.4475238945578));
#15777=CARTESIAN_POINT('Ctrl Pts',(-0.637465598794932,-3.16341758238275,
17.4592798946777));
#15778=CARTESIAN_POINT('Ctrl Pts',(-0.474028805680539,-3.19199854637558,
17.4700647636785));
#15779=CARTESIAN_POINT('Ctrl Pts',(-0.0520602623034604,-3.23266323718004,
17.4983527741121));
#15780=CARTESIAN_POINT('Ctrl Pts',(0.207054034465362,-3.22644491174887,
17.5161926589888));
#15781=CARTESIAN_POINT('Ctrl Pts',(0.512925487908727,-3.18207581288612,
17.5363480696752));
#15782=CARTESIAN_POINT('Ctrl Pts',(0.563031351146764,-3.17359345543301,
17.5396166830902));
#15783=CARTESIAN_POINT('Ctrl Pts',(0.624029143904995,-3.16177691512979,
17.5435383611158));
#15784=CARTESIAN_POINT('Ctrl Pts',(0.635128219274363,-3.15956607583364,
17.5442495996316));
#15785=CARTESIAN_POINT('Ctrl Pts',(0.652512403471344,-3.15600799054425,
17.5453596660837));
#15786=CARTESIAN_POINT('Ctrl Pts',(0.658805391426698,-3.15470035518508,
17.5457606958203));
#15787=CARTESIAN_POINT('Ctrl Pts',(0.670564923271226,-3.15222009115228,
17.5465085212806));
#15788=CARTESIAN_POINT('Ctrl Pts',(0.676032266710425,-3.15105207737857,
17.5468555654922));
#15789=CARTESIAN_POINT('Ctrl Pts',(0.68851966122885,-3.14835034101348,17.5476467755903));
#15790=CARTESIAN_POINT('Ctrl Pts',(0.695537627944248,-3.14680736686099,
17.5480904049825));
#15791=CARTESIAN_POINT('Ctrl Pts',(0.71386231002847,-3.14271419432294,17.5492462060343));
#15792=CARTESIAN_POINT('Ctrl Pts',(0.725160649341641,-3.14012642212542,
17.5499562764328));
#15793=CARTESIAN_POINT('Ctrl Pts',(0.799857766536948,-3.12259312881603,
17.5546353418392));
#15794=CARTESIAN_POINT('Ctrl Pts',(0.862809779745145,-3.10578829101587,
17.5585049655511));
#15795=CARTESIAN_POINT('Ctrl Pts',(0.94064497658008,-3.08246072137817,17.5632460170238));
#15796=CARTESIAN_POINT('Ctrl Pts',(0.956041436503322,-3.07772023705804,
17.5641816842582));
#15797=CARTESIAN_POINT('Ctrl Pts',(0.999474290684799,-3.06399012986382,
17.5668167182767));
#15798=CARTESIAN_POINT('Ctrl Pts',(1.02742435444135,-3.05473135401561,17.5685071624843));
#15799=CARTESIAN_POINT('Ctrl Pts',(1.27646377247133,-2.96842935815827,17.5835532989296));
#15800=CARTESIAN_POINT('Ctrl Pts',(1.48867332729716,-2.86788986957592,17.5963139995897));
#15801=CARTESIAN_POINT('Ctrl Pts',(1.78951810417125,-2.68289224549854,17.616471124758));
#15802=CARTESIAN_POINT('Ctrl Pts',(1.88737031194414,-2.61497889888649,17.6233938588013));
#15803=CARTESIAN_POINT('Ctrl Pts',(2.00457702756722,-2.52362126834575,17.6322979263554));
#15804=CARTESIAN_POINT('Ctrl Pts',(2.027665756965,-2.50510775311956,17.6340832592697));
#15805=CARTESIAN_POINT('Ctrl Pts',(2.06084179821304,-2.47774665658751,17.6366962003277));
#15806=CARTESIAN_POINT('Ctrl Pts',(2.07113442707925,-2.46914956775208,17.6375136478914));
#15807=CARTESIAN_POINT('Ctrl Pts',(2.08907879426095,-2.45397009440952,17.6389509366892));
#15808=CARTESIAN_POINT('Ctrl Pts',(2.09675387637832,-2.44741549621207,17.6395696297688));
#15809=CARTESIAN_POINT('Ctrl Pts',(2.11258558980024,-2.43376592056368,17.6408541010662));
#15810=CARTESIAN_POINT('Ctrl Pts',(2.12073755476609,-2.42666574739381,17.6415200909433));
#15811=CARTESIAN_POINT('Ctrl Pts',(2.14161706181175,-2.40829461365892,17.6432378565532));
#15812=CARTESIAN_POINT('Ctrl Pts',(2.15429129691026,-2.39696382447206,17.6442921360255));
#15813=CARTESIAN_POINT('Ctrl Pts',(2.20354447733288,-2.35222519811304,17.6484352167897));
#15814=CARTESIAN_POINT('Ctrl Pts',(2.2394392245659,-2.3180774718112,17.651555397475));
#15815=CARTESIAN_POINT('Ctrl Pts',(2.52114212272694,-2.03743400127064,17.676882874069));
#15816=CARTESIAN_POINT('Ctrl Pts',(2.72629240519677,-1.75343074881565,17.7009745820447));
#15817=CARTESIAN_POINT('Ctrl Pts',(2.9084817701896,-1.38937034365275,17.7280018457015));
#15818=CARTESIAN_POINT('Ctrl Pts',(2.93349290594752,-1.33575311400802,17.7318856011806));
#15819=CARTESIAN_POINT('Ctrl Pts',(2.96609490004213,-1.26052369690841,17.7371741338384));
#15820=CARTESIAN_POINT('Ctrl Pts',(2.97495177228867,-1.2394760843413,17.7386366668875));
#15821=CARTESIAN_POINT('Ctrl Pts',(2.98992246798089,-1.20281431434058,17.7411524961937));
#15822=CARTESIAN_POINT('Ctrl Pts',(2.9961394248586,-1.18724353630641,17.7422111994446));
#15823=CARTESIAN_POINT('Ctrl Pts',(3.00497141438551,-1.16461196419871,17.7437350845145));
#15824=CARTESIAN_POINT('Ctrl Pts',(3.00768354164911,-1.15758971334505,17.7442058571449));
#15825=CARTESIAN_POINT('Ctrl Pts',(3.01238189582363,-1.14529673009271,17.7450262901231));
#15826=CARTESIAN_POINT('Ctrl Pts',(3.01437894290325,-1.14003020871351,17.7453765951951));
#15827=CARTESIAN_POINT('Ctrl Pts',(3.01855692737781,-1.12892448357784,17.7461127831511));
#15828=CARTESIAN_POINT('Ctrl Pts',(3.02073473209977,-1.12308418797962,17.7464984784391));
#15829=CARTESIAN_POINT('Ctrl Pts',(3.02651483127294,-1.10744504630501,17.7475275056477));
#15830=CARTESIAN_POINT('Ctrl Pts',(3.03008651500919,-1.09763485416361,17.748169030717));
#15831=CARTESIAN_POINT('Ctrl Pts',(3.04549131867436,-1.05467487996011,17.7509617455538));
#15832=CARTESIAN_POINT('Ctrl Pts',(3.05682908966866,-1.02134843568971,17.7530851314645));
#15833=CARTESIAN_POINT('Ctrl Pts',(3.0715023371318,-0.975782481764143,17.755938623624));
#15834=CARTESIAN_POINT('Ctrl Pts',(3.0753144841719,-0.963700623448405,17.7566905184771));
#15835=CARTESIAN_POINT('Ctrl Pts',(3.17409445625344,-0.644080883971602,
17.7764650134878));
#15836=CARTESIAN_POINT('Ctrl Pts',(3.22254141043166,-0.324034029265177,
17.7935926669874));
#15837=CARTESIAN_POINT('Ctrl Pts',(3.22282044166776,0.108035746430257,17.8184236692774));
#15838=CARTESIAN_POINT('Ctrl Pts',(3.21724779405089,0.21807368094822,17.8248759566217));
#15839=CARTESIAN_POINT('Ctrl Pts',(3.2040066183689,0.347657188749756,17.8327224978492));
#15840=CARTESIAN_POINT('Ctrl Pts',(3.20176935274758,0.367691330990646,17.8339425495846));
#15841=CARTESIAN_POINT('Ctrl Pts',(3.19781499259019,0.400322921404961,17.8359416502096));
#15842=CARTESIAN_POINT('Ctrl Pts',(3.19621102356402,0.412933715995833,17.8367171221811));
#15843=CARTESIAN_POINT('Ctrl Pts',(3.19321229096217,0.435445516168138,17.8381067501153));
#15844=CARTESIAN_POINT('Ctrl Pts',(3.19184597583925,0.445350194386083,17.8387199968769));
#15845=CARTESIAN_POINT('Ctrl Pts',(3.18885901489756,0.466283169355085,17.8400200255195));
#15846=CARTESIAN_POINT('Ctrl Pts',(3.18722720255972,0.477309716199698,17.8407071546686));
#15847=CARTESIAN_POINT('Ctrl Pts',(3.18273185233956,0.506634525906609,17.8425408761129));
#15848=CARTESIAN_POINT('Ctrl Pts',(3.17976775608376,0.524916737218566,17.8436906510749));
#15849=CARTESIAN_POINT('Ctrl Pts',(3.16488131649599,0.611977458316588,17.8491980017644));
#15850=CARTESIAN_POINT('Ctrl Pts',(3.15088481514664,0.680377701780069,17.8536211727373));
#15851=CARTESIAN_POINT('Ctrl Pts',(3.0722107847683,1.00996372701713,17.8754206937213));
#15852=CARTESIAN_POINT('Ctrl Pts',(2.9772221379522,1.26277805420599,17.893766371748));
#15853=CARTESIAN_POINT('Ctrl Pts',(2.78674723024425,1.62473750826042,17.9213260861595));
#15854=CARTESIAN_POINT('Ctrl Pts',(2.71350851561203,1.74430876684402,17.9306470408837));
#15855=CARTESIAN_POINT('Ctrl Pts',(2.62406159944196,1.87100061137568,17.9404805789223));
#15856=CARTESIAN_POINT('Ctrl Pts',(2.61532452819609,1.88319414775847,17.9414264885495));
#15857=CARTESIAN_POINT('Ctrl Pts',(2.60227152039478,1.90114498447032,17.9428176970123));
#15858=CARTESIAN_POINT('Ctrl Pts',(2.59802107899454,1.90694934209511,17.9432673341457));
#15859=CARTESIAN_POINT('Ctrl Pts',(2.59043253064196,1.91723971695551,17.9440640421342));
#15860=CARTESIAN_POINT('Ctrl Pts',(2.58710215520272,1.92173132053647,17.944411640325));
#15861=CARTESIAN_POINT('Ctrl Pts',(2.5799218381257,1.93136275970628,17.9451566572599));
#15862=CARTESIAN_POINT('Ctrl Pts',(2.57606822990046,1.93649974877812,17.9455538131495));
#15863=CARTESIAN_POINT('Ctrl Pts',(2.5653966297188,1.95063712270634,17.9466463579134));
#15864=CARTESIAN_POINT('Ctrl Pts',(2.5585465749378,1.95961335087945,17.9473395321758));
#15865=CARTESIAN_POINT('Ctrl Pts',(2.52084339555108,2.00848440851368,17.951111831092));
#15866=CARTESIAN_POINT('Ctrl Pts',(2.4891023364133,2.04768924885605,17.9541318431589));
#15867=CARTESIAN_POINT('Ctrl Pts',(2.28909041658033,2.28320594578005,17.9723482904326));
#15868=CARTESIAN_POINT('Ctrl Pts',(2.09860524255749,2.45944120224401,17.9863684462292));
#15869=CARTESIAN_POINT('Ctrl Pts',(1.75475706810696,2.70821613460346,18.0103294489913));
#15870=CARTESIAN_POINT('Ctrl Pts',(1.61314684000517,2.79487988029072,18.0198778043431));
#15871=CARTESIAN_POINT('Ctrl Pts',(1.44596845230781,2.88023857575102,18.0311675990326));
#15872=CARTESIAN_POINT('Ctrl Pts',(1.4263252655106,2.8900164737955,18.0324940693776));
#15873=CARTESIAN_POINT('Ctrl Pts',(1.39479402428708,2.90531218800568,18.0346239255348));
#15874=CARTESIAN_POINT('Ctrl Pts',(1.38296928604833,2.91095950261216,18.0354227902043));
#15875=CARTESIAN_POINT('Ctrl Pts',(1.36198760539736,2.92082333392642,18.0368406660793));
#15876=CARTESIAN_POINT('Ctrl Pts',(1.3528446509083,2.92506932090614,18.0374586445365));
#15877=CARTESIAN_POINT('Ctrl Pts',(1.33382624617676,2.93379322418341,18.0387444424319));
#15878=CARTESIAN_POINT('Ctrl Pts',(1.32394782933076,2.93826433083612,18.0394124874795));
#15879=CARTESIAN_POINT('Ctrl Pts',(1.2983883234577,2.94967784950554,18.041141564178));
#15880=CARTESIAN_POINT('Ctrl Pts',(1.28267420156842,2.95654503240895,18.042205163103));
#15881=CARTESIAN_POINT('Ctrl Pts',(1.21552066309157,2.98525546664666,18.0467532827428));
#15882=CARTESIAN_POINT('Ctrl Pts',(1.16357512410711,3.005883062115,18.0502788037774));
#15883=CARTESIAN_POINT('Ctrl Pts',(1.02528184481835,3.05667749467831,18.0596900436848));
#15884=CARTESIAN_POINT('Ctrl Pts',(0.938145620133956,3.08453569894457,18.0656465561971));
#15885=CARTESIAN_POINT('Ctrl Pts',(0.6117131875876,3.17378696959399,18.0880286222714));
#15886=CARTESIAN_POINT('Ctrl Pts',(0.366805261952291,3.21131671021937,18.1050278394368));
#15887=CARTESIAN_POINT('Ctrl Pts',(0.0313047657450737,3.22382076755654,
18.1273374032897));
#15888=CARTESIAN_POINT('Ctrl Pts',(-0.0575265271992821,3.22345996427573,
18.1331421980008));
#15889=CARTESIAN_POINT('Ctrl Pts',(-0.16003808526958,3.2188035388841,18.1396412252152));
#15890=CARTESIAN_POINT('Ctrl Pts',(-0.173834755698983,3.21808792677811,
18.1405116985285));
#15891=CARTESIAN_POINT('Ctrl Pts',(-0.194665230427495,3.21687312776981,
18.1418191662402));
#15892=CARTESIAN_POINT('Ctrl Pts',(-0.201702489088259,3.21643955022421,
18.1422597030531));
#15893=CARTESIAN_POINT('Ctrl Pts',(-0.21430590901598,3.21562150574251,18.1430465178));
#15894=CARTESIAN_POINT('Ctrl Pts',(-0.219872524467502,3.21524567729424,
18.143393272275));
#15895=CARTESIAN_POINT('Ctrl Pts',(-0.23194415688964,3.21439916706936,18.1441435748152));
#15896=CARTESIAN_POINT('Ctrl Pts',(-0.23844870982701,3.21392319630281,18.1445468220878));
#15897=CARTESIAN_POINT('Ctrl Pts',(-0.256666856056883,3.21253447087215,
18.1456734525681));
#15898=CARTESIAN_POINT('Ctrl Pts',(-0.268377110289065,3.21157739095852,
18.1463943875404));
#15899=CARTESIAN_POINT('Ctrl Pts',(-0.337499059629746,3.20554733960997,
18.1506320763358));
#15900=CARTESIAN_POINT('Ctrl Pts',(-0.394775523023678,3.19899868746676,
18.1540711706208));
#15901=CARTESIAN_POINT('Ctrl Pts',(-0.702324638331072,3.15544822325933,
18.1722941354599));
#15902=CARTESIAN_POINT('Ctrl Pts',(-0.947775027874227,3.0906087361959,18.1860247379155));
#15903=CARTESIAN_POINT('Ctrl Pts',(-1.33514323720598,2.93772300548985,18.2095503232889));
#15904=CARTESIAN_POINT('Ctrl Pts',(-1.48235002958322,2.86626096733015,18.2189687358203));
#15905=CARTESIAN_POINT('Ctrl Pts',(-1.64240637987474,2.77292232708381,18.2301131129387));
#15906=CARTESIAN_POINT('Ctrl Pts',(-1.6612068788083,2.76170031289673,18.2314367682599));
#15907=CARTESIAN_POINT('Ctrl Pts',(-1.69106248285487,2.7434643424562,18.2335629569377));
#15908=CARTESIAN_POINT('Ctrl Pts',(-1.70219193274676,2.73657295451891,18.2343609939906));
#15909=CARTESIAN_POINT('Ctrl Pts',(-1.72181540523769,2.72425601806597,18.2357779119073));
#15910=CARTESIAN_POINT('Ctrl Pts',(-1.73032658930183,2.71885803828966,18.2363957646589));
#15911=CARTESIAN_POINT('Ctrl Pts',(-1.74794677968179,2.70756667920123,18.2376818105535));
#15912=CARTESIAN_POINT('Ctrl Pts',(-1.75705161524303,2.70166705640866,18.2383502318377));
#15913=CARTESIAN_POINT('Ctrl Pts',(-1.78049375351206,2.68630872756395,18.240081377511));
#15914=CARTESIAN_POINT('Ctrl Pts',(-1.79478539634146,2.6767812665121,18.2411466808569));
#15915=CARTESIAN_POINT('Ctrl Pts',(-1.85545430813714,2.63563230046035,18.2457119695986));
#15916=CARTESIAN_POINT('Ctrl Pts',(-1.90107499766036,2.60291788705741,18.2492533414002));
#15917=CARTESIAN_POINT('Ctrl Pts',(-2.01916376293855,2.51347597222458,18.2587176474169));
#15918=CARTESIAN_POINT('Ctrl Pts',(-2.09009266109183,2.45481036023131,18.2647123721423));
#15919=CARTESIAN_POINT('Ctrl Pts',(-2.33802641140208,2.23120024137729,18.2868002331147));
#15920=CARTESIAN_POINT('Ctrl Pts',(-2.49881685709087,2.04951737930807,18.303434122281));
#15921=CARTESIAN_POINT('Ctrl Pts',(-2.69107138038537,1.77562972968123,18.3257032110472));
#15922=CARTESIAN_POINT('Ctrl Pts',(-2.74107900340771,1.69741435656781,18.3317783952958));
#15923=CARTESIAN_POINT('Ctrl Pts',(-2.7946469161099,1.60507347299005,18.3385405136848));
#15924=CARTESIAN_POINT('Ctrl Pts',(-2.80156991802783,1.59295896067324,18.339419782127));
#15925=CARTESIAN_POINT('Ctrl Pts',(-2.81188697164123,1.57462990789696,18.3407378267085));
#15926=CARTESIAN_POINT('Ctrl Pts',(-2.81533947349657,1.5684487047318,18.3411802291892));
#15927=CARTESIAN_POINT('Ctrl Pts',(-2.82147728786471,1.55737427405552,18.3419690529458));
#15928=CARTESIAN_POINT('Ctrl Pts',(-2.82417027513916,1.55248541829707,18.3423159612009));
#15929=CARTESIAN_POINT('Ctrl Pts',(-2.82997206078908,1.54188778783922,18.3430650923667));
#15930=CARTESIAN_POINT('Ctrl Pts',(-2.83307628355408,1.53617661369418,18.3434670225946));
#15931=CARTESIAN_POINT('Ctrl Pts',(-2.84169552640974,1.52020387139251,18.3445862582335));
#15932=CARTESIAN_POINT('Ctrl Pts',(-2.84717228359785,1.5099216114046,18.3453011669901));
#15933=CARTESIAN_POINT('Ctrl Pts',(-2.87863828516783,1.45006623422994,18.349431806165));
#15934=CARTESIAN_POINT('Ctrl Pts',(-2.90339004261751,1.39984913486108,18.3527743805958));
#15935=CARTESIAN_POINT('Ctrl Pts',(-3.03322489957583,1.11815826409865,18.3709913416747));
#15936=CARTESIAN_POINT('Ctrl Pts',(-3.11195176420353,0.875508309364952,
18.3847853205575));
#15937=CARTESIAN_POINT('Ctrl Pts',(-3.19321191555972,0.465208420673437,
18.4084102668637));
#15938=CARTESIAN_POINT('Ctrl Pts',(-3.21274434882842,0.302133241127508,
18.4178616161261));
#15939=CARTESIAN_POINT('Ctrl Pts',(-3.22072151790662,0.1164061052905,18.4290428354201));
#15940=CARTESIAN_POINT('Ctrl Pts',(-3.22143836837094,0.0945107387812838,
18.4303672102604));
#15941=CARTESIAN_POINT('Ctrl Pts',(-3.22222693543087,0.0595196439731538,
18.4324943363956));
#15942=CARTESIAN_POINT('Ctrl Pts',(-3.22244216114432,0.0464275949480485,
18.4332925850442));
#15943=CARTESIAN_POINT('Ctrl Pts',(-3.22268185015237,0.0232560852781683,
18.4347097478172));
#15944=CARTESIAN_POINT('Ctrl Pts',(-3.22273882181897,0.0131770815811676,
18.4353276326444));
#15945=CARTESIAN_POINT('Ctrl Pts',(-3.22275893885171,-0.00774956298596178,
18.4366136148195));
#15946=CARTESIAN_POINT('Ctrl Pts',(-3.2227145976839,-0.0185970681394861,
18.4372819396603));
#15947=CARTESIAN_POINT('Ctrl Pts',(-3.22245862833361,-0.046612614277827,
18.4390125550256));
#15948=CARTESIAN_POINT('Ctrl Pts',(-3.22216457033418,-0.0637793887244116,
18.4400774215106));
#15949=CARTESIAN_POINT('Ctrl Pts',(-3.22032514702766,-0.136993269624943,
18.444638303431));
#15950=CARTESIAN_POINT('Ctrl Pts',(-3.21745453969237,-0.192994446388077,
18.448175605989));
#15951=CARTESIAN_POINT('Ctrl Pts',(-3.20603011011104,-0.340482031065212,
18.4576262782298));
#15952=CARTESIAN_POINT('Ctrl Pts',(-3.19502283927822,-0.431721692830996,
18.4636111815406));
#15953=CARTESIAN_POINT('Ctrl Pts',(-3.14068799958351,-0.762512781591523,
18.4857867267707));
#15954=CARTESIAN_POINT('Ctrl Pts',(-3.07417094454756,-0.997399013706139,
18.5025275184392));
#15955=CARTESIAN_POINT('Ctrl Pts',(-2.94711902925174,-1.3072849562709,18.5248062695083));
#15956=CARTESIAN_POINT('Ctrl Pts',(-2.9087782588942,-1.39050959865773,18.5308000860973));
#15957=CARTESIAN_POINT('Ctrl Pts',(-2.86058575656031,-1.48437200659344,
18.5374831954123));
#15958=CARTESIAN_POINT('Ctrl Pts',(-2.8541509164316,-1.49670761582106,18.5383599118175));
#15959=CARTESIAN_POINT('Ctrl Pts',(-2.84432517987452,-1.51524976111916,
18.5396748883754));
#15960=CARTESIAN_POINT('Ctrl Pts',(-2.84099350732603,-1.52148725299845,
18.5401167504258));
#15961=CARTESIAN_POINT('Ctrl Pts',(-2.83499575726047,-1.53262773184451,
18.5409049911504));
#15962=CARTESIAN_POINT('Ctrl Pts',(-2.83233745923613,-1.53753478877048,
18.5412518537816));
#15963=CARTESIAN_POINT('Ctrl Pts',(-2.82655233887873,-1.54814785195048,
18.5420013193396));
#15964=CARTESIAN_POINT('Ctrl Pts',(-2.82342098920803,-1.55385128483619,
18.542403627253));
#15965=CARTESIAN_POINT('Ctrl Pts',(-2.81462113180413,-1.56976489458433,
18.5435249819914));
#15966=CARTESIAN_POINT('Ctrl Pts',(-2.80891430043262,-1.5799539241454,18.5442416174317));
#15967=CARTESIAN_POINT('Ctrl Pts',(-2.77530316458965,-1.639205808861,18.5484025631841));
#15968=CARTESIAN_POINT('Ctrl Pts',(-2.74616729720722,-1.68756315886799,
18.551772456958));
#15969=CARTESIAN_POINT('Ctrl Pts',(-2.57910444111927,-1.94904447804319,
18.5699908557284));
#15970=CARTESIAN_POINT('Ctrl Pts',(-2.41762815720409,-2.14607905625322,
18.5837667029164));
#15971=CARTESIAN_POINT('Ctrl Pts',(-2.1166709531064,-2.43570250297297,18.6073593806759));
#15972=CARTESIAN_POINT('Ctrl Pts',(-1.99018748854851,-2.54009565574716,
18.6167973163546));
#15973=CARTESIAN_POINT('Ctrl Pts',(-1.83839186153147,-2.64705769737862,
18.6279659805628));
#15974=CARTESIAN_POINT('Ctrl Pts',(-1.8203258116047,-2.65951367601743,18.629292548026));
#15975=CARTESIAN_POINT('Ctrl Pts',(-1.79127010416872,-2.67911192493322,
18.6314225307015));
#15976=CARTESIAN_POINT('Ctrl Pts',(-1.78036143893364,-2.68637347202601,
18.632221423913));
#15977=CARTESIAN_POINT('Ctrl Pts',(-1.76098332835991,-2.69910298136446,
18.633639332837));
#15978=CARTESIAN_POINT('Ctrl Pts',(-1.75253189703156,-2.70459814630406,
18.6342573156413));
#15979=CARTESIAN_POINT('Ctrl Pts',(-1.73493688792836,-2.71592141412555,
18.6355431050426));
#15980=CARTESIAN_POINT('Ctrl Pts',(-1.72578941272728,-2.72174319712899,
18.636211137162));
#15981=CARTESIAN_POINT('Ctrl Pts',(-1.70209976081654,-2.7366527047816,18.6379401427575));
#15982=CARTESIAN_POINT('Ctrl Pts',(-1.68751426088323,-2.74567063271529,
18.6390036831066));
#15983=CARTESIAN_POINT('Ctrl Pts',(-1.62509861138716,-2.78357580128347,
18.6435512138504));
#15984=CARTESIAN_POINT('Ctrl Pts',(-1.57659588191112,-2.81133145193748,
18.6470761913566));
#15985=CARTESIAN_POINT('Ctrl Pts',(-1.51009990082008,-2.84712166642673,
18.6519001379075));
#15986=CARTESIAN_POINT('Ctrl Pts',(-1.49271811462675,-2.85627309264525,
18.6531602851047));
#15987=CARTESIAN_POINT('Ctrl Pts',(-1.47525539597219,-2.86526422501572,
18.654425498672));
#15988=CARTESIAN_POINT('Origin',(0.,0.,4.68922655072688));
#15989=CARTESIAN_POINT('',(-1.4752556264295,-2.8652641063588,20.1529125281009));
#15990=CARTESIAN_POINT('',(-1.47525540330815,-2.86526422123861,19.9090518554891));
#15991=CARTESIAN_POINT('',(-1.47525540501186,-2.86526422036142,4.68922655072688));
#15992=CARTESIAN_POINT('Ctrl Pts',(-1.4752556264295,-2.8652641063588,20.1529125281009));
#15993=CARTESIAN_POINT('Ctrl Pts',(-1.58150907081783,-2.81055676147094,
20.1448299054891));
#15994=CARTESIAN_POINT('Ctrl Pts',(-1.68472792541289,-2.74993488249402,
20.1367792763065));
#15995=CARTESIAN_POINT('Ctrl Pts',(-1.83114972518741,-2.65257561597443,
20.1252774331368));
#15996=CARTESIAN_POINT('Ctrl Pts',(-1.87706363638319,-2.62028619182486,
20.1216588491543));
#15997=CARTESIAN_POINT('Ctrl Pts',(-1.93147404658425,-2.57985688621777,
20.1173782547665));
#15998=CARTESIAN_POINT('Ctrl Pts',(-1.94079651661166,-2.57285103278714,
20.1166451165578));
#15999=CARTESIAN_POINT('Ctrl Pts',(-1.95525918022703,-2.56185897430235,
20.1155084529471));
#16000=CARTESIAN_POINT('Ctrl Pts',(-1.96042556803217,-2.55790763321436,
20.1151025536105));
#16001=CARTESIAN_POINT('Ctrl Pts',(-1.97000465665147,-2.55053531419898,
20.1143502899173));
#16002=CARTESIAN_POINT('Ctrl Pts',(-1.97442038699685,-2.54711854304556,
20.1140036484861));
#16003=CARTESIAN_POINT('Ctrl Pts',(-1.98441579419683,-2.53934275940705,
20.1132192755135));
#16004=CARTESIAN_POINT('Ctrl Pts',(-1.98998998592631,-2.53497683464435,
20.1127820434794));
#16005=CARTESIAN_POINT('Ctrl Pts',(-2.00650207559223,-2.52195589310432,
20.1114872815208));
#16006=CARTESIAN_POINT('Ctrl Pts',(-2.01739839043408,-2.51324806907348,
20.1106334244813));
#16007=CARTESIAN_POINT('Ctrl Pts',(-2.10015011911816,-2.44623180122144,
20.1041501092195));
#16008=CARTESIAN_POINT('Ctrl Pts',(-2.16952796855151,-2.38491769116596,
20.0987216065889));
#16009=CARTESIAN_POINT('Ctrl Pts',(-2.41055768199051,-2.15266626570666,
20.0794825403089));
#16010=CARTESIAN_POINT('Ctrl Pts',(-2.56545013902381,-1.96551235365663,
20.0663155778298));
#16011=CARTESIAN_POINT('Ctrl Pts',(-2.74822324564669,-1.68577691012337,
20.0472923993586));
#16012=CARTESIAN_POINT('Ctrl Pts',(-2.79520317876447,-1.60667733424567,
20.041984409537));
#16013=CARTESIAN_POINT('Ctrl Pts',(-2.8652997216595,-1.47625333857415,20.033253450469));
#16014=CARTESIAN_POINT('Ctrl Pts',(-2.89056812406987,-1.42614226424106,
20.0299040493047));
#16015=CARTESIAN_POINT('Ctrl Pts',(-2.92184569172013,-1.35986411281836,
20.0254692123888));
#16016=CARTESIAN_POINT('Ctrl Pts',(-2.92905251293947,-1.3442708098536,20.0244255044938));
#16017=CARTESIAN_POINT('Ctrl Pts',(-2.94060812459597,-1.31873393349066,
20.0227154025471));
#16018=CARTESIAN_POINT('Ctrl Pts',(-2.94503201840642,-1.30882456264583,
20.022051607653));
#16019=CARTESIAN_POINT('Ctrl Pts',(-2.95346938574099,-1.28966577351694,
20.020767748919));
#16020=CARTESIAN_POINT('Ctrl Pts',(-2.95748967348966,-1.28041948103156,
20.0201479283208));
#16021=CARTESIAN_POINT('Ctrl Pts',(-2.96663237393668,-1.25911931682916,
20.0187195215883));
#16022=CARTESIAN_POINT('Ctrl Pts',(-2.97172480178461,-1.24705284187155,
20.0179099225834));
#16023=CARTESIAN_POINT('Ctrl Pts',(-2.98513939882458,-1.21471823187708,
20.0157391763686));
#16024=CARTESIAN_POINT('Ctrl Pts',(-2.99332855008379,-1.19439598384677,
20.0143735475846));
#16025=CARTESIAN_POINT('Ctrl Pts',(-3.0610310977998,-1.02131450143205,20.002729642939));
#16026=CARTESIAN_POINT('Ctrl Pts',(-3.10900619999056,-0.864326578313328,
19.9920637161607));
#16027=CARTESIAN_POINT('Ctrl Pts',(-3.20042614120463,-0.456172900680657,
19.9641661210332));
#16028=CARTESIAN_POINT('Ctrl Pts',(-3.22643892361054,-0.202258031982122,
19.9466067707527));
#16029=CARTESIAN_POINT('Ctrl Pts',(-3.22142602316887,0.107972034062188,
19.926313550146));
#16030=CARTESIAN_POINT('Ctrl Pts',(-3.21906799093133,0.163846730134829,
19.9227086017824));
#16031=CARTESIAN_POINT('Ctrl Pts',(-3.21446315792113,0.231257128744744,
19.918441914501));
#16032=CARTESIAN_POINT('Ctrl Pts',(-3.21360626694635,0.242874502679417,
19.9177095752111));
#16033=CARTESIAN_POINT('Ctrl Pts',(-3.2121730023703,0.260968261074762,19.9165738779011));
#16034=CARTESIAN_POINT('Ctrl Pts',(-3.21163999934969,0.267447839391077,
19.9161681523385));
#16035=CARTESIAN_POINT('Ctrl Pts',(-3.21061279111775,0.279489257392999,
19.9154160452666));
#16036=CARTESIAN_POINT('Ctrl Pts',(-3.21012374463268,0.285051371403494,
19.9150693877194));
#16037=CARTESIAN_POINT('Ctrl Pts',(-3.20898141921467,0.297667597554251,
19.9142847674698));
#16038=CARTESIAN_POINT('Ctrl Pts',(-3.20831933684626,0.304720827283359,
19.9138473055874));
#16039=CARTESIAN_POINT('Ctrl Pts',(-3.20628294834694,0.325672006859688,
19.9125512314547));
#16040=CARTESIAN_POINT('Ctrl Pts',(-3.20484153427973,0.339563480716554,
19.9116963031328));
#16041=CARTESIAN_POINT('Ctrl Pts',(-3.19310183453127,0.44596150386417,19.905179108522));
#16042=CARTESIAN_POINT('Ctrl Pts',(-3.17888955565601,0.538001568397257,
19.8997201786849));
#16043=CARTESIAN_POINT('Ctrl Pts',(-3.11355387372116,0.866152352006445,
19.8804933316663));
#16044=CARTESIAN_POINT('Ctrl Pts',(-3.0399242278032,1.09695529577948,19.8673605761409));
#16045=CARTESIAN_POINT('Ctrl Pts',(-2.90357876720631,1.40136242090686,19.8483724114345));
#16046=CARTESIAN_POINT('Ctrl Pts',(-2.86238353099329,1.4836929866749,19.8430609684286));
#16047=CARTESIAN_POINT('Ctrl Pts',(-2.79047631111842,1.61323012332937,19.8343248481446));
#16048=CARTESIAN_POINT('Ctrl Pts',(-2.76195151809205,1.66159342433065,19.8309738528987));
#16049=CARTESIAN_POINT('Ctrl Pts',(-2.7230673863931,1.72375078348942,19.8265371988607));
#16050=CARTESIAN_POINT('Ctrl Pts',(-2.71383917252834,1.73824327477094,19.8254933113669));
#16051=CARTESIAN_POINT('Ctrl Pts',(-2.69859350641019,1.76176855212355,19.8237829890729));
#16052=CARTESIAN_POINT('Ctrl Pts',(-2.69264545031103,1.77084607418422,19.8231191547228));
#16053=CARTESIAN_POINT('Ctrl Pts',(-2.68108336264871,1.78829841403298,19.8218352715958));
#16054=CARTESIAN_POINT('Ctrl Pts',(-2.67547565072834,1.79667728147751,19.8212154663399));
#16055=CARTESIAN_POINT('Ctrl Pts',(-2.66249406823364,1.81587840811226,19.8197871693867));
#16056=CARTESIAN_POINT('Ctrl Pts',(-2.65509340388234,1.82668225615488,19.8189776653276));
#16057=CARTESIAN_POINT('Ctrl Pts',(-2.6351381933721,1.85543636043771,19.8168073392544));
#16058=CARTESIAN_POINT('Ctrl Pts',(-2.62246630946823,1.87330398046892,19.8154420383921));
#16059=CARTESIAN_POINT('Ctrl Pts',(-2.51356803836523,2.02358229134073,19.8038147869979));
#16060=CARTESIAN_POINT('Ctrl Pts',(-2.40757998259418,2.1485933910969,19.7931664667038));
#16061=CARTESIAN_POINT('Ctrl Pts',(-2.11417688084498,2.44556808878349,19.7653240969013));
#16062=CARTESIAN_POINT('Ctrl Pts',(-1.9150838537895,2.60441857064274,19.7478035137965));
#16063=CARTESIAN_POINT('Ctrl Pts',(-1.65129683131018,2.76813011624045,19.7274896915165));
#16064=CARTESIAN_POINT('Ctrl Pts',(-1.602389759136,2.79672550612217,19.7238366312137));
#16065=CARTESIAN_POINT('Ctrl Pts',(-1.54250491723111,2.82965242776748,19.7195208984084));
#16066=CARTESIAN_POINT('Ctrl Pts',(-1.53222811654846,2.83523037695365,19.7187857564271));
#16067=CARTESIAN_POINT('Ctrl Pts',(-1.51618177126293,2.84382713819689,19.7176466695234));
#16068=CARTESIAN_POINT('Ctrl Pts',(-1.51043317629794,2.84688453878517,19.7172403346019));
#16069=CARTESIAN_POINT('Ctrl Pts',(-1.49973850177118,2.85253100850274,19.7164876772946));
#16070=CARTESIAN_POINT('Ctrl Pts',(-1.49479500791652,2.85512462305829,19.7161410752378));
#16071=CARTESIAN_POINT('Ctrl Pts',(-1.48357465924153,2.86097427310295,19.7153573174425));
#16072=CARTESIAN_POINT('Ctrl Pts',(-1.47729382795224,2.86422249642826,19.7149206579408));
#16073=CARTESIAN_POINT('Ctrl Pts',(-1.45863136126096,2.8737963444861,19.7136291617364));
#16074=CARTESIAN_POINT('Ctrl Pts',(-1.4462192378485,2.88006263992137,19.7127779705053));
#16075=CARTESIAN_POINT('Ctrl Pts',(-1.35206956634523,2.9268322306399,19.7063770091189));
#16076=CARTESIAN_POINT('Ctrl Pts',(-1.2686777431929,2.96393304996601,19.701022470257));
#16077=CARTESIAN_POINT('Ctrl Pts',(-0.957054131969724,3.0870060763848,19.6817522891793));
#16078=CARTESIAN_POINT('Ctrl Pts',(-0.720854904344486,3.15054610207915,
19.668501139492));
#16079=CARTESIAN_POINT('Ctrl Pts',(-0.388962476747943,3.20050818343474,
19.6493922600195));
#16080=CARTESIAN_POINT('Ctrl Pts',(-0.297650857714207,3.21028760149491,
19.644093403267));
#16081=CARTESIAN_POINT('Ctrl Pts',(-0.15012324660166,3.21973932758882,19.6353760964909));
#16082=CARTESIAN_POINT('Ctrl Pts',(-0.0941142254685356,3.22186285627564,
19.6320309136472));
#16083=CARTESIAN_POINT('Ctrl Pts',(-0.0209117142161527,3.2227278941025,
19.6276008855463));
#16084=CARTESIAN_POINT('Ctrl Pts',(-0.00374160312160156,3.22279356488666,
19.6265576533029));
#16085=CARTESIAN_POINT('Ctrl Pts',(0.024278181707385,3.22267681621623,19.6248481349166));
#16086=CARTESIAN_POINT('Ctrl Pts',(0.0351280006634178,3.22257681225764,
19.6241844445094));
#16087=CARTESIAN_POINT('Ctrl Pts',(0.0560591366900466,3.22227817014431,
19.622900650278));
#16088=CARTESIAN_POINT('Ctrl Pts',(0.0661404460757551,3.22208700538951,
19.6222807889551));
#16089=CARTESIAN_POINT('Ctrl Pts',(0.0893180377935905,3.22153868352731,
19.6208520910531));
#16090=CARTESIAN_POINT('Ctrl Pts',(0.102413304188272,3.22114897331931,19.6200422402536));
#16091=CARTESIAN_POINT('Ctrl Pts',(0.137415421972493,3.21989366573872,19.6178703796962));
#16092=CARTESIAN_POINT('Ctrl Pts',(0.159316127206305,3.21888436420238,19.6165038811304));
#16093=CARTESIAN_POINT('Ctrl Pts',(0.345579019831747,3.20839483362228,19.6048155857783));
#16094=CARTESIAN_POINT('Ctrl Pts',(0.50897657726643,3.18655773930985,19.5941027114151));
#16095=CARTESIAN_POINT('Ctrl Pts',(0.920293432848455,3.09914011912911,19.5660507218547));
#16096=CARTESIAN_POINT('Ctrl Pts',(1.16337590182619,3.01631590251475,19.5483803251273));
#16097=CARTESIAN_POINT('Ctrl Pts',(1.44267641763328,2.88230902421551,19.5281421813263));
#16098=CARTESIAN_POINT('Ctrl Pts',(1.49066523205695,2.85778559960499,19.5246712743163));
#16099=CARTESIAN_POINT('Ctrl Pts',(1.54814494884393,2.82656992430758,19.5205415936416));
#16100=CARTESIAN_POINT('Ctrl Pts',(1.55824082667222,2.82101681228522,19.5198173071995));
#16101=CARTESIAN_POINT('Ctrl Pts',(1.57396235251129,2.81225923136103,19.518691353531));
#16102=CARTESIAN_POINT('Ctrl Pts',(1.57960837523857,2.80909182016631,19.5182873827851));
#16103=CARTESIAN_POINT('Ctrl Pts',(1.59010907634868,2.80315927132294,19.5175368439194));
#16104=CARTESIAN_POINT('Ctrl Pts',(1.59496605857384,2.80039855159085,19.5171900102636));
#16105=CARTESIAN_POINT('Ctrl Pts',(1.60599937265803,2.79408917454232,19.516402832119));
#16106=CARTESIAN_POINT('Ctrl Pts',(1.61217112067303,2.79053266962419,19.5159630019649));
#16107=CARTESIAN_POINT('Ctrl Pts',(1.63098363640777,2.77960860674593,19.5146236873949));
#16108=CARTESIAN_POINT('Ctrl Pts',(1.64358627478455,2.77217528396755,19.5137283547015));
#16109=CARTESIAN_POINT('Ctrl Pts',(1.81834669798318,2.66748689738016,19.5013328501473));
#16110=CARTESIAN_POINT('Ctrl Pts',(1.97171501116726,2.55621453241845,19.4906847032626));
#16111=CARTESIAN_POINT('Ctrl Pts',(2.22632928955124,2.33485562904533,19.4718063333693));
#16112=CARTESIAN_POINT('Ctrl Pts',(2.33135668770654,2.22999264012755,19.4635740262155));
#16113=CARTESIAN_POINT('Ctrl Pts',(2.48772705920942,2.05070032794521,19.4500155588232));
#16114=CARTESIAN_POINT('Ctrl Pts',(2.54381445235653,1.98069785013082,19.4448346071155));
#16115=CARTESIAN_POINT('Ctrl Pts',(2.62954086749114,1.8640464455862,19.4362937802165));
#16116=CARTESIAN_POINT('Ctrl Pts',(2.6610281800176,1.81881357012862,19.433003349463));
#16117=CARTESIAN_POINT('Ctrl Pts',(2.70072714124068,1.7585453463084,19.428635774692));
#16118=CARTESIAN_POINT('Ctrl Pts',(2.71000169836993,1.744218909385,19.4275987680179));
#16119=CARTESIAN_POINT('Ctrl Pts',(2.72497357010668,1.72068411948888,19.425896886214));
#16120=CARTESIAN_POINT('Ctrl Pts',(2.73073911634198,1.71151940415405,19.42523456219));
#16121=CARTESIAN_POINT('Ctrl Pts',(2.74178891683205,1.69375704825495,19.4239515985712));
#16122=CARTESIAN_POINT('Ctrl Pts',(2.74707919256204,1.68516328854851,19.4233311917428));
#16123=CARTESIAN_POINT('Ctrl Pts',(2.7591721815659,1.66531062372396,19.4218986246328));
#16124=CARTESIAN_POINT('Ctrl Pts',(2.76594646278878,1.6540346906137,19.4210854322));
#16125=CARTESIAN_POINT('Ctrl Pts',(2.78391987389931,1.62369837462909,19.4188987642791));
#16126=CARTESIAN_POINT('Ctrl Pts',(2.79499207600717,1.60456396936572,19.4175207033215));
#16127=CARTESIAN_POINT('Ctrl Pts',(2.91479996675928,1.39251501572033,19.4022591189098));
#16128=CARTESIAN_POINT('Ctrl Pts',(3.00355053241839,1.18903596725833,19.3876437110219));
#16129=CARTESIAN_POINT('Ctrl Pts',(3.11860587063777,0.827823499110241,19.3620682756189));
#16130=CARTESIAN_POINT('Ctrl Pts',(3.15537866889177,0.674226593354248,19.3513167057866));
#16131=CARTESIAN_POINT('Ctrl Pts',(3.19075236969728,0.457247319535713,19.3366982276522));
#16132=CARTESIAN_POINT('Ctrl Pts',(3.19897302871177,0.395661876423688,19.3326133971996));
#16133=CARTESIAN_POINT('Ctrl Pts',(3.20785573059182,0.310382054362313,19.3270780147799));
#16134=CARTESIAN_POINT('Ctrl Pts',(3.21004436785005,0.286863443872466,19.3255641214724));
#16135=CARTESIAN_POINT('Ctrl Pts',(3.21338092958647,0.246164437055192,19.3229686007711));
#16136=CARTESIAN_POINT('Ctrl Pts',(3.21465007854317,0.228995266056595,19.3218811141053));
#16137=CARTESIAN_POINT('Ctrl Pts',(3.21628184103584,0.204221952866047,19.3203235210708));
#16138=CARTESIAN_POINT('Ctrl Pts',(3.21675516676079,0.196625753492516,19.3198474815529));
#16139=CARTESIAN_POINT('Ctrl Pts',(3.21753275924213,0.183391345602903,19.3190209114062));
#16140=CARTESIAN_POINT('Ctrl Pts',(3.21784912478964,0.177753915601158,19.3186697072606));
#16141=CARTESIAN_POINT('Ctrl Pts',(3.21848164862976,0.165927228029126,19.3179348118808));
#16142=CARTESIAN_POINT('Ctrl Pts',(3.21879477083492,0.159737886394153,19.3175512923402));
#16143=CARTESIAN_POINT('Ctrl Pts',(3.21957949075374,0.143286416133132,19.316534659293));
#16144=CARTESIAN_POINT('Ctrl Pts',(3.22001988250982,0.133022769719706,19.3159032761931));
#16145=CARTESIAN_POINT('Ctrl Pts',(3.22169539694781,0.0890672795835738,
19.3132108993376));
#16146=CARTESIAN_POINT('Ctrl Pts',(3.2224509186319,0.055357896520954,19.3111753121586));
#16147=CARTESIAN_POINT('Ctrl Pts',(3.22272298602462,0.0148435258586338,
19.3087572402425));
#16148=CARTESIAN_POINT('Ctrl Pts',(3.22274712721112,0.00804552500573022,
19.3083524684467));
#16149=CARTESIAN_POINT('Ctrl Pts',(3.22277849800885,-0.0730004198150295,
19.3035377036578));
#16150=CARTESIAN_POINT('Ctrl Pts',(3.22024136583333,-0.147232271517654,
19.2992369287868));
#16151=CARTESIAN_POINT('Ctrl Pts',(3.19469428419743,-0.518366387926518,
19.2779955576693));
#16152=CARTESIAN_POINT('Ctrl Pts',(3.13318255256786,-0.811143990175159,
19.2619329255183));
#16153=CARTESIAN_POINT('Ctrl Pts',(3.00780883092955,-1.15950601489482,19.2402985590405));
#16154=CARTESIAN_POINT('Ctrl Pts',(2.9809803197666,-1.22683466623455,19.236000756736));
#16155=CARTESIAN_POINT('Ctrl Pts',(2.94413189172934,-1.31094637945692,19.2304562542369));
#16156=CARTESIAN_POINT('Ctrl Pts',(2.93619694034723,-1.3286235387898,19.2292810116694));
#16157=CARTESIAN_POINT('Ctrl Pts',(2.92332017341804,-1.35663105958172,19.2274025483642));
#16158=CARTESIAN_POINT('Ctrl Pts',(2.9184817895145,-1.36700867117513,19.2267029038936));
#16159=CARTESIAN_POINT('Ctrl Pts',(2.90933101346451,-1.38636569493844,19.2253909993415));
#16160=CARTESIAN_POINT('Ctrl Pts',(2.90503208207378,-1.39535134807705,19.2247792132542));
#16161=CARTESIAN_POINT('Ctrl Pts',(2.89534851832123,-1.41535326722515,19.2234110764857));
#16162=CARTESIAN_POINT('Ctrl Pts',(2.88994255463398,-1.42635897930154,19.2226539864985));
#16163=CARTESIAN_POINT('Ctrl Pts',(2.87391119076928,-1.45853109063794,19.2204280669516));
#16164=CARTESIAN_POINT('Ctrl Pts',(2.86311529546831,-1.47961117571212,19.2189532647551));
#16165=CARTESIAN_POINT('Ctrl Pts',(2.76478590054308,-1.6665029103353,19.2057290642957));
#16166=CARTESIAN_POINT('Ctrl Pts',(2.66318513963721,-1.82447151263482,19.1934664007828));
#16167=CARTESIAN_POINT('Ctrl Pts',(2.42455401711833,-2.13275030578677,19.167326124335));
#16168=CARTESIAN_POINT('Ctrl Pts',(2.28585811544675,-2.28077572209119,19.1534538480813));
#16169=CARTESIAN_POINT('Ctrl Pts',(2.07290344763074,-2.46898359281224,19.1346206446238));
#16170=CARTESIAN_POINT('Ctrl Pts',(2.00956486801986,-2.52080547366079,19.1292867495923));
#16171=CARTESIAN_POINT('Ctrl Pts',(1.93351400892478,-2.57833757250679,19.1232492555536));
#16172=CARTESIAN_POINT('Ctrl Pts',(1.92265922222932,-2.58644207182011,19.122395913323));
#16173=CARTESIAN_POINT('Ctrl Pts',(1.90612276766789,-2.59862703663872,19.1211089862628));
#16174=CARTESIAN_POINT('Ctrl Pts',(1.90047854601656,-2.6027577258163,19.1206720204612));
#16175=CARTESIAN_POINT('Ctrl Pts',(1.89030933609136,-2.61014928377143,19.1198889082281));
#16176=CARTESIAN_POINT('Ctrl Pts',(1.885789313741,-2.61341679326787,19.1195423058356));
#16177=CARTESIAN_POINT('Ctrl Pts',(1.87592674035221,-2.62050750522005,19.1187892428794));
#16178=CARTESIAN_POINT('Ctrl Pts',(1.87058099143988,-2.62432609947103,19.1183831001334));
#16179=CARTESIAN_POINT('Ctrl Pts',(1.85546872011168,-2.63505151332524,19.1172405603097));
#16180=CARTESIAN_POINT('Ctrl Pts',(1.84567524572291,-2.64192042782369,19.11650672306));
#16181=CARTESIAN_POINT('Ctrl Pts',(1.78541957253379,-2.68368376002771,19.1120303698343));
#16182=CARTESIAN_POINT('Ctrl Pts',(1.73400400122666,-2.71718840584321,19.1083760564091));
#16183=CARTESIAN_POINT('Ctrl Pts',(1.45619144123849,-2.88712326548705,19.0893163305726));
#16184=CARTESIAN_POINT('Ctrl Pts',(1.21459615008605,-2.99679133710031,19.075020832308));
#16185=CARTESIAN_POINT('Ctrl Pts',(0.820498522098549,-3.12009221940006,
19.0515996174903));
#16186=CARTESIAN_POINT('Ctrl Pts',(0.675816620101371,-3.15459298521018,
19.0429970513988));
#16187=CARTESIAN_POINT('Ctrl Pts',(0.507989311013196,-3.18253521482162,
19.0327610077907));
#16188=CARTESIAN_POINT('Ctrl Pts',(0.486661383154679,-3.18586631814296,
19.0314557516721));
#16189=CARTESIAN_POINT('Ctrl Pts',(0.45243582464647,-3.19086014258285,19.0293534063145));
#16190=CARTESIAN_POINT('Ctrl Pts',(0.439558566487385,-3.19265953145594,
19.0285606517345));
#16191=CARTESIAN_POINT('Ctrl Pts',(0.416691597288479,-3.19571385433673,
19.027149656768));
#16192=CARTESIAN_POINT('Ctrl Pts',(0.406706176182196,-3.19700000135308,
19.0265324141123));
#16193=CARTESIAN_POINT('Ctrl Pts',(0.385903552373792,-3.19958039377482,
19.0252441605964));
#16194=CARTESIAN_POINT('Ctrl Pts',(0.37508550066179,-3.20086661866584,19.0245729041152));
#16195=CARTESIAN_POINT('Ctrl Pts',(0.347002890967104,-3.2040612137061,19.0228268618194));
#16196=CARTESIAN_POINT('Ctrl Pts',(0.329729230712132,-3.20588488297499,
19.0217494140295));
#16197=CARTESIAN_POINT('Ctrl Pts',(0.254830727000385,-3.21318057491867,
19.0170620932696));
#16198=CARTESIAN_POINT('Ctrl Pts',(0.197082041550582,-3.21723888991693,
19.0134080413902));
#16199=CARTESIAN_POINT('Ctrl Pts',(0.04328563498193,-3.22389080046199,19.0035638996268));
#16200=CARTESIAN_POINT('Ctrl Pts',(-0.0528163788317471,-3.22374830327729,
18.9972946626481));
#16201=CARTESIAN_POINT('Ctrl Pts',(-0.290174780290116,-3.21278019237065,
18.9815453994762));
#16202=CARTESIAN_POINT('Ctrl Pts',(-0.430996169123826,-3.1969353721517,
18.9719632255826));
#16203=CARTESIAN_POINT('Ctrl Pts',(-0.753288694418371,-3.1389866440437,
18.9497987822883));
#16204=CARTESIAN_POINT('Ctrl Pts',(-0.933099434442101,-3.0903111096826,
18.9372514345219));
#16205=CARTESIAN_POINT('Ctrl Pts',(-1.12150649419319,-3.02135004532682,
18.9245347098674));
#16206=CARTESIAN_POINT('Ctrl Pts',(-1.13525290509136,-3.01621182505879,
18.9236095613343));
#16207=CARTESIAN_POINT('Ctrl Pts',(-1.15562712053581,-3.00843719929124,
18.922242854601));
#16208=CARTESIAN_POINT('Ctrl Pts',(-1.1622818173033,-3.00587248619864,18.9217971732528));
#16209=CARTESIAN_POINT('Ctrl Pts',(-1.17413503282518,-3.00125902039302,
18.9210046857931));
#16210=CARTESIAN_POINT('Ctrl Pts',(-1.17933677590245,-2.99921882386719,
18.9206573749229));
#16211=CARTESIAN_POINT('Ctrl Pts',(-1.1905482801737,-2.99478783657652,18.9199098291231));
#16212=CARTESIAN_POINT('Ctrl Pts',(-1.19655614087605,-2.99239248712474,
18.9195098739371));
#16213=CARTESIAN_POINT('Ctrl Pts',(-1.21322110132825,-2.98568991114394,
18.9184020951802));
#16214=CARTESIAN_POINT('Ctrl Pts',(-1.22386255480651,-2.98134368069958,
18.9176965882952));
#16215=CARTESIAN_POINT('Ctrl Pts',(-1.28385358468796,-2.95646653970393,
18.9137286453667));
#16216=CARTESIAN_POINT('Ctrl Pts',(-1.33271285124997,-2.93476603096161,
18.9105327837608));
#16217=CARTESIAN_POINT('Ctrl Pts',(-1.41269118604885,-2.89683455101536,
18.905325133276));
#16218=CARTESIAN_POINT('Ctrl Pts',(-1.44410934605154,-2.88130057567452,
18.903285620779));
#16219=CARTESIAN_POINT('Ctrl Pts',(-1.47525548819429,-2.86526417753278,
18.9012640026169));
#16220=CARTESIAN_POINT('',(3.22274909203151,0.00241915483385854,19.0621741053498));
#16221=CARTESIAN_POINT('Ctrl Pts',(-1.47525539597219,-2.86526422501572,
18.654425498672));
#16222=CARTESIAN_POINT('Ctrl Pts',(-1.41144708398913,-2.8981175848347,18.6590485555753));
#16223=CARTESIAN_POINT('Ctrl Pts',(-1.34655824498599,-2.92883077286582,
18.6637399058522));
#16224=CARTESIAN_POINT('Ctrl Pts',(-1.05392432190458,-3.05555739076919,
18.6848308599967));
#16225=CARTESIAN_POINT('Ctrl Pts',(-0.816634087221224,-3.12734400873752,
18.7018403219975));
#16226=CARTESIAN_POINT('Ctrl Pts',(-0.486223261711201,-3.18709402826258,
18.7241514003409));
#16227=CARTESIAN_POINT('Ctrl Pts',(-0.398337112113005,-3.19926742450981,
18.7299489907558));
#16228=CARTESIAN_POINT('Ctrl Pts',(-0.296305891333724,-3.2091293402707,
18.7364409869867));
#16229=CARTESIAN_POINT('Ctrl Pts',(-0.282550351901905,-3.2103697012255,
18.7373112136248));
#16230=CARTESIAN_POINT('Ctrl Pts',(-0.26176186273103,-3.21210958524966,
18.7386183845476));
#16231=CARTESIAN_POINT('Ctrl Pts',(-0.254734758486197,-3.21267450350909,
18.7390588689056));
#16232=CARTESIAN_POINT('Ctrl Pts',(-0.242143065127759,-3.21364519295148,
18.7398456273208));
#16233=CARTESIAN_POINT('Ctrl Pts',(-0.23657924651088,-3.21405957502829,
18.7401923776251));
#16234=CARTESIAN_POINT('Ctrl Pts',(-0.224508543681847,-3.21492706278769,
18.740942713798));
#16235=CARTESIAN_POINT('Ctrl Pts',(-0.218001371343994,-3.21537486292088,
18.7413459986431));
#16236=CARTESIAN_POINT('Ctrl Pts',(-0.19976630781111,-3.21657412327742,
18.7424728403003));
#16237=CARTESIAN_POINT('Ctrl Pts',(-0.188035458177054,-3.21728120385095,
18.7431939473967));
#16238=CARTESIAN_POINT('Ctrl Pts',(-0.118703746524175,-3.22107968863735,
18.7474347471748));
#16239=CARTESIAN_POINT('Ctrl Pts',(-0.0610281615454945,-3.22268854529622,
18.750876647311));
#16240=CARTESIAN_POINT('Ctrl Pts',(0.249602492011957,-3.22301013794714,
18.7690998249373));
#16241=CARTESIAN_POINT('Ctrl Pts',(0.501715478025962,-3.19349397726525,
18.7828286133357));
#16242=CARTESIAN_POINT('Ctrl Pts',(0.906658883228421,-3.09689503042297,
18.8063463238252));
#16243=CARTESIAN_POINT('Ctrl Pts',(1.06238520286678,-3.0469848183783,18.8157585454186));
#16244=CARTESIAN_POINT('Ctrl Pts',(1.23397521955806,-2.9772309678316,18.8268989886587));
#16245=CARTESIAN_POINT('Ctrl Pts',(1.25421790558573,-2.96876009255208,18.8282255405014));
#16246=CARTESIAN_POINT('Ctrl Pts',(1.28640856389834,-2.95490140226963,18.8303555028277));
#16247=CARTESIAN_POINT('Ctrl Pts',(1.29841313498423,-2.94964618443391,18.8311543914486));
#16248=CARTESIAN_POINT('Ctrl Pts',(1.31959511261298,-2.94021902675593,18.832572295057));
#16249=CARTESIAN_POINT('Ctrl Pts',(1.32878567448206,-2.93607694281898,18.833190277162));
#16250=CARTESIAN_POINT('Ctrl Pts',(1.33812432300256,-2.93181528966114,18.8338210809947));
#16251=CARTESIAN_POINT('Ctrl Pts',(1.33829207043237,-2.93173872142791,18.8338324128837));
#16252=CARTESIAN_POINT('Ctrl Pts',(1.33865440448754,-2.9315732966456,18.8338568917751));
#16253=CARTESIAN_POINT('Ctrl Pts',(1.33884898883243,-2.9314844351219,18.8338700389496));
#16254=CARTESIAN_POINT('Ctrl Pts',(1.33921163754135,-2.93131877940916,18.8338945438315));
#16255=CARTESIAN_POINT('Ctrl Pts',(1.33937970398714,-2.93124199021328,18.8339059013573));
#16256=CARTESIAN_POINT('Ctrl Pts',(1.339692941405,-2.93109884014989,18.8339270709544));
#16257=CARTESIAN_POINT('Ctrl Pts',(1.33983811505365,-2.93103248249264,18.8339368829661));
#16258=CARTESIAN_POINT('Ctrl Pts',(1.34010869714778,-2.93090877738365,18.8339551724155));
#16259=CARTESIAN_POINT('Ctrl Pts',(1.34023410819899,-2.93085143204747,18.8339636498499));
#16260=CARTESIAN_POINT('Ctrl Pts',(1.34046786643706,-2.93074452584053,18.833979452234));
#16261=CARTESIAN_POINT('Ctrl Pts',(1.34057621625092,-2.93069496623512,18.8339867772273));
#16262=CARTESIAN_POINT('Ctrl Pts',(1.34077818258811,-2.93060257254258,18.8340004319043));
#16263=CARTESIAN_POINT('Ctrl Pts',(1.34087180185896,-2.93055973903892,18.8340067616739));
#16264=CARTESIAN_POINT('Ctrl Pts',(1.3410742718813,-2.93046709145935,18.834020451678));
#16265=CARTESIAN_POINT('Ctrl Pts',(1.34118312428248,-2.93041727471893,18.8340278121276));
#16266=CARTESIAN_POINT('Ctrl Pts',(1.34139727358124,-2.93031925399564,18.8340422933924));
#16267=CARTESIAN_POINT('Ctrl Pts',(1.34150256491635,-2.93027105303097,18.8340494138057));
#16268=CARTESIAN_POINT('Ctrl Pts',(1.34170970930445,-2.93017621159662,18.8340634228487));
#16269=CARTESIAN_POINT('Ctrl Pts',(1.34181156326627,-2.93012957115092,18.834070311516));
#16270=CARTESIAN_POINT('Ctrl Pts',(1.34201195401537,-2.93003779660355,18.8340838651873));
#16271=CARTESIAN_POINT('Ctrl Pts',(1.34211049177097,-2.92999266246921,18.8340905302344));
#16272=CARTESIAN_POINT('Ctrl Pts',(1.34230436658175,-2.92990384841405,18.8341036444773));
#16273=CARTESIAN_POINT('Ctrl Pts',(1.34239970473408,-2.92986016837412,18.8341100937265));
#16274=CARTESIAN_POINT('Ctrl Pts',(1.34258729253158,-2.92977421224376,18.8341227839013));
#16275=CARTESIAN_POINT('Ctrl Pts',(1.34267954334087,-2.92973193597798,18.8341290248862));
#16276=CARTESIAN_POINT('Ctrl Pts',(1.34286106445551,-2.92964873896367,18.8341413057813));
#16277=CARTESIAN_POINT('Ctrl Pts',(1.34295033599251,-2.92960781798504,18.8341473457568));
#16278=CARTESIAN_POINT('Ctrl Pts',(1.34312600243163,-2.92952728492555,18.8341592316067));
#16279=CARTESIAN_POINT('Ctrl Pts',(1.34321239869068,-2.92948767253496,18.8341650775562));
#16280=CARTESIAN_POINT('Ctrl Pts',(1.34338241451021,-2.92940971175856,18.8341765820659));
#16281=CARTESIAN_POINT('Ctrl Pts',(1.34346603554994,-2.92937136298623,18.8341822407105));
#16282=CARTESIAN_POINT('Ctrl Pts',(1.3436305972863,-2.92929588612408,18.8341933770839));
#16283=CARTESIAN_POINT('Ctrl Pts',(1.34371153949483,-2.92925875761347,18.8341988549002));
#16284=CARTESIAN_POINT('Ctrl Pts',(1.34387083601108,-2.92918567968094,18.8342096358293));
#16285=CARTESIAN_POINT('Ctrl Pts',(1.34394919204544,-2.92914972972171,18.8342149390451));
#16286=CARTESIAN_POINT('Ctrl Pts',(1.34410339855715,-2.92907897186964,18.8342253763051));
#16287=CARTESIAN_POINT('Ctrl Pts',(1.3441792508224,-2.92904416339651,18.8342305104569));
#16288=CARTESIAN_POINT('Ctrl Pts',(1.34432856920439,-2.92897563442441,18.8342406176337));
#16289=CARTESIAN_POINT('Ctrl Pts',(1.34440201662103,-2.92894192273188,18.8342455893803));
#16290=CARTESIAN_POINT('Ctrl Pts',(1.34454658297553,-2.92887556151379,18.8342553756139));
#16291=CARTESIAN_POINT('Ctrl Pts',(1.34461770197756,-2.92884291216728,18.8342601900938));
#16292=CARTESIAN_POINT('Ctrl Pts',(1.34475769107534,-2.92877863972968,18.834269667147));
#16293=CARTESIAN_POINT('Ctrl Pts',(1.34482656124352,-2.92874701680036,18.8342743297146));
#16294=CARTESIAN_POINT('Ctrl Pts',(1.34496212922607,-2.92868476262546,18.8342835080944));
#16295=CARTESIAN_POINT('Ctrl Pts',(1.34502882713768,-2.92865413151767,18.8342880239033));
#16296=CARTESIAN_POINT('Ctrl Pts',(1.3555316014687,-2.92383028347042,18.8349991420772));
#16297=CARTESIAN_POINT('Ctrl Pts',(1.36594187343311,-2.91898137062315,18.8357076702584));
#16298=CARTESIAN_POINT('Ctrl Pts',(1.39472831273764,-2.90538546276715,18.8376772155866));
#16299=CARTESIAN_POINT('Ctrl Pts',(1.41304763236518,-2.89652000020959,18.8389423402925));
#16300=CARTESIAN_POINT('Ctrl Pts',(1.45372256568881,-2.87635804568532,18.8417780579109));
#16301=CARTESIAN_POINT('Ctrl Pts',(1.47603273893388,-2.864973333465,18.8433516816669));
#16302=CARTESIAN_POINT('Ctrl Pts',(1.54471926499953,-2.82890787114527,18.8482539967374));
#16303=CARTESIAN_POINT('Ctrl Pts',(1.5906246673697,-2.8033533505077,18.8516128199475));
#16304=CARTESIAN_POINT('Ctrl Pts',(1.76993406431116,-2.69771345288985,18.8650655338483));
#16305=CARTESIAN_POINT('Ctrl Pts',(1.89807506545773,-2.60914267118674,18.8754406178092));
#16306=CARTESIAN_POINT('Ctrl Pts',(2.19757436559864,-2.36835486473635,18.9013832556073));
#16307=CARTESIAN_POINT('Ctrl Pts',(2.36008820460303,-2.20645334753572,18.9170503024327));
#16308=CARTESIAN_POINT('Ctrl Pts',(2.51910484713755,-2.01017331778175,18.9332152231008));
#16309=CARTESIAN_POINT('Ctrl Pts',(2.53390764186923,-1.99148139324945,18.9347287371475));
#16310=CARTESIAN_POINT('Ctrl Pts',(2.55398018834381,-1.9655489963369,18.9367912321941));
#16311=CARTESIAN_POINT('Ctrl Pts',(2.55942881391245,-1.95844882764018,18.9373521463012));
#16312=CARTESIAN_POINT('Ctrl Pts',(2.56806622478967,-1.94709570397389,18.9382429020261));
#16313=CARTESIAN_POINT('Ctrl Pts',(2.57127413946588,-1.94285746158336,18.9385740757507));
#16314=CARTESIAN_POINT('Ctrl Pts',(2.57790233280137,-1.93405523512263,18.9392590387867));
#16315=CARTESIAN_POINT('Ctrl Pts',(2.58132098781501,-1.92949010059257,18.9396127059518));
#16316=CARTESIAN_POINT('Ctrl Pts',(2.58948315772167,-1.91853014885856,18.9404580723942));
#16317=CARTESIAN_POINT('Ctrl Pts',(2.5942151680183,-1.91212672733993,18.9409489683024));
#16318=CARTESIAN_POINT('Ctrl Pts',(2.61030816014087,-1.89017976378948,18.9426214271854));
#16319=CARTESIAN_POINT('Ctrl Pts',(2.62155382595271,-1.87455162896909,18.9437952552479));
#16320=CARTESIAN_POINT('Ctrl Pts',(2.68468333444436,-1.78514104273174,18.9504200944338));
#16321=CARTESIAN_POINT('Ctrl Pts',(2.73359640057202,-1.70930012724519,18.9556916366246));
#16322=CARTESIAN_POINT('Ctrl Pts',(2.90189607001275,-1.42260096633018,18.9747551100313));
#16323=CARTESIAN_POINT('Ctrl Pts',(3.00058569078484,-1.20053787915899,18.9879287755434));
#16324=CARTESIAN_POINT('Ctrl Pts',(3.09252404420871,-0.909080226280977,
19.0053563879611));
#16325=CARTESIAN_POINT('Ctrl Pts',(3.10979736006618,-0.848110596943444,
19.009005038856));
#16326=CARTESIAN_POINT('Ctrl Pts',(3.14340939593379,-0.714578214367164,
19.0170438762466));
#16327=CARTESIAN_POINT('Ctrl Pts',(3.15905556683538,-0.641881058450411,
19.0214506154029));
#16328=CARTESIAN_POINT('Ctrl Pts',(3.17562244515314,-0.549473968270774,
19.0271181295656));
#16329=CARTESIAN_POINT('Ctrl Pts',(3.1788963119542,-0.530205401495658,19.0283034490697));
#16330=CARTESIAN_POINT('Ctrl Pts',(3.18381564484577,-0.499567256271762,
19.0301942563104));
#16331=CARTESIAN_POINT('Ctrl Pts',(3.18557596675757,-0.488216405429767,
19.0308960844592));
#16332=CARTESIAN_POINT('Ctrl Pts',(3.18860115029231,-0.467996289951824,
19.0321487444159));
#16333=CARTESIAN_POINT('Ctrl Pts',(3.18988978738244,-0.459130662040544,
19.0326988140614));
#16334=CARTESIAN_POINT('Ctrl Pts',(3.19246118852457,-0.440906286102035,
19.0338313070568));
#16335=CARTESIAN_POINT('Ctrl Pts',(3.19373980388004,-0.431547048913755,
19.0344138564375));
#16336=CARTESIAN_POINT('Ctrl Pts',(3.19648766264385,-0.410751899432377,
19.035710377853));
#16337=CARTESIAN_POINT('Ctrl Pts',(3.19793671442684,-0.399313492478713,
19.0364249826057));
#16338=CARTESIAN_POINT('Ctrl Pts',(3.20138806936181,-0.370845010632214,
19.0382072294497));
#16339=CARTESIAN_POINT('Ctrl Pts',(3.20331587446157,-0.353806419702777,
19.0392772088441));
#16340=CARTESIAN_POINT('Ctrl Pts',(3.21694690436431,-0.224070826567322,
19.0474500812389));
#16341=CARTESIAN_POINT('Ctrl Pts',(3.2228341227182,-0.110857004473895,19.0547344658747));
#16342=CARTESIAN_POINT('Ctrl Pts',(3.22274909203151,0.00241915483385854,
19.0621741053498));
#16343=CARTESIAN_POINT('Ctrl Pts',(3.22274909510165,0.00241506138934033,
19.0621738365046));
#16344=CARTESIAN_POINT('Ctrl Pts',(3.22257571361233,0.233781866502874,19.0773693093119));
#16345=CARTESIAN_POINT('Ctrl Pts',(3.19748646516631,0.464455112312948,19.0932022669885));
#16346=CARTESIAN_POINT('Ctrl Pts',(3.12345943544361,0.801971971738992,19.1164103917512));
#16347=CARTESIAN_POINT('Ctrl Pts',(3.09308090398364,0.912147907119489,19.1239794830628));
#16348=CARTESIAN_POINT('Ctrl Pts',(3.05002227525443,1.04113175163933,19.1326611875246));
#16349=CARTESIAN_POINT('Ctrl Pts',(3.04292174037639,1.06170548949412,19.1340403176688));
#16350=CARTESIAN_POINT('Ctrl Pts',(3.03280502634267,1.09008309910926,19.1359331767385));
#16351=CARTESIAN_POINT('Ctrl Pts',(3.02996625960551,1.09794897883596,19.1364568455494));
#16352=CARTESIAN_POINT('Ctrl Pts',(3.02511371521723,1.11123263876078,19.1373393908265));
#16353=CARTESIAN_POINT('Ctrl Pts',(3.02311593428994,1.11665617671798,19.1376992097038));
#16354=CARTESIAN_POINT('Ctrl Pts',(3.01928372423851,1.12697412315389,19.1383827268384));
#16355=CARTESIAN_POINT('Ctrl Pts',(3.01745196880854,1.1318694706423,19.1387065867933));
#16356=CARTESIAN_POINT('Ctrl Pts',(3.01261503131926,1.14470094247849,19.1395543871147));
#16357=CARTESIAN_POINT('Ctrl Pts',(3.00959037505906,1.15262975530922,19.14007716581));
#16358=CARTESIAN_POINT('Ctrl Pts',(2.99898192020575,1.18011222217206,19.1418857002611));
#16359=CARTESIAN_POINT('Ctrl Pts',(2.99123840527567,1.19960421419486,19.1431622471303));
#16360=CARTESIAN_POINT('Ctrl Pts',(2.88715549902908,1.45432611834879,19.1597805028388));
#16361=CARTESIAN_POINT('Ctrl Pts',(2.76348893439609,1.677468820385,19.1736720097659));
#16362=CARTESIAN_POINT('Ctrl Pts',(2.54248959412162,1.98423612103214,19.1948604344727));
#16363=CARTESIAN_POINT('Ctrl Pts',(2.46439515289904,2.08043257470821,19.2018560436664));
#16364=CARTESIAN_POINT('Ctrl Pts',(2.34155844371033,2.21509385933022,19.2124327210213));
#16365=CARTESIAN_POINT('Ctrl Pts',(2.30098485551773,2.25721174392057,19.2158647779638));
#16366=CARTESIAN_POINT('Ctrl Pts',(2.24000443729592,2.31715969222176,19.2209535899304));
#16367=CARTESIAN_POINT('Ctrl Pts',(2.22048174427643,2.33587449917993,19.2225728256336));
#16368=CARTESIAN_POINT('Ctrl Pts',(2.18494913950105,2.36908869248058,19.2255040093059));
#16369=CARTESIAN_POINT('Ctrl Pts',(2.16902447605159,2.38367715145035,19.2268120926198));
#16370=CARTESIAN_POINT('Ctrl Pts',(2.14418234442706,2.40597976196341,19.2288447498348));
#16371=CARTESIAN_POINT('Ctrl Pts',(2.13536695048044,2.41380705983496,19.2295645366471));
#16372=CARTESIAN_POINT('Ctrl Pts',(2.12642692555814,2.42165771831261,19.2302930365842));
#16373=CARTESIAN_POINT('Ctrl Pts',(2.12634494758734,2.4217296996716,19.2302997166374));
#16374=CARTESIAN_POINT('Ctrl Pts',(2.12617967318954,2.42187480520795,19.2303131839302));
#16375=CARTESIAN_POINT('Ctrl Pts',(2.12609637664471,2.42194792925109,19.2303199711756));
#16376=CARTESIAN_POINT('Ctrl Pts',(2.12592842233624,2.42209535697728,19.2303336563253));
#16377=CARTESIAN_POINT('Ctrl Pts',(2.12584376443013,2.42216966053609,19.2303405542372));
#16378=CARTESIAN_POINT('Ctrl Pts',(2.12567304284607,2.42231948564346,19.2303544643375));
#16379=CARTESIAN_POINT('Ctrl Pts',(2.12558697905882,2.42239500702632,19.2303614765305));
#16380=CARTESIAN_POINT('Ctrl Pts',(2.12541339949649,2.42254730754527,19.2303756189457));
#16381=CARTESIAN_POINT('Ctrl Pts',(2.12532588357581,2.42262408653442,19.230382749175));
#16382=CARTESIAN_POINT('Ctrl Pts',(2.12514935159806,2.42277894367654,19.2303971315718));
#16383=CARTESIAN_POINT('Ctrl Pts',(2.12506033540586,2.4228570216595,19.2304043837455));
#16384=CARTESIAN_POINT('Ctrl Pts',(2.12491014938738,2.42298873834555,19.2304166191967));
#16385=CARTESIAN_POINT('Ctrl Pts',(2.12484898181302,2.42304237965559,19.2304216023674));
#16386=CARTESIAN_POINT('Ctrl Pts',(2.12472164845756,2.4231540369567,19.2304319757578));
#16387=CARTESIAN_POINT('Ctrl Pts',(2.12465548235526,2.42321205253306,19.230437365992));
#16388=CARTESIAN_POINT('Ctrl Pts',(2.12451769323387,2.42333285842221,19.2304485908422));
#16389=CARTESIAN_POINT('Ctrl Pts',(2.12444606980804,2.42339564826911,19.2304544254776));
#16390=CARTESIAN_POINT('Ctrl Pts',(2.12429685715508,2.42352644628159,19.2304665805429));
#16391=CARTESIAN_POINT('Ctrl Pts',(2.12421926744352,2.42359445389836,19.2304729009961));
#16392=CARTESIAN_POINT('Ctrl Pts',(2.12405755639071,2.4237361803939,19.2304860737391));
#16393=CARTESIAN_POINT('Ctrl Pts',(2.12397343448553,2.42380989861222,19.2304929260556));
#16394=CARTESIAN_POINT('Ctrl Pts',(2.12379802851159,2.42396359529586,19.2305072138272));
#16395=CARTESIAN_POINT('Ctrl Pts',(2.12370674374051,2.42404357300368,19.2305146493166));
#16396=CARTESIAN_POINT('Ctrl Pts',(2.12351630738218,2.42421040179192,19.2305301607597));
#16397=CARTESIAN_POINT('Ctrl Pts',(2.12341715501037,2.42429725192308,19.2305382367501));
#16398=CARTESIAN_POINT('Ctrl Pts',(2.12321019414125,2.42447851187231,19.2305550934004));
#16399=CARTESIAN_POINT('Ctrl Pts',(2.12310238466953,2.42457292058755,19.230563874107));
#16400=CARTESIAN_POINT('Ctrl Pts',(2.12287722273016,2.42477006828284,19.2305822123214));
#16401=CARTESIAN_POINT('Ctrl Pts',(2.12275986911201,2.42487280592497,19.2305917698838));
#16402=CARTESIAN_POINT('Ctrl Pts',(2.12251461956958,2.42508747906139,19.2306117430751));
#16403=CARTESIAN_POINT('Ctrl Pts',(2.12238672223894,2.42519941296603,19.2306221587716));
#16404=CARTESIAN_POINT('Ctrl Pts',(2.12211925381301,2.42543346012375,19.2306439402293));
#16405=CARTESIAN_POINT('Ctrl Pts',(2.12197968102787,2.42555557144983,19.2306553060716));
#16406=CARTESIAN_POINT('Ctrl Pts',(2.12168759008914,2.42581107541734,19.230679091196));
#16407=CARTESIAN_POINT('Ctrl Pts',(2.12153506450358,2.42594447043604,19.2306915110146));
#16408=CARTESIAN_POINT('Ctrl Pts',(2.12121560090079,2.42622381205055,19.2307175233392));
#16409=CARTESIAN_POINT('Ctrl Pts',(2.12104866203641,2.42636975437433,19.2307311158305));
#16410=CARTESIAN_POINT('Ctrl Pts',(2.12075350799421,2.42662773202234,19.2307551469606));
#16411=CARTESIAN_POINT('Ctrl Pts',(2.12062530156263,2.42673977217675,19.2307655850946));
#16412=CARTESIAN_POINT('Ctrl Pts',(2.1202954851253,2.42702795408887,19.2307924368673));
#16413=CARTESIAN_POINT('Ctrl Pts',(2.12009386477938,2.42720407850242,19.2308088509091));
#16414=CARTESIAN_POINT('Ctrl Pts',(2.11957162365641,2.42766016482273,19.230851364989));
#16415=CARTESIAN_POINT('Ctrl Pts',(2.11925097118889,2.4279400867375,19.2308774664831));
#16416=CARTESIAN_POINT('Ctrl Pts',(2.11133468747185,2.43484804958631,19.2315218156038));
#16417=CARTESIAN_POINT('Ctrl Pts',(2.10370812179963,2.44144041944195,19.2321415419821));
#16418=CARTESIAN_POINT('Ctrl Pts',(2.08609652225864,2.45652001720474,19.2335703292408));
#16419=CARTESIAN_POINT('Ctrl Pts',(2.07609045106348,2.46498229729061,19.2343804063808));
#16420=CARTESIAN_POINT('Ctrl Pts',(2.04919159886154,2.48745108432295,19.2365537609265));
#16421=CARTESIAN_POINT('Ctrl Pts',(2.03220713606083,2.50134628218794,19.2379215386953));
#16422=CARTESIAN_POINT('Ctrl Pts',(1.88738910441523,2.61737512304025,19.2495479094667));
#16423=CARTESIAN_POINT('Ctrl Pts',(1.75211009938113,2.70979440964908,19.2601925364903));
#16424=CARTESIAN_POINT('Ctrl Pts',(1.39079336838108,2.91823572082224,19.2880124635982));
#16425=CARTESIAN_POINT('Ctrl Pts',(1.15699553393417,3.01856958470996,19.3055130634214));
#16426=CARTESIAN_POINT('Ctrl Pts',(0.859310904607945,3.10659592343055,19.3258274673674));
#16427=CARTESIAN_POINT('Ctrl Pts',(0.804339278287263,3.12128062342996,19.329496753474));
#16428=CARTESIAN_POINT('Ctrl Pts',(0.737619803548651,3.13722354726431,19.3338288298399));
#16429=CARTESIAN_POINT('Ctrl Pts',(0.72622076435119,3.139881840363,19.334564729004));
#16430=CARTESIAN_POINT('Ctrl Pts',(0.708457302187487,3.14392242622939,19.335704644825));
#16431=CARTESIAN_POINT('Ctrl Pts',(0.702102883003066,3.1453475983794,19.3361110580181));
#16432=CARTESIAN_POINT('Ctrl Pts',(0.690295429859775,3.14795821470906,19.3368636499795));
#16433=CARTESIAN_POINT('Ctrl Pts',(0.684843688567357,3.1491487460892,19.3372101095524));
#16434=CARTESIAN_POINT('Ctrl Pts',(0.672483946041851,3.15181420747561,19.337993270266));
#16435=CARTESIAN_POINT('Ctrl Pts',(0.665574188270009,3.1532805866719,19.3384294772263));
#16436=CARTESIAN_POINT('Ctrl Pts',(0.645076709243011,3.15756015597896,19.3397188111984));
#16437=CARTESIAN_POINT('Ctrl Pts',(0.631475373786384,3.16030836593499,19.3405683095803));
#16438=CARTESIAN_POINT('Ctrl Pts',(0.52903137793221,3.18031984489479,19.3469240674594));
#16439=CARTESIAN_POINT('Ctrl Pts',(0.439505752586364,3.19392336490035,19.3522381804442));
#16440=CARTESIAN_POINT('Ctrl Pts',(0.106249106673691,3.23028059638407,19.3715259399356));
#16441=CARTESIAN_POINT('Ctrl Pts',(-0.139258832592949,3.22902807506504,
19.3848234414536));
#16442=CARTESIAN_POINT('Ctrl Pts',(-0.473337921352233,3.18911904278954,
19.4039799646665));
#16443=CARTESIAN_POINT('Ctrl Pts',(-0.563892696915195,3.17435854375601,
19.4092742090918));
#16444=CARTESIAN_POINT('Ctrl Pts',(-0.708528007674001,3.14439848719691,
19.417984395934));
#16445=CARTESIAN_POINT('Ctrl Pts',(-0.763057725260847,3.13161238315833,
19.4213272160721));
#16446=CARTESIAN_POINT('Ctrl Pts',(-0.833825371675357,3.11306076831362,
19.4257543261987));
#16447=CARTESIAN_POINT('Ctrl Pts',(-0.850391164562575,3.10857635376277,
19.4267970655948));
#16448=CARTESIAN_POINT('Ctrl Pts',(-0.877366355964989,3.10104232096191,
19.4285058278988));
#16449=CARTESIAN_POINT('Ctrl Pts',(-0.887797710056435,3.09807204894377,
19.4291692578335));
#16450=CARTESIAN_POINT('Ctrl Pts',(-0.907894141976137,3.09223986640998,
19.4304525836808));
#16451=CARTESIAN_POINT('Ctrl Pts',(-0.917561189606142,3.08938515308372,
19.4310722374624));
#16452=CARTESIAN_POINT('Ctrl Pts',(-0.939758340571584,3.08271688113162,
19.432500506646));
#16453=CARTESIAN_POINT('Ctrl Pts',(-0.952278841997937,3.07887221346227,
19.433310135907));
#16454=CARTESIAN_POINT('Ctrl Pts',(-0.985689749266093,3.06838943896977,
19.4354815077615));
#16455=CARTESIAN_POINT('Ctrl Pts',(-1.00653616406198,3.0616144340987,19.4368477378353));
#16456=CARTESIAN_POINT('Ctrl Pts',(-1.18263861392223,3.00238886084082,19.4484881738583));
#16457=CARTESIAN_POINT('Ctrl Pts',(-1.33373061961618,2.93838746724878,19.4591496921086));
#16458=CARTESIAN_POINT('Ctrl Pts',(-1.70491113282351,2.74661474782247,19.4870153917478));
#16459=CARTESIAN_POINT('Ctrl Pts',(-1.915957641142,2.60378878879702,19.5045455434699));
#16460=CARTESIAN_POINT('Ctrl Pts',(-2.15065158148517,2.40083068483367,19.5248439959419));
#16461=CARTESIAN_POINT('Ctrl Pts',(-2.1922864089605,2.36287355148469,19.5284763657729));
#16462=CARTESIAN_POINT('Ctrl Pts',(-2.2413233330016,2.31575549072658,19.5327708339352));
#16463=CARTESIAN_POINT('Ctrl Pts',(-2.24969518935308,2.30762330997188,19.5335045990551));
#16464=CARTESIAN_POINT('Ctrl Pts',(-2.26266409403743,2.29488803072314,19.5346419342408));
#16465=CARTESIAN_POINT('Ctrl Pts',(-2.26729159466737,2.29031628875332,19.5350478837161));
#16466=CARTESIAN_POINT('Ctrl Pts',(-2.27586361075188,2.28179612054045,19.5358000558898));
#16467=CARTESIAN_POINT('Ctrl Pts',(-2.27981167394376,2.27785149703018,19.5361465566314));
#16468=CARTESIAN_POINT('Ctrl Pts',(-2.28874047043527,2.26888401115437,19.5369303688514));
#16469=CARTESIAN_POINT('Ctrl Pts',(-2.2937149142901,2.26385500668586,19.5373671826831));
#16470=CARTESIAN_POINT('Ctrl Pts',(-2.30843101844807,2.24887919444394,19.5386599761996));
#16471=CARTESIAN_POINT('Ctrl Pts',(-2.31812497260019,2.23888544275162,19.5395122982776));
#16472=CARTESIAN_POINT('Ctrl Pts',(-2.39129210720271,2.16247083377905,19.5459538318366));
#16473=CARTESIAN_POINT('Ctrl Pts',(-2.45197011327385,2.09341921234325,19.5513449833047));
#16474=CARTESIAN_POINT('Ctrl Pts',(-2.66205968332149,1.83264728213634,19.5705991427137));
#16475=CARTESIAN_POINT('Ctrl Pts',(-2.79261739876554,1.62679408855662,19.5838080707924));
#16476=CARTESIAN_POINT('Ctrl Pts',(-2.93895816844397,1.3255518241652,19.6028748324302));
#16477=CARTESIAN_POINT('Ctrl Pts',(-2.97555715281676,1.24121732841146,19.6081792234531));
#16478=CARTESIAN_POINT('Ctrl Pts',(-3.02860796877706,1.10308500903541,19.616904578623));
#16479=CARTESIAN_POINT('Ctrl Pts',(-3.04734384197765,1.0502179290835,19.6202520865171));
#16480=CARTESIAN_POINT('Ctrl Pts',(-3.07000154359415,0.980562554144265,
19.6246845406797));
#16481=CARTESIAN_POINT('Ctrl Pts',(-3.0751823230422,0.964191922056175,19.6257278088227));
#16482=CARTESIAN_POINT('Ctrl Pts',(-3.08342224532108,0.937412661608031,
19.6274372198243));
#16483=CARTESIAN_POINT('Ctrl Pts',(-3.08656013262519,0.927028470017138,
19.6281007659076));
#16484=CARTESIAN_POINT('Ctrl Pts',(-3.09251223786166,0.906965935963204,
19.6293841634253));
#16485=CARTESIAN_POINT('Ctrl Pts',(-3.09533360127239,0.897289832480227,
19.630003771906));
#16486=CARTESIAN_POINT('Ctrl Pts',(-3.1017155579208,0.875014050540049,19.6314317172765));
#16487=CARTESIAN_POINT('Ctrl Pts',(-3.10524483249448,0.862405654564231,
19.6322410665247));
#16488=CARTESIAN_POINT('Ctrl Pts',(-3.11447286694119,0.828647163133197,
19.6344111991212));
#16489=CARTESIAN_POINT('Ctrl Pts',(-3.1200329143053,0.807460175655846,19.6357764619065));
#16490=CARTESIAN_POINT('Ctrl Pts',(-3.16536230969041,0.627266740960554,
19.6474175383769));
#16491=CARTESIAN_POINT('Ctrl Pts',(-3.19315789070699,0.465521324437458,
19.6580808194204));
#16492=CARTESIAN_POINT('Ctrl Pts',(-3.23236142276593,0.0495422632228797,
19.685948416339));
#16493=CARTESIAN_POINT('Ctrl Pts',(-3.22622005801688,-0.205217290080257,
19.7034786047808));
#16494=CARTESIAN_POINT('Ctrl Pts',(-3.18225876866391,-0.512366327591324,
19.7237770376986));
#16495=CARTESIAN_POINT('Ctrl Pts',(-3.17281742835111,-0.567908978396284,
19.7274093619145));
#16496=CARTESIAN_POINT('Ctrl Pts',(-3.15966744969356,-0.634630114524239,
19.7317037835819));
#16497=CARTESIAN_POINT('Ctrl Pts',(-3.15734841410374,-0.646068708967421,
19.7324375460487));
#16498=CARTESIAN_POINT('Ctrl Pts',(-3.15364014572805,-0.663862717085865,
19.7335748780255));
#16499=CARTESIAN_POINT('Ctrl Pts',(-3.15229375207197,-0.670226811092926,
19.7339808269241));
#16500=CARTESIAN_POINT('Ctrl Pts',(-3.14975639720097,-0.682043509433465,
19.7347329985767));
#16501=CARTESIAN_POINT('Ctrl Pts',(-3.14857055271795,-0.687497044168862,
19.7350794993705));
#16502=CARTESIAN_POINT('Ctrl Pts',(-3.14584958693042,-0.699855680598632,
19.7358633124055));
#16503=CARTESIAN_POINT('Ctrl Pts',(-3.14430589884105,-0.706758808946262,
19.7363001269957));
#16504=CARTESIAN_POINT('Ctrl Pts',(-3.13965642136871,-0.727233769513876,
19.7375929248387));
#16505=CARTESIAN_POINT('Ctrl Pts',(-3.13648535284086,-0.740790825672001,
19.7384452504484));
#16506=CARTESIAN_POINT('Ctrl Pts',(-3.11172217067486,-0.843648920727268,
19.7448868931244));
#16507=CARTESIAN_POINT('Ctrl Pts',(-3.08640591243335,-0.932019473435434,
19.7502781425933));
#16508=CARTESIAN_POINT('Ctrl Pts',(-2.9805025239281,-1.24970455136136,19.7695322608739));
#16509=CARTESIAN_POINT('Ctrl Pts',(-2.87783637579601,-1.47079151425014,
19.7827410774952));
#16510=CARTESIAN_POINT('Ctrl Pts',(-2.70343455100568,-1.75670271328719,
19.8018077256279));
#16511=CARTESIAN_POINT('Ctrl Pts',(-2.65224805277895,-1.83306877464473,
19.8071121286915));
#16512=CARTESIAN_POINT('Ctrl Pts',(-2.56468345938699,-1.95234769687855,
19.8158375018593));
#16513=CARTESIAN_POINT('Ctrl Pts',(-2.53032271894615,-1.99667952822963,
19.8191850153139));
#16514=CARTESIAN_POINT('Ctrl Pts',(-2.48395474598055,-2.05338287236936,
19.8236174758151));
#16515=CARTESIAN_POINT('Ctrl Pts',(-2.4729792275753,-2.06658803897859,19.8246607445848));
#16516=CARTESIAN_POINT('Ctrl Pts',(-2.4548984534088,-2.08799157675144,19.8263701563554));
#16517=CARTESIAN_POINT('Ctrl Pts',(-2.44785630927522,-2.09624300254644,
19.8270337025763));
#16518=CARTESIAN_POINT('Ctrl Pts',(-2.43419105997023,-2.11209209881246,
19.8283171001792));
#16519=CARTESIAN_POINT('Ctrl Pts',(-2.42757369983697,-2.11969457197999,
19.8289367086063));
#16520=CARTESIAN_POINT('Ctrl Pts',(-2.41227840547815,-2.13710128099154,
19.8303646535934));
#16521=CARTESIAN_POINT('Ctrl Pts',(-2.40357621304076,-2.14688387453169,
19.8311740025101));
#16522=CARTESIAN_POINT('Ctrl Pts',(-2.38015677030373,-2.17289003584273,
19.8333441336393));
#16523=CARTESIAN_POINT('Ctrl Pts',(-2.36533352474845,-2.18901681983613,
19.8347093952794));
#16524=CARTESIAN_POINT('Ctrl Pts',(-2.23820550853008,-2.32452531060372,
19.8463504135067));
#16525=CARTESIAN_POINT('Ctrl Pts',(-2.11712615437145,-2.43531188296846,
19.8570136329685));
#16526=CARTESIAN_POINT('Ctrl Pts',(-1.82787122541351,-2.66204535638539,
19.8815266994009));
#16527=CARTESIAN_POINT('Ctrl Pts',(-1.65612355608179,-2.77213957406373,
19.8954708340483));
#16528=CARTESIAN_POINT('Ctrl Pts',(-1.47525540330811,-2.86526422123863,
19.9090518554891));
#16529=CARTESIAN_POINT('Origin',(0.,0.,4.68922655072688));
#16530=CARTESIAN_POINT('',(-1.47286814312172,-2.86060451358776,21.4037167033623));
#16531=CARTESIAN_POINT('',(-1.47525512068018,-2.86526436675691,21.1585511949183));
#16532=CARTESIAN_POINT('',(-1.47525540501186,-2.86526422036142,4.68922655072688));
#16533=CARTESIAN_POINT('',(3.22288743813532,-0.00297411405783051,20.5607735307834));
#16534=CARTESIAN_POINT('Ctrl Pts',(3.22288743813532,-0.00297411405783051,
20.5607735307834));
#16535=CARTESIAN_POINT('Ctrl Pts',(3.21520567054372,0.825027405902577,20.6119075522263));
#16536=CARTESIAN_POINT('Ctrl Pts',(2.46751291112442,2.73910351537692,20.7293525531237));
#16537=CARTESIAN_POINT('Ctrl Pts',(-0.758236137317192,3.73602587213299,
20.9131085334756));
#16538=CARTESIAN_POINT('Ctrl Pts',(-3.55335956546679,1.38074152385103,21.112041471839));
#16539=CARTESIAN_POINT('Ctrl Pts',(-3.16575851074329,-1.59892501153937,
21.275577528468));
#16540=CARTESIAN_POINT('Ctrl Pts',(-1.92022651981776,-2.63131100466499,
21.3728026056424));
#16541=CARTESIAN_POINT('Ctrl Pts',(-1.47286814312172,-2.86060451358776,
21.4037167033623));
#16542=CARTESIAN_POINT('Ctrl Pts',(3.22274863154765,-0.00296990870983751,
20.5606936678279));
#16543=CARTESIAN_POINT('Ctrl Pts',(3.22255702526824,-0.210888378631545,
20.5466283729016));
#16544=CARTESIAN_POINT('Ctrl Pts',(3.20224496926727,-0.418325185966235,
20.5324657971094));
#16545=CARTESIAN_POINT('Ctrl Pts',(3.15908206884142,-0.637620041575319,
20.518181388141));
#16546=CARTESIAN_POINT('Ctrl Pts',(3.1559721229632,-0.652839042730332,20.5171938674373));
#16547=CARTESIAN_POINT('Ctrl Pts',(3.15091550430859,-0.676703448685813,
20.5156519965644));
#16548=CARTESIAN_POINT('Ctrl Pts',(3.14904304839768,-0.685364104943512,
20.5150938098942));
#16549=CARTESIAN_POINT('Ctrl Pts',(3.1454329574484,-0.701734658377767,20.5140414607767));
#16550=CARTESIAN_POINT('Ctrl Pts',(3.14370263853446,-0.70944608264459,20.5135469029785));
#16551=CARTESIAN_POINT('Ctrl Pts',(3.14067682238565,-0.722702625013594,
20.5126988029036));
#16552=CARTESIAN_POINT('Ctrl Pts',(3.13939496920804,-0.72825079208872,20.5123444837374));
#16553=CARTESIAN_POINT('Ctrl Pts',(3.13688399774121,-0.738989034692541,
20.5116599683094));
#16554=CARTESIAN_POINT('Ctrl Pts',(3.13565670042801,-0.744179458682553,
20.5113296656626));
#16555=CARTESIAN_POINT('Ctrl Pts',(3.13231537774037,-0.758155386377132,
20.5104417418585));
#16556=CARTESIAN_POINT('Ctrl Pts',(3.13017725927639,-0.76693516390364,20.5098854995544));
#16557=CARTESIAN_POINT('Ctrl Pts',(3.12212946917851,-0.799387544907498,
20.5078348572979));
#16558=CARTESIAN_POINT('Ctrl Pts',(3.11598777851726,-0.823002500528097,
20.5063532493039));
#16559=CARTESIAN_POINT('Ctrl Pts',(3.06178724070192,-1.02209477404303,20.4939344040308));
#16560=CARTESIAN_POINT('Ctrl Pts',(2.99920953173441,-1.19330578281535,20.4837203162587));
#16561=CARTESIAN_POINT('Ctrl Pts',(2.87583190712063,-1.4587566095342,20.4673516209356));
#16562=CARTESIAN_POINT('Ctrl Pts',(2.82401428160712,-1.55670251602427,20.4611867627293));
#16563=CARTESIAN_POINT('Ctrl Pts',(2.69206053692797,-1.77776652101174,20.4466380028718));
#16564=CARTESIAN_POINT('Ctrl Pts',(2.60835517109728,-1.89845190222038,20.4381960080741));
#16565=CARTESIAN_POINT('Ctrl Pts',(2.49540547378774,-2.03966524559805,20.4273968919483));
#16566=CARTESIAN_POINT('Ctrl Pts',(2.47366209540388,-2.0659812427616,20.4253423585494));
#16567=CARTESIAN_POINT('Ctrl Pts',(2.44430161146891,-2.10038814427956,20.4225973701187));
#16568=CARTESIAN_POINT('Ctrl Pts',(2.4370543160944,-2.10879277788329,20.4219220975046));
#16569=CARTESIAN_POINT('Ctrl Pts',(2.422633370982,-2.12534301273849,20.4205828268747));
#16570=CARTESIAN_POINT('Ctrl Pts',(2.4154616919937,-2.13349014104704,20.4199189156074));
#16571=CARTESIAN_POINT('Ctrl Pts',(2.40154942518816,-2.14913460820212,20.4186349848711));
#16572=CARTESIAN_POINT('Ctrl Pts',(2.39481453444172,-2.15663686042271,20.4180152094677));
#16573=CARTESIAN_POINT('Ctrl Pts',(2.37925279366811,-2.17380889753686,20.4165871262543));
#16574=CARTESIAN_POINT('Ctrl Pts',(2.37040204296757,-2.18345669197984,20.4157778070735));
#16575=CARTESIAN_POINT('Ctrl Pts',(2.3465936800498,-2.2090937154951,20.4136082990189));
#16576=CARTESIAN_POINT('Ctrl Pts',(2.33153170497183,-2.22498467715795,20.412243636602));
#16577=CARTESIAN_POINT('Ctrl Pts',(2.20285382459719,-2.35800338760957,20.4006486714134));
#16578=CARTESIAN_POINT('Ctrl Pts',(2.08067272930059,-2.46648158922455,20.390034475905));
#16579=CARTESIAN_POINT('Ctrl Pts',(1.81292074882527,-2.67010310770066,20.3676030363587));
#16580=CARTESIAN_POINT('Ctrl Pts',(1.66679074097349,-2.76368164665189,20.355786790884));
#16581=CARTESIAN_POINT('Ctrl Pts',(1.43228552428668,-2.88846221882935,20.3379143046628));
#16582=CARTESIAN_POINT('Ctrl Pts',(1.34887693653242,-2.92834240706479,20.3317553119291));
#16583=CARTESIAN_POINT('Ctrl Pts',(1.22128111550323,-2.98273916011704,20.3227342276422));
#16584=CARTESIAN_POINT('Ctrl Pts',(1.17830904076372,-2.9999747988446,20.3197620595982));
#16585=CARTESIAN_POINT('Ctrl Pts',(1.12472705459159,-3.02013684708874,20.3161498424875));
#16586=CARTESIAN_POINT('Ctrl Pts',(1.11445635505942,-3.02394189152159,20.3154616579489));
#16587=CARTESIAN_POINT('Ctrl Pts',(1.09815557219796,-3.02988660438592,20.3143763167279));
#16588=CARTESIAN_POINT('Ctrl Pts',(1.09213828426504,-3.03206076224097,20.3139771533421));
#16589=CARTESIAN_POINT('Ctrl Pts',(1.08084422142813,-3.03610353353027,20.3132307762371));
#16590=CARTESIAN_POINT('Ctrl Pts',(1.0755691143866,-3.03797629649145,20.3128833260842));
#16591=CARTESIAN_POINT('Ctrl Pts',(1.06346238302641,-3.04223892925854,20.3120885295093));
#16592=CARTESIAN_POINT('Ctrl Pts',(1.05662757989833,-3.04461953331037,20.3116417370742));
#16593=CARTESIAN_POINT('Ctrl Pts',(1.03866701523993,-3.05080754388606,20.3104725065262));
#16594=CARTESIAN_POINT('Ctrl Pts',(1.02752821529575,-3.05457715812865,20.3097522491478));
#16595=CARTESIAN_POINT('Ctrl Pts',(0.951480412198136,-3.07985034135917,
20.3048664235266));
#16596=CARTESIAN_POINT('Ctrl Pts',(0.885916736396182,-3.09934608524292,
20.3008104733203));
#16597=CARTESIAN_POINT('Ctrl Pts',(0.792185486093892,-3.12399963083853,
20.2951666747592));
#16598=CARTESIAN_POINT('Ctrl Pts',(0.764497875989363,-3.1308903865538,20.2935183760302));
#16599=CARTESIAN_POINT('Ctrl Pts',(0.486427029054515,-3.19618649732061,
20.2771200303123));
#16600=CARTESIAN_POINT('Ctrl Pts',(0.229993707192357,-3.22480013484399,
20.2631807265878));
#16601=CARTESIAN_POINT('Ctrl Pts',(-0.107817291833416,-3.22195662129813,
20.2438394675536));
#16602=CARTESIAN_POINT('Ctrl Pts',(-0.188449265195834,-3.21824711955131,
20.2391571262057));
#16603=CARTESIAN_POINT('Ctrl Pts',(-0.319515712341894,-3.20727484932672,
20.2313799938083));
#16604=CARTESIAN_POINT('Ctrl Pts',(-0.370068567194212,-3.20183557855471,
20.2283400132662));
#16605=CARTESIAN_POINT('Ctrl Pts',(-0.436521147958708,-3.19309081671208,
20.2242822137591));
#16606=CARTESIAN_POINT('Ctrl Pts',(-0.452556315503421,-3.19085763436655,
20.2232983124319));
#16607=CARTESIAN_POINT('Ctrl Pts',(-0.479310679560346,-3.18692588653344,
20.2216484882992));
#16608=CARTESIAN_POINT('Ctrl Pts',(-0.490039463727698,-3.18529380956157,
20.2209846823272));
#16609=CARTESIAN_POINT('Ctrl Pts',(-0.510719701399489,-3.18204094963412,
20.2197008167466));
#16610=CARTESIAN_POINT('Ctrl Pts',(-0.520672207161982,-3.18042759193602,
20.2190810004579));
#16611=CARTESIAN_POINT('Ctrl Pts',(-0.543534810750672,-3.17661124383535,
20.217652624557));
#16612=CARTESIAN_POINT('Ctrl Pts',(-0.556439312019799,-3.17437621728409,
20.2168430522169));
#16613=CARTESIAN_POINT('Ctrl Pts',(-0.590893704973165,-3.16819225723482,
20.2146724239986));
#16614=CARTESIAN_POINT('Ctrl Pts',(-0.612417258319161,-3.16410218115768,
20.213306887312));
#16615=CARTESIAN_POINT('Ctrl Pts',(-0.794565218114907,-3.12756084875824,
20.2016676644578));
#16616=CARTESIAN_POINT('Ctrl Pts',(-0.952515678574345,-3.08312665038861,
20.1910066877899));
#16617=CARTESIAN_POINT('Ctrl Pts',(-1.23270251018825,-2.98071306369046,
20.1711098801217));
#16618=CARTESIAN_POINT('Ctrl Pts',(-1.35589394543767,-2.92672056723879,
20.1619922847839));
#16619=CARTESIAN_POINT('Ctrl Pts',(-1.4752556264295,-2.8652641063588,20.1529125281009));
#16620=CARTESIAN_POINT('Ctrl Pts',(-1.47525540330811,-2.86526422123863,
19.9090518554891));
#16621=CARTESIAN_POINT('Ctrl Pts',(-1.43059364733655,-2.88825948161633,
19.9124054158376));
#16622=CARTESIAN_POINT('Ctrl Pts',(-1.38537564121385,-2.91022009359238,
19.9157346329231));
#16623=CARTESIAN_POINT('Ctrl Pts',(-1.2884052929316,-2.95453925547849,19.9227095951287));
#16624=CARTESIAN_POINT('Ctrl Pts',(-1.23656546639833,-2.97660833423677,
19.9263420874058));
#16625=CARTESIAN_POINT('Ctrl Pts',(-1.173315447835,-3.00159701465284,19.9306366803748));
#16626=CARTESIAN_POINT('Ctrl Pts',(-1.16243730808193,-3.00582655739098,
19.9313704526167));
#16627=CARTESIAN_POINT('Ctrl Pts',(-1.14546075708148,-3.01232128603614,
19.9325077964155));
#16628=CARTESIAN_POINT('Ctrl Pts',(-1.13937819040285,-3.01462721034128,
19.9329137474391));
#16629=CARTESIAN_POINT('Ctrl Pts',(-1.12806404462338,-3.01887731146156,
19.9336659210117));
#16630=CARTESIAN_POINT('Ctrl Pts',(-1.122834447533,-3.02082629665752,19.934012421613));
#16631=CARTESIAN_POINT('Ctrl Pts',(-1.11096515309334,-3.02521470729258,
19.9347962316453));
#16632=CARTESIAN_POINT('Ctrl Pts',(-1.10432248725709,-3.02764585825333,
19.9352330434412));
#16633=CARTESIAN_POINT('Ctrl Pts',(-1.08458191114903,-3.03479710553718,
19.9365258253445));
#16634=CARTESIAN_POINT('Ctrl Pts',(-1.07146116147525,-3.03945429138847,
19.9373781379427));
#16635=CARTESIAN_POINT('Ctrl Pts',(-0.971537604603511,-3.07419450798429,
19.9438193786349));
#16636=CARTESIAN_POINT('Ctrl Pts',(-0.883505585124597,-3.10064162017366,
19.9492102670712));
#16637=CARTESIAN_POINT('Ctrl Pts',(-0.558966391189524,-3.18319293008847,
19.9684645368859));
#16638=CARTESIAN_POINT('Ctrl Pts',(-0.317451220646878,-3.21627090049025,
19.9816737641273));
#16639=CARTESIAN_POINT('Ctrl Pts',(0.017371273963098,-3.22401316464108,
20.0007408304169));
#16640=CARTESIAN_POINT('Ctrl Pts',(0.109286574692442,-3.22220687777445,
20.0060451891133));
#16641=CARTESIAN_POINT('Ctrl Pts',(0.256967022909014,-3.21297847584007,
20.0147704959626));
#16642=CARTESIAN_POINT('Ctrl Pts',(0.312836077540626,-3.20802053450097,
20.0181179889282));
#16643=CARTESIAN_POINT('Ctrl Pts',(0.385603084667792,-3.19964414589995,
20.0225504260731));
#16644=CARTESIAN_POINT('Ctrl Pts',(0.402645022190167,-3.19754427141391,
20.0235936925333));
#16645=CARTESIAN_POINT('Ctrl Pts',(0.430424712482557,-3.19389571023135,
20.0253031014704));
#16646=CARTESIAN_POINT('Ctrl Pts',(0.441173005347996,-3.19242879572148,
20.025966647184));
#16647=CARTESIAN_POINT('Ctrl Pts',(0.461893078703285,-3.18949430697291,
20.0272500444734));
#16648=CARTESIAN_POINT('Ctrl Pts',(0.471865796048477,-3.18803416186256,
20.0278696530981));
#16649=CARTESIAN_POINT('Ctrl Pts',(0.494777328685117,-3.18456973330488,
20.0292975994978));
#16650=CARTESIAN_POINT('Ctrl Pts',(0.507711041074096,-3.18253334340763,
20.0301069496362));
#16651=CARTESIAN_POINT('Ctrl Pts',(0.542248440319117,-3.17687959969929,
20.0322770861719));
#16652=CARTESIAN_POINT('Ctrl Pts',(0.563827963357143,-3.17312075904579,
20.0336423520319));
#16653=CARTESIAN_POINT('Ctrl Pts',(0.74654716372541,-3.13937099560035,20.0452835848779));
#16654=CARTESIAN_POINT('Ctrl Pts',(0.905195752620308,-3.09735191204722,
20.0559470312609));
#16655=CARTESIAN_POINT('Ctrl Pts',(1.2997804612932,-2.95993042531818,20.0838151461165));
#16656=CARTESIAN_POINT('Ctrl Pts',(1.52889307559395,-2.84835014186709,20.1013456978682));
#16657=CARTESIAN_POINT('Ctrl Pts',(1.78990399511722,-2.68058445922449,20.1216439373497));
#16658=CARTESIAN_POINT('Ctrl Pts',(1.83647744846099,-2.64889426983437,20.1252758102766));
#16659=CARTESIAN_POINT('Ctrl Pts',(1.89167286329933,-2.6091813933757,20.1295697719503));
#16660=CARTESIAN_POINT('Ctrl Pts',(1.90110929303378,-2.60231382255424,20.1303035081653));
#16661=CARTESIAN_POINT('Ctrl Pts',(1.91574691020634,-2.59153885765746,20.1314408083938));
#16662=CARTESIAN_POINT('Ctrl Pts',(1.92097381189348,-2.58766680438355,20.1318467515854));
#16663=CARTESIAN_POINT('Ctrl Pts',(1.93066350703265,-2.5804432047977,20.1325989180819));
#16664=CARTESIAN_POINT('Ctrl Pts',(1.93512927498804,-2.57709592378187,20.1329454193927));
#16665=CARTESIAN_POINT('Ctrl Pts',(1.94523555673107,-2.56947975820593,20.1337292404925));
#16666=CARTESIAN_POINT('Ctrl Pts',(1.9508707114145,-2.56520390390303,20.1341660625877));
#16667=CARTESIAN_POINT('Ctrl Pts',(1.96755560463566,-2.55245692589137,20.1354589032418));
#16668=CARTESIAN_POINT('Ctrl Pts',(1.97856474330087,-2.54393258335488,20.1363112637982));
#16669=CARTESIAN_POINT('Ctrl Pts',(2.06180923517692,-2.47860933068432,20.1427539864464));
#16670=CARTESIAN_POINT('Ctrl Pts',(2.13164810818292,-2.41880988654524,20.1481462058679));
#16671=CARTESIAN_POINT('Ctrl Pts',(2.37646464157625,-2.19033378829858,20.1673999172869));
#16672=CARTESIAN_POINT('Ctrl Pts',(2.53477886146611,-2.00500761500875,20.1806076309195));
#16673=CARTESIAN_POINT('Ctrl Pts',(2.72220038006782,-1.72748032725434,20.1996731557343));
#16674=CARTESIAN_POINT('Ctrl Pts',(2.77034849214687,-1.64916054216864,20.2049776778626));
#16675=CARTESIAN_POINT('Ctrl Pts',(2.84238438129296,-1.51990588878749,20.2137032290034));
#16676=CARTESIAN_POINT('Ctrl Pts',(2.86840192106599,-1.47021519686481,20.2170507974422));
#16677=CARTESIAN_POINT('Ctrl Pts',(2.9006738132955,-1.40445855511251,20.2214833206224));
#16678=CARTESIAN_POINT('Ctrl Pts',(2.90811552800719,-1.3889839675746,20.2225265955898));
#16679=CARTESIAN_POINT('Ctrl Pts',(2.92005624595743,-1.3636373279111,20.2242360149641));
#16680=CARTESIAN_POINT('Ctrl Pts',(2.92462975280815,-1.35380059316961,20.2248995625466));
#16681=CARTESIAN_POINT('Ctrl Pts',(2.93335660632352,-1.33478019549209,20.2261829609906));
#16682=CARTESIAN_POINT('Ctrl Pts',(2.93751671077762,-1.32559975873509,20.2268025688877));
#16683=CARTESIAN_POINT('Ctrl Pts',(2.9469817590324,-1.30444911794695,20.2282305100838));
#16684=CARTESIAN_POINT('Ctrl Pts',(2.95225693048704,-1.29246585937163,20.229039855722));
#16685=CARTESIAN_POINT('Ctrl Pts',(2.96616171916738,-1.26034995417123,20.2312099723427));
#16686=CARTESIAN_POINT('Ctrl Pts',(2.97465923040746,-1.24016118949239,20.2325752226589));
#16687=CARTESIAN_POINT('Ctrl Pts',(3.04498798364075,-1.06818867824241,20.2442156649899));
#16688=CARTESIAN_POINT('Ctrl Pts',(3.09535393480341,-0.912002300567566,
20.2548782755466));
#16689=CARTESIAN_POINT('Ctrl Pts',(3.19293068539289,-0.505764808144659,
20.282743773313));
#16690=CARTESIAN_POINT('Ctrl Pts',(3.22284582310859,-0.252714055134884,
20.3002724897376));
#16691=CARTESIAN_POINT('Ctrl Pts',(3.22272882498705,0.0565890285072366,
20.3205073847095));
#16692=CARTESIAN_POINT('Ctrl Pts',(3.22128091307601,0.11195331730861,20.3240790385116));
#16693=CARTESIAN_POINT('Ctrl Pts',(3.21783469679233,0.178266586000064,20.328275425723));
#16694=CARTESIAN_POINT('Ctrl Pts',(3.21720601370459,0.189273836510378,20.3289692737853));
#16695=CARTESIAN_POINT('Ctrl Pts',(3.21608497941296,0.207277976993981,20.3300995100013));
#16696=CARTESIAN_POINT('Ctrl Pts',(3.21562625717631,0.214276762442052,20.3305377148613));
#16697=CARTESIAN_POINT('Ctrl Pts',(3.21476178402536,0.22683768393226,20.3313220336635));
#16698=CARTESIAN_POINT('Ctrl Pts',(3.2143644426741,0.232400288401883,20.331668611077));
#16699=CARTESIAN_POINT('Ctrl Pts',(3.21346902791398,0.244493904199337,20.3324204468636));
#16700=CARTESIAN_POINT('Ctrl Pts',(3.21296548478553,0.2510244170038,20.3328253940434));
#16701=CARTESIAN_POINT('Ctrl Pts',(3.21149279830193,0.269393111152186,20.3339615913295));
#16702=CARTESIAN_POINT('Ctrl Pts',(3.21047810202809,0.281227680896662,20.3346903257257));
#16703=CARTESIAN_POINT('Ctrl Pts',(3.20395303145869,0.352686741949944,20.3390720920251));
#16704=CARTESIAN_POINT('Ctrl Pts',(3.19684684816458,0.412158047780392,20.3426411780582));
#16705=CARTESIAN_POINT('Ctrl Pts',(3.15131524322269,0.720088476940664,20.3608762159645));
#16706=CARTESIAN_POINT('Ctrl Pts',(3.08556915115906,0.963640744857692,20.3745244198022));
#16707=CARTESIAN_POINT('Ctrl Pts',(2.93178788686179,1.34802195342613,20.3979169732379));
#16708=CARTESIAN_POINT('Ctrl Pts',(2.86007993088528,1.49414722746266,20.4072883198121));
#16709=CARTESIAN_POINT('Ctrl Pts',(2.7665690792335,1.65308551433941,20.4183800688993));
#16710=CARTESIAN_POINT('Ctrl Pts',(2.75528367714294,1.67182774537481,20.4197026878485));
#16711=CARTESIAN_POINT('Ctrl Pts',(2.73694482775648,1.70159389875943,20.421827526181));
#16712=CARTESIAN_POINT('Ctrl Pts',(2.73001341266207,1.71269248414219,20.4226252583894));
#16713=CARTESIAN_POINT('Ctrl Pts',(2.71762434755924,1.73226355709479,20.4240418236202));
#16714=CARTESIAN_POINT('Ctrl Pts',(2.71219415423518,1.74075328285015,20.4246596302377));
#16715=CARTESIAN_POINT('Ctrl Pts',(2.70083445733673,1.75833118296704,20.4259457683132));
#16716=CARTESIAN_POINT('Ctrl Pts',(2.69489870136719,1.76741514639021,20.4266143288479));
#16717=CARTESIAN_POINT('Ctrl Pts',(2.67944367762728,1.79080833973204,20.4283462401536));
#16718=CARTESIAN_POINT('Ctrl Pts',(2.66985571581806,1.80507156907996,20.4294121742095));
#16719=CARTESIAN_POINT('Ctrl Pts',(2.62841608890123,1.86566542037911,20.4339838327829));
#16720=CARTESIAN_POINT('Ctrl Pts',(2.59547065082444,1.91123260109075,20.4375310874418));
#16721=CARTESIAN_POINT('Ctrl Pts',(2.50538165199908,2.02920802967106,20.4470151165299));
#16722=CARTESIAN_POINT('Ctrl Pts',(2.44629576541941,2.10006117389156,20.4530240540219));
#16723=CARTESIAN_POINT('Ctrl Pts',(2.22314640179419,2.34543811945696,20.4749682767047));
#16724=CARTESIAN_POINT('Ctrl Pts',(2.04280962477906,2.50407153022852,20.4914294610284));
#16725=CARTESIAN_POINT('Ctrl Pts',(1.82179466870766,2.65858914126104,20.5093885050216));
#16726=CARTESIAN_POINT('Ctrl Pts',(1.79676740234166,2.67556704894589,20.5113921426775));
#16727=CARTESIAN_POINT('Ctrl Pts',(1.715914209649,2.72876973637368,20.517761598418));
#16728=CARTESIAN_POINT('Ctrl Pts',(1.65919983656839,2.76362139095914,20.522074508461));
#16729=CARTESIAN_POINT('Ctrl Pts',(1.59132073202676,2.80249030937626,20.5270221392162));
#16730=CARTESIAN_POINT('Ctrl Pts',(1.58116735857222,2.80823136515241,20.5277567005687));
#16731=CARTESIAN_POINT('Ctrl Pts',(1.56468968310015,2.81743069236902,20.5289396426155));
#16732=CARTESIAN_POINT('Ctrl Pts',(1.55838466428329,2.82092303177971,20.529390128335));
#16733=CARTESIAN_POINT('Ctrl Pts',(1.54716633851884,2.82708775313512,20.5301877701745));
#16734=CARTESIAN_POINT('Ctrl Pts',(1.54225774521927,2.82976852268922,20.5305354583536));
#16735=CARTESIAN_POINT('Ctrl Pts',(1.53170577647935,2.83549574207186,20.53128003427));
#16736=CARTESIAN_POINT('Ctrl Pts',(1.52606029464082,2.83853812160837,20.5316766624953));
#16737=CARTESIAN_POINT('Ctrl Pts',(1.5104848697193,2.84687190111473,20.5327662675448));
#16738=CARTESIAN_POINT('Ctrl Pts',(1.50053612632213,2.85212824139069,20.5334570494147));
#16739=CARTESIAN_POINT('Ctrl Pts',(1.44635048270484,2.88039479698909,20.5371923321958));
#16740=CARTESIAN_POINT('Ctrl Pts',(1.40160893316019,2.90242948925155,20.5401790810496));
#16741=CARTESIAN_POINT('Ctrl Pts',(1.12140652716319,3.03243431434718,20.5583972938457));
#16742=CARTESIAN_POINT('Ctrl Pts',(0.874131878556189,3.11273753382656,20.5724421024193));
#16743=CARTESIAN_POINT('Ctrl Pts',(0.457025189978494,3.19449346324033,20.5964381437279));
#16744=CARTESIAN_POINT('Ctrl Pts',(0.291962332503283,3.21378402454912,20.6059953026084));
#16745=CARTESIAN_POINT('Ctrl Pts',(0.104232790564992,3.22113872450317,20.6172949558947));
#16746=CARTESIAN_POINT('Ctrl Pts',(0.0822965744579971,3.22177379629132,
20.6186216148224));
#16747=CARTESIAN_POINT('Ctrl Pts',(0.0472532656245252,3.22243020607399,
20.6207517166503));
#16748=CARTESIAN_POINT('Ctrl Pts',(0.0341493206615145,3.22259571154476,
20.6215506367417));
#16749=CARTESIAN_POINT('Ctrl Pts',(0.0109641388187761,3.22274711633592,
20.6229685767907));
#16750=CARTESIAN_POINT('Ctrl Pts',(0.000883235815767659,3.2227656452833,
20.6235865636895));
#16751=CARTESIAN_POINT('Ctrl Pts',(-0.0200402444660291,3.22270593092331,
20.624872345095));
#16752=CARTESIAN_POINT('Ctrl Pts',(-0.0308826578445186,3.22262026702658,
20.625540365042));
#16753=CARTESIAN_POINT('Ctrl Pts',(-0.0588701856281349,3.22225788748839,
20.6272693036906));
#16754=CARTESIAN_POINT('Ctrl Pts',(-0.0760137250679063,3.22189904986492,
20.6283327888876));
#16755=CARTESIAN_POINT('Ctrl Pts',(-0.148998447703224,3.2197885506647,20.6328797652262));
#16756=CARTESIAN_POINT('Ctrl Pts',(-0.204789093561608,3.21672187873367,
20.6364042310468));
#16757=CARTESIAN_POINT('Ctrl Pts',(-0.351579871151899,3.20481901177623,
20.6458119421613));
#16758=CARTESIAN_POINT('Ctrl Pts',(-0.442327499869453,3.19355870535963,
20.6517659150887));
#16759=CARTESIAN_POINT('Ctrl Pts',(-0.776325528478468,3.13760606711091,
20.674163348959));
#16760=CARTESIAN_POINT('Ctrl Pts',(-1.01464607421257,3.06883215841772,20.6911823289542));
#16761=CARTESIAN_POINT('Ctrl Pts',(-1.32447853273326,2.9393401510836,20.713494840073));
#16762=CARTESIAN_POINT('Ctrl Pts',(-1.40477267742463,2.90182368975267,20.7192857620217));
#16763=CARTESIAN_POINT('Ctrl Pts',(-1.49568364174185,2.85468713671611,20.7257712492287));
#16764=CARTESIAN_POINT('Ctrl Pts',(-1.50790058231765,2.84825280735781,20.7266412469668));
#16765=CARTESIAN_POINT('Ctrl Pts',(-1.52629159731091,2.83841526376611,20.7279481424801));
#16766=CARTESIAN_POINT('Ctrl Pts',(-1.53249629291243,2.83507008097799,20.7283885781568));
#16767=CARTESIAN_POINT('Ctrl Pts',(-1.54359222503694,2.82904077955072,20.7291752843002));
#16768=CARTESIAN_POINT('Ctrl Pts',(-1.54848749310999,2.82636430326622,20.7295220307416));
#16769=CARTESIAN_POINT('Ctrl Pts',(-1.55909120527533,2.82053092986941,20.7302723981622));
#16770=CARTESIAN_POINT('Ctrl Pts',(-1.564797005452,2.81736941955191,20.7306757179039));
#16771=CARTESIAN_POINT('Ctrl Pts',(-1.5807575489111,2.80846244444094,20.7318027557087));
#16772=CARTESIAN_POINT('Ctrl Pts',(-1.59099063962236,2.80267809868083,20.7325240226806));
#16773=CARTESIAN_POINT('Ctrl Pts',(-1.65129116581673,2.76815599566594,20.7367677147697));
#16774=CARTESIAN_POINT('Ctrl Pts',(-1.70061424802841,2.73813116351675,20.7402122235753));
#16775=CARTESIAN_POINT('Ctrl Pts',(-1.96152439243689,2.56953331030511,20.7584356009522));
#16776=CARTESIAN_POINT('Ctrl Pts',(-2.15706493037836,2.40773268599829,20.7721627041973));
#16777=CARTESIAN_POINT('Ctrl Pts',(-2.44447442685418,2.10650358354623,20.7956827307223));
#16778=CARTESIAN_POINT('Ctrl Pts',(-2.54809538238246,1.97990204823421,20.8050992443411));
#16779=CARTESIAN_POINT('Ctrl Pts',(-2.65420633500666,1.82805515489491,20.8162414977202));
#16780=CARTESIAN_POINT('Ctrl Pts',(-2.66656394562522,1.80998165896321,20.8175651114207));
#16781=CARTESIAN_POINT('Ctrl Pts',(-2.68601406075094,1.78090352893238,20.8196912458699));
#16782=CARTESIAN_POINT('Ctrl Pts',(-2.69322546249081,1.76997895868048,20.8204892706818));
#16783=CARTESIAN_POINT('Ctrl Pts',(-2.70587104179589,1.75056592169788,20.8219061744347));
#16784=CARTESIAN_POINT('Ctrl Pts',(-2.71133236162739,1.74209527930201,20.8225240253321));
#16785=CARTESIAN_POINT('Ctrl Pts',(-2.72258989951244,1.72445339395382,20.8238100749195));
#16786=CARTESIAN_POINT('Ctrl Pts',(-2.72837971126088,1.71527823265415,20.8244785017883));
#16787=CARTESIAN_POINT('Ctrl Pts',(-2.74321608235527,1.69150173674997,20.8262096781686));
#16788=CARTESIAN_POINT('Ctrl Pts',(-2.75219234481016,1.67685714319281,20.8272750068103));
#16789=CARTESIAN_POINT('Ctrl Pts',(-2.79000285477184,1.61404857269709,20.8318405508547));
#16790=CARTESIAN_POINT('Ctrl Pts',(-2.81769165543471,1.56520983261283,20.8353821584189));
#16791=CARTESIAN_POINT('Ctrl Pts',(-2.887367285934,1.43446696320475,20.8448472545682));
#16792=CARTESIAN_POINT('Ctrl Pts',(-2.92714336674572,1.3514490350802,20.8508425485672));
#16793=CARTESIAN_POINT('Ctrl Pts',(-3.05835586934631,1.04452739272671,20.8729250471122));
#16794=CARTESIAN_POINT('Ctrl Pts',(-3.12807125861198,0.812239784608602,
20.8895524387025));
#16795=CARTESIAN_POINT('Ctrl Pts',(-3.18770530887634,0.482985157539663,
20.9118209845893));
#16796=CARTESIAN_POINT('Ctrl Pts',(-3.20029910267135,0.390933432686804,
20.9179011624078));
#16797=CARTESIAN_POINT('Ctrl Pts',(-3.21019258239435,0.284562630579857,
20.9246681250829));
#16798=CARTESIAN_POINT('Ctrl Pts',(-3.21139471910581,0.270658976312678,
20.9255475475012));
#16799=CARTESIAN_POINT('Ctrl Pts',(-3.21307061028902,0.249689704848372,
20.9268657771642));
#16800=CARTESIAN_POINT('Ctrl Pts',(-3.21361143624875,0.242629830184885,
20.9273082122274));
#16801=CARTESIAN_POINT('Ctrl Pts',(-3.21453698031546,0.230001560988902,
20.9280970711628));
#16802=CARTESIAN_POINT('Ctrl Pts',(-3.21493050237897,0.2244339152739,20.9284439821962));
#16803=CARTESIAN_POINT('Ctrl Pts',(-3.21575098718649,0.212380316170144,
20.929193093328));
#16804=CARTESIAN_POINT('Ctrl Pts',(-3.216172792279,0.20589410446725,20.9295950008836));
#16805=CARTESIAN_POINT('Ctrl Pts',(-3.21729568418752,0.187781032326448,
20.9307141093516));
#16806=CARTESIAN_POINT('Ctrl Pts',(-3.21795337358538,0.17615144245827,20.9314289144922));
#16807=CARTESIAN_POINT('Ctrl Pts',(-3.22140390745169,0.108647058728933,
20.9355577441873));
#16808=CARTESIAN_POINT('Ctrl Pts',(-3.22280470667723,0.0527069175510339,
20.9388986876561));
#16809=CARTESIAN_POINT('Ctrl Pts',(-3.22249238833365,-0.257458018862945,
20.9571155695141));
#16810=CARTESIAN_POINT('Ctrl Pts',(-3.19215944264278,-0.510771299372993,
20.9709106357355));
#16811=CARTESIAN_POINT('Ctrl Pts',(-3.09378614221512,-0.917339506017467,
20.9945372654579));
#16812=CARTESIAN_POINT('Ctrl Pts',(-3.04309930352166,-1.07357376295313,
21.0039891562796));
#16813=CARTESIAN_POINT('Ctrl Pts',(-2.97241861120438,-1.24552201332927,
21.0151709814409));
#16814=CARTESIAN_POINT('Ctrl Pts',(-2.96388348962222,-1.26569826956019,
21.0164953680751));
#16815=CARTESIAN_POINT('Ctrl Pts',(-2.94991939163909,-1.29779220053816,
21.0186225095763));
#16816=CARTESIAN_POINT('Ctrl Pts',(-2.94462223104488,-1.30976674314188,
21.019420761693));
#16817=CARTESIAN_POINT('Ctrl Pts',(-2.9351186366654,-1.33090110139177,21.0208379284795));
#16818=CARTESIAN_POINT('Ctrl Pts',(-2.9309419043456,-1.3400741407368,21.0214558138328));
#16819=CARTESIAN_POINT('Ctrl Pts',(-2.92218081748639,-1.35907854925507,
21.0227417949653));
#16820=CARTESIAN_POINT('Ctrl Pts',(-2.91758972435345,-1.36890665454996,
21.0234101182268));
#16821=CARTESIAN_POINT('Ctrl Pts',(-2.90560406909069,-1.3942300157804,21.0251407249081));
#16822=CARTESIAN_POINT('Ctrl Pts',(-2.89813521475951,-1.40968954092806,
21.0262055842394));
#16823=CARTESIAN_POINT('Ctrl Pts',(-2.86575059353019,-1.47537609712777,
21.0307663940314));
#16824=CARTESIAN_POINT('Ctrl Pts',(-2.8396511648637,-1.52500548098698,21.0343036299909));
#16825=CARTESIAN_POINT('Ctrl Pts',(-2.76740708042064,-1.65409029240971,
21.0437540791577));
#16826=CARTESIAN_POINT('Ctrl Pts',(-2.71913897162283,-1.73229252164342,
21.0497388217944));
#16827=CARTESIAN_POINT('Ctrl Pts',(-2.53102936976523,-2.0097881813213,21.07191572751));
#16828=CARTESIAN_POINT('Ctrl Pts',(-2.37209054798314,-2.19511493300139,
21.088658188419));
#16829=CARTESIAN_POINT('Ctrl Pts',(-2.12674616973946,-2.42310789164414,
21.1109371020969));
#16830=CARTESIAN_POINT('Ctrl Pts',(-2.05704101931461,-2.48255649322211,
21.1169296606735));
#16831=CARTESIAN_POINT('Ctrl Pts',(-1.97393166968701,-2.54752916970758,
21.1236115473473));
#16832=CARTESIAN_POINT('Ctrl Pts',(-1.96291583197397,-2.55602671349855,
21.1244882236578));
#16833=CARTESIAN_POINT('Ctrl Pts',(-1.94621821876125,-2.56873552755151,
21.1258031520079));
#16834=CARTESIAN_POINT('Ctrl Pts',(-1.94057721188963,-2.57299973814683,
21.1262450055616));
#16835=CARTESIAN_POINT('Ctrl Pts',(-1.93045915347212,-2.58059608710188,
21.1270332371268));
#16836=CARTESIAN_POINT('Ctrl Pts',(-1.92598745573521,-2.58393518299284,
21.1273800990478));
#16837=CARTESIAN_POINT('Ctrl Pts',(-1.91628349109191,-2.59114211863501,
21.1281295698948));
#16838=CARTESIAN_POINT('Ctrl Pts',(-1.91104819375541,-2.59500572255781,
21.1285318837708));
#16839=CARTESIAN_POINT('Ctrl Pts',(-1.896383515664,-2.60575968037963,21.1296532719735));
#16840=CARTESIAN_POINT('Ctrl Pts',(-1.88692821635097,-2.61261475660756,
21.1303699346826));
#16841=CARTESIAN_POINT('Ctrl Pts',(-1.83155358487942,-2.65230383777476,
21.1345313613818));
#16842=CARTESIAN_POINT('Ctrl Pts',(-1.78481207014196,-2.68398043156078,
21.1379016887379));
#16843=CARTESIAN_POINT('Ctrl Pts',(-1.65226489266357,-2.76881227520234,
21.1471413340034));
#16844=CARTESIAN_POINT('Ctrl Pts',(-1.56483039988362,-2.81914422829277,
21.1528793324542));
#16845=CARTESIAN_POINT('Ctrl Pts',(-1.47525512068014,-2.86526436675694,
21.1585511949183));
#16846=CARTESIAN_POINT('Origin',(0.,0.,4.68922655072688));
#16847=CARTESIAN_POINT('',(-1.47525567074797,-2.86526408354029,22.6538402050192));
#16848=CARTESIAN_POINT('',(-1.47525540254685,-2.86526422163059,22.4042343665403));
#16849=CARTESIAN_POINT('',(-1.47525540501186,-2.86526422036142,4.68922655072688));
#16850=CARTESIAN_POINT('',(3.21778804064233,0.000208849362278093,21.8109814966979));
#16851=CARTESIAN_POINT('Ctrl Pts',(-1.47525567074797,-2.86526408354029,
22.6538402050192));
#16852=CARTESIAN_POINT('Ctrl Pts',(-1.59395129052928,-2.80415055924728,
22.6463741799665));
#16853=CARTESIAN_POINT('Ctrl Pts',(-1.70883224031351,-2.73567054746652,
22.6388641912748));
#16854=CARTESIAN_POINT('Ctrl Pts',(-1.89870517497142,-2.60582223290445,
22.6255690687147));
#16855=CARTESIAN_POINT('Ctrl Pts',(-1.97571020711639,-2.54793197975155,
22.6199016273927));
#16856=CARTESIAN_POINT('Ctrl Pts',(-2.06493547434476,-2.47437538588842,
22.6129308383243));
#16857=CARTESIAN_POINT('Ctrl Pts',(-2.07975612873059,-2.46193145382807,
22.6117589647593));
#16858=CARTESIAN_POINT('Ctrl Pts',(-2.10393967710873,-2.44125190312021,
22.6098230902081));
#16859=CARTESIAN_POINT('Ctrl Pts',(-2.11336857710181,-2.43309397061587,
22.6090622919252));
#16860=CARTESIAN_POINT('Ctrl Pts',(-2.13025681712948,-2.41830994659176,
22.6076885960526));
#16861=CARTESIAN_POINT('Ctrl Pts',(-2.13773321125937,-2.41170350968555,
22.6070765240084));
#16862=CARTESIAN_POINT('Ctrl Pts',(-2.15361492482094,-2.39753792604147,
22.6057678265943));
#16863=CARTESIAN_POINT('Ctrl Pts',(-2.16201137145421,-2.38996907421465,
22.605070795996));
#16864=CARTESIAN_POINT('Ctrl Pts',(-2.18457767229459,-2.36941078420404,
22.6031833981221));
#16865=CARTESIAN_POINT('Ctrl Pts',(-2.19867124373978,-2.35633864431985,
22.6019895141823));
#16866=CARTESIAN_POINT('Ctrl Pts',(-2.26953082816861,-2.28942538429351,
22.5959087262619));
#16867=CARTESIAN_POINT('Ctrl Pts',(-2.32443553587578,-2.23365988856786,
22.5909385365495));
#16868=CARTESIAN_POINT('Ctrl Pts',(-2.55443533166249,-1.98238281204841,
22.5689347652013));
#16869=CARTESIAN_POINT('Ctrl Pts',(-2.70729118301288,-1.76791284089322,
22.551023846707));
#16870=CARTESIAN_POINT('Ctrl Pts',(-2.89775382083268,-1.41700004791609,
22.5241359849261));
#16871=CARTESIAN_POINT('Ctrl Pts',(-2.95534375634447,-1.29260148780202,
22.5150322898949));
#16872=CARTESIAN_POINT('Ctrl Pts',(-3.01026399239769,-1.150935558751,22.5053984875968));
#16873=CARTESIAN_POINT('Ctrl Pts',(-3.01558138979936,-1.1369304579617,22.5044538574264));
#16874=CARTESIAN_POINT('Ctrl Pts',(-3.02330682749529,-1.11614744085675,
22.5030640696143));
#16875=CARTESIAN_POINT('Ctrl Pts',(-3.02579005383667,-1.10939796078506,
22.5026145876036));
#16876=CARTESIAN_POINT('Ctrl Pts',(-3.03016431509733,-1.09738464916309,
22.5018179435708));
#16877=CARTESIAN_POINT('Ctrl Pts',(-3.03206425801083,-1.09212416038817,
22.5014702555993));
#16878=CARTESIAN_POINT('Ctrl Pts',(-3.03611811845573,-1.0808078660793,22.5007248041255));
#16879=CARTESIAN_POINT('Ctrl Pts',(-3.03826761196424,-1.07475057217456,
22.5003273049443));
#16880=CARTESIAN_POINT('Ctrl Pts',(-3.04414960466641,-1.05801638564751,
22.4992332385375));
#16881=CARTESIAN_POINT('Ctrl Pts',(-3.04784408357195,-1.04732609009186,
22.4985388951071));
#16882=CARTESIAN_POINT('Ctrl Pts',(-3.06778219979724,-0.988634360706152,
22.4947507245502));
#16883=CARTESIAN_POINT('Ctrl Pts',(-3.0829492140565,-0.94027141500147,22.4917165902451));
#16884=CARTESIAN_POINT('Ctrl Pts',(-3.16846841782635,-0.643209970583038,
22.4734950773695));
#16885=CARTESIAN_POINT('Ctrl Pts',(-3.20984010007619,-0.387128211958623,
22.4594804483602));
#16886=CARTESIAN_POINT('Ctrl Pts',(-3.22679472407655,0.0366577776000503,
22.4355343236601));
#16887=CARTESIAN_POINT('Ctrl Pts',(-3.22064835929335,0.2023893017631,22.4259957306645));
#16888=CARTESIAN_POINT('Ctrl Pts',(-3.19929825503873,0.388702664193861,
22.4147165712294));
#16889=CARTESIAN_POINT('Ctrl Pts',(-3.19657747944004,0.410477121535496,
22.4133900098312));
#16890=CARTESIAN_POINT('Ctrl Pts',(-3.19187676228284,0.445210160735792,
22.4112598935972));
#16891=CARTESIAN_POINT('Ctrl Pts',(-3.19003972375883,0.458187631543052,
22.4104608598315));
#16892=CARTESIAN_POINT('Ctrl Pts',(-3.18664934270805,0.48112910692513,22.4090426145696));
#16893=CARTESIAN_POINT('Ctrl Pts',(-3.18512829190906,0.491097761470688,
22.4084244359355));
#16894=CARTESIAN_POINT('Ctrl Pts',(-3.18187392370323,0.511774922358287,
22.4071381517292));
#16895=CARTESIAN_POINT('Ctrl Pts',(-3.18013327650125,0.522482130392948,
22.4064698200499));
#16896=CARTESIAN_POINT('Ctrl Pts',(-3.17549981627052,0.550102631730018,
22.4047398493039));
#16897=CARTESIAN_POINT('Ctrl Pts',(-3.17252595247678,0.567001808706687,
22.4036756395635));
#16898=CARTESIAN_POINT('Ctrl Pts',(-3.1592826060433,0.638889811009705,22.3991234820072));
#16899=CARTESIAN_POINT('Ctrl Pts',(-3.14771780532546,0.693627249082833,
22.3955944507245));
#16900=CARTESIAN_POINT('Ctrl Pts',(-3.11348233097286,0.837095632719853,
22.3861720499949));
#16901=CARTESIAN_POINT('Ctrl Pts',(-3.08844551759512,0.925204363725221,
22.3802076910293));
#16902=CARTESIAN_POINT('Ctrl Pts',(-2.98245007986553,1.24563382940991,22.3578843759559));
#16903=CARTESIAN_POINT('Ctrl Pts',(-2.87873813428715,1.46951127851072,22.340958487716));
#16904=CARTESIAN_POINT('Ctrl Pts',(-2.70391060322844,1.75584939025165,22.3186584077431));
#16905=CARTESIAN_POINT('Ctrl Pts',(-2.65406555130686,1.83032206604534,22.3128008144069));
#16906=CARTESIAN_POINT('Ctrl Pts',(-2.59300324952485,1.91380339232455,22.3062500744374));
#16907=CARTESIAN_POINT('Ctrl Pts',(-2.58475677157753,1.92492642054307,22.3053776043138));
#16908=CARTESIAN_POINT('Ctrl Pts',(-2.57219837354516,1.94163923371114,22.3040676446802));
#16909=CARTESIAN_POINT('Ctrl Pts',(-2.56793948074423,1.94726839758761,22.303626594299));
#16910=CARTESIAN_POINT('Ctrl Pts',(-2.56027977441543,1.95732373257563,22.3028391172023));
#16911=CARTESIAN_POINT('Ctrl Pts',(-2.55688593841843,1.96175508584873,22.302492211615));
#16912=CARTESIAN_POINT('Ctrl Pts',(-2.54950266752828,1.97134376053639,22.3017418658776));
#16913=CARTESIAN_POINT('Ctrl Pts',(-2.54550910161745,1.97649778378345,22.3013387252002));
#16914=CARTESIAN_POINT('Ctrl Pts',(-2.53428447724387,1.99089363052469,22.300213091656));
#16915=CARTESIAN_POINT('Ctrl Pts',(-2.52701845699144,2.00010824395954,22.2994930389822));
#16916=CARTESIAN_POINT('Ctrl Pts',(-2.48395238004216,2.05411441393317,22.2952741657301));
#16917=CARTESIAN_POINT('Ctrl Pts',(-2.44700991682696,2.09798685874913,22.2918521928202));
#16918=CARTESIAN_POINT('Ctrl Pts',(-2.24065786219948,2.33017668466074,22.273624769719));
#16919=CARTESIAN_POINT('Ctrl Pts',(-2.05065486161858,2.49902227565613,22.2598781434133));
#16920=CARTESIAN_POINT('Ctrl Pts',(-1.70881839437805,2.7372865768509,22.2363394714562));
#16921=CARTESIAN_POINT('Ctrl Pts',(-1.56792633257803,2.82035365922715,22.2269257542924));
#16922=CARTESIAN_POINT('Ctrl Pts',(-1.40166323893353,2.90205776206202,22.2157836563833));
#16923=CARTESIAN_POINT('Ctrl Pts',(-1.38187105645885,2.91153420666235,22.2144570897182));
#16924=CARTESIAN_POINT('Ctrl Pts',(-1.35010510066578,2.92634679603342,22.2123269666227));
#16925=CARTESIAN_POINT('Ctrl Pts',(-1.33819265137013,2.93181339333739,22.211527931309));
#16926=CARTESIAN_POINT('Ctrl Pts',(-1.31705672322591,2.94135697235125,22.2101096842547));
#16927=CARTESIAN_POINT('Ctrl Pts',(-1.30784678057482,2.94546363852328,22.209491505385));
#16928=CARTESIAN_POINT('Ctrl Pts',(-1.2886896691464,2.95389813194206,22.2082052216403));
#16929=CARTESIAN_POINT('Ctrl Pts',(-1.27873963224085,2.95821909019347,22.207536890663));
#16930=CARTESIAN_POINT('Ctrl Pts',(-1.25299496510242,2.96924495524708,22.2058069237774));
#16931=CARTESIAN_POINT('Ctrl Pts',(-1.23716841760577,2.97587403546525,22.2047427172173));
#16932=CARTESIAN_POINT('Ctrl Pts',(-1.1695233091085,3.00357486230951,22.2001905916544));
#16933=CARTESIAN_POINT('Ctrl Pts',(-1.11721636204581,3.0234208591613,22.1966615899032));
#16934=CARTESIAN_POINT('Ctrl Pts',(-0.977998455384767,3.07213608949535,
22.1872392879752));
#16935=CARTESIAN_POINT('Ctrl Pts',(-0.890332533671326,3.09867820479817,
22.1812750001309));
#16936=CARTESIAN_POINT('Ctrl Pts',(-0.563428271747264,3.18263489796652,
22.1589512017364));
#16937=CARTESIAN_POINT('Ctrl Pts',(-0.318999298178052,3.21633957864115,
22.1420247028377));
#16938=CARTESIAN_POINT('Ctrl Pts',(0.0164072852926216,3.22395242924655,
22.1197245435649));
#16939=CARTESIAN_POINT('Ctrl Pts',(0.105998843521479,3.22225168076818,22.1138673903833));
#16940=CARTESIAN_POINT('Ctrl Pts',(0.209231663251922,3.21598062512818,22.1073170794617));
#16941=CARTESIAN_POINT('Ctrl Pts',(0.223046778683697,3.21505200903909,22.1064446241078));
#16942=CARTESIAN_POINT('Ctrl Pts',(0.243895259891753,3.21351559639254,22.105134682241));
#16943=CARTESIAN_POINT('Ctrl Pts',(0.250933107399983,3.21297369486896,22.1046936349974));
#16944=CARTESIAN_POINT('Ctrl Pts',(0.263532938620348,3.21196187829281,22.1039061612739));
#16945=CARTESIAN_POINT('Ctrl Pts',(0.269095512498012,3.21150063429049,22.1035592559397));
#16946=CARTESIAN_POINT('Ctrl Pts',(0.281153390932553,3.21046925622811,22.1028089082071));
#16947=CARTESIAN_POINT('Ctrl Pts',(0.287648152437793,3.20989386375882,22.1024057652952));
#16948=CARTESIAN_POINT('Ctrl Pts',(0.305826824667847,3.20822773769851,22.1012801191968));
#16949=CARTESIAN_POINT('Ctrl Pts',(0.317506731082661,3.20709288128821,22.1005600562913));
#16950=CARTESIAN_POINT('Ctrl Pts',(0.386223443863662,3.20003706707863,22.0963409993511));
#16951=CARTESIAN_POINT('Ctrl Pts',(0.443104151032635,3.19265805112663,22.0929188607913));
#16952=CARTESIAN_POINT('Ctrl Pts',(0.749980879806487,3.14448702791497,22.0746914259509));
#16953=CARTESIAN_POINT('Ctrl Pts',(0.994720160776134,3.07584597266029,22.0609449073278));
#16954=CARTESIAN_POINT('Ctrl Pts',(1.37991334895783,2.91695679789033,22.0374063976115));
#16955=CARTESIAN_POINT('Ctrl Pts',(1.5259393122153,2.84328976111937,22.0279927296228));
#16956=CARTESIAN_POINT('Ctrl Pts',(1.68618817838258,2.74653552841282,22.0167340207944));
#16957=CARTESIAN_POINT('Ctrl Pts',(1.70649564461843,2.73396425535425,22.0152895437326));
#16958=CARTESIAN_POINT('Ctrl Pts',(1.73706053886546,2.71456993622543,22.0130875549612));
#16959=CARTESIAN_POINT('Ctrl Pts',(1.74742195055384,2.70791169989794,22.0123361592619));
#16960=CARTESIAN_POINT('Ctrl Pts',(1.7657622079298,2.69597716689805,22.010997243));
#16961=CARTESIAN_POINT('Ctrl Pts',(1.7737562493654,2.69072440507944,22.010410609565));
#16962=CARTESIAN_POINT('Ctrl Pts',(1.78206910837562,2.6852090094271,22.0097973764916));
#16963=CARTESIAN_POINT('Ctrl Pts',(1.78241145366999,2.68498177668975,22.0097721162636));
#16964=CARTESIAN_POINT('Ctrl Pts',(1.78303958452356,2.68456467983984,22.0097257586782));
#16965=CARTESIAN_POINT('Ctrl Pts',(1.78332538578223,2.68437483385814,22.009704661884));
#16966=CARTESIAN_POINT('Ctrl Pts',(1.78385673916683,2.68402175541997,22.0096654319599));
#16967=CARTESIAN_POINT('Ctrl Pts',(1.78410229623998,2.68385853688113,22.0096472995028));
#16968=CARTESIAN_POINT('Ctrl Pts',(1.78456335181609,2.6835519881005,22.0096132486726));
#16969=CARTESIAN_POINT('Ctrl Pts',(1.7847788554715,2.68340866558655,22.009597330592));
#16970=CARTESIAN_POINT('Ctrl Pts',(1.78518662470617,2.68313740438402,22.0095672066249));
#16971=CARTESIAN_POINT('Ctrl Pts',(1.7853788938218,2.68300947097285,22.0095530009377));
#16972=CARTESIAN_POINT('Ctrl Pts',(1.78574498937772,2.68276581889266,22.009525948762));
#16973=CARTESIAN_POINT('Ctrl Pts',(1.78591881833183,2.68265010398946,22.009513102416));
#16974=CARTESIAN_POINT('Ctrl Pts',(1.78625153667906,2.68242857251684,22.0094885109731));
#16975=CARTESIAN_POINT('Ctrl Pts',(1.78641042791563,2.68232275872559,22.0094767659818));
#16976=CARTESIAN_POINT('Ctrl Pts',(1.7867159093031,2.68211928388161,22.0094541829101));
#16977=CARTESIAN_POINT('Ctrl Pts',(1.78686250086671,2.68202162491706,22.0094433449083));
#16978=CARTESIAN_POINT('Ctrl Pts',(1.78714542080856,2.68183311080744,22.0094224256734));
#16979=CARTESIAN_POINT('Ctrl Pts',(1.78728175025666,2.68174225729088,22.0094123445027));
#16980=CARTESIAN_POINT('Ctrl Pts',(1.7875457534526,2.68156628957007,22.0093928204693));
#16981=CARTESIAN_POINT('Ctrl Pts',(1.78767342806627,2.68148117663183,22.009383377654));
#16982=CARTESIAN_POINT('Ctrl Pts',(1.78792141284636,2.68131583460374,22.0093650351524));
#16983=CARTESIAN_POINT('Ctrl Pts',(1.78804172368694,2.68123560653776,22.0093561355053));
#16984=CARTESIAN_POINT('Ctrl Pts',(1.78827603459676,2.68107933589541,22.0093388016557));
#16985=CARTESIAN_POINT('Ctrl Pts',(1.78839003520651,2.68100329415175,22.0093303674852));
#16986=CARTESIAN_POINT('Ctrl Pts',(1.78861259754135,2.68085481804755,22.0093139002929));
#16987=CARTESIAN_POINT('Ctrl Pts',(1.78872115972714,2.68078238435662,22.0093058672959));
#16988=CARTESIAN_POINT('Ctrl Pts',(1.7889335758828,2.68064063969209,22.0092901485569));
#16989=CARTESIAN_POINT('Ctrl Pts',(1.78903743022243,2.68057132927904,22.0092824628363));
#16990=CARTESIAN_POINT('Ctrl Pts',(1.78924105001169,2.68043542019606,22.0092673929587));
#16991=CARTESIAN_POINT('Ctrl Pts',(1.78934081577337,2.68036882198999,22.0092600088193));
#16992=CARTESIAN_POINT('Ctrl Pts',(1.78953678895431,2.68023798511654,22.0092455029544));
#16993=CARTESIAN_POINT('Ctrl Pts',(1.78963299664239,2.6801737468327,22.0092383812429));
#16994=CARTESIAN_POINT('Ctrl Pts',(1.78982231271286,2.68004732494618,22.0092243663532));
#16995=CARTESIAN_POINT('Ctrl Pts',(1.78991542132132,2.67998514166629,22.0092174731868));
#16996=CARTESIAN_POINT('Ctrl Pts',(1.79009894011211,2.67986256344072,22.0092038857921));
#16997=CARTESIAN_POINT('Ctrl Pts',(1.79018935049083,2.67980216876373,22.0091971915734));
#16998=CARTESIAN_POINT('Ctrl Pts',(1.79036782611743,2.67968293290854,22.0091839759859));
#16999=CARTESIAN_POINT('Ctrl Pts',(1.79045589151262,2.67962409196991,22.0091774546265));
#17000=CARTESIAN_POINT('Ctrl Pts',(1.79062999123189,2.6795077547394,22.0091645615606));
#17001=CARTESIAN_POINT('Ctrl Pts',(1.79071602566652,2.67945025865919,22.0091581898631));
#17002=CARTESIAN_POINT('Ctrl Pts',(1.79099388431743,2.67926454872842,22.0091376105219));
#17003=CARTESIAN_POINT('Ctrl Pts',(1.79118569753948,2.67913631841781,22.0091234022527));
#17004=CARTESIAN_POINT('Ctrl Pts',(1.79156939066867,2.6788797535923,22.0090949771682));
#17005=CARTESIAN_POINT('Ctrl Pts',(1.79176127054781,2.67875141906682,22.0090807603532));
#17006=CARTESIAN_POINT('Ctrl Pts',(1.79214538799836,2.67849445104486,22.0090522966071));
#17007=CARTESIAN_POINT('Ctrl Pts',(1.79233762551632,2.67836581746414,22.0090380496727));
#17008=CARTESIAN_POINT('Ctrl Pts',(1.79272273506006,2.67810806570047,22.0090095051474));
#17009=CARTESIAN_POINT('Ctrl Pts',(1.79291560699319,2.67797894737269,22.0089952075509));
#17010=CARTESIAN_POINT('Ctrl Pts',(1.80340648599425,2.67095417552641,22.0082174193466));
#17011=CARTESIAN_POINT('Ctrl Pts',(1.81366452662376,2.66399927542424,22.0074516857675));
#17012=CARTESIAN_POINT('Ctrl Pts',(1.84539382376048,2.64221876609504,22.0050667876261));
#17013=CARTESIAN_POINT('Ctrl Pts',(1.86672490895186,2.62719173687639,22.0034399535533));
#17014=CARTESIAN_POINT('Ctrl Pts',(2.05440155226368,2.49154022336499,21.9889129138892));
#17015=CARTESIAN_POINT('Ctrl Pts',(2.20900862282055,2.35554484432636,21.9753926897263));
#17016=CARTESIAN_POINT('Ctrl Pts',(2.52132880371376,2.02286214952885,21.9446692896455));
#17017=CARTESIAN_POINT('Ctrl Pts',(2.67111581519442,1.82050118546984,21.9274017204445));
#17018=CARTESIAN_POINT('Ctrl Pts',(2.80647432485881,1.58438324492992,21.9100271370072));
#17019=CARTESIAN_POINT('Ctrl Pts',(2.81685238460383,1.56585794456482,21.9086815099155));
#17020=CARTESIAN_POINT('Ctrl Pts',(2.83114285715885,1.53974688552513,21.906810776752));
#17021=CARTESIAN_POINT('Ctrl Pts',(2.83520912492648,1.5322465764312,21.9062763821614));
#17022=CARTESIAN_POINT('Ctrl Pts',(2.84172308973391,1.52011672740408,21.9054170214908));
#17023=CARTESIAN_POINT('Ctrl Pts',(2.84418933805486,1.51549727610832,21.9050908866655));
#17024=CARTESIAN_POINT('Ctrl Pts',(2.84935108089058,1.50577199957431,21.9044067024821));
#17025=CARTESIAN_POINT('Ctrl Pts',(2.85204412901494,1.50066491389003,21.9040488156069));
#17026=CARTESIAN_POINT('Ctrl Pts',(2.85858644406345,1.48817687076824,21.9031770502427));
#17027=CARTESIAN_POINT('Ctrl Pts',(2.86242089972674,1.48078811897645,21.9026641065641));
#17028=CARTESIAN_POINT('Ctrl Pts',(2.87605793273143,1.45425951856528,21.900832327141));
#17029=CARTESIAN_POINT('Ctrl Pts',(2.88569777376022,1.43503602593669,21.8995233504325));
#17030=CARTESIAN_POINT('Ctrl Pts',(2.96660010267425,1.26959055024847,21.8884021931337));
#17031=CARTESIAN_POINT('Ctrl Pts',(3.02689960620394,1.11824370915806,21.8791827574043));
#17032=CARTESIAN_POINT('Ctrl Pts',(3.15335679161336,0.714368169763034,21.8554513473008));
#17033=CARTESIAN_POINT('Ctrl Pts',(3.20076165487119,0.45726867794257,21.8411029445533));
#17034=CARTESIAN_POINT('Ctrl Pts',(3.21956011058785,0.150742852665705,21.8229367508855));
#17035=CARTESIAN_POINT('Ctrl Pts',(3.22140363024258,0.104158682245796,21.8201506984579));
#17036=CARTESIAN_POINT('Ctrl Pts',(3.22246428113639,0.0447753340969706,
21.8165606977749));
#17037=CARTESIAN_POINT('Ctrl Pts',(3.22261649317016,0.0319969438730099,
21.8157859246616));
#17038=CARTESIAN_POINT('Ctrl Pts',(3.22273083041161,0.0128237021512873,
21.8146199070751));
#17039=CARTESIAN_POINT('Ctrl Pts',(3.22274993082051,0.00642922219497983,
21.8142304413701));
#17040=CARTESIAN_POINT('Ctrl Pts',(3.22274999981242,3.47713463869469E-5,
21.8138403813771));
#17041=CARTESIAN_POINT('Ctrl Pts',(-1.47286814312172,-2.86060451358776,
21.4037167033623));
#17042=CARTESIAN_POINT('Ctrl Pts',(-0.960639331001378,-3.1231473602644,
21.4391135850969));
#17043=CARTESIAN_POINT('Ctrl Pts',(0.704518003503453,-3.50470367487752,
21.5408214462859));
#17044=CARTESIAN_POINT('Ctrl Pts',(2.81881824515291,-2.1837009951111,21.6765070282561));
#17045=CARTESIAN_POINT('Ctrl Pts',(3.21708968004072,-0.552330809057621,
21.7767957284918));
#17046=CARTESIAN_POINT('Ctrl Pts',(3.2174269477886,0.000221517408381389,
21.8107734492731));
#17047=CARTESIAN_POINT('',(3.22274864473311,-0.00295556608512274,21.5646308008574));
#17048=CARTESIAN_POINT('Ctrl Pts',(-1.47525512068015,-2.86526436675693,
21.1585511949183));
#17049=CARTESIAN_POINT('Ctrl Pts',(-1.33950807638485,-2.93515722709376,
21.1671466307572));
#17050=CARTESIAN_POINT('Ctrl Pts',(-1.19884492489093,-2.99537723415258,
21.1755968604717));
#17051=CARTESIAN_POINT('Ctrl Pts',(-0.899465629869808,-3.09902033723927,
21.1934919964054));
#17052=CARTESIAN_POINT('Ctrl Pts',(-0.740786060354651,-3.14073097250001,
21.2029340534885));
#17053=CARTESIAN_POINT('Ctrl Pts',(-0.558089735586257,-3.17413502792007,
21.2141048776658));
#17054=CARTESIAN_POINT('Ctrl Pts',(-0.536504182726207,-3.17785470940248,
21.2154290499623));
#17055=CARTESIAN_POINT('Ctrl Pts',(-0.501958106984388,-3.18344578158891,
21.2175559122077));
#17056=CARTESIAN_POINT('Ctrl Pts',(-0.489020949228741,-3.18545875640527,
21.2183541012963));
#17057=CARTESIAN_POINT('Ctrl Pts',(-0.466103564706559,-3.18888171882243,
21.2197711951427));
#17058=CARTESIAN_POINT('Ctrl Pts',(-0.456128258359685,-3.19032383276872,
21.2203890709369));
#17059=CARTESIAN_POINT('Ctrl Pts',(-0.435402827530088,-3.19322088506343,
21.2216750710259));
#17060=CARTESIAN_POINT('Ctrl Pts',(-0.424651807406015,-3.19466838355501,
21.222343422996));
#17061=CARTESIAN_POINT('Ctrl Pts',(-0.39686473737466,-3.19826684230201,
21.2240741875394));
#17062=CARTESIAN_POINT('Ctrl Pts',(-0.379818605891042,-3.20033595464038,
21.225139176916));
#17063=CARTESIAN_POINT('Ctrl Pts',(-0.308115007466941,-3.20845862817185,
21.2296331346792));
#17064=CARTESIAN_POINT('Ctrl Pts',(-0.253326450116323,-3.21324862636154,
21.233101655442));
#17065=CARTESIAN_POINT('Ctrl Pts',(-0.108743703005732,-3.22216841205644,
21.2423517675451));
#17066=CARTESIAN_POINT('Ctrl Pts',(-0.0188576932707636,-3.22394734568775,
21.248201726647));
#17067=CARTESIAN_POINT('Ctrl Pts',(0.32913764104249,-3.21628111846667,21.2712055080523));
#17068=CARTESIAN_POINT('Ctrl Pts',(0.585647945511776,-3.17959032228132,
21.289011533561));
#17069=CARTESIAN_POINT('Ctrl Pts',(0.838613857033333,-3.11172913699444,
21.3063582333857));
#17070=CARTESIAN_POINT('Ctrl Pts',(0.842208054769976,-3.11075827024362,
21.3066046337369));
#17071=CARTESIAN_POINT('Ctrl Pts',(0.920165065851668,-3.08955546496622,
21.3119474498516));
#17072=CARTESIAN_POINT('Ctrl Pts',(0.993787133678537,-3.06666691940676,
21.316963441133));
#17073=CARTESIAN_POINT('Ctrl Pts',(1.07800331495973,-3.03713259557178,21.3226122754996));
#17074=CARTESIAN_POINT('Ctrl Pts',(1.08946019955861,-3.03304171331183,21.3233788028289));
#17075=CARTESIAN_POINT('Ctrl Pts',(1.1077345490467,-3.02639962800358,21.3245980238515));
#17076=CARTESIAN_POINT('Ctrl Pts',(1.11456687938823,-3.02389007957721,21.3250530905193));
#17077=CARTESIAN_POINT('Ctrl Pts',(1.12665525077406,-3.01940342477296,21.3258567945723));
#17078=CARTESIAN_POINT('Ctrl Pts',(1.13191469660646,-3.01743570223392,21.3262059853068));
#17079=CARTESIAN_POINT('Ctrl Pts',(1.14306127972063,-3.01323217303237,21.3269449841012));
#17080=CARTESIAN_POINT('Ctrl Pts',(1.14894700354903,-3.01099285991152,21.3273345782617));
#17081=CARTESIAN_POINT('Ctrl Pts',(1.16464103778939,-3.00496910775478,21.3283718565764));
#17082=CARTESIAN_POINT('Ctrl Pts',(1.17443755662519,-3.00115386446673,21.329017717207));
#17083=CARTESIAN_POINT('Ctrl Pts',(1.2221666206223,-2.98229633681415,21.3321572309124));
#17084=CARTESIAN_POINT('Ctrl Pts',(1.25983171720971,-2.96658171880922,21.3346126650525));
#17085=CARTESIAN_POINT('Ctrl Pts',(1.36720005157037,-2.91937160855032,21.3415761941654));
#17086=CARTESIAN_POINT('Ctrl Pts',(1.43609691118943,-2.88610357271859,21.3460005577997));
#17087=CARTESIAN_POINT('Ctrl Pts',(1.65816342658134,-2.76895132924326,21.3603187328803));
#17088=CARTESIAN_POINT('Ctrl Pts',(1.80570754010328,-2.67507424181031,21.3699390637197));
#17089=CARTESIAN_POINT('Ctrl Pts',(2.09125523990477,-2.45895253000787,21.3900784150237));
#17090=CARTESIAN_POINT('Ctrl Pts',(2.22783781776974,-2.33591979532386,21.4005880111145));
#17091=CARTESIAN_POINT('Ctrl Pts',(2.36837593722782,-2.18572785803136,21.4129564952059));
#17092=CARTESIAN_POINT('Ctrl Pts',(2.38338261920232,-2.16935430533993,21.4142989408526));
#17093=CARTESIAN_POINT('Ctrl Pts',(2.40702432127102,-2.14301778947604,21.4164495998106));
#17094=CARTESIAN_POINT('Ctrl Pts',(2.41576968775737,-2.1331545037367,21.4172531498078));
#17095=CARTESIAN_POINT('Ctrl Pts',(2.43110390863767,-2.11564487131514,21.4186764612445));
#17096=CARTESIAN_POINT('Ctrl Pts',(2.43771785326446,-2.10802065936518,21.419295163645));
#17097=CARTESIAN_POINT('Ctrl Pts',(2.45134110985849,-2.09216662447021,21.420579618525));
#17098=CARTESIAN_POINT('Ctrl Pts',(2.45834503832784,-2.08393236200208,21.4212455824865));
#17099=CARTESIAN_POINT('Ctrl Pts',(2.47625568841935,-2.06265951807285,21.4229632053543));
#17100=CARTESIAN_POINT('Ctrl Pts',(2.48710081044941,-2.04956972624567,21.4240173672019));
#17101=CARTESIAN_POINT('Ctrl Pts',(2.53147277884801,-1.99514307719448,21.4283897737));
#17102=CARTESIAN_POINT('Ctrl Pts',(2.56407504241998,-1.95306655282825,21.4317448886286));
#17103=CARTESIAN_POINT('Ctrl Pts',(2.6768404675664,-1.79983889683936,21.4438823209671));
#17104=CARTESIAN_POINT('Ctrl Pts',(2.75093057672508,-1.68441916529371,21.4528859333923));
#17105=CARTESIAN_POINT('Ctrl Pts',(2.87096507175701,-1.46827427041668,21.4694296951672));
#17106=CARTESIAN_POINT('Ctrl Pts',(2.91950367172001,-1.36922117344101,21.4768991879181));
#17107=CARTESIAN_POINT('Ctrl Pts',(3.03429855343958,-1.10096044481153,21.4966461558731));
#17108=CARTESIAN_POINT('Ctrl Pts',(3.09150258183659,-0.92828287185256,21.508884305806));
#17109=CARTESIAN_POINT('Ctrl Pts',(3.13730125473036,-0.737343887368482,
21.5213310729406));
#17110=CARTESIAN_POINT('Ctrl Pts',(3.14064352229288,-0.722975419068099,
21.5222611186853));
#17111=CARTESIAN_POINT('Ctrl Pts',(3.14545813538205,-0.701613666799873,
21.5236335390728));
#17112=CARTESIAN_POINT('Ctrl Pts',(3.14700601629606,-0.694637858609409,
21.5240800875861));
#17113=CARTESIAN_POINT('Ctrl Pts',(3.14972282611667,-0.682198574760167,
21.524873412208));
#17114=CARTESIAN_POINT('Ctrl Pts',(3.15090075822329,-0.676737164818766,
21.525220698444));
#17115=CARTESIAN_POINT('Ctrl Pts',(3.15340886380438,-0.664959966208358,
21.5259673920913));
#17116=CARTESIAN_POINT('Ctrl Pts',(3.15473426512354,-0.658643254852206,
21.5263665242143));
#17117=CARTESIAN_POINT('Ctrl Pts',(3.15742019752989,-0.645648284617995,
21.527184923401));
#17118=CARTESIAN_POINT('Ctrl Pts',(3.15877853968128,-0.638969600537329,
21.5276040657581));
#17119=CARTESIAN_POINT('Ctrl Pts',(3.16217827962945,-0.621977983445314,
21.5286668132887));
#17120=CARTESIAN_POINT('Ctrl Pts',(3.16419043798832,-0.611659188647948,
21.5293088245528));
#17121=CARTESIAN_POINT('Ctrl Pts',(3.20361203272885,-0.404094879550618,
21.5421584531868));
#17122=CARTESIAN_POINT('Ctrl Pts',(3.22256448354999,-0.203764881871651,
21.5534055260314));
#17123=CARTESIAN_POINT('Ctrl Pts',(3.22274864473311,-0.00295556608512274,
21.5646308008574));
#17124=CARTESIAN_POINT('Ctrl Pts',(3.22274864368595,-0.00295670769533594,
21.5646307370412));
#17125=CARTESIAN_POINT('Ctrl Pts',(3.22295282629112,0.219597998984461,21.5770715831944));
#17126=CARTESIAN_POINT('Ctrl Pts',(3.20010444854947,0.441562064382687,21.5894492096769));
#17127=CARTESIAN_POINT('Ctrl Pts',(3.14673634528828,0.69687401531595,21.6048156091233));
#17128=CARTESIAN_POINT('Ctrl Pts',(3.13823688387506,0.734201676282312,21.6070896830952));
#17129=CARTESIAN_POINT('Ctrl Pts',(3.12429679400706,0.790750022564981,21.6105811709925));
#17130=CARTESIAN_POINT('Ctrl Pts',(3.11933890778647,0.810086912924945,21.6117834248368));
#17131=CARTESIAN_POINT('Ctrl Pts',(3.10979440434312,0.845925306397751,21.614027806844));
#17132=CARTESIAN_POINT('Ctrl Pts',(3.10525525136024,0.86243879062455,21.6150683829872));
#17133=CARTESIAN_POINT('Ctrl Pts',(3.09762897389315,0.889342322691042,21.616774491472));
#17134=CARTESIAN_POINT('Ctrl Pts',(3.09462063337281,0.899754498625532,21.6174374463735));
#17135=CARTESIAN_POINT('Ctrl Pts',(3.08871236438747,0.919823435719477,21.6187204808833));
#17136=CARTESIAN_POINT('Ctrl Pts',(3.08581952256584,0.929482164047732,21.6193403217328));
#17137=CARTESIAN_POINT('Ctrl Pts',(3.07905938034888,0.951673747629037,21.6207699237972));
#17138=CARTESIAN_POINT('Ctrl Pts',(3.07516081999333,0.964196822564485,21.6215807050466));
#17139=CARTESIAN_POINT('Ctrl Pts',(3.06452385157253,0.997644406488598,21.623757177833));
#17140=CARTESIAN_POINT('Ctrl Pts',(3.05764770551607,1.01852406399257,21.6251273900306));
#17141=CARTESIAN_POINT('Ctrl Pts',(2.97678679442496,1.25586026475295,21.6408371547048));
#17142=CARTESIAN_POINT('Ctrl Pts',(2.88018608059178,1.46387664779887,21.6559615330626));
#17143=CARTESIAN_POINT('Ctrl Pts',(2.70765625881592,1.75100442390043,21.6785803442124));
#17144=CARTESIAN_POINT('Ctrl Pts',(2.64842710458284,1.83936209436748,21.6858011659358));
#17145=CARTESIAN_POINT('Ctrl Pts',(2.51373232281548,2.02026837872625,21.700979927261));
#17146=CARTESIAN_POINT('Ctrl Pts',(2.43726475125761,2.11189033486796,21.7089097039046));
#17147=CARTESIAN_POINT('Ctrl Pts',(2.33895678800487,2.21720868162038,21.7181355393821));
#17148=CARTESIAN_POINT('Ctrl Pts',(2.32181664457092,2.23515116972683,21.7197113277131));
#17149=CARTESIAN_POINT('Ctrl Pts',(2.29973084143584,2.25774258635489,21.7216985157936));
#17150=CARTESIAN_POINT('Ctrl Pts',(2.29497596244741,2.26257571432059,21.7221238319612));
#17151=CARTESIAN_POINT('Ctrl Pts',(2.28568246253389,2.27196271496768,21.7229501835752));
#17152=CARTESIAN_POINT('Ctrl Pts',(2.28114539962296,2.27651807926786,21.7233513350811));
#17153=CARTESIAN_POINT('Ctrl Pts',(2.27263773403242,2.2850090910286,21.7240992656313));
#17154=CARTESIAN_POINT('Ctrl Pts',(2.26867056720638,2.2889479405013,21.7244462939011));
#17155=CARTESIAN_POINT('Ctrl Pts',(2.25958292584611,2.29792387884901,21.7252373095417));
#17156=CARTESIAN_POINT('Ctrl Pts',(2.25445585761577,2.30295417674287,21.7256807614283));
#17157=CARTESIAN_POINT('Ctrl Pts',(2.23861198667107,2.31839538667485,21.7270426298571));
#17158=CARTESIAN_POINT('Ctrl Pts',(2.22783938872911,2.32874912212685,21.7279566866643));
#17159=CARTESIAN_POINT('Ctrl Pts',(2.1205391453096,2.4304512467272,21.7369488467762));
#17160=CARTESIAN_POINT('Ctrl Pts',(2.01850774736131,2.51583284858812,21.7446097803966));
#17161=CARTESIAN_POINT('Ctrl Pts',(1.73102869093033,2.72761684924705,21.7648130241963));
#17162=CARTESIAN_POINT('Ctrl Pts',(1.53720297659449,2.84136638498967,21.7770803494871));
#17163=CARTESIAN_POINT('Ctrl Pts',(1.22818359270064,2.98177341482338,21.7965542219053));
#17164=CARTESIAN_POINT('Ctrl Pts',(1.12075412501294,3.02379124447066,21.8033010148054));
#17165=CARTESIAN_POINT('Ctrl Pts',(0.990978726205584,3.06668181516498,21.8115360485272));
#17166=CARTESIAN_POINT('Ctrl Pts',(0.970578767855779,3.07319914951331,21.8128328261443));
#17167=CARTESIAN_POINT('Ctrl Pts',(0.93849983260424,3.08309639808588,21.8148761928178));
#17168=CARTESIAN_POINT('Ctrl Pts',(0.926863867253536,3.0866144399477,21.8156182376361));
#17169=CARTESIAN_POINT('Ctrl Pts',(0.905666518172883,3.09289261932481,21.8169716976677));
#17170=CARTESIAN_POINT('Ctrl Pts',(0.896111683248289,3.09567447326493,21.817582392299));
#17171=CARTESIAN_POINT('Ctrl Pts',(0.875464235851754,3.10158229790063,21.8189034597646));
#17172=CARTESIAN_POINT('Ctrl Pts',(0.86436746181194,3.10469310308352,21.8196143186824));
#17173=CARTESIAN_POINT('Ctrl Pts',(0.834248176430598,3.112962577351,21.821546214587));
#17174=CARTESIAN_POINT('Ctrl Pts',(0.815194877462533,3.11800630399879,21.8227709705366));
#17175=CARTESIAN_POINT('Ctrl Pts',(0.72226220243879,3.14169710593575,21.8287584645775));
#17176=CARTESIAN_POINT('Ctrl Pts',(0.647788816692424,3.15789351661783,21.8335995835933));
#17177=CARTESIAN_POINT('Ctrl Pts',(0.541870914711993,3.17702413104094,21.8405499499866));
#17178=CARTESIAN_POINT('Ctrl Pts',(0.510846240653213,3.18216002648297,21.8425934826073));
#17179=CARTESIAN_POINT('Ctrl Pts',(0.228988224158424,3.22459138493855,21.8612258034302));
#17180=CARTESIAN_POINT('Ctrl Pts',(-0.0253405976808572,3.23260809533602,
21.8786177615519));
#17181=CARTESIAN_POINT('Ctrl Pts',(-0.357675158241974,3.20384033930764,
21.9009738786876));
#17182=CARTESIAN_POINT('Ctrl Pts',(-0.4371408368981,3.19396839345557,21.9062822783302));
#17183=CARTESIAN_POINT('Ctrl Pts',(-0.557680685416124,3.17441003154079,
21.9142028767085));
#17184=CARTESIAN_POINT('Ctrl Pts',(-0.599066495246496,3.16686067466407,
21.9168982172272));
#17185=CARTESIAN_POINT('Ctrl Pts',(-0.650813328018528,3.15637050398897,
21.9202281266089));
#17186=CARTESIAN_POINT('Ctrl Pts',(-0.661321207210347,3.15418563419551,
21.9209022132087));
#17187=CARTESIAN_POINT('Ctrl Pts',(-0.67797790443711,3.15063536289355,21.9219672077881));
#17188=CARTESIAN_POINT('Ctrl Pts',(-0.684133860205735,3.14930438220198,
21.9223600372643));
#17189=CARTESIAN_POINT('Ctrl Pts',(-0.695770929613101,3.14675259716486,
21.9231011241821));
#17190=CARTESIAN_POINT('Ctrl Pts',(-0.701252684778172,3.14553552941198,
21.923449579583));
#17191=CARTESIAN_POINT('Ctrl Pts',(-0.713831201254937,3.14270831179557,
21.924247716182));
#17192=CARTESIAN_POINT('Ctrl Pts',(-0.720925705135605,3.14108844941254,
21.924696833898));
#17193=CARTESIAN_POINT('Ctrl Pts',(-0.739860132272624,3.13669769114947,
21.925892832266));
#17194=CARTESIAN_POINT('Ctrl Pts',(-0.751690096958051,3.13388376139916,
21.9266373072449));
#17195=CARTESIAN_POINT('Ctrl Pts',(-0.838251190800964,3.11277558950185,
21.9320662977008));
#17196=CARTESIAN_POINT('Ctrl Pts',(-0.912328405000588,3.09187579131151,
21.9366117456639));
#17197=CARTESIAN_POINT('Ctrl Pts',(-1.01944935674911,3.05746710897152,21.9431311272733));
#17198=CARTESIAN_POINT('Ctrl Pts',(-1.05312470906741,3.04603194245208,21.9451726580142));
#17199=CARTESIAN_POINT('Ctrl Pts',(-1.29679423462334,2.95876468941543,21.9599315535288));
#17200=CARTESIAN_POINT('Ctrl Pts',(-1.49859496734826,2.86184968974938,21.9721255693895));
#17201=CARTESIAN_POINT('Ctrl Pts',(-1.7670368015759,2.6966913951922,21.9900692075541));
#17202=CARTESIAN_POINT('Ctrl Pts',(-1.84320972511707,2.64521067585503,21.9953738345733));
#17203=CARTESIAN_POINT('Ctrl Pts',(-1.96215709237816,2.55718644597886,22.0040995425003));
#17204=CARTESIAN_POINT('Ctrl Pts',(-2.00635836832358,2.52265504906626,22.0074471593772));
#17205=CARTESIAN_POINT('Ctrl Pts',(-2.06288515274036,2.47606891137863,22.0118797377743));
#17206=CARTESIAN_POINT('Ctrl Pts',(-2.07604831800045,2.46504275234092,22.0129230182015));
#17207=CARTESIAN_POINT('Ctrl Pts',(-2.09738259994558,2.44687994628014,22.0146324442743));
#17208=CARTESIAN_POINT('Ctrl Pts',(-2.10560701442335,2.43980620917381,22.0152959930562));
#17209=CARTESIAN_POINT('Ctrl Pts',(-2.12140365397103,2.42608031336815,22.0165793922412));
#17210=CARTESIAN_POINT('Ctrl Pts',(-2.1289807040943,2.4194338816973,22.0171989996714));
#17211=CARTESIAN_POINT('Ctrl Pts',(-2.14632859348215,2.40407207815753,22.018626937528));
#17212=CARTESIAN_POINT('Ctrl Pts',(-2.156077698355,2.39533253196708,22.019436280278));
#17213=CARTESIAN_POINT('Ctrl Pts',(-2.18199361258413,2.37181390900654,22.0216063841181));
#17214=CARTESIAN_POINT('Ctrl Pts',(-2.19806323658842,2.35692921277075,22.0229716244587));
#17215=CARTESIAN_POINT('Ctrl Pts',(-2.33307114566668,2.22929480060283,22.0346115595203));
#17216=CARTESIAN_POINT('Ctrl Pts',(-2.44338256528359,2.10780531015908,22.0452736337356));
#17217=CARTESIAN_POINT('Ctrl Pts',(-2.69985356445187,1.77802891565876,22.0731374537039));
#17218=CARTESIAN_POINT('Ctrl Pts',(-2.83149784131443,1.55987539728716,22.0906649940966));
#17219=CARTESIAN_POINT('Ctrl Pts',(-2.95941181492372,1.27717557502508,22.1109648388526));
#17220=CARTESIAN_POINT('Ctrl Pts',(-2.98130184259496,1.22520854647347,22.1146004542298));
#17221=CARTESIAN_POINT('Ctrl Pts',(-3.00606652050387,1.1618166462215,22.118898230362));
#17222=CARTESIAN_POINT('Ctrl Pts',(-3.0102554097266,1.15091972925438,22.1196321841571));
#17223=CARTESIAN_POINT('Ctrl Pts',(-3.01668630368315,1.13391517742121,22.1207697475211));
#17224=CARTESIAN_POINT('Ctrl Pts',(-3.01896913263,1.12782324076915,22.1211757380117));
#17225=CARTESIAN_POINT('Ctrl Pts',(-3.02317605894916,1.11649237628293,22.1219279472487));
#17226=CARTESIAN_POINT('Ctrl Pts',(-3.02510497612679,1.11125541340866,22.1222744442827));
#17227=CARTESIAN_POINT('Ctrl Pts',(-3.02944757651277,1.09937025869898,22.1230581985766));
#17228=CARTESIAN_POINT('Ctrl Pts',(-3.03185297887558,1.09271913193039,22.1234949584975));
#17229=CARTESIAN_POINT('Ctrl Pts',(-3.03892694265621,1.07295587966443,22.1247874445107));
#17230=CARTESIAN_POINT('Ctrl Pts',(-3.0435325500688,1.05982117141884,22.1256395155764));
#17231=CARTESIAN_POINT('Ctrl Pts',(-3.07785030995952,0.959881673521503,
22.1320733059404));
#17232=CARTESIAN_POINT('Ctrl Pts',(-3.10393147585281,0.871864739967578,
22.1374575030244));
#17233=CARTESIAN_POINT('Ctrl Pts',(-3.18528373571642,0.546992208606677,
22.1567145906095));
#17234=CARTESIAN_POINT('Ctrl Pts',(-3.21746735844233,0.305204731909847,
22.1699314351238));
#17235=CARTESIAN_POINT('Ctrl Pts',(-3.22392200778803,-0.0297789318281736,
22.1890062553779));
#17236=CARTESIAN_POINT('Ctrl Pts',(-3.22176255867939,-0.121671627717367,
22.194309786876));
#17237=CARTESIAN_POINT('Ctrl Pts',(-3.21196866190613,-0.269294113501907,
22.2030338572505));
#17238=CARTESIAN_POINT('Ctrl Pts',(-3.20679703277196,-0.325137231871912,
22.2063809681983));
#17239=CARTESIAN_POINT('Ctrl Pts',(-3.19814263192213,-0.397864399675196,
22.2108129698619));
#17240=CARTESIAN_POINT('Ctrl Pts',(-3.195977543996,-0.414897451391854,22.2118561932592));
#17241=CARTESIAN_POINT('Ctrl Pts',(-3.1922226605767,-0.442662086495636,
22.2135655493634));
#17242=CARTESIAN_POINT('Ctrl Pts',(-3.19071458648495,-0.453404521991138,
22.2142290856169));
#17243=CARTESIAN_POINT('Ctrl Pts',(-3.18770072665389,-0.474113097061738,
22.2155124770625));
#17244=CARTESIAN_POINT('Ctrl Pts',(-3.18620236428957,-0.484080201647737,
22.2161320893705));
#17245=CARTESIAN_POINT('Ctrl Pts',(-3.18265008980904,-0.506978704304749,
22.2175600621141));
#17246=CARTESIAN_POINT('Ctrl Pts',(-3.18056408718891,-0.519904875848573,
22.2183694350351));
#17247=CARTESIAN_POINT('Ctrl Pts',(-3.17477774499518,-0.554421939029222,
22.2205396723911));
#17248=CARTESIAN_POINT('Ctrl Pts',(-3.17093599157242,-0.575988121122701,
22.221905016943));
#17249=CARTESIAN_POINT('Ctrl Pts',(-3.13647413144644,-0.758639188682412,
22.2335502534206));
#17250=CARTESIAN_POINT('Ctrl Pts',(-3.09382621544345,-0.9171848398229,22.2442179330315));
#17251=CARTESIAN_POINT('Ctrl Pts',(-2.9548060603783,-1.31141319276203,22.2720993486826));
#17252=CARTESIAN_POINT('Ctrl Pts',(-2.84226314543941,-1.54020091533875,
22.2896392452633));
#17253=CARTESIAN_POINT('Ctrl Pts',(-2.67347616072602,-1.80049849873391,
22.3099325313362));
#17254=CARTESIAN_POINT('Ctrl Pts',(-2.64170245852142,-1.84680227835355,
22.3135528176121));
#17255=CARTESIAN_POINT('Ctrl Pts',(-2.60188667582506,-1.90169378285213,
22.3178349670948));
#17256=CARTESIAN_POINT('Ctrl Pts',(-2.59498915959727,-1.91109518050673,
22.3185680279477));
#17257=CARTESIAN_POINT('Ctrl Pts',(-2.58416578109671,-1.92568093421766,
22.3197045113805));
#17258=CARTESIAN_POINT('Ctrl Pts',(-2.5802750789569,-1.93089108012031,22.3201103077295));
#17259=CARTESIAN_POINT('Ctrl Pts',(-2.57301559457092,-1.94055132975122,
22.3208623416454));
#17260=CARTESIAN_POINT('Ctrl Pts',(-2.56965105406861,-1.94500441499229,
22.3212088563431));
#17261=CARTESIAN_POINT('Ctrl Pts',(-2.56199409194724,-1.95508412013192,
22.3219928853447));
#17262=CARTESIAN_POINT('Ctrl Pts',(-2.557694705479,-1.96070534241777,22.3224299008504));
#17263=CARTESIAN_POINT('Ctrl Pts',(-2.54487271110028,-1.97735548534706,
22.3237238450113));
#17264=CARTESIAN_POINT('Ctrl Pts',(-2.53629690409943,-1.98834349690016,
22.3245771063966));
#17265=CARTESIAN_POINT('Ctrl Pts',(-2.47036674278148,-2.07169786429477,
22.3310478300525));
#17266=CARTESIAN_POINT('Ctrl Pts',(-2.40999153727165,-2.14163211295888,
22.3364651978303));
#17267=CARTESIAN_POINT('Ctrl Pts',(-2.180546989088,-2.38539117508947,22.355708484335));
#17268=CARTESIAN_POINT('Ctrl Pts',(-1.99501578242429,-2.54259732980843,
22.3688876917867));
#17269=CARTESIAN_POINT('Ctrl Pts',(-1.71720405350204,-2.72869629653299,
22.3879241436484));
#17270=CARTESIAN_POINT('Ctrl Pts',(-1.63865613057525,-2.7765765601685,22.3932316875754));
#17271=CARTESIAN_POINT('Ctrl Pts',(-1.53074825105566,-2.83617857605774,
22.4005007344283));
#17272=CARTESIAN_POINT('Ctrl Pts',(-1.50310616526436,-2.85092453600792,
22.4023607307207));
#17273=CARTESIAN_POINT('Ctrl Pts',(-1.47525540254685,-2.86526422163059,
22.4042343665403));
#17274=CARTESIAN_POINT('Origin',(0.,0.,4.68922655072688));
#17275=CARTESIAN_POINT('',(-1.47525540579296,-2.86526421995924,23.9007338658376));
#17276=CARTESIAN_POINT('',(-1.47525500221108,-2.86526442775378,23.6562919783988));
#17277=CARTESIAN_POINT('',(-1.47525540501186,-2.86526422036142,4.68922655072688));
#17278=CARTESIAN_POINT('Ctrl Pts',(-1.47525540579296,-2.86526421995924,
23.9007338658376));
#17279=CARTESIAN_POINT('Ctrl Pts',(-1.48875271027542,-2.85831478358173,
23.8997646385843));
#17280=CARTESIAN_POINT('Ctrl Pts',(-1.50220145552381,-2.85126969437684,
23.8988004124447));
#17281=CARTESIAN_POINT('Ctrl Pts',(-1.52589489557367,-2.83864375982311,
23.897105029872));
#17282=CARTESIAN_POINT('Ctrl Pts',(-1.53615950369407,-2.83310211897691,
23.8963716693393));
#17283=CARTESIAN_POINT('Ctrl Pts',(-1.55210108942648,-2.82438348745219,
23.8952347368373));
#17284=CARTESIAN_POINT('Ctrl Pts',(-1.55779879517731,-2.82124490101643,
23.894828789153));
#17285=CARTESIAN_POINT('Ctrl Pts',(-1.56836922331773,-2.81538038542728,
23.8940764818429));
#17286=CARTESIAN_POINT('Ctrl Pts',(-1.57324431774014,-2.81265907153875,
23.893729844854));
#17287=CARTESIAN_POINT('Ctrl Pts',(-1.58428490758782,-2.80645844629098,
23.8929455404901));
#17288=CARTESIAN_POINT('Ctrl Pts',(-1.59044601114441,-2.80297148880649,
23.892508372258));
#17289=CARTESIAN_POINT('Ctrl Pts',(-1.60870730267693,-2.79255667502932,
23.891213974424));
#17290=CARTESIAN_POINT('Ctrl Pts',(-1.62077426029396,-2.78557045906161,
23.8903604146455));
#17291=CARTESIAN_POINT('Ctrl Pts',(-1.71243620091211,-2.73170509875028,
23.8838872560959));
#17292=CARTESIAN_POINT('Ctrl Pts',(-1.79003590821606,-2.68149685281321,
23.8784678993994));
#17293=CARTESIAN_POINT('Ctrl Pts',(-2.0630153805818,-2.48773493809652,23.859225156025));
#17294=CARTESIAN_POINT('Ctrl Pts',(-2.24420385971488,-2.32560089572219,
23.8460479142645));
#17295=CARTESIAN_POINT('Ctrl Pts',(-2.46669661789865,-2.07604890384023,
23.8270142340914));
#17296=CARTESIAN_POINT('Ctrl Pts',(-2.52491456150852,-2.00483809378753,
23.8217073091781));
#17297=CARTESIAN_POINT('Ctrl Pts',(-2.6136276653639,-1.88632338112434,23.8129779418232));
#17298=CARTESIAN_POINT('Ctrl Pts',(-2.64606908504447,-1.84053885911269,
23.8096290323431));
#17299=CARTESIAN_POINT('Ctrl Pts',(-2.6868592157698,-1.7796629384393,23.8051947559183));
#17300=CARTESIAN_POINT('Ctrl Pts',(-2.69630647563498,-1.76531696629811,
23.8041511034358));
#17301=CARTESIAN_POINT('Ctrl Pts',(-2.71153419442991,-1.7417857611663,23.8024410694734));
#17302=CARTESIAN_POINT('Ctrl Pts',(-2.71738381780613,-1.73264552275831,
23.8017772867525));
#17303=CARTESIAN_POINT('Ctrl Pts',(-2.72857912661839,-1.71495631756338,
23.8004934355404));
#17304=CARTESIAN_POINT('Ctrl Pts',(-2.73393108272204,-1.70641145466359,
23.7998736102047));
#17305=CARTESIAN_POINT('Ctrl Pts',(-2.74614298890772,-1.68670916070973,
23.7984451695837));
#17306=CARTESIAN_POINT('Ctrl Pts',(-2.75297516010459,-1.6755348006101,23.7976355412705));
#17307=CARTESIAN_POINT('Ctrl Pts',(-2.7710547481496,-1.64555561019883,23.7954646653593));
#17308=CARTESIAN_POINT('Ctrl Pts',(-2.78217866129356,-1.62667745476488,
23.7940989353455));
#17309=CARTESIAN_POINT('Ctrl Pts',(-2.87493272628677,-1.46553159785942,
23.7824498804748));
#17310=CARTESIAN_POINT('Ctrl Pts',(-2.94577183589392,-1.31735895194564,
23.771778508006));
#17311=CARTESIAN_POINT('Ctrl Pts',(-3.09699272308924,-0.927116093120989,
23.7438635566282));
#17312=CARTESIAN_POINT('Ctrl Pts',(-3.1605184295348,-0.679725471421503,
23.7262919199643));
#17313=CARTESIAN_POINT('Ctrl Pts',(-3.20166293237947,-0.372253308075372,
23.7060050770208));
#17314=CARTESIAN_POINT('Ctrl Pts',(-3.20761717592135,-0.316876945858572,
23.7024152314184));
#17315=CARTESIAN_POINT('Ctrl Pts',(-3.21307732194036,-0.249773999825745,
23.6981639540094));
#17316=CARTESIAN_POINT('Ctrl Pts',(-3.2139581249819,-0.238172434101687,
23.697432503885));
#17317=CARTESIAN_POINT('Ctrl Pts',(-3.21523294183536,-0.220083894300012,
23.6962978821074));
#17318=CARTESIAN_POINT('Ctrl Pts',(-3.21567018579925,-0.213600207691208,
23.6958923500173));
#17319=CARTESIAN_POINT('Ctrl Pts',(-3.21644668269606,-0.201542751211144,
23.6951404170441));
#17320=CARTESIAN_POINT('Ctrl Pts',(-3.21679105756146,-0.195969476926079,
23.6947937412779));
#17321=CARTESIAN_POINT('Ctrl Pts',(-3.21753972307367,-0.183319223632285,
23.6940088444651));
#17322=CARTESIAN_POINT('Ctrl Pts',(-3.21793515095062,-0.176241805068105,
23.6935711257052));
#17323=CARTESIAN_POINT('Ctrl Pts',(-3.21904132884225,-0.155196901350837,
23.6922735843386));
#17324=CARTESIAN_POINT('Ctrl Pts',(-3.21968452484479,-0.141225818795976,
23.6914174580281));
#17325=CARTESIAN_POINT('Ctrl Pts',(-3.22393620534607,-0.0336317711185114,
23.6848618100823));
#17326=CARTESIAN_POINT('Ctrl Pts',(-3.22355171424692,0.060113775093909,
23.6793683455703));
#17327=CARTESIAN_POINT('Ctrl Pts',(-3.20759897087588,0.394187455297721,
23.6601550106887));
#17328=CARTESIAN_POINT('Ctrl Pts',(-3.16920797392257,0.632620013166034,
23.6470608257321));
#17329=CARTESIAN_POINT('Ctrl Pts',(-3.07991139420277,0.953280937335598,
23.6281122548646));
#17330=CARTESIAN_POINT('Ctrl Pts',(-3.05141588401044,1.04089284080986,23.6227970742574));
#17331=CARTESIAN_POINT('Ctrl Pts',(-2.99956384621368,1.17978367425377,23.6140553680762));
#17332=CARTESIAN_POINT('Ctrl Pts',(-2.97854638125127,1.23188216228027,23.6107026479809));
#17333=CARTESIAN_POINT('Ctrl Pts',(-2.94933581202357,1.29916555280818,23.6062640278208));
#17334=CARTESIAN_POINT('Ctrl Pts',(-2.94236657469603,1.31487329732081,23.605219946086));
#17335=CARTESIAN_POINT('Ctrl Pts',(-2.93079126862344,1.34040960132749,23.6035093854782));
#17336=CARTESIAN_POINT('Ctrl Pts',(-2.92626052308691,1.35027208592793,23.6028455084534));
#17337=CARTESIAN_POINT('Ctrl Pts',(-2.91742512242411,1.369251571109,23.6015615989215));
#17338=CARTESIAN_POINT('Ctrl Pts',(-2.91312732808619,1.37837163951038,23.6009418102373));
#17339=CARTESIAN_POINT('Ctrl Pts',(-2.903149595988,1.39928961865373,23.5995136319135));
#17340=CARTESIAN_POINT('Ctrl Pts',(-2.89744043801717,1.41107331969898,23.598704230462));
#17341=CARTESIAN_POINT('Ctrl Pts',(-2.88199132391127,1.44247119519334,23.596534358403));
#17342=CARTESIAN_POINT('Ctrl Pts',(-2.87212312011212,1.46202116425962,23.595169411892));
#17343=CARTESIAN_POINT('Ctrl Pts',(-2.78694188367448,1.62658321611399,23.5835601028071));
#17344=CARTESIAN_POINT('Ctrl Pts',(-2.70091150987591,1.76575209718652,23.5729307481273));
#17345=CARTESIAN_POINT('Ctrl Pts',(-2.45557125247942,2.10248263817414,23.545146443374));
#17346=CARTESIAN_POINT('Ctrl Pts',(-2.28282668360327,2.2888776074864,23.5276660902053));
#17347=CARTESIAN_POINT('Ctrl Pts',(-2.0463505639998,2.49035386858803,23.507330104981));
#17348=CARTESIAN_POINT('Ctrl Pts',(-2.00166338426604,2.52641201793135,23.5036263665698));
#17349=CARTESIAN_POINT('Ctrl Pts',(-1.94670460576587,2.56838403069828,23.4992590450277));
#17350=CARTESIAN_POINT('Ctrl Pts',(-1.93733660678491,2.57545767452516,23.4985209991513));
#17351=CARTESIAN_POINT('Ctrl Pts',(-1.92270459545324,2.58638108631401,23.4973784011217));
#17352=CARTESIAN_POINT('Ctrl Pts',(-1.91746730860678,2.59026624253812,23.4969714356072));
#17353=CARTESIAN_POINT('Ctrl Pts',(-1.90772531440475,2.59744737035686,23.4962182059047));
#17354=CARTESIAN_POINT('Ctrl Pts',(-1.9032238788766,2.60074750496953,23.4958716582934));
#17355=CARTESIAN_POINT('Ctrl Pts',(-1.89301121552978,2.60819399364402,23.4950887794584));
#17356=CARTESIAN_POINT('Ctrl Pts',(-1.88729494194033,2.61233328175545,23.4946529397857));
#17357=CARTESIAN_POINT('Ctrl Pts',(-1.87032817688808,2.62453455667243,23.4933661131065));
#17358=CARTESIAN_POINT('Ctrl Pts',(-1.85903912693928,2.63254300418508,23.4925187325518));
#17359=CARTESIAN_POINT('Ctrl Pts',(-1.77443800079849,2.69174340063261,23.4862310817583));
#17360=CARTESIAN_POINT('Ctrl Pts',(-1.69906817421084,2.73994219679098,23.4809783123533));
#17361=CARTESIAN_POINT('Ctrl Pts',(-1.40908674704744,2.90880972599167,23.4616610906431));
#17362=CARTESIAN_POINT('Ctrl Pts',(-1.18289324916057,3.00790247008734,23.4482908659303));
#17363=CARTESIAN_POINT('Ctrl Pts',(-0.860129455762939,3.10719688098047,
23.4290622701824));
#17364=CARTESIAN_POINT('Ctrl Pts',(-0.771545523450982,3.13036910503995,
23.4237782834243));
#17365=CARTESIAN_POINT('Ctrl Pts',(-0.627442167056525,3.16157579305901,
23.4150832101366));
#17366=CARTESIAN_POINT('Ctrl Pts',(-0.572488010865,3.17198708610934,23.411744902349));
#17367=CARTESIAN_POINT('Ctrl Pts',(-0.50035837014777,3.18371692151814,23.4073227125596));
#17368=CARTESIAN_POINT('Ctrl Pts',(-0.483402089809228,3.18633556562968,
23.4062802567528));
#17369=CARTESIAN_POINT('Ctrl Pts',(-0.455692701324049,3.19038859576823,
23.4045716909189));
#17370=CARTESIAN_POINT('Ctrl Pts',(-0.444951691057949,3.1919043247132,23.4039081710456));
#17371=CARTESIAN_POINT('Ctrl Pts',(-0.424211089088408,3.19472443339366,
23.4026244817923));
#17372=CARTESIAN_POINT('Ctrl Pts',(-0.414212612275054,3.19603616399614,
23.4020045537042));
#17373=CARTESIAN_POINT('Ctrl Pts',(-0.391204066117126,3.19894494361641,
23.4005753791653));
#17374=CARTESIAN_POINT('Ctrl Pts',(-0.378190147285311,3.20050958098428,
23.3997651162847));
#17375=CARTESIAN_POINT('Ctrl Pts',(-0.343362164731023,3.20448149153999,
23.3975914315978));
#17376=CARTESIAN_POINT('Ctrl Pts',(-0.321532748517927,3.20674536858439,
23.3962235091299));
#17377=CARTESIAN_POINT('Ctrl Pts',(-0.134621460510709,3.22420181814927,
23.3844618970442));
#17378=CARTESIAN_POINT('Ctrl Pts',(0.0313564630761837,3.22685634812576,
23.3736714333013));
#17379=CARTESIAN_POINT('Ctrl Pts',(0.455215587198073,3.20092719503514,23.3453341553017));
#17380=CARTESIAN_POINT('Ctrl Pts',(0.710791378113481,3.15403362566845,23.3274478114267));
#17381=CARTESIAN_POINT('Ctrl Pts',(1.00587878474419,3.06216265899071,23.3073012665032));
#17382=CARTESIAN_POINT('Ctrl Pts',(1.05340769754504,3.04613938704135,23.3040761364205));
#17383=CARTESIAN_POINT('Ctrl Pts',(1.11114255435295,3.02516229162713,23.300199134563));
#17384=CARTESIAN_POINT('Ctrl Pts',(1.12171877131148,3.02125663818086,23.2994906171829));
#17385=CARTESIAN_POINT('Ctrl Pts',(1.13828451505387,3.0150401543997,23.2983837619123));
#17386=CARTESIAN_POINT('Ctrl Pts',(1.14428788259771,3.01276683686317,23.2979832437277));
#17387=CARTESIAN_POINT('Ctrl Pts',(1.15551032170329,3.00847881086517,23.2972357148469));
#17388=CARTESIAN_POINT('Ctrl Pts',(1.16073088063015,3.00646847352917,23.296888459463));
#17389=CARTESIAN_POINT('Ctrl Pts',(1.17266227986133,3.00183820966729,23.2960959058726));
#17390=CARTESIAN_POINT('Ctrl Pts',(1.17936957636924,2.99920937320804,23.2956511500624));
#17391=CARTESIAN_POINT('Ctrl Pts',(1.20005521802352,2.99102178633977,23.2942817530546));
#17392=CARTESIAN_POINT('Ctrl Pts',(1.21400373849476,2.98538754535174,23.2933615402977));
#17393=CARTESIAN_POINT('Ctrl Pts',(1.36499757930785,2.92316316154815,23.2834295072034));
#17394=CARTESIAN_POINT('Ctrl Pts',(1.49803995606594,2.85726956071792,23.274937967947));
#17395=CARTESIAN_POINT('Ctrl Pts',(1.7809426066236,2.69193830402996,23.2564761480718));
#17396=CARTESIAN_POINT('Ctrl Pts',(1.92797198300684,2.58867008066652,23.2465897220523));
#17397=CARTESIAN_POINT('Ctrl Pts',(2.13900779772982,2.41244641903759,23.2309634626143));
#17398=CARTESIAN_POINT('Ctrl Pts',(2.20960228444923,2.34795819939839,23.2254560971678));
#17399=CARTESIAN_POINT('Ctrl Pts',(2.31803511588966,2.23967793582064,23.2164277445039));
#17400=CARTESIAN_POINT('Ctrl Pts',(2.35774326056414,2.19783760717109,23.2129870667544));
#17401=CARTESIAN_POINT('Ctrl Pts',(2.40790540192232,2.14205743894685,23.2084482725536));
#17402=CARTESIAN_POINT('Ctrl Pts',(2.41940060032458,2.12906533793723,23.2073944093924));
#17403=CARTESIAN_POINT('Ctrl Pts',(2.43793988712447,2.1077678354039,23.2056718450925));
#17404=CARTESIAN_POINT('Ctrl Pts',(2.44504785384933,2.09951830879859,23.2050058165746));
#17405=CARTESIAN_POINT('Ctrl Pts',(2.45864792505329,2.08357129455813,23.2037205467818));
#17406=CARTESIAN_POINT('Ctrl Pts',(2.46514603902508,2.07587908161381,23.2031015644378));
#17407=CARTESIAN_POINT('Ctrl Pts',(2.47995895730957,2.05817649263383,23.2016792285407));
#17408=CARTESIAN_POINT('Ctrl Pts',(2.48824935169024,2.04814600568415,23.2008748902739));
#17409=CARTESIAN_POINT('Ctrl Pts',(2.51015308774261,2.02131556056798,23.1987273814628));
#17410=CARTESIAN_POINT('Ctrl Pts',(2.52365830095084,2.00442856259152,23.1973798788996));
#17411=CARTESIAN_POINT('Ctrl Pts',(2.63005464137795,1.86861005134807,23.1865731667816));
#17412=CARTESIAN_POINT('Ctrl Pts',(2.71464438528026,1.74344062173389,23.1767877507673));
#17413=CARTESIAN_POINT('Ctrl Pts',(2.90306114011268,1.4174838026103,23.1517684696872));
#17414=CARTESIAN_POINT('Ctrl Pts',(2.99514153334151,1.21084359295108,23.1362746097849));
#17415=CARTESIAN_POINT('Ctrl Pts',(3.09173564680503,0.913691271382811,23.1154725986853));
#17416=CARTESIAN_POINT('Ctrl Pts',(3.11523825088789,0.830032815332193,23.1097762521839));
#17417=CARTESIAN_POINT('Ctrl Pts',(3.13970055603478,0.727154948565412,23.103043566939));
#17418=CARTESIAN_POINT('Ctrl Pts',(3.14390604538316,0.708751521121015,23.1018496750971));
#17419=CARTESIAN_POINT('Ctrl Pts',(3.14964199882737,0.682594506694165,23.1001686658204));
#17420=CARTESIAN_POINT('Ctrl Pts',(3.15130593303898,0.674871025362513,23.0996742653177));
#17421=CARTESIAN_POINT('Ctrl Pts',(3.15412014314777,0.661570936860086,23.0988263498159));
#17422=CARTESIAN_POINT('Ctrl Pts',(3.15528406786835,0.655997282738108,23.0984720588096));
#17423=CARTESIAN_POINT('Ctrl Pts',(3.15750978518016,0.645196072755283,23.0977875308402));
#17424=CARTESIAN_POINT('Ctrl Pts',(3.15857337140228,0.639968963512682,23.0974571878117));
#17425=CARTESIAN_POINT('Ctrl Pts',(3.16140438853635,0.625876640648765,23.0965690148814));
#17426=CARTESIAN_POINT('Ctrl Pts',(3.16314752195943,0.617006512198318,23.0960125652215));
#17427=CARTESIAN_POINT('Ctrl Pts',(3.16946162142782,0.584146383218771,23.093960347199));
#17428=CARTESIAN_POINT('Ctrl Pts',(3.17379731526415,0.560111284524072,23.0924773961873));
#17429=CARTESIAN_POINT('Ctrl Pts',(3.20756711307151,0.359906082999947,23.0802577253081));
#17430=CARTESIAN_POINT('Ctrl Pts',(3.22258585402157,0.181594249522542,23.0702174695967));
#17431=CARTESIAN_POINT('Ctrl Pts',(3.22284147777808,-0.0989148519579887,
23.0545274662005));
#17432=CARTESIAN_POINT('Ctrl Pts',(3.21810585105701,-0.200713015188227,
23.0488570418605));
#17433=CARTESIAN_POINT('Ctrl Pts',(3.19226216798212,-0.475181664647695,
23.0333220153033));
#17434=CARTESIAN_POINT('Ctrl Pts',(3.161993280815,-0.646623485682562,23.0233364748469));
#17435=CARTESIAN_POINT('Ctrl Pts',(3.11246721164436,-0.836154088841001,
23.0115559094806));
#17436=CARTESIAN_POINT('Ctrl Pts',(3.10666124681708,-0.857474002019736,
23.0102202533736));
#17437=CARTESIAN_POINT('Ctrl Pts',(3.09705070864397,-0.8913851173586,23.0080782917782));
#17438=CARTESIAN_POINT('Ctrl Pts',(3.0933874288049,-0.904015888481335,23.0072765880475));
#17439=CARTESIAN_POINT('Ctrl Pts',(3.08677684194699,-0.926298073510278,
23.005855248115));
#17440=CARTESIAN_POINT('Ctrl Pts',(3.08386130371733,-0.93595878580489,23.0052366597524));
#17441=CARTESIAN_POINT('Ctrl Pts',(3.07772312887552,-0.955957722521362,
23.003951154834));
#17442=CARTESIAN_POINT('Ctrl Pts',(3.07449366567224,-0.966293702981811,
23.0032840202717));
#17443=CARTESIAN_POINT('Ctrl Pts',(3.06603862197241,-0.992882771972261,
23.0015606358833));
#17444=CARTESIAN_POINT('Ctrl Pts',(3.06073592314277,-1.00911080710241,23.0005018524689));
#17445=CARTESIAN_POINT('Ctrl Pts',(3.03775570048504,-1.0775901547028,22.9960039567947));
#17446=CARTESIAN_POINT('Ctrl Pts',(3.01886802422476,-1.12942263245547,22.9925249697677));
#17447=CARTESIAN_POINT('Ctrl Pts',(2.96576367896452,-1.26428854014951,22.9832694525274));
#17448=CARTESIAN_POINT('Ctrl Pts',(2.92939239713902,-1.34641655279006,22.9774250204547));
#17449=CARTESIAN_POINT('Ctrl Pts',(2.7775155876934,-1.65398231035852,22.9547564098506));
#17450=CARTESIAN_POINT('Ctrl Pts',(2.63902914746187,-1.86701855753947,22.937310216342));
#17451=CARTESIAN_POINT('Ctrl Pts',(2.42248544806351,-2.1271944469441,22.9148472242023));
#17452=CARTESIAN_POINT('Ctrl Pts',(2.36533777002322,-2.19056431023942,22.9092782688143));
#17453=CARTESIAN_POINT('Ctrl Pts',(2.2961755887461,-2.26138951720568,22.9030097420775));
#17454=CARTESIAN_POINT('Ctrl Pts',(2.28655093236064,-2.27112080970236,22.9021474495248));
#17455=CARTESIAN_POINT('Ctrl Pts',(2.27189308446883,-2.2857534245131,22.9008497392909));
#17456=CARTESIAN_POINT('Ctrl Pts',(2.26690552636812,-2.29069994579695,22.9004108569802));
#17457=CARTESIAN_POINT('Ctrl Pts',(2.25792754650664,-2.29954601727544,22.8996257034039));
#17458=CARTESIAN_POINT('Ctrl Pts',(2.25394315354121,-2.30345153041103,22.8992789654171));
#17459=CARTESIAN_POINT('Ctrl Pts',(2.24526196853389,-2.31191675972358,22.8985272077707));
#17460=CARTESIAN_POINT('Ctrl Pts',(2.24056143511393,-2.31647250545193,22.898122497205));
#17461=CARTESIAN_POINT('Ctrl Pts',(2.22731035954894,-2.32923734801768,22.896988032879));
#17462=CARTESIAN_POINT('Ctrl Pts',(2.21872825697574,-2.33741374022947,22.8962607814737));
#17463=CARTESIAN_POINT('Ctrl Pts',(2.16687451582886,-2.38627322480307,22.8919100020742));
#17464=CARTESIAN_POINT('Ctrl Pts',(2.12252703318354,-2.42580401137874,22.888369035569));
#17465=CARTESIAN_POINT('Ctrl Pts',(1.88456453261065,-2.62639499312878,22.8701312708296));
#17466=CARTESIAN_POINT('Ctrl Pts',(1.67364355903417,-2.76558799224177,22.8564605816914));
#17467=CARTESIAN_POINT('Ctrl Pts',(1.30336323045572,-2.95191703952021,22.8330393530403));
#17468=CARTESIAN_POINT('Ctrl Pts',(1.15277208258352,-3.01391376466645,22.8236635865327));
#17469=CARTESIAN_POINT('Ctrl Pts',(0.977349803980756,-3.07105581845121,
22.8125666016822));
#17470=CARTESIAN_POINT('Ctrl Pts',(0.95647365042571,-3.07762158155267,22.8112435862415));
#17471=CARTESIAN_POINT('Ctrl Pts',(0.923006754674466,-3.08777386302082,
22.809118089944));
#17472=CARTESIAN_POINT('Ctrl Pts',(0.910457990425474,-3.09149723242082,
22.8083200988784));
#17473=CARTESIAN_POINT('Ctrl Pts',(0.888204862771429,-3.09795276235891,
22.8069030603088));
#17474=CARTESIAN_POINT('Ctrl Pts',(0.878509652988541,-3.10071604343185,
22.8062850398243));
#17475=CARTESIAN_POINT('Ctrl Pts',(0.85834826725502,-3.10636019375571,22.8049984420609));
#17476=CARTESIAN_POINT('Ctrl Pts',(0.847880195402882,-3.10923375944567,
22.8043296354802));
#17477=CARTESIAN_POINT('Ctrl Pts',(0.820795351329398,-3.11652180430177,
22.8025970533432));
#17478=CARTESIAN_POINT('Ctrl Pts',(0.804157577363971,-3.12085625073552,
22.8015306923564));
#17479=CARTESIAN_POINT('Ctrl Pts',(0.732940287609785,-3.13880236361801,
22.7969568415844));
#17480=CARTESIAN_POINT('Ctrl Pts',(0.678046882550519,-3.15111623472367,
22.7934077796714));
#17481=CARTESIAN_POINT('Ctrl Pts',(0.532324772573121,-3.17982121514614,
22.7839182756014));
#17482=CARTESIAN_POINT('Ctrl Pts',(0.441070830339947,-3.19375744201291,
22.7779055800829));
#17483=CARTESIAN_POINT('Ctrl Pts',(0.112155686638735,-3.22962372138143,
22.7560140286166));
#17484=CARTESIAN_POINT('Ctrl Pts',(-0.127153782166928,-3.2290657790248,
22.7396144245407));
#17485=CARTESIAN_POINT('Ctrl Pts',(-0.390190164926113,-3.19914888458184,
22.721979896988));
#17486=CARTESIAN_POINT('Ctrl Pts',(-0.416147008387024,-3.19587604228232,
22.7202448461282));
#17487=CARTESIAN_POINT('Ctrl Pts',(-0.512369581614551,-3.18255133010016,
22.7138383990972));
#17488=CARTESIAN_POINT('Ctrl Pts',(-0.582342889367659,-3.17049428846126,
22.7092298097286));
#17489=CARTESIAN_POINT('Ctrl Pts',(-0.66350721219585,-3.15373065283494,
22.7039859813775));
#17490=CARTESIAN_POINT('Ctrl Pts',(-0.675134832243465,-3.15126194084545,
22.7032372189929));
#17491=CARTESIAN_POINT('Ctrl Pts',(-0.693781405861316,-3.14719505822461,
22.7020407323728));
#17492=CARTESIAN_POINT('Ctrl Pts',(-0.700808997814038,-3.14563763402576,
22.7015907705632));
#17493=CARTESIAN_POINT('Ctrl Pts',(-0.713301301468496,-3.14282520229928,
22.7007927225703));
#17494=CARTESIAN_POINT('Ctrl Pts',(-0.718768019083035,-3.14157946508569,
22.7004441113043));
#17495=CARTESIAN_POINT('Ctrl Pts',(-0.730417322589379,-3.13889286147994,
22.6997025800503));
#17496=CARTESIAN_POINT('Ctrl Pts',(-0.736598896133194,-3.13744799619852,
22.6993098935338));
#17497=CARTESIAN_POINT('Ctrl Pts',(-0.753432967160025,-3.13346074872979,
22.6982425815647));
#17498=CARTESIAN_POINT('Ctrl Pts',(-0.764076954978999,-3.13088229014925,
22.6975700035096));
#17499=CARTESIAN_POINT('Ctrl Pts',(-0.819092971003341,-3.11725763072769,
22.694104409404));
#17500=CARTESIAN_POINT('Ctrl Pts',(-0.863241875330294,-3.10532162499291,
22.6913597319615));
#17501=CARTESIAN_POINT('Ctrl Pts',(-0.993858879870399,-3.06700705535381,
22.6833074784171));
#17502=CARTESIAN_POINT('Ctrl Pts',(-1.0794912669506,-3.03792507448772,22.6781177175005));
#17503=CARTESIAN_POINT('Ctrl Pts',(-1.27010386193754,-2.96411041299132,
22.6665399313435));
#17504=CARTESIAN_POINT('Ctrl Pts',(-1.3740659605566,-2.91736423536877,22.6602050979509));
#17505=CARTESIAN_POINT('Ctrl Pts',(-1.47525567074797,-2.86526408354028,
22.6538402050192));
#17506=CARTESIAN_POINT('Ctrl Pts',(-1.47525540254685,-2.86526422163059,
22.4042343665403));
#17507=CARTESIAN_POINT('Ctrl Pts',(-1.45322971877909,-2.87660471467408,
22.4057161252439));
#17508=CARTESIAN_POINT('Ctrl Pts',(-1.43107352007128,-2.88769110816536,
22.4072064089249));
#17509=CARTESIAN_POINT('Ctrl Pts',(-1.39334536297762,-2.90602842271961,
22.4097448328548));
#17510=CARTESIAN_POINT('Ctrl Pts',(-1.37784003467455,-2.91341197143045,
22.4107882650628));
#17511=CARTESIAN_POINT('Ctrl Pts',(-1.35244495756436,-2.92525689314817,
22.4124978773526));
#17512=CARTESIAN_POINT('Ctrl Pts',(-1.34259025589495,-2.92979293711636,
22.4131614594788));
#17513=CARTESIAN_POINT('Ctrl Pts',(-1.32353623876708,-2.93844703382913,
22.4144448792718));
#17514=CARTESIAN_POINT('Ctrl Pts',(-1.3143401267935,-2.94257186375562,22.4150644737297));
#17515=CARTESIAN_POINT('Ctrl Pts',(-1.29315479607141,-2.95195522121264,
22.4164923187807));
#17516=CARTESIAN_POINT('Ctrl Pts',(-1.28115264258673,-2.95718393964771,
22.4173015812674));
#17517=CARTESIAN_POINT('Ctrl Pts',(-1.24898913782493,-2.97096335986562,
22.4194713299308));
#17518=CARTESIAN_POINT('Ctrl Pts',(-1.22877220429694,-2.97938181235266,
22.4208362930542));
#17519=CARTESIAN_POINT('Ctrl Pts',(-1.05674718003269,-3.0489653534888,22.432462148492));
#17520=CARTESIAN_POINT('Ctrl Pts',(-0.900592327912983,-3.09868087281126,
22.44310933739));
#17521=CARTESIAN_POINT('Ctrl Pts',(-0.494677170092165,-3.19463046798923,
22.4709270680005));
#17522=CARTESIAN_POINT('Ctrl Pts',(-0.241991377949537,-3.22363220156942,
22.4884224802909));
#17523=CARTESIAN_POINT('Ctrl Pts',(0.0684599282487246,-3.22252663922272,
22.5087397288792));
#17524=CARTESIAN_POINT('Ctrl Pts',(0.125432129728662,-3.22081238668123,
22.5124155379076));
#17525=CARTESIAN_POINT('Ctrl Pts',(0.194024557188503,-3.2169254217495,22.5167542553459));
#17526=CARTESIAN_POINT('Ctrl Pts',(0.205712796867072,-3.21619914697916,
22.5174905288601));
#17527=CARTESIAN_POINT('Ctrl Pts',(0.223895667099289,-3.2149697849469,22.5186308973221));
#17528=CARTESIAN_POINT('Ctrl Pts',(0.230393027895031,-3.21451070030062,
22.5190373918159));
#17529=CARTESIAN_POINT('Ctrl Pts',(0.242454076700921,-3.21362174520985,
22.519790057545));
#17530=CARTESIAN_POINT('Ctrl Pts',(0.248017987581257,-3.21319712734198,
22.5201365100683));
#17531=CARTESIAN_POINT('Ctrl Pts',(0.260620812775867,-3.21220239454543,
22.5209195573232));
#17532=CARTESIAN_POINT('Ctrl Pts',(0.267658955773023,-3.21162359519485,
22.5213556584787));
#17533=CARTESIAN_POINT('Ctrl Pts',(0.288512380968579,-3.20983963457576,
22.5226443897481));
#17534=CARTESIAN_POINT('Ctrl Pts',(0.302322058350977,-3.20856841328594,
22.5234933962686));
#17535=CARTESIAN_POINT('Ctrl Pts',(0.405958338277836,-3.19835334426186,
22.5298345006264));
#17536=CARTESIAN_POINT('Ctrl Pts',(0.495390763805186,-3.18572715539188,
22.5351354525269));
#17537=CARTESIAN_POINT('Ctrl Pts',(0.82513642869662,-3.12494774557831,22.5544292372362));
#17538=CARTESIAN_POINT('Ctrl Pts',(1.06024714340263,-3.0532013308953,22.5677420892157));
#17539=CARTESIAN_POINT('Ctrl Pts',(1.36904463361923,-2.91894494336931,22.5869140683537));
#17540=CARTESIAN_POINT('Ctrl Pts',(1.45151829549291,-2.87882189653155,22.5922064237613));
#17541=CARTESIAN_POINT('Ctrl Pts',(1.58142040089381,-2.80862272796431,22.6009137863255));
#17542=CARTESIAN_POINT('Ctrl Pts',(1.62997103252234,-2.78072759767424,22.6042557332862));
#17543=CARTESIAN_POINT('Ctrl Pts',(1.69241992837157,-2.74264959980722,22.6086818479368));
#17544=CARTESIAN_POINT('Ctrl Pts',(1.70699964601392,-2.73359913521743,22.609724488767));
#17545=CARTESIAN_POINT('Ctrl Pts',(1.73067483450581,-2.71863933031513,22.6114331301467));
#17546=CARTESIAN_POINT('Ctrl Pts',(1.73981410325174,-2.71279967426767,22.6120965384314));
#17547=CARTESIAN_POINT('Ctrl Pts',(1.7573901449328,-2.70144388162747,22.6133798509383));
#17548=CARTESIAN_POINT('Ctrl Pts',(1.7658308682519,-2.69593406969343,22.6139995131828));
#17549=CARTESIAN_POINT('Ctrl Pts',(1.78518017991956,-2.68317365352163,22.615427842815));
#17550=CARTESIAN_POINT('Ctrl Pts',(1.79607063487128,-2.67589599875276,22.6162375243417));
#17551=CARTESIAN_POINT('Ctrl Pts',(1.82506886688489,-2.65626086585125,22.6184091275367));
#17552=CARTESIAN_POINT('Ctrl Pts',(1.84309517689008,-2.6437848412629,22.6197755381873));
#17553=CARTESIAN_POINT('Ctrl Pts',(1.99555464559333,-2.53595043628054,22.6314752691923));
#17554=CARTESIAN_POINT('Ctrl Pts',(2.12259614317261,-2.43060766860434,22.6422005871061));
#17555=CARTESIAN_POINT('Ctrl Pts',(2.42498203397414,-2.13801623190877,22.6702716084906));
#17556=CARTESIAN_POINT('Ctrl Pts',(2.58707952297347,-1.9387280699498,22.6879478879665));
#17557=CARTESIAN_POINT('Ctrl Pts',(2.75256116690646,-1.67702198786059,22.7081735603941));
#17558=CARTESIAN_POINT('Ctrl Pts',(2.78009839957447,-1.63096579200221,22.711629231731));
#17559=CARTESIAN_POINT('Ctrl Pts',(2.81213002539656,-1.57422191485976,22.7157431282652));
#17560=CARTESIAN_POINT('Ctrl Pts',(2.81773184586419,-1.5641729991261,22.716466302724));
#17561=CARTESIAN_POINT('Ctrl Pts',(2.82639911570345,-1.54842740960731,22.7175908240267));
#17562=CARTESIAN_POINT('Ctrl Pts',(2.82950136289644,-1.54275125771672,22.7179944660571));
#17563=CARTESIAN_POINT('Ctrl Pts',(2.8352503489719,-1.53215672031368,22.7187445744796));
#17564=CARTESIAN_POINT('Ctrl Pts',(2.83790136472362,-1.52724084600527,22.7190913051145));
#17565=CARTESIAN_POINT('Ctrl Pts',(2.84390506021006,-1.51603836712711,22.7198784731553));
#17566=CARTESIAN_POINT('Ctrl Pts',(2.84724967412906,-1.50974753437871,22.7203183951823));
#17567=CARTESIAN_POINT('Ctrl Pts',(2.85740604107431,-1.49049078840475,22.7216587308275));
#17568=CARTESIAN_POINT('Ctrl Pts',(2.8641504039159,-1.47748927456935,22.7225549821171));
#17569=CARTESIAN_POINT('Ctrl Pts',(2.95591769727314,-1.29759405893309,22.7348426695496));
#17570=CARTESIAN_POINT('Ctrl Pts',(3.02633539781646,-1.12361696688319,22.7453982109505));
#17571=CARTESIAN_POINT('Ctrl Pts',(3.1293267469082,-0.787622524820779,22.7650658293388));
#17572=CARTESIAN_POINT('Ctrl Pts',(3.16535963327044,-0.627320475467666,
22.774168184583));
#17573=CARTESIAN_POINT('Ctrl Pts',(3.20663054694032,-0.344266472164632,
22.790545412426));
#17574=CARTESIAN_POINT('Ctrl Pts',(3.21736139637587,-0.222664446991262,
22.7976735473106));
#17575=CARTESIAN_POINT('Ctrl Pts',(3.22185521262994,-0.0789966814373223,
22.8063364478945));
#17576=CARTESIAN_POINT('Ctrl Pts',(3.22231531574506,-0.0572316074707122,
22.8076551765737));
#17577=CARTESIAN_POINT('Ctrl Pts',(3.22268533933331,-0.0236081262736721,
22.8097028226332));
#17578=CARTESIAN_POINT('Ctrl Pts',(3.22275038269521,-0.0117518040262375,
22.8104268650091));
#17579=CARTESIAN_POINT('Ctrl Pts',(3.2227497082,0.0090526696822713,22.8117009667173));
#17580=CARTESIAN_POINT('Ctrl Pts',(3.2227121502267,0.0180007428272791,22.8122501348685));
#17581=CARTESIAN_POINT('Ctrl Pts',(3.22254193397476,0.038356080270456,22.8135021183827));
#17582=CARTESIAN_POINT('Ctrl Pts',(3.22238597089199,0.049762981753632,22.8142056593519));
#17583=CARTESIAN_POINT('Ctrl Pts',(3.22179545835401,0.0808692748110246,
22.8161296118064));
#17584=CARTESIAN_POINT('Ctrl Pts',(3.22124080728934,0.10056564379393,22.8173537785317));
#17585=CARTESIAN_POINT('Ctrl Pts',(3.21734128608028,0.204997011659307,22.8238767937529));
#17586=CARTESIAN_POINT('Ctrl Pts',(3.2108337955714,0.289573637821328,22.8292741629082));
#17587=CARTESIAN_POINT('Ctrl Pts',(3.16499073090659,0.682157441107763,22.8548818038269));
#17588=CARTESIAN_POINT('Ctrl Pts',(3.08460691186131,0.983690953556932,22.8763613576528));
#17589=CARTESIAN_POINT('Ctrl Pts',(2.92951063011695,1.34575621022412,22.9024810845322));
#17590=CARTESIAN_POINT('Ctrl Pts',(2.89365089797501,1.42122462742229,22.9079304255786));
#17591=CARTESIAN_POINT('Ctrl Pts',(2.84858017312797,1.50728029147035,22.91408131592));
#17592=CARTESIAN_POINT('Ctrl Pts',(2.84218777350976,1.51929969239818,22.9149389292062));
#17593=CARTESIAN_POINT('Ctrl Pts',(2.8323898255087,1.53744415824987,22.9162309139965));
#17594=CARTESIAN_POINT('Ctrl Pts',(2.82904024007949,1.54359903653728,22.9166687067913));
#17595=CARTESIAN_POINT('Ctrl Pts',(2.82298903246918,1.55463229763009,22.917452586366));
#17596=CARTESIAN_POINT('Ctrl Pts',(2.82029481243083,1.55951461382646,22.9177991343051));
#17597=CARTESIAN_POINT('Ctrl Pts',(2.81440600240956,1.57012081772729,22.9185512492832));
#17598=CARTESIAN_POINT('Ctrl Pts',(2.81120662775958,1.5758419421079,22.9189565032595));
#17599=CARTESIAN_POINT('Ctrl Pts',(2.80214943465217,1.59192265550082,22.9200944299139));
#17600=CARTESIAN_POINT('Ctrl Pts',(2.79625158380103,1.60225974348419,22.920824574595));
#17601=CARTESIAN_POINT('Ctrl Pts',(2.76012656288475,1.66476858811073,22.9252330921424));
#17602=CARTESIAN_POINT('Ctrl Pts',(2.72849522372141,1.71612003983682,22.9288263234556));
#17603=CARTESIAN_POINT('Ctrl Pts',(2.55623141859803,1.97896270108199,22.9472312328831));
#17604=CARTESIAN_POINT('Ctrl Pts',(2.39239369164449,2.17418734575289,22.9610081970418));
#17605=CARTESIAN_POINT('Ctrl Pts',(2.09099404675542,2.45750872924679,22.9843988896392));
#17606=CARTESIAN_POINT('Ctrl Pts',(1.96672143661653,2.55804656304713,22.9936107804568));
#17607=CARTESIAN_POINT('Ctrl Pts',(1.81758991005193,2.66138318731217,23.004524376293));
#17608=CARTESIAN_POINT('Ctrl Pts',(1.79953180769067,2.67362652367145,23.0058433965151));
#17609=CARTESIAN_POINT('Ctrl Pts',(1.77046118004956,2.69290837859514,23.0079635453069));
#17610=CARTESIAN_POINT('Ctrl Pts',(1.7595275370096,2.7000650296207,23.0087602183328));
#17611=CARTESIAN_POINT('Ctrl Pts',(1.74008756295458,2.71262130486216,23.0101755588696));
#17612=CARTESIAN_POINT('Ctrl Pts',(1.73159882021473,2.71804793786105,23.0107932059048));
#17613=CARTESIAN_POINT('Ctrl Pts',(1.71390818691025,2.72924059211383,23.0120796677778));
#17614=CARTESIAN_POINT('Ctrl Pts',(1.70470233228443,2.73500007979567,23.0127487149544));
#17615=CARTESIAN_POINT('Ctrl Pts',(1.68082210430534,2.74977293469941,23.0144833014221));
#17616=CARTESIAN_POINT('Ctrl Pts',(1.66610442334965,2.75871531163775,23.0155514391407));
#17617=CARTESIAN_POINT('Ctrl Pts',(1.60275878491916,2.7965119462749,23.0201454239629));
#17618=CARTESIAN_POINT('Ctrl Pts',(1.55345015803031,2.82420019499376,23.0237133071182));
#17619=CARTESIAN_POINT('Ctrl Pts',(1.42121651061605,2.89394242332094,23.0332666167134));
#17620=CARTESIAN_POINT('Ctrl Pts',(1.33716089620935,2.93372753619857,23.0393255236725));
#17621=CARTESIAN_POINT('Ctrl Pts',(1.04136394055334,3.05837902265784,23.0605704412725));
#17622=CARTESIAN_POINT('Ctrl Pts',(0.822415701266829,3.12437841206829,23.0762177835746));
#17623=CARTESIAN_POINT('Ctrl Pts',(0.573999951462098,3.17131779024787,23.0931085944807));
#17624=CARTESIAN_POINT('Ctrl Pts',(0.549580979137327,3.17564060693655,23.0947592266122));
#17625=CARTESIAN_POINT('Ctrl Pts',(0.445160801710962,3.19288526264021,23.1017702736428));
#17626=CARTESIAN_POINT('Ctrl Pts',(0.364730125412771,3.20307021839355,23.1070528435679));
#17627=CARTESIAN_POINT('Ctrl Pts',(0.270535637951425,3.21140321009051,23.1130395310566));
#17628=CARTESIAN_POINT('Ctrl Pts',(0.25706958178469,3.21250919911265,23.113890631234));
#17629=CARTESIAN_POINT('Ctrl Pts',(0.236631518856113,3.21405847476445,23.1151747665248));
#17630=CARTESIAN_POINT('Ctrl Pts',(0.229664568085354,3.21456381850995,23.115611162306));
#17631=CARTESIAN_POINT('Ctrl Pts',(0.217134250674989,3.21543175337516,23.1163935569701));
#17632=CARTESIAN_POINT('Ctrl Pts',(0.21157156659384,3.21580256189583,23.1167400091665));
#17633=CARTESIAN_POINT('Ctrl Pts',(0.199449049380686,3.21657905748449,23.1174930897281));
#17634=CARTESIAN_POINT('Ctrl Pts',(0.192888949202968,3.21697911268353,23.1178993986197));
#17635=CARTESIAN_POINT('Ctrl Pts',(0.174366564217251,3.21805180350586,23.1190432783253));
#17636=CARTESIAN_POINT('Ctrl Pts',(0.162401537999565,3.21867781234849,23.1197782786353));
#17637=CARTESIAN_POINT('Ctrl Pts',(0.0887405114761992,3.22211994937534,
23.1242806168026));
#17638=CARTESIAN_POINT('Ctrl Pts',(0.0269730687194685,3.22322904189556,
23.1279585490219));
#17639=CARTESIAN_POINT('Ctrl Pts',(-0.303325724759565,3.21966295143925,
23.1472856278898));
#17640=CARTESIAN_POINT('Ctrl Pts',(-0.570464585437034,3.18321141872032,
23.1617933982917));
#17641=CARTESIAN_POINT('Ctrl Pts',(-0.96930712064195,3.07690504461795,23.1852360772557));
#17642=CARTESIAN_POINT('Ctrl Pts',(-1.10594368261036,3.0304755125018,23.1935946473569));
#17643=CARTESIAN_POINT('Ctrl Pts',(-1.25879865212571,2.96681703591995,23.2035577791438));
#17644=CARTESIAN_POINT('Ctrl Pts',(-1.27851060878884,2.95837589909697,23.204854493787));
#17645=CARTESIAN_POINT('Ctrl Pts',(-1.30999681723802,2.94451928369802,23.2069455564645));
#17646=CARTESIAN_POINT('Ctrl Pts',(-1.32182540470833,2.93922831114069,23.2077356426877));
#17647=CARTESIAN_POINT('Ctrl Pts',(-1.34277843906696,2.92970387552569,23.2091433928295));
#17648=CARTESIAN_POINT('Ctrl Pts',(-1.3519156302161,2.92549873693816,23.2097600730665));
#17649=CARTESIAN_POINT('Ctrl Pts',(-1.37092116156382,2.91664391612797,23.211048674904));
#17650=CARTESIAN_POINT('Ctrl Pts',(-1.38078586454126,2.91198677131387,23.2117208495585));
#17651=CARTESIAN_POINT('Ctrl Pts',(-1.40636545964738,2.8997513931425,23.2134726117019));
#17652=CARTESIAN_POINT('Ctrl Pts',(-1.4220426351027,2.89209555042265,23.2145548956032));
#17653=CARTESIAN_POINT('Ctrl Pts',(-1.49014442177158,2.85815090288789,23.2192948656409));
#17654=CARTESIAN_POINT('Ctrl Pts',(-1.54190529446969,2.83056254407517,23.222997977272));
#17655=CARTESIAN_POINT('Ctrl Pts',(-1.67795808770123,2.7532075694892,23.2330101747358));
#17656=CARTESIAN_POINT('Ctrl Pts',(-1.7607791835209,2.70099036201501,23.2394018164512));
#17657=CARTESIAN_POINT('Ctrl Pts',(-1.99724843279668,2.53639815068872,23.2585137970964));
#17658=CARTESIAN_POINT('Ctrl Pts',(-2.14346854841691,2.41409430318514,23.2714967982452));
#17659=CARTESIAN_POINT('Ctrl Pts',(-2.37287063611332,2.18485183189304,23.293324933616));
#17660=CARTESIAN_POINT('Ctrl Pts',(-2.46171182421877,2.08424471841882,23.3022304452959));
#17661=CARTESIAN_POINT('Ctrl Pts',(-2.55321365195604,1.9665810858594,23.3116810594943));
#17662=CARTESIAN_POINT('Ctrl Pts',(-2.56231025316098,1.9547141240218,23.3126238880156));
#17663=CARTESIAN_POINT('Ctrl Pts',(-2.57565531422471,1.93705159573314,23.3140114499348));
#17664=CARTESIAN_POINT('Ctrl Pts',(-2.57996735778249,1.93130464126623,23.3144604894685));
#17665=CARTESIAN_POINT('Ctrl Pts',(-2.58760051863936,1.92106022126617,23.3152565408995));
#17666=CARTESIAN_POINT('Ctrl Pts',(-2.59092918167654,1.91656849473916,23.3156040768049));
#17667=CARTESIAN_POINT('Ctrl Pts',(-2.59805988422804,1.90689373530676,23.3163494093141));
#17668=CARTESIAN_POINT('Ctrl Pts',(-2.60185810040356,1.90170799726412,23.3167469406906));
#17669=CARTESIAN_POINT('Ctrl Pts',(-2.61230190729453,1.8873591159388,23.3178415785149));
#17670=CARTESIAN_POINT('Ctrl Pts',(-2.61891485326957,1.87817216664992,23.3185364563075));
#17671=CARTESIAN_POINT('Ctrl Pts',(-2.65496455115509,1.82752997849801,23.3223353897162));
#17672=CARTESIAN_POINT('Ctrl Pts',(-2.68346734418187,1.78541487472923,23.3253793433852));
#17673=CARTESIAN_POINT('Ctrl Pts',(-2.85058457376423,1.52543655327208,23.3435947394204));
#17674=CARTESIAN_POINT('Ctrl Pts',(-2.96361104755742,1.29221865707019,23.3575973108754));
#17675=CARTESIAN_POINT('Ctrl Pts',(-3.1014722915409,0.891312107713129,23.3815331415055));
#17676=CARTESIAN_POINT('Ctrl Pts',(-3.14318038357564,0.730735256595542,
23.3910750167604));
#17677=CARTESIAN_POINT('Ctrl Pts',(-3.1762234250391,0.546080278224665,23.4023575552931));
#17678=CARTESIAN_POINT('Ctrl Pts',(-3.17986732999179,0.524445081228607,
23.4036838866644));
#17679=CARTESIAN_POINT('Ctrl Pts',(-3.18533421847902,0.48983178616469,23.405813561776));
#17680=CARTESIAN_POINT('Ctrl Pts',(-3.18729947627955,0.476876611609087,
23.4066123856015));
#17681=CARTESIAN_POINT('Ctrl Pts',(-3.19063675225289,0.453934244447489,
23.4080302141841));
#17682=CARTESIAN_POINT('Ctrl Pts',(-3.19204102731129,0.443951866087993,
23.408648186422));
#17683=CARTESIAN_POINT('Ctrl Pts',(-3.19485857372319,0.423218427691894,
23.4099339964793));
#17684=CARTESIAN_POINT('Ctrl Pts',(-3.19626446314255,0.412466508557065,
23.4106020600329));
#17685=CARTESIAN_POINT('Ctrl Pts',(-3.19975381011422,0.384691116111979,
23.4123312385098));
#17686=CARTESIAN_POINT('Ctrl Pts',(-3.20175566604097,0.3676579073031,23.4133949212816));
#17687=CARTESIAN_POINT('Ctrl Pts',(-3.20970259377268,0.295044567339758,
23.4179438840133));
#17688=CARTESIAN_POINT('Ctrl Pts',(-3.21433676661224,0.239333567620247,
23.4214701832064));
#17689=CARTESIAN_POINT('Ctrl Pts',(-3.22272915547479,0.0922064123224363,
23.4308840257047));
#17690=CARTESIAN_POINT('Ctrl Pts',(-3.22404749420441,0.000707038482247822,
23.4368424113532));
#17691=CARTESIAN_POINT('Ctrl Pts',(-3.21452647127309,-0.33739220971479,
23.4592128334957));
#17692=CARTESIAN_POINT('Ctrl Pts',(-3.17927327264488,-0.582425782554848,
23.4761971399821));
#17693=CARTESIAN_POINT('Ctrl Pts',(-3.09375545997647,-0.907030975617503,
23.4985045490449));
#17694=CARTESIAN_POINT('Ctrl Pts',(-3.06754393824343,-0.992071242905942,
23.5043198767823));
#17695=CARTESIAN_POINT('Ctrl Pts',(-3.03323088349472,-1.08895315502894,
23.5108291816523));
#17696=CARTESIAN_POINT('Ctrl Pts',(-3.02853304113299,-1.10195108843948,
23.511700014462));
#17697=CARTESIAN_POINT('Ctrl Pts',(-3.02131207321517,-1.12153495057391,
23.5130079146903));
#17698=CARTESIAN_POINT('Ctrl Pts',(-3.01885077921384,-1.1281432817695,23.5134485279367));
#17699=CARTESIAN_POINT('Ctrl Pts',(-3.01440326990669,-1.13996562148953,
23.5142354247814));
#17700=CARTESIAN_POINT('Ctrl Pts',(-3.01242519481193,-1.14518257889654,
23.5145821853487));
#17701=CARTESIAN_POINT('Ctrl Pts',(-3.00810580697121,-1.15648585789314,
23.5153324389512));
#17702=CARTESIAN_POINT('Ctrl Pts',(-3.00575957414438,-1.16257019988449,
23.5157356315296));
#17703=CARTESIAN_POINT('Ctrl Pts',(-2.99913589097792,-1.17959290091133,
23.5168619546224));
#17704=CARTESIAN_POINT('Ctrl Pts',(-2.99481703801444,-1.19051519231958,
23.5175826390556));
#17705=CARTESIAN_POINT('Ctrl Pts',(-2.96897885107539,-1.25482900932327,
23.5218158049831));
#17706=CARTESIAN_POINT('Ctrl Pts',(-2.94609034479315,-1.30766352404179,
23.5252508200958));
#17707=CARTESIAN_POINT('Ctrl Pts',(-2.81503165242162,-1.58925638332999,
23.5434734793986));
#17708=CARTESIAN_POINT('Ctrl Pts',(-2.6816134242665,-1.8053019174713,23.5572067219746));
#17709=CARTESIAN_POINT('Ctrl Pts',(-2.42266749240785,-2.13155217463521,
23.5807364962922));
#17710=CARTESIAN_POINT('Ctrl Pts',(-2.31147676360101,-2.25164323143822,
23.5901563358516));
#17711=CARTESIAN_POINT('Ctrl Pts',(-2.17561538761024,-2.37766580007576,
23.6013023089783));
#17712=CARTESIAN_POINT('Ctrl Pts',(-2.15941163707981,-2.39239175660236,
23.6026259955672));
#17713=CARTESIAN_POINT('Ctrl Pts',(-2.13328259973132,-2.41565607505237,
23.6047522249843));
#17714=CARTESIAN_POINT('Ctrl Pts',(-2.12345297697207,-2.42430121270163,
23.6055502712333));
#17715=CARTESIAN_POINT('Ctrl Pts',(-2.10596257794367,-2.4394960058312,23.6069671997905));
#17716=CARTESIAN_POINT('Ctrl Pts',(-2.09832319094735,-2.44607009810282,
23.6075850539353));
#17717=CARTESIAN_POINT('Ctrl Pts',(-2.08239667358617,-2.45964618579822,
23.6088710970561));
#17718=CARTESIAN_POINT('Ctrl Pts',(-2.07410478265755,-2.46664237606973,
23.6095395141452));
#17719=CARTESIAN_POINT('Ctrl Pts',(-2.05259453974916,-2.48460625272461,
23.611270636752));
#17720=CARTESIAN_POINT('Ctrl Pts',(-2.03932368092161,-2.49551026479727,
23.6123359210962));
#17721=CARTESIAN_POINT('Ctrl Pts',(-1.98231557615219,-2.54159260307848,
23.6169010180691));
#17722=CARTESIAN_POINT('Ctrl Pts',(-1.937752691411,-2.57572938624767,23.6204422127806));
#17723=CARTESIAN_POINT('Ctrl Pts',(-1.81784856679591,-2.66270711685815,
23.6299059253152));
#17724=CARTESIAN_POINT('Ctrl Pts',(-1.74110066664023,-2.71351221541542,
23.6359002224553));
#17725=CARTESIAN_POINT('Ctrl Pts',(-1.60108505231167,-2.79781132438933,
23.646712344991));
#17726=CARTESIAN_POINT('Ctrl Pts',(-1.53870409157046,-2.83259603402492,
23.6514881034905));
#17727=CARTESIAN_POINT('Ctrl Pts',(-1.47525500221108,-2.86526442775378,
23.6562919783988));
#17728=CARTESIAN_POINT('Origin',(0.,0.,4.68922655072688));
#17729=CARTESIAN_POINT('',(-1.4752554489605,-2.86526419773332,25.1553455282223));
#17730=CARTESIAN_POINT('',(-1.47525540501177,-2.86526422036146,24.9102129806979));
#17731=CARTESIAN_POINT('',(-1.47525540501186,-2.86526422036142,4.68922655072688));
#17732=CARTESIAN_POINT('',(3.22274971917068,-0.00134539409721628,24.3082009925199));
#17733=CARTESIAN_POINT('Ctrl Pts',(-1.4752554489605,-2.86526419773332,25.1553455282223));
#17734=CARTESIAN_POINT('Ctrl Pts',(-1.6729476371766,-2.76347725671983,25.1405536479666));
#17735=CARTESIAN_POINT('Ctrl Pts',(-1.85960157496954,-2.64149118000024,
25.1252848161754));
#17736=CARTESIAN_POINT('Ctrl Pts',(-2.10472042139451,-2.44233335256714,
25.104262226728));
#17737=CARTESIAN_POINT('Ctrl Pts',(-2.17461939367043,-2.38030970656153,
25.0981454939901));
#17738=CARTESIAN_POINT('Ctrl Pts',(-2.25177214785347,-2.30560948181583,
25.091342864128));
#17739=CARTESIAN_POINT('Ctrl Pts',(-2.26174977643724,-2.29582247874771,
25.0904621128427));
#17740=CARTESIAN_POINT('Ctrl Pts',(-2.27669012753043,-2.28097563375094,
25.089142195969));
#17741=CARTESIAN_POINT('Ctrl Pts',(-2.28170019225532,-2.27596397456147,
25.0886993903266));
#17742=CARTESIAN_POINT('Ctrl Pts',(-2.2906283785988,-2.26697383575064,25.0879100215358));
#17743=CARTESIAN_POINT('Ctrl Pts',(-2.29455271577956,-2.2630016740854,25.0875629696937));
#17744=CARTESIAN_POINT('Ctrl Pts',(-2.30302290155424,-2.25438357977174,
25.0868137188299));
#17745=CARTESIAN_POINT('Ctrl Pts',(-2.30756501123034,-2.24973410218541,
25.0864118116754));
#17746=CARTESIAN_POINT('Ctrl Pts',(-2.32020282131241,-2.23671901497513,
25.0852931019164));
#17747=CARTESIAN_POINT('Ctrl Pts',(-2.32826740325088,-2.22832313468614,
25.0845786912661));
#17748=CARTESIAN_POINT('Ctrl Pts',(-2.37471680402311,-2.17943809116738,
25.0804595282793));
#17749=CARTESIAN_POINT('Ctrl Pts',(-2.41209311506719,-2.13799858941098,
25.0771274479861));
#17750=CARTESIAN_POINT('Ctrl Pts',(-2.61381780098597,-1.90231595568482,
25.058905277118));
#17751=CARTESIAN_POINT('Ctrl Pts',(-2.75580311829823,-1.69009649929761,
25.0450993882415));
#17752=CARTESIAN_POINT('Ctrl Pts',(-2.94581325347143,-1.31726635967942,
25.0214636371805));
#17753=CARTESIAN_POINT('Ctrl Pts',(-3.00900307551504,-1.16571712665636,
25.0120147998813));
#17754=CARTESIAN_POINT('Ctrl Pts',(-3.06725195365497,-0.989223488618128,
25.0008360956684));
#17755=CARTESIAN_POINT('Ctrl Pts',(-3.07390651490528,-0.968347230562795,
24.9995114760654));
#17756=CARTESIAN_POINT('Ctrl Pts',(-3.08419785144542,-0.934886472816387,
24.9973838896407));
#17757=CARTESIAN_POINT('Ctrl Pts',(-3.08797174725157,-0.922344612465189,
24.9965854267481));
#17758=CARTESIAN_POINT('Ctrl Pts',(-3.0945153487017,-0.90010775881865,24.9951678422757));
#17759=CARTESIAN_POINT('Ctrl Pts',(-3.09731622015955,-0.890422062565233,
24.994549750359));
#17760=CARTESIAN_POINT('Ctrl Pts',(-3.10303722031383,-0.870284629476614,
24.9932632951313));
#17761=CARTESIAN_POINT('Ctrl Pts',(-3.10595009718327,-0.85983098115339,
24.9925947039665));
#17762=CARTESIAN_POINT('Ctrl Pts',(-3.11333727880239,-0.832792663152279,
24.9908633062624));
#17763=CARTESIAN_POINT('Ctrl Pts',(-3.11773183896444,-0.816186739216616,
24.9897979209897));
#17764=CARTESIAN_POINT('Ctrl Pts',(-3.13591382390471,-0.745191468872054,
24.9852339221997));
#17765=CARTESIAN_POINT('Ctrl Pts',(-3.14841162837986,-0.690484913627083,
24.9816939588657));
#17766=CARTESIAN_POINT('Ctrl Pts',(-3.17760629628235,-0.545335699095486,
24.9722349572338));
#17767=CARTESIAN_POINT('Ctrl Pts',(-3.19187014628047,-0.454461488905316,
24.9662442416565));
#17768=CARTESIAN_POINT('Ctrl Pts',(-3.22953527826587,-0.122295075124919,
24.9441291584514));
#17769=CARTESIAN_POINT('Ctrl Pts',(-3.22958907876854,0.120804237530324,
24.9274609781128));
#17770=CARTESIAN_POINT('Ctrl Pts',(-3.19203217200052,0.453415756912826,
24.9051884974746));
#17771=CARTESIAN_POINT('Ctrl Pts',(-3.17771971835471,0.544753228201643,
24.8991392126235));
#17772=CARTESIAN_POINT('Ctrl Pts',(-3.15675078290543,0.649027329570261,
24.8924020075446));
#17773=CARTESIAN_POINT('Ctrl Pts',(-3.15391313751876,0.662679347366521,
24.8915233322234));
#17774=CARTESIAN_POINT('Ctrl Pts',(-3.14950126455894,0.683234560676992,
24.8902059106636));
#17775=CARTESIAN_POINT('Ctrl Pts',(-3.14799279164465,0.690151480754959,
24.8897635442948));
#17776=CARTESIAN_POINT('Ctrl Pts',(-3.14525390208734,0.702514502483954,
24.8889746497863));
#17777=CARTESIAN_POINT('Ctrl Pts',(-3.14403211844039,0.707962410433881,
24.8886276354098));
#17778=CARTESIAN_POINT('Ctrl Pts',(-3.14135620704655,0.719750689922282,
24.8878781144852));
#17779=CARTESIAN_POINT('Ctrl Pts',(-3.13989704375085,0.726089823372296,
24.8874759016928));
#17780=CARTESIAN_POINT('Ctrl Pts',(-3.13576774699403,0.743783744039376,
24.8863554775728));
#17781=CARTESIAN_POINT('Ctrl Pts',(-3.13305511408969,0.755128653116896,
24.8856396701029));
#17782=CARTESIAN_POINT('Ctrl Pts',(-3.11692203213957,0.821017490441438,
24.8814961112207));
#17783=CARTESIAN_POINT('Ctrl Pts',(-3.10213811351939,0.875221507299935,
24.8781420420911));
#17784=CARTESIAN_POINT('Ctrl Pts',(-3.01268248788995,1.17236958577065,24.8599187943197));
#17785=CARTESIAN_POINT('Ctrl Pts',(-2.9108864933613,1.40622663247106,24.846127555343));
#17786=CARTESIAN_POINT('Ctrl Pts',(-2.70000639353231,1.76718081087724,24.8225144987084));
#17787=CARTESIAN_POINT('Ctrl Pts',(-2.60669838954595,1.9021239733909,24.8130729713214));
#17788=CARTESIAN_POINT('Ctrl Pts',(-2.48974914338014,2.04639848110886,24.8019024446313));
#17789=CARTESIAN_POINT('Ctrl Pts',(-2.47578041442358,2.0632762402786,24.8005779844864));
#17790=CARTESIAN_POINT('Ctrl Pts',(-2.45318821007887,2.09001356201534,24.7984506058183));
#17791=CARTESIAN_POINT('Ctrl Pts',(-2.44467467129812,2.09996543472617,24.7976521898178));
#17792=CARTESIAN_POINT('Ctrl Pts',(-2.42950004153543,2.11748642653252,24.7962346596094));
#17793=CARTESIAN_POINT('Ctrl Pts',(-2.42286360749482,2.12507674077382,24.7956165748016));
#17794=CARTESIAN_POINT('Ctrl Pts',(-2.40901029674304,2.14077199264923,24.7943301054563));
#17795=CARTESIAN_POINT('Ctrl Pts',(-2.40178788970076,2.1488718581152,24.7936614929211));
#17796=CARTESIAN_POINT('Ctrl Pts',(-2.38302707541794,2.16969920545936,24.7919299777081));
#17797=CARTESIAN_POINT('Ctrl Pts',(-2.37142767854558,2.18237105721132,24.7908644956327));
#17798=CARTESIAN_POINT('Ctrl Pts',(-2.32150312194548,2.23604352947094,24.7862995203618));
#17799=CARTESIAN_POINT('Ctrl Pts',(-2.282213696084,2.27612992099538,24.7827586553437));
#17800=CARTESIAN_POINT('Ctrl Pts',(-2.17581952672817,2.37915701479309,24.773296632497));
#17801=CARTESIAN_POINT('Ctrl Pts',(-2.10703564796589,2.44028214893733,24.7673037404475));
#17802=CARTESIAN_POINT('Ctrl Pts',(-1.84811748796279,2.65125473882761,24.7452086250471));
#17803=CARTESIAN_POINT('Ctrl Pts',(-1.6438952129299,2.78249592997477,24.7285647116915));
#17804=CARTESIAN_POINT('Ctrl Pts',(-1.34383369240142,2.93066808635624,24.7062948952702));
#17805=CARTESIAN_POINT('Ctrl Pts',(-1.25900668477802,2.96809872995206,24.7002275843406));
#17806=CARTESIAN_POINT('Ctrl Pts',(-1.15967553281428,3.00690289742189,24.6934725241263));
#17807=CARTESIAN_POINT('Ctrl Pts',(-1.146641657436,3.01189729272933,24.6925929433587));
#17808=CARTESIAN_POINT('Ctrl Pts',(-1.12694563712223,3.01929813933051,24.6912744333829));
#17809=CARTESIAN_POINT('Ctrl Pts',(-1.12030753341063,3.02176748874773,24.6908318753605));
#17810=CARTESIAN_POINT('Ctrl Pts',(-1.10842178268842,3.02614439329539,24.6900427739945));
#17811=CARTESIAN_POINT('Ctrl Pts',(-1.10317728683387,3.02806020627151,24.689695743342));
#17812=CARTESIAN_POINT('Ctrl Pts',(-1.09181407924996,3.03217774264091,24.6889463405642));
#17813=CARTESIAN_POINT('Ctrl Pts',(-1.08569369323693,3.03437457358939,24.6885442613695));
#17814=CARTESIAN_POINT('Ctrl Pts',(-1.06858563783361,3.04045689341282,24.6874245867104));
#17815=CARTESIAN_POINT('Ctrl Pts',(-1.05758334777731,3.04430137441449,24.6867093898967));
#17816=CARTESIAN_POINT('Ctrl Pts',(-0.993591021593331,3.06627313684402,
24.6825765194278));
#17817=CARTESIAN_POINT('Ctrl Pts',(-0.940152947678015,3.08307758315236,
24.6792320845371));
#17818=CARTESIAN_POINT('Ctrl Pts',(-0.641838643400723,3.16840843410577,
24.661009325323));
#17819=CARTESIAN_POINT('Ctrl Pts',(-0.389937988087602,3.20916571835361,
24.6472116799436));
#17820=CARTESIAN_POINT('Ctrl Pts',(0.0279135230043758,3.2267944853697,24.623588683288));
#17821=CARTESIAN_POINT('Ctrl Pts',(0.191938285503035,3.22120025181376,24.6141439418682));
#17822=CARTESIAN_POINT('Ctrl Pts',(0.37658978821368,3.20074643222523,24.6029698197408));
#17823=CARTESIAN_POINT('Ctrl Pts',(0.398340583107129,3.19811230814808,24.601645289459));
#17824=CARTESIAN_POINT('Ctrl Pts',(0.433047640480566,3.1935495664764,24.5995178194098));
#17825=CARTESIAN_POINT('Ctrl Pts',(0.446022174967081,3.19176335337657,24.5987193827837));
#17826=CARTESIAN_POINT('Ctrl Pts',(0.468965041662789,3.18846216994225,24.5973018287075));
#17827=CARTESIAN_POINT('Ctrl Pts',(0.478937885533747,3.18697940338271,24.5966837407731));
#17828=CARTESIAN_POINT('Ctrl Pts',(0.499630038966506,3.18380356731472,24.5953972776388));
#17829=CARTESIAN_POINT('Ctrl Pts',(0.510348069211088,3.18210310560857,24.5947286745044));
#17830=CARTESIAN_POINT('Ctrl Pts',(0.538009619951665,3.17757113372551,24.5929972109834));
#17831=CARTESIAN_POINT('Ctrl Pts',(0.55493928815878,3.1746582539048,24.5919317714914));
#17832=CARTESIAN_POINT('Ctrl Pts',(0.627071446577371,3.16165275117239,24.5873672257987));
#17833=CARTESIAN_POINT('Ctrl Pts',(0.682025766080417,3.15025505851074,24.5838267574572));
#17834=CARTESIAN_POINT('Ctrl Pts',(0.826187375948994,3.1164066697373,24.5743660637734));
#17835=CARTESIAN_POINT('Ctrl Pts',(0.914774531885293,3.09156289642311,24.5683741292643));
#17836=CARTESIAN_POINT('Ctrl Pts',(1.17885253166699,3.00515923969121,24.5499927190242));
#17837=CARTESIAN_POINT('Ctrl Pts',(1.35019111875876,2.93217500841037,24.5373326160988));
#17838=CARTESIAN_POINT('Ctrl Pts',(1.64427291870194,2.77563938895823,24.5148589401816));
#17839=CARTESIAN_POINT('Ctrl Pts',(1.76939813693502,2.69760045319533,24.5050345372913));
#17840=CARTESIAN_POINT('Ctrl Pts',(1.9009395391703,2.60245508195972,24.494740329168));
#17841=CARTESIAN_POINT('Ctrl Pts',(1.91305950899005,2.59355873673594,24.4937922514419));
#17842=CARTESIAN_POINT('Ctrl Pts',(1.9308930914166,2.58027543184358,24.4923983841245));
#17843=CARTESIAN_POINT('Ctrl Pts',(1.93665475892088,2.57595376157947,24.4919482341003));
#17844=CARTESIAN_POINT('Ctrl Pts',(1.94668006870897,2.56838140013181,24.4911653587003));
#17845=CARTESIAN_POINT('Ctrl Pts',(1.95095013328329,2.56513935010743,24.4908320355451));
#17846=CARTESIAN_POINT('Ctrl Pts',(1.96014725859599,2.55812017465189,24.4901143918472));
#17847=CARTESIAN_POINT('Ctrl Pts',(1.96507149092677,2.55433947243311,24.4897303298131));
#17848=CARTESIAN_POINT('Ctrl Pts',(1.97813132114702,2.54425234516561,24.4887121028772));
#17849=CARTESIAN_POINT('Ctrl Pts',(1.98624776170592,2.53792106958016,24.4880796725364));
#17850=CARTESIAN_POINT('Ctrl Pts',(2.00428239561474,2.52371354138743,24.4866749169837));
#17851=CARTESIAN_POINT('Ctrl Pts',(2.01418483147779,2.51581744900714,24.4859039340546));
#17852=CARTESIAN_POINT('Ctrl Pts',(2.04405939667445,2.49170634999754,24.483578107108));
#17853=CARTESIAN_POINT('Ctrl Pts',(2.06388464684956,2.47531000159465,24.4820348462725));
#17854=CARTESIAN_POINT('Ctrl Pts',(2.1372194358587,2.41316524279882,24.4763178423725));
#17855=CARTESIAN_POINT('Ctrl Pts',(2.18942474387131,2.36590236463068,24.4722308882994));
#17856=CARTESIAN_POINT('Ctrl Pts',(2.29056578578179,2.26811912021095,24.4641800867823));
#17857=CARTESIAN_POINT('Ctrl Pts',(2.33947898128169,2.21763268243842,24.4602181756911));
#17858=CARTESIAN_POINT('Ctrl Pts',(2.57607961297247,1.95687385586951,24.4404725230852));
#17859=CARTESIAN_POINT('Ctrl Pts',(2.73724060734724,1.72425072498668,24.4249599727797));
#17860=CARTESIAN_POINT('Ctrl Pts',(2.88161592510557,1.4434539565627,24.4061058217089));
#17861=CARTESIAN_POINT('Ctrl Pts',(2.89665826072096,1.41302528372264,24.404063191413));
#17862=CARTESIAN_POINT('Ctrl Pts',(2.91684885417585,1.37050455237372,24.4012071157634));
#17863=CARTESIAN_POINT('Ctrl Pts',(2.92240833796023,1.35860938625818,24.4004079489244));
#17864=CARTESIAN_POINT('Ctrl Pts',(2.93185748149023,1.33806546744392,24.3990272677861));
#17865=CARTESIAN_POINT('Ctrl Pts',(2.93578197246169,1.32943284676682,24.3984469638973));
#17866=CARTESIAN_POINT('Ctrl Pts',(2.94381077507445,1.31156313276792,24.397245379705));
#17867=CARTESIAN_POINT('Ctrl Pts',(2.94790983958032,1.30232380945377,24.3966239268906));
#17868=CARTESIAN_POINT('Ctrl Pts',(2.95737658454358,1.28071198523998,24.3951697665496));
#17869=CARTESIAN_POINT('Ctrl Pts',(2.96271016872835,1.26832483976613,24.3943359025323));
#17870=CARTESIAN_POINT('Ctrl Pts',(2.97965479520074,1.22828114036154,24.3916388190147));
#17871=CARTESIAN_POINT('Ctrl Pts',(2.99095725913929,1.20049649483063,24.3897651644836));
#17872=CARTESIAN_POINT('Ctrl Pts',(3.06672367198217,1.00652677323359,24.3766654881088));
#17873=CARTESIAN_POINT('Ctrl Pts',(3.11768058812873,0.835427827277531,24.3649864569444));
#17874=CARTESIAN_POINT('Ctrl Pts',(3.19988227671476,0.443180281133057,24.3381105219092));
#17875=CARTESIAN_POINT('Ctrl Pts',(3.22284262905124,0.221210429567681,24.3228189241854));
#17876=CARTESIAN_POINT('Ctrl Pts',(3.22274971917068,-0.00134539409721628,
24.3082009925199));
#17877=CARTESIAN_POINT('Ctrl Pts',(3.22274971730435,-0.00134985730486836,
24.3082006993672));
#17878=CARTESIAN_POINT('Ctrl Pts',(3.22272611847844,-0.0576914493070022,
24.3045000684272));
#17879=CARTESIAN_POINT('Ctrl Pts',(3.22122503310341,-0.114027358852287,
24.3008485886178));
#17880=CARTESIAN_POINT('Ctrl Pts',(3.21763171638925,-0.181932434322062,
24.2965283935334));
#17881=CARTESIAN_POINT('Ctrl Pts',(3.216953041538,-0.193562421226479,24.2957913636844));
#17882=CARTESIAN_POINT('Ctrl Pts',(3.21574738020973,-0.212460450845194,
24.2945986987601));
#17883=CARTESIAN_POINT('Ctrl Pts',(3.21525878745669,-0.21973071835699,24.2941410634133));
#17884=CARTESIAN_POINT('Ctrl Pts',(3.21435594844119,-0.232516647997579,
24.2933384153753));
#17885=CARTESIAN_POINT('Ctrl Pts',(3.21395215492318,-0.238032984740623,
24.2929928356879));
#17886=CARTESIAN_POINT('Ctrl Pts',(3.21312678841451,-0.248923405379457,
24.2923120331622));
#17887=CARTESIAN_POINT('Ctrl Pts',(3.21270592952824,-0.25429752705337,24.2919767729835));
#17888=CARTESIAN_POINT('Ctrl Pts',(3.21177217405417,-0.265848604809996,
24.2912576917194));
#17889=CARTESIAN_POINT('Ctrl Pts',(3.21125494200837,-0.272025141616444,
24.2908741176208));
#17890=CARTESIAN_POINT('Ctrl Pts',(3.20983274749543,-0.288438746112081,
24.2898571834809));
#17891=CARTESIAN_POINT('Ctrl Pts',(3.20889662305333,-0.298673143100265,
24.2892255556648));
#17892=CARTESIAN_POINT('Ctrl Pts',(3.20467668553058,-0.34249655741897,24.286530826195));
#17893=CARTESIAN_POINT('Ctrl Pts',(3.20091418699029,-0.376038731325203,
24.2844931858975));
#17894=CARTESIAN_POINT('Ctrl Pts',(3.19574890328151,-0.416358111283861,
24.2820672109328));
#17895=CARTESIAN_POINT('Ctrl Pts',(3.19485054474195,-0.42319632322785,24.2816565748235));
#17896=CARTESIAN_POINT('Ctrl Pts',(3.18845352662548,-0.470708243187338,
24.2788087941088));
#17897=CARTESIAN_POINT('Ctrl Pts',(3.18220002482987,-0.511278227520204,
24.2764042004489));
#17898=CARTESIAN_POINT('Ctrl Pts',(3.13231992230041,-0.798340774617772,
24.2595135074652));
#17899=CARTESIAN_POINT('Ctrl Pts',(3.06087826987678,-1.03914359726351,24.2459311725056));
#17900=CARTESIAN_POINT('Ctrl Pts',(2.92363227638845,-1.35945570862508,24.2261474396549));
#17901=CARTESIAN_POINT('Ctrl Pts',(2.88089121046845,-1.44782909361593,24.2204997571257));
#17902=CARTESIAN_POINT('Ctrl Pts',(2.8062170288156,-1.58578568515502,24.2112628227676));
#17903=CARTESIAN_POINT('Ctrl Pts',(2.77683940710086,-1.63668338424854,24.2077588242451));
#17904=CARTESIAN_POINT('Ctrl Pts',(2.7369487043779,-1.70162695297487,24.2031480172696));
#17905=CARTESIAN_POINT('Ctrl Pts',(2.72768846474372,-1.7164317982755,24.2020872596129));
#17906=CARTESIAN_POINT('Ctrl Pts',(2.71244543505698,-1.74036675915395,24.2003562313325));
#17907=CARTESIAN_POINT('Ctrl Pts',(2.70653569253712,-1.74954315034476,24.1996886836483));
#17908=CARTESIAN_POINT('Ctrl Pts',(2.69508894200696,-1.76712036576084,24.1984024204139));
#17909=CARTESIAN_POINT('Ctrl Pts',(2.68955897647542,-1.77552564070816,24.1977839743252));
#17910=CARTESIAN_POINT('Ctrl Pts',(2.67681702397765,-1.79469665829309,24.1963656067243));
#17911=CARTESIAN_POINT('Ctrl Pts',(2.66957931922211,-1.80544502149589,24.1955647189245));
#17912=CARTESIAN_POINT('Ctrl Pts',(2.65019728662681,-1.83385697006,24.1934324056417));
#17913=CARTESIAN_POINT('Ctrl Pts',(2.63794137482374,-1.85144330505086,24.192096744609));
#17914=CARTESIAN_POINT('Ctrl Pts',(2.54217306659655,-1.985982334368,24.1817543975051));
#17915=CARTESIAN_POINT('Ctrl Pts',(2.45110923366623,-2.0973371635772,24.1724530051659));
#17916=CARTESIAN_POINT('Ctrl Pts',(2.21079083088228,-2.35410047327926,24.1491339007185));
#17917=CARTESIAN_POINT('Ctrl Pts',(2.05428412735991,-2.4918450984332,24.1349007799878));
#17918=CARTESIAN_POINT('Ctrl Pts',(1.81911399923169,-2.66151580122257,24.1154524185763));
#17919=CARTESIAN_POINT('Ctrl Pts',(1.75080032782474,-2.70694332886011,24.1100094466256));
#17920=CARTESIAN_POINT('Ctrl Pts',(1.65651091706464,-2.7645797371878,24.1028383669054));
#17921=CARTESIAN_POINT('Ctrl Pts',(1.63200121828692,-2.7791188685191,24.1010042582028));
#17922=CARTESIAN_POINT('Ctrl Pts',(1.59549065752063,-2.8001272812595,24.0983196034499));
#17923=CARTESIAN_POINT('Ctrl Pts',(1.58363707821053,-2.80684820551168,24.09745529088));
#17924=CARTESIAN_POINT('Ctrl Pts',(1.56211690328792,-2.81887031844465,24.0958997672088));
#17925=CARTESIAN_POINT('Ctrl Pts',(1.55246512261849,-2.8241974334514,24.0952070320824));
#17926=CARTESIAN_POINT('Ctrl Pts',(1.53723218844534,-2.83250327040854,24.0941216665714));
#17927=CARTESIAN_POINT('Ctrl Pts',(1.53166938281182,-2.83551520564763,24.0937269671112));
#17928=CARTESIAN_POINT('Ctrl Pts',(1.52608297889153,-2.83851868134005,24.0933322802369));
#17929=CARTESIAN_POINT('Ctrl Pts',(1.52606826931835,-2.83852658965151,24.0933312409977));
#17930=CARTESIAN_POINT('Ctrl Pts',(1.52603876597003,-2.83854245124831,24.0933291565938));
#17931=CARTESIAN_POINT('Ctrl Pts',(1.52602397223478,-2.83855040451053,24.0933281114321));
#17932=CARTESIAN_POINT('Ctrl Pts',(1.52599429994296,-2.83856635633676,24.09332601514));
#17933=CARTESIAN_POINT('Ctrl Pts',(1.52597942145734,-2.83857435486092,24.0933249640146));
#17934=CARTESIAN_POINT('Ctrl Pts',(1.52594957915564,-2.83859039747959,24.0933228557596));
#17935=CARTESIAN_POINT('Ctrl Pts',(1.52593461528087,-2.83859844160393,24.0933217986259));
#17936=CARTESIAN_POINT('Ctrl Pts',(1.52590460158884,-2.83861457574676,24.0933196783114));
#17937=CARTESIAN_POINT('Ctrl Pts',(1.52588955181141,-2.83862266574209,24.0933186151335));
#17938=CARTESIAN_POINT('Ctrl Pts',(1.52585936573625,-2.83863889193224,24.0933164826902));
#17939=CARTESIAN_POINT('Ctrl Pts',(1.52584422940474,-2.83864702814344,24.0933154134225));
#17940=CARTESIAN_POINT('Ctrl Pts',(1.52581386970112,-2.83866334703966,24.0933132687632));
#17941=CARTESIAN_POINT('Ctrl Pts',(1.52579864621495,-2.8386715297842,24.0933121933637));
#17942=CARTESIAN_POINT('Ctrl Pts',(1.52576811152512,-2.83868794210552,24.0933100363934));
#17943=CARTESIAN_POINT('Ctrl Pts',(1.52575280035856,-2.83869617166053,24.0933089548254));
#17944=CARTESIAN_POINT('Ctrl Pts',(1.52572208969444,-2.83871267792711,24.0933067854752));
#17945=CARTESIAN_POINT('Ctrl Pts',(1.52570669016765,-2.83872095465252,24.093305697691));
#17946=CARTESIAN_POINT('Ctrl Pts',(1.52567580207615,-2.83873755563428,24.0933035158591));
#17947=CARTESIAN_POINT('Ctrl Pts',(1.52566031365799,-2.83874587980999,24.0933024218218));
#17948=CARTESIAN_POINT('Ctrl Pts',(1.52562924723898,-2.83876257597951,24.0933002274456));
#17949=CARTESIAN_POINT('Ctrl Pts',(1.52561366918939,-2.83877094799761,24.0932991271033));
#17950=CARTESIAN_POINT('Ctrl Pts',(1.52558242299352,-2.83878774012247,24.0932969200811));
#17951=CARTESIAN_POINT('Ctrl Pts',(1.52556675473582,-2.83879616028718,24.0932958133936));
#17952=CARTESIAN_POINT('Ctrl Pts',(1.52553532736088,-2.83881304910943,24.0932935936275));
#17953=CARTESIAN_POINT('Ctrl Pts',(1.52551956836973,-2.83882151769728,24.093292480558));
#17954=CARTESIAN_POINT('Ctrl Pts',(1.52081608179185,-2.84134903316195,24.0929602737499));
#17955=CARTESIAN_POINT('Ctrl Pts',(1.51612218716979,-2.84385643043855,24.0926299394626));
#17956=CARTESIAN_POINT('Ctrl Pts',(1.505127765827,-2.84969450276225,24.0918589687811));
#17957=CARTESIAN_POINT('Ctrl Pts',(1.49882239364927,-2.85301591042443,24.0914189239173));
#17958=CARTESIAN_POINT('Ctrl Pts',(1.47952275217551,-2.8631005180928,24.0900783058564));
#17959=CARTESIAN_POINT('Ctrl Pts',(1.46649313046066,-2.86979617186681,24.0891818961851));
#17960=CARTESIAN_POINT('Ctrl Pts',(1.3534305405323,-2.92692558378284,24.0814742459288));
#17961=CARTESIAN_POINT('Ctrl Pts',(1.25086482383982,-2.97220633841499,24.074958445455));
#17962=CARTESIAN_POINT('Ctrl Pts',(0.938878597766879,-3.09092231841185,
24.0559336421543));
#17963=CARTESIAN_POINT('Ctrl Pts',(0.724030821360556,-3.14818670966018,
24.043817715302));
#17964=CARTESIAN_POINT('Ctrl Pts',(0.414149559277967,-3.197351884165,24.0259558215109));
#17965=CARTESIAN_POINT('Ctrl Pts',(0.32273079920224,-3.20786873594387,24.0206465905525));
#17966=CARTESIAN_POINT('Ctrl Pts',(0.175012104098916,-3.21848384762885,
24.0119137764077));
#17967=CARTESIAN_POINT('Ctrl Pts',(0.118939287106756,-3.22104336867269,
24.0085638022479));
#17968=CARTESIAN_POINT('Ctrl Pts',(0.045654698846357,-3.22247239507271,
24.0041283121576));
#17969=CARTESIAN_POINT('Ctrl Pts',(0.0284765932823386,-3.22266997292476,
24.0030845396962));
#17970=CARTESIAN_POINT('Ctrl Pts',(0.000445749918927757,-3.22276824116028,
24.001374358534));
#17971=CARTESIAN_POINT('Ctrl Pts',(-0.0104065000985307,-3.22275146964891,
24.0007105494556));
#17972=CARTESIAN_POINT('Ctrl Pts',(-0.0313405787650945,-3.22261337834556,
23.9994266819546));
#17973=CARTESIAN_POINT('Ctrl Pts',(-0.0414223426062536,-3.22249955841968,
23.9988068668742));
#17974=CARTESIAN_POINT('Ctrl Pts',(-0.0645981823043494,-3.22212913407854,
23.997378499618));
#17975=CARTESIAN_POINT('Ctrl Pts',(-0.0776914929905667,-3.22184001862488,
23.9965689347545));
#17976=CARTESIAN_POINT('Ctrl Pts',(-0.112682024448718,-3.22085396949826,
23.994398339621));
#17977=CARTESIAN_POINT('Ctrl Pts',(-0.134574211536866,-3.22001355195475,
23.9930328287572));
#17978=CARTESIAN_POINT('Ctrl Pts',(-0.320111452152123,-3.21099559303374,
23.9813949179584));
#17979=CARTESIAN_POINT('Ctrl Pts',(-0.48289642428386,-3.19057367892996,
23.9707353284948));
#17980=CARTESIAN_POINT('Ctrl Pts',(-0.892458755343471,-3.10712708071275,
23.9428577648043));
#17981=CARTESIAN_POINT('Ctrl Pts',(-1.1346241356111,-3.02710168051018,23.9253125334914));
#17982=CARTESIAN_POINT('Ctrl Pts',(-1.40200467514313,-2.90209940887585,
23.9060049343196));
#17983=CARTESIAN_POINT('Ctrl Pts',(-1.43880709431877,-2.88403057601107,
23.9033511807881));
#17984=CARTESIAN_POINT('Ctrl Pts',(-1.47525540579296,-2.86526421995924,
23.9007338658376));
#17985=CARTESIAN_POINT('',(3.22274871883436,0.00294606298623907,24.0644510358235));
#17986=CARTESIAN_POINT('Ctrl Pts',(-1.47525500221108,-2.86526442775378,
23.6562919783988));
#17987=CARTESIAN_POINT('Ctrl Pts',(-1.35501449326435,-2.92717334288701,
23.66539566089));
#17988=CARTESIAN_POINT('Ctrl Pts',(-1.23093834006357,-2.98148176035773,
23.6746058007793));
#17989=CARTESIAN_POINT('Ctrl Pts',(-1.06125504918383,-3.04333723869333,
23.6867427906442));
#17990=CARTESIAN_POINT('Ctrl Pts',(-1.01843236752905,-3.05793387479908,
23.6897675694313));
#17991=CARTESIAN_POINT('Ctrl Pts',(-0.896131251797879,-3.09676744961024,
23.6982752342562));
#17992=CARTESIAN_POINT('Ctrl Pts',(-0.815996610383085,-3.11884145230336,
23.7036952953616));
#17993=CARTESIAN_POINT('Ctrl Pts',(-0.721854105060323,-3.14089621823618,
23.7098174001187));
#17994=CARTESIAN_POINT('Ctrl Pts',(-0.708597134893948,-3.14391356727594,
23.7106738953522));
#17995=CARTESIAN_POINT('Ctrl Pts',(-0.688482717532451,-3.14835800983582,
23.7119645330641));
#17996=CARTESIAN_POINT('Ctrl Pts',(-0.681639256307718,-3.14984674816108,
23.7124020863922));
#17997=CARTESIAN_POINT('Ctrl Pts',(-0.669338399808847,-3.15248073145383,
23.7131857109715));
#17998=CARTESIAN_POINT('Ctrl Pts',(-0.663882863291371,-3.15363412604507,
23.7135322420379));
#17999=CARTESIAN_POINT('Ctrl Pts',(-0.652004743979297,-3.15611317622217,
23.7142845204303));
#18000=CARTESIAN_POINT('Ctrl Pts',(-0.64558111997756,-3.15743338593735,
23.7146899536029));
#18001=CARTESIAN_POINT('Ctrl Pts',(-0.627495999504634,-3.1610928162827,
23.7158276049144));
#18002=CARTESIAN_POINT('Ctrl Pts',(-0.615825375341265,-3.16338713089543,
23.7165573005808));
#18003=CARTESIAN_POINT('Ctrl Pts',(-0.545596904617962,-3.17678988256905,
23.7209230150544));
#18004=CARTESIAN_POINT('Ctrl Pts',(-0.486748636447364,-3.18633751389046,
23.7244759221006));
#18005=CARTESIAN_POINT('Ctrl Pts',(-0.178351781968121,-3.22762754863927,
23.7427058563803));
#18006=CARTESIAN_POINT('Ctrl Pts',(0.0740337350894962,-3.23170749934384,
23.756361700223));
#18007=CARTESIAN_POINT('Ctrl Pts',(0.48616298444265,-3.19001820592334,23.7797667809561));
#18008=CARTESIAN_POINT('Ctrl Pts',(0.646489030090305,-3.16142567068359,
23.7891427035139));
#18009=CARTESIAN_POINT('Ctrl Pts',(0.825147708080403,-3.11540166303046,
23.8002395684217));
#18010=CARTESIAN_POINT('Ctrl Pts',(0.846278637719261,-3.10972807385802,
23.8015622885838));
#18011=CARTESIAN_POINT('Ctrl Pts',(0.879952695819982,-3.10031805667791,
23.8036872587954));
#18012=CARTESIAN_POINT('Ctrl Pts',(0.892533907208071,-3.09671955720899,
23.8044850207787));
#18013=CARTESIAN_POINT('Ctrl Pts',(0.914765038984831,-3.09021424025871,
23.8059016204532));
#18014=CARTESIAN_POINT('Ctrl Pts',(0.924423949925147,-3.08733857624765,
23.8065194315728));
#18015=CARTESIAN_POINT('Ctrl Pts',(0.944454518431882,-3.08127262228611,
23.8078055606249));
#18016=CARTESIAN_POINT('Ctrl Pts',(0.954823855481484,-3.07807516325195,
23.8084741075427));
#18017=CARTESIAN_POINT('Ctrl Pts',(0.981573251099225,-3.0696786232762,23.8102059439827));
#18018=CARTESIAN_POINT('Ctrl Pts',(0.997928063356344,-3.06440083203845,
23.8112718163663));
#18019=CARTESIAN_POINT('Ctrl Pts',(1.06661739791045,-3.04162619505369,23.8157785566935));
#18020=CARTESIAN_POINT('Ctrl Pts',(1.11853767362501,-3.02291836625736,23.819259273343));
#18021=CARTESIAN_POINT('Ctrl Pts',(1.25406706855988,-2.97011500583209,23.8285482522597));
#18022=CARTESIAN_POINT('Ctrl Pts',(1.33676343911608,-2.93382488745419,23.834425563345));
#18023=CARTESIAN_POINT('Ctrl Pts',(1.59670386779309,-2.80648049592037,23.8535589079507));
#18024=CARTESIAN_POINT('Ctrl Pts',(1.76706723784177,-2.70245417439077,23.8671501579441));
#18025=CARTESIAN_POINT('Ctrl Pts',(2.03630191168107,-2.50165529906279,23.8897674708355));
#18026=CARTESIAN_POINT('Ctrl Pts',(2.140585387477,-2.41302877311659,23.8988554990754));
#18027=CARTESIAN_POINT('Ctrl Pts',(2.24970502970148,-2.30763278737043,23.9084746082637));
#18028=CARTESIAN_POINT('Ctrl Pts',(2.26040347840411,-2.29715431289018,23.9094188920179));
#18029=CARTESIAN_POINT('Ctrl Pts',(2.27612957281539,-2.28153531948098,23.9108081763813));
#18030=CARTESIAN_POINT('Ctrl Pts',(2.28121349740218,-2.27645211413106,23.911257498303));
#18031=CARTESIAN_POINT('Ctrl Pts',(2.29022094497711,-2.26738546476366,23.9120538598688));
#18032=CARTESIAN_POINT('Ctrl Pts',(2.29415114698657,-2.26340878745183,23.9124014250934));
#18033=CARTESIAN_POINT('Ctrl Pts',(2.30257549373215,-2.25484033533461,23.9131466079634));
#18034=CARTESIAN_POINT('Ctrl Pts',(2.30706624983459,-2.25024535612596,23.9135439615046));
#18035=CARTESIAN_POINT('Ctrl Pts',(2.31626327062054,-2.24077841545018,23.9143580627839));
#18036=CARTESIAN_POINT('Ctrl Pts',(2.32096798053656,-2.23590498036585,23.9147746906139));
#18037=CARTESIAN_POINT('Ctrl Pts',(2.34278176513552,-2.2131658460865,23.9167074534881));
#18038=CARTESIAN_POINT('Ctrl Pts',(2.3597007016229,-2.19511779775449,23.9182094898553));
#18039=CARTESIAN_POINT('Ctrl Pts',(2.4603058140135,-2.0852911203896,23.9271722835486));
#18040=CARTESIAN_POINT('Ctrl Pts',(2.5388459193516,-1.98892229591896,23.9343035936125));
#18041=CARTESIAN_POINT('Ctrl Pts',(2.67497785140488,-1.80063858862975,23.9474288538256));
#18042=CARTESIAN_POINT('Ctrl Pts',(2.73387462724788,-1.70989363532544,23.953442110129));
#18043=CARTESIAN_POINT('Ctrl Pts',(2.89936381633995,-1.42443695814654,23.9718991429425));
#18044=CARTESIAN_POINT('Ctrl Pts',(2.99049838142456,-1.22156937410308,23.9844482723722));
#18045=CARTESIAN_POINT('Ctrl Pts',(3.06700682795415,-0.989987288220592,
23.9991153671845));
#18046=CARTESIAN_POINT('Ctrl Pts',(3.07372163147684,-0.968938082916184,
24.0004509022121));
#18047=CARTESIAN_POINT('Ctrl Pts',(3.08408632943807,-0.935255021296776,
24.0025925643959));
#18048=CARTESIAN_POINT('Ctrl Pts',(3.08787632344865,-0.92266475240612,24.0033940899914));
#18049=CARTESIAN_POINT('Ctrl Pts',(3.09443776181317,-0.900374513825484,
24.0048150503338));
#18050=CARTESIAN_POINT('Ctrl Pts',(3.0972409212201,-0.890684006326842,24.0054334374104));
#18051=CARTESIAN_POINT('Ctrl Pts',(3.10295746209706,-0.870568616125252,
24.006718460023));
#18052=CARTESIAN_POINT('Ctrl Pts',(3.1058639082949,-0.860141910117466,24.0073853131027));
#18053=CARTESIAN_POINT('Ctrl Pts',(3.11321653887819,-0.833241557047083,
24.0091078315793));
#18054=CARTESIAN_POINT('Ctrl Pts',(3.11758447447725,-0.816747045776657,
24.010166027344));
#18055=CARTESIAN_POINT('Ctrl Pts',(3.12675520766976,-0.780970098158403,
24.0124658587325));
#18056=CARTESIAN_POINT('Ctrl Pts',(3.13151103668481,-0.761676454577913,
24.0137089685928));
#18057=CARTESIAN_POINT('Ctrl Pts',(3.14484963700839,-0.705326261651034,
24.0173484380911));
#18058=CARTESIAN_POINT('Ctrl Pts',(3.15295492175332,-0.668161236810485,
24.0197598422052));
#18059=CARTESIAN_POINT('Ctrl Pts',(3.20206604532974,-0.422131776493012,
24.0357991765311));
#18060=CARTESIAN_POINT('Ctrl Pts',(3.22294311519104,-0.209825326838229,
24.0500514525995));
#18061=CARTESIAN_POINT('Ctrl Pts',(3.22274865402096,0.00294542120983694,
24.0644511057929));
#18062=CARTESIAN_POINT('Ctrl Pts',(3.22274865344138,0.00294605528672446,
24.0644511487053));
#18063=CARTESIAN_POINT('Ctrl Pts',(3.22257424051969,0.193739829951134,24.0773634697639));
#18064=CARTESIAN_POINT('Ctrl Pts',(3.20545713209499,0.38416323532263,24.0903280746391));
#18065=CARTESIAN_POINT('Ctrl Pts',(3.1680420070958,0.591630312469549,24.1038803127039));
#18066=CARTESIAN_POINT('Ctrl Pts',(3.16431396051559,0.611255911091983,24.1051562853375));
#18067=CARTESIAN_POINT('Ctrl Pts',(3.1583337291344,0.6412155863569,24.1070936217749));
#18068=CARTESIAN_POINT('Ctrl Pts',(3.15621283004422,0.651574977527513,24.1077615797314));
#18069=CARTESIAN_POINT('Ctrl Pts',(3.15263594041671,0.668618713616982,24.1088571419945));
#18070=CARTESIAN_POINT('Ctrl Pts',(3.15120960487839,0.675309103398219,24.109286333799));
#18071=CARTESIAN_POINT('Ctrl Pts',(3.14839236198354,0.688320408276996,24.1101192671277));
#18072=CARTESIAN_POINT('Ctrl Pts',(3.14700369587475,0.694641770517087,24.1105231315873));
#18073=CARTESIAN_POINT('Ctrl Pts',(3.14438127631797,0.70641003762993,24.1112734370777));
#18074=CARTESIAN_POINT('Ctrl Pts',(3.14315242014287,0.711857862594848,24.1116201436863));
#18075=CARTESIAN_POINT('Ctrl Pts',(3.14032474832309,0.724243553994647,24.1124069797451));
#18076=CARTESIAN_POINT('Ctrl Pts',(3.13871710354107,0.731179319092189,24.112846595562));
#18077=CARTESIAN_POINT('Ctrl Pts',(3.13373785625912,0.752341928964205,24.1141850723056));
#18078=CARTESIAN_POINT('Ctrl Pts',(3.13029235685533,0.766551439356025,24.1150797877288));
#18079=CARTESIAN_POINT('Ctrl Pts',(3.08084063353047,0.964599082230346,24.1275004397034));
#18080=CARTESIAN_POINT('Ctrl Pts',(3.01879557047716,1.1440828570201,24.1381704702521));
#18081=CARTESIAN_POINT('Ctrl Pts',(2.89741941620183,1.41513912309252,24.1547879539275));
#18082=CARTESIAN_POINT('Ctrl Pts',(2.84864104414521,1.51092747489552,24.1607653099469));
#18083=CARTESIAN_POINT('Ctrl Pts',(2.7303686184339,1.71701921436141,24.1741611830375));
#18084=CARTESIAN_POINT('Ctrl Pts',(2.65878889794799,1.82589830084581,24.1816066354104));
#18085=CARTESIAN_POINT('Ctrl Pts',(2.54802211060111,1.97400629539456,24.1925187698509));
#18086=CARTESIAN_POINT('Ctrl Pts',(2.51410726639772,2.01702296614655,24.1957891554825));
#18087=CARTESIAN_POINT('Ctrl Pts',(2.4681434522575,2.07236103966723,24.2001423084582));
#18088=CARTESIAN_POINT('Ctrl Pts',(2.4570674392062,2.08548123009915,24.2011855405999));
#18089=CARTESIAN_POINT('Ctrl Pts',(2.43882364003762,2.10674499904715,24.2028949074325));
#18090=CARTESIAN_POINT('Ctrl Pts',(2.43171855068622,2.11494210888023,24.203558445607));
#18091=CARTESIAN_POINT('Ctrl Pts',(2.41793229060742,2.13068594338065,24.2048418382391));
#18092=CARTESIAN_POINT('Ctrl Pts',(2.41125682657882,2.13823751343846,24.2054614497991));
#18093=CARTESIAN_POINT('Ctrl Pts',(2.39582833611797,2.15552675295422,24.2068894171928));
#18094=CARTESIAN_POINT('Ctrl Pts',(2.38705121559434,2.16524259260801,24.2076987854872));
#18095=CARTESIAN_POINT('Ctrl Pts',(2.3634322150114,2.19106950381674,24.2098690023689));
#18096=CARTESIAN_POINT('Ctrl Pts',(2.34848507152311,2.20708296991166,24.2112343309402));
#18097=CARTESIAN_POINT('Ctrl Pts',(2.22028468992882,2.34165222240276,24.2228787541535));
#18098=CARTESIAN_POINT('Ctrl Pts',(2.09831732878074,2.45154011020355,24.2335455738464));
#18099=CARTESIAN_POINT('Ctrl Pts',(1.7673728713867,2.70685483234764,24.2614242813834));
#18100=CARTESIAN_POINT('Ctrl Pts',(1.54857277478894,2.83770814833509,24.2789622729782));
#18101=CARTESIAN_POINT('Ctrl Pts',(1.26547648421944,2.96442813989084,24.2992514917287));
#18102=CARTESIAN_POINT('Ctrl Pts',(1.21367736426211,2.9860095596947,24.3028692077757));
#18103=CARTESIAN_POINT('Ctrl Pts',(1.15051361895523,3.01041037375209,24.3071454164687));
#18104=CARTESIAN_POINT('Ctrl Pts',(1.13966691919165,3.01453338491351,24.307874994511));
#18105=CARTESIAN_POINT('Ctrl Pts',(1.12267045947586,3.02088917357439,24.309010547216));
#18106=CARTESIAN_POINT('Ctrl Pts',(1.1165358969297,3.0231619130095,24.3094188475786));
#18107=CARTESIAN_POINT('Ctrl Pts',(1.10515842710991,3.02733769536926,24.3101731645203));
#18108=CARTESIAN_POINT('Ctrl Pts',(1.09991754618758,3.02924579114625,24.3105194731006));
#18109=CARTESIAN_POINT('Ctrl Pts',(1.08806529401254,3.03352613537252,24.311300057659));
#18110=CARTESIAN_POINT('Ctrl Pts',(1.08145112281534,3.03589037502868,24.3117338532452));
#18111=CARTESIAN_POINT('Ctrl Pts',(1.06192221602457,3.04279907468965,24.3130094840718));
#18112=CARTESIAN_POINT('Ctrl Pts',(1.04898599961458,3.04728295205405,24.3138478043363));
#18113=CARTESIAN_POINT('Ctrl Pts',(0.955073852361015,3.07916534133483,24.3198881296645));
#18114=CARTESIAN_POINT('Ctrl Pts',(0.873057049286566,3.10341738120102,24.3249189096906));
#18115=CARTESIAN_POINT('Ctrl Pts',(0.545200965533929,3.18633318101863,24.3444250860297));
#18116=CARTESIAN_POINT('Ctrl Pts',(0.293791480015071,3.21926484363748,24.3581294537396));
#18117=CARTESIAN_POINT('Ctrl Pts',(-0.048898636982619,3.22363584253016,
24.3776584188829));
#18118=CARTESIAN_POINT('Ctrl Pts',(-0.138902661482797,3.22101278182098,
24.3828583027745));
#18119=CARTESIAN_POINT('Ctrl Pts',(-0.283591862806194,3.21072023353168,
24.3914156364599));
#18120=CARTESIAN_POINT('Ctrl Pts',(-0.338397613738702,3.20540719286101,
24.3947027484781));
#18121=CARTESIAN_POINT('Ctrl Pts',(-0.410085940613719,3.19659852064754,
24.399073436722));
#18122=CARTESIAN_POINT('Ctrl Pts',(-0.427116544299522,3.19436754627795,
24.4001170203681));
#18123=CARTESIAN_POINT('Ctrl Pts',(-0.454873866964155,3.19050545076618,
24.4018268184557));
#18124=CARTESIAN_POINT('Ctrl Pts',(-0.465611761865991,3.18895609077262,
24.4024904338522));
#18125=CARTESIAN_POINT('Ctrl Pts',(-0.486309487350851,3.1858628696838,24.4037738742214));
#18126=CARTESIAN_POINT('Ctrl Pts',(-0.496270313999639,3.18432644584016,
24.4043934557498));
#18127=CARTESIAN_POINT('Ctrl Pts',(-0.519151583812424,3.18068711982856,
24.4058212082679));
#18128=CARTESIAN_POINT('Ctrl Pts',(-0.53206668295296,3.17855217952802,24.4066303907225));
#18129=CARTESIAN_POINT('Ctrl Pts',(-0.566548107276294,3.17263615981567,
24.4087997852522));
#18130=CARTESIAN_POINT('Ctrl Pts',(-0.588089213208508,3.1687139346304,24.4101644719775));
#18131=CARTESIAN_POINT('Ctrl Pts',(-0.770085840178279,3.13365611754573,
24.4217763231803));
#18132=CARTESIAN_POINT('Ctrl Pts',(-0.927973620651493,3.09057975835651,
24.4324087088191));
#18133=CARTESIAN_POINT('Ctrl Pts',(-1.32025717203633,2.9507747803975,24.4601814736142));
#18134=CARTESIAN_POINT('Ctrl Pts',(-1.54777290994755,2.83805299065389,24.4776458692179));
#18135=CARTESIAN_POINT('Ctrl Pts',(-1.8079936417756,2.66844369592543,24.4979804078286));
#18136=CARTESIAN_POINT('Ctrl Pts',(-1.85538233226048,2.63571435154134,24.5016954876566));
#18137=CARTESIAN_POINT('Ctrl Pts',(-1.91135408391638,2.59479885318771,24.5060741613684));
#18138=CARTESIAN_POINT('Ctrl Pts',(-1.92079856470474,2.58781537333286,24.5068126715601));
#18139=CARTESIAN_POINT('Ctrl Pts',(-1.93542694946986,2.57687458191231,24.5079557441687));
#18140=CARTESIAN_POINT('Ctrl Pts',(-1.94063726323917,2.57295299256633,24.5083627241473));
#18141=CARTESIAN_POINT('Ctrl Pts',(-1.95028330828932,2.56564684038222,24.5091158314141));
#18142=CARTESIAN_POINT('Ctrl Pts',(-1.95472211262946,2.56226660503796,24.5094622428762));
#18143=CARTESIAN_POINT('Ctrl Pts',(-1.96475112774461,2.55458808655141,24.5102446173204));
#18144=CARTESIAN_POINT('Ctrl Pts',(-1.97033600920023,2.55028298410312,24.5106800903161));
#18145=CARTESIAN_POINT('Ctrl Pts',(-1.9868240186762,2.53748672037562,24.5119652461032));
#18146=CARTESIAN_POINT('Ctrl Pts',(-1.99768687527023,2.52894359397724,24.5128113351084));
#18147=CARTESIAN_POINT('Ctrl Pts',(-2.07802741129571,2.46491884539269,24.5190671529117));
#18148=CARTESIAN_POINT('Ctrl Pts',(-2.14524427402452,2.40664765655043,24.5242915035578));
#18149=CARTESIAN_POINT('Ctrl Pts',(-2.3895978880475,2.17642966234909,24.5436224866327));
#18150=CARTESIAN_POINT('Ctrl Pts',(-2.54919781335098,1.98711577753219,24.5570263705841));
#18151=CARTESIAN_POINT('Ctrl Pts',(-2.73618867289765,1.70521375745317,24.5762892272467));
#18152=CARTESIAN_POINT('Ctrl Pts',(-2.78347382147463,1.62688475057072,24.5815693907238));
#18153=CARTESIAN_POINT('Ctrl Pts',(-2.8541848172216,1.49762156696859,24.5902585224235));
#18154=CARTESIAN_POINT('Ctrl Pts',(-2.87972632738041,1.44790090747874,24.5935948304297));
#18155=CARTESIAN_POINT('Ctrl Pts',(-2.9113980488819,1.38209011206338,24.5980145159087));
#18156=CARTESIAN_POINT('Ctrl Pts',(-2.9187114480335,1.36657789471678,24.5990565196174));
#18157=CARTESIAN_POINT('Ctrl Pts',(-2.93044621215406,1.34116372530757,24.6007643793668));
#18158=CARTESIAN_POINT('Ctrl Pts',(-2.93494208563866,1.33129639442586,24.6014276477208));
#18159=CARTESIAN_POINT('Ctrl Pts',(-2.94352139200188,1.31221225380076,24.6027108741476));
#18160=CARTESIAN_POINT('Ctrl Pts',(-2.94761154979834,1.30299859248107,24.6033305912352));
#18161=CARTESIAN_POINT('Ctrl Pts',(-2.95691885318268,1.28176447401976,24.6047593122509));
#18162=CARTESIAN_POINT('Ctrl Pts',(-2.9621060211994,1.26973114563209,24.6055693321315));
#18163=CARTESIAN_POINT('Ctrl Pts',(-2.97578197872324,1.23746538673076,24.6077424331641));
#18164=CARTESIAN_POINT('Ctrl Pts',(-2.98413766058743,1.21717761746544,24.609110013031));
#18165=CARTESIAN_POINT('Ctrl Pts',(-3.05384232050255,1.04290029460675,24.6208700248884));
#18166=CARTESIAN_POINT('Ctrl Pts',(-3.10342397328423,0.884498958261372,
24.6316591409857));
#18167=CARTESIAN_POINT('Ctrl Pts',(-3.19858321653192,0.471146846063818,
24.6599636844443));
#18168=CARTESIAN_POINT('Ctrl Pts',(-3.22605645590846,0.213236944793662,
24.6778163764528));
#18169=CARTESIAN_POINT('Ctrl Pts',(-3.22172401930047,-0.0957679684971617,
24.6979667566994));
#18170=CARTESIAN_POINT('Ctrl Pts',(-3.21982357415144,-0.146335201340634,
24.7012211786082));
#18171=CARTESIAN_POINT('Ctrl Pts',(-3.21604275273868,-0.208120908132821,
24.7051282270333));
#18172=CARTESIAN_POINT('Ctrl Pts',(-3.21529309003917,-0.219398390933108,
24.7058385276252));
#18173=CARTESIAN_POINT('Ctrl Pts',(-3.21402429071297,-0.237079501621139,
24.7069474576459));
#18174=CARTESIAN_POINT('Ctrl Pts',(-3.21354531693471,-0.243485788293864,
24.7073482816055));
#18175=CARTESIAN_POINT('Ctrl Pts',(-3.21261364118703,-0.255465099830885,
24.7080959297796));
#18176=CARTESIAN_POINT('Ctrl Pts',(-3.21216559704645,-0.261038316189161,
24.7084430012344));
#18177=CARTESIAN_POINT('Ctrl Pts',(-3.21110819325681,-0.273776251626151,
24.7092345413308));
#18178=CARTESIAN_POINT('Ctrl Pts',(-3.21048935919157,-0.280940103289656,
24.7096784717646));
#18179=CARTESIAN_POINT('Ctrl Pts',(-3.20850728258521,-0.30302312887516,
24.7110432743543));
#18180=CARTESIAN_POINT('Ctrl Pts',(-3.20706396082666,-0.31793516684402,
24.711959759517));
#18181=CARTESIAN_POINT('Ctrl Pts',(-3.19131590654687,-0.469602983688038,
24.7212338855888));
#18182=CARTESIAN_POINT('Ctrl Pts',(-3.16837484478286,-0.605338543827791,
24.7291446796844));
#18183=CARTESIAN_POINT('Ctrl Pts',(-3.07645205249276,-0.995412548454738,
24.7517891888525));
#18184=CARTESIAN_POINT('Ctrl Pts',(-2.98492084996148,-1.24324188511642,
24.7661457550968));
#18185=CARTESIAN_POINT('Ctrl Pts',(-2.82896886549267,-1.54563396641735,
24.7859969054275));
#18186=CARTESIAN_POINT('Ctrl Pts',(-2.79122723321879,-1.61279208315098,
24.7905614757138));
#18187=CARTESIAN_POINT('Ctrl Pts',(-2.74115883796554,-1.69485440751456,
24.7963681591959));
#18188=CARTESIAN_POINT('Ctrl Pts',(-2.73105412203849,-1.71108930091418,
24.7975284408806));
#18189=CARTESIAN_POINT('Ctrl Pts',(-2.71476026594254,-1.73675602643589,
24.7993816360599));
#18190=CARTESIAN_POINT('Ctrl Pts',(-2.70866495111433,-1.74624711149348,
24.8000710586049));
#18191=CARTESIAN_POINT('Ctrl Pts',(-2.69708500631615,-1.76407186918021,
24.8013737606688));
#18192=CARTESIAN_POINT('Ctrl Pts',(-2.69161124864599,-1.77241247273957,
24.8019866273004));
#18193=CARTESIAN_POINT('Ctrl Pts',(-2.67919474143217,-1.79114187815173,
24.8033703942696));
#18194=CARTESIAN_POINT('Ctrl Pts',(-2.67223015257595,-1.8015159435289,24.8041421137755));
#18195=CARTESIAN_POINT('Ctrl Pts',(-2.65427230438663,-1.82793169459387,
24.8061208047689));
#18196=CARTESIAN_POINT('Ctrl Pts',(-2.64319397347033,-1.84391467746543,
24.8073310015509));
#18197=CARTESIAN_POINT('Ctrl Pts',(-2.57560407308937,-1.93956748158224,
24.8146532787511));
#18198=CARTESIAN_POINT('Ctrl Pts',(-2.51564431600867,-2.01672723703995,
24.8208980368232));
#18199=CARTESIAN_POINT('Ctrl Pts',(-2.29286218676216,-2.27799627353853,
24.8432841146092));
#18200=CARTESIAN_POINT('Ctrl Pts',(-2.11260008273383,-2.44609423178966,
24.8600822154122));
#18201=CARTESIAN_POINT('Ctrl Pts',(-1.84204021754391,-2.64598590899664,
24.8827048183809));
#18202=CARTESIAN_POINT('Ctrl Pts',(-1.76679712149156,-2.69680994220845,
24.8887499449085));
#18203=CARTESIAN_POINT('Ctrl Pts',(-1.65046625954378,-2.76842558155146,
24.8976314203449));
#18204=CARTESIAN_POINT('Ctrl Pts',(-1.61091764544294,-2.79162388744239,
24.9005739217351));
#18205=CARTESIAN_POINT('Ctrl Pts',(-1.56131714403665,-2.81931311054701,
24.904157648408));
#18206=CARTESIAN_POINT('Ctrl Pts',(-1.55172175648461,-2.82460567835484,
24.9048460720236));
#18207=CARTESIAN_POINT('Ctrl Pts',(-1.53652518306164,-2.83288690619727,
24.9059284729544));
#18208=CARTESIAN_POINT('Ctrl Pts',(-1.53094194720685,-2.83590807633515,
24.9063244780817));
#18209=CARTESIAN_POINT('Ctrl Pts',(-1.52041282290657,-2.8415653820085,24.9070680905975));
#18210=CARTESIAN_POINT('Ctrl Pts',(-1.51546904594834,-2.84420508113547,
24.9074159157253));
#18211=CARTESIAN_POINT('Ctrl Pts',(-1.50416561272706,-2.85020264020476,
24.9082081927912));
#18212=CARTESIAN_POINT('Ctrl Pts',(-1.49780159394352,-2.85355211416973,
24.9086521101939));
#18213=CARTESIAN_POINT('Ctrl Pts',(-1.48604397850216,-2.859690144328,24.909468398825));
#18214=CARTESIAN_POINT('Ctrl Pts',(-1.48065364408144,-2.86248479733007,
24.9098411429068));
#18215=CARTESIAN_POINT('Ctrl Pts',(-1.47525540501177,-2.86526422036146,
24.9102129806979));
#18216=CARTESIAN_POINT('Origin',(0.,0.,4.68922655072688));
#18217=CARTESIAN_POINT('',(-1.47525541363878,-2.86526421591962,26.4061645232028));
#18218=CARTESIAN_POINT('',(-1.47525540475399,-2.86526422049419,26.1560859507638));
#18219=CARTESIAN_POINT('',(-1.47525540501186,-2.86526422036142,4.68922655072688));
#18220=CARTESIAN_POINT('Ctrl Pts',(-1.47525541363878,-2.86526421591962,
26.4061645232028));
#18221=CARTESIAN_POINT('Ctrl Pts',(-1.49437271054214,-2.85542118099316,
26.4049081860839));
#18222=CARTESIAN_POINT('Ctrl Pts',(-1.51339234256502,-2.84538638249555,
26.4036461231082));
#18223=CARTESIAN_POINT('Ctrl Pts',(-1.58152110791012,-2.8085650247018,26.3990792002463));
#18224=CARTESIAN_POINT('Ctrl Pts',(-1.6300275542405,-2.78069345911704,26.3957401893084));
#18225=CARTESIAN_POINT('Ctrl Pts',(-1.69243203781556,-2.74264211624054,
26.3913171978019));
#18226=CARTESIAN_POINT('Ctrl Pts',(-1.70701021100412,-2.73359252673386,
26.3902746625154));
#18227=CARTESIAN_POINT('Ctrl Pts',(-1.73068561384604,-2.71863247652253,
26.3885659991755));
#18228=CARTESIAN_POINT('Ctrl Pts',(-1.73982661520454,-2.71279165820974,
26.387902461847));
#18229=CARTESIAN_POINT('Ctrl Pts',(-1.75740785646367,-2.70143237511691,
26.3866187618656));
#18230=CARTESIAN_POINT('Ctrl Pts',(-1.7658520368185,-2.69592021982569,26.3859988406283));
#18231=CARTESIAN_POINT('Ctrl Pts',(-1.78521192476018,-2.68315257480135,
26.3845697149569));
#18232=CARTESIAN_POINT('Ctrl Pts',(-1.79610946193147,-2.67586997975815,
26.3837594943195));
#18233=CARTESIAN_POINT('Ctrl Pts',(-1.82513239980708,-2.6562173908634,26.3815859966515));
#18234=CARTESIAN_POINT('Ctrl Pts',(-1.84317614086882,-2.64372857525326,
26.3802182201753));
#18235=CARTESIAN_POINT('Ctrl Pts',(-1.99459951884756,-2.53661852262063,
26.368597475364));
#18236=CARTESIAN_POINT('Ctrl Pts',(-2.12070576701038,-2.43217047499999,
26.357958917567));
#18237=CARTESIAN_POINT('Ctrl Pts',(-2.42083720081386,-2.14243240948653,
26.3301372753071));
#18238=CARTESIAN_POINT('Ctrl Pts',(-2.58189619254346,-1.94532169329057,
26.3126277107222));
#18239=CARTESIAN_POINT('Ctrl Pts',(-2.74871538784876,-1.6834229981886,26.2923078985636));
#18240=CARTESIAN_POINT('Ctrl Pts',(-2.77798441571817,-1.63467207753564,
26.2886410349935));
#18241=CARTESIAN_POINT('Ctrl Pts',(-2.81170771435265,-1.5749775564791,26.2843112435461));
#18242=CARTESIAN_POINT('Ctrl Pts',(-2.81740967441512,-1.5647547126614,26.283575305766));
#18243=CARTESIAN_POINT('Ctrl Pts',(-2.82619781648782,-1.54879498095685,
26.2824352565669));
#18244=CARTESIAN_POINT('Ctrl Pts',(-2.82932244802206,-1.54307954359416,
26.282028748756));
#18245=CARTESIAN_POINT('Ctrl Pts',(-2.83509271784213,-1.53244836985969,
26.2812759348151));
#18246=CARTESIAN_POINT('Ctrl Pts',(-2.83774288742173,-1.52753527967774,
26.2809293479846));
#18247=CARTESIAN_POINT('Ctrl Pts',(-2.84371932136872,-1.51638647109498,
26.2801458325333));
#18248=CARTESIAN_POINT('Ctrl Pts',(-2.84703784000565,-1.51014669759899,
26.2797093988586));
#18249=CARTESIAN_POINT('Ctrl Pts',(-2.85681593115487,-1.49161426989157,
26.2784191897046));
#18250=CARTESIAN_POINT('Ctrl Pts',(-2.86321670628529,-1.47929054062845,
26.277569048921));
#18251=CARTESIAN_POINT('Ctrl Pts',(-2.91082968553497,-1.38615204423006,
26.2711998180889));
#18252=CARTESIAN_POINT('Ctrl Pts',(-2.94869692591549,-1.30366278618734,
26.2658737775924));
#18253=CARTESIAN_POINT('Ctrl Pts',(-3.07554994633257,-0.993411060313955,
26.2465909873751));
#18254=CARTESIAN_POINT('Ctrl Pts',(-3.14202378558033,-0.75734613622741,
26.2333069327312));
#18255=CARTESIAN_POINT('Ctrl Pts',(-3.19585665350666,-0.425478441997348,
26.2141647708085));
#18256=CARTESIAN_POINT('Ctrl Pts',(-3.20667074374613,-0.334353818609813,
26.2088697659733));
#18257=CARTESIAN_POINT('Ctrl Pts',(-3.21780506728464,-0.187044021619061,
26.2001582178935));
#18258=CARTESIAN_POINT('Ctrl Pts',(-3.22056964652205,-0.131093459642534,
26.1968148151285));
#18259=CARTESIAN_POINT('Ctrl Pts',(-3.22227486113773,-0.057939481492352,
26.1923868164082));
#18260=CARTESIAN_POINT('Ctrl Pts',(-3.22253776982305,-0.0407746068155915,
26.191343785054));
#18261=CARTESIAN_POINT('Ctrl Pts',(-3.22274300451921,-0.0127594163426344,
26.1896345131272));
#18262=CARTESIAN_POINT('Ctrl Pts',(-3.22276769618982,-0.00190990202893975,
26.1889708668458));
#18263=CARTESIAN_POINT('Ctrl Pts',(-3.22270963174659,0.0190228131898359,
26.187687099813));
#18264=CARTESIAN_POINT('Ctrl Pts',(-3.22263433849987,0.029105920484238,
26.1870672212501));
#18265=CARTESIAN_POINT('Ctrl Pts',(-3.22235239782335,0.0522902485944937,
26.1856384001866));
#18266=CARTESIAN_POINT('Ctrl Pts',(-3.22211316955261,0.0653908273462473,
26.1848284428948));
#18267=CARTESIAN_POINT('Ctrl Pts',(-3.22125996871502,0.10041258012561,26.1826561109859));
#18268=CARTESIAN_POINT('Ctrl Pts',(-3.22050213272348,0.122329256601399,
26.1812892444995));
#18269=CARTESIAN_POINT('Ctrl Pts',(-3.21213918072427,0.30900030424193,26.1695820796339));
#18270=CARTESIAN_POINT('Ctrl Pts',(-3.19212199837172,0.472928631508612,
26.1588492419612));
#18271=CARTESIAN_POINT('Ctrl Pts',(-3.10912343611939,0.886186050045341,
26.1307279401542));
#18272=CARTESIAN_POINT('Ctrl Pts',(-3.0287247347511,1.13083886826542,26.1130063861888));
#18273=CARTESIAN_POINT('Ctrl Pts',(-2.89775588321677,1.41135899989619,26.0927917337991));
#18274=CARTESIAN_POINT('Ctrl Pts',(-2.87416576400806,1.45879927303017,26.0893807721315));
#18275=CARTESIAN_POINT('Ctrl Pts',(-2.8440596043192,1.5157750299234,26.08531254131));
#18276=CARTESIAN_POINT('Ctrl Pts',(-2.83864982639682,1.52588208806886,26.0845919773385));
#18277=CARTESIAN_POINT('Ctrl Pts',(-2.83010687907828,1.54164015214328,26.0834705299127));
#18278=CARTESIAN_POINT('Ctrl Pts',(-2.82701051411813,1.54731084805639,26.0830673722838));
#18279=CARTESIAN_POINT('Ctrl Pts',(-2.82120413899288,1.55786905716693,26.082317551557));
#18280=CARTESIAN_POINT('Ctrl Pts',(-2.81849849832215,1.56275878137027,26.0819706278102));
#18281=CARTESIAN_POINT('Ctrl Pts',(-2.81230621662895,1.57388128789339,26.0811822257736));
#18282=CARTESIAN_POINT('Ctrl Pts',(-2.80881157552127,1.58010952152227,26.0807412682462));
#18283=CARTESIAN_POINT('Ctrl Pts',(-2.7996646739533,1.59628511584858,26.0795972624647));
#18284=CARTESIAN_POINT('Ctrl Pts',(-2.79398003779248,1.60621418719133,26.0788962450794));
#18285=CARTESIAN_POINT('Ctrl Pts',(-2.75699408722439,1.67002519823566,26.0743974479795));
#18286=CARTESIAN_POINT('Ctrl Pts',(-2.72418615432642,1.72302395019538,26.0706905155826));
#18287=CARTESIAN_POINT('Ctrl Pts',(-2.67099725941925,1.80362523847452,26.065046009274));
#18288=CARTESIAN_POINT('Ctrl Pts',(-2.65168003124508,1.83190706926713,26.0630640634911));
#18289=CARTESIAN_POINT('Ctrl Pts',(-2.49330237884658,2.05602762619528,26.0473021819558));
#18290=CARTESIAN_POINT('Ctrl Pts',(-2.33319286146725,2.23607459412244,26.0342366444799));
#18291=CARTESIAN_POINT('Ctrl Pts',(-2.08603228759355,2.45826706444388,26.0153175519517));
#18292=CARTESIAN_POINT('Ctrl Pts',(-2.01490339364569,2.51689690658847,26.0099996941659));
#18293=CARTESIAN_POINT('Ctrl Pts',(-1.89651154265684,2.60624617539733,26.0012539871689));
#18294=CARTESIAN_POINT('Ctrl Pts',(-1.85078334287712,2.63891561001192,25.9979000319302));
#18295=CARTESIAN_POINT('Ctrl Pts',(-1.78998559265168,2.67999338123181,25.9934600038957));
#18296=CARTESIAN_POINT('Ctrl Pts',(-1.77566816281349,2.68950097659732,25.9924157831253));
#18297=CARTESIAN_POINT('Ctrl Pts',(-1.75218593978261,2.70482528143308,25.9907050519338));
#18298=CARTESIAN_POINT('Ctrl Pts',(-1.7430664779944,2.71071109109505,25.9900411443617));
#18299=CARTESIAN_POINT('Ctrl Pts',(-1.72541925539808,2.72197494465727,25.9887572159145));
#18300=CARTESIAN_POINT('Ctrl Pts',(-1.71689563762671,2.72735926713962,25.9881374390785));
#18301=CARTESIAN_POINT('Ctrl Pts',(-1.69724507644035,2.7396437968091,25.9867093456047));
#18302=CARTESIAN_POINT('Ctrl Pts',(-1.68610112445136,2.74651633399251,25.9859000175483));
#18303=CARTESIAN_POINT('Ctrl Pts',(-1.65620977337386,2.76470001101707,25.9837304702251));
#18304=CARTESIAN_POINT('Ctrl Pts',(-1.63738871685967,2.77588816705966,25.9823657771605));
#18305=CARTESIAN_POINT('Ctrl Pts',(-1.47732507113802,2.86884357390341,25.9707692663852));
#18306=CARTESIAN_POINT('Ctrl Pts',(-1.33019516362041,2.93995223189422,25.960153437564));
#18307=CARTESIAN_POINT('Ctrl Pts',(-0.942959360718093,3.09206976477965,
25.9324097068884));
#18308=CARTESIAN_POINT('Ctrl Pts',(-0.697533641748336,3.15650272467688,
25.9149571458457));
#18309=CARTESIAN_POINT('Ctrl Pts',(-0.38972318356811,3.19962353091047,25.8946053717871));
#18310=CARTESIAN_POINT('Ctrl Pts',(-0.332130243342614,3.20611375231449,
25.8908661657931));
#18311=CARTESIAN_POINT('Ctrl Pts',(-0.262662480216537,3.21204989268341,
25.8864627831021));
#18312=CARTESIAN_POINT('Ctrl Pts',(-0.250929763105865,3.212987761519,25.8857227337543));
#18313=CARTESIAN_POINT('Ctrl Pts',(-0.232682182355056,3.21434583958339,
25.8845777138272));
#18314=CARTESIAN_POINT('Ctrl Pts',(-0.226170879295409,3.21481055578477,
25.884170313712));
#18315=CARTESIAN_POINT('Ctrl Pts',(-0.214090159539857,3.21563588007138,
25.883416687781));
#18316=CARTESIAN_POINT('Ctrl Pts',(-0.208521269174806,3.21600180203053,
25.88307017596));
#18317=CARTESIAN_POINT('Ctrl Pts',(-0.195917006706123,3.21679712875393,
25.8822878950178));
#18318=CARTESIAN_POINT('Ctrl Pts',(-0.188881177474731,3.21721791989632,
25.8818526142516));
#18319=CARTESIAN_POINT('Ctrl Pts',(-0.168068098858618,3.21839417361032,
25.8805689663746));
#18320=CARTESIAN_POINT('Ctrl Pts',(-0.154287108349068,3.21908425589985,
25.8797241792717));
#18321=CARTESIAN_POINT('Ctrl Pts',(-0.0523551337836735,3.22353240064719,
25.873510975362));
#18322=CARTESIAN_POINT('Ctrl Pts',(0.0359211975048042,3.22375788540087,
25.8683250717388));
#18323=CARTESIAN_POINT('Ctrl Pts',(0.371646429713838,3.21081998576538,25.8489730159192));
#18324=CARTESIAN_POINT('Ctrl Pts',(0.617272739477642,3.17277090328384,25.8355214044319));
#18325=CARTESIAN_POINT('Ctrl Pts',(0.944158300769834,3.08269696195949,25.8162124459223));
#18326=CARTESIAN_POINT('Ctrl Pts',(1.03111293246459,3.05471106301876,25.8109404613762));
#18327=CARTESIAN_POINT('Ctrl Pts',(1.16912857282546,3.00372650825073,25.8022633386962));
#18328=CARTESIAN_POINT('Ctrl Pts',(1.22098529756291,2.98302344792547,25.7989305863978));
#18329=CARTESIAN_POINT('Ctrl Pts',(1.28802998936638,2.95421568644553,25.7945147312533));
#18330=CARTESIAN_POINT('Ctrl Pts',(1.30372954555167,2.94732095807808,25.7934729039606));
#18331=CARTESIAN_POINT('Ctrl Pts',(1.32926776931012,2.93586143703773,25.7917651091758));
#18332=CARTESIAN_POINT('Ctrl Pts',(1.3391398651957,2.93137162381514,25.7911017273223));
#18333=CARTESIAN_POINT('Ctrl Pts',(1.35814802523645,2.92261068428971,25.7898181227612));
#18334=CARTESIAN_POINT('Ctrl Pts',(1.36728708424706,2.91834632899168,25.7891981403655));
#18335=CARTESIAN_POINT('Ctrl Pts',(1.38826279639535,2.90843874298913,25.7877685787723));
#18336=CARTESIAN_POINT('Ctrl Pts',(1.40008526271293,2.90276605370462,25.7869579813511));
#18337=CARTESIAN_POINT('Ctrl Pts',(1.43161731489114,2.88739880746558,25.784782815391));
#18338=CARTESIAN_POINT('Ctrl Pts',(1.4512626906602,2.8775747729237,25.7834137365536));
#18339=CARTESIAN_POINT('Ctrl Pts',(1.61819188513292,2.79195452590625,25.7716593513023));
#18340=CARTESIAN_POINT('Ctrl Pts',(1.75950712511285,2.70512006808577,25.7608779760199));
#18341=CARTESIAN_POINT('Ctrl Pts',(2.10278566920486,2.45587006619376,25.7325699925155));
#18342=CARTESIAN_POINT('Ctrl Pts',(2.29300298319346,2.27928474748005,25.7147045927497));
#18343=CARTESIAN_POINT('Ctrl Pts',(2.49268967147371,2.04332222545695,25.6945500088097));
#18344=CARTESIAN_POINT('Ctrl Pts',(2.52440207495043,2.00401156563133,25.6913018536659));
#18345=CARTESIAN_POINT('Ctrl Pts',(2.56206467587449,1.95501145997342,25.6874010961321));
#18346=CARTESIAN_POINT('Ctrl Pts',(2.56890286016903,1.94601729590215,25.6866910429428));
#18347=CARTESIAN_POINT('Ctrl Pts',(2.57955514038087,1.93185250882174,25.6855823265757));
#18348=CARTESIAN_POINT('Ctrl Pts',(2.58340123618463,1.92670622895617,25.6851814712272));
#18349=CARTESIAN_POINT('Ctrl Pts',(2.59056706332564,1.91705793870523,25.6844336530476));
#18350=CARTESIAN_POINT('Ctrl Pts',(2.5938904261035,1.91255883776215,25.6840864434813));
#18351=CARTESIAN_POINT('Ctrl Pts',(2.60146245635767,1.90225193655187,25.6832944359735));
#18352=CARTESIAN_POINT('Ctrl Pts',(2.60570338954346,1.8964385542495,25.6828501775964));
#18353=CARTESIAN_POINT('Ctrl Pts',(2.61872516459041,1.87846243151777,25.6814838357579));
#18354=CARTESIAN_POINT('Ctrl Pts',(2.62744073267527,1.86625234380372,25.6805661522207));
#18355=CARTESIAN_POINT('Ctrl Pts',(2.71641383109504,1.73974655704221,25.6711598212987));
#18356=CARTESIAN_POINT('Ctrl Pts',(2.78925709261912,1.62039414413956,25.6631322666994));
#18357=CARTESIAN_POINT('Ctrl Pts',(2.97876577006997,1.25900496468641,25.640089116359));
#18358=CARTESIAN_POINT('Ctrl Pts',(3.07321818239486,1.00671122790793,25.6254510885371));
#18359=CARTESIAN_POINT('Ctrl Pts',(3.15166239159618,0.676859120536802,25.6056083701586));
#18360=CARTESIAN_POINT('Ctrl Pts',(3.16574868803345,0.607575694019345,25.6014102747691));
#18361=CARTESIAN_POINT('Ctrl Pts',(3.18064994066027,0.519547459453553,25.5960148388657));
#18362=CARTESIAN_POINT('Ctrl Pts',(3.18359581662186,0.501179869437657,25.594885736852));
#18363=CARTESIAN_POINT('Ctrl Pts',(3.18805537691094,0.471746946906356,25.5930707229158));
#18364=CARTESIAN_POINT('Ctrl Pts',(3.18967087233505,0.460697286062864,25.5923880524716));
#18365=CARTESIAN_POINT('Ctrl Pts',(3.19262393919032,0.439738471302244,25.591090657871));
#18366=CARTESIAN_POINT('Ctrl Pts',(3.1939728895837,0.429831033367234,25.5904763030397));
#18367=CARTESIAN_POINT('Ctrl Pts',(3.19692897016848,0.407337350763026,25.5890789997735));
#18368=CARTESIAN_POINT('Ctrl Pts',(3.19850791154475,0.394747628261893,25.5882951677072));
#18369=CARTESIAN_POINT('Ctrl Pts',(3.20239255516062,0.36221867696752,25.5862652378278));
#18370=CARTESIAN_POINT('Ctrl Pts',(3.20458637018652,0.342266875186208,25.5850156266128));
#18371=CARTESIAN_POINT('Ctrl Pts',(3.21743641385172,0.214419066251236,25.5769781240502));
#18372=CARTESIAN_POINT('Ctrl Pts',(3.2228273664416,0.106075080822275,25.5700256830872));
#18373=CARTESIAN_POINT('Ctrl Pts',(3.22253004394657,-0.306044497767057,
25.5430379482098));
#18374=CARTESIAN_POINT('Ctrl Pts',(3.17938233664151,-0.608154744361235,
25.5219614943874));
#18375=CARTESIAN_POINT('Ctrl Pts',(3.07682501481297,-0.9608965408928,25.4978213706456));
#18376=CARTESIAN_POINT('Ctrl Pts',(3.05723242423208,-1.02152117786369,25.4936982065713));
#18377=CARTESIAN_POINT('Ctrl Pts',(3.03198943907334,-1.09237824555657,25.4889413528803));
#18378=CARTESIAN_POINT('Ctrl Pts',(3.02806643335732,-1.10320617952953,25.4882161867629));
#18379=CARTESIAN_POINT('Ctrl Pts',(3.02160887787926,-1.12073577615488,25.4870453056268));
#18380=CARTESIAN_POINT('Ctrl Pts',(3.0191099164248,-1.12745031186814,25.4865975541884));
#18381=CARTESIAN_POINT('Ctrl Pts',(3.01462115357479,-1.13938936104428,25.4858028075223));
#18382=CARTESIAN_POINT('Ctrl Pts',(3.01264013315002,-1.14461707371888,25.4854552959889));
#18383=CARTESIAN_POINT('Ctrl Pts',(3.00834582421124,-1.15586093790372,25.4847089125904));
#18384=CARTESIAN_POINT('Ctrl Pts',(3.00602809456509,-1.16187529547134,25.4843103119873));
#18385=CARTESIAN_POINT('Ctrl Pts',(2.99956368114646,-1.17850120194175,25.4832101015586));
#18386=CARTESIAN_POINT('Ctrl Pts',(2.9953786994894,-1.18909790006061,25.4825107569396));
#18387=CARTESIAN_POINT('Ctrl Pts',(2.97181891517139,-1.24783940086567,25.4786433417351));
#18388=CARTESIAN_POINT('Ctrl Pts',(2.95133834891464,-1.29553598827984,25.4755379483662));
#18389=CARTESIAN_POINT('Ctrl Pts',(2.82245084429516,-1.57675873404769,25.4573187184982));
#18390=CARTESIAN_POINT('Ctrl Pts',(2.68752086255833,-1.79712500200104,25.4433557999287));
#18391=CARTESIAN_POINT('Ctrl Pts',(2.42527693164959,-2.1287225013982,25.4194844173228));
#18392=CARTESIAN_POINT('Ctrl Pts',(2.31296150564206,-2.25025023270954,25.4099656748329));
#18393=CARTESIAN_POINT('Ctrl Pts',(2.17575163625645,-2.37754150098549,25.3987087397883));
#18394=CARTESIAN_POINT('Ctrl Pts',(2.15951824532447,-2.39229590210928,25.3973826054119));
#18395=CARTESIAN_POINT('Ctrl Pts',(2.1333485937216,-2.41559787128308,25.3952530454883));
#18396=CARTESIAN_POINT('Ctrl Pts',(2.1235084433974,-2.42425270566822,25.3944541372393));
#18397=CARTESIAN_POINT('Ctrl Pts',(2.10600369936517,-2.43946052695069,25.3930360372909));
#18398=CARTESIAN_POINT('Ctrl Pts',(2.09836057881077,-2.44603804588409,25.3924178777503));
#18399=CARTESIAN_POINT('Ctrl Pts',(2.08243068585523,-2.45961738807783,25.3911315560763));
#18400=CARTESIAN_POINT('Ctrl Pts',(2.07413918615,-2.46661344539334,25.3904631674521));
#18401=CARTESIAN_POINT('Ctrl Pts',(2.05263946229159,-2.48456905064676,25.3887328835356));
#18402=CARTESIAN_POINT('Ctrl Pts',(2.03937886019739,-2.4954650820639,25.3876684158016));
#18403=CARTESIAN_POINT('Ctrl Pts',(1.98250036970407,-2.54144510725271,25.3831136621017));
#18404=CARTESIAN_POINT('Ctrl Pts',(1.93806160108567,-2.57549365081135,25.3795822343522));
#18405=CARTESIAN_POINT('Ctrl Pts',(1.81858447788489,-2.66219222654825,25.370151814655));
#18406=CARTESIAN_POINT('Ctrl Pts',(1.74215191392776,-2.71282531005347,25.3641816828319));
#18407=CARTESIAN_POINT('Ctrl Pts',(1.45363185537698,-2.88673111548388,25.3418989449745));
#18408=CARTESIAN_POINT('Ctrl Pts',(1.22985105380373,-2.9889317710809,25.3250240770169));
#18409=CARTESIAN_POINT('Ctrl Pts',(0.910962818808793,-3.09263396318484,
25.3027303509747));
#18410=CARTESIAN_POINT('Ctrl Pts',(0.824126256946801,-3.11689865661018,
25.2968357138401));
#18411=CARTESIAN_POINT('Ctrl Pts',(0.722880128331746,-3.14066141647,25.2902488795338));
#18412=CARTESIAN_POINT('Ctrl Pts',(0.709360904013251,-3.14374250487621,
25.2893751749596));
#18413=CARTESIAN_POINT('Ctrl Pts',(0.68892575259181,-3.14826122686638,25.2880637304746));
#18414=CARTESIAN_POINT('Ctrl Pts',(0.682024499934543,-3.14976348777506,
25.2876224179387));
#18415=CARTESIAN_POINT('Ctrl Pts',(0.669660180402132,-3.15241240378854,
25.2868346589009));
#18416=CARTESIAN_POINT('Ctrl Pts',(0.66419904253405,-3.15356755980093,25.2864877320594));
#18417=CARTESIAN_POINT('Ctrl Pts',(0.652355374406069,-3.15604063653776,
25.2857375525362));
#18418=CARTESIAN_POINT('Ctrl Pts',(0.645971858863781,-3.15735338429617,
25.2853345981811));
#18419=CARTESIAN_POINT('Ctrl Pts',(0.628097095651578,-3.16097278824571,
25.2842100112925));
#18420=CARTESIAN_POINT('Ctrl Pts',(0.616597043908371,-3.16323616330999,
25.2834908116318));
#18421=CARTESIAN_POINT('Ctrl Pts',(0.548997496520677,-3.1761580613752,25.2792872152649));
#18422=CARTESIAN_POINT('Ctrl Pts',(0.492631200712093,-3.18538752932543,
25.2758790184597));
#18423=CARTESIAN_POINT('Ctrl Pts',(0.184918369037335,-3.22740819305677,
25.257652545334));
#18424=CARTESIAN_POINT('Ctrl Pts',(-0.0694002118302224,-3.23196052668063,
25.243896944248));
#18425=CARTESIAN_POINT('Ctrl Pts',(-0.484336893456944,-3.19034014590634,
25.2203396369695));
#18426=CARTESIAN_POINT('Ctrl Pts',(-0.645529871143418,-3.16166621710592,
25.2109164908922));
#18427=CARTESIAN_POINT('Ctrl Pts',(-0.825048781025056,-3.11542802100435,
25.1997665247601));
#18428=CARTESIAN_POINT('Ctrl Pts',(-0.846201556099869,-3.10974920778379,
25.1984424665445));
#18429=CARTESIAN_POINT('Ctrl Pts',(-0.879905957921855,-3.10033135925477,
25.196315611554));
#18430=CARTESIAN_POINT('Ctrl Pts',(-0.892495757754961,-3.09673058989817,
25.1955173137582));
#18431=CARTESIAN_POINT('Ctrl Pts',(-0.914739517777484,-3.09022180866905,
25.1940999203274));
#18432=CARTESIAN_POINT('Ctrl Pts',(-0.924402487324136,-3.08734501633968,
25.1934818534303));
#18433=CARTESIAN_POINT('Ctrl Pts',(-0.944439002983095,-3.08127738487787,
25.1921953484504));
#18434=CARTESIAN_POINT('Ctrl Pts',(-0.954810234245806,-3.07807939548043,
25.1915266820076));
#18435=CARTESIAN_POINT('Ctrl Pts',(-0.981559330887052,-3.06968306147691,
25.1897948703804));
#18436=CARTESIAN_POINT('Ctrl Pts',(-0.997911967463315,-3.06440606067968,
25.1887291441229));
#18437=CARTESIAN_POINT('Ctrl Pts',(-1.06752679241671,-3.04132502929298,
25.1841617047714));
#18438=CARTESIAN_POINT('Ctrl Pts',(-1.12035822226353,-3.02226209980034,
25.1806185642969));
#18439=CARTESIAN_POINT('Ctrl Pts',(-1.25841668476385,-2.96832968213159,
25.1711489156346));
#18440=CARTESIAN_POINT('Ctrl Pts',(-1.34268926780302,-2.93117325529551,
25.1651505293845));
#18441=CARTESIAN_POINT('Ctrl Pts',(-1.44199506580101,-2.88220685618616,
25.1578253909253));
#18442=CARTESIAN_POINT('Ctrl Pts',(-1.45866412097157,-2.87380667246934,
25.1565869376027));
#18443=CARTESIAN_POINT('Ctrl Pts',(-1.4752554489605,-2.86526419773332,25.1553455282223));
#18444=CARTESIAN_POINT('Ctrl Pts',(-1.47525540501177,-2.86526422036146,
24.9102129806979));
#18445=CARTESIAN_POINT('Ctrl Pts',(-1.47010109142369,-2.86791805204857,
24.9105680165818));
#18446=CARTESIAN_POINT('Ctrl Pts',(-1.46493957140812,-2.87055799903562,
24.9109222262282));
#18447=CARTESIAN_POINT('Ctrl Pts',(-1.39676361540044,-2.90519597405743,
24.9155837535852));
#18448=CARTESIAN_POINT('Ctrl Pts',(-1.33271501509627,-2.9351294004825,24.9197713314932));
#18449=CARTESIAN_POINT('Ctrl Pts',(-1.25829580640014,-2.96697059226284,
24.924478492948));
#18450=CARTESIAN_POINT('Ctrl Pts',(-1.24884357958254,-2.9709615529812,24.9250734888276));
#18451=CARTESIAN_POINT('Ctrl Pts',(-1.03636170021782,-3.05948335896664,
24.9383877171935));
#18452=CARTESIAN_POINT('Ctrl Pts',(-0.825215433198304,-3.12306210268755,
24.9504081753233));
#18453=CARTESIAN_POINT('Ctrl Pts',(-0.456167805628342,-3.19410767991887,
24.971602815464));
#18454=CARTESIAN_POINT('Ctrl Pts',(-0.301190365982923,-3.21242723253861,
24.9805496897514));
#18455=CARTESIAN_POINT('Ctrl Pts',(-0.111382936911088,-3.22100578062201,
24.9918991759716));
#18456=CARTESIAN_POINT('Ctrl Pts',(-0.0772374843166383,-3.22200537445344,
24.993955607795));
#18457=CARTESIAN_POINT('Ctrl Pts',(-0.0288775855290607,-3.22265193484467,
24.9968914380177));
#18458=CARTESIAN_POINT('Ctrl Pts',(-0.014670698650808,-3.22274792197344,
24.9977567530613));
#18459=CARTESIAN_POINT('Ctrl Pts',(0.00976608084689957,-3.22275143890781,
24.9992502250413));
#18460=CARTESIAN_POINT('Ctrl Pts',(0.0199958329956215,-3.22270420239774,
24.9998769529635));
#18461=CARTESIAN_POINT('Ctrl Pts',(0.0395335503398872,-3.22252095662318,
25.0010769230916));
#18462=CARTESIAN_POINT('Ctrl Pts',(0.0488415053722538,-3.22239332203931,
25.0016498956716));
#18463=CARTESIAN_POINT('Ctrl Pts',(0.0729413329623558,-3.22195841340573,
25.0031368326643));
#18464=CARTESIAN_POINT('Ctrl Pts',(0.0877317500108615,-3.22158960515778,
25.0040527219152));
#18465=CARTESIAN_POINT('Ctrl Pts',(0.137656959396089,-3.22000063003307,
25.0071558590937));
#18466=CARTESIAN_POINT('Ctrl Pts',(0.172773178415079,-3.21830743818157,
25.0093578761422));
#18467=CARTESIAN_POINT('Ctrl Pts',(0.475526297662532,-3.19874041866013,
25.0285162816521));
#18468=CARTESIAN_POINT('Ctrl Pts',(0.739943130008288,-3.14809363678248,
25.046554721667));
#18469=CARTESIAN_POINT('Ctrl Pts',(1.1670624026617,-3.00945485327862,25.0769473875398));
#18470=CARTESIAN_POINT('Ctrl Pts',(1.3341645479222,-2.93919601225401,25.0891515879971));
#18471=CARTESIAN_POINT('Ctrl Pts',(1.50922628807391,-2.84756559677658,25.1017027157977));
#18472=CARTESIAN_POINT('Ctrl Pts',(1.52389249379347,-2.8397439165504,25.1027521812782));
#18473=CARTESIAN_POINT('Ctrl Pts',(1.54508914626236,-2.82822795414327,25.104265258898));
#18474=CARTESIAN_POINT('Ctrl Pts',(1.55166795683564,-2.82462393690155,25.10473435378));
#18475=CARTESIAN_POINT('Ctrl Pts',(1.56316115830566,-2.81827543670574,25.1055528722427));
#18476=CARTESIAN_POINT('Ctrl Pts',(1.56808102009867,-2.81554100668402,25.1059029312325));
#18477=CARTESIAN_POINT('Ctrl Pts',(1.578445402496,-2.80974495076227,25.1066396744275));
#18478=CARTESIAN_POINT('Ctrl Pts',(1.5838881859675,-2.80668038667009,25.1070261655977));
#18479=CARTESIAN_POINT('Ctrl Pts',(1.59845537602588,-2.79842244798054,25.1080595875942));
#18480=CARTESIAN_POINT('Ctrl Pts',(1.60756346484215,-2.79320022557334,25.1087046844843));
#18481=CARTESIAN_POINT('Ctrl Pts',(1.6475532515346,-2.77001124730437,25.1115331455017));
#18482=CARTESIAN_POINT('Ctrl Pts',(1.67816181636323,-2.75157540169006,25.1136878253895));
#18483=CARTESIAN_POINT('Ctrl Pts',(1.71713325622863,-2.72721022269436,25.1164263224175));
#18484=CARTESIAN_POINT('Ctrl Pts',(1.72578183238854,-2.72174563293803,25.1170337372833));
#18485=CARTESIAN_POINT('Ctrl Pts',(1.98767207771296,-2.55452049905674,25.135422108806));
#18486=CARTESIAN_POINT('Ctrl Pts',(2.21710462046362,-2.35815812711824,25.1515142473993));
#18487=CARTESIAN_POINT('Ctrl Pts',(2.47460826050053,-2.06646250324366,25.1737018618524));
#18488=CARTESIAN_POINT('Ctrl Pts',(2.53042811490196,-1.99771997989967,25.1788192749131));
#18489=CARTESIAN_POINT('Ctrl Pts',(2.61598551955279,-1.88300768116648,25.1872645971845));
#18490=CARTESIAN_POINT('Ctrl Pts',(2.64750702368279,-1.83842437772233,25.1905250682591));
#18491=CARTESIAN_POINT('Ctrl Pts',(2.68734100232911,-1.77893369165561,25.1948582181709));
#18492=CARTESIAN_POINT('Ctrl Pts',(2.69669021677924,-1.76472904424039,25.1958915536155));
#18493=CARTESIAN_POINT('Ctrl Pts',(2.71179878197142,-1.74137354358707,25.1975887816865));
#18494=CARTESIAN_POINT('Ctrl Pts',(2.71762535161924,-1.732266404436,25.1982501486094));
#18495=CARTESIAN_POINT('Ctrl Pts',(2.72880226009761,-1.71460130941519,25.1995322305522));
#18496=CARTESIAN_POINT('Ctrl Pts',(2.7341584464433,-1.70604718897399,25.2001527181771));
#18497=CARTESIAN_POINT('Ctrl Pts',(2.74641569090647,-1.6862657239521,25.2015868778526));
#18498=CARTESIAN_POINT('Ctrl Pts',(2.75328820314347,-1.67502098529253,25.2024015910473));
#18499=CARTESIAN_POINT('Ctrl Pts',(2.77155127020434,-1.64472304151933,25.2045955053693));
#18500=CARTESIAN_POINT('Ctrl Pts',(2.7828140970968,-1.62559404152753,25.2059793415106));
#18501=CARTESIAN_POINT('Ctrl Pts',(2.88465072034203,-1.44847260779442,25.218782792207));
#18502=CARTESIAN_POINT('Ctrl Pts',(2.96186256586661,-1.28321197411695,25.2306855246905));
#18503=CARTESIAN_POINT('Ctrl Pts',(3.07170926747236,-0.984514746010875,
25.2520078567417));
#18504=CARTESIAN_POINT('Ctrl Pts',(3.11056663850006,-0.853838636210736,
25.2612689727067));
#18505=CARTESIAN_POINT('Ctrl Pts',(3.17476986617113,-0.574176488503076,
25.280631938811));
#18506=CARTESIAN_POINT('Ctrl Pts',(3.19815401276076,-0.425046380349274,
25.2906947173426));
#18507=CARTESIAN_POINT('Ctrl Pts',(3.21223363682343,-0.260533980371119,
25.3011560356797));
#18508=CARTESIAN_POINT('Ctrl Pts',(3.21336032413091,-0.246248528329243,
25.3020591401973));
#18509=CARTESIAN_POINT('Ctrl Pts',(3.21489996658276,-0.224912500200095,
25.3033995797485));
#18510=CARTESIAN_POINT('Ctrl Pts',(3.21538507255571,-0.21786754077303,25.3038408160532));
#18511=CARTESIAN_POINT('Ctrl Pts',(3.21621205365255,-0.205252833759815,
25.3046283827993));
#18512=CARTESIAN_POINT('Ctrl Pts',(3.21656262130947,-0.199683761425398,
25.304975193697));
#18513=CARTESIAN_POINT('Ctrl Pts',(3.21729106429761,-0.187611827915032,
25.3057250514247));
#18514=CARTESIAN_POINT('Ctrl Pts',(3.21766368898523,-0.181108742865714,
25.3061278005241));
#18515=CARTESIAN_POINT('Ctrl Pts',(3.21863421146345,-0.163221704695553,
25.3072324037904));
#18516=CARTESIAN_POINT('Ctrl Pts',(3.21919143563325,-0.151835509312136,
25.3079320140038));
#18517=CARTESIAN_POINT('Ctrl Pts',(3.2217089439719,-0.094122445573838,25.3114612795503));
#18518=CARTESIAN_POINT('Ctrl Pts',(3.22272978911153,-0.0477574733226213,
25.31424163644));
#18519=CARTESIAN_POINT('Ctrl Pts',(3.22285979380732,0.25498716482006,25.3321310784655));
#18520=CARTESIAN_POINT('Ctrl Pts',(3.19237868881762,0.510483406774052,25.346048409827));
#18521=CARTESIAN_POINT('Ctrl Pts',(3.09152430083769,0.926270538982161,25.3701712204234));
#18522=CARTESIAN_POINT('Ctrl Pts',(3.03789809185504,1.08934073481875,25.3800253101296));
#18523=CARTESIAN_POINT('Ctrl Pts',(2.96303239009753,1.2676919057717,25.3916579564016));
#18524=CARTESIAN_POINT('Ctrl Pts',(2.95429017678988,1.28793370444762,25.3929907891746));
#18525=CARTESIAN_POINT('Ctrl Pts',(2.94000966252351,1.32008836065332,25.3951289324715));
#18526=CARTESIAN_POINT('Ctrl Pts',(2.93460493502323,1.33206004481214,25.3959296654773));
#18527=CARTESIAN_POINT('Ctrl Pts',(2.92492113602611,1.3531650425915,25.3973497063676));
#18528=CARTESIAN_POINT('Ctrl Pts',(2.92067206725409,1.36231198935958,25.3979679710289));
#18529=CARTESIAN_POINT('Ctrl Pts',(2.91177153598466,1.38123907067606,25.3992532210831));
#18530=CARTESIAN_POINT('Ctrl Pts',(2.90711357713681,1.39101599314151,25.3999204264105));
#18531=CARTESIAN_POINT('Ctrl Pts',(2.89497895385345,1.41615904328004,25.4016448835219));
#18532=CARTESIAN_POINT('Ctrl Pts',(2.8874292648706,1.43148936473785,25.4027046765637));
#18533=CARTESIAN_POINT('Ctrl Pts',(2.85491583646753,1.49620700609004,25.4072146919106));
#18534=CARTESIAN_POINT('Ctrl Pts',(2.82880539939994,1.54500460773669,25.4107050646256));
#18535=CARTESIAN_POINT('Ctrl Pts',(2.75686399170324,1.67151268749512,25.419999024889));
#18536=CARTESIAN_POINT('Ctrl Pts',(2.70900648816065,1.74800892101746,25.4258712313088));
#18537=CARTESIAN_POINT('Ctrl Pts',(2.51508350619347,2.0308507388661,25.4485387622528));
#18538=CARTESIAN_POINT('Ctrl Pts',(2.34815043254383,2.22174985186993,25.465950338774));
#18539=CARTESIAN_POINT('Ctrl Pts',(2.09744719467626,2.44828252933649,25.4883716774367));
#18540=CARTESIAN_POINT('Ctrl Pts',(2.03200587536802,2.50286375834532,25.4939327530386));
#18541=CARTESIAN_POINT('Ctrl Pts',(1.95362912244848,2.56313049264066,25.5001933390471));
#18542=CARTESIAN_POINT('Ctrl Pts',(1.94273227991247,2.57139961394655,25.5010551361368));
#18543=CARTESIAN_POINT('Ctrl Pts',(1.9261627860281,2.58380800045034,25.502352160349));
#18544=CARTESIAN_POINT('Ctrl Pts',(1.92052887681625,2.58799839586592,25.5027908479605));
#18545=CARTESIAN_POINT('Ctrl Pts',(1.91039526410906,2.5954842714369,25.5035756820394));
#18546=CARTESIAN_POINT('Ctrl Pts',(1.90590068063647,2.59878649862991,25.503922294686));
#18547=CARTESIAN_POINT('Ctrl Pts',(1.89611379765902,2.60593799850107,25.5046738065878));
#18548=CARTESIAN_POINT('Ctrl Pts',(1.89081835604461,2.60978281317564,25.5050783968277));
#18549=CARTESIAN_POINT('Ctrl Pts',(1.87590046745913,2.62054487389166,25.5062125831724));
#18550=CARTESIAN_POINT('Ctrl Pts',(1.86625140679478,2.6274252980218,25.5069396778203));
#18551=CARTESIAN_POINT('Ctrl Pts',(1.80801314655396,2.66847037035459,25.5112906149421));
#18552=CARTESIAN_POINT('Ctrl Pts',(1.75852151529367,2.70134203194403,25.5148318784238));
#18553=CARTESIAN_POINT('Ctrl Pts',(1.49468842334272,2.86625005101672,25.533063955319));
#18554=CARTESIAN_POINT('Ctrl Pts',(1.26631592072286,2.97421458041884,25.5467295148741));
#18555=CARTESIAN_POINT('Ctrl Pts',(0.873432310175584,3.10639997962796,25.5701504681611));
#18556=CARTESIAN_POINT('Ctrl Pts',(0.71549007624331,3.14653277513683,25.5795321458239));
#18557=CARTESIAN_POINT('Ctrl Pts',(0.533651235126052,3.17833489656605,25.5906354450536));
#18558=CARTESIAN_POINT('Ctrl Pts',(0.512059641735634,3.18188485690694,25.591958292369));
#18559=CARTESIAN_POINT('Ctrl Pts',(0.477500013444488,3.18720607317653,25.5940834282585));
#18560=CARTESIAN_POINT('Ctrl Pts',(0.46455419742577,3.1891187192481,25.5948812276468));
#18561=CARTESIAN_POINT('Ctrl Pts',(0.441618644275081,3.19236465683933,25.5962978705928));
#18562=CARTESIAN_POINT('Ctrl Pts',(0.431633571066053,3.19373004273566,25.5969156873693));
#18563=CARTESIAN_POINT('Ctrl Pts',(0.410884725613852,3.19646821454506,25.5982018050918));
#18564=CARTESIAN_POINT('Ctrl Pts',(0.400120109974482,3.19783351619854,25.5988703349082));
#18565=CARTESIAN_POINT('Ctrl Pts',(0.372290697451221,3.2012204690819,25.6006020773233));
#18566=CARTESIAN_POINT('Ctrl Pts',(0.355216427234059,3.20316002198835,25.6016678722519));
#18567=CARTESIAN_POINT('Ctrl Pts',(0.282235045044691,3.2108596520424,25.6062381249456));
#18568=CARTESIAN_POINT('Ctrl Pts',(0.226200743915026,3.21529297381659,25.6097840811051));
#18569=CARTESIAN_POINT('Ctrl Pts',(0.0780347690067315,3.22312340359168,
25.6192637554885));
#18570=CARTESIAN_POINT('Ctrl Pts',(-0.0141710490152691,3.22403637401961,
25.6252695544228));
#18571=CARTESIAN_POINT('Ctrl Pts',(-0.346175018937811,3.21308129275034,
25.6472472935348));
#18572=CARTESIAN_POINT('Ctrl Pts',(-0.584407122278165,3.17839303284131,
25.6637485455824));
#18573=CARTESIAN_POINT('Ctrl Pts',(-0.848747723883929,3.10915606410736,
25.6819433555861));
#18574=CARTESIAN_POINT('Ctrl Pts',(-0.880795843332628,3.10022949799484,
25.6841458484747));
#18575=CARTESIAN_POINT('Ctrl Pts',(-0.973453389274151,3.07286816634295,
25.6904935795256));
#18576=CARTESIAN_POINT('Ctrl Pts',(-1.03366867620657,3.05313946555433,25.6945936825781));
#18577=CARTESIAN_POINT('Ctrl Pts',(-1.10408097369853,3.02774749603523,25.6993270957404));
#18578=CARTESIAN_POINT('Ctrl Pts',(-1.11487353984538,3.02379012097276,25.7000508940034));
#18579=CARTESIAN_POINT('Ctrl Pts',(-1.13235076515305,3.01727534777119,25.7012199258521));
#18580=CARTESIAN_POINT('Ctrl Pts',(-1.13904837306857,3.01475332088161,25.701667186482));
#18581=CARTESIAN_POINT('Ctrl Pts',(-1.15096053372758,3.01022235690101,25.7024612889562));
#18582=CARTESIAN_POINT('Ctrl Pts',(-1.15617830516967,3.00822215212013,25.7028086448979));
#18583=CARTESIAN_POINT('Ctrl Pts',(-1.16740437658695,3.00388517459287,25.7035549417811));
#18584=CARTESIAN_POINT('Ctrl Pts',(-1.1734108584724,3.00154394929566,25.7039536103394));
#18585=CARTESIAN_POINT('Ctrl Pts',(-1.19002360054986,2.99501109395673,25.7050545931568));
#18586=CARTESIAN_POINT('Ctrl Pts',(-1.20061482088088,2.99078111598788,25.7057546359492));
#18587=CARTESIAN_POINT('Ctrl Pts',(-1.25947415259899,2.96691050650974,25.7096357679536));
#18588=CARTESIAN_POINT('Ctrl Pts',(-1.30728588202886,2.94615638373286,25.7127536468805));
#18589=CARTESIAN_POINT('Ctrl Pts',(-1.58793357505434,2.81615428020016,25.7309669342036));
#18590=CARTESIAN_POINT('Ctrl Pts',(-1.80753628552859,2.68050371676083,25.7449160392112));
#18591=CARTESIAN_POINT('Ctrl Pts',(-2.1379570022102,2.41714328814122,25.7687743877321));
#18592=CARTESIAN_POINT('Ctrl Pts',(-2.25908622280888,2.30433517592237,25.7782955072118));
#18593=CARTESIAN_POINT('Ctrl Pts',(-2.38587579809243,2.16660916269908,25.789554807394));
#18594=CARTESIAN_POINT('Ctrl Pts',(-2.40056498196974,2.15032237553653,25.7908806926979));
#18595=CARTESIAN_POINT('Ctrl Pts',(-2.42376126730017,2.12406933128858,25.7930097866939));
#18596=CARTESIAN_POINT('Ctrl Pts',(-2.43237597160157,2.11419874415947,25.793808479411));
#18597=CARTESIAN_POINT('Ctrl Pts',(-2.44751206631606,2.09664109027487,25.7952261561976));
#18598=CARTESIAN_POINT('Ctrl Pts',(-2.45405806216484,2.08897539479246,25.7958441084824));
#18599=CARTESIAN_POINT('Ctrl Pts',(-2.46757135054734,2.07299946793814,25.7971299576332));
#18600=CARTESIAN_POINT('Ctrl Pts',(-2.47453286803614,2.06468453874194,25.7977980806337));
#18601=CARTESIAN_POINT('Ctrl Pts',(-2.49239810925198,2.04312591689781,25.7995275860462));
#18602=CARTESIAN_POINT('Ctrl Pts',(-2.50323818480358,2.02983014538208,25.8005915381517));
#18603=CARTESIAN_POINT('Ctrl Pts',(-2.5489700786539,1.972814722008,25.8051432101366));
#18604=CARTESIAN_POINT('Ctrl Pts',(-2.58282488921608,1.92827937503314,25.8086720100585));
#18605=CARTESIAN_POINT('Ctrl Pts',(-2.66899821100947,1.80857680826852,25.8180942181685));
#18606=CARTESIAN_POINT('Ctrl Pts',(-2.71929870977416,1.73202585282671,25.8240586253813));
#18607=CARTESIAN_POINT('Ctrl Pts',(-2.89251861697601,1.44222279007025,25.8463898010553));
#18608=CARTESIAN_POINT('Ctrl Pts',(-2.99414926742237,1.21726135352744,25.8633242131051));
#18609=CARTESIAN_POINT('Ctrl Pts',(-3.09648059811592,0.897736045159045,
25.88562480691));
#18610=CARTESIAN_POINT('Ctrl Pts',(-3.12021129328243,0.811422677912189,
25.8914757642803));
#18611=CARTESIAN_POINT('Ctrl Pts',(-3.14343081987345,0.710740297192464,
25.8980198175318));
#18612=CARTESIAN_POINT('Ctrl Pts',(-3.14645400196757,0.697234766103892,
25.8988918562314));
#18613=CARTESIAN_POINT('Ctrl Pts',(-3.15088703937895,0.676814754007573,
25.9002012071683));
#18614=CARTESIAN_POINT('Ctrl Pts',(-3.15236129430654,0.669914635291291,
25.900642076693));
#18615=CARTESIAN_POINT('Ctrl Pts',(-3.1549607840734,0.657549348745187,25.9014292489397));
#18616=CARTESIAN_POINT('Ctrl Pts',(-3.15609449370041,0.652086070591065,
25.9017760300653));
#18617=CARTESIAN_POINT('Ctrl Pts',(-3.15852181317187,0.640234333613007,
25.9025261201796));
#18618=CARTESIAN_POINT('Ctrl Pts',(-3.15981022901334,0.633844905808195,
25.9029291298352));
#18619=CARTESIAN_POINT('Ctrl Pts',(-3.16336323487426,0.615944984740043,
25.9040544250691));
#18620=CARTESIAN_POINT('Ctrl Pts',(-3.16558440157427,0.604425831967209,
25.9047742717628));
#18621=CARTESIAN_POINT('Ctrl Pts',(-3.17828981901766,0.536542783782793,
25.908992360624));
#18622=CARTESIAN_POINT('Ctrl Pts',(-3.18733217787319,0.479915472416386,
25.9124137784638));
#18623=CARTESIAN_POINT('Ctrl Pts',(-3.22809801298606,0.172070089679958,
25.9306354520374));
#18624=CARTESIAN_POINT('Ctrl Pts',(-3.23164476085394,-0.0819980360926485,
25.944377519278));
#18625=CARTESIAN_POINT('Ctrl Pts',(-3.18846563613236,-0.496535652854962,
25.9679212632499));
#18626=CARTESIAN_POINT('Ctrl Pts',(-3.15917021131018,-0.657642721423987,
25.9773458373937));
#18627=CARTESIAN_POINT('Ctrl Pts',(-3.11223764979869,-0.837002902610053,
25.9884971058933));
#18628=CARTESIAN_POINT('Ctrl Pts',(-3.10647887204644,-0.858129377821875,
25.9898208961599));
#18629=CARTESIAN_POINT('Ctrl Pts',(-3.09693401816565,-0.891789562433464,
25.99194726066));
#18630=CARTESIAN_POINT('Ctrl Pts',(-3.09328601480736,-0.904361962489312,
25.9927453374005));
#18631=CARTESIAN_POINT('Ctrl Pts',(-3.0866940265825,-0.926573866471151,
25.99416230124));
#18632=CARTESIAN_POINT('Ctrl Pts',(-3.08378121439741,-0.936222495901261,
25.9947801600045));
#18633=CARTESIAN_POINT('Ctrl Pts',(-3.07763913691372,-0.956228321906986,
25.9960661939311));
#18634=CARTESIAN_POINT('Ctrl Pts',(-3.07440274083129,-0.966583179680249,
25.9967345971128));
#18635=CARTESIAN_POINT('Ctrl Pts',(-3.06590786355911,-0.993288232785968,
25.9984656432495));
#18636=CARTESIAN_POINT('Ctrl Pts',(-3.06057090491577,-1.00961292523463,
25.9995308645988));
#18637=CARTESIAN_POINT('Ctrl Pts',(-3.0372392983666,-1.0790942603101,26.0040953258754));
#18638=CARTESIAN_POINT('Ctrl Pts',(-3.01798922051134,-1.13181597626786,
26.0076359335564));
#18639=CARTESIAN_POINT('Ctrl Pts',(-2.96357926822258,-1.26955766709326,
26.017097678874));
#18640=CARTESIAN_POINT('Ctrl Pts',(-2.92614057401631,-1.35361647611715,
26.0230905587328));
#18641=CARTESIAN_POINT('Ctrl Pts',(-2.77725904504195,-1.65275378951183,
26.0451955829062));
#18642=CARTESIAN_POINT('Ctrl Pts',(-2.64527698026023,-1.85667921391031,
26.0618502977985));
#18643=CARTESIAN_POINT('Ctrl Pts',(-2.43301822012873,-2.11544433817904,
26.0841211590778));
#18644=CARTESIAN_POINT('Ctrl Pts',(-2.37126342539103,-2.18444401198808,
26.090180373709));
#18645=CARTESIAN_POINT('Ctrl Pts',(-2.29687918883406,-2.26067645077101,
26.0969269963779));
#18646=CARTESIAN_POINT('Ctrl Pts',(-2.28707548880475,-2.27059413991579,
26.0978057703499));
#18647=CARTESIAN_POINT('Ctrl Pts',(-2.27219884906777,-2.28544963957684,
26.0991232205506));
#18648=CARTESIAN_POINT('Ctrl Pts',(-2.26717366077266,-2.29043473142491,
26.0995655183789));
#18649=CARTESIAN_POINT('Ctrl Pts',(-2.25815671478434,-2.29932097921762,
26.1003542291657));
#18650=CARTESIAN_POINT('Ctrl Pts',(-2.25417122301862,-2.3032283457979,26.1007011285181));
#18651=CARTESIAN_POINT('Ctrl Pts',(-2.24552123316595,-2.31166481612752,
26.1014503241284));
#18652=CARTESIAN_POINT('Ctrl Pts',(-2.24085318901503,-2.31619015146988,
26.1018523272533));
#18653=CARTESIAN_POINT('Ctrl Pts',(-2.22777861075561,-2.32878849725721,
26.1029719718064));
#18654=CARTESIAN_POINT('Ctrl Pts',(-2.21934182922676,-2.33683017316534,
26.1036872137409));
#18655=CARTESIAN_POINT('Ctrl Pts',(-2.17007105831757,-2.38328600668653,
26.1078236783229));
#18656=CARTESIAN_POINT('Ctrl Pts',(-2.12828112889404,-2.42067777856386,
26.1111715035696));
#18657=CARTESIAN_POINT('Ctrl Pts',(-1.89832407643467,-2.6158713245219,26.1288857019329));
#18658=CARTESIAN_POINT('Ctrl Pts',(-1.69357044304955,-2.75285907548838,
26.1422438874597));
#18659=CARTESIAN_POINT('Ctrl Pts',(-1.47525540475399,-2.86526422049419,
26.1560859507638));
#18660=CARTESIAN_POINT('Origin',(0.,0.,4.68922655072688));
#18661=CARTESIAN_POINT('',(-1.47525554463415,-2.86526414847326,27.6514736540563));
#18662=CARTESIAN_POINT('',(-1.47306432504218,-2.86105893806618,27.4070470808673));
#18663=CARTESIAN_POINT('',(-1.47525540501186,-2.86526422036142,4.68922655072688));
#18664=CARTESIAN_POINT('',(3.22274925660414,0.00218896264416769,26.8128035160936));
#18665=CARTESIAN_POINT('Ctrl Pts',(-1.47525554463428,-2.8652641484732,27.6514736540563));
#18666=CARTESIAN_POINT('Ctrl Pts',(-1.65781619981529,-2.77126806126031,
27.6397127301564));
#18667=CARTESIAN_POINT('Ctrl Pts',(-1.8310890777546,-2.65998124407618,27.6284558794886));
#18668=CARTESIAN_POINT('Ctrl Pts',(-2.12150031454677,-2.43150621874824,
27.6075843331467));
#18669=CARTESIAN_POINT('Ctrl Pts',(-2.24239055477045,-2.32048706666372,
27.5981388813136));
#18670=CARTESIAN_POINT('Ctrl Pts',(-2.3692664448582,-2.1847595100256,27.586963964455));
#18671=CARTESIAN_POINT('Ctrl Pts',(-2.38406442299321,-2.16860194459106,
27.585639418676));
#18672=CARTESIAN_POINT('Ctrl Pts',(-2.40744299694422,-2.1425469215207,27.5835119284357));
#18673=CARTESIAN_POINT('Ctrl Pts',(-2.41613015887314,-2.13274568148426,
27.5827134872523));
#18674=CARTESIAN_POINT('Ctrl Pts',(-2.43139879995696,-2.11530591056285,
27.5812959279024));
#18675=CARTESIAN_POINT('Ctrl Pts',(-2.43800466632634,-2.10768889141537,
27.5806778392771));
#18676=CARTESIAN_POINT('Ctrl Pts',(-2.4516461706162,-2.09180935662655,27.5793913775149));
#18677=CARTESIAN_POINT('Ctrl Pts',(-2.45867602606526,-2.08354206211609,
27.5787227764574));
#18678=CARTESIAN_POINT('Ctrl Pts',(-2.47672561001715,-2.06209672629191,
27.5769913243568));
#18679=CARTESIAN_POINT('Ctrl Pts',(-2.48768186026355,-2.04886593011761,
27.5759258942726));
#18680=CARTESIAN_POINT('Ctrl Pts',(-2.53397552710368,-1.99204281909594,
27.5713614434812));
#18681=CARTESIAN_POINT('Ctrl Pts',(-2.56827512270222,-1.94762132366348,
27.5678210627718));
#18682=CARTESIAN_POINT('Ctrl Pts',(-2.65568252578835,-1.82809350382125,
27.5583606627113));
#18683=CARTESIAN_POINT('Ctrl Pts',(-2.70676205448498,-1.75157420410728,
27.5523689397276));
#18684=CARTESIAN_POINT('Ctrl Pts',(-2.88022666122077,-1.46597166777845,
27.53026304279));
#18685=CARTESIAN_POINT('Ctrl Pts',(-2.98220811835585,-1.2454711537758,27.5136060344059));
#18686=CARTESIAN_POINT('Ctrl Pts',(-3.08768649294699,-0.927831165239926,
27.491334533395));
#18687=CARTESIAN_POINT('Ctrl Pts',(-3.11305367507109,-0.838796060182682,
27.4852767118327));
#18688=CARTESIAN_POINT('Ctrl Pts',(-3.1377963425146,-0.735218477075609,
27.4785312208174));
#18689=CARTESIAN_POINT('Ctrl Pts',(-3.14094892689835,-0.721631451156521,
27.4776522796681));
#18690=CARTESIAN_POINT('Ctrl Pts',(-3.14556877668978,-0.70111679772442,
27.4763345385518));
#18691=CARTESIAN_POINT('Ctrl Pts',(-3.14710153516616,-0.694204308950701,
27.475892115906));
#18692=CARTESIAN_POINT('Ctrl Pts',(-3.14980221429636,-0.681831904779727,
27.4751031606674));
#18693=CARTESIAN_POINT('Ctrl Pts',(-3.15097873466117,-0.676373972630644,
27.4747561415229));
#18694=CARTESIAN_POINT('Ctrl Pts',(-3.15349513424233,-0.664551205778928,
27.4740066553424));
#18695=CARTESIAN_POINT('Ctrl Pts',(-3.1548299272449,-0.658185383245754,
27.4736044818195));
#18696=CARTESIAN_POINT('Ctrl Pts',(-3.15850403298194,-0.640395054282058,
27.4724842780107));
#18697=CARTESIAN_POINT('Ctrl Pts',(-3.16080065070426,-0.628961690493888,
27.4717686500512));
#18698=CARTESIAN_POINT('Ctrl Pts',(-3.17378873323489,-0.562434234991849,
27.4676282369089));
#18699=CARTESIAN_POINT('Ctrl Pts',(-3.18310239484079,-0.507077135994187,
27.4642770033284));
#18700=CARTESIAN_POINT('Ctrl Pts',(-3.22657605741547,-0.199828863328797,
27.446053902051));
#18701=CARTESIAN_POINT('Ctrl Pts',(-3.23229104254463,0.0551957693487739,
27.4322607795362));
#18702=CARTESIAN_POINT('Ctrl Pts',(-3.19229938154424,0.471373402217451,
27.4086447978982));
#18703=CARTESIAN_POINT('Ctrl Pts',(-3.16421096649143,0.633029812475711,
27.399202322738));
#18704=CARTESIAN_POINT('Ctrl Pts',(-3.11857454046651,0.813074652908923,
27.388030735815));
#18705=CARTESIAN_POINT('Ctrl Pts',(-3.11297519364108,0.834255933821996,
27.3867062549834));
#18706=CARTESIAN_POINT('Ctrl Pts',(-3.10368431314574,0.868005052095016,
27.3845788493627));
#18707=CARTESIAN_POINT('Ctrl Pts',(-3.10013130601678,0.880610562982961,
27.3837804272787));
#18708=CARTESIAN_POINT('Ctrl Pts',(-3.09370721945747,0.902881420213494,
27.3823628900305));
#18709=CARTESIAN_POINT('Ctrl Pts',(-3.09086741519973,0.912555662234955,
27.3817448043006));
#18710=CARTESIAN_POINT('Ctrl Pts',(-3.08487683176028,0.932614746954922,
27.3804583367874));
#18711=CARTESIAN_POINT('Ctrl Pts',(-3.08171890510906,0.94299730574905,27.3797897270251));
#18712=CARTESIAN_POINT('Ctrl Pts',(-3.07342671183496,0.969773645987834,
27.3780582270596));
#18713=CARTESIAN_POINT('Ctrl Pts',(-3.06821374650669,0.986142517489724,
27.3769927575448));
#18714=CARTESIAN_POINT('Ctrl Pts',(-3.04541302715994,1.05580618511765,27.3724279089894));
#18715=CARTESIAN_POINT('Ctrl Pts',(-3.026566509117,1.1086756664749,27.3688871609821));
#18716=CARTESIAN_POINT('Ctrl Pts',(-2.97321351935743,1.24682770039801,27.3594255302163));
#18717=CARTESIAN_POINT('Ctrl Pts',(-2.9364213816863,1.33116674010156,27.3534329206279));
#18718=CARTESIAN_POINT('Ctrl Pts',(-2.78988411921005,1.63133627184148,27.3313351882926));
#18719=CARTESIAN_POINT('Ctrl Pts',(-2.65953566533557,1.83618261639722,27.3146880981289));
#18720=CARTESIAN_POINT('Ctrl Pts',(-2.44930034128831,2.09657509953146,27.2924174543771));
#18721=CARTESIAN_POINT('Ctrl Pts',(-2.38801935173462,2.16611780864668,27.2863520406239));
#18722=CARTESIAN_POINT('Ctrl Pts',(-2.31415464812323,2.24298918048435,27.2795991817342));
#18723=CARTESIAN_POINT('Ctrl Pts',(-2.30442290956503,2.25298630036574,27.2787200049193));
#18724=CARTESIAN_POINT('Ctrl Pts',(-2.28965423258522,2.26796190428536,27.2774019805127));
#18725=CARTESIAN_POINT('Ctrl Pts',(-2.28466545230893,2.27298734650806,27.2769595079822));
#18726=CARTESIAN_POINT('Ctrl Pts',(-2.27571351294254,2.28194582390838,27.2761704989037));
#18727=CARTESIAN_POINT('Ctrl Pts',(-2.27175667287515,2.28588502708855,27.275823475525));
#18728=CARTESIAN_POINT('Ctrl Pts',(-2.26316860777285,2.2943904881566,27.2750740201062));
#18729=CARTESIAN_POINT('Ctrl Pts',(-2.25853380585969,2.29895300276161,27.2746718813645));
#18730=CARTESIAN_POINT('Ctrl Pts',(-2.24555188109058,2.3116553030422,27.2735518726754));
#18731=CARTESIAN_POINT('Ctrl Pts',(-2.23717425257016,2.31976396731924,27.2728364036987));
#18732=CARTESIAN_POINT('Ctrl Pts',(-2.18824664750787,2.36660916822393,27.2686987739655));
#18733=CARTESIAN_POINT('Ctrl Pts',(-2.14673239669259,2.40433010348607,27.2653500492854));
#18734=CARTESIAN_POINT('Ctrl Pts',(-1.91170920050757,2.60693476467362,27.2471270757482));
#18735=CARTESIAN_POINT('Ctrl Pts',(-1.70018623211788,2.74956997773852,27.2333322852882));
#18736=CARTESIAN_POINT('Ctrl Pts',(-1.32836325871861,2.94081940147733,27.2097146712626));
#18737=CARTESIAN_POINT('Ctrl Pts',(-1.17716375683939,3.00453702726673,27.2002723556666));
#18738=CARTESIAN_POINT('Ctrl Pts',(-1.00100026283659,3.06342887193728,27.1891003750793));
#18739=CARTESIAN_POINT('Ctrl Pts',(-0.980142726357965,3.07016582275797,
27.1877753174509));
#18740=CARTESIAN_POINT('Ctrl Pts',(-0.946712647478207,3.08058830796385,
27.1856471603357));
#18741=CARTESIAN_POINT('Ctrl Pts',(-0.934183307509532,3.08441091621679,
27.1848485686419));
#18742=CARTESIAN_POINT('Ctrl Pts',(-0.911969338819483,3.09104046441739,
27.1834308351092));
#18743=CARTESIAN_POINT('Ctrl Pts',(-0.902294133196074,3.09387855630155,
27.1828127236548));
#18744=CARTESIAN_POINT('Ctrl Pts',(-0.882179360938241,3.09967657697798,
27.1815263071502));
#18745=CARTESIAN_POINT('Ctrl Pts',(-0.871737858464647,3.10262927341308,
27.1808577746406));
#18746=CARTESIAN_POINT('Ctrl Pts',(-0.844733051331343,3.11011873696422,
27.1791266994719));
#18747=CARTESIAN_POINT('Ctrl Pts',(-0.828148201914945,3.11457589782154,
27.1780615799017));
#18748=CARTESIAN_POINT('Ctrl Pts',(-0.757264618021113,3.13301960038357,
27.1735002602618));
#18749=CARTESIAN_POINT('Ctrl Pts',(-0.702644190887562,3.14571963497021,
27.1699627707197));
#18750=CARTESIAN_POINT('Ctrl Pts',(-0.557733315106304,3.17545117037993,
27.1605120560273));
#18751=CARTESIAN_POINT('Ctrl Pts',(-0.467002854492969,3.19005680256146,
27.1545273096502));
#18752=CARTESIAN_POINT('Ctrl Pts',(-0.13418607197542,3.22913041977734,27.1323597384297));
#18753=CARTESIAN_POINT('Ctrl Pts',(0.109815592445874,3.2300487079109,27.1156274520607));
#18754=CARTESIAN_POINT('Ctrl Pts',(0.44271860617565,3.19351266656144,27.0933490476567));
#18755=CARTESIAN_POINT('Ctrl Pts',(0.533393435017489,3.17962540915764,27.0873484228968));
#18756=CARTESIAN_POINT('Ctrl Pts',(0.637017339159052,3.15919613512662,27.0806584777717));
#18757=CARTESIAN_POINT('Ctrl Pts',(0.650656520955948,3.1564152798355,27.0797813347808));
#18758=CARTESIAN_POINT('Ctrl Pts',(0.671199908990393,3.15208792549332,27.078465755437));
#18759=CARTESIAN_POINT('Ctrl Pts',(0.678117533000828,3.15060696082114,27.0780237136284));
#18760=CARTESIAN_POINT('Ctrl Pts',(0.690485545853977,3.14791652388995,27.0772351691785));
#18761=CARTESIAN_POINT('Ctrl Pts',(0.695937700745256,3.1467156605998,27.0768881821161));
#18762=CARTESIAN_POINT('Ctrl Pts',(0.707739386280071,3.1440841090703,27.0761384599764));
#18763=CARTESIAN_POINT('Ctrl Pts',(0.714087692662342,3.14264835652323,27.0757360200563));
#18764=CARTESIAN_POINT('Ctrl Pts',(0.731817595176636,3.13858200917598,27.0746143214456));
#18765=CARTESIAN_POINT('Ctrl Pts',(0.743189439121718,3.135908718099,27.0738974754793));
#18766=CARTESIAN_POINT('Ctrl Pts',(0.809431389883048,3.11995599682877,27.0697356565637));
#18767=CARTESIAN_POINT('Ctrl Pts',(0.863963231513516,3.10529757549453,27.0663651268802));
#18768=CARTESIAN_POINT('Ctrl Pts',(1.16149695882205,3.01687330508875,27.0481409843214));
#18769=CARTESIAN_POINT('Ctrl Pts',(1.39552806495163,2.91601239501047,27.0343606466419));
#18770=CARTESIAN_POINT('Ctrl Pts',(1.75693146033795,2.70667619707327,27.0107689084841));
#18771=CARTESIAN_POINT('Ctrl Pts',(1.89208228380004,2.6139851596062,27.0013374462024));
#18772=CARTESIAN_POINT('Ctrl Pts',(2.03670462064768,2.49768565046564,26.9901755756113));
#18773=CARTESIAN_POINT('Ctrl Pts',(2.05366783180704,2.48375677561358,26.9888486957158));
#18774=CARTESIAN_POINT('Ctrl Pts',(2.08053237720843,2.46123432875514,26.9867181645616));
#18775=CARTESIAN_POINT('Ctrl Pts',(2.09052603392217,2.45275157469747,26.9859190371874));
#18776=CARTESIAN_POINT('Ctrl Pts',(2.10811572221947,2.43763560804012,26.9845006835427));
#18777=CARTESIAN_POINT('Ctrl Pts',(2.11573293645051,2.43102723016447,26.983882490659));
#18778=CARTESIAN_POINT('Ctrl Pts',(2.12363994420259,2.42410212903047,26.9832365843784));
#18779=CARTESIAN_POINT('Ctrl Pts',(2.12396089129666,2.42382092507454,26.9832103596731));
#18780=CARTESIAN_POINT('Ctrl Pts',(2.12448388156465,2.42336251347108,26.9831676141479));
#18781=CARTESIAN_POINT('Ctrl Pts',(2.12468595658513,2.42318534590571,26.9831510950932));
#18782=CARTESIAN_POINT('Ctrl Pts',(2.12501667403802,2.42289531900333,26.9831240551864));
#18783=CARTESIAN_POINT('Ctrl Pts',(2.12514533144021,2.42278247311706,26.9831135348179));
#18784=CARTESIAN_POINT('Ctrl Pts',(2.12544085444423,2.42252322714103,26.9830893671044));
#18785=CARTESIAN_POINT('Ctrl Pts',(2.12560771661837,2.42237681767885,26.983075719244));
#18786=CARTESIAN_POINT('Ctrl Pts',(2.12592706069774,2.42209655799667,26.9830495959493));
#18787=CARTESIAN_POINT('Ctrl Pts',(2.12607954760934,2.42196270840443,26.9830371204282));
#18788=CARTESIAN_POINT('Ctrl Pts',(2.12637159164145,2.42170630986765,26.983013224081));
#18789=CARTESIAN_POINT('Ctrl Pts',(2.12651115245028,2.42158376181839,26.9830018032192));
#18790=CARTESIAN_POINT('Ctrl Pts',(2.12677863139575,2.42134884816812,26.9829799116317));
#18791=CARTESIAN_POINT('Ctrl Pts',(2.12690654581621,2.42123648924487,26.9829694414299));
#18792=CARTESIAN_POINT('Ctrl Pts',(2.12715185014933,2.42102098159565,26.9829493602763));
#18793=CARTESIAN_POINT('Ctrl Pts',(2.12726924146242,2.42091783446856,26.9829397493917));
#18794=CARTESIAN_POINT('Ctrl Pts',(2.12749449537281,2.42071988368759,26.982921305876));
#18795=CARTESIAN_POINT('Ctrl Pts',(2.12760235914042,2.42062508135858,26.9829124733004));
#18796=CARTESIAN_POINT('Ctrl Pts',(2.12780944186967,2.42044305015498,26.9828955144633));
#18797=CARTESIAN_POINT('Ctrl Pts',(2.12790866180641,2.42035582238697,26.9828873882482));
#18798=CARTESIAN_POINT('Ctrl Pts',(2.128099243805,2.42018825421044,26.9828717780495));
#18799=CARTESIAN_POINT('Ctrl Pts',(2.12819060667789,2.42010791473224,26.9828642941053));
#18800=CARTESIAN_POINT('Ctrl Pts',(2.12836617707482,2.41995351016512,26.9828499112095));
#18801=CARTESIAN_POINT('Ctrl Pts',(2.12845038529192,2.41987944584585,26.9828430122899));
#18802=CARTESIAN_POINT('Ctrl Pts',(2.12861227528996,2.41973704246755,26.9828297481773));
#18803=CARTESIAN_POINT('Ctrl Pts',(2.12868995764406,2.41966870406467,26.9828233830119));
#18804=CARTESIAN_POINT('Ctrl Pts',(2.1288393602953,2.41953725941216,26.9828111403813));
#18805=CARTESIAN_POINT('Ctrl Pts',(2.12891108108067,2.41947415371153,26.9828052629389));
#18806=CARTESIAN_POINT('Ctrl Pts',(2.12904906831265,2.41935273058916,26.9827939543311));
#18807=CARTESIAN_POINT('Ctrl Pts',(2.12911533516649,2.41929441363614,26.9827885231854));
#18808=CARTESIAN_POINT('Ctrl Pts',(2.12924287225998,2.41918216761212,26.9827780698118));
#18809=CARTESIAN_POINT('Ctrl Pts',(2.12930414285475,2.41912823892906,26.9827730475998));
#18810=CARTESIAN_POINT('Ctrl Pts',(2.12945437320062,2.41899600020402,26.9827607329064));
#18811=CARTESIAN_POINT('Ctrl Pts',(2.12954333065476,2.41891768760537,26.9827534403187));
#18812=CARTESIAN_POINT('Ctrl Pts',(2.12971974953185,2.41876236214608,26.9827389766738));
#18813=CARTESIAN_POINT('Ctrl Pts',(2.12980721111147,2.41868534943636,26.9827318056223));
#18814=CARTESIAN_POINT('Ctrl Pts',(2.12998068616536,2.4185325824143,26.9827175811755));
#18815=CARTESIAN_POINT('Ctrl Pts',(2.13006669977602,2.41845682825688,26.9827105277867));
#18816=CARTESIAN_POINT('Ctrl Pts',(2.13023732496138,2.41830653858357,26.98269653494));
#18817=CARTESIAN_POINT('Ctrl Pts',(2.13032193666402,2.41823200321696,26.9826895954886));
#18818=CARTESIAN_POINT('Ctrl Pts',(2.13048980233284,2.41808411288109,26.9826758269335));
#18819=CARTESIAN_POINT('Ctrl Pts',(2.13057305642712,2.41801075804864,26.9826689978354));
#18820=CARTESIAN_POINT('Ctrl Pts',(2.13073824948652,2.41786519198312,26.9826554465398));
#18821=CARTESIAN_POINT('Ctrl Pts',(2.13082018858066,2.41779298087441,26.9826487243471));
#18822=CARTESIAN_POINT('Ctrl Pts',(2.13975179572824,2.40992094663764,26.9819159332282));
#18823=CARTESIAN_POINT('Ctrl Pts',(2.14855847974299,2.40207268198773,26.9811878322361));
#18824=CARTESIAN_POINT('Ctrl Pts',(2.17337713017793,2.37970932694403,26.979119976195));
#18825=CARTESIAN_POINT('Ctrl Pts',(2.18928622110668,2.36508148613681,26.9777754502592));
#18826=CARTESIAN_POINT('Ctrl Pts',(2.22478825923671,2.33177347566321,26.9747313544002));
#18827=CARTESIAN_POINT('Ctrl Pts',(2.24429519063882,2.31300440239998,26.9730280092599));
#18828=CARTESIAN_POINT('Ctrl Pts',(2.3052369928669,2.25287098159566,26.9676072573075));
#18829=CARTESIAN_POINT('Ctrl Pts',(2.3457805017552,2.21062398217785,26.9638519641924));
#18830=CARTESIAN_POINT('Ctrl Pts',(2.46840265004866,2.07567620416749,26.9520167012964));
#18831=CARTESIAN_POINT('Ctrl Pts',(2.54630033850352,1.97934151531673,26.9437873128926));
#18832=CARTESIAN_POINT('Ctrl Pts',(2.76658110839767,1.67233484702046,26.9183583337546));
#18833=CARTESIAN_POINT('Ctrl Pts',(2.88977645563576,1.44909647270064,26.9008597999752));
#18834=CARTESIAN_POINT('Ctrl Pts',(2.99337899916188,1.19425302280171,26.8833020401578));
#18835=CARTESIAN_POINT('Ctrl Pts',(3.00109375128844,1.17473165681126,26.8819720718141));
#18836=CARTESIAN_POINT('Ctrl Pts',(3.01166073617319,1.14720933649259,26.8801193649455));
#18837=CARTESIAN_POINT('Ctrl Pts',(3.01467271529979,1.13927085236154,26.8795875686246));
#18838=CARTESIAN_POINT('Ctrl Pts',(3.01948888966352,1.12642432018076,26.8787312784983));
#18839=CARTESIAN_POINT('Ctrl Pts',(3.02131254998701,1.12152368682939,26.8784056315513));
#18840=CARTESIAN_POINT('Ctrl Pts',(3.02512747309933,1.11119519438116,26.8777214540606));
#18841=CARTESIAN_POINT('Ctrl Pts',(3.02711606903218,1.10576638306868,26.8773630901564));
#18842=CARTESIAN_POINT('Ctrl Pts',(3.03194575885721,1.09247079357676,26.8764884173594));
#18843=CARTESIAN_POINT('Ctrl Pts',(3.03477088212172,1.08459818189439,26.8759730580219));
#18844=CARTESIAN_POINT('Ctrl Pts',(3.0448363611382,1.0562020297449,26.8741230624216));
#18845=CARTESIAN_POINT('Ctrl Pts',(3.05189962312081,1.03561573164215,26.8727985457858));
#18846=CARTESIAN_POINT('Ctrl Pts',(3.09470752271064,0.906606719356821,26.864592628539));
#18847=CARTESIAN_POINT('Ctrl Pts',(3.12488229447489,0.796408584558225,26.8579968505618));
#18848=CARTESIAN_POINT('Ctrl Pts',(3.19792077192141,0.46054610066478,26.8384941356114));
#18849=CARTESIAN_POINT('Ctrl Pts',(3.22259336429628,0.23170490280408,26.8259554958184));
#18850=CARTESIAN_POINT('Ctrl Pts',(3.22274925660414,0.00218896264416769,
26.8128035160936));
#18851=CARTESIAN_POINT('Ctrl Pts',(3.22274925938025,0.00218487163455499,
26.812803281666));
#18852=CARTESIAN_POINT('Ctrl Pts',(3.22282586991472,-0.11081789673651,26.8063278673062));
#18853=CARTESIAN_POINT('Ctrl Pts',(3.21695904115532,-0.22373863276078,26.7997274087064));
#18854=CARTESIAN_POINT('Ctrl Pts',(3.2032990818962,-0.35400002154735,26.791857615261));
#18855=CARTESIAN_POINT('Ctrl Pts',(3.20127368655899,-0.371870659126245,
26.7907724378864));
#18856=CARTESIAN_POINT('Ctrl Pts',(3.19766221446762,-0.40151595118787,26.7889626733654));
#18857=CARTESIAN_POINT('Ctrl Pts',(3.19616039951728,-0.413300606782162,
26.7882407322455));
#18858=CARTESIAN_POINT('Ctrl Pts',(3.19333552719224,-0.43453047307473,26.7869355052361));
#18859=CARTESIAN_POINT('Ctrl Pts',(3.19203562979979,-0.443978666451927,
26.7863529560028));
#18860=CARTESIAN_POINT('Ctrl Pts',(3.18929325563838,-0.46327657895039,26.785159628212));
#18861=CARTESIAN_POINT('Ctrl Pts',(3.18784704306445,-0.473125655139622,
26.7845487372277));
#18862=CARTESIAN_POINT('Ctrl Pts',(3.18462666541318,-0.494371931787416,
26.7832268636517));
#18863=CARTESIAN_POINT('Ctrl Pts',(3.18283690298084,-0.505766594860303,
26.7825153925917));
#18864=CARTESIAN_POINT('Ctrl Pts',(3.17781813311832,-0.536636936309397,
26.780580889161));
#18865=CARTESIAN_POINT('Ctrl Pts',(3.17447132019761,-0.556092706161243,
26.7793541227819));
#18866=CARTESIAN_POINT('Ctrl Pts',(3.15728261115944,-0.650798072895399,
26.773344753271));
#18867=CARTESIAN_POINT('Ctrl Pts',(3.14094366649954,-0.725563850861264,
26.768483090343));
#18868=CARTESIAN_POINT('Ctrl Pts',(3.10621929689288,-0.861129482699843,
26.7594448787204));
#18869=CARTESIAN_POINT('Ctrl Pts',(3.08866707250532,-0.922104778427121,
26.7552952450145));
#18870=CARTESIAN_POINT('Ctrl Pts',(2.99631415848239,-1.21060935231673,26.7352726325752));
#18871=CARTESIAN_POINT('Ctrl Pts',(2.89811279011069,-1.42982528152186,26.7188151032878));
#18872=CARTESIAN_POINT('Ctrl Pts',(2.7306887777384,-1.71394708060185,26.6968304959542));
#18873=CARTESIAN_POINT('Ctrl Pts',(2.68157778680158,-1.78980989015985,26.6908982231299));
#18874=CARTESIAN_POINT('Ctrl Pts',(2.61819748508275,-1.87923676115799,26.6839168555513));
#18875=CARTESIAN_POINT('Ctrl Pts',(2.60691404549134,-1.89485832646647,26.6826978005048));
#18876=CARTESIAN_POINT('Ctrl Pts',(2.5907684981817,-1.91679409845154,26.6809877894722));
#18877=CARTESIAN_POINT('Ctrl Pts',(2.58602231376956,-1.9231925600227,26.6804892123659));
#18878=CARTESIAN_POINT('Ctrl Pts',(2.57783629803442,-1.93414325632453,26.6796363874198));
#18879=CARTESIAN_POINT('Ctrl Pts',(2.57440803011895,-1.9387040547454,26.6792813401163));
#18880=CARTESIAN_POINT('Ctrl Pts',(2.56776165081248,-1.9474973519895,26.6785971106331));
#18881=CARTESIAN_POINT('Ctrl Pts',(2.56454517435413,-1.9517309960804,26.6782678139882));
#18882=CARTESIAN_POINT('Ctrl Pts',(2.55588564643758,-1.96307061650966,26.6773861110432));
#18883=CARTESIAN_POINT('Ctrl Pts',(2.55042339512233,-1.97016197130031,26.6768350490692));
#18884=CARTESIAN_POINT('Ctrl Pts',(2.53030613709133,-1.99605528196499,26.6748237055083));
#18885=CARTESIAN_POINT('Ctrl Pts',(2.5154717655646,-2.01471777424034,26.6733755904247));
#18886=CARTESIAN_POINT('Ctrl Pts',(2.35613980287337,-2.21066296036537,26.6581671547071));
#18887=CARTESIAN_POINT('Ctrl Pts',(2.19334680755055,-2.37227449380517,26.6455566901088));
#18888=CARTESIAN_POINT('Ctrl Pts',(1.89336608041769,-2.61256316101187,26.6240649359234));
#18889=CARTESIAN_POINT('Ctrl Pts',(1.76506558768164,-2.70089973017839,26.6153158363823));
#18890=CARTESIAN_POINT('Ctrl Pts',(1.58558389696391,-2.80620764940771,26.6031906303567));
#18891=CARTESIAN_POINT('Ctrl Pts',(1.53962963072683,-2.83168109577019,26.6000967564946));
#18892=CARTESIAN_POINT('Ctrl Pts',(1.47087546430418,-2.86762452903817,26.5954707591397));
#18893=CARTESIAN_POINT('Ctrl Pts',(1.44854183317959,-2.87897057573071,26.593968553581));
#18894=CARTESIAN_POINT('Ctrl Pts',(1.40782601998691,-2.89906152721095,26.591229433639));
#18895=CARTESIAN_POINT('Ctrl Pts',(1.38948879685016,-2.90789489066779,26.5899956376444));
#18896=CARTESIAN_POINT('Ctrl Pts',(1.36067314126448,-2.92144110569147,26.5880560130512));
#18897=CARTESIAN_POINT('Ctrl Pts',(1.35025088353301,-2.92627272780803,26.5873543139805));
#18898=CARTESIAN_POINT('Ctrl Pts',(1.33973635302105,-2.93107899454848,26.5866461870607));
#18899=CARTESIAN_POINT('Ctrl Pts',(1.33966958388279,-2.93110951243872,26.5866416903202));
#18900=CARTESIAN_POINT('Ctrl Pts',(1.33953387203146,-2.93117153608009,26.5866325504364));
#18901=CARTESIAN_POINT('Ctrl Pts',(1.33946492923982,-2.93120304168481,26.5866279072872));
#18902=CARTESIAN_POINT('Ctrl Pts',(1.33932479338795,-2.93126707524969,26.5866184694192));
#18903=CARTESIAN_POINT('Ctrl Pts',(1.33925360024441,-2.93129960305304,26.5866136746942));
#18904=CARTESIAN_POINT('Ctrl Pts',(1.33910888402373,-2.93136571682251,26.5866039283072));
#18905=CARTESIAN_POINT('Ctrl Pts',(1.33903536085931,-2.93139930262017,26.5865989766387));
#18906=CARTESIAN_POINT('Ctrl Pts',(1.33888589550201,-2.9314675724449,26.5865889103625));
#18907=CARTESIAN_POINT('Ctrl Pts',(1.33880995323971,-2.93150225627913,26.586583795749));
#18908=CARTESIAN_POINT('Ctrl Pts',(1.33865559563525,-2.93157274619029,26.586573399941));
#18909=CARTESIAN_POINT('Ctrl Pts',(1.3385771614073,-2.93160856065243,26.5865681174734));
#18910=CARTESIAN_POINT('Ctrl Pts',(1.3384177031863,-2.9316813643756,26.5865573780954));
#18911=CARTESIAN_POINT('Ctrl Pts',(1.33833668076369,-2.93171835266499,26.58655192129));
#18912=CARTESIAN_POINT('Ctrl Pts',(1.33817195333232,-2.93179354564366,26.5865408269824));
#18913=CARTESIAN_POINT('Ctrl Pts',(1.33808824982571,-2.93183174937478,26.5865351895806));
#18914=CARTESIAN_POINT('Ctrl Pts',(1.33791806393331,-2.93190941635902,26.5865237275923));
#18915=CARTESIAN_POINT('Ctrl Pts',(1.33783158288042,-2.93194887871225,26.5865179030946));
#18916=CARTESIAN_POINT('Ctrl Pts',(1.337655741717,-2.93202910776756,26.5865060601647));
#18917=CARTESIAN_POINT('Ctrl Pts',(1.33756638284808,-2.93206987359099,26.586500041815));
#18918=CARTESIAN_POINT('Ctrl Pts',(1.33738468195895,-2.9321527561265,26.5864878041672));
#18919=CARTESIAN_POINT('Ctrl Pts',(1.33729234107312,-2.93219487198691,26.5864815849445));
#18920=CARTESIAN_POINT('Ctrl Pts',(1.3371045680401,-2.93228050288938,26.5864689382659));
#18921=CARTESIAN_POINT('Ctrl Pts',(1.33700913688059,-2.93232401712314,26.5864625108754));
#18922=CARTESIAN_POINT('Ctrl Pts',(1.33681507096482,-2.93241249490759,26.5864494402919));
#18923=CARTESIAN_POINT('Ctrl Pts',(1.33671643706481,-2.9324574576846,26.5864427971554));
#18924=CARTESIAN_POINT('Ctrl Pts',(1.33651584883393,-2.93254888465101,26.5864292872069));
#18925=CARTESIAN_POINT('Ctrl Pts',(1.33641389529651,-2.93259534806815,26.5864224204471));
#18926=CARTESIAN_POINT('Ctrl Pts',(1.33620654650832,-2.93268983034023,26.5864084550794));
#18927=CARTESIAN_POINT('Ctrl Pts',(1.33610115192091,-2.93273784845299,26.5864013565149));
#18928=CARTESIAN_POINT('Ctrl Pts',(1.33588679290125,-2.93283549715756,26.5863869189032));
#18929=CARTESIAN_POINT('Ctrl Pts',(1.33577782901695,-2.93288512702751,26.5863795798915));
#18930=CARTESIAN_POINT('Ctrl Pts',(1.33557523126474,-2.93297739076114,26.5863659343418));
#18931=CARTESIAN_POINT('Ctrl Pts',(1.33548159238519,-2.93302002882444,26.5863596274726));
#18932=CARTESIAN_POINT('Ctrl Pts',(1.3352795757446,-2.93311200455708,26.5863460209864));
#18933=CARTESIAN_POINT('Ctrl Pts',(1.33517119968111,-2.93316133961647,26.586338721478));
#18934=CARTESIAN_POINT('Ctrl Pts',(1.33493737618472,-2.93326776533605,26.5863229725933));
#18935=CARTESIAN_POINT('Ctrl Pts',(1.33481192986262,-2.93332485302804,26.5863145232839));
#18936=CARTESIAN_POINT('Ctrl Pts',(1.33454126183888,-2.93344800676647,26.5862962926457));
#18937=CARTESIAN_POINT('Ctrl Pts',(1.33439604061519,-2.93351406929371,26.5862865113384));
#18938=CARTESIAN_POINT('Ctrl Pts',(1.33408268889166,-2.93365658791416,26.5862654055879));
#18939=CARTESIAN_POINT('Ctrl Pts',(1.33391455807964,-2.93373303972201,26.5862540811092));
#18940=CARTESIAN_POINT('Ctrl Pts',(1.33355175632577,-2.93389797392922,26.5862296444129));
#18941=CARTESIAN_POINT('Ctrl Pts',(1.33335708414848,-2.93398645095311,26.5862165320925));
#18942=CARTESIAN_POINT('Ctrl Pts',(1.33299563058492,-2.93415068544491,26.5861921859174));
#18943=CARTESIAN_POINT('Ctrl Pts',(1.33282885134609,-2.93422644815883,26.5861809522279));
#18944=CARTESIAN_POINT('Ctrl Pts',(1.32348033633171,-2.93847223148143,26.5855512644567));
#18945=CARTESIAN_POINT('Ctrl Pts',(1.31427916940426,-2.9425991091253,26.5849313286266));
#18946=CARTESIAN_POINT('Ctrl Pts',(1.29307332661465,-2.95199098331864,26.5835020988738));
#18947=CARTESIAN_POINT('Ctrl Pts',(1.28105565545905,-2.95722603009173,26.5826917882655));
#18948=CARTESIAN_POINT('Ctrl Pts',(1.24883077170862,-2.97103029672416,26.5805178922718));
#18949=CARTESIAN_POINT('Ctrl Pts',(1.22856767045543,-2.97946652289181,26.5791498048508));
#18950=CARTESIAN_POINT('Ctrl Pts',(1.05679288327298,-3.04893204777257,26.5675407676242));
#18951=CARTESIAN_POINT('Ctrl Pts',(0.900952952378805,-3.09855886776507,
26.5569151848866));
#18952=CARTESIAN_POINT('Ctrl Pts',(0.495527185882263,-3.19448636872886,
26.5291312511289));
#18953=CARTESIAN_POINT('Ctrl Pts',(0.243006374883721,-3.22354358082419,
26.5116470754176));
#18954=CARTESIAN_POINT('Ctrl Pts',(-0.0676383208765035,-3.22255018002376,
26.4913132309825));
#18955=CARTESIAN_POINT('Ctrl Pts',(-0.124959999337608,-3.22083693580544,
26.4876143413083));
#18956=CARTESIAN_POINT('Ctrl Pts',(-0.193924656320438,-3.21693153131852,
26.4832519524339));
#18957=CARTESIAN_POINT('Ctrl Pts',(-0.205636401191146,-3.21620411821422,
26.4825141822825));
#18958=CARTESIAN_POINT('Ctrl Pts',(-0.223849264150498,-3.21497302938225,
26.4813719175965));
#18959=CARTESIAN_POINT('Ctrl Pts',(-0.230353125159929,-3.21451357319154,
26.4809650119228));
#18960=CARTESIAN_POINT('Ctrl Pts',(-0.242422233832086,-3.21362415017293,
26.4802118366673));
#18961=CARTESIAN_POINT('Ctrl Pts',(-0.247987706845663,-3.21319946720083,
26.4798652840179));
#18962=CARTESIAN_POINT('Ctrl Pts',(-0.26058906060733,-3.21220496388882,
26.4790823223573));
#18963=CARTESIAN_POINT('Ctrl Pts',(-0.267624172065996,-3.2116264872033,
26.4786464053393));
#18964=CARTESIAN_POINT('Ctrl Pts',(-0.288453704431659,-3.20984481764432,
26.4773591384643));
#18965=CARTESIAN_POINT('Ctrl Pts',(-0.302242542533823,-3.20857581403445,
26.4765113987285));
#18966=CARTESIAN_POINT('Ctrl Pts',(-0.405173996976067,-3.19843346836605,
26.4702132736777));
#18967=CARTESIAN_POINT('Ctrl Pts',(-0.49392894998173,-3.18593471000097,
26.4649510967362));
#18968=CARTESIAN_POINT('Ctrl Pts',(-0.823926422260698,-3.12533787396944,
26.4456384830663));
#18969=CARTESIAN_POINT('Ctrl Pts',(-1.0599270876327,-3.05338505479416,26.4322794705481));
#18970=CARTESIAN_POINT('Ctrl Pts',(-1.34969414152482,-2.92734523078933,
26.414286725607));
#18971=CARTESIAN_POINT('Ctrl Pts',(-1.41299276552639,-2.89732175120204,
26.4102562562727));
#18972=CARTESIAN_POINT('Ctrl Pts',(-1.47525541363878,-2.86526421591962,
26.4061645232028));
#18973=CARTESIAN_POINT('',(3.21940908233495,-0.00238856237501944,26.5642265507269));
#18974=CARTESIAN_POINT('Ctrl Pts',(-1.47525540475399,-2.86526422049419,
26.1560859507638));
#18975=CARTESIAN_POINT('Ctrl Pts',(-1.46764044335333,-2.86918498036092,
26.156568770356));
#18976=CARTESIAN_POINT('Ctrl Pts',(-1.46000897820681,-2.87307583278742,
26.1570521035361));
#18977=CARTESIAN_POINT('Ctrl Pts',(-1.30595814504514,-2.95084516714172,
26.16679927672));
#18978=CARTESIAN_POINT('Ctrl Pts',(-1.15414623481615,-3.01346144532023,
26.1762494445484));
#18979=CARTESIAN_POINT('Ctrl Pts',(-0.977417527058379,-3.07103438507643,
26.1874290175851));
#18980=CARTESIAN_POINT('Ctrl Pts',(-0.956525440761596,-3.07760560524402,
26.1887530375465));
#18981=CARTESIAN_POINT('Ctrl Pts',(-0.92304008146664,-3.08776391163117,
26.1908797013164));
#18982=CARTESIAN_POINT('Ctrl Pts',(-0.910488879267811,-3.09148814630701,
26.1916778456073));
#18983=CARTESIAN_POINT('Ctrl Pts',(-0.888235651919161,-3.09794392686131,
26.1930948876133));
#18984=CARTESIAN_POINT('Ctrl Pts',(-0.878542795701445,-3.10070664522986,
26.1937127566156));
#18985=CARTESIAN_POINT('Ctrl Pts',(-0.858390510585305,-3.10634849645055,
26.1949987701897));
#18986=CARTESIAN_POINT('Ctrl Pts',(-0.847929198296684,-3.10922037175426,
26.1956671425741));
#18987=CARTESIAN_POINT('Ctrl Pts',(-0.820870895580562,-3.11650179491454,
26.1973980193688));
#18988=CARTESIAN_POINT('Ctrl Pts',(-0.804252966834529,-3.12083155775106,
26.1984631012167));
#18989=CARTESIAN_POINT('Ctrl Pts',(-0.733203124191961,-3.1387382636165,
26.2030261550677));
#18990=CARTESIAN_POINT('Ctrl Pts',(-0.678459038817052,-3.15102481793287,
26.2065654631099));
#18991=CARTESIAN_POINT('Ctrl Pts',(-0.533223099603586,-3.179660885973,26.2160228537045));
#18992=CARTESIAN_POINT('Ctrl Pts',(-0.442309085280903,-3.19357642378303,
26.2220125964033));
#18993=CARTESIAN_POINT('Ctrl Pts',(-0.109722320735569,-3.23000903986616,
26.2441460620574));
#18994=CARTESIAN_POINT('Ctrl Pts',(0.133673291029568,-3.22910419147909,
26.2608353902054));
#18995=CARTESIAN_POINT('Ctrl Pts',(0.466180526924267,-3.190185896532,26.2831093112432));
#18996=CARTESIAN_POINT('Ctrl Pts',(0.557220002835747,-3.17555028862907,
26.2891421071121));
#18997=CARTESIAN_POINT('Ctrl Pts',(0.661163076989448,-3.15423129277377,
26.2958630832165));
#18998=CARTESIAN_POINT('Ctrl Pts',(0.674792952130234,-3.15134354695577,
26.2967410323165));
#18999=CARTESIAN_POINT('Ctrl Pts',(0.695316189556948,-3.1468560536317,26.2980574909063));
#19000=CARTESIAN_POINT('Ctrl Pts',(0.702223503362877,-3.14532188803192,
26.2984996140915));
#19001=CARTESIAN_POINT('Ctrl Pts',(0.714570140462353,-3.14253690924731,
26.2992881364272));
#19002=CARTESIAN_POINT('Ctrl Pts',(0.720011299888353,-3.14129470779614,
26.2996350209954));
#19003=CARTESIAN_POINT('Ctrl Pts',(0.731785834247685,-3.13857441358129,
26.3003843244804));
#19004=CARTESIAN_POINT('Ctrl Pts',(0.738117951353907,-3.13709128787278,
26.300786449512));
#19005=CARTESIAN_POINT('Ctrl Pts',(0.755794412267653,-3.13289457598759,
26.3019067779972));
#19006=CARTESIAN_POINT('Ctrl Pts',(0.767128713543755,-3.13013852160256,
26.3026225772049));
#19007=CARTESIAN_POINT('Ctrl Pts',(0.832997717855822,-3.11374250859242,
26.3067688093427));
#19008=CARTESIAN_POINT('Ctrl Pts',(0.887186716091496,-3.0987381671683,26.3101254391457));
#19009=CARTESIAN_POINT('Ctrl Pts',(1.18390322436164,-3.0081577439854,26.3283431138471));
#19010=CARTESIAN_POINT('Ctrl Pts',(1.41724969787939,-2.90552411867305,26.3421277450282));
#19011=CARTESIAN_POINT('Ctrl Pts',(1.7773175230257,-2.69334597295007,26.365734231375));
#19012=CARTESIAN_POINT('Ctrl Pts',(1.91192769710494,-2.59951767631807,26.3751767648808));
#19013=CARTESIAN_POINT('Ctrl Pts',(2.0558054133444,-2.4819877530351,26.3863504920979));
#19014=CARTESIAN_POINT('Ctrl Pts',(2.07265749311309,-2.467932329606,26.387677078521));
#19015=CARTESIAN_POINT('Ctrl Pts',(2.09934191257006,-2.44521018093835,26.3898070858959));
#19016=CARTESIAN_POINT('Ctrl Pts',(2.10926738659486,-2.43665352045053,26.3906059846795));
#19017=CARTESIAN_POINT('Ctrl Pts',(2.12673528682884,-2.42140789765445,26.3920239000555));
#19018=CARTESIAN_POINT('Ctrl Pts',(2.13429907633432,-2.41474359635906,26.3926418837084));
#19019=CARTESIAN_POINT('Ctrl Pts',(2.14879599602678,-2.40184933105798,26.3938341396676));
#19020=CARTESIAN_POINT('Ctrl Pts',(2.15573361964947,-2.39562455318779,26.3944081899572));
#19021=CARTESIAN_POINT('Ctrl Pts',(2.17384979557704,-2.37922740930883,26.395916440901));
#19022=CARTESIAN_POINT('Ctrl Pts',(2.18498386242145,-2.36900643886014,26.3968527025562));
#19023=CARTESIAN_POINT('Ctrl Pts',(2.22647069933631,-2.33038063473043,26.4003767636376));
#19024=CARTESIAN_POINT('Ctrl Pts',(2.25634377315805,-2.30146870369513,26.4029863306109));
#19025=CARTESIAN_POINT('Ctrl Pts',(2.32914064679154,-2.22823414681796,26.4095306633531));
#19026=CARTESIAN_POINT('Ctrl Pts',(2.37136526263424,-2.18324289586147,26.4134941670493));
#19027=CARTESIAN_POINT('Ctrl Pts',(2.49236435097461,-2.04666217932373,26.425362428195));
#19028=CARTESIAN_POINT('Ctrl Pts',(2.56730534970951,-1.9518311241881,26.4334000256452));
#19029=CARTESIAN_POINT('Ctrl Pts',(2.7813350911386,-1.6472799421725,26.4584603722913));
#19030=CARTESIAN_POINT('Ctrl Pts',(2.90135541885982,-1.42530937226928,26.4757693486689));
#19031=CARTESIAN_POINT('Ctrl Pts',(3.00219262680771,-1.17192445927172,26.4931785280334));
#19032=CARTESIAN_POINT('Ctrl Pts',(3.00984133775829,-1.15213830956013,26.4945227961182));
#19033=CARTESIAN_POINT('Ctrl Pts',(3.02028996461847,-1.12429479626733,26.4963918564774));
#19034=CARTESIAN_POINT('Ctrl Pts',(3.02325391467622,-1.11630015255855,26.4969259179949));
#19035=CARTESIAN_POINT('Ctrl Pts',(3.02798618761696,-1.10337872355117,26.4977848054628));
#19036=CARTESIAN_POINT('Ctrl Pts',(3.02977427220268,-1.09845929392863,26.4981107984835));
#19037=CARTESIAN_POINT('Ctrl Pts',(3.03350889949543,-1.08810598495214,26.4987947381134));
#19038=CARTESIAN_POINT('Ctrl Pts',(3.03545284031187,-1.08267120253822,26.4991525221424));
#19039=CARTESIAN_POINT('Ctrl Pts',(3.04016430873015,-1.06938665385681,26.5000241203941));
#19040=CARTESIAN_POINT('Ctrl Pts',(3.04291607167315,-1.06153126373979,26.5005369997594));
#19041=CARTESIAN_POINT('Ctrl Pts',(3.05266950472866,-1.03333879748522,26.5023689950491));
#19042=CARTESIAN_POINT('Ctrl Pts',(3.05949815986373,-1.0129418753169,26.5036782465789));
#19043=CARTESIAN_POINT('Ctrl Pts',(3.11626315913772,-0.837574239613999,
26.5148089846184));
#19044=CARTESIAN_POINT('Ctrl Pts',(3.15460002089174,-0.679072388780371,
26.5240365978845));
#19045=CARTESIAN_POINT('Ctrl Pts',(3.20859782668131,-0.347710788668034,
26.5428622399681));
#19046=CARTESIAN_POINT('Ctrl Pts',(3.2226268427006,-0.175138493841783,26.552424709566));
#19047=CARTESIAN_POINT('Ctrl Pts',(3.22274919271196,-0.0022810906157154,
26.5623024648959));
#19048=CARTESIAN_POINT('Ctrl Pts',(3.21940908233495,-0.00238856237501944,
26.5642265507269));
#19049=CARTESIAN_POINT('Ctrl Pts',(3.21459332503562,0.701948265465156,26.607604666478));
#19050=CARTESIAN_POINT('Ctrl Pts',(2.63997125700238,2.4901339051279,26.7172937616837));
#19051=CARTESIAN_POINT('Ctrl Pts',(-0.317098310746752,3.79898125969958,
26.8932938363438));
#19052=CARTESIAN_POINT('Ctrl Pts',(-3.36796503595531,1.78595113785612,27.0922267747072));
#19053=CARTESIAN_POINT('Ctrl Pts',(-3.32895242825944,-1.36033153994631,
27.2634778562151));
#19054=CARTESIAN_POINT('Ctrl Pts',(-2.03006326125809,-2.57117805515723,
27.3684179582684));
#19055=CARTESIAN_POINT('Ctrl Pts',(-1.47306432504222,-2.86105893806616,
27.4070470808673));
#19056=CARTESIAN_POINT('Origin',(0.,0.,4.68922655072688));
#19057=CARTESIAN_POINT('',(-1.4752555406476,-2.86526415052584,28.9026236394039));
#19058=CARTESIAN_POINT('',(-1.47525540425972,-2.86526422074867,28.6587956971472));
#19059=CARTESIAN_POINT('',(-1.47525540501186,-2.86526422036142,4.68922655072688));
#19060=CARTESIAN_POINT('Ctrl Pts',(-1.4752555406476,-2.86526415052584,28.9026236394039));
#19061=CARTESIAN_POINT('Ctrl Pts',(-1.56730140613998,-2.81787195004184,
28.8956334603849));
#19062=CARTESIAN_POINT('Ctrl Pts',(-1.6570868159356,-2.76603248162266,28.8886853090942));
#19063=CARTESIAN_POINT('Ctrl Pts',(-1.79111221064324,-2.6797640429632,28.8782617696498));
#19064=CARTESIAN_POINT('Ctrl Pts',(-1.83714954367225,-2.64841475594034,
28.8746717941389));
#19065=CARTESIAN_POINT('Ctrl Pts',(-1.89179829599422,-2.60909028932208,
28.8704203841509));
#19066=CARTESIAN_POINT('Ctrl Pts',(-1.90120547345437,-2.6022433952295,28.8696889263588));
#19067=CARTESIAN_POINT('Ctrl Pts',(-1.91580878973593,-2.59149309709788,
28.8685542953062));
#19068=CARTESIAN_POINT('Ctrl Pts',(-1.92103043799582,-2.58762475046121,
28.8681487615474));
#19069=CARTESIAN_POINT('Ctrl Pts',(-1.93071717602593,-2.58040305560169,
28.8673968270738));
#19070=CARTESIAN_POINT('Ctrl Pts',(-1.93518520739461,-2.57705392977,28.8670501514661));
#19071=CARTESIAN_POINT('Ctrl Pts',(-1.94530536430558,-2.56942694902911,
28.8662652570443));
#19072=CARTESIAN_POINT('Ctrl Pts',(-1.95095208179233,-2.56514205914806,
28.8658275405044));
#19073=CARTESIAN_POINT('Ctrl Pts',(-1.96769755226864,-2.5523478393405,28.8645300118211));
#19074=CARTESIAN_POINT('Ctrl Pts',(-1.97875527216978,-2.54378472742606,
28.8636738958671));
#19075=CARTESIAN_POINT('Ctrl Pts',(-2.06345495108211,-2.47730668540049,
28.8571185829835));
#19076=CARTESIAN_POINT('Ctrl Pts',(-2.13460316244975,-2.41627143657345,
28.8516254193862));
#19077=CARTESIAN_POINT('Ctrl Pts',(-2.37871511001782,-2.18764541868971,
28.8324119683121));
#19078=CARTESIAN_POINT('Ctrl Pts',(-2.53544491927282,-2.00389856810038,
28.8193174483597));
#19079=CARTESIAN_POINT('Ctrl Pts',(-2.72181609712744,-1.72809599534153,
28.8003685331252));
#19080=CARTESIAN_POINT('Ctrl Pts',(-2.7700805469508,-1.64962130828407,28.7950533843081));
#19081=CARTESIAN_POINT('Ctrl Pts',(-2.84226670632227,-1.52012918119093,
28.7863117256357));
#19082=CARTESIAN_POINT('Ctrl Pts',(-2.86832828819597,-1.47036220366954,
28.7829590202086));
#19083=CARTESIAN_POINT('Ctrl Pts',(-2.90064640220615,-1.40451533067834,
28.7785204167684));
#19084=CARTESIAN_POINT('Ctrl Pts',(-2.90809419787725,-1.38902879135833,
28.777476336685));
#19085=CARTESIAN_POINT('Ctrl Pts',(-2.92004322761825,-1.36366524788142,
28.7757657781034));
#19086=CARTESIAN_POINT('Ctrl Pts',(-2.92461910900727,-1.35382363035624,
28.7751019014415));
#19087=CARTESIAN_POINT('Ctrl Pts',(-2.93334958183195,-1.33479565505211,
28.7738179921341));
#19088=CARTESIAN_POINT('Ctrl Pts',(-2.937510955514,-1.32561253484125,28.7731982033091));
#19089=CARTESIAN_POINT('Ctrl Pts',(-2.9469776713719,-1.30445836206339,28.7717700239772));
#19090=CARTESIAN_POINT('Ctrl Pts',(-2.95225325622351,-1.29247426160268,
28.7709606216537));
#19091=CARTESIAN_POINT('Ctrl Pts',(-2.96615660276967,-1.26036191230788,
28.7687907457362));
#19092=CARTESIAN_POINT('Ctrl Pts',(-2.97465235863254,-1.24017758776531,
28.7674257962138));
#19093=CARTESIAN_POINT('Ctrl Pts',(-3.04479537790896,-1.06866267115801,
28.7558163348866));
#19094=CARTESIAN_POINT('Ctrl Pts',(-3.09504711095917,-0.912955425733579,
28.7451868192979));
#19095=CARTESIAN_POINT('Ctrl Pts',(-3.1925407174096,-0.50788733750899,28.7174020277814));
#19096=CARTESIAN_POINT('Ctrl Pts',(-3.22257121850819,-0.255529787699744,
28.6999213396051));
#19097=CARTESIAN_POINT('Ctrl Pts',(-3.22278954261968,0.0551348078913998,
28.6795855422955));
#19098=CARTESIAN_POINT('Ctrl Pts',(-3.2212963744716,0.112529628370398,28.6758822291109));
#19099=CARTESIAN_POINT('Ctrl Pts',(-3.21765197086125,0.181579560390752,
28.6715153401291));
#19100=CARTESIAN_POINT('Ctrl Pts',(-3.21696926498658,0.193297957757453,
28.6707773184156));
#19101=CARTESIAN_POINT('Ctrl Pts',(-3.21580771864204,0.211520213369535,
28.669634749598));
#19102=CARTESIAN_POINT('Ctrl Pts',(-3.2153731458202,0.21802664715179,28.6692277893272));
#19103=CARTESIAN_POINT('Ctrl Pts',(-3.21452994628046,0.230099851262853,
28.668474564397));
#19104=CARTESIAN_POINT('Ctrl Pts',(-3.21412660988983,0.235666827152145,
28.6681280163452));
#19105=CARTESIAN_POINT('Ctrl Pts',(-3.21318051955694,0.248270660596358,
28.6673451302571));
#19106=CARTESIAN_POINT('Ctrl Pts',(-3.2126291135446,0.255306782552613,28.6669092838105));
#19107=CARTESIAN_POINT('Ctrl Pts',(-3.2109278740279,0.276136434802271,28.6656224185816));
#19108=CARTESIAN_POINT('Ctrl Pts',(-3.20971227091084,0.289924639771291,
28.6647750065724));
#19109=CARTESIAN_POINT('Ctrl Pts',(-3.19998012148806,0.392737296411756,
28.6584864401568));
#19110=CARTESIAN_POINT('Ctrl Pts',(-3.18784924156409,0.481389369630846,
28.6532328483776));
#19111=CARTESIAN_POINT('Ctrl Pts',(-3.12855841077339,0.811672530400887,
28.6339160319763));
#19112=CARTESIAN_POINT('Ctrl Pts',(-3.05746574546789,1.04814477075452,28.6205467893947));
#19113=CARTESIAN_POINT('Ctrl Pts',(-2.92395360223317,1.35830442625515,28.6013191719088));
#19114=CARTESIAN_POINT('Ctrl Pts',(-2.88420043543491,1.44079197707685,28.596035050863));
#19115=CARTESIAN_POINT('Ctrl Pts',(-2.81459010734627,1.57077299908811,28.5873397767587));
#19116=CARTESIAN_POINT('Ctrl Pts',(-2.78690968122773,1.61937615903619,28.5840014068452));
#19117=CARTESIAN_POINT('Ctrl Pts',(-2.74910389112307,1.6819154957271,28.5795791462205));
#19118=CARTESIAN_POINT('Ctrl Pts',(-2.74011083716814,1.69652719438238,28.5785366833908));
#19119=CARTESIAN_POINT('Ctrl Pts',(-2.72524237199105,1.72025848188921,28.576828108941));
#19120=CARTESIAN_POINT('Ctrl Pts',(-2.71943675623714,1.72942156656025,28.5761645875254));
#19121=CARTESIAN_POINT('Ctrl Pts',(-2.70814500026648,1.74704605284769,28.5748808973243));
#19122=CARTESIAN_POINT('Ctrl Pts',(-2.70266518156472,1.75551136877768,28.5742609698417));
#19123=CARTESIAN_POINT('Ctrl Pts',(-2.68997140563666,1.77492062045923,28.5728317996216));
#19124=CARTESIAN_POINT('Ctrl Pts',(-2.68273026819452,1.78584648613132,28.5720215404742));
#19125=CARTESIAN_POINT('Ctrl Pts',(-2.66318747184001,1.81494674485511,28.5698478723153));
#19126=CARTESIAN_POINT('Ctrl Pts',(-2.6507666498961,1.83303991395204,28.5684799627496));
#19127=CARTESIAN_POINT('Ctrl Pts',(-2.54295203211013,1.9867037546689,28.556719018445));
#19128=CARTESIAN_POINT('Ctrl Pts',(-2.43742929097225,2.11483335468626,28.5459292616739));
#19129=CARTESIAN_POINT('Ctrl Pts',(-2.14305584948308,2.42083701885942,28.5175948048162));
#19130=CARTESIAN_POINT('Ctrl Pts',(-1.94175708752973,2.5850949708056,28.4997106673666));
#19131=CARTESIAN_POINT('Ctrl Pts',(-1.68057142571857,2.75033009865859,28.4795632837662));
#19132=CARTESIAN_POINT('Ctrl Pts',(-1.6375381045039,2.77616742812961,28.4763357359406));
#19133=CARTESIAN_POINT('Ctrl Pts',(-1.58411530609293,2.80656790781641,28.4724562387807));
#19134=CARTESIAN_POINT('Ctrl Pts',(-1.57428509144624,2.8120937366892,28.4717475595407));
#19135=CARTESIAN_POINT('Ctrl Pts',(-1.5588131888252,2.82068435302337,28.4706405081177));
#19136=CARTESIAN_POINT('Ctrl Pts',(-1.55319111532613,2.82378401051268,28.4702399543904));
#19137=CARTESIAN_POINT('Ctrl Pts',(-1.54265271608918,2.82955322543462,28.4694923950618));
#19138=CARTESIAN_POINT('Ctrl Pts',(-1.53773875762237,2.83222675150089,28.4691451445569));
#19139=CARTESIAN_POINT('Ctrl Pts',(-1.52648154739398,2.83831350147256,28.468352648757));
#19140=CARTESIAN_POINT('Ctrl Pts',(-1.52013380828977,2.8417182574009,28.4679079455588));
#19141=CARTESIAN_POINT('Ctrl Pts',(-1.50049836641492,2.85216555825527,28.4665388718724));
#19142=CARTESIAN_POINT('Ctrl Pts',(-1.48717251860614,2.85913651992215,28.4656189268024));
#19143=CARTESIAN_POINT('Ctrl Pts',(-1.34343909618597,2.93304894054213,28.4557895320587));
#19144=CARTESIAN_POINT('Ctrl Pts',(-1.20864005544456,2.99112108815557,28.4473884955365));
#19145=CARTESIAN_POINT('Ctrl Pts',(-0.900818392295055,3.09950702296103,
28.4289936604746));
#19146=CARTESIAN_POINT('Ctrl Pts',(-0.726604121829914,3.1449108959695,28.419089350069));
#19147=CARTESIAN_POINT('Ctrl Pts',(-0.419874762316938,3.19798873386393,
28.4014040101522));
#19148=CARTESIAN_POINT('Ctrl Pts',(-0.28899849413919,3.21246024709217,28.3937865778758));
#19149=CARTESIAN_POINT('Ctrl Pts',(-0.126422222750853,3.22042081285705,
28.384044698385));
#19150=CARTESIAN_POINT('Ctrl Pts',(-0.095211274930035,3.2214946064501,28.3821621965311));
#19151=CARTESIAN_POINT('Ctrl Pts',(-0.0502854838666851,3.22238682238048,
28.3794329076833));
#19152=CARTESIAN_POINT('Ctrl Pts',(-0.036579080523726,3.22257155462921,
28.378597613325));
#19153=CARTESIAN_POINT('Ctrl Pts',(-0.0127282929175396,3.22274082958144,
28.377139385869));
#19154=CARTESIAN_POINT('Ctrl Pts',(-0.00258431627414837,3.22276492808057,
28.3765177035535));
#19155=CARTESIAN_POINT('Ctrl Pts',(0.0169836838643136,3.22271902784754,
28.3753155339019));
#19156=CARTESIAN_POINT('Ctrl Pts',(0.0264076303351211,3.22265558383299,
28.3747352590598));
#19157=CARTESIAN_POINT('Ctrl Pts',(0.0487343638289391,3.22240733606204,
28.3733573387506));
#19158=CARTESIAN_POINT('Ctrl Pts',(0.0616365120751564,3.22218637113183,
28.372558564387));
#19159=CARTESIAN_POINT('Ctrl Pts',(0.107109419009939,3.22113437718066,28.3697343063039));
#19160=CARTESIAN_POINT('Ctrl Pts',(0.139667690023879,3.2198869411829,28.3676958127546));
#19161=CARTESIAN_POINT('Ctrl Pts',(0.465678489294179,3.20244235497597,28.3471136937416));
#19162=CARTESIAN_POINT('Ctrl Pts',(0.7555762000239,3.14666881789368,28.3272361943177));
#19163=CARTESIAN_POINT('Ctrl Pts',(1.0958761747199,3.03141307400087,28.302956158424));
#19164=CARTESIAN_POINT('Ctrl Pts',(1.15727564909789,3.00850850121993,28.2985442141292));
#19165=CARTESIAN_POINT('Ctrl Pts',(1.30100887108474,2.94983803926124,28.2881971643166));
#19166=CARTESIAN_POINT('Ctrl Pts',(1.38263763859029,2.91247055332315,28.2823054340372));
#19167=CARTESIAN_POINT('Ctrl Pts',(1.47971836405638,2.86302634781193,28.2753667317354));
#19168=CARTESIAN_POINT('Ctrl Pts',(1.496751822055,2.85415842771832,28.2741519597263));
#19169=CARTESIAN_POINT('Ctrl Pts',(1.52072866172942,2.8414019755943,28.2724468802679));
#19170=CARTESIAN_POINT('Ctrl Pts',(1.52773807629044,2.83763937507344,28.2719490097452));
#19171=CARTESIAN_POINT('Ctrl Pts',(1.53974883055604,2.83113468973272,28.2710970165854));
#19172=CARTESIAN_POINT('Ctrl Pts',(1.54475693186797,2.82840522486325,28.2707420984575));
#19173=CARTESIAN_POINT('Ctrl Pts',(1.55442210340478,2.82310428187572,28.2700578234322));
#19174=CARTESIAN_POINT('Ctrl Pts',(1.55908005719206,2.82053456602478,28.2697283534778));
#19175=CARTESIAN_POINT('Ctrl Pts',(1.57157123910579,2.81360299030571,28.2688455767616));
#19176=CARTESIAN_POINT('Ctrl Pts',(1.57939273289979,2.80921991777122,28.268293620265));
#19177=CARTESIAN_POINT('Ctrl Pts',(1.60802705950632,2.79301618882706,28.2662754953155));
#19178=CARTESIAN_POINT('Ctrl Pts',(1.62872691792977,2.78099607335252,28.2648216002393));
#19179=CARTESIAN_POINT('Ctrl Pts',(1.91319153093075,2.61154568013603,28.2448841753249));
#19180=CARTESIAN_POINT('Ctrl Pts',(2.15330288411082,2.41740014490797,28.2284434616139));
#19181=CARTESIAN_POINT('Ctrl Pts',(2.43075995837453,2.11840690419145,28.2053109327814));
#19182=CARTESIAN_POINT('Ctrl Pts',(2.49570619507922,2.04149209539067,28.1995259562613));
#19183=CARTESIAN_POINT('Ctrl Pts',(2.5933502967196,1.91421755332677,28.1900854965365));
#19184=CARTESIAN_POINT('Ctrl Pts',(2.62842539247341,1.86576361463846,28.1865202649179));
#19185=CARTESIAN_POINT('Ctrl Pts',(2.67203403547143,1.80184917202555,28.1818398975896));
#19186=CARTESIAN_POINT('Ctrl Pts',(2.68181850609958,1.78725370520843,28.1807725865446));
#19187=CARTESIAN_POINT('Ctrl Pts',(2.69749960686758,1.76344353274449,28.1790335109529));
#19188=CARTESIAN_POINT('Ctrl Pts',(2.70346962117239,1.754277408212,28.1783645175095));
#19189=CARTESIAN_POINT('Ctrl Pts',(2.714836822928,1.73662882238479,28.1770772848122));
#19190=CARTESIAN_POINT('Ctrl Pts',(2.7202412176886,1.72815113800746,28.1764593249424));
#19191=CARTESIAN_POINT('Ctrl Pts',(2.73249302874545,1.70873228020672,28.175044619613));
#19192=CARTESIAN_POINT('Ctrl Pts',(2.73931452811414,1.69777503393014,28.1742469248899));
#19193=CARTESIAN_POINT('Ctrl Pts',(2.75719866560456,1.66865969404883,28.1721286418673));
#19194=CARTESIAN_POINT('Ctrl Pts',(2.76814759469602,1.65043282660585,28.1708039061596));
#19195=CARTESIAN_POINT('Ctrl Pts',(2.84851180265212,1.51359965977129,28.1608673305479));
#19196=CARTESIAN_POINT('Ctrl Pts',(2.91044829388982,1.39078585238741,28.1519868885576));
#19197=CARTESIAN_POINT('Ctrl Pts',(3.07225266434821,1.01144220168224,28.1246958417585));
#19198=CARTESIAN_POINT('Ctrl Pts',(3.14731893748563,0.745733117929703,28.1056640971676));
#19199=CARTESIAN_POINT('Ctrl Pts',(3.19690835386103,0.412048353809459,28.0835228103653));
#19200=CARTESIAN_POINT('Ctrl Pts',(3.2042839568045,0.350103425478123,28.0794907410019));
#19201=CARTESIAN_POINT('Ctrl Pts',(3.21093134597867,0.276010592693664,28.07479091633));
#19202=CARTESIAN_POINT('Ctrl Pts',(3.21193818098715,0.264036149225777,28.0740351806047));
#19203=CARTESIAN_POINT('Ctrl Pts',(3.21339276254581,0.245495068481021,28.0728712131674));
#19204=CARTESIAN_POINT('Ctrl Pts',(3.21388739670759,0.238932371501747,28.0724604236894));
#19205=CARTESIAN_POINT('Ctrl Pts',(3.21476401304575,0.226806086757986,28.0717036611553));
#19206=CARTESIAN_POINT('Ctrl Pts',(3.21515165535152,0.221243066530169,28.07135738207));
#19207=CARTESIAN_POINT('Ctrl Pts',(3.21599195248036,0.20871520250622,28.0705795532071));
#19208=CARTESIAN_POINT('Ctrl Pts',(3.21643642170772,0.201749898277124,28.0701484677452));
#19209=CARTESIAN_POINT('Ctrl Pts',(3.21751758941432,0.183894330845261,28.0690467792619));
#19210=CARTESIAN_POINT('Ctrl Pts',(3.21812163422095,0.173002076138211,28.0683779668696));
#19211=CARTESIAN_POINT('Ctrl Pts',(3.22136408164091,0.108622479298039,28.064442927649));
#19212=CARTESIAN_POINT('Ctrl Pts',(3.22272444204836,0.0550756954540183,
28.0612435129122));
#19213=CARTESIAN_POINT('Ctrl Pts',(3.2228698137111,-0.253878048904672,28.0430802842878));
#19214=CARTESIAN_POINT('Ctrl Pts',(3.19263149051261,-0.508405650129438,
28.0292239853636));
#19215=CARTESIAN_POINT('Ctrl Pts',(3.09404473860994,-0.916536046534449,
28.0055111022969));
#19216=CARTESIAN_POINT('Ctrl Pts',(3.04326992817971,-1.07314900636673,27.9960381728304));
#19217=CARTESIAN_POINT('Ctrl Pts',(2.97244162849883,-1.24546730509061,27.9848325130077));
#19218=CARTESIAN_POINT('Ctrl Pts',(2.9639018875871,-1.26565540621398,27.9835073693319));
#19219=CARTESIAN_POINT('Ctrl Pts',(2.94993064919438,-1.29776667241523,27.9813791001097));
#19220=CARTESIAN_POINT('Ctrl Pts',(2.94463113864726,-1.30974677722233,27.9805804831155));
#19221=CARTESIAN_POINT('Ctrl Pts',(2.9351236271155,-1.33089012412469,27.9791627203008));
#19222=CARTESIAN_POINT('Ctrl Pts',(2.93094536261163,-1.34006660530723,27.9785446050068));
#19223=CARTESIAN_POINT('Ctrl Pts',(2.92218138179114,-1.35907736154886,27.9772581960992));
#19224=CARTESIAN_POINT('Ctrl Pts',(2.91758892960006,-1.36890837386063,27.9765896751037));
#19225=CARTESIAN_POINT('Ctrl Pts',(2.90560043784443,-1.3942376243295,27.9748586632506));
#19226=CARTESIAN_POINT('Ctrl Pts',(2.89813008746458,-1.40970012244849,27.9737935958398));
#19227=CARTESIAN_POINT('Ctrl Pts',(2.86574534841454,-1.47538614238162,27.9692328019503));
#19228=CARTESIAN_POINT('Ctrl Pts',(2.8396475232972,-1.52501212372549,27.9656957978354));
#19229=CARTESIAN_POINT('Ctrl Pts',(2.76741372445882,-1.65407819803234,27.9562467089573));
#19230=CARTESIAN_POINT('Ctrl Pts',(2.71915542877751,-1.73226575513604,27.9502631335601));
#19231=CARTESIAN_POINT('Ctrl Pts',(2.53104417150926,-2.00977294184958,27.92808564831));
#19232=CARTESIAN_POINT('Ctrl Pts',(2.37208730220164,-2.19512155269858,27.9113411980645));
#19233=CARTESIAN_POINT('Ctrl Pts',(2.12673200897618,-2.42311969521352,27.8890616081365));
#19234=CARTESIAN_POINT('Ctrl Pts',(2.05703928030839,-2.48255732361178,27.8830701511568));
#19235=CARTESIAN_POINT('Ctrl Pts',(1.97394111242947,-2.54752186798342,27.8763891156045));
#19236=CARTESIAN_POINT('Ctrl Pts',(1.96292313737278,-2.55602111814378,27.8755122645675));
#19237=CARTESIAN_POINT('Ctrl Pts',(1.94622176959726,-2.56873284278501,27.8741970362539));
#19238=CARTESIAN_POINT('Ctrl Pts',(1.94057915915971,-2.57299827504003,27.8737550563143));
#19239=CARTESIAN_POINT('Ctrl Pts',(1.93045794271807,-2.58059699701065,27.8729665785583));
#19240=CARTESIAN_POINT('Ctrl Pts',(1.92598469257059,-2.58393724674888,27.872619596667));
#19241=CARTESIAN_POINT('Ctrl Pts',(1.91627694861952,-2.59114696404619,27.8718698360079));
#19242=CARTESIAN_POINT('Ctrl Pts',(1.91103942048759,-2.59501219037771,27.8714673526652));
#19243=CARTESIAN_POINT('Ctrl Pts',(1.89636739487758,-2.60577144069221,27.8703454103461));
#19244=CARTESIAN_POINT('Ctrl Pts',(1.88690694838235,-2.61263014515534,27.8696283657912));
#19245=CARTESIAN_POINT('Ctrl Pts',(1.83147959453778,-2.65235616708054,27.865463043079));
#19246=CARTESIAN_POINT('Ctrl Pts',(1.78468879618386,-2.68406362557993,27.8620893546808));
#19247=CARTESIAN_POINT('Ctrl Pts',(1.52323049267443,-2.85137654975856,27.8438650317798));
#19248=CARTESIAN_POINT('Ctrl Pts',(1.29393408151033,-2.96248899890195,27.8300867796373));
#19249=CARTESIAN_POINT('Ctrl Pts',(0.899230482662645,-3.09908172474494,
27.8064939488572));
#19250=CARTESIAN_POINT('Ctrl Pts',(0.740674528355421,-3.14075051844045,
27.7970590206089));
#19251=CARTESIAN_POINT('Ctrl Pts',(0.558103498970576,-3.1741326246658,27.7858958758337));
#19252=CARTESIAN_POINT('Ctrl Pts',(0.536515574185392,-3.17785280289918,
27.7845715598268));
#19253=CARTESIAN_POINT('Ctrl Pts',(0.501964126384027,-3.1834448449483,27.7824443689563));
#19254=CARTESIAN_POINT('Ctrl Pts',(0.489023971128397,-3.18545830497288,
27.7816459953445));
#19255=CARTESIAN_POINT('Ctrl Pts',(0.466100322918885,-3.18888220307942,
27.7802285141865));
#19256=CARTESIAN_POINT('Ctrl Pts',(0.456121751412183,-3.19032477349268,
27.7796104358032));
#19257=CARTESIAN_POINT('Ctrl Pts',(0.435388575861488,-3.19322284361722,
27.778323953687));
#19258=CARTESIAN_POINT('Ctrl Pts',(0.424633074340968,-3.19467088892615,
27.7776553218265));
#19259=CARTESIAN_POINT('Ctrl Pts',(0.396832323636302,-3.19827091397259,
27.7759237003514));
#19260=CARTESIAN_POINT('Ctrl Pts',(0.379776981062006,-3.20034094409897,
27.7748581307385));
#19261=CARTESIAN_POINT('Ctrl Pts',(0.306926621458607,-3.20859235250207,
27.7702922722666));
#19262=CARTESIAN_POINT('Ctrl Pts',(0.250994584633007,-3.21345140223122,
27.7667505916761));
#19263=CARTESIAN_POINT('Ctrl Pts',(0.103121815996642,-3.22241368507305,
27.7572858358354));
#19264=CARTESIAN_POINT('Ctrl Pts',(0.0110880832878357,-3.22404382618611,
27.7512909748323));
#19265=CARTESIAN_POINT('Ctrl Pts',(-0.322511287510997,-3.21566869440334,
27.7292143150351));
#19266=CARTESIAN_POINT('Ctrl Pts',(-0.562664986094939,-3.18244119714941,
27.712592776094));
#19267=CARTESIAN_POINT('Ctrl Pts',(-0.886877231683784,-3.09970995953979,
27.6903242884185));
#19268=CARTESIAN_POINT('Ctrl Pts',(-0.975892956717132,-3.07284713220161,
27.6842392585968));
#19269=CARTESIAN_POINT('Ctrl Pts',(-1.07680962772249,-3.03756374251452,
27.6774673688189));
#19270=CARTESIAN_POINT('Ctrl Pts',(-1.08995829745498,-3.03287048694802,
27.6765875863793));
#19271=CARTESIAN_POINT('Ctrl Pts',(-1.10973159759125,-3.02566744934744,
27.6752688339925));
#19272=CARTESIAN_POINT('Ctrl Pts',(-1.11637892962338,-3.02322110016826,
27.6748262332957));
#19273=CARTESIAN_POINT('Ctrl Pts',(-1.12825175385037,-3.01880716805993,
27.674037085855));
#19274=CARTESIAN_POINT('Ctrl Pts',(-1.13348023036993,-3.01684790914915,
27.6736900515636));
#19275=CARTESIAN_POINT('Ctrl Pts',(-1.14478644820545,-3.01257760535221,
27.6729406750253));
#19276=CARTESIAN_POINT('Ctrl Pts',(-1.15086227722091,-3.01026175953171,
27.6725386255255));
#19277=CARTESIAN_POINT('Ctrl Pts',(-1.1678065109035,-3.00374454423159,27.6714191174302));
#19278=CARTESIAN_POINT('Ctrl Pts',(-1.17865933057876,-2.99950254642598,
27.6707040563288));
#19279=CARTESIAN_POINT('Ctrl Pts',(-1.24150512116496,-2.97454450017287,
27.6665735563675));
#19280=CARTESIAN_POINT('Ctrl Pts',(-1.29297790424187,-2.95253432964939,
27.6632312580994));
#19281=CARTESIAN_POINT('Ctrl Pts',(-1.3881557296679,-2.90886866196291,27.6570810831785));
#19282=CARTESIAN_POINT('Ctrl Pts',(-1.43196670842019,-2.8875525283001,27.6542624077881));
#19283=CARTESIAN_POINT('Ctrl Pts',(-1.47525554463427,-2.8652641484732,27.6514736540563));
#19284=CARTESIAN_POINT('',(3.21884143381304,0.00209368326018609,27.8142265507269));
#19285=CARTESIAN_POINT('Ctrl Pts',(-1.47306432504222,-2.86105893806616,
27.4070470808673));
#19286=CARTESIAN_POINT('Ctrl Pts',(-1.07391560553436,-3.06878928672532,
27.4347289377229));
#19287=CARTESIAN_POINT('Ctrl Pts',(0.418901930152219,-3.50240078110557,
27.528721774033));
#19288=CARTESIAN_POINT('Ctrl Pts',(2.67358561891793,-2.43681984067852,27.6644482639862));
#19289=CARTESIAN_POINT('Ctrl Pts',(3.21482490205533,-0.675841793750365,
27.7724928970838));
#19290=CARTESIAN_POINT('Ctrl Pts',(3.21884143381304,0.00209368326018609,
27.8142265507269));
#19291=CARTESIAN_POINT('Ctrl Pts',(3.22274921939152,0.00224308077548155,
27.8119771806639));
#19292=CARTESIAN_POINT('Ctrl Pts',(3.22257607314387,0.251011177117484,27.8282186241532));
#19293=CARTESIAN_POINT('Ctrl Pts',(3.1935980450414,0.498915594153727,27.8452516809599));
#19294=CARTESIAN_POINT('Ctrl Pts',(3.11031910459803,0.851415556667762,27.8695745293279));
#19295=CARTESIAN_POINT('Ctrl Pts',(3.07841230804907,0.960404269788171,27.8770937384884));
#19296=CARTESIAN_POINT('Ctrl Pts',(3.03363325978313,1.08796018786871,27.8857242084574));
#19297=CARTESIAN_POINT('Ctrl Pts',(3.02624122259666,1.10835565049853,27.8870987860038));
#19298=CARTESIAN_POINT('Ctrl Pts',(3.01571870519125,1.13649813074565,27.8889864768415));
#19299=CARTESIAN_POINT('Ctrl Pts',(3.01276339773523,1.14430940876292,27.889509460113));
#19300=CARTESIAN_POINT('Ctrl Pts',(3.0077122949801,1.15750494297383,27.8903911848325));
#19301=CARTESIAN_POINT('Ctrl Pts',(3.00563233826743,1.16289517639047,27.8907508647554));
#19302=CARTESIAN_POINT('Ctrl Pts',(3.00164236546227,1.17315302199276,27.8914343676146));
#19303=CARTESIAN_POINT('Ctrl Pts',(2.9997349884051,1.17802160566625,27.891758351038));
#19304=CARTESIAN_POINT('Ctrl Pts',(2.99469697702712,1.19078956082788,27.892606951605));
#19305=CARTESIAN_POINT('Ctrl Pts',(2.99154691090777,1.19868129462142,27.8931304028289));
#19306=CARTESIAN_POINT('Ctrl Pts',(2.98048912814422,1.22606881118217,27.8949436094309));
#19307=CARTESIAN_POINT('Ctrl Pts',(2.97242155166803,1.24550003840723,27.8962240925894));
#19308=CARTESIAN_POINT('Ctrl Pts',(2.86462766411943,1.49811370527821,27.9128101040785));
#19309=CARTESIAN_POINT('Ctrl Pts',(2.73788882694887,1.71884910249097,27.9266727029701));
#19310=CARTESIAN_POINT('Ctrl Pts',(2.51225204886022,2.02242967384565,27.9478690919664));
#19311=CARTESIAN_POINT('Ctrl Pts',(2.43222102155652,2.11800137929118,27.9549062916998));
#19312=CARTESIAN_POINT('Ctrl Pts',(2.30689457976131,2.25116777397641,27.9655186265763));
#19313=CARTESIAN_POINT('Ctrl Pts',(2.26578064690093,2.29254365810444,27.9689420244304));
#19314=CARTESIAN_POINT('Ctrl Pts',(2.20402952564179,2.35140384540231,27.9740190152276));
#19315=CARTESIAN_POINT('Ctrl Pts',(2.18425782009189,2.36978140426878,27.9756352945981));
#19316=CARTESIAN_POINT('Ctrl Pts',(2.14826715620852,2.40240120467486,27.978562607641));
#19317=CARTESIAN_POINT('Ctrl Pts',(2.13213141452947,2.41673310874959,27.9798698062973));
#19318=CARTESIAN_POINT('Ctrl Pts',(2.10697029466606,2.43863331107665,27.981900827569));
#19319=CARTESIAN_POINT('Ctrl Pts',(2.09804512935101,2.44631618518651,27.9826198682644));
#19320=CARTESIAN_POINT('Ctrl Pts',(2.08899527053964,2.45402044286706,27.9833476023839));
#19321=CARTESIAN_POINT('Ctrl Pts',(2.08891239022315,2.45409099267298,27.9833542669965));
#19322=CARTESIAN_POINT('Ctrl Pts',(2.08874529176614,2.4542332164761,27.9833677035697));
#19323=CARTESIAN_POINT('Ctrl Pts',(2.08866107351799,2.45430489033056,27.9833744755353));
#19324=CARTESIAN_POINT('Ctrl Pts',(2.08849125527679,2.45444939890083,27.9833881303352));
#19325=CARTESIAN_POINT('Ctrl Pts',(2.08840565516912,2.45452223346824,27.9833950131749));
#19326=CARTESIAN_POINT('Ctrl Pts',(2.08823302754129,2.45466910157774,27.9834088933833));
#19327=CARTESIAN_POINT('Ctrl Pts',(2.08814599989535,2.45474313496867,27.9834158907581));
#19328=CARTESIAN_POINT('Ctrl Pts',(2.08797046964609,2.45489244039011,27.9834300038475));
#19329=CARTESIAN_POINT('Ctrl Pts',(2.08788196692128,2.45496771225276,27.9834371195675));
#19330=CARTESIAN_POINT('Ctrl Pts',(2.08770343710085,2.45511953582353,27.9834514733073));
#19331=CARTESIAN_POINT('Ctrl Pts',(2.08761340984913,2.4551960873794,27.9834587113353));
#19332=CARTESIAN_POINT('Ctrl Pts',(2.08746200265783,2.45532481689282,27.9834708839738));
#19333=CARTESIAN_POINT('Ctrl Pts',(2.08740062496582,2.45537699750615,27.9834758184754));
#19334=CARTESIAN_POINT('Ctrl Pts',(2.08727283071188,2.45548563430343,27.9834860924525));
#19335=CARTESIAN_POINT('Ctrl Pts',(2.08720641383123,2.45554209008118,27.983491431943));
#19336=CARTESIAN_POINT('Ctrl Pts',(2.08706807579079,2.45565967072472,27.9835025532808));
#19337=CARTESIAN_POINT('Ctrl Pts',(2.08699615423903,2.45572079512318,27.9835083351472));
#19338=CARTESIAN_POINT('Ctrl Pts',(2.08684629011748,2.45584814969989,27.9835203827395));
#19339=CARTESIAN_POINT('Ctrl Pts',(2.08676834707553,2.45591437933108,27.9835266484884));
#19340=CARTESIAN_POINT('Ctrl Pts',(2.08660586485907,2.45605243012866,27.9835397100328));
#19341=CARTESIAN_POINT('Ctrl Pts',(2.08652132514239,2.45612425062967,27.9835465058541));
#19342=CARTESIAN_POINT('Ctrl Pts',(2.08634500801427,2.45627402472399,27.9835606790614));
#19343=CARTESIAN_POINT('Ctrl Pts',(2.08625322993715,2.45635197754244,27.9835680564799));
#19344=CARTESIAN_POINT('Ctrl Pts',(2.08606171846324,2.45651462165027,27.9835834505016));
#19345=CARTESIAN_POINT('Ctrl Pts',(2.08596198426455,2.45659931202109,27.9835914671443));
#19346=CARTESIAN_POINT('Ctrl Pts',(2.0857537555314,2.45677610987276,27.9836082042443));
#19347=CARTESIAN_POINT('Ctrl Pts',(2.08564526007494,2.45686821622198,27.9836169247457));
#19348=CARTESIAN_POINT('Ctrl Pts',(2.08541860331951,2.45706060882681,27.9836351422523));
#19349=CARTESIAN_POINT('Ctrl Pts',(2.08530044088219,2.45716089375034,27.9836446393129));
#19350=CARTESIAN_POINT('Ctrl Pts',(2.08505342827,2.45737050367132,27.9836644919592));
#19351=CARTESIAN_POINT('Ctrl Pts',(2.08492457674086,2.45747982704971,27.9836748476105));
#19352=CARTESIAN_POINT('Ctrl Pts',(2.08465502725945,2.45770848838087,27.9836965104265));
#19353=CARTESIAN_POINT('Ctrl Pts',(2.08451432765261,2.45782782438952,27.9837078176721));
#19354=CARTESIAN_POINT('Ctrl Pts',(2.08421977720324,2.45807760729837,27.9837314883751));
#19355=CARTESIAN_POINT('Ctrl Pts',(2.08406591899574,2.45820805638353,27.983743852361));
#19356=CARTESIAN_POINT('Ctrl Pts',(2.08374354384588,2.45848133097957,27.9837697574909));
#19357=CARTESIAN_POINT('Ctrl Pts',(2.08357502609899,2.45862415222707,27.983783298622));
#19358=CARTESIAN_POINT('Ctrl Pts',(2.08327991972498,2.45887420704946,27.9838070108846));
#19359=CARTESIAN_POINT('Ctrl Pts',(2.08315334029556,2.45898144581048,27.9838171814793));
#19360=CARTESIAN_POINT('Ctrl Pts',(2.08282680123457,2.45925804811655,27.9838434180564));
#19361=CARTESIAN_POINT('Ctrl Pts',(2.08262683195259,2.4594273947406,27.9838594844227));
#19362=CARTESIAN_POINT('Ctrl Pts',(2.08210727006256,2.4598672837748,27.9839012264972));
#19363=CARTESIAN_POINT('Ctrl Pts',(2.08178764721452,2.46013778673742,27.9839269036214));
#19364=CARTESIAN_POINT('Ctrl Pts',(2.07377182236681,2.46691905276118,27.98457081878));
#19365=CARTESIAN_POINT('Ctrl Pts',(2.06604523529416,2.47339367391275,27.9851905356148));
#19366=CARTESIAN_POINT('Ctrl Pts',(2.04820544090066,2.48820090474618,27.9866192548276));
#19367=CARTESIAN_POINT('Ctrl Pts',(2.03807158744352,2.49650825490682,27.9874292731499));
#19368=CARTESIAN_POINT('Ctrl Pts',(2.01083480395291,2.51855957954558,27.9896023672832));
#19369=CARTESIAN_POINT('Ctrl Pts',(1.99364194249327,2.53219089548667,27.9909699417642));
#19370=CARTESIAN_POINT('Ctrl Pts',(1.84747586323729,2.64566692077758,28.0025635483795));
#19371=CARTESIAN_POINT('Ctrl Pts',(1.71125339721264,2.73574813183232,28.0131730544195));
#19372=CARTESIAN_POINT('Ctrl Pts',(1.34819853107613,2.93807203849513,28.0408887938268));
#19373=CARTESIAN_POINT('Ctrl Pts',(1.11390373337955,3.03465317275966,28.0583184593761));
#19374=CARTESIAN_POINT('Ctrl Pts',(0.814657340601489,3.11862857407769,28.0786729404069));
#19375=CARTESIAN_POINT('Ctrl Pts',(0.758151901353665,3.1328449477799,28.0824325500714));
#19376=CARTESIAN_POINT('Ctrl Pts',(0.689785591019008,3.14808708364392,28.0868564777877));
#19377=CARTESIAN_POINT('Ctrl Pts',(0.678268845443517,3.15058848966412,28.0875974892631));
#19378=CARTESIAN_POINT('Ctrl Pts',(0.660350015807509,3.15437760197879,28.0887435853003));
#19379=CARTESIAN_POINT('Ctrl Pts',(0.653957443689285,3.15570909034423,28.0891511076388));
#19380=CARTESIAN_POINT('Ctrl Pts',(0.642095993973149,3.15814208319243,28.0899047102472));
#19381=CARTESIAN_POINT('Ctrl Pts',(0.636628352748044,3.15924880696951,28.09025107791));
#19382=CARTESIAN_POINT('Ctrl Pts',(0.624253987844057,3.16172011471793,28.0910327101437));
#19383=CARTESIAN_POINT('Ctrl Pts',(0.61734566776465,3.16307626431387,28.0914674886988));
#19384=CARTESIAN_POINT('Ctrl Pts',(0.59691599291627,3.1670172663204,28.0927486971762));
#19385=CARTESIAN_POINT('Ctrl Pts',(0.583382255670844,3.16953817254749,28.0935915660775));
#19386=CARTESIAN_POINT('Ctrl Pts',(0.483748943329586,3.18743690988595,28.0997562607256));
#19387=CARTESIAN_POINT('Ctrl Pts',(0.397062934537069,3.19939229983461,28.1048987659791));
#19388=CARTESIAN_POINT('Ctrl Pts',(0.0623539005114043,3.23173728192384,
28.1242752762209));
#19389=CARTESIAN_POINT('Ctrl Pts',(-0.187229242884563,3.22691404424233,
28.1377811631889));
#19390=CARTESIAN_POINT('Ctrl Pts',(-0.524118949688076,3.18115193908655,
28.1571436545183));
#19391=CARTESIAN_POINT('Ctrl Pts',(-0.613885474878969,3.16505467031161,
28.1624074400635));
#19392=CARTESIAN_POINT('Ctrl Pts',(-0.757263198003658,3.13301441173895,
28.1710720742139));
#19393=CARTESIAN_POINT('Ctrl Pts',(-0.811354530415077,3.11944387908896,
28.1744007979795));
#19394=CARTESIAN_POINT('Ctrl Pts',(-0.881570880155421,3.09987805720281,
28.1788118352579));
#19395=CARTESIAN_POINT('Ctrl Pts',(-0.898040275123139,3.09514698082008,
28.1798529804518));
#19396=CARTESIAN_POINT('Ctrl Pts',(-0.924865532663639,3.08720890426697,
28.1815597870033));
#19397=CARTESIAN_POINT('Ctrl Pts',(-0.935244463482718,3.08408055359756,
28.182222866838));
#19398=CARTESIAN_POINT('Ctrl Pts',(-0.955245465200354,3.07794173248781,
28.1835059776897));
#19399=CARTESIAN_POINT('Ctrl Pts',(-0.964869592864692,3.07493835262666,
28.1841257690598));
#19400=CARTESIAN_POINT('Ctrl Pts',(-0.986976702521,3.06792543115246,28.185555019243));
#19401=CARTESIAN_POINT('Ctrl Pts',(-0.999449561716827,3.06388479350141,
28.1863654964604));
#19402=CARTESIAN_POINT('Ctrl Pts',(-1.03275239016484,3.05287120065304,28.1885406226128));
#19403=CARTESIAN_POINT('Ctrl Pts',(-1.05353601949692,3.04576129796855,28.1899097834372));
#19404=CARTESIAN_POINT('Ctrl Pts',(-1.22782880847757,2.98413981823065,28.2014924303112));
#19405=CARTESIAN_POINT('Ctrl Pts',(-1.37705056332874,2.91828225952964,28.2120883586319));
#19406=CARTESIAN_POINT('Ctrl Pts',(-1.74306767766489,2.72240289107818,28.2397703227242));
#19407=CARTESIAN_POINT('Ctrl Pts',(-1.95073956424826,2.577668002044,28.2571794558204));
#19408=CARTESIAN_POINT('Ctrl Pts',(-2.18326933659519,2.37126396516293,28.2775460223032));
#19409=CARTESIAN_POINT('Ctrl Pts',(-2.22606677235845,2.33113396004733,28.2813322407518));
#19410=CARTESIAN_POINT('Ctrl Pts',(-2.27613796553347,2.28154617693156,28.2857831833612));
#19411=CARTESIAN_POINT('Ctrl Pts',(-2.28448243609273,2.27319093016324,28.2865256720649));
#19412=CARTESIAN_POINT('Ctrl Pts',(-2.29737323038721,2.26014081540648,28.2876735533898));
#19413=CARTESIAN_POINT('Ctrl Pts',(-2.30195141261688,2.25547776777263,28.2880813957598));
#19414=CARTESIAN_POINT('Ctrl Pts',(-2.31041124451165,2.246808527487,28.2888352916699));
#19415=CARTESIAN_POINT('Ctrl Pts',(-2.31429664178473,2.24280621823188,28.2891816344996));
#19416=CARTESIAN_POINT('Ctrl Pts',(-2.32305771646215,2.23373451359271,28.2899628333745));
#19417=CARTESIAN_POINT('Ctrl Pts',(-2.32792718908079,2.22865924622503,28.2903972057273));
#19418=CARTESIAN_POINT('Ctrl Pts',(-2.34225664283052,2.21362599170567,28.2916761079214));
#19419=CARTESIAN_POINT('Ctrl Pts',(-2.35166976523652,2.20362327608519,28.2925170958168));
#19420=CARTESIAN_POINT('Ctrl Pts',(-2.41998729411171,2.13009032611836,28.2986298395416));
#19421=CARTESIAN_POINT('Ctrl Pts',(-2.47637824169873,2.06426185303856,28.3037256803751));
#19422=CARTESIAN_POINT('Ctrl Pts',(-2.68662498248649,1.79779252691876,28.3232922850509));
#19423=CARTESIAN_POINT('Ctrl Pts',(-2.81931375597962,1.58161236519609,28.3370021425064));
#19424=CARTESIAN_POINT('Ctrl Pts',(-2.96278569365995,1.27120688746138,28.356495879952));
#19425=CARTESIAN_POINT('Ctrl Pts',(-2.99681444426538,1.18876718280264,28.3616484392442));
#19426=CARTESIAN_POINT('Ctrl Pts',(-3.04619657884746,1.05347774459922,28.3701464831773));
#19427=CARTESIAN_POINT('Ctrl Pts',(-3.06369206125675,1.00145862039529,28.3734234203789));
#19428=CARTESIAN_POINT('Ctrl Pts',(-3.08486723836728,0.932738945623363,
28.377775370779));
#19429=CARTESIAN_POINT('Ctrl Pts',(-3.08975492775471,0.916418184076646,
28.3788106042556));
#19430=CARTESIAN_POINT('Ctrl Pts',(-3.0975343353287,0.889671649575213,28.3805101598316));
#19431=CARTESIAN_POINT('Ctrl Pts',(-3.10050340540402,0.879268577376793,
28.3811719427035));
#19432=CARTESIAN_POINT('Ctrl Pts',(-3.10614027082547,0.859134441693939,
28.3824542709243));
#19433=CARTESIAN_POINT('Ctrl Pts',(-3.10881486019964,0.849405399237961,
28.3830745858877));
#19434=CARTESIAN_POINT('Ctrl Pts',(-3.11487295958612,0.826956617192837,
28.384507536301));
#19435=CARTESIAN_POINT('Ctrl Pts',(-3.11822430483926,0.814228455365824,
28.3853212072951));
#19436=CARTESIAN_POINT('Ctrl Pts',(-3.12700390657879,0.780034843515834,
28.3875104938558));
#19437=CARTESIAN_POINT('Ctrl Pts',(-3.13228900254007,0.758533686731404,
28.3888907139592));
#19438=CARTESIAN_POINT('Ctrl Pts',(-3.18770001294623,0.522646962907515,
28.4040745982243));
#19439=CARTESIAN_POINT('Ctrl Pts',(-3.21594261043893,0.303760319097149,
28.418601064146));
#19440=CARTESIAN_POINT('Ctrl Pts',(-3.22573092070898,-0.0727969716174191,
28.444009805387));
#19441=CARTESIAN_POINT('Ctrl Pts',(-3.2183852464577,-0.229428189198327,
28.4546842291684));
#19442=CARTESIAN_POINT('Ctrl Pts',(-3.19207297921126,-0.448158922934147,
28.469345485301));
#19443=CARTESIAN_POINT('Ctrl Pts',(-3.18258959060561,-0.51117594651035,
28.4735385197517));
#19444=CARTESIAN_POINT('Ctrl Pts',(-3.16696442362315,-0.59752103879161,
28.4792060028004));
#19445=CARTESIAN_POINT('Ctrl Pts',(-3.16242072979904,-0.621120161174069,
28.4807468889327));
#19446=CARTESIAN_POINT('Ctrl Pts',(-3.15412308036939,-0.661762490831342,
28.4833840558576));
#19447=CARTESIAN_POINT('Ctrl Pts',(-3.15049394862088,-0.6788298107568,28.4844864423929));
#19448=CARTESIAN_POINT('Ctrl Pts',(-3.1450742742891,-0.70333769149491,28.4860612957598));
#19449=CARTESIAN_POINT('Ctrl Pts',(-3.14339564384017,-0.71080231303224,
28.4865398776583));
#19450=CARTESIAN_POINT('Ctrl Pts',(-3.14043101691081,-0.72376966104113,
28.4873692801408));
#19451=CARTESIAN_POINT('Ctrl Pts',(-3.13915710809486,-0.729275083153306,
28.4877207888519));
#19452=CARTESIAN_POINT('Ctrl Pts',(-3.13646068134632,-0.740790182765554,
28.4884546681015));
#19453=CARTESIAN_POINT('Ctrl Pts',(-3.13503536907279,-0.746799127407396,
28.4888368753577));
#19454=CARTESIAN_POINT('Ctrl Pts',(-3.13121430848532,-0.762704526290787,
28.4898466509665));
#19455=CARTESIAN_POINT('Ctrl Pts',(-3.1287888932895,-0.772593882862759,
28.4904725291888));
#19456=CARTESIAN_POINT('Ctrl Pts',(-3.11831393122708,-0.814445935150837,
28.4931135910754));
#19457=CARTESIAN_POINT('Ctrl Pts',(-3.10982083949059,-0.846296931862167,
28.4951045430408));
#19458=CARTESIAN_POINT('Ctrl Pts',(-3.00932650970986,-1.20120819765783,
28.5171336328838));
#19459=CARTESIAN_POINT('Ctrl Pts',(-2.86783908636949,-1.50815085994854,
28.5349257467128));
#19460=CARTESIAN_POINT('Ctrl Pts',(-2.61859242532193,-1.88200172304735,
28.5607348492581));
#19461=CARTESIAN_POINT('Ctrl Pts',(-2.55081475842756,-1.9728904394345,28.5673737263348));
#19462=CARTESIAN_POINT('Ctrl Pts',(-2.46473523618494,-2.07645240823694,
28.5754924658662));
#19463=CARTESIAN_POINT('Ctrl Pts',(-2.45091016842202,-2.0927526610991,28.5767874914401));
#19464=CARTESIAN_POINT('Ctrl Pts',(-2.42922117196581,-2.11781505994916,
28.5788061063841));
#19465=CARTESIAN_POINT('Ctrl Pts',(-2.42146947602971,-2.12667385871358,
28.5795250407584));
#19466=CARTESIAN_POINT('Ctrl Pts',(-2.4077331227778,-2.14219957808712,28.5807947102052));
#19467=CARTESIAN_POINT('Ctrl Pts',(-2.40176884148812,-2.1488844204272,28.5813445862375));
#19468=CARTESIAN_POINT('Ctrl Pts',(-2.38809389098022,-2.16408342609565,
28.5826021947668));
#19469=CARTESIAN_POINT('Ctrl Pts',(-2.38036545228784,-2.17258137139112,
28.583310676397));
#19470=CARTESIAN_POINT('Ctrl Pts',(-2.35936430081158,-2.19542699191894,
28.5852299433384));
#19471=CARTESIAN_POINT('Ctrl Pts',(-2.34600638830898,-2.20969535901384,
28.5864443664798));
#19472=CARTESIAN_POINT('Ctrl Pts',(-2.28121362315127,-2.2776545333578,28.5923056407815));
#19473=CARTESIAN_POINT('Ctrl Pts',(-2.22806435475452,-2.32967240789121,
28.59702695154));
#19474=CARTESIAN_POINT('Ctrl Pts',(-2.12735875441497,-2.42163386167715,
28.6058257864524));
#19475=CARTESIAN_POINT('Ctrl Pts',(-2.08035433042835,-2.46213138061419,
28.6098784692821));
#19476=CARTESIAN_POINT('Ctrl Pts',(-1.86440644164759,-2.6375848025991,28.6282463302184));
#19477=CARTESIAN_POINT('Ctrl Pts',(-1.68331208770662,-2.75668492091963,
28.6430345672061));
#19478=CARTESIAN_POINT('Ctrl Pts',(-1.48621546801644,-2.8596012301885,28.6579680349496));
#19479=CARTESIAN_POINT('Ctrl Pts',(-1.48073943600392,-2.86244062514127,
28.6583820282506));
#19480=CARTESIAN_POINT('Ctrl Pts',(-1.47525540425972,-2.86526422074867,
28.6587956971472));
#19481=CARTESIAN_POINT('Origin',(0.,0.,4.68922655072688));
#19482=CARTESIAN_POINT('',(-1.47525540759407,-2.86526421903189,30.1566970682534));
#19483=CARTESIAN_POINT('',(-1.47525514454518,-2.86526435446941,29.9088139162969));
#19484=CARTESIAN_POINT('',(-1.47525540501186,-2.86526422036142,4.68922655072688));
#19485=CARTESIAN_POINT('',(3.22274868255297,-0.00291403553407739,29.310403850828));
#19486=CARTESIAN_POINT('Ctrl Pts',(-1.47525540759407,-2.86526421903189,
30.1566970682534));
#19487=CARTESIAN_POINT('Ctrl Pts',(-1.50490610286469,-2.84999779150791,
30.154597938539));
#19488=CARTESIAN_POINT('Ctrl Pts',(-1.53431835049294,-2.83427187172883,
30.1524827770642));
#19489=CARTESIAN_POINT('Ctrl Pts',(-1.64400800730423,-2.77341588983146,
30.1444684001732));
#19490=CARTESIAN_POINT('Ctrl Pts',(-1.72257584965478,-2.72531244714196,
30.1384684071173));
#19491=CARTESIAN_POINT('Ctrl Pts',(-1.99881463056546,-2.53946301663847,
30.1164416417455));
#19492=CARTESIAN_POINT('Ctrl Pts',(-2.18293532940145,-2.38304657637613,
30.0998803456669));
#19493=CARTESIAN_POINT('Ctrl Pts',(-2.41203203292022,-2.13938840339235,
30.0776166587306));
#19494=CARTESIAN_POINT('Ctrl Pts',(-2.47316296225755,-2.06841722126229,
30.0714850674834));
#19495=CARTESIAN_POINT('Ctrl Pts',(-2.5397775560768,-1.9838959275375,30.0646680376241));
#19496=CARTESIAN_POINT('Ctrl Pts',(-2.54836160950185,-1.97285737181948,
30.0637868364812));
#19497=CARTESIAN_POINT('Ctrl Pts',(-2.56118825328611,-1.95613970131652,
30.0624663789496));
#19498=CARTESIAN_POINT('Ctrl Pts',(-2.5654842668996,-1.95050205803763,30.0620234781831));
#19499=CARTESIAN_POINT('Ctrl Pts',(-2.57313142474656,-1.94039774611296,
30.0612340066121));
#19500=CARTESIAN_POINT('Ctrl Pts',(-2.57648958087305,-1.93593651326108,
30.060886946582));
#19501=CARTESIAN_POINT('Ctrl Pts',(-2.58373102965776,-1.92626419842136,
30.0601377538574));
#19502=CARTESIAN_POINT('Ctrl Pts',(-2.58761014880304,-1.92105010744374,
30.0597359126225));
#19503=CARTESIAN_POINT('Ctrl Pts',(-2.59839098708726,-1.90646721622962,
30.0586175725132));
#19504=CARTESIAN_POINT('Ctrl Pts',(-2.60525785831271,-1.89707260526927,
30.05790346303));
#19505=CARTESIAN_POINT('Ctrl Pts',(-2.64470485135637,-1.84248676699358,
30.0537895354871));
#19506=CARTESIAN_POINT('Ctrl Pts',(-2.67616186533482,-1.79649096180906,
30.0504621736318));
#19507=CARTESIAN_POINT('Ctrl Pts',(-2.8445781288749,-1.53598686739862,30.0322402161111));
#19508=CARTESIAN_POINT('Ctrl Pts',(-2.95695714947211,-1.30664163470692,
30.0184311705247));
#19509=CARTESIAN_POINT('Ctrl Pts',(-3.09545853092004,-0.911675496904819,
29.9947905460419));
#19510=CARTESIAN_POINT('Ctrl Pts',(-3.13783021194043,-0.753011836779592,
29.9853401520876));
#19511=CARTESIAN_POINT('Ctrl Pts',(-3.17196637725484,-0.570286756058514,
29.9741597063892));
#19512=CARTESIAN_POINT('Ctrl Pts',(-3.17577038064421,-0.548707696021086,
29.9728350528568));
#19513=CARTESIAN_POINT('Ctrl Pts',(-3.18149611941506,-0.514170740524261,
29.970707422226));
#19514=CARTESIAN_POINT('Ctrl Pts',(-3.18355945428613,-0.501236771736976,
29.9699089493559));
#19515=CARTESIAN_POINT('Ctrl Pts',(-3.18707151827445,-0.478324532890017,
29.9684913533374));
#19516=CARTESIAN_POINT('Ctrl Pts',(-3.18855237811255,-0.468351310154998,
29.9678732599077));
#19517=CARTESIAN_POINT('Ctrl Pts',(-3.19152985868076,-0.447629854386223,
29.9665868076826));
#19518=CARTESIAN_POINT('Ctrl Pts',(-3.1930190381003,-0.436880696650159,
29.9659182210636));
#19519=CARTESIAN_POINT('Ctrl Pts',(-3.19672512506709,-0.409097903782639,
29.9641868483567));
#19520=CARTESIAN_POINT('Ctrl Pts',(-3.19886016688344,-0.392053866741262,
29.9631214836763));
#19521=CARTESIAN_POINT('Ctrl Pts',(-3.20738727843857,-0.319268456753296,
29.9585576925809));
#19522=CARTESIAN_POINT('Ctrl Pts',(-3.21245904686602,-0.263385145945472,
29.955017921029));
#19523=CARTESIAN_POINT('Ctrl Pts',(-3.22198659378827,-0.115645711667687,
29.9455595619427));
#19524=CARTESIAN_POINT('Ctrl Pts',(-3.22397393531682,-0.0236871870202732,
29.939569309236));
#19525=CARTESIAN_POINT('Ctrl Pts',(-3.21689571194008,0.310597353811148,
29.91745003743));
#19526=CARTESIAN_POINT('Ctrl Pts',(-3.18443400471036,0.551592131422609,
29.9007767585704));
#19527=CARTESIAN_POINT('Ctrl Pts',(-3.10272593463277,0.876205680846315,
29.8785038258521));
#19528=CARTESIAN_POINT('Ctrl Pts',(-3.07634491150773,0.964753882003094,
29.8724584314665));
#19529=CARTESIAN_POINT('Ctrl Pts',(-3.04164295766476,1.06523239009345,29.8657250030753));
#19530=CARTESIAN_POINT('Ctrl Pts',(-3.03700626142552,1.0783806894635,29.8648464491974));
#19531=CARTESIAN_POINT('Ctrl Pts',(-3.02988673806894,1.09815938237161,29.8635291736297));
#19532=CARTESIAN_POINT('Ctrl Pts',(-3.02746721971465,1.1048121607055,29.8630868329737));
#19533=CARTESIAN_POINT('Ctrl Pts',(-3.02310025304166,1.11669762895154,29.8622979662095));
#19534=CARTESIAN_POINT('Ctrl Pts',(-3.02116111639402,1.12193326219123,29.8619509540083));
#19535=CARTESIAN_POINT('Ctrl Pts',(-3.01693315721173,1.13325822474451,29.861201417195));
#19536=CARTESIAN_POINT('Ctrl Pts',(-3.01463950802597,1.13934565319328,29.8607991864493));
#19537=CARTESIAN_POINT('Ctrl Pts',(-3.00818118580303,1.15633023222274,29.8596786616032));
#19538=CARTESIAN_POINT('Ctrl Pts',(-3.00397570337287,1.16721190698896,29.8589627720606));
#19539=CARTESIAN_POINT('Ctrl Pts',(-2.97917000023897,1.23037445263301,29.8548177738978));
#19540=CARTESIAN_POINT('Ctrl Pts',(-2.9572629226252,1.28213574929113,29.8514624073917));
#19541=CARTESIAN_POINT('Ctrl Pts',(-2.82887585685594,1.56465944789737,29.8332390918432));
#19542=CARTESIAN_POINT('Ctrl Pts',(-2.6967347660721,1.78279182494002,29.8194487141062));
#19543=CARTESIAN_POINT('Ctrl Pts',(-2.43950448500101,2.11229207460431,29.795836995626));
#19544=CARTESIAN_POINT('Ctrl Pts',(-2.32899849705148,2.23354326204648,29.786395902388));
#19545=CARTESIAN_POINT('Ctrl Pts',(-2.19381695475127,2.36088218734613,29.7752258613584));
#19546=CARTESIAN_POINT('Ctrl Pts',(-2.17771735488412,2.37574085695693,29.7739014106908));
#19547=CARTESIAN_POINT('Ctrl Pts',(-2.15175360627969,2.3992176850227,29.7717740443706));
#19548=CARTESIAN_POINT('Ctrl Pts',(-2.141986064573,2.40794202037586,29.7709756311572));
#19549=CARTESIAN_POINT('Ctrl Pts',(-2.12460532064257,2.42327700639462,29.7695581041739));
#19550=CARTESIAN_POINT('Ctrl Pts',(-2.11701372012307,2.42991195794515,29.7689400197886));
#19551=CARTESIAN_POINT('Ctrl Pts',(-2.10118646647693,2.44361428377264,29.7676535496038));
#19552=CARTESIAN_POINT('Ctrl Pts',(-2.09294601058157,2.45067589185952,29.7669849357982));
#19553=CARTESIAN_POINT('Ctrl Pts',(-2.07156912354722,2.46880822541172,29.7652534135996));
#19554=CARTESIAN_POINT('Ctrl Pts',(-2.0583796866194,2.47981566548539,29.7641879257696));
#19555=CARTESIAN_POINT('Ctrl Pts',(-2.00172712233524,2.52633252606068,29.7596228924428));
#19556=CARTESIAN_POINT('Ctrl Pts',(-1.95743058142145,2.56080697913076,29.7560819738151));
#19557=CARTESIAN_POINT('Ctrl Pts',(-1.83821555419165,2.6486869656554,29.7466197713309));
#19558=CARTESIAN_POINT('Ctrl Pts',(-1.76187566129761,2.70006864616016,29.7406267498669));
#19559=CARTESIAN_POINT('Ctrl Pts',(-1.49558015937302,2.86319692247284,29.7199671586201));
#19560=CARTESIAN_POINT('Ctrl Pts',(-1.29641039046421,2.95870987086433,29.7048734255436));
#19561=CARTESIAN_POINT('Ctrl Pts',(-1.04907995493489,3.04751626004872,29.6872705465333));
#19562=CARTESIAN_POINT('Ctrl Pts',(-1.00879545775868,3.06108739848742,29.684439599267));
#19563=CARTESIAN_POINT('Ctrl Pts',(-0.898515013775821,3.09582530028794,
29.6768066825273));
#19564=CARTESIAN_POINT('Ctrl Pts',(-0.828043247235926,3.11541486172981,
29.6720552170986));
#19565=CARTESIAN_POINT('Ctrl Pts',(-0.745303572827527,3.13540810105431,
29.6666686595058));
#19566=CARTESIAN_POINT('Ctrl Pts',(-0.733630998414152,3.13815980225944,
29.6659131543855));
#19567=CARTESIAN_POINT('Ctrl Pts',(-0.714897712427233,3.14246576491344,
29.6647080025157));
#19568=CARTESIAN_POINT('Ctrl Pts',(-0.707846789998971,3.14406150499464,
29.6642560673893));
#19569=CARTESIAN_POINT('Ctrl Pts',(-0.695314062728149,3.14685357083816,
29.663455800664));
#19570=CARTESIAN_POINT('Ctrl Pts',(-0.689834436398883,3.14805932192016,
29.6631069332413));
#19571=CARTESIAN_POINT('Ctrl Pts',(-0.678166418906133,3.15059485388289,
29.6623662840839));
#19572=CARTESIAN_POINT('Ctrl Pts',(-0.671977264520974,3.1519207132548,29.6619747284339));
#19573=CARTESIAN_POINT('Ctrl Pts',(-0.655151028549342,3.15547346634429,
29.660913684378));
#19574=CARTESIAN_POINT('Ctrl Pts',(-0.644506410036485,3.15766482741931,
29.6602462029593));
#19575=CARTESIAN_POINT('Ctrl Pts',(-0.590978076600973,3.16840251597339,
29.6569075785604));
#19576=CARTESIAN_POINT('Ctrl Pts',(-0.547932345980393,3.17612974757747,
29.6542804549792));
#19577=CARTESIAN_POINT('Ctrl Pts',(-0.420990496588037,3.19625952686892,
29.6466667092065));
#19578=CARTESIAN_POINT('Ctrl Pts',(-0.336742964529679,3.20623052794022,
29.6417836779992));
#19579=CARTESIAN_POINT('Ctrl Pts',(-0.000406068110473529,3.23263136135832,
29.6226259748287));
#19580=CARTESIAN_POINT('Ctrl Pts',(0.252827473807959,3.22272999536765,29.6088767928467));
#19581=CARTESIAN_POINT('Ctrl Pts',(0.551060381577973,3.1756708729986,29.5914456505624));
#19582=CARTESIAN_POINT('Ctrl Pts',(0.599622859111373,3.16686045339623,29.5885701662931));
#19583=CARTESIAN_POINT('Ctrl Pts',(0.658405049910383,3.15479539712077,29.5850345670279));
#19584=CARTESIAN_POINT('Ctrl Pts',(0.66883700636404,3.15260023831344,29.5844049980047));
#19585=CARTESIAN_POINT('Ctrl Pts',(0.726216945248131,3.14022836569188,29.5809300848203));
#19586=CARTESIAN_POINT('Ctrl Pts',(0.772941837253632,3.12905509538947,29.5780558895651));
#19587=CARTESIAN_POINT('Ctrl Pts',(0.83564318239307,3.11257131438671,29.5741312797917));
#19588=CARTESIAN_POINT('Ctrl Pts',(0.851854700707565,3.10817362251126,29.5731104163109));
#19589=CARTESIAN_POINT('Ctrl Pts',(0.878401343913244,3.10074903867069,29.5714283234233));
#19590=CARTESIAN_POINT('Ctrl Pts',(0.888757120313623,3.09779668449126,29.5707695307421));
#19591=CARTESIAN_POINT('Ctrl Pts',(0.908811495637516,3.09197049588435,29.5694885964141));
#19592=CARTESIAN_POINT('Ctrl Pts',(0.918511754298188,3.08910278811082,29.5688666618729));
#19593=CARTESIAN_POINT('Ctrl Pts',(0.941158191586101,3.08229167561428,29.5674091057734));
#19594=CARTESIAN_POINT('Ctrl Pts',(0.954093276208391,3.07831231788811,29.5665723115074));
#19595=CARTESIAN_POINT('Ctrl Pts',(0.991525026363504,3.06653819863982,29.5641381735354));
#19596=CARTESIAN_POINT('Ctrl Pts',(1.01595353181547,3.05853179825947,29.5625338882188));
#19597=CARTESIAN_POINT('Ctrl Pts',(1.07397794084757,3.03874256004082,29.5586847772657));
#19598=CARTESIAN_POINT('Ctrl Pts',(1.10747893281186,3.02669377612345,29.5564313496067));
#19599=CARTESIAN_POINT('Ctrl Pts',(1.22145268042145,2.98355704726474,29.5486562195386));
#19600=CARTESIAN_POINT('Ctrl Pts',(1.3008680387229,2.94979652479162,29.5430496902575));
#19601=CARTESIAN_POINT('Ctrl Pts',(1.5692307863845,2.82276608566618,29.523462784395));
#19602=CARTESIAN_POINT('Ctrl Pts',(1.75032820285449,2.71419076092588,29.5090736483039));
#19603=CARTESIAN_POINT('Ctrl Pts',(2.02516560274469,2.51040240796522,29.4860565816094));
#19604=CARTESIAN_POINT('Ctrl Pts',(2.12593312182075,2.42566125694342,29.4773275899195));
#19605=CARTESIAN_POINT('Ctrl Pts',(2.23206697039844,2.32469730196501,29.4680400626352));
#19606=CARTESIAN_POINT('Ctrl Pts',(2.24281378251912,2.31433075926442,29.4670985445374));
#19607=CARTESIAN_POINT('Ctrl Pts',(2.25862280068223,2.29886758863895,29.4657124405473));
#19608=CARTESIAN_POINT('Ctrl Pts',(2.26374045923784,2.29382830251894,29.4652635627232));
#19609=CARTESIAN_POINT('Ctrl Pts',(2.27281277292758,2.28483499045654,29.4644675819881));
#19610=CARTESIAN_POINT('Ctrl Pts',(2.27677401771419,2.2808877456708,29.4641199564936));
#19611=CARTESIAN_POINT('Ctrl Pts',(2.28527049176272,2.2723771105962,29.4633741836911));
#19612=CARTESIAN_POINT('Ctrl Pts',(2.28980232408721,2.26781045759979,29.4629763031123));
#19613=CARTESIAN_POINT('Ctrl Pts',(2.29908552762998,2.25839972951307,29.4621609785315));
#19614=CARTESIAN_POINT('Ctrl Pts',(2.30383534056257,2.2535541544712,29.4617436555735));
#19615=CARTESIAN_POINT('Ctrl Pts',(2.32591364009411,2.23088797274666,29.4598028926061));
#19616=CARTESIAN_POINT('Ctrl Pts',(2.3430514512872,2.21288169405233,29.4582936932344));
#19617=CARTESIAN_POINT('Ctrl Pts',(2.44182459071909,2.10666903662449,29.4495664899157));
#19618=CARTESIAN_POINT('Ctrl Pts',(2.51869134286943,2.01414047870905,29.4426556672));
#19619=CARTESIAN_POINT('Ctrl Pts',(2.65366956281472,1.83181023506072,29.4298260869321));
#19620=CARTESIAN_POINT('Ctrl Pts',(2.7128309768901,1.74299740215409,29.423891139486));
#19621=CARTESIAN_POINT('Ctrl Pts',(2.88400737534978,1.45613556190016,29.4052128235388));
#19622=CARTESIAN_POINT('Ctrl Pts',(2.97952181420673,1.24910348356683,29.3923721342071));
#19623=CARTESIAN_POINT('Ctrl Pts',(3.05949903246884,1.01294912582522,29.3773765367186));
#19624=CARTESIAN_POINT('Ctrl Pts',(3.06633334115026,0.992068579045114,29.3760483795231));
#19625=CARTESIAN_POINT('Ctrl Pts',(3.07690537680614,0.958615073740874,29.3739161844441));
#19626=CARTESIAN_POINT('Ctrl Pts',(3.08078084459804,0.94608611500234,29.3731166817402));
#19627=CARTESIAN_POINT('Ctrl Pts',(3.08750109455554,0.923881089110192,29.3716978934421));
#19628=CARTESIAN_POINT('Ctrl Pts',(3.09037714762243,0.914214612373763,29.3710796433387));
#19629=CARTESIAN_POINT('Ctrl Pts',(3.09625148195943,0.894126347238917,29.369793498447));
#19630=CARTESIAN_POINT('Ctrl Pts',(3.09924262354071,0.883702619770213,29.3691253789827));
#19631=CARTESIAN_POINT('Ctrl Pts',(3.10682642850287,0.856761931016188,29.3673965754224));
#19632=CARTESIAN_POINT('Ctrl Pts',(3.11133996447568,0.84022322654944,29.3663333272389));
#19633=CARTESIAN_POINT('Ctrl Pts',(3.12082918296896,0.804327183420667,29.3640211458183));
#19634=CARTESIAN_POINT('Ctrl Pts',(3.12575715484874,0.78495807983831,29.3627707123131));
#19635=CARTESIAN_POINT('Ctrl Pts',(3.13961206620811,0.728301870177439,29.3591044824234));
#19636=CARTESIAN_POINT('Ctrl Pts',(3.14805391131739,0.690900795586383,29.3566733796703));
#19637=CARTESIAN_POINT('Ctrl Pts',(3.20053145333622,0.4374261572385,29.340120566228));
#19638=CARTESIAN_POINT('Ctrl Pts',(3.22294799654118,0.217515291900805,29.3253254145322));
#19639=CARTESIAN_POINT('Ctrl Pts',(3.22274868255297,-0.00291403553407739,
29.310403850828));
#19640=CARTESIAN_POINT('Ctrl Pts',(3.22274868160926,-0.00291507903117872,
29.3104037801903));
#19641=CARTESIAN_POINT('Ctrl Pts',(3.22256534304824,-0.205603959681518,
29.2966831237793));
#19642=CARTESIAN_POINT('Ctrl Pts',(3.20326082911173,-0.407852858796435,
29.2829337678001));
#19643=CARTESIAN_POINT('Ctrl Pts',(3.16309348166168,-0.617307007073877,
29.2694106703809));
#19644=CARTESIAN_POINT('Ctrl Pts',(3.16106077110211,-0.627632952541531,
29.2687459302496));
#19645=CARTESIAN_POINT('Ctrl Pts',(3.1576273091046,-0.644634672970911,29.2676548391535));
#19646=CARTESIAN_POINT('Ctrl Pts',(3.1562558987221,-0.651316197072443,29.2672269192357));
#19647=CARTESIAN_POINT('Ctrl Pts',(3.15354462065916,-0.664315889376073,
29.2663961111621));
#19648=CARTESIAN_POINT('Ctrl Pts',(3.15220695277181,-0.670634478685622,
29.2659931025164));
#19649=CARTESIAN_POINT('Ctrl Pts',(3.14967635126913,-0.682413129140914,
29.2652434127691));
#19650=CARTESIAN_POINT('Ctrl Pts',(3.14848822261914,-0.687874050417935,
29.2648964719155));
#19651=CARTESIAN_POINT('Ctrl Pts',(3.14574871482761,-0.700309671938866,
29.2641078428984));
#19652=CARTESIAN_POINT('Ctrl Pts',(3.14418834579419,-0.707282307104274,
29.2636666766864));
#19653=CARTESIAN_POINT('Ctrl Pts',(3.13933752253749,-0.728625289511433,
29.2623192395386));
#19654=CARTESIAN_POINT('Ctrl Pts',(3.13597158940063,-0.742978534409029,
29.2614171941518));
#19655=CARTESIAN_POINT('Ctrl Pts',(3.089482932111,-0.935272765366997,29.2493813237167));
#19656=CARTESIAN_POINT('Ctrl Pts',(3.03136414155181,-1.10927518939484,29.2390454697405));
#19657=CARTESIAN_POINT('Ctrl Pts',(2.91544766044806,-1.37776192229644,29.2226713131795));
#19658=CARTESIAN_POINT('Ctrl Pts',(2.86704942961926,-1.4758354527137,29.2165935885301));
#19659=CARTESIAN_POINT('Ctrl Pts',(2.74824608468614,-1.68858484280817,29.2028692994063));
#19660=CARTESIAN_POINT('Ctrl Pts',(2.67546130473401,-1.80168726048934,29.1951934683402));
#19661=CARTESIAN_POINT('Ctrl Pts',(2.56329817344162,-1.95413261530896,29.1840275288447));
#19662=CARTESIAN_POINT('Ctrl Pts',(2.52963819606918,-1.99751391985591,29.1807495327771));
#19663=CARTESIAN_POINT('Ctrl Pts',(2.48400786674977,-2.05331875648277,29.1763874888711));
#19664=CARTESIAN_POINT('Ctrl Pts',(2.47302154446911,-2.06653754395756,29.1753431765623));
#19665=CARTESIAN_POINT('Ctrl Pts',(2.45492580917966,-2.08795944629466,29.1736323330609));
#19666=CARTESIAN_POINT('Ctrl Pts',(2.44787967264201,-2.09621575264933,29.1729684053765));
#19667=CARTESIAN_POINT('Ctrl Pts',(2.43420871949357,-2.11207175866517,29.171684464469));
#19668=CARTESIAN_POINT('Ctrl Pts',(2.42758967739156,-2.11967628621569,29.1710646954275));
#19669=CARTESIAN_POINT('Ctrl Pts',(2.41229345480022,-2.13708428721178,29.1696366577884));
#19670=CARTESIAN_POINT('Ctrl Pts',(2.40359204442231,-2.14686614361002,29.1688273780311));
#19671=CARTESIAN_POINT('Ctrl Pts',(2.38018131644951,-2.17286303055339,29.1666580443978));
#19672=CARTESIAN_POINT('Ctrl Pts',(2.36536616874142,-2.18898142940791,29.1652935181092));
#19673=CARTESIAN_POINT('Ctrl Pts',(2.23881732764216,-2.32387758097412,29.1537054128931));
#19674=CARTESIAN_POINT('Ctrl Pts',(2.11839832906726,-2.43414955835226,29.1430984663776));
#19675=CARTESIAN_POINT('Ctrl Pts',(1.79146236147033,-2.69083719126962,29.1153810232071));
#19676=CARTESIAN_POINT('Ctrl Pts',(1.57511053416741,-2.82293531037656,29.0979463293549));
#19677=CARTESIAN_POINT('Ctrl Pts',(1.29266224771272,-2.95271579735184,29.0775892870927));
#19678=CARTESIAN_POINT('Ctrl Pts',(1.23911345335635,-2.97558483673494,29.073832022879));
#19679=CARTESIAN_POINT('Ctrl Pts',(1.17406089214567,-3.0013057517665,29.0694136140893));
#19680=CARTESIAN_POINT('Ctrl Pts',(1.16312739045241,-3.0055598276544,29.0686758897867));
#19681=CARTESIAN_POINT('Ctrl Pts',(1.14603338497877,-3.01210362198886,29.0675303734807));
#19682=CARTESIAN_POINT('Ctrl Pts',(1.13988882690843,-3.0144343106465,29.0671201912356));
#19683=CARTESIAN_POINT('Ctrl Pts',(1.12851637022563,-3.01870824532816,29.0663639965173));
#19684=CARTESIAN_POINT('Ctrl Pts',(1.12329059885219,-3.02065670006162,29.0660176815883));
#19685=CARTESIAN_POINT('Ctrl Pts',(1.11150250143589,-3.02501712908773,29.0652390816793));
#19686=CARTESIAN_POINT('Ctrl Pts',(1.10493738799372,-3.02742131404998,29.0648072652107));
#19687=CARTESIAN_POINT('Ctrl Pts',(1.08564142753255,-3.034416484567,29.0635432391056));
#19688=CARTESIAN_POINT('Ctrl Pts',(1.07288923917483,-3.03894873375401,29.0627144483772));
#19689=CARTESIAN_POINT('Ctrl Pts',(0.983152201627766,-3.07020686216032,
29.0569257809611));
#19690=CARTESIAN_POINT('Ctrl Pts',(0.905199431957328,-3.09408708161769,
29.0521213336498));
#19691=CARTESIAN_POINT('Ctrl Pts',(0.577940644502667,-3.18091009518054,
29.0325512088994));
#19692=CARTESIAN_POINT('Ctrl Pts',(0.322457362576845,-3.21686866800029,
29.0186238319458));
#19693=CARTESIAN_POINT('Ctrl Pts',(-0.0244965292561324,-3.22391103655472,
28.9988486067735));
#19694=CARTESIAN_POINT('Ctrl Pts',(-0.114425116185241,-3.22197261273145,
28.9936538743263));
#19695=CARTESIAN_POINT('Ctrl Pts',(-0.259056058253541,-3.21279228997703,
28.9851042261706));
#19696=CARTESIAN_POINT('Ctrl Pts',(-0.313860790535886,-3.20790199344572,
28.9818194808435));
#19697=CARTESIAN_POINT('Ctrl Pts',(-0.385575746276679,-3.19964747495353,
28.9774511558123));
#19698=CARTESIAN_POINT('Ctrl Pts',(-0.402624079715029,-3.19754694301061,
28.9764075028551));
#19699=CARTESIAN_POINT('Ctrl Pts',(-0.430414018425829,-3.1938971646164,
28.9746974683103));
#19700=CARTESIAN_POINT('Ctrl Pts',(-0.44116617140963,-3.19242975334629,
28.9740336854851));
#19701=CARTESIAN_POINT('Ctrl Pts',(-0.46189358693377,-3.18949424450099,
28.9727498342086));
#19702=CARTESIAN_POINT('Ctrl Pts',(-0.471869787077632,-3.18803358227474,
28.9721300089135));
#19703=CARTESIAN_POINT('Ctrl Pts',(-0.494789209224281,-3.1845679058044,
28.9707015685828));
#19704=CARTESIAN_POINT('Ctrl Pts',(-0.507727324821025,-3.18253076398856,
28.9698919405207));
#19705=CARTESIAN_POINT('Ctrl Pts',(-0.542276322214073,-3.17687489103105,
28.9677210657206));
#19706=CARTESIAN_POINT('Ctrl Pts',(-0.563863023052856,-3.17311457968817,
28.9663553365741));
#19707=CARTESIAN_POINT('Ctrl Pts',(-0.746702636286027,-3.13934005677025,
28.9547063258453));
#19708=CARTESIAN_POINT('Ctrl Pts',(-0.905460592489548,-3.09728061484943,
28.9440350000521));
#19709=CARTESIAN_POINT('Ctrl Pts',(-1.20274089852636,-2.99370695645388,
28.9230375612164));
#19710=CARTESIAN_POINT('Ctrl Pts',(-1.3413890507256,-2.9341887838544,28.9127897747778));
#19711=CARTESIAN_POINT('Ctrl Pts',(-1.4752555406476,-2.86526415052584,28.9026236394039));
#19712=CARTESIAN_POINT('Ctrl Pts',(-1.47525540425972,-2.86526422074867,
28.6587956971472));
#19713=CARTESIAN_POINT('Ctrl Pts',(-1.40396999219795,-2.90196735919833,
28.6641728647368));
#19714=CARTESIAN_POINT('Ctrl Pts',(-1.3313329276085,-2.93600090125158,28.6694959185801));
#19715=CARTESIAN_POINT('Ctrl Pts',(-1.21664140494405,-2.98460551359186,
28.6775868870742));
#19716=CARTESIAN_POINT('Ctrl Pts',(-1.17543153260819,-3.00107440122143,
28.6804330269589));
#19717=CARTESIAN_POINT('Ctrl Pts',(-1.1237423023483,-3.02050300089093,28.6839161440751));
#19718=CARTESIAN_POINT('Ctrl Pts',(-1.11357292367107,-3.02426693465933,
28.6845972822034));
#19719=CARTESIAN_POINT('Ctrl Pts',(-1.09744394476884,-3.03014427507075,
28.6856708397806));
#19720=CARTESIAN_POINT('Ctrl Pts',(-1.0914968996138,-3.03229155250976,28.6860652327261));
#19721=CARTESIAN_POINT('Ctrl Pts',(-1.08026160193583,-3.03631090353643,
28.6868075487327));
#19722=CARTESIAN_POINT('Ctrl Pts',(-1.07497484724119,-3.03818664828513,
28.6871556795278));
#19723=CARTESIAN_POINT('Ctrl Pts',(-1.06285910381106,-3.04244973997234,
28.6879508676203));
#19724=CARTESIAN_POINT('Ctrl Pts',(-1.05602696245719,-3.0448279018325,28.6883973759602));
#19725=CARTESIAN_POINT('Ctrl Pts',(-1.03782773461022,-3.05109414481469,
28.6895818573481));
#19726=CARTESIAN_POINT('Ctrl Pts',(-1.02644669036383,-3.05494174896131,
28.6903174972633));
#19727=CARTESIAN_POINT('Ctrl Pts',(-0.945255347244536,-3.08188525732524,
28.6955311188072));
#19728=CARTESIAN_POINT('Ctrl Pts',(-0.874688204289027,-3.10265157735439,
28.6998821778984));
#19729=CARTESIAN_POINT('Ctrl Pts',(-0.577957695183423,-3.17904185304228,
28.7176707123769));
#19730=CARTESIAN_POINT('Ctrl Pts',(-0.346806425840722,-3.21248883264467,
28.73036260275));
#19731=CARTESIAN_POINT('Ctrl Pts',(0.0525160222780035,-3.22662981942941,
28.7529268929991));
#19732=CARTESIAN_POINT('Ctrl Pts',(0.219270651318447,-3.21959738789219,
28.7625308840943));
#19733=CARTESIAN_POINT('Ctrl Pts',(0.407795520838591,-3.19692985981318,
28.7739614183635));
#19734=CARTESIAN_POINT('Ctrl Pts',(0.430839345416441,-3.19390593636074,
28.7753680890368));
#19735=CARTESIAN_POINT('Ctrl Pts',(0.465894098769699,-3.18891961264384,
28.7775232068439));
#19736=CARTESIAN_POINT('Ctrl Pts',(0.477930270913111,-3.18713794130816,
28.7782659223024));
#19737=CARTESIAN_POINT('Ctrl Pts',(0.499792445413534,-3.18377513656193,
28.7796200863225));
#19738=CARTESIAN_POINT('Ctrl Pts',(0.509621803679512,-3.18221655805529,
28.7802308105047));
#19739=CARTESIAN_POINT('Ctrl Pts',(0.53080882967596,-3.17875638578577,28.7815513521264));
#19740=CARTESIAN_POINT('Ctrl Pts',(0.542163810837095,-3.17683939955025,
28.7822616524814));
#19741=CARTESIAN_POINT('Ctrl Pts',(0.572886769222668,-3.17148313205629,
28.7841905795537));
#19742=CARTESIAN_POINT('Ctrl Pts',(0.592233686408896,-3.16792735716365,
28.785412906091));
#19743=CARTESIAN_POINT('Ctrl Pts',(0.685927946182076,-3.14981899119338,
28.7913704394246));
#19744=CARTESIAN_POINT('Ctrl Pts',(0.759773804354028,-3.13282604629927,
28.7961830864327));
#19745=CARTESIAN_POINT('Ctrl Pts',(0.87699065171407,-3.10146474954353,28.8040170238609));
#19746=CARTESIAN_POINT('Ctrl Pts',(0.920776848315933,-3.08874827181873,
28.8069876221633));
#19747=CARTESIAN_POINT('Ctrl Pts',(1.17616572146954,-3.00866469720912,28.8245690270011));
#19748=CARTESIAN_POINT('Ctrl Pts',(1.38060677875684,-2.9205027506252,28.8397379188287));
#19749=CARTESIAN_POINT('Ctrl Pts',(1.65535713550674,-2.76668259807285,28.8609260244795));
#19750=CARTESIAN_POINT('Ctrl Pts',(1.73438754721218,-2.71783776856526,28.8671163102619));
#19751=CARTESIAN_POINT('Ctrl Pts',(1.8496900150307,-2.63949417640251,28.8761832508512));
#19752=CARTESIAN_POINT('Ctrl Pts',(1.88760861915842,-2.61251160702068,28.8791708839483));
#19753=CARTESIAN_POINT('Ctrl Pts',(1.93376225015725,-2.57813931891385,28.882801609748));
#19754=CARTESIAN_POINT('Ctrl Pts',(1.94255909407012,-2.57151763793293,28.8834933558206));
#19755=CARTESIAN_POINT('Ctrl Pts',(1.95638340748184,-2.56100018965169,28.884579788304));
#19756=CARTESIAN_POINT('Ctrl Pts',(1.9614334787735,-2.55713447406964,28.8849765274964));
#19757=CARTESIAN_POINT('Ctrl Pts',(1.97091051274624,-2.54983542562625,28.8857207396868));
#19758=CARTESIAN_POINT('Ctrl Pts',(1.97533991252699,-2.54640554066325,28.8860684349561));
#19759=CARTESIAN_POINT('Ctrl Pts',(1.98542017193474,-2.53855780921815,28.8868594280023));
#19760=CARTESIAN_POINT('Ctrl Pts',(1.99106523364058,-2.53413264206891,28.8873021976337));
#19761=CARTESIAN_POINT('Ctrl Pts',(2.00596194063047,-2.52237459872266,28.8884702405812));
#19762=CARTESIAN_POINT('Ctrl Pts',(2.01518825011847,-2.51500959243648,28.8891932824551));
#19763=CARTESIAN_POINT('Ctrl Pts',(2.07834517174276,-2.46402317407827,28.8941416757975));
#19764=CARTESIAN_POINT('Ctrl Pts',(2.13090008533058,-2.41871768971775,28.8982541898969));
#19765=CARTESIAN_POINT('Ctrl Pts',(2.20228957414053,-2.35304092544874,28.9038996444825));
#19766=CARTESIAN_POINT('Ctrl Pts',(2.22238244325534,-2.33407311599751,28.9054954685767));
#19767=CARTESIAN_POINT('Ctrl Pts',(2.41885297919624,-2.14376608856944,28.9211975881544));
#19768=CARTESIAN_POINT('Ctrl Pts',(2.57532111485968,-1.95302748641564,28.9345590400097));
#19769=CARTESIAN_POINT('Ctrl Pts',(2.75612272864558,-1.67260349494436,28.9535927331154));
#19770=CARTESIAN_POINT('Ctrl Pts',(2.80063040280429,-1.59696041740749,28.9586666214574));
#19771=CARTESIAN_POINT('Ctrl Pts',(2.86757268797092,-1.47176323342458,28.9670465993361));
#19772=CARTESIAN_POINT('Ctrl Pts',(2.89193758341982,-1.42329077376705,28.970286610484));
#19773=CARTESIAN_POINT('Ctrl Pts',(2.92230106935959,-1.35888257761859,28.9745963909198));
#19774=CARTESIAN_POINT('Ctrl Pts',(2.92941412101072,-1.34347991805939,28.9756273554906));
#19775=CARTESIAN_POINT('Ctrl Pts',(2.94085673881402,-1.31817901150173,28.977321676591));
#19776=CARTESIAN_POINT('Ctrl Pts',(2.94525879437391,-1.30831375986799,28.9779825242725));
#19777=CARTESIAN_POINT('Ctrl Pts',(2.95367877681639,-1.28918624599409,28.9792643020775));
#19778=CARTESIAN_POINT('Ctrl Pts',(2.95770294795101,-1.27992685785367,28.9798850085528));
#19779=CARTESIAN_POINT('Ctrl Pts',(2.96688777363738,-1.25851846646698,28.9813206935619));
#19780=CARTESIAN_POINT('Ctrl Pts',(2.97201740303294,-1.24635642555943,28.982136720303));
#19781=CARTESIAN_POINT('Ctrl Pts',(2.98560068114123,-1.21359058612412,28.9843364721306));
#19782=CARTESIAN_POINT('Ctrl Pts',(2.99391559255992,-1.19293039292791,28.9857248708156));
#19783=CARTESIAN_POINT('Ctrl Pts',(3.07649546443753,-0.981440032530335,
28.9999536340679));
#19784=CARTESIAN_POINT('Ctrl Pts',(3.1326127666368,-0.784065332646564,29.013413091123));
#19785=CARTESIAN_POINT('Ctrl Pts',(3.20505859250885,-0.390016707707387,
29.0403759663423));
#19786=CARTESIAN_POINT('Ctrl Pts',(3.22284016615892,-0.194467152849475,
29.0537891193601));
#19787=CARTESIAN_POINT('Ctrl Pts',(3.22271722593296,0.0717007493025189,
29.0713365201397));
#19788=CARTESIAN_POINT('Ctrl Pts',(3.22039028229918,0.14189930542022,29.0758939041521));
#19789=CARTESIAN_POINT('Ctrl Pts',(3.21499221206757,0.223792271955602,29.0810864052186));
#19790=CARTESIAN_POINT('Ctrl Pts',(3.21414783218013,0.235609056908833,29.0818326238974));
#19791=CARTESIAN_POINT('Ctrl Pts',(3.21268668472616,0.254584861328354,29.0830257592115));
#19792=CARTESIAN_POINT('Ctrl Pts',(3.21211111186224,0.26174681135929,29.0834748948519));
#19793=CARTESIAN_POINT('Ctrl Pts',(3.21104402255572,0.274490888215193,29.0842719132135));
#19794=CARTESIAN_POINT('Ctrl Pts',(3.21056189399288,0.280073720927902,29.0846203170239));
#19795=CARTESIAN_POINT('Ctrl Pts',(3.20950215639828,0.291982569170837,29.0853618883162));
#19796=CARTESIAN_POINT('Ctrl Pts',(3.20892040648182,0.298308127845474,29.0857548199946));
#19797=CARTESIAN_POINT('Ctrl Pts',(3.20728242496246,0.315559004206297,29.0868238798402));
#19798=CARTESIAN_POINT('Ctrl Pts',(3.20618906392951,0.326480831086335,29.087497948285));
#19799=CARTESIAN_POINT('Ctrl Pts',(3.20021562258018,0.383224416561684,29.0909865984107));
#19800=CARTESIAN_POINT('Ctrl Pts',(3.19440870488997,0.428945824171261,29.0937520649199));
#19801=CARTESIAN_POINT('Ctrl Pts',(3.17415335876158,0.565009832966689,29.1018875723163));
#19802=CARTESIAN_POINT('Ctrl Pts',(3.15683655997082,0.654882479877528,29.1071368810512));
#19803=CARTESIAN_POINT('Ctrl Pts',(3.08056946531086,0.976365585140953,29.1258427994704));
#19804=CARTESIAN_POINT('Ctrl Pts',(2.99974492977684,1.20196942756836,29.1388913276044));
#19805=CARTESIAN_POINT('Ctrl Pts',(2.88188213627333,1.44281906994326,29.1543467970422));
#19806=CARTESIAN_POINT('Ctrl Pts',(2.868681135622,1.4688907353864,29.1560402125599));
#19807=CARTESIAN_POINT('Ctrl Pts',(2.81941619220345,1.56299007899431,29.1622331727083));
#19808=CARTESIAN_POINT('Ctrl Pts',(2.78127419751381,1.62989510969802,29.1667929441243));
#19809=CARTESIAN_POINT('Ctrl Pts',(2.73037025714497,1.71218779377524,29.1726333473387));
#19810=CARTESIAN_POINT('Ctrl Pts',(2.71981067782974,1.72891255766319,29.1738327135409));
#19811=CARTESIAN_POINT('Ctrl Pts',(2.70284721757682,1.7552400599415,29.1757409309371));
#19812=CARTESIAN_POINT('Ctrl Pts',(2.69654444135584,1.76490759529053,29.176446006175));
#19813=CARTESIAN_POINT('Ctrl Pts',(2.68471085993894,1.78284721020861,29.1777626527426));
#19814=CARTESIAN_POINT('Ctrl Pts',(2.67919339063614,1.79112795423892,29.1783737165681));
#19815=CARTESIAN_POINT('Ctrl Pts',(2.66686158549637,1.80945133527866,29.1797333053164));
#19816=CARTESIAN_POINT('Ctrl Pts',(2.66002871843932,1.81948126166461,29.1804825279099));
#19817=CARTESIAN_POINT('Ctrl Pts',(2.64003061574145,1.84848293416519,29.1826636448888));
#19818=CARTESIAN_POINT('Ctrl Pts',(2.62671813177074,1.86735176690557,29.1841011542546));
#19819=CARTESIAN_POINT('Ctrl Pts',(2.51911292595528,2.01644144190624,29.1956096258624));
#19820=CARTESIAN_POINT('Ctrl Pts',(2.41541305500278,2.1395634685583,29.2060523943513));
#19821=CARTESIAN_POINT('Ctrl Pts',(2.13030543509723,2.43081155771247,29.2331990204489));
#19822=CARTESIAN_POINT('Ctrl Pts',(1.93795346992231,2.5867692885241,29.250216023592));
#19823=CARTESIAN_POINT('Ctrl Pts',(1.67364821176006,2.75489222714048,29.2708290805123));
#19824=CARTESIAN_POINT('Ctrl Pts',(1.61650972287745,2.78880391382018,29.2751338136682));
#19825=CARTESIAN_POINT('Ctrl Pts',(1.54815548818489,2.82656470714442,29.2800732326752));
#19826=CARTESIAN_POINT('Ctrl Pts',(1.53792080739249,2.83214636965665,29.2808073920191));
#19827=CARTESIAN_POINT('Ctrl Pts',(1.52131124925244,2.84108809547771,29.2819898148161));
#19828=CARTESIAN_POINT('Ctrl Pts',(1.51495510381144,2.84448246948307,29.2824401803591));
#19829=CARTESIAN_POINT('Ctrl Pts',(1.50364543539903,2.85047351249694,29.2832376898377));
#19830=CARTESIAN_POINT('Ctrl Pts',(1.49869649159102,2.85307862994574,29.2835853651635));
#19831=CARTESIAN_POINT('Ctrl Pts',(1.48805705073403,2.85864389500602,29.2843300030355));
#19832=CARTESIAN_POINT('Ctrl Pts',(1.48236450612242,2.86159993314565,29.2847267055979));
#19833=CARTESIAN_POINT('Ctrl Pts',(1.46665712192126,2.86969705278641,29.2858167246806));
#19834=CARTESIAN_POINT('Ctrl Pts',(1.4566239983704,2.87480274526202,29.2865078434825));
#19835=CARTESIAN_POINT('Ctrl Pts',(1.40193496656332,2.90227328450517,29.290248312243));
#19836=CARTESIAN_POINT('Ctrl Pts',(1.35678781225537,2.92365171319271,29.2932397205461));
#19837=CARTESIAN_POINT('Ctrl Pts',(1.07460349449837,3.04932830812556,29.3114576644985));
#19838=CARTESIAN_POINT('Ctrl Pts',(0.826187780816833,3.12579918209925,29.3254990040934));
#19839=CARTESIAN_POINT('Ctrl Pts',(0.407963346515534,3.20112777082683,29.349490132611));
#19840=CARTESIAN_POINT('Ctrl Pts',(0.242646346792784,3.21788208299025,29.359046072379));
#19841=CARTESIAN_POINT('Ctrl Pts',(0.0548488916515991,3.22235794675189,
29.370344360395));
#19842=CARTESIAN_POINT('Ctrl Pts',(0.032905956164449,3.22265671449435,29.3716709932229));
#19843=CARTESIAN_POINT('Ctrl Pts',(-0.00214273177335041,3.22277593224936,
29.37380106105));
#19844=CARTESIAN_POINT('Ctrl Pts',(-0.0152475465529373,3.22274057366517,
29.3745999734712));
#19845=CARTESIAN_POINT('Ctrl Pts',(-0.0384321778173136,3.22253660266174,
29.3760179046385));
#19846=CARTESIAN_POINT('Ctrl Pts',(-0.0485121605683872,3.22240061978577,
29.3766358903689));
#19847=CARTESIAN_POINT('Ctrl Pts',(-0.069432302913408,3.22202021798673,
29.3779216740557));
#19848=CARTESIAN_POINT('Ctrl Pts',(-0.0802721848751933,3.22176838111275,
29.3785896974758));
#19849=CARTESIAN_POINT('Ctrl Pts',(-0.108251176547647,3.22097706971161,
29.3803186552264));
#19850=CARTESIAN_POINT('Ctrl Pts',(-0.125387452674089,3.22035550354695,
29.38138215616));
#19851=CARTESIAN_POINT('Ctrl Pts',(-0.198333773731072,3.2171264843759,29.3859292906803));
#19852=CARTESIAN_POINT('Ctrl Pts',(-0.254073125289005,3.21320483610382,
29.3894539024931));
#19853=CARTESIAN_POINT('Ctrl Pts',(-0.400671620884013,3.19905243871314,
29.3988621017981));
#19854=CARTESIAN_POINT('Ctrl Pts',(-0.49124109159605,3.18640141235104,29.4048164260533));
#19855=CARTESIAN_POINT('Ctrl Pts',(-0.824309834902664,3.12533962759615,
29.4272117624473));
#19856=CARTESIAN_POINT('Ctrl Pts',(-1.06151258024309,3.05293462985347,29.4442280392737));
#19857=CARTESIAN_POINT('Ctrl Pts',(-1.36931872167645,2.91872148500965,29.4665401409083));
#19858=CARTESIAN_POINT('Ctrl Pts',(-1.44905421151699,2.87996768340037,29.472332954282));
#19859=CARTESIAN_POINT('Ctrl Pts',(-1.53925768142025,2.83142967827752,29.478820287786));
#19860=CARTESIAN_POINT('Ctrl Pts',(-1.5513754705336,2.82480838258828,29.4796903505045));
#19861=CARTESIAN_POINT('Ctrl Pts',(-1.5696146349845,2.81468953000495,29.480997324202));
#19862=CARTESIAN_POINT('Ctrl Pts',(-1.57576752290986,2.81124953866858,29.481437773699));
#19863=CARTESIAN_POINT('Ctrl Pts',(-1.58676994787959,2.80505076999256,29.4822244946813));
#19864=CARTESIAN_POINT('Ctrl Pts',(-1.59162363381234,2.80229957348605,29.4825712422186));
#19865=CARTESIAN_POINT('Ctrl Pts',(-1.60213656782863,2.79630444133275,29.4833216007648));
#19866=CARTESIAN_POINT('Ctrl Pts',(-1.60779310213573,2.79305593447331,29.4837249105969));
#19867=CARTESIAN_POINT('Ctrl Pts',(-1.62361447085714,2.78390584659214,29.4848518927007));
#19868=CARTESIAN_POINT('Ctrl Pts',(-1.63375706294691,2.77796572726383,29.4855731142718));
#19869=CARTESIAN_POINT('Ctrl Pts',(-1.69350980301012,2.74253043790169,29.489815984749));
#19870=CARTESIAN_POINT('Ctrl Pts',(-1.74235631050502,2.71176033250252,29.4932597525121));
#19871=CARTESIAN_POINT('Ctrl Pts',(-2.00065102691814,2.53918874729656,29.5114830729581));
#19872=CARTESIAN_POINT('Ctrl Pts',(-2.19369724152766,2.37440579334918,29.5252106547641));
#19873=CARTESIAN_POINT('Ctrl Pts',(-2.47646698755928,2.06879805338074,29.548731441992));
#19874=CARTESIAN_POINT('Ctrl Pts',(-2.57813864954197,1.94061970938887,29.558148215819));
#19875=CARTESIAN_POINT('Ctrl Pts',(-2.68191255561879,1.78716030795524,29.5692907602122));
#19876=CARTESIAN_POINT('Ctrl Pts',(-2.69399176085513,1.76889945404617,29.5706143796169));
#19877=CARTESIAN_POINT('Ctrl Pts',(-2.71299398607165,1.73952652931348,29.5727405214983));
#19878=CARTESIAN_POINT('Ctrl Pts',(-2.72003711778324,1.72849269150688,29.5735385479879));
#19879=CARTESIAN_POINT('Ctrl Pts',(-2.73238369020971,1.70888809189005,29.5749554536819));
#19880=CARTESIAN_POINT('Ctrl Pts',(-2.73771454344464,1.70033473647812,29.5755733048334));
#19881=CARTESIAN_POINT('Ctrl Pts',(-2.74870036211992,1.68252238851788,29.5768593539146));
#19882=CARTESIAN_POINT('Ctrl Pts',(-2.75434886209182,1.67325957635592,29.577527780018));
#19883=CARTESIAN_POINT('Ctrl Pts',(-2.76881903952392,1.64925853776594,29.5792589521897));
#19884=CARTESIAN_POINT('Ctrl Pts',(-2.77756976598455,1.63447813527753,29.5803242773644));
#19885=CARTESIAN_POINT('Ctrl Pts',(-2.81441290685011,1.5710979148245,29.5848897864165));
#19886=CARTESIAN_POINT('Ctrl Pts',(-2.84134968918131,1.52184098136778,29.5884313616665));
#19887=CARTESIAN_POINT('Ctrl Pts',(-2.90901258580667,1.39004707684882,29.5978963495169));
#19888=CARTESIAN_POINT('Ctrl Pts',(-2.94751120579408,1.30643035158349,29.6038915654883));
#19889=CARTESIAN_POINT('Ctrl Pts',(-3.07400896998979,0.99752342459847,29.625974800896));
#19890=CARTESIAN_POINT('Ctrl Pts',(-3.14015841323614,0.764182201518884,
29.6426030850781));
#19891=CARTESIAN_POINT('Ctrl Pts',(-3.19473614475354,0.434049400776789,
29.6648717052604));
#19892=CARTESIAN_POINT('Ctrl Pts',(-3.20591589905586,0.341825482980683,
29.6709511967882));
#19893=CARTESIAN_POINT('Ctrl Pts',(-3.2141770306316,0.235325972411949,29.6777174937204));
#19894=CARTESIAN_POINT('Ctrl Pts',(-3.21516589940946,0.221405856701903,
29.6785968949952));
#19895=CARTESIAN_POINT('Ctrl Pts',(-3.21652017215728,0.200413763289398,
29.6799150992434));
#19896=CARTESIAN_POINT('Ctrl Pts',(-3.21695272392094,0.193346499172079,
29.6803575298326));
#19897=CARTESIAN_POINT('Ctrl Pts',(-3.21768460241923,0.180705603581696,
29.6811463839373));
#19898=CARTESIAN_POINT('Ctrl Pts',(-3.21799274311681,0.175132585882723,
29.6814932945891));
#19899=CARTESIAN_POINT('Ctrl Pts',(-3.21862838948232,0.163067781524378,
29.682242408471));
#19900=CARTESIAN_POINT('Ctrl Pts',(-3.21895073380752,0.156575815615226,
29.6826443191391));
#19901=CARTESIAN_POINT('Ctrl Pts',(-3.21979588877823,0.138447375079245,
29.6837634450653));
#19902=CARTESIAN_POINT('Ctrl Pts',(-3.22027526303739,0.126808836387373,
29.6844782644303));
#19903=CARTESIAN_POINT('Ctrl Pts',(-3.22269088586834,0.0592554099718082,
29.6886073424715));
#19904=CARTESIAN_POINT('Ctrl Pts',(-3.22323405306892,0.00329651312935113,
29.6919485097842));
#19905=CARTESIAN_POINT('Ctrl Pts',(-3.21816668937871,-0.306828167702081,
29.7101654024707));
#19906=CARTESIAN_POINT('Ctrl Pts',(-3.18395454746291,-0.559643820509983,
29.723960319426));
#19907=CARTESIAN_POINT('Ctrl Pts',(-3.079361943721,-0.96465228794684,29.7475867180965));
#19908=CARTESIAN_POINT('Ctrl Pts',(-3.026286824543,-1.12008999879813,29.7570385346208));
#19909=CARTESIAN_POINT('Ctrl Pts',(-2.95297955811983,-1.29093346616297,
29.7682202766622));
#19910=CARTESIAN_POINT('Ctrl Pts',(-2.94413621208154,-1.31097651128621,
29.7695446616785));
#19911=CARTESIAN_POINT('Ctrl Pts',(-2.9296818711405,-1.34285261538615,29.7716718010717));
#19912=CARTESIAN_POINT('Ctrl Pts',(-2.92420180454128,-1.35474455566887,
29.7724700527126));
#19913=CARTESIAN_POINT('Ctrl Pts',(-2.91437540815084,-1.37573076338613,
29.7738872189485));
#19914=CARTESIAN_POINT('Ctrl Pts',(-2.9100585735824,-1.38483870815884,29.7745051042296));
#19915=CARTESIAN_POINT('Ctrl Pts',(-2.90100723800875,-1.40370660688985,
29.7757910855052));
#19916=CARTESIAN_POINT('Ctrl Pts',(-2.89626604918457,-1.41346319405193,
29.7764594089833));
#19917=CARTESIAN_POINT('Ctrl Pts',(-2.8838936670672,-1.43859989601201,29.7781900168559));
#19918=CARTESIAN_POINT('Ctrl Pts',(-2.87618873774572,-1.4539431454608,29.7792548771685));
#19919=CARTESIAN_POINT('Ctrl Pts',(-2.84280108237013,-1.51912577303895,
29.7838156968553));
#19920=CARTESIAN_POINT('Ctrl Pts',(-2.81594398727527,-1.56834942905493,
29.7873529419509));
#19921=CARTESIAN_POINT('Ctrl Pts',(-2.74172967717129,-1.69631220044069,
29.7968034217194));
#19922=CARTESIAN_POINT('Ctrl Pts',(-2.69226844888869,-1.77376570788618,
29.8027881863976));
#19923=CARTESIAN_POINT('Ctrl Pts',(-2.49992934405106,-2.04834321412894,
29.8249649056176));
#19924=CARTESIAN_POINT('Ctrl Pts',(-2.33817105111614,-2.23120992218163,
29.8417071376863));
#19925=CARTESIAN_POINT('Ctrl Pts',(-2.08936213317222,-2.45541594605325,
29.8639860290489));
#19926=CARTESIAN_POINT('Ctrl Pts',(-2.01875212402243,-2.51379092722465,
29.8699787600656));
#19927=CARTESIAN_POINT('Ctrl Pts',(-1.93465462152868,-2.57748377393532,
29.8766608143329));
#19928=CARTESIAN_POINT('Ctrl Pts',(-1.92350976937498,-2.58581153471196,
29.8775374961406));
#19929=CARTESIAN_POINT('Ctrl Pts',(-1.90661924858856,-2.5982629979883,29.8788524311));
#19930=CARTESIAN_POINT('Ctrl Pts',(-1.90091353298779,-2.60244026025053,
29.8792942858187));
#19931=CARTESIAN_POINT('Ctrl Pts',(-1.8906802196346,-2.60988065150266,29.8800825186397));
#19932=CARTESIAN_POINT('Ctrl Pts',(-1.8861578684914,-2.61315081935606,29.880429380658));
#19933=CARTESIAN_POINT('Ctrl Pts',(-1.87634459448594,-2.62020817107423,
29.8811788507798));
#19934=CARTESIAN_POINT('Ctrl Pts',(-1.87105070652266,-2.62399107323361,
29.8815811638383));
#19935=CARTESIAN_POINT('Ctrl Pts',(-1.85622298900629,-2.63451896254672,
29.8827025474526));
#19936=CARTESIAN_POINT('Ctrl Pts',(-1.84666378497292,-2.64122827940597,
29.8834192064229));
#19937=CARTESIAN_POINT('Ctrl Pts',(-1.7906882474572,-2.6800633699564,29.8875805671746));
#19938=CARTESIAN_POINT('Ctrl Pts',(-1.74346759721204,-2.71101931098909,
29.8909508350776));
#19939=CARTESIAN_POINT('Ctrl Pts',(-1.62366007748064,-2.78513420718741,
29.8992222652674));
#19940=CARTESIAN_POINT('Ctrl Pts',(-1.5502013178676,-2.82667638698033,29.9040479009646));
#19941=CARTESIAN_POINT('Ctrl Pts',(-1.4752551445451,-2.86526435446945,29.9088139162969));
#19942=CARTESIAN_POINT('Origin',(0.,0.,4.68922655072688));
#19943=CARTESIAN_POINT('',(-1.47525569888183,-2.86526406905484,31.4041249682223));
#19944=CARTESIAN_POINT('',(-1.47525540353836,-2.86526422112008,31.1543403726568));
#19945=CARTESIAN_POINT('',(-1.47525540501186,-2.86526422036142,4.68922655072688));
#19946=CARTESIAN_POINT('Ctrl Pts',(-1.47525569888183,-2.86526406905484,
31.4041249682223));
#19947=CARTESIAN_POINT('Ctrl Pts',(-1.54049706273102,-2.83167285669126,
31.4000144140638));
#19948=CARTESIAN_POINT('Ctrl Pts',(-1.60460828957561,-2.79584454116413,
31.3958833098916));
#19949=CARTESIAN_POINT('Ctrl Pts',(-1.74615649069285,-2.71026000447311,
31.3864664849392));
#19950=CARTESIAN_POINT('Ctrl Pts',(-1.8227617937159,-2.65934377138192,31.3811594019167));
#19951=CARTESIAN_POINT('Ctrl Pts',(-1.94243829536211,-2.57219732526237,
31.3724297982344));
#19952=CARTESIAN_POINT('Ctrl Pts',(-1.98692227495442,-2.5379922986544,31.3690808157502));
#19953=CARTESIAN_POINT('Ctrl Pts',(-2.04382805416653,-2.49182252769639,
31.3646464561045));
#19954=CARTESIAN_POINT('Ctrl Pts',(-2.0570802935324,-2.48089364397653,31.363602795394));
#19955=CARTESIAN_POINT('Ctrl Pts',(-2.07856103402427,-2.46288841685041,
31.3618927513368));
#19956=CARTESIAN_POINT('Ctrl Pts',(-2.08684238861338,-2.45587543791435,
31.3612289668083));
#19957=CARTESIAN_POINT('Ctrl Pts',(-2.10274938745271,-2.44226620881424,
31.3599451144795));
#19958=CARTESIAN_POINT('Ctrl Pts',(-2.11037981649738,-2.43567572709953,
31.3593252898474));
#19959=CARTESIAN_POINT('Ctrl Pts',(-2.12785095248667,-2.42044199073886,
31.3578968542589));
#19960=CARTESIAN_POINT('Ctrl Pts',(-2.13767009626727,-2.41177437956257,
31.357087230298));
#19961=CARTESIAN_POINT('Ctrl Pts',(-2.16377429672397,-2.38844687315969,
31.3549163736471));
#19962=CARTESIAN_POINT('Ctrl Pts',(-2.17996291368153,-2.37368054500649,
31.3535506586662));
#19963=CARTESIAN_POINT('Ctrl Pts',(-2.31603995033572,-2.24699267417088,
31.341902368894));
#19964=CARTESIAN_POINT('Ctrl Pts',(-2.42735533987515,-2.12625220959061,
31.3312318054368));
#19965=CARTESIAN_POINT('Ctrl Pts',(-2.68674547701507,-1.79785815037375,
31.3033194410212));
#19966=CARTESIAN_POINT('Ctrl Pts',(-2.8202812194864,-1.58015958259838,31.2857496387808));
#19967=CARTESIAN_POINT('Ctrl Pts',(-2.95013811989943,-1.29842478745623,
31.2654618482006));
#19968=CARTESIAN_POINT('Ctrl Pts',(-2.97214620391831,-1.24722479423274,
31.2618697520665));
#19969=CARTESIAN_POINT('Ctrl Pts',(-2.99713367544048,-1.1846698729509,31.2576161779332));
#19970=CARTESIAN_POINT('Ctrl Pts',(-3.00139183226039,-1.17383987635848,
31.2568845950233));
#19971=CARTESIAN_POINT('Ctrl Pts',(-3.00793651343244,-1.15692598202071,
31.2557498126236));
#19972=CARTESIAN_POINT('Ctrl Pts',(-3.01026340255732,-1.15085796070127,
31.2553442516362));
#19973=CARTESIAN_POINT('Ctrl Pts',(-3.01455545987411,-1.13956312768473,
31.2545922926781));
#19974=CARTESIAN_POINT('Ctrl Pts',(-3.01652537991746,-1.13433829859165,
31.2542456196517));
#19975=CARTESIAN_POINT('Ctrl Pts',(-3.02096498219883,-1.12246976560065,
31.2534607642309));
#19976=CARTESIAN_POINT('Ctrl Pts',(-3.0234263275321,-1.11582303373404,31.253023083904));
#19977=CARTESIAN_POINT('Ctrl Pts',(-3.03067807514303,-1.09603990659993,
31.2517257621092));
#19978=CARTESIAN_POINT('Ctrl Pts',(-3.03540500891705,-1.08288019664208,
31.2508698150855));
#19979=CARTESIAN_POINT('Ctrl Pts',(-3.07111359810302,-0.981396798428517,
31.2443199610372));
#19980=CARTESIAN_POINT('Ctrl Pts',(-3.09832295956663,-0.891782936280663,
31.2388316999514));
#19981=CARTESIAN_POINT('Ctrl Pts',(-3.18146583494294,-0.567806714320533,
31.2196163521395));
#19982=CARTESIAN_POINT('Ctrl Pts',(-3.21499791107935,-0.328527242136726,
31.2065163718238));
#19983=CARTESIAN_POINT('Ctrl Pts',(-3.22406238880603,0.0043147249046562,
31.1875618446388));
#19984=CARTESIAN_POINT('Ctrl Pts',(-3.2226227795599,0.096422956578223,31.182247215611));
#19985=CARTESIAN_POINT('Ctrl Pts',(-3.21395960204302,0.244409437609208,
31.1735063337456));
#19986=CARTESIAN_POINT('Ctrl Pts',(-3.20921208528118,0.300382273167392,
31.1701538681618));
#19987=CARTESIAN_POINT('Ctrl Pts',(-3.20110541513175,0.373278676709265,
31.1657155381103));
#19988=CARTESIAN_POINT('Ctrl Pts',(-3.19906959685009,0.390341576046077,
31.1646714850309));
#19989=CARTESIAN_POINT('Ctrl Pts',(-3.19552548077266,0.418153391734688,
31.1629609595805));
#19990=CARTESIAN_POINT('Ctrl Pts',(-3.19409914914591,0.428912553039472,
31.1622970888515));
#19991=CARTESIAN_POINT('Ctrl Pts',(-3.19124306187078,0.449652010736602,
31.1610131832165));
#19992=CARTESIAN_POINT('Ctrl Pts',(-3.18982076472645,0.45963321891602,31.1603933920889));
#19993=CARTESIAN_POINT('Ctrl Pts',(-3.18644363235984,0.482561910714854,
31.1589651962708));
#19994=CARTESIAN_POINT('Ctrl Pts',(-3.18445668596398,0.495504416694939,
31.1581557796873));
#19995=CARTESIAN_POINT('Ctrl Pts',(-3.17893589646574,0.530060130984325,
31.1559858406746));
#19996=CARTESIAN_POINT('Ctrl Pts',(-3.17526057334678,0.551649734347801,
31.1546208419077));
#19997=CARTESIAN_POINT('Ctrl Pts',(-3.1422953499445,0.734037756801617,31.1430088904198));
#19998=CARTESIAN_POINT('Ctrl Pts',(-3.10103669955303,0.892405907189711,
31.132376742876));
#19999=CARTESIAN_POINT('Ctrl Pts',(-2.96565101060818,1.28655298327257,31.1045839755335));
#20000=CARTESIAN_POINT('Ctrl Pts',(-2.85538558413461,1.51560965706892,31.0870977927304));
#20001=CARTESIAN_POINT('Ctrl Pts',(-2.68869285935838,1.77773195480971,31.0667650693938));
#20002=CARTESIAN_POINT('Ctrl Pts',(-2.65666160965921,1.82525347509511,31.0630687227994));
#20003=CARTESIAN_POINT('Ctrl Pts',(-2.61656374430491,1.8814487418211,31.0587089212942));
#20004=CARTESIAN_POINT('Ctrl Pts',(-2.60969727513731,1.89096148512838,31.0579712959332));
#20005=CARTESIAN_POINT('Ctrl Pts',(-2.59893438391404,1.90570200565681,31.0568292062978));
#20006=CARTESIAN_POINT('Ctrl Pts',(-2.59507386988263,1.91095569752275,31.0564223320511));
#20007=CARTESIAN_POINT('Ctrl Pts',(-2.58787856888038,1.92068561490598,31.055669185379));
#20008=CARTESIAN_POINT('Ctrl Pts',(-2.58454812680498,1.92516484996496,31.0553226300729));
#20009=CARTESIAN_POINT('Ctrl Pts',(-2.57697912184891,1.93528964331584,31.0545396248657));
#20010=CARTESIAN_POINT('Ctrl Pts',(-2.57273364691588,1.94092992718386,31.0541036671901));
#20011=CARTESIAN_POINT('Ctrl Pts',(-2.56010427991879,1.95759430307416,31.0528161688916));
#20012=CARTESIAN_POINT('Ctrl Pts',(-2.55166769308742,1.96857851748845,31.0519682403198));
#20013=CARTESIAN_POINT('Ctrl Pts',(-2.4880820055722,2.05026981782221,31.0456645919791));
#20014=CARTESIAN_POINT('Ctrl Pts',(-2.43006868209291,2.11870898558736,31.0403974542612));
#20015=CARTESIAN_POINT('Ctrl Pts',(-2.20264746053282,2.36534967227088,31.0210872459879));
#20016=CARTESIAN_POINT('Ctrl Pts',(-2.01589314191846,2.52640532284587,31.0077341262375));
#20017=CARTESIAN_POINT('Ctrl Pts',(-1.7369210814528,2.71617524019865,30.9885225928932));
#20018=CARTESIAN_POINT('Ctrl Pts',(-1.65905174396757,2.76442546979597,30.9832362985634));
#20019=CARTESIAN_POINT('Ctrl Pts',(-1.53047184248708,2.83670639101246,30.9745377745647));
#20020=CARTESIAN_POINT('Ctrl Pts',(-1.48100262988593,2.86284436320936,30.9711983993155));
#20021=CARTESIAN_POINT('Ctrl Pts',(-1.41550513974602,2.89529915609879,30.9667749924335));
#20022=CARTESIAN_POINT('Ctrl Pts',(-1.40006953146704,2.90279473840227,30.9657324159737));
#20023=CARTESIAN_POINT('Ctrl Pts',(-1.37477928726068,2.91482712197039,30.964023702122));
#20024=CARTESIAN_POINT('Ctrl Pts',(-1.36496017315769,2.91943812415988,30.9633601557511));
#20025=CARTESIAN_POINT('Ctrl Pts',(-1.34596882389628,2.92823960346182,30.9620764502105));
#20026=CARTESIAN_POINT('Ctrl Pts',(-1.33679982089459,2.93243678283953,30.9614565325207));
#20027=CARTESIAN_POINT('Ctrl Pts',(-1.31566848609356,2.94199010561221,30.9600274321575));
#20028=CARTESIAN_POINT('Ctrl Pts',(-1.30369293757034,2.94731641721606,30.9592172333981));
#20029=CARTESIAN_POINT('Ctrl Pts',(-1.2715820962703,2.96136421675292,30.9570438325861));
#20030=CARTESIAN_POINT('Ctrl Pts',(-1.25138993735685,2.9699532383585,30.9556761317178));
#20031=CARTESIAN_POINT('Ctrl Pts',(-1.07807091397471,3.0415956560808,30.9439259803328));
#20032=CARTESIAN_POINT('Ctrl Pts',(-0.920406057871046,3.09295628540771,
30.9331476492001));
#20033=CARTESIAN_POINT('Ctrl Pts',(-0.508391983690069,3.19287117832151,
30.904858124988));
#20034=CARTESIAN_POINT('Ctrl Pts',(-0.250868985372037,3.22334449882516,
30.8870089342507));
#20035=CARTESIAN_POINT('Ctrl Pts',(0.0582938486393527,3.22262268236336,
30.8668480082903));
#20036=CARTESIAN_POINT('Ctrl Pts',(0.10905700270632,3.22130445347779,30.8635819177435));
#20037=CARTESIAN_POINT('Ctrl Pts',(0.171073999725646,3.21822611402835,30.8596626680382));
#20038=CARTESIAN_POINT('Ctrl Pts',(0.182374135131546,3.21760552557616,30.8589514272067));
#20039=CARTESIAN_POINT('Ctrl Pts',(0.200088061438667,3.21653908083966,30.8578412718011));
#20040=CARTESIAN_POINT('Ctrl Pts',(0.206504055790797,3.21613354317833,30.8574401558536));
#20041=CARTESIAN_POINT('Ctrl Pts',(0.218499544670998,3.21533929656842,30.8566921133601));
#20042=CARTESIAN_POINT('Ctrl Pts',(0.224079178379036,3.21495526648418,30.8563449384982));
#20043=CARTESIAN_POINT('Ctrl Pts',(0.236829158162078,3.21404436832022,30.8555533498293));
#20044=CARTESIAN_POINT('Ctrl Pts',(0.243998746662671,3.21350803105829,30.8551094734122));
#20045=CARTESIAN_POINT('Ctrl Pts',(0.266089974185052,3.21178108801797,30.8537454748703));
#20046=CARTESIAN_POINT('Ctrl Pts',(0.281005411508791,3.21051049063543,30.8528297308612));
#20047=CARTESIAN_POINT('Ctrl Pts',(0.430928253530235,3.1966862288378,30.8436725143295));
#20048=CARTESIAN_POINT('Ctrl Pts',(0.565042596116501,3.17572641435453,30.8358654207246));
#20049=CARTESIAN_POINT('Ctrl Pts',(0.881951424925628,3.10547770356722,30.8175139443786));
#20050=CARTESIAN_POINT('Ctrl Pts',(1.06249494998204,3.04843178168042,30.8071207834093));
#20051=CARTESIAN_POINT('Ctrl Pts',(1.32719462947861,2.93840302586508,30.7908435446531));
#20052=CARTESIAN_POINT('Ctrl Pts',(1.41563049331865,2.89683378837911,30.7852204827145));
#20053=CARTESIAN_POINT('Ctrl Pts',(1.55385759683216,2.82401745936542,30.7760201045856));
#20054=CARTESIAN_POINT('Ctrl Pts',(1.60492094477216,2.79531324724433,30.7725271622462));
#20055=CARTESIAN_POINT('Ctrl Pts',(1.67013783343983,2.75627673126546,30.7679289231176));
#20056=CARTESIAN_POINT('Ctrl Pts',(1.68503088304417,2.74719724566579,30.7668693605738));
#20057=CARTESIAN_POINT('Ctrl Pts',(1.70911854077668,2.73224274398326,30.7651397996345));
#20058=CARTESIAN_POINT('Ctrl Pts',(1.71835843647854,2.72644106439706,30.7644725154302));
#20059=CARTESIAN_POINT('Ctrl Pts',(1.73606338099305,2.71519847485267,30.7631864263824));
#20060=CARTESIAN_POINT('Ctrl Pts',(1.74453276832865,2.70976460919209,30.7625678891817));
#20061=CARTESIAN_POINT('Ctrl Pts',(1.76385788737466,2.69723767452166,30.7611488423101));
#20062=CARTESIAN_POINT('Ctrl Pts',(1.77469648085034,2.69011860568836,30.7603473631959));
#20063=CARTESIAN_POINT('Ctrl Pts',(1.80336345908475,2.67104074401438,30.7582124483637));
#20064=CARTESIAN_POINT('Ctrl Pts',(1.82111558333641,2.65896905169235,30.7568747606541));
#20065=CARTESIAN_POINT('Ctrl Pts',(1.95773006115948,2.56405945033691,30.7464567432735));
#20066=CARTESIAN_POINT('Ctrl Pts',(2.07098836663216,2.47348028582223,30.7370766980317));
#20067=CARTESIAN_POINT('Ctrl Pts',(2.33146681896542,2.23469487041166,30.7136373847543));
#20068=CARTESIAN_POINT('Ctrl Pts',(2.47113258664423,2.07920484032101,30.6993659779647));
#20069=CARTESIAN_POINT('Ctrl Pts',(2.64268674453016,1.84630635200738,30.679974775298));
#20070=CARTESIAN_POINT('Ctrl Pts',(2.68812795877596,1.77949719303746,30.6746168887248));
#20071=CARTESIAN_POINT('Ctrl Pts',(2.75354887707876,1.67507842042336,30.6666233229205));
#20072=CARTESIAN_POINT('Ctrl Pts',(2.7753725972629,1.63866607136462,30.6639032197766));
#20073=CARTESIAN_POINT('Ctrl Pts',(2.80178477506933,1.59255577540493,30.6605520964186));
#20074=CARTESIAN_POINT('Ctrl Pts',(2.80705167734764,1.58325383684642,30.6598807474611));
#20075=CARTESIAN_POINT('Ctrl Pts',(2.81534415602522,1.56843693169881,30.6588189927131));
#20076=CARTESIAN_POINT('Ctrl Pts',(2.81839998076755,1.5629391144897,30.6584266858936));
#20077=CARTESIAN_POINT('Ctrl Pts',(2.82415556812372,1.55251230976243,30.6576858473924));
#20078=CARTESIAN_POINT('Ctrl Pts',(2.82685849974318,1.54758526995826,30.6573371217821));
#20079=CARTESIAN_POINT('Ctrl Pts',(2.8330421339967,1.53624317590814,30.6565374057121));
#20080=CARTESIAN_POINT('Ctrl Pts',(2.83651394110666,1.52982335349463,30.6560869855057));
#20081=CARTESIAN_POINT('Ctrl Pts',(2.84574430403583,1.51261576489752,30.6548855001183));
#20082=CARTESIAN_POINT('Ctrl Pts',(2.85146338551973,1.501806801233,30.6541368745573));
#20083=CARTESIAN_POINT('Ctrl Pts',(2.89345264334473,1.42134323672057,30.6486070921127));
#20084=CARTESIAN_POINT('Ctrl Pts',(2.92723075776941,1.35040997656245,30.6439708702697));
#20085=CARTESIAN_POINT('Ctrl Pts',(3.04832021717778,1.07017268621329,30.6262973206752));
#20086=CARTESIAN_POINT('Ctrl Pts',(3.11604440259237,0.853116488909561,30.6139241494622));
#20087=CARTESIAN_POINT('Ctrl Pts',(3.19318041282869,0.466611307229636,30.5916712309533));
#20088=CARTESIAN_POINT('Ctrl Pts',(3.2130969796351,0.300206582904236,30.5820298296068));
#20089=CARTESIAN_POINT('Ctrl Pts',(3.22096377766471,0.109777502715783,30.5705568331624));
#20090=CARTESIAN_POINT('Ctrl Pts',(3.22167227122581,0.0865245070454551,
30.5691488248579));
#20091=CARTESIAN_POINT('Ctrl Pts',(3.2223679454749,0.0510940992607525,30.566991920158));
#20092=CARTESIAN_POINT('Ctrl Pts',(3.22253796761573,0.0389207383701022,
30.566248768067));
#20093=CARTESIAN_POINT('Ctrl Pts',(3.2227136708738,0.0177508262931659,30.5649526866344));
#20094=CARTESIAN_POINT('Ctrl Pts',(3.22275066524682,0.00875461658659629,
30.5644007476076));
#20095=CARTESIAN_POINT('Ctrl Pts',(3.2227491527339,-0.0114245863545412,
30.5631600379063));
#20096=CARTESIAN_POINT('Ctrl Pts',(3.22269010644003,-0.0226074196351687,
30.5624706285465));
#20097=CARTESIAN_POINT('Ctrl Pts',(3.22237706742979,-0.0524624874323674,
30.5606250826662));
#20098=CARTESIAN_POINT('Ctrl Pts',(3.22201898686414,-0.0711329874130248,
30.5594656924567));
#20099=CARTESIAN_POINT('Ctrl Pts',(3.21950594560912,-0.161287200730689,
30.5538412841109));
#20100=CARTESIAN_POINT('Ctrl Pts',(3.21513434264981,-0.232684209076111,
30.5493072526171));
#20101=CARTESIAN_POINT('Ctrl Pts',(3.18314952522559,-0.570391177725851,
30.5274655471515));
#20102=CARTESIAN_POINT('Ctrl Pts',(3.12479772400483,-0.832695382683397,
30.5092072556514));
#20103=CARTESIAN_POINT('Ctrl Pts',(2.98780638003923,-1.21595981197791,30.4817858873665));
#20104=CARTESIAN_POINT('Ctrl Pts',(2.93242147285564,-1.34404571259879,30.4725114262139));
#20105=CARTESIAN_POINT('Ctrl Pts',(2.86207593314905,-1.48150730125619,30.4627203838548));
#20106=CARTESIAN_POINT('Ctrl Pts',(2.85514973213737,-1.49481188059214,30.4617745474452));
#20107=CARTESIAN_POINT('Ctrl Pts',(2.84476370194231,-1.51442689362191,30.4603833321143));
#20108=CARTESIAN_POINT('Ctrl Pts',(2.84137533746258,-1.52077464801888,30.4599336162215));
#20109=CARTESIAN_POINT('Ctrl Pts',(2.8353152461268,-1.53203665224649,30.4591367151749));
#20110=CARTESIAN_POINT('Ctrl Pts',(2.83265196154433,-1.53695533936767,30.4587890027692));
#20111=CARTESIAN_POINT('Ctrl Pts',(2.82690195247177,-1.54750902830305,30.4580436745375));
#20112=CARTESIAN_POINT('Ctrl Pts',(2.82381118769628,-1.55314172550802,30.4576463221048));
#20113=CARTESIAN_POINT('Ctrl Pts',(2.81523830804946,-1.56865499986002,30.4565530736595));
#20114=CARTESIAN_POINT('Ctrl Pts',(2.80972097959947,-1.57851615935056,30.4558593959542));
#20115=CARTESIAN_POINT('Ctrl Pts',(2.779255255878,-1.63230191652864,30.4520816209732));
#20116=CARTESIAN_POINT('Ctrl Pts',(2.75332709287934,-1.67566700257382,30.4490568307441));
#20117=CARTESIAN_POINT('Ctrl Pts',(2.58851219322617,-1.9371588184228,30.4308348997187));
#20118=CARTESIAN_POINT('Ctrl Pts',(2.42479647900398,-2.13854444366878,30.416813403412));
#20119=CARTESIAN_POINT('Ctrl Pts',(2.11958316106935,-2.43329622748664,30.3928574525194));
#20120=CARTESIAN_POINT('Ctrl Pts',(1.99173330265579,-2.5390059179462,30.383316334553));
#20121=CARTESIAN_POINT('Ctrl Pts',(1.838397560125,-2.64705374646689,30.3720343478765));
#20122=CARTESIAN_POINT('Ctrl Pts',(1.8203308608015,-2.65951022680665,30.3707077322552));
#20123=CARTESIAN_POINT('Ctrl Pts',(1.79127237559914,-2.67911041881263,30.3685775453819));
#20124=CARTESIAN_POINT('Ctrl Pts',(1.78036157415552,-2.68637339494712,30.3677784956791));
#20125=CARTESIAN_POINT('Ctrl Pts',(1.76097861270702,-2.69910607004278,30.3663602319654));
#20126=CARTESIAN_POINT('Ctrl Pts',(1.75252446740648,-2.70460297256803,30.3657420509058));
#20127=CARTESIAN_POINT('Ctrl Pts',(1.73492274372522,-2.71593046823951,30.3644557714514));
#20128=CARTESIAN_POINT('Ctrl Pts',(1.72577125871732,-2.72175472682334,30.3637874469982));
#20129=CARTESIAN_POINT('Ctrl Pts',(1.70206890478329,-2.73667195952448,30.3620575159931));
#20130=CARTESIAN_POINT('Ctrl Pts',(1.68747465287437,-2.7456950391897,30.3609933389918));
#20131=CARTESIAN_POINT('Ctrl Pts',(1.62499990890735,-2.78363459208889,30.356441510777));
#20132=CARTESIAN_POINT('Ctrl Pts',(1.57644539967755,-2.81141699422034,30.3529127834915));
#20133=CARTESIAN_POINT('Ctrl Pts',(1.44657510623723,-2.88130522581978,30.343491399806));
#20134=CARTESIAN_POINT('Ctrl Pts',(1.36414987205505,-2.92123124314398,30.3375277729438));
#20135=CARTESIAN_POINT('Ctrl Pts',(1.05434274108739,-3.05532593201959,30.3151995017479));
#20136=CARTESIAN_POINT('Ctrl Pts',(0.818117910257989,-3.12687108220597,
30.298267348129));
#20137=CARTESIAN_POINT('Ctrl Pts',(0.488009825825243,-3.18684390698463,
30.2759664506942));
#20138=CARTESIAN_POINT('Ctrl Pts',(0.399314636015608,-3.1991684353077,30.2701133695743));
#20139=CARTESIAN_POINT('Ctrl Pts',(0.296433884548542,-3.20911766110724,
30.2635670281546));
#20140=CARTESIAN_POINT('Ctrl Pts',(0.282645724258407,-3.21036144717234,
30.2626947095551));
#20141=CARTESIAN_POINT('Ctrl Pts',(0.261816170163801,-3.21210517770268,
30.2613849321946));
#20142=CARTESIAN_POINT('Ctrl Pts',(0.254780655932871,-3.21267088249002,
30.260943914004));
#20143=CARTESIAN_POINT('Ctrl Pts',(0.242178158558334,-3.21364255269438,
30.2601564715131));
#20144=CARTESIAN_POINT('Ctrl Pts',(0.236611948808043,-3.21405717189382,
30.2598095685211));
#20145=CARTESIAN_POINT('Ctrl Pts',(0.224540875129676,-3.21492480071507,
30.2590592023079));
#20146=CARTESIAN_POINT('Ctrl Pts',(0.218035724807319,-3.21537252948138,
30.2586560387003));
#20147=CARTESIAN_POINT('Ctrl Pts',(0.199818324534206,-3.21657083514405,
30.257530276326));
#20148=CARTESIAN_POINT('Ctrl Pts',(0.188103126212695,-3.21727719105762,
30.2568101186542));
#20149=CARTESIAN_POINT('Ctrl Pts',(0.119100684118839,-3.22105942829446,
30.2525893598998));
#20150=CARTESIAN_POINT('Ctrl Pts',(0.0617394618062305,-3.22266938956621,
30.2491656866355));
#20151=CARTESIAN_POINT('Ctrl Pts',(-0.248902013345923,-3.22308983224044,
30.2309381426778));
#20152=CARTESIAN_POINT('Ctrl Pts',(-0.501346255244765,-3.19357775135259,
30.2171926214421));
#20153=CARTESIAN_POINT('Ctrl Pts',(-0.906700856111815,-3.09688779334011,
30.193651224675));
#20154=CARTESIAN_POINT('Ctrl Pts',(-1.0625173357958,-3.04694387582986,30.1842334347241));
#20155=CARTESIAN_POINT('Ctrl Pts',(-1.2341504148667,-2.97715802610212,30.173089459085));
#20156=CARTESIAN_POINT('Ctrl Pts',(-1.25435227359172,-2.96870299901701,
30.1717655182531));
#20157=CARTESIAN_POINT('Ctrl Pts',(-1.28649269723778,-2.95486472733944,
30.1696388162053));
#20158=CARTESIAN_POINT('Ctrl Pts',(-1.29848756447217,-2.9496133736288,30.1688405529336));
#20159=CARTESIAN_POINT('Ctrl Pts',(-1.31966087720477,-2.94018951421828,
30.1674231994489));
#20160=CARTESIAN_POINT('Ctrl Pts',(-1.3288524224391,-2.93604673771598,30.1668051377803));
#20161=CARTESIAN_POINT('Ctrl Pts',(-1.34789803597533,-2.92735482013418,
30.1655186223799));
#20162=CARTESIAN_POINT('Ctrl Pts',(-1.35774885287747,-2.92279889938476,
30.1648499401821));
#20163=CARTESIAN_POINT('Ctrl Pts',(-1.38313657176366,-2.91090124890507,
30.1631180419268));
#20164=CARTESIAN_POINT('Ctrl Pts',(-1.39863794910964,-2.90348492778955,
30.1620522443065));
#20165=CARTESIAN_POINT('Ctrl Pts',(-1.43458046966549,-2.88593433101557,
30.1595612713528));
#20166=CARTESIAN_POINT('Ctrl Pts',(-1.4549737214081,-2.87570676985225,30.1581329162072));
#20167=CARTESIAN_POINT('Ctrl Pts',(-1.47525540759407,-2.86526421903189,
30.1566970682534));
#20168=CARTESIAN_POINT('',(3.22274869089678,-0.00290479312253886,30.3149198866253));
#20169=CARTESIAN_POINT('Ctrl Pts',(-1.4752551445451,-2.86526435446945,29.9088139162969));
#20170=CARTESIAN_POINT('Ctrl Pts',(-1.32485372920929,-2.94270239657363,
29.9183783199176));
#20171=CARTESIAN_POINT('Ctrl Pts',(-1.16846286164701,-3.00824305892808,
29.9277144246265));
#20172=CARTESIAN_POINT('Ctrl Pts',(-0.851862684615299,-3.112442056773,29.9465412399396));
#20173=CARTESIAN_POINT('Ctrl Pts',(-0.692562113047588,-3.15171586102294,
29.9559833170831));
#20174=CARTESIAN_POINT('Ctrl Pts',(-0.509374902386215,-3.18231590788476,
29.9671541637009));
#20175=CARTESIAN_POINT('Ctrl Pts',(-0.4877348670029,-3.18570431647154,29.968478336435));
#20176=CARTESIAN_POINT('Ctrl Pts',(-0.453107146559448,-3.19076525292545,
29.9706051992506));
#20177=CARTESIAN_POINT('Ctrl Pts',(-0.440140653869682,-3.19257970650865,
29.971403388468));
#20178=CARTESIAN_POINT('Ctrl Pts',(-0.417173495792871,-3.1956510172556,
29.9728204824632));
#20179=CARTESIAN_POINT('Ctrl Pts',(-0.407177257856685,-3.19694007242823,
29.9734383582769));
#20180=CARTESIAN_POINT('Ctrl Pts',(-0.386409859560162,-3.19951913003204,
29.9747243583272));
#20181=CARTESIAN_POINT('Ctrl Pts',(-0.375637917694197,-3.20080167976545,
29.9753927102387));
#20182=CARTESIAN_POINT('Ctrl Pts',(-0.347798963901124,-3.20397382868587,
29.9771234744598));
#20183=CARTESIAN_POINT('Ctrl Pts',(-0.330723126053853,-3.20578143510953,
29.9781884635707));
#20184=CARTESIAN_POINT('Ctrl Pts',(-0.261600732279352,-3.21254042142824,
29.9825136451671));
#20185=CARTESIAN_POINT('Ctrl Pts',(-0.209454085725985,-3.21636120036841,
29.9858091754865));
#20186=CARTESIAN_POINT('Ctrl Pts',(-0.0723877919872352,-3.22305672261099,
29.9945618329305));
#20187=CARTESIAN_POINT('Ctrl Pts',(0.012588494431664,-3.22384462017334,
30.0000798910321));
#20188=CARTESIAN_POINT('Ctrl Pts',(0.370305917249913,-3.21301839814294,
30.0236731377819));
#20189=CARTESIAN_POINT('Ctrl Pts',(0.640931400912043,-3.17014162748544,
30.0425334838655));
#20190=CARTESIAN_POINT('Ctrl Pts',(0.973906804136973,-3.07296183525789,
30.0654414448459));
#20191=CARTESIAN_POINT('Ctrl Pts',(1.04418499877582,-3.04979810988885,30.0702500252699));
#20192=CARTESIAN_POINT('Ctrl Pts',(1.12491472290792,-3.02007112008365,30.0756944460744));
#20193=CARTESIAN_POINT('Ctrl Pts',(1.13619687186787,-3.01584472133704,30.0764534755096));
#20194=CARTESIAN_POINT('Ctrl Pts',(1.15422461886513,-3.00897583380398,30.0776630728587));
#20195=CARTESIAN_POINT('Ctrl Pts',(1.16098533999302,-3.00637374289373,30.0781159563752));
#20196=CARTESIAN_POINT('Ctrl Pts',(1.17296694083972,-3.00171577612577,30.0789171905565));
#20197=CARTESIAN_POINT('Ctrl Pts',(1.17819129129456,-2.99966903639722,30.0792660827025));
#20198=CARTESIAN_POINT('Ctrl Pts',(1.18928602265496,-2.99528900483679,30.0800059871108));
#20199=CARTESIAN_POINT('Ctrl Pts',(1.19515488423319,-2.99295209959919,30.0803967775628));
#20200=CARTESIAN_POINT('Ctrl Pts',(1.21085322373667,-2.98664768441831,30.0814405670009));
#20201=CARTESIAN_POINT('Ctrl Pts',(1.22067016258588,-2.98264887001018,30.0820917022877));
#20202=CARTESIAN_POINT('Ctrl Pts',(1.26915576276783,-2.96261935430214,30.0853005707879));
#20203=CARTESIAN_POINT('Ctrl Pts',(1.30753127377072,-2.94588393266936,30.0878180149808));
#20204=CARTESIAN_POINT('Ctrl Pts',(1.4177226146433,-2.89525214197987,30.0950119147973));
#20205=CARTESIAN_POINT('Ctrl Pts',(1.48862865463231,-2.85944205439147,30.0995978907407));
#20206=CARTESIAN_POINT('Ctrl Pts',(1.6995345611077,-2.7429527563825,30.1133165368947));
#20207=CARTESIAN_POINT('Ctrl Pts',(1.83485805341036,-2.65433739575478,30.1222370050728));
#20208=CARTESIAN_POINT('Ctrl Pts',(2.1155308730456,-2.43878029477274,30.1421070957447));
#20209=CARTESIAN_POINT('Ctrl Pts',(2.2572735480932,-2.30820744233556,30.1530923352389));
#20210=CARTESIAN_POINT('Ctrl Pts',(2.40147453404029,-2.14930984201592,30.1659945889721));
#20211=CARTESIAN_POINT('Ctrl Pts',(2.41625751356064,-2.13267726690592,30.1673395620991));
#20212=CARTESIAN_POINT('Ctrl Pts',(2.4395295315613,-2.1059409579539,30.1694935107113));
#20213=CARTESIAN_POINT('Ctrl Pts',(2.44813097432026,-2.09593568083501,30.1702978002006));
#20214=CARTESIAN_POINT('Ctrl Pts',(2.46320463085365,-2.07818248064839,30.1717219714086));
#20215=CARTESIAN_POINT('Ctrl Pts',(2.4697023715187,-2.07045639141828,30.1723407899316));
#20216=CARTESIAN_POINT('Ctrl Pts',(2.48307933527197,-2.05439804467347,30.1736250420898));
#20217=CARTESIAN_POINT('Ctrl Pts',(2.4899531614543,-2.046061475231,30.1742906850085));
#20218=CARTESIAN_POINT('Ctrl Pts',(2.50751825059293,-2.02453894905689,30.1760065393413));
#20219=CARTESIAN_POINT('Ctrl Pts',(2.51814738323025,-2.01130292891549,30.1770592438148));
#20220=CARTESIAN_POINT('Ctrl Pts',(2.56153955655275,-1.95638529373948,30.1814172070548));
#20221=CARTESIAN_POINT('Ctrl Pts',(2.59337464158526,-1.91398425971639,30.184759029172));
#20222=CARTESIAN_POINT('Ctrl Pts',(2.70876901566231,-1.7521236673462,30.1974394895382));
#20223=CARTESIAN_POINT('Ctrl Pts',(2.7852287580075,-1.62783849958295,30.2070350036993));
#20224=CARTESIAN_POINT('Ctrl Pts',(2.90641699151178,-1.39715633109783,30.2245044350131));
#20225=CARTESIAN_POINT('Ctrl Pts',(2.9543523452791,-1.29271282751195,30.2322968160354));
#20226=CARTESIAN_POINT('Ctrl Pts',(3.0269647015746,-1.1092369646233,30.2456396261825));
#20227=CARTESIAN_POINT('Ctrl Pts',(3.05436485626434,-1.03139629245465,30.2511975464793));
#20228=CARTESIAN_POINT('Ctrl Pts',(3.10453143215176,-0.869258632403087,
30.2624688219088));
#20229=CARTESIAN_POINT('Ctrl Pts',(3.12692291176562,-0.78490894975683,30.2681683621354));
#20230=CARTESIAN_POINT('Ctrl Pts',(3.14885289283336,-0.686317917875907,
30.2745645576127));
#20231=CARTESIAN_POINT('Ctrl Pts',(3.15175401612548,-0.672869573423179,
30.2754313632553));
#20232=CARTESIAN_POINT('Ctrl Pts',(3.15600906688295,-0.652513500472056,
30.2767344173874));
#20233=CARTESIAN_POINT('Ctrl Pts',(3.15742658503816,-0.645619439665913,
30.2771741735542));
#20234=CARTESIAN_POINT('Ctrl Pts',(3.15992711405623,-0.633252962864281,
30.2779601508414));
#20235=CARTESIAN_POINT('Ctrl Pts',(3.16101850703718,-0.627782351471588,
30.2783068441306));
#20236=CARTESIAN_POINT('Ctrl Pts',(3.16335686477289,-0.615900612076316,
30.279057651223));
#20237=CARTESIAN_POINT('Ctrl Pts',(3.16459854341345,-0.609488538591633,
30.2794614607852));
#20238=CARTESIAN_POINT('Ctrl Pts',(3.16711650688184,-0.596270527922909,
30.2802911471517));
#20239=CARTESIAN_POINT('Ctrl Pts',(3.16839036745164,-0.589464156778562,
30.280716886519));
#20240=CARTESIAN_POINT('Ctrl Pts',(3.1715905858526,-0.572054933614299,30.2818021453007));
#20241=CARTESIAN_POINT('Ctrl Pts',(3.17348573548982,-0.561446333459101,
30.2824599716221));
#20242=CARTESIAN_POINT('Ctrl Pts',(3.20671468066524,-0.369893363558426,
30.2942782071231));
#20243=CARTESIAN_POINT('Ctrl Pts',(3.22258313323825,-0.186584217027832,
30.3046373579577));
#20244=CARTESIAN_POINT('Ctrl Pts',(3.22274869089678,-0.00290479312253886,
30.3149198866253));
#20245=CARTESIAN_POINT('Ctrl Pts',(3.22274868914525,-0.00290673572484593,
30.3149197778768));
#20246=CARTESIAN_POINT('Ctrl Pts',(3.22299387022043,0.268929806518607,30.3301374173408));
#20247=CARTESIAN_POINT('Ctrl Pts',(3.18884801419423,0.539685140348905,30.3451725098073));
#20248=CARTESIAN_POINT('Ctrl Pts',(3.11297967882882,0.834591324622212,30.3633797714072));
#20249=CARTESIAN_POINT('Ctrl Pts',(3.10435840602317,0.86610849669144,30.365348112516));
#20250=CARTESIAN_POINT('Ctrl Pts',(3.09137296792005,0.910892705231855,30.3681794413213));
#20251=CARTESIAN_POINT('Ctrl Pts',(3.08739929600207,0.924271564355853,30.3690296899358));
#20252=CARTESIAN_POINT('Ctrl Pts',(3.08037585612877,0.947367863832681,30.3705053229563));
#20253=CARTESIAN_POINT('Ctrl Pts',(3.07736667263886,0.957097509555341,30.3711293679604));
#20254=CARTESIAN_POINT('Ctrl Pts',(3.07150315950228,0.975742554942193,30.3723299386522));
#20255=CARTESIAN_POINT('Ctrl Pts',(3.06865600022167,0.98466011481312,30.3729062225381));
#20256=CARTESIAN_POINT('Ctrl Pts',(3.06111994013475,1.00791357656737,30.3744144305873));
#20257=CARTESIAN_POINT('Ctrl Pts',(3.05636921845122,1.0222290613023,30.3753483909337));
#20258=CARTESIAN_POINT('Ctrl Pts',(3.03964970001899,1.0714518300963,30.3785789312619));
#20259=CARTESIAN_POINT('Ctrl Pts',(3.02718230933927,1.10618552075993,30.3808919785199));
#20260=CARTESIAN_POINT('Ctrl Pts',(2.93606491307461,1.34694978546955,30.3971661942472));
#20261=CARTESIAN_POINT('Ctrl Pts',(2.83705805865563,1.54461003308747,30.4118281129002));
#20262=CARTESIAN_POINT('Ctrl Pts',(2.66107604981017,1.82107033357091,30.4339821368988));
#20263=CARTESIAN_POINT('Ctrl Pts',(2.59899486772562,1.90862492348789,30.441265520862));
#20264=CARTESIAN_POINT('Ctrl Pts',(2.48040093553641,2.0593375522211,30.4541381952754));
#20265=CARTESIAN_POINT('Ctrl Pts',(2.42554285634798,2.12367695504919,30.4597535932905));
#20266=CARTESIAN_POINT('Ctrl Pts',(2.33864856792758,2.21782344081351,30.4680719323454));
#20267=CARTESIAN_POINT('Ctrl Pts',(2.30843324873756,2.24925639293838,30.4708674635473));
#20268=CARTESIAN_POINT('Ctrl Pts',(2.2701371149384,2.28751086217601,30.4742819446518));
#20269=CARTESIAN_POINT('Ctrl Pts',(2.26264993918842,2.29491693207852,30.4749435745963));
#20270=CARTESIAN_POINT('Ctrl Pts',(2.25053885884961,2.30677993019094,30.4760041130781));
#20271=CARTESIAN_POINT('Ctrl Pts',(2.24593777582064,2.31125989676106,30.4764047895648));
#20272=CARTESIAN_POINT('Ctrl Pts',(2.23730539585466,2.31961492372251,30.4771523109207));
#20273=CARTESIAN_POINT('Ctrl Pts',(2.2332774503664,2.32349320183066,30.4774994021357));
#20274=CARTESIAN_POINT('Ctrl Pts',(2.22404408222566,2.33233729041339,30.4782911798068));
#20275=CARTESIAN_POINT('Ctrl Pts',(2.21883212167112,2.33729615884314,30.4787353268226));
#20276=CARTESIAN_POINT('Ctrl Pts',(2.20270222450377,2.352540213345,30.4801014585476));
#20277=CARTESIAN_POINT('Ctrl Pts',(2.19172887048058,2.36276683651309,30.4810190438877));
#20278=CARTESIAN_POINT('Ctrl Pts',(2.07764972801598,2.46760430996102,30.4904421005458));
#20279=CARTESIAN_POINT('Ctrl Pts',(1.96854325791587,2.55549350279578,30.4984846196199));
#20280=CARTESIAN_POINT('Ctrl Pts',(1.63425776547915,2.7906145360599,30.5215615069101));
#20281=CARTESIAN_POINT('Ctrl Pts',(1.39600310008242,2.91710501024149,30.5362192696091));
#20282=CARTESIAN_POINT('Ctrl Pts',(1.07937316053417,3.03742848432863,30.5560479170053));
#20283=CARTESIAN_POINT('Ctrl Pts',(1.01314538403693,3.06015580632849,30.5602061506008));
#20284=CARTESIAN_POINT('Ctrl Pts',(0.928422490394513,3.08617828473099,30.5655620767027));
#20285=CARTESIAN_POINT('Ctrl Pts',(0.910564579107442,3.09149427469589,30.566692977984));
#20286=CARTESIAN_POINT('Ctrl Pts',(0.881927602823141,3.09974935519481,30.5685100534215));
#20287=CARTESIAN_POINT('Ctrl Pts',(0.871177436669819,3.10278781590461,30.569192971159));
#20288=CARTESIAN_POINT('Ctrl Pts',(0.850780681171142,3.10843846208108,30.5704903000512));
#20289=CARTESIAN_POINT('Ctrl Pts',(0.841137295452415,3.11106179408419,30.5711043390545));
#20290=CARTESIAN_POINT('Ctrl Pts',(0.819240825401045,3.11690913623143,30.5725001869886));
#20291=CARTESIAN_POINT('Ctrl Pts',(0.806980673304221,3.12010581216021,30.5732828742488));
#20292=CARTESIAN_POINT('Ctrl Pts',(0.775300955426744,3.12816667820165,30.5753083647325));
#20293=CARTESIAN_POINT('Ctrl Pts',(0.755854568688049,3.13292230670779,30.5765546574748));
#20294=CARTESIAN_POINT('Ctrl Pts',(0.631613941120976,3.16208138750361,30.5845370279462));
#20295=CARTESIAN_POINT('Ctrl Pts',(0.525708111837543,3.18140244171346,30.5914350954561));
#20296=CARTESIAN_POINT('Ctrl Pts',(0.172200902407954,3.22776140336313,30.614775027036));
#20297=CARTESIAN_POINT('Ctrl Pts',(-0.0775480296026197,3.2314172595377,
30.6318448310135));
#20298=CARTESIAN_POINT('Ctrl Pts',(-0.405272945825708,3.19817945815858,
30.6539250427879));
#20299=CARTESIAN_POINT('Ctrl Pts',(-0.485036647610255,3.1870580873313,30.6592648836753));
#20300=CARTESIAN_POINT('Ctrl Pts',(-0.606000017891726,3.16554497551066,
30.6672346703614));
#20301=CARTESIAN_POINT('Ctrl Pts',(-0.647547137155879,3.15730805121099,
30.6699485062906));
#20302=CARTESIAN_POINT('Ctrl Pts',(-0.699354139006458,3.14597129502787,
30.6732928843781));
#20303=CARTESIAN_POINT('Ctrl Pts',(-0.709774929078797,3.14363661362401,
30.6739635714577));
#20304=CARTESIAN_POINT('Ctrl Pts',(-0.726311354266359,3.13984536177924,
30.6750244366579));
#20305=CARTESIAN_POINT('Ctrl Pts',(-0.732434554206835,3.13842264595356,
30.6754165114065));
#20306=CARTESIAN_POINT('Ctrl Pts',(-0.744022277752315,3.13569449670675,
30.6761570154587));
#20307=CARTESIAN_POINT('Ctrl Pts',(-0.749487480946366,3.1343927071772,30.6765056379766));
#20308=CARTESIAN_POINT('Ctrl Pts',(-0.762044560734919,3.13136694026463,
30.6773052443543));
#20309=CARTESIAN_POINT('Ctrl Pts',(-0.769134001743944,3.12963316012505,
30.67775565752));
#20310=CARTESIAN_POINT('Ctrl Pts',(-0.788089971592249,3.12492902215584,
30.6789573873019));
#20311=CARTESIAN_POINT('Ctrl Pts',(-0.799945716954668,3.12191512661602,
30.6797062617465));
#20312=CARTESIAN_POINT('Ctrl Pts',(-0.887947450061585,3.09900963527778,
30.6852465706928));
#20313=CARTESIAN_POINT('Ctrl Pts',(-0.963365966683503,3.07640043542946,
30.6898924345344));
#20314=CARTESIAN_POINT('Ctrl Pts',(-1.05770200740286,3.04430978747947,30.6956606566191));
#20315=CARTESIAN_POINT('Ctrl Pts',(-1.0774509066064,3.03737636637863,30.6968657690571));
#20316=CARTESIAN_POINT('Ctrl Pts',(-1.31911400067984,2.94987994456055,30.7115978890921));
#20317=CARTESIAN_POINT('Ctrl Pts',(-1.53159893128865,2.84535915862341,30.7244532486862));
#20318=CARTESIAN_POINT('Ctrl Pts',(-1.80826268273697,2.6692214784955,30.7431256140288));
#20319=CARTESIAN_POINT('Ctrl Pts',(-1.88360770977575,2.6165965107142,30.7484283434048));
#20320=CARTESIAN_POINT('Ctrl Pts',(-2.00115126855666,2.52678746529781,30.7571512147674));
#20321=CARTESIAN_POINT('Ctrl Pts',(-2.04480607404662,2.49159162754908,30.7604979552525));
#20322=CARTESIAN_POINT('Ctrl Pts',(-2.10059938843576,2.44415518329824,30.7649295346038));
#20323=CARTESIAN_POINT('Ctrl Pts',(-2.11359073944614,2.43292961655727,30.7659727162362));
#20324=CARTESIAN_POINT('Ctrl Pts',(-2.13464259878507,2.41444325045045,30.7676820211003));
#20325=CARTESIAN_POINT('Ctrl Pts',(-2.14275734803602,2.40724451958692,30.7683455481789));
#20326=CARTESIAN_POINT('Ctrl Pts',(-2.15834156805202,2.3932782596782,30.7696289339581));
#20327=CARTESIAN_POINT('Ctrl Pts',(-2.16581594782148,2.38651637939239,30.7702485498394));
#20328=CARTESIAN_POINT('Ctrl Pts',(-2.18292704329954,2.37088981895917,30.7716765481376));
#20329=CARTESIAN_POINT('Ctrl Pts',(-2.19254165056297,2.36200129390854,30.7724859431582));
#20330=CARTESIAN_POINT('Ctrl Pts',(-2.21809670025177,2.33808564810473,30.774656278314));
#20331=CARTESIAN_POINT('Ctrl Pts',(-2.23393831657579,2.32295437514376,30.7760216992005));
#20332=CARTESIAN_POINT('Ctrl Pts',(-2.36707820650148,2.19316302346191,30.7876708219113));
#20333=CARTESIAN_POINT('Ctrl Pts',(-2.47560092440002,2.06988130496887,30.7983426108006));
#20334=CARTESIAN_POINT('Ctrl Pts',(-2.72720752968395,1.73582465102214,30.8262370123137));
#20335=CARTESIAN_POINT('Ctrl Pts',(-2.85558399503191,1.5153822753524,30.8437860602046));
#20336=CARTESIAN_POINT('Ctrl Pts',(-2.97899039845763,1.23079918560959,30.864074536397));
#20337=CARTESIAN_POINT('Ctrl Pts',(-2.99991858613339,1.17887226070512,30.8676835152072));
#20338=CARTESIAN_POINT('Ctrl Pts',(-3.0235566542196,1.11550815050646,30.8719541333152));
#20339=CARTESIAN_POINT('Ctrl Pts',(-3.02756930238077,1.10457114039206,30.8726865325431));
#20340=CARTESIAN_POINT('Ctrl Pts',(-3.03372841488643,1.08749791715335,30.8738222157482));
#20341=CARTESIAN_POINT('Ctrl Pts',(-3.03591572071721,1.08137669365312,30.8742278682005));
#20342=CARTESIAN_POINT('Ctrl Pts',(-3.03994675504478,1.06998712258704,30.8749797723577));
#20343=CARTESIAN_POINT('Ctrl Pts',(-3.04179529959364,1.06472065448502,30.8753263003351));
#20344=CARTESIAN_POINT('Ctrl Pts',(-3.04595766561037,1.0527628353469,30.8761105338018));
#20345=CARTESIAN_POINT('Ctrl Pts',(-3.04826311948865,1.04606866161011,30.8765477394076));
#20346=CARTESIAN_POINT('Ctrl Pts',(-3.05504639134056,1.02615972766939,30.8778427686254));
#20347=CARTESIAN_POINT('Ctrl Pts',(-3.05946054002329,1.01292322527341,30.8786969158437));
#20348=CARTESIAN_POINT('Ctrl Pts',(-3.09256877316825,0.911451912199076,
30.8851954861471));
#20349=CARTESIAN_POINT('Ctrl Pts',(-3.11752924805369,0.822034712855346,
30.8906378634238));
#20350=CARTESIAN_POINT('Ctrl Pts',(-3.19350514445047,0.496119742796025,
30.9098710069783));
#20351=CARTESIAN_POINT('Ctrl Pts',(-3.22172690357942,0.255143882280493,
30.9230220295249));
#20352=CARTESIAN_POINT('Ctrl Pts',(-3.22310147156134,-0.0787385245298545,
30.9420296622394));
#20353=CARTESIAN_POINT('Ctrl Pts',(-3.21954004625433,-0.170712646760827,
30.9473400942806));
#20354=CARTESIAN_POINT('Ctrl Pts',(-3.20747926518954,-0.318347104908386,
30.9560744787626));
#20355=CARTESIAN_POINT('Ctrl Pts',(-3.20144853731525,-0.374158791742361,
30.9594247757065));
#20356=CARTESIAN_POINT('Ctrl Pts',(-3.19167323932266,-0.446804782395326,
30.9638604091472));
#20357=CARTESIAN_POINT('Ctrl Pts',(-3.18924664304082,-0.463808594428457,
30.9649039915441));
#20358=CARTESIAN_POINT('Ctrl Pts',(-3.18506572742602,-0.491519661958937,
30.9666137880989));
#20359=CARTESIAN_POINT('Ctrl Pts',(-3.18339303508522,-0.502239032468734,
30.9672774032209));
#20360=CARTESIAN_POINT('Ctrl Pts',(-3.18006209212615,-0.522899829960585,
30.9685608434203));
#20361=CARTESIAN_POINT('Ctrl Pts',(-3.17841126675701,-0.532842338426372,
30.9691804250553));
#20362=CARTESIAN_POINT('Ctrl Pts',(-3.17450915189105,-0.555680273227197,
30.9706081783366));
#20363=CARTESIAN_POINT('Ctrl Pts',(-3.17222588769866,-0.5685699875837,30.9714173614512));
#20364=CARTESIAN_POINT('Ctrl Pts',(-3.16591387550435,-0.602981172921261,
30.9735867589013));
#20365=CARTESIAN_POINT('Ctrl Pts',(-3.16174428036182,-0.624475803688521,
30.9749514479059));
#20366=CARTESIAN_POINT('Ctrl Pts',(-3.12459629645006,-0.806059201737283,
30.9865634144551));
#20367=CARTESIAN_POINT('Ctrl Pts',(-3.07970718062468,-0.963443071882241,
30.9971959220118));
#20368=CARTESIAN_POINT('Ctrl Pts',(-2.93539951244614,-1.35409832722291,
31.0249690537506));
#20369=CARTESIAN_POINT('Ctrl Pts',(-2.82006744379474,-1.5803060287256,31.0424337011622));
#20370=CARTESIAN_POINT('Ctrl Pts',(-2.64747750384873,-1.83855787917176,
31.0627680974446));
#20371=CARTESIAN_POINT('Ctrl Pts',(-2.61420825132768,-1.88556315239567,
31.0664828565777));
#20372=CARTESIAN_POINT('Ctrl Pts',(-2.57265509806996,-1.94105673855285,
31.0708612041755));
#20373=CARTESIAN_POINT('Ctrl Pts',(-2.56556368168135,-1.95042008838233,
31.0715996962196));
#20374=CARTESIAN_POINT('Ctrl Pts',(-2.55445566390821,-1.96492146101508,
31.0727427468899));
#20375=CARTESIAN_POINT('Ctrl Pts',(-2.55047447660281,-1.97008630085497,
31.0731497229313));
#20376=CARTESIAN_POINT('Ctrl Pts',(-2.54305795604091,-1.97964767684539,
31.0739028266103));
#20377=CARTESIAN_POINT('Ctrl Pts',(-2.53962691434688,-1.98404733534443,
31.0742492383984));
#20378=CARTESIAN_POINT('Ctrl Pts',(-2.5318335601699,-1.9939874901052,31.0750316182666));
#20379=CARTESIAN_POINT('Ctrl Pts',(-2.52746448968699,-1.99952257869295,
31.0754670963315));
#20380=CARTESIAN_POINT('Ctrl Pts',(-2.51447923929541,-2.01586276893567,
31.0767522809537));
#20381=CARTESIAN_POINT('Ctrl Pts',(-2.50581155714943,-2.02662700168541,
31.0775983934848));
#20382=CARTESIAN_POINT('Ctrl Pts',(-2.44086039385233,-2.10623486132251,
31.0838548882697));
#20383=CARTESIAN_POINT('Ctrl Pts',(-2.38181284063194,-2.17278518222201,
31.0890798469625));
#20384=CARTESIAN_POINT('Ctrl Pts',(-2.14880108849659,-2.41447114586384,
31.1084105179707));
#20385=CARTESIAN_POINT('Ctrl Pts',(-1.95767567534258,-2.57187430493659,
31.1218136658013));
#20386=CARTESIAN_POINT('Ctrl Pts',(-1.67365375859619,-2.75560626005268,
31.1410757937894));
#20387=CARTESIAN_POINT('Ctrl Pts',(-1.5947847966252,-2.80198899188276,31.1463560636249));
#20388=CARTESIAN_POINT('Ctrl Pts',(-1.50116695529643,-2.85181143492072,
31.1526101846239));
#20389=CARTESIAN_POINT('Ctrl Pts',(-1.48823366213642,-2.85858202895638,
31.1534738563823));
#20390=CARTESIAN_POINT('Ctrl Pts',(-1.47525540353836,-2.86526422112008,
31.1543403726568));
#20391=CARTESIAN_POINT('Origin',(0.,0.,4.68922655072688));
#20392=CARTESIAN_POINT('',(-1.47525540501496,-2.86526422035982,32.6506479065737));
#20393=CARTESIAN_POINT('',(-1.47525529429555,-2.86526427736657,32.4060211118892));
#20394=CARTESIAN_POINT('',(-1.47525540501186,-2.86526422036142,4.68922655072688));
#20395=CARTESIAN_POINT('',(3.22274870594889,0.00297136373924148,31.8105144221227));
#20396=CARTESIAN_POINT('Ctrl Pts',(-1.47525540501479,-2.8652642203599,32.6506479065737));
#20397=CARTESIAN_POINT('Ctrl Pts',(-1.48291685166428,-2.86131952635942,
32.6501042669168));
#20398=CARTESIAN_POINT('Ctrl Pts',(-1.49056256546604,-2.85734405767437,
32.6495624097806));
#20399=CARTESIAN_POINT('Ctrl Pts',(-1.50444135845292,-2.85005676738993,
32.6485801507047));
#20400=CARTESIAN_POINT('Ctrl Pts',(-1.51067963242588,-2.84675507003948,
32.6481391379674));
#20401=CARTESIAN_POINT('Ctrl Pts',(-1.52183173724427,-2.84080567452559,
32.6473517013386));
#20402=CARTESIAN_POINT('Ctrl Pts',(-1.52674956358572,-2.83816569081889,
32.647004798786));
#20403=CARTESIAN_POINT('Ctrl Pts',(-1.53739765880858,-2.83241390308338,
32.6462544291026));
#20404=CARTESIAN_POINT('Ctrl Pts',(-1.54312533261345,-2.82929749042332,
32.6458512616093));
#20405=CARTESIAN_POINT('Ctrl Pts',(-1.55913576696437,-2.82052317263687,
32.6447254774036));
#20406=CARTESIAN_POINT('Ctrl Pts',(-1.56939726116582,-2.81482638074299,
32.6440053019387));
#20407=CARTESIAN_POINT('Ctrl Pts',(-1.62963732957346,-2.78095155615464,
32.6397842235566));
#20408=CARTESIAN_POINT('Ctrl Pts',(-1.67889080003837,-2.75149704841219,
32.6363602620487));
#20409=CARTESIAN_POINT('Ctrl Pts',(-1.94114493311019,-2.58499802795509,
32.6181326975254));
#20410=CARTESIAN_POINT('Ctrl Pts',(-2.13822831928392,-2.42451330176459,
32.6043873635631));
#20411=CARTESIAN_POINT('Ctrl Pts',(-2.4282090504413,-2.12523425899002,32.580846263));
#20412=CARTESIAN_POINT('Ctrl Pts',(-2.53281406830006,-1.99941550664937,
32.5714285732258));
#20413=CARTESIAN_POINT('Ctrl Pts',(-2.64010319616985,-1.84836475590185,
32.5602847096252));
#20414=CARTESIAN_POINT('Ctrl Pts',(-2.65260220675551,-1.83038210593846,
32.55896077099));
#20415=CARTESIAN_POINT('Ctrl Pts',(-2.67228001905848,-1.80144622911154,
32.5568340718041));
#20416=CARTESIAN_POINT('Ctrl Pts',(-2.67957715277906,-1.79057401159564,
32.5560358091785));
#20417=CARTESIAN_POINT('Ctrl Pts',(-2.69237522670015,-1.77125233915481,
32.5546184564413));
#20418=CARTESIAN_POINT('Ctrl Pts',(-2.6979031846448,-1.76282092480332,32.5540003948706));
#20419=CARTESIAN_POINT('Ctrl Pts',(-2.70929967996856,-1.74525946568782,
32.5527138792752));
#20420=CARTESIAN_POINT('Ctrl Pts',(-2.71516183322567,-1.73612544858693,
32.5520451967824));
#20421=CARTESIAN_POINT('Ctrl Pts',(-2.73018608392119,-1.71245344605958,
32.5503132969058));
#20422=CARTESIAN_POINT('Ctrl Pts',(-2.739278151372,-1.69787162316168,32.5492474979498));
#20423=CARTESIAN_POINT('Ctrl Pts',(-2.77758991251153,-1.63531857714893,
32.5446793247281));
#20424=CARTESIAN_POINT('Ctrl Pts',(-2.80566792003677,-1.58666299280107,
32.5411355065275));
#20425=CARTESIAN_POINT('Ctrl Pts',(-2.8763871670721,-1.45636361290657,32.5316635861376));
#20426=CARTESIAN_POINT('Ctrl Pts',(-2.91682248917228,-1.37358732552068,
32.5256635630037));
#20427=CARTESIAN_POINT('Ctrl Pts',(-3.05000621350855,-1.06845308928956,
32.5036370978224));
#20428=CARTESIAN_POINT('Ctrl Pts',(-3.12129772791029,-0.837625034367631,
32.4870761631634));
#20429=CARTESIAN_POINT('Ctrl Pts',(-3.18366981582592,-0.509046704729985,
32.4648125038878));
#20430=CARTESIAN_POINT('Ctrl Pts',(-3.19711491829628,-0.416343384846984,
32.458680632028));
#20431=CARTESIAN_POINT('Ctrl Pts',(-3.20790715398496,-0.30926490388749,
32.45186333026));
#20432=CARTESIAN_POINT('Ctrl Pts',(-3.20921884682066,-0.295343019639964,
32.450982120647));
#20433=CARTESIAN_POINT('Ctrl Pts',(-3.21105882877317,-0.274351960802021,
32.4496616529361));
#20434=CARTESIAN_POINT('Ctrl Pts',(-3.2116544574235,-0.267289073160047,
32.4492187503789));
#20435=CARTESIAN_POINT('Ctrl Pts',(-3.21267766233792,-0.254658555870999,
32.4484292768727));
#20436=CARTESIAN_POINT('Ctrl Pts',(-3.21311407302239,-0.24909174513666,
32.4480822166881));
#20437=CARTESIAN_POINT('Ctrl Pts',(-3.21402709001161,-0.237043582791671,
32.4473330250569));
#20438=CARTESIAN_POINT('Ctrl Pts',(-3.21449855988002,-0.23056193476432,
32.4469311850621));
#20439=CARTESIAN_POINT('Ctrl Pts',(-3.21575950149652,-0.212470691377941,
32.4458128519063));
#20440=CARTESIAN_POINT('Ctrl Pts',(-3.21650571625871,-0.200858042067644,
32.4450987480883));
#20441=CARTESIAN_POINT('Ctrl Pts',(-3.22046029516785,-0.133628419595537,
32.4409849189462));
#20442=CARTESIAN_POINT('Ctrl Pts',(-3.22228923452116,-0.0779360269604391,
32.4376576457728));
#20443=CARTESIAN_POINT('Ctrl Pts',(-3.22442804807954,0.232260052644628,
32.4194356922017));
#20444=CARTESIAN_POINT('Ctrl Pts',(-3.19603478523003,0.486076309874904,
32.4056265872412));
#20445=CARTESIAN_POINT('Ctrl Pts',(-3.10071736806259,0.893626156200001,
32.3819858711514));
#20446=CARTESIAN_POINT('Ctrl Pts',(-3.05123667663764,1.05021911223644,32.3725354479807));
#20447=CARTESIAN_POINT('Ctrl Pts',(-2.98188533857926,1.22268455073457,32.3613549695967));
#20448=CARTESIAN_POINT('Ctrl Pts',(-2.97350350116868,1.24292983521008,32.3600303154276));
#20449=CARTESIAN_POINT('Ctrl Pts',(-2.95978271976823,1.27513738871831,32.3579026839672));
#20450=CARTESIAN_POINT('Ctrl Pts',(-2.95457606746857,1.2871555313712,32.3571042109099));
#20451=CARTESIAN_POINT('Ctrl Pts',(-2.94523190351983,1.30836854741294,32.3556866146746));
#20452=CARTESIAN_POINT('Ctrl Pts',(-2.94112420537878,1.31757642140256,32.3550685212166));
#20453=CARTESIAN_POINT('Ctrl Pts',(-2.93250583111739,1.33665435914517,32.3537820690478));
#20454=CARTESIAN_POINT('Ctrl Pts',(-2.92798838154686,1.34652120602452,32.3531134825141));
#20455=CARTESIAN_POINT('Ctrl Pts',(-2.91619181230212,1.3719467678322,32.3513821102763));
#20456=CARTESIAN_POINT('Ctrl Pts',(-2.90883805138723,1.38747028519196,32.3503167459823));
#20457=CARTESIAN_POINT('Ctrl Pts',(-2.87693628750076,1.45344524931114,32.3457529587842));
#20458=CARTESIAN_POINT('Ctrl Pts',(-2.85119836716688,1.50330726322978,32.3422131908309));
#20459=CARTESIAN_POINT('Ctrl Pts',(-2.77988127803945,1.63304366064887,32.3327548438015));
#20460=CARTESIAN_POINT('Ctrl Pts',(-2.732164972664,1.71167857876124,32.3267645997801));
#20461=CARTESIAN_POINT('Ctrl Pts',(-2.54664308495737,1.98984883403533,32.3046452495708));
#20462=CARTESIAN_POINT('Ctrl Pts',(-2.38981749171377,2.17569455868383,32.2879718752486));
#20463=CARTESIAN_POINT('Ctrl Pts',(-2.14653953429876,2.40562101123155,32.2656989340353));
#20464=CARTESIAN_POINT('Ctrl Pts',(-2.07672679368562,2.46614145844884,32.2596536124603));
#20465=CARTESIAN_POINT('Ctrl Pts',(-1.99348738271045,2.53225590744613,32.2529202547534));
#20466=CARTESIAN_POINT('Ctrl Pts',(-1.98251412065642,2.54085609662356,32.2520417031501));
#20467=CARTESIAN_POINT('Ctrl Pts',(-1.96588527119318,2.55371548435117,32.2507244303169));
#20468=CARTESIAN_POINT('Ctrl Pts',(-1.96027106154988,2.55802756866145,32.2502820901424));
#20469=CARTESIAN_POINT('Ctrl Pts',(-1.95020358792304,2.56570744631809,32.2494932238978));
#20470=CARTESIAN_POINT('Ctrl Pts',(-1.94575575393921,2.56908218670173,32.2491462117374));
#20471=CARTESIAN_POINT('Ctrl Pts',(-1.93610658207787,2.57636394594035,32.2483966746265));
#20472=CARTESIAN_POINT('Ctrl Pts',(-1.93090219386008,2.58026676888646,32.2479944435444));
#20473=CARTESIAN_POINT('Ctrl Pts',(-1.91633178574284,2.59112449336481,32.2468739168112));
#20474=CARTESIAN_POINT('Ctrl Pts',(-1.90693965508675,2.59804442123703,32.246158025731));
#20475=CARTESIAN_POINT('Ctrl Pts',(-1.85208969634267,2.63799904999241,32.242013000598));
#20476=CARTESIAN_POINT('Ctrl Pts',(-1.80580858729125,2.66989353088683,32.2386576097807));
#20477=CARTESIAN_POINT('Ctrl Pts',(-1.54576415520346,2.83924476229148,32.2204342929575));
#20478=CARTESIAN_POINT('Ctrl Pts',(-1.31713942681308,2.95226500538679,32.2066439313556));
#20479=CARTESIAN_POINT('Ctrl Pts',(-0.923183504161726,3.0920368868483,32.1830322379499));
#20480=CARTESIAN_POINT('Ctrl Pts',(-0.764844786626363,3.13495803900215,
32.1735911528506));
#20481=CARTESIAN_POINT('Ctrl Pts',(-0.582422252100943,3.16976053568869,
32.1624211209254));
#20482=CARTESIAN_POINT('Ctrl Pts',(-0.560861262169621,3.17364650546416,
32.1610966704355));
#20483=CARTESIAN_POINT('Ctrl Pts',(-0.526350821919155,3.17950371827202,
32.1589693043467));
#20484=CARTESIAN_POINT('Ctrl Pts',(-0.513425830534473,3.18161641164266,
32.1581708911856));
#20485=CARTESIAN_POINT('Ctrl Pts',(-0.490528346930976,3.18521603020549,
32.1567533642627));
#20486=CARTESIAN_POINT('Ctrl Pts',(-0.480561023402479,3.18673505603114,
32.1561352798853));
#20487=CARTESIAN_POINT('Ctrl Pts',(-0.459850850816696,3.18979192578056,
32.1548488096849));
#20488=CARTESIAN_POINT('Ctrl Pts',(-0.449107047726601,3.19132232622173,
32.1541801958554));
#20489=CARTESIAN_POINT('Ctrl Pts',(-0.421336279817834,3.19513511871768,
32.1524486735259));
#20490=CARTESIAN_POINT('Ctrl Pts',(-0.404298596104516,3.19733565868851,
32.1513831855879));
#20491=CARTESIAN_POINT('Ctrl Pts',(-0.33259650445973,3.20601423419007,32.1468852620894));
#20492=CARTESIAN_POINT('Ctrl Pts',(-0.277791051929911,3.21122706031571,
32.1434131902558));
#20493=CARTESIAN_POINT('Ctrl Pts',(-0.133116213764621,3.22125661575129,
32.1341522968375));
#20494=CARTESIAN_POINT('Ctrl Pts',(-0.0431368919750242,3.22371694527691,
32.1282949313381));
#20495=CARTESIAN_POINT('Ctrl Pts',(0.300614868560171,3.2187222732619,32.105573491936));
#20496=CARTESIAN_POINT('Ctrl Pts',(0.553055718134541,3.18506744055155,32.0880851896187));
#20497=CARTESIAN_POINT('Ctrl Pts',(0.812424153067238,3.11869826125232,32.0703246460258));
#20498=CARTESIAN_POINT('Ctrl Pts',(0.825905350060756,3.11515524676999,32.069402395148));
#20499=CARTESIAN_POINT('Ctrl Pts',(0.908409492889777,3.09289897274025,32.0637653167548));
#20500=CARTESIAN_POINT('Ctrl Pts',(0.976822732889488,3.07197834679629,32.0591209523462));
#20501=CARTESIAN_POINT('Ctrl Pts',(1.05575794869457,3.04493589773411,32.0538414071602));
#20502=CARTESIAN_POINT('Ctrl Pts',(1.06700606105942,3.04101258523069,32.0530909933535));
#20503=CARTESIAN_POINT('Ctrl Pts',(1.08502274271987,3.03461614234726,32.0518923838326));
#20504=CARTESIAN_POINT('Ctrl Pts',(1.09180509595619,3.03218256680718,32.051441938148));
#20505=CARTESIAN_POINT('Ctrl Pts',(1.1038511843549,3.02781465286966,32.0506433469181));
#20506=CARTESIAN_POINT('Ctrl Pts',(1.10911809454526,3.02588930126551,32.0502946736556));
#20507=CARTESIAN_POINT('Ctrl Pts',(1.12033226315809,3.02175667825614,32.0495533624632));
#20508=CARTESIAN_POINT('Ctrl Pts',(1.12627802443907,3.01954559756382,32.0491609561795));
#20509=CARTESIAN_POINT('Ctrl Pts',(1.14224573251456,3.01355387867224,32.0481087419447));
#20510=CARTESIAN_POINT('Ctrl Pts',(1.15225552809678,3.00974076934065,32.0474508492471));
#20511=CARTESIAN_POINT('Ctrl Pts',(1.20251027283317,2.99030937682275,32.0441556224705));
#20512=CARTESIAN_POINT('Ctrl Pts',(1.24245968629992,2.97393266175769,32.0415612190032));
#20513=CARTESIAN_POINT('Ctrl Pts',(1.358337920506,2.92368706619062,32.034076058665));
#20514=CARTESIAN_POINT('Ctrl Pts',(1.43330317111045,2.88767587363463,32.0292847309871));
#20515=CARTESIAN_POINT('Ctrl Pts',(1.66073380245944,2.76738265637367,32.0146630105339));
#20516=CARTESIAN_POINT('Ctrl Pts',(1.80782125190431,2.67361727356417,32.0050688274867));
#20517=CARTESIAN_POINT('Ctrl Pts',(2.08587570415357,2.4628790620077,31.9854123896935));
#20518=CARTESIAN_POINT('Ctrl Pts',(2.21630260841923,2.34619722437109,31.9753777585279));
#20519=CARTESIAN_POINT('Ctrl Pts',(2.35184971830429,2.20349934428614,31.9635420559775));
#20520=CARTESIAN_POINT('Ctrl Pts',(2.36691201604515,2.18731203278201,31.9622055180295));
#20521=CARTESIAN_POINT('Ctrl Pts',(2.39066840783102,2.16124852720196,31.9600624081833));
#20522=CARTESIAN_POINT('Ctrl Pts',(2.39947082140512,2.15147168275718,31.9592604459019));
#20523=CARTESIAN_POINT('Ctrl Pts',(2.41491941238188,2.13410019412087,31.9578388059321));
#20524=CARTESIAN_POINT('Ctrl Pts',(2.42159027873963,2.12652766854324,31.9572201775346));
#20525=CARTESIAN_POINT('Ctrl Pts',(2.43534402894336,2.11076626999908,31.9559347463029));
#20526=CARTESIAN_POINT('Ctrl Pts',(2.44242142475973,2.10257279663996,31.9552677262408));
#20527=CARTESIAN_POINT('Ctrl Pts',(2.46054668406639,2.08137424878591,31.9535449721046));
#20528=CARTESIAN_POINT('Ctrl Pts',(2.47153267709984,2.06831693798482,31.9524867079808));
#20529=CARTESIAN_POINT('Ctrl Pts',(2.51670714489029,2.01375134489924,31.9480756228174));
#20530=CARTESIAN_POINT('Ctrl Pts',(2.54995608343093,1.97147983560572,31.9446851104949));
#20531=CARTESIAN_POINT('Ctrl Pts',(2.66122441568723,1.82249124422599,31.9328182695657));
#20532=CARTESIAN_POINT('Ctrl Pts',(2.73371871044321,1.71183075866648,31.9241401991683));
#20533=CARTESIAN_POINT('Ctrl Pts',(2.85280109727604,1.50310984478794,31.9080764178577));
#20534=CARTESIAN_POINT('Ctrl Pts',(2.90162968875457,1.40654076892554,31.9007542135455));
#20535=CARTESIAN_POINT('Ctrl Pts',(3.0217968900951,1.13587268191479,31.880708316817));
#20536=CARTESIAN_POINT('Ctrl Pts',(3.08291080104405,0.957674669974966,31.8680121563428));
#20537=CARTESIAN_POINT('Ctrl Pts',(3.13166055473726,0.760942752618961,31.8551660512304));
#20538=CARTESIAN_POINT('Ctrl Pts',(3.13508355637754,0.74671468209955,31.854243537446));
#20539=CARTESIAN_POINT('Ctrl Pts',(3.14002863266406,0.725526356139643,31.8528799559708));
#20540=CARTESIAN_POINT('Ctrl Pts',(3.14162467860461,0.718583807569237,31.8524347920099));
#20541=CARTESIAN_POINT('Ctrl Pts',(3.1444313686651,0.706187045110335,31.8516428673776));
#20542=CARTESIAN_POINT('Ctrl Pts',(3.14565085889075,0.700734935988452,31.8512956048356));
#20543=CARTESIAN_POINT('Ctrl Pts',(3.14825276542802,0.688958628620088,31.8505477601554));
#20544=CARTESIAN_POINT('Ctrl Pts',(3.14963030308985,0.682633446716022,31.8501474599121));
#20545=CARTESIAN_POINT('Ctrl Pts',(3.15242455401594,0.669614667962316,31.8493262901574));
#20546=CARTESIAN_POINT('Ctrl Pts',(3.15383903013294,0.662920618405464,31.8489055482326));
#20547=CARTESIAN_POINT('Ctrl Pts',(3.15738542756784,0.645868909381281,31.847837469423));
#20548=CARTESIAN_POINT('Ctrl Pts',(3.15948772584706,0.635505077497406,31.8471917491857));
#20549=CARTESIAN_POINT('Ctrl Pts',(3.16541355592326,0.605535766752645,31.8453339588908));
#20550=CARTESIAN_POINT('Ctrl Pts',(3.16910595080587,0.585904480663125,31.8441286821797));
#20551=CARTESIAN_POINT('Ctrl Pts',(3.20579579446999,0.380332896570112,31.8316171952126));
#20552=CARTESIAN_POINT('Ctrl Pts',(3.22257452653606,0.191850745334481,31.8210686942788));
#20553=CARTESIAN_POINT('Ctrl Pts',(3.22274863087502,0.00297063851481531,
31.8105142503188));
#20554=CARTESIAN_POINT('Ctrl Pts',(3.22274863019977,0.00297137098221913,
31.8105142912484));
#20555=CARTESIAN_POINT('Ctrl Pts',(3.22294655442589,-0.211697222216134,
31.7985188106586));
#20556=CARTESIAN_POINT('Ctrl Pts',(3.2016966095535,-0.425834942704719,31.7865487754178));
#20557=CARTESIAN_POINT('Ctrl Pts',(3.15179628169263,-0.67360854883105,31.7716561250349));
#20558=CARTESIAN_POINT('Ctrl Pts',(3.14361538969645,-0.71080966747438,31.7693932376667));
#20559=CARTESIAN_POINT('Ctrl Pts',(3.13016127318282,-0.767205098686855,
31.7659172523452));
#20560=CARTESIAN_POINT('Ctrl Pts',(3.12536623256774,-0.786510740601612,
31.7647191473432));
#20561=CARTESIAN_POINT('Ctrl Pts',(3.11612273591884,-0.822306718833107,
31.7624817651706));
#20562=CARTESIAN_POINT('Ctrl Pts',(3.1117213005569,-0.838808545103621,31.7614440228271));
#20563=CARTESIAN_POINT('Ctrl Pts',(3.10431479167114,-0.86571619452275,31.7597412387505));
#20564=CARTESIAN_POINT('Ctrl Pts',(3.10138801985981,-0.876143367827872,
31.759078753382));
#20565=CARTESIAN_POINT('Ctrl Pts',(3.09563292462377,-0.896256759208142,
31.7577956929485));
#20566=CARTESIAN_POINT('Ctrl Pts',(3.09281155450412,-0.905944847697968,
31.7571753518048));
#20567=CARTESIAN_POINT('Ctrl Pts',(3.08620925219622,-0.928225664958481,
31.7557432476211));
#20568=CARTESIAN_POINT('Ctrl Pts',(3.08239668162054,-0.940808759699964,
31.7549304545748));
#20569=CARTESIAN_POINT('Ctrl Pts',(3.07197399351923,-0.974464515102667,
31.7527455582349));
#20570=CARTESIAN_POINT('Ctrl Pts',(3.06522417562286,-0.995492853822492,
31.7513688810894));
#20571=CARTESIAN_POINT('Ctrl Pts',(2.98786019161372,-1.22826293802806,31.7359988258656));
#20572=CARTESIAN_POINT('Ctrl Pts',(2.8956613494858,-1.43214815950187,31.721261031844));
#20573=CARTESIAN_POINT('Ctrl Pts',(2.72883652109949,-1.71790006338102,31.6989330237154));
#20574=CARTESIAN_POINT('Ctrl Pts',(2.66987420867143,-1.80817617550761,31.6916127097813));
#20575=CARTESIAN_POINT('Ctrl Pts',(2.53399560215951,-1.99503961220759,31.6760524739148));
#20576=CARTESIAN_POINT('Ctrl Pts',(2.45582078760895,-2.09051841347114,31.6678439800124));
#20577=CARTESIAN_POINT('Ctrl Pts',(2.35564755857946,-2.19946624834774,31.6583674354191));
#20578=CARTESIAN_POINT('Ctrl Pts',(2.33872687586444,-2.217449860821,31.6567994498702));
#20579=CARTESIAN_POINT('Ctrl Pts',(2.31690385102352,-2.24011606033941,31.6548204451901));
#20580=CARTESIAN_POINT('Ctrl Pts',(2.31219170242051,-2.24497949921201,31.654395650719));
#20581=CARTESIAN_POINT('Ctrl Pts',(2.30297950624752,-2.25442769347834,31.6535701493753));
#20582=CARTESIAN_POINT('Ctrl Pts',(2.29848101320443,-2.25901391429292,31.653169327547));
#20583=CARTESIAN_POINT('Ctrl Pts',(2.29003997410059,-2.26756824987753,31.6524215381755));
#20584=CARTESIAN_POINT('Ctrl Pts',(2.28610085519934,-2.27153950687205,31.6520743241006));
#20585=CARTESIAN_POINT('Ctrl Pts',(2.27706998687222,-2.28059677025413,31.6512822625145));
#20586=CARTESIAN_POINT('Ctrl Pts',(2.27197153662212,-2.28567598157656,31.6508379548484));
#20587=CARTESIAN_POINT('Ctrl Pts',(2.25619032144485,-2.30129266981563,31.6494713104575));
#20588=CARTESIAN_POINT('Ctrl Pts',(2.2454507632227,-2.31177282812969,31.6485533764769));
#20589=CARTESIAN_POINT('Ctrl Pts',(2.1335791968284,-2.41942714647603,31.6391108323562));
#20590=CARTESIAN_POINT('Ctrl Pts',(2.02626580448385,-2.5099890502429,31.6310512680974));
#20591=CARTESIAN_POINT('Ctrl Pts',(1.73639877619137,-2.7238594319444,31.6107127573063));
#20592=CARTESIAN_POINT('Ctrl Pts',(1.5465211439489,-2.83597668525063,31.5986561905489));
#20593=CARTESIAN_POINT('Ctrl Pts',(1.24375160228321,-2.97523799235726,31.5795137198177));
#20594=CARTESIAN_POINT('Ctrl Pts',(1.13838318882406,-3.01712424606775,31.5728742948988));
#20595=CARTESIAN_POINT('Ctrl Pts',(1.01145877586732,-3.05998295056648,31.56479783105));
#20596=CARTESIAN_POINT('Ctrl Pts',(0.991819204731621,-3.066404922301,31.563546083599));
#20597=CARTESIAN_POINT('Ctrl Pts',(0.960688594364407,-3.07625400998359,
31.5615581660108));
#20598=CARTESIAN_POINT('Ctrl Pts',(0.949237637500321,-3.07980668398456,
31.5608261371693));
#20599=CARTESIAN_POINT('Ctrl Pts',(0.928339535615406,-3.0861627262168,31.5594886097369));
#20600=CARTESIAN_POINT('Ctrl Pts',(0.918898810472238,-3.08898683046013,
31.5588838009211));
#20601=CARTESIAN_POINT('Ctrl Pts',(0.898281742825715,-3.09505135380699,
31.5575616628602));
#20602=CARTESIAN_POINT('Ctrl Pts',(0.887100537242835,-3.09827461715767,
31.5568437813052));
#20603=CARTESIAN_POINT('Ctrl Pts',(0.856476170187395,-3.10692349498022,
31.5548751231888));
#20604=CARTESIAN_POINT('Ctrl Pts',(0.836999354375975,-3.11222702973482,
31.5536203888655));
#20605=CARTESIAN_POINT('Ctrl Pts',(0.738362382420617,-3.13809299553197,
31.5472515022911));
#20606=CARTESIAN_POINT('Ctrl Pts',(0.658495765406616,-3.15581812446404,
31.5420464654003));
#20607=CARTESIAN_POINT('Ctrl Pts',(0.554484208805832,-3.17478164349647,
31.5352012997161));
#20608=CARTESIAN_POINT('Ctrl Pts',(0.530874763144241,-3.17881474184123,
31.5336432337452));
#20609=CARTESIAN_POINT('Ctrl Pts',(0.252787149857518,-3.22313483687704,
31.5152425679041));
#20610=CARTESIAN_POINT('Ctrl Pts',(-0.00557936023520656,-3.23302320659039,
31.4975601948538));
#20611=CARTESIAN_POINT('Ctrl Pts',(-0.339963207176285,-3.20571553381336,
31.4750931836018));
#20612=CARTESIAN_POINT('Ctrl Pts',(-0.41736182553296,-3.19656031329922,
31.4699312181219));
#20613=CARTESIAN_POINT('Ctrl Pts',(-0.53516792649685,-3.17827287853875,
31.4622025396388));
#20614=CARTESIAN_POINT('Ctrl Pts',(-0.57585529802097,-3.17115345868604,
31.4595570325029));
#20615=CARTESIAN_POINT('Ctrl Pts',(-0.626774243737929,-3.16123130933243,
31.4562855962421));
#20616=CARTESIAN_POINT('Ctrl Pts',(-0.637141878815733,-3.15915804880541,
31.4556215584571));
#20617=CARTESIAN_POINT('Ctrl Pts',(-0.653682858163162,-3.1557655376065,
31.4545656239615));
#20618=CARTESIAN_POINT('Ctrl Pts',(-0.659862747861199,-3.15447912705302,
31.4541718974085));
#20619=CARTESIAN_POINT('Ctrl Pts',(-0.671532218276745,-3.15201420768962,
31.4534299552215));
#20620=CARTESIAN_POINT('Ctrl Pts',(-0.677022429572355,-3.15083952558238,
31.4530815367481));
#20621=CARTESIAN_POINT('Ctrl Pts',(-0.689603751460724,-3.14811323138528,
31.45228455325));
#20622=CARTESIAN_POINT('Ctrl Pts',(-0.696692703623661,-3.14655200668855,
31.4518365450466));
#20623=CARTESIAN_POINT('Ctrl Pts',(-0.715577525245787,-3.14232598697329,
31.4506457217876));
#20624=CARTESIAN_POINT('Ctrl Pts',(-0.727363905694022,-3.13961869697579,
31.4499052787004));
#20625=CARTESIAN_POINT('Ctrl Pts',(-0.812425515832031,-3.11957562500354,
31.4445797656049));
#20626=CARTESIAN_POINT('Ctrl Pts',(-0.885094839887949,-3.09974134431951,
31.4401278429332));
#20627=CARTESIAN_POINT('Ctrl Pts',(-1.00402594848297,-3.06275593034443,
31.4329043418943));
#20628=CARTESIAN_POINT('Ctrl Pts',(-1.05070383265645,-3.04705821908434,
31.4300856262903));
#20629=CARTESIAN_POINT('Ctrl Pts',(-1.22655498250397,-2.98339790531444,
31.4194672774839));
#20630=CARTESIAN_POINT('Ctrl Pts',(-1.35289316253756,-2.9282656021495,31.4118344611414));
#20631=CARTESIAN_POINT('Ctrl Pts',(-1.47525569888183,-2.86526406905484,
31.4041249682223));
#20632=CARTESIAN_POINT('Ctrl Pts',(-1.47525540353836,-2.86526422112008,
31.1543403726568));
#20633=CARTESIAN_POINT('Ctrl Pts',(-1.4385464654136,-2.88416476750862,31.1567913095114));
#20634=CARTESIAN_POINT('Ctrl Pts',(-1.40147779098518,-2.90235806517172,
31.1592650689877));
#20635=CARTESIAN_POINT('Ctrl Pts',(-1.34853185279998,-2.92709301561504,
31.1628014532052));
#20636=CARTESIAN_POINT('Ctrl Pts',(-1.33293650732094,-2.93422765474034,
31.1638434624792));
#20637=CARTESIAN_POINT('Ctrl Pts',(-1.30738902028689,-2.94566954875886,
31.1655513290561));
#20638=CARTESIAN_POINT('Ctrl Pts',(-1.29747064165849,-2.9500517063844,31.1662145986323));
#20639=CARTESIAN_POINT('Ctrl Pts',(-1.27828912902419,-2.95841107465922,
31.1674978258099));
#20640=CARTESIAN_POINT('Ctrl Pts',(-1.26902906603944,-2.96239504622687,
31.1681175424174));
#20641=CARTESIAN_POINT('Ctrl Pts',(-1.24768941140512,-2.97145762254765,
31.1695462600095));
#20642=CARTESIAN_POINT('Ctrl Pts',(-1.23559729415399,-2.97650610421951,
31.1703562769307));
#20643=CARTESIAN_POINT('Ctrl Pts',(-1.20317665311436,-2.98981017834674,
31.172529364861));
#20644=CARTESIAN_POINT('Ctrl Pts',(-1.18279432534424,-2.99793203835976,
31.1738969344998));
#20645=CARTESIAN_POINT('Ctrl Pts',(-1.00773512017665,-3.06562573231448,
31.1856564167914));
#20646=CARTESIAN_POINT('Ctrl Pts',(-0.848782439136819,-3.11338150543386,
31.1964449722444));
#20647=CARTESIAN_POINT('Ctrl Pts',(-0.434395662077885,-3.20377934986971,
31.2247473238573));
#20648=CARTESIAN_POINT('Ctrl Pts',(-0.176211266408086,-3.22828864967506,
31.2425983151369));
#20649=CARTESIAN_POINT('Ctrl Pts',(0.132728582943767,-3.22041351035558,
31.2627493596028));
#20650=CARTESIAN_POINT('Ctrl Pts',(0.183299244577456,-3.21793134201322,
31.2660056624235));
#20651=CARTESIAN_POINT('Ctrl Pts',(0.245067901590247,-3.21343851158656,
31.2699146502115));
#20652=CARTESIAN_POINT('Ctrl Pts',(0.256337977231287,-3.21255913479016,
31.2706250753855));
#20653=CARTESIAN_POINT('Ctrl Pts',(0.274005718662339,-3.21108699711769,
31.2717341563601));
#20654=CARTESIAN_POINT('Ctrl Pts',(0.280406506083703,-3.21053438386452,
31.2721350076566));
#20655=CARTESIAN_POINT('Ctrl Pts',(0.29237468242913,-3.20946504407314,31.2728826793606));
#20656=CARTESIAN_POINT('Ctrl Pts',(0.297942316656516,-3.20895297575298,
31.2732297471742));
#20657=CARTESIAN_POINT('Ctrl Pts',(0.31066653726288,-3.20774929785889,31.2740212433305));
#20658=CARTESIAN_POINT('Ctrl Pts',(0.317822147739402,-3.20704822852074,
31.2744651336936));
#20659=CARTESIAN_POINT('Ctrl Pts',(0.339876926421341,-3.20481287643749,
31.2758296904556));
#20660=CARTESIAN_POINT('Ctrl Pts',(0.354768043041343,-3.20319864414155,
31.2767459721483));
#20661=CARTESIAN_POINT('Ctrl Pts',(0.505824072391171,-3.18575749115097,
31.2859943710882));
#20662=CARTESIAN_POINT('Ctrl Pts',(0.640876943737671,-3.16135970489541,
31.2938823933859));
#20663=CARTESIAN_POINT('Ctrl Pts',(1.028700637433,-3.06541128591255,31.3164594356302));
#20664=CARTESIAN_POINT('Ctrl Pts',(1.27475853586173,-2.97152514696446,31.3307709033711));
#20665=CARTESIAN_POINT('Ctrl Pts',(1.57575540490046,-2.81233220896481,31.3506271984647));
#20666=CARTESIAN_POINT('Ctrl Pts',(1.64344145130215,-2.77332224217286,31.3552544523252));
#20667=CARTESIAN_POINT('Ctrl Pts',(1.72592224567952,-2.72170514570515,31.3611313730312));
#20668=CARTESIAN_POINT('Ctrl Pts',(1.74211273117079,-2.71137044784312,31.362296751054));
#20669=CARTESIAN_POINT('Ctrl Pts',(1.76767863291337,-2.69472771757317,31.3641562109556));
#20670=CARTESIAN_POINT('Ctrl Pts',(1.7771150878358,-2.68851393534968,31.3648467605085));
#20671=CARTESIAN_POINT('Ctrl Pts',(1.79481964606716,-2.67672177813273,31.3661504214758));
#20672=CARTESIAN_POINT('Ctrl Pts',(1.80309492706077,-2.67115437964214,31.3667631130432));
#20673=CARTESIAN_POINT('Ctrl Pts',(1.82165525362025,-2.65854191490187,31.3681449219851));
#20674=CARTESIAN_POINT('Ctrl Pts',(1.83192548822038,-2.65147543358933,31.368914848862));
#20675=CARTESIAN_POINT('Ctrl Pts',(1.85803464987177,-2.63328680023688,31.3708859184999));
#20676=CARTESIAN_POINT('Ctrl Pts',(1.87381468587425,-2.62208135439037,31.3720902444273));
#20677=CARTESIAN_POINT('Ctrl Pts',(1.96757747455022,-2.55422149283098,31.3793256191301));
#20678=CARTESIAN_POINT('Ctrl Pts',(2.0430802414395,-2.49423906658596,31.3854857708941));
#20679=CARTESIAN_POINT('Ctrl Pts',(2.30396033408986,-2.26718395342923,31.4080219771351));
#20680=CARTESIAN_POINT('Ctrl Pts',(2.47247462645146,-2.08211338324742,31.4250874709857));
#20681=CARTESIAN_POINT('Ctrl Pts',(2.66988731846174,-1.80713996142825,31.4478408691678));
#20682=CARTESIAN_POINT('Ctrl Pts',(2.71882086717044,-1.73264782152367,31.4537708082675));
#20683=CARTESIAN_POINT('Ctrl Pts',(2.78788242528316,-1.61736830213692,31.4625046006794));
#20684=CARTESIAN_POINT('Ctrl Pts',(2.81033694880198,-1.57802895209662,31.4654108346381));
#20685=CARTESIAN_POINT('Ctrl Pts',(2.83716596401702,-1.5286353388717,31.4689567372364));
#20686=CARTESIAN_POINT('Ctrl Pts',(2.84232719818813,-1.51901705492339,31.4696424499297));
#20687=CARTESIAN_POINT('Ctrl Pts',(2.85040827864743,-1.50377205276406,31.470721560723));
#20688=CARTESIAN_POINT('Ctrl Pts',(2.85336050637855,-1.49816272945965,31.4711169663542));
#20689=CARTESIAN_POINT('Ctrl Pts',(2.85889265290075,-1.48757581080624,31.4718600934118));
#20690=CARTESIAN_POINT('Ctrl Pts',(2.86147610101475,-1.48260025546768,31.4722080288655));
#20691=CARTESIAN_POINT('Ctrl Pts',(2.86735107478382,-1.47121287374998,31.4730013735598));
#20692=CARTESIAN_POINT('Ctrl Pts',(2.87063408080551,-1.46479673758719,31.4734462429657));
#20693=CARTESIAN_POINT('Ctrl Pts',(2.8792905639763,-1.44773807893706,31.4746235092059));
#20694=CARTESIAN_POINT('Ctrl Pts',(2.88462661645523,-1.43707654314635,31.4753536178085));
#20695=CARTESIAN_POINT('Ctrl Pts',(2.92166846062267,-1.36202855789241,31.4804549427931));
#20696=CARTESIAN_POINT('Ctrl Pts',(2.95127750749413,-1.2966229967614,31.4847052830448));
#20697=CARTESIAN_POINT('Ctrl Pts',(2.98840002265576,-1.206744045536,31.4903566161616));
#20698=CARTESIAN_POINT('Ctrl Pts',(2.99784112788908,-1.18309531003444,31.4918262255357));
#20699=CARTESIAN_POINT('Ctrl Pts',(3.0953211307437,-0.930258938984102,31.5073788004879));
#20700=CARTESIAN_POINT('Ctrl Pts',(3.15717797308431,-0.691833870314143,
31.5207207850651));
#20701=CARTESIAN_POINT('Ctrl Pts',(3.20810843219345,-0.329581809502716,
31.5415894227408));
#20702=CARTESIAN_POINT('Ctrl Pts',(3.21817157940083,-0.209644786509443,
31.5485814650545));
#20703=CARTESIAN_POINT('Ctrl Pts',(3.22233468156651,-0.0596859423883815,
31.5575690418416));
#20704=CARTESIAN_POINT('Ctrl Pts',(3.22274842593739,-0.0299283243626218,
31.5593642408183));
#20705=CARTESIAN_POINT('Ctrl Pts',(3.22275069678397,0.013125637980479,31.5619801628055));
#20706=CARTESIAN_POINT('Ctrl Pts',(3.22266912042875,0.0264209749777316,
31.5627905376577));
#20707=CARTESIAN_POINT('Ctrl Pts',(3.22238066351417,0.0498264277796811,
31.564221802491));
#20708=CARTESIAN_POINT('Ctrl Pts',(3.2222084637789,0.0599368479843692,31.5648415949953));
#20709=CARTESIAN_POINT('Ctrl Pts',(3.22175472590328,0.0808079060521612,
31.5661242706762));
#20710=CARTESIAN_POINT('Ctrl Pts',(3.22146685216968,0.0915682665137558,
31.5667873453523));
#20711=CARTESIAN_POINT('Ctrl Pts',(3.22059198451827,0.119108030738224,31.5684890342999));
#20712=CARTESIAN_POINT('Ctrl Pts',(3.21992776934796,0.135884497714904,31.5695300629698));
#20713=CARTESIAN_POINT('Ctrl Pts',(3.21663558675833,0.20530894412162,31.573856787698));
#20714=CARTESIAN_POINT('Ctrl Pts',(3.21284731003834,0.25789124199196,31.5771786793638));
#20715=CARTESIAN_POINT('Ctrl Pts',(3.19965030994605,0.394293153660462,31.5859178210813));
#20716=CARTESIAN_POINT('Ctrl Pts',(3.18823830804634,0.477874151793341,31.5913939256647));
#20717=CARTESIAN_POINT('Ctrl Pts',(3.14445865283243,0.725576076223137,31.60797138609));
#20718=CARTESIAN_POINT('Ctrl Pts',(3.10258378118853,0.887719845045409,31.6192996306446));
#20719=CARTESIAN_POINT('Ctrl Pts',(3.01491037780936,1.14325576822739,31.6375796691943));
#20720=CARTESIAN_POINT('Ctrl Pts',(2.97684767686744,1.23899080969529,31.6445258937912));
#20721=CARTESIAN_POINT('Ctrl Pts',(2.90234166504304,1.40302872606525,31.6564414513898));
#20722=CARTESIAN_POINT('Ctrl Pts',(2.86789988402392,1.47215119937337,31.6614661483235));
#20723=CARTESIAN_POINT('Ctrl Pts',(2.82519005897335,1.55066656982373,31.6671235811861));
#20724=CARTESIAN_POINT('Ctrl Pts',(2.81931389094956,1.56132471810529,31.667890449156));
#20725=CARTESIAN_POINT('Ctrl Pts',(2.80982639210189,1.57830485284822,31.6691101071988));
#20726=CARTESIAN_POINT('Ctrl Pts',(2.80625383981955,1.5846482105625,31.6695652728674));
#20727=CARTESIAN_POINT('Ctrl Pts',(2.79988749849229,1.59586311874077,31.6703690891598));
#20728=CARTESIAN_POINT('Ctrl Pts',(2.79710243476334,1.60073953824306,31.670718293671));
#20729=CARTESIAN_POINT('Ctrl Pts',(2.79116765895107,1.61106806384799,31.6714572524936));
#20730=CARTESIAN_POINT('Ctrl Pts',(2.7880147175561,1.61651821611255,31.6718467932604));
#20731=CARTESIAN_POINT('Ctrl Pts',(2.77944833126341,1.63122639470243,31.6728970701508));
#20732=CARTESIAN_POINT('Ctrl Pts',(2.7740045568614,1.64046679424992,31.6735558669272));
#20733=CARTESIAN_POINT('Ctrl Pts',(2.74655482399039,1.68653329691992,31.6768358705896));
#20734=CARTESIAN_POINT('Ctrl Pts',(2.72386005418996,1.72294654131337,31.6794146908492));
#20735=CARTESIAN_POINT('Ctrl Pts',(2.65565096034204,1.82766827149937,31.6868233460114));
#20736=CARTESIAN_POINT('Ctrl Pts',(2.60824427205007,1.89470764372552,31.6915564897157));
#20737=CARTESIAN_POINT('Ctrl Pts',(2.43181052036207,2.12501657687448,31.7080531236677));
#20738=CARTESIAN_POINT('Ctrl Pts',(2.2895999767914,2.27752815325309,31.7194497364084));
#20739=CARTESIAN_POINT('Ctrl Pts',(2.02606675822561,2.51033633097974,31.7394241746705));
#20740=CARTESIAN_POINT('Ctrl Pts',(1.91223555627755,2.59809210189347,31.7477507939705));
#20741=CARTESIAN_POINT('Ctrl Pts',(1.77513748361164,2.68988170841189,31.7576784157971));
#20742=CARTESIAN_POINT('Ctrl Pts',(1.75721426616615,2.70162445202023,31.7589741839566));
#20743=CARTESIAN_POINT('Ctrl Pts',(1.72827034813277,2.72017774348512,31.761064011697));
#20744=CARTESIAN_POINT('Ctrl Pts',(1.71732316860249,2.72710221283988,31.7618538175989));
#20745=CARTESIAN_POINT('Ctrl Pts',(1.69780236276659,2.73928564734107,31.7632612457228));
#20746=CARTESIAN_POINT('Ctrl Pts',(1.68924525600514,2.74457085573782,31.7638778858263));
#20747=CARTESIAN_POINT('Ctrl Pts',(1.67135380611016,2.7555059548212,31.7651665837162));
#20748=CARTESIAN_POINT('Ctrl Pts',(1.66201524342205,2.76114866282097,31.7658388954553));
#20749=CARTESIAN_POINT('Ctrl Pts',(1.6376618091582,2.77569560493259,31.7675914098761));
#20750=CARTESIAN_POINT('Ctrl Pts',(1.62260307893132,2.7845253673347,31.7686743132924));
#20751=CARTESIAN_POINT('Ctrl Pts',(1.55656196973952,2.82253127977033,31.7734207842086));
#20752=CARTESIAN_POINT('Ctrl Pts',(1.50486175287006,2.85043125926927,31.7771299314323));
#20753=CARTESIAN_POINT('Ctrl Pts',(1.36486941962881,2.92110769792734,31.7871628044619));
#20754=CARTESIAN_POINT('Ctrl Pts',(1.27534328842244,2.96128944846798,31.7935695094477));
#20755=CARTESIAN_POINT('Ctrl Pts',(1.00592154060091,3.06772795527495,31.8127877456447));
#20756=CARTESIAN_POINT('Ctrl Pts',(0.821794032291912,3.12209533876354,31.825866376912));
#20757=CARTESIAN_POINT('Ctrl Pts',(0.504123477055967,3.18582947391031,31.8476665198329));
#20758=CARTESIAN_POINT('Ctrl Pts',(0.372802525880266,3.20385338677006,31.8564568862512));
#20759=CARTESIAN_POINT('Ctrl Pts',(0.225836699110293,3.21486211855393,31.8658009966638));
#20760=CARTESIAN_POINT('Ctrl Pts',(0.210934196695225,3.21587428872627,31.8667428345717));
#20761=CARTESIAN_POINT('Ctrl Pts',(0.188856508110901,3.21721966268327,31.8681292238262));
#20762=CARTESIAN_POINT('Ctrl Pts',(0.181686631686446,3.21763253166805,31.8685780709914));
#20763=CARTESIAN_POINT('Ctrl Pts',(0.168933205012346,3.21832415812376,31.8693739112689));
#20764=CARTESIAN_POINT('Ctrl Pts',(0.163350260748968,3.21861235760456,31.869721427318));
#20765=CARTESIAN_POINT('Ctrl Pts',(0.151344318712029,3.21920080185935,31.8704668622995));
#20766=CARTESIAN_POINT('Ctrl Pts',(0.144921181813532,3.219496351647,31.8708645152377));
#20767=CARTESIAN_POINT('Ctrl Pts',(0.127179279637503,3.22025951193936,31.8719598308866));
#20768=CARTESIAN_POINT('Ctrl Pts',(0.115858737551582,3.2206866744906,31.8726552603862));
#20769=CARTESIAN_POINT('Ctrl Pts',(0.0535859592466406,3.22270767314267,
31.8764628696621));
#20770=CARTESIAN_POINT('Ctrl Pts',(0.0026005191167779,3.22315220177833,
31.879514623337));
#20771=CARTESIAN_POINT('Ctrl Pts',(-0.30644653896629,3.21851252337684,31.8977297161829));
#20772=CARTESIAN_POINT('Ctrl Pts',(-0.563142152439043,3.18365098370623,
31.9117265874135));
#20773=CARTESIAN_POINT('Ctrl Pts',(-0.97323564475835,3.07674618037183,31.9356542255654));
#20774=CARTESIAN_POINT('Ctrl Pts',(-1.13003988695846,3.02267329175473,31.945193963887));
#20775=CARTESIAN_POINT('Ctrl Pts',(-1.30211085083626,2.94806821739571,31.9564741096689));
#20776=CARTESIAN_POINT('Ctrl Pts',(-1.32214932118541,2.93913593056156,31.9578003951808));
#20777=CARTESIAN_POINT('Ctrl Pts',(-1.35400758018509,2.92454316587647,31.9599300105496));
#20778=CARTESIAN_POINT('Ctrl Pts',(-1.36588697026365,2.91901388019633,31.9607288208967));
#20779=CARTESIAN_POINT('Ctrl Pts',(-1.38684524465525,2.90910285995094,31.9621466338735));
#20780=CARTESIAN_POINT('Ctrl Pts',(-1.39593796128396,2.90475065831416,31.9627646040593));
#20781=CARTESIAN_POINT('Ctrl Pts',(-1.41476884922265,2.89562847219811,31.9640504181318));
#20782=CARTESIAN_POINT('Ctrl Pts',(-1.42450365209201,2.89085186170273,31.9647184877937));
#20783=CARTESIAN_POINT('Ctrl Pts',(-1.44957296956339,2.87839363555183,31.9664476998643));
#20784=CARTESIAN_POINT('Ctrl Pts',(-1.4648704512151,2.87063864986549,31.9675114103111));
#20785=CARTESIAN_POINT('Ctrl Pts',(-1.52976180869564,2.83708852395585,31.9720606513543));
#20786=CARTESIAN_POINT('Ctrl Pts',(-1.57873944633834,2.81012875383744,31.9755872074281));
#20787=CARTESIAN_POINT('Ctrl Pts',(-1.70595887772636,2.73572498833287,31.9850019091354));
#20788=CARTESIAN_POINT('Ctrl Pts',(-1.78291999315527,2.68620191243504,31.9909609131953));
#20789=CARTESIAN_POINT('Ctrl Pts',(-2.05925853040386,2.49127153967934,32.0133274329423));
#20790=CARTESIAN_POINT('Ctrl Pts',(-2.24383584015036,2.32640596420908,32.030306753817));
#20791=CARTESIAN_POINT('Ctrl Pts',(-2.46694642894772,2.07562343896931,32.0526134550647));
#20792=CARTESIAN_POINT('Ctrl Pts',(-2.52332550241131,2.00670597860277,32.0584323169291));
#20793=CARTESIAN_POINT('Ctrl Pts',(-2.5850855280914,1.92448471831555,32.0649450697155));
#20794=CARTESIAN_POINT('Ctrl Pts',(-2.59331599054158,1.91337942078905,32.0658160228391));
#20795=CARTESIAN_POINT('Ctrl Pts',(-2.60563741479335,1.89652865979826,32.0671240678157));
#20796=CARTESIAN_POINT('Ctrl Pts',(-2.60978126059345,1.89082232610839,32.067564706639));
#20797=CARTESIAN_POINT('Ctrl Pts',(-2.61716997635998,1.88057704095503,32.0683516309602));
#20798=CARTESIAN_POINT('Ctrl Pts',(-2.62042180798153,1.8760432409532,32.0686983935701));
#20799=CARTESIAN_POINT('Ctrl Pts',(-2.62744857736224,1.86619239491428,32.069448630815));
#20800=CARTESIAN_POINT('Ctrl Pts',(-2.63121914591467,1.86087234636604,32.0698518051053));
#20801=CARTESIAN_POINT('Ctrl Pts',(-2.64173504824622,1.84593916661408,32.0709780254229));
#20802=CARTESIAN_POINT('Ctrl Pts',(-2.64844410444986,1.83630044041457,32.0716986260889));
#20803=CARTESIAN_POINT('Ctrl Pts',(-2.68771429101991,1.77921905537042,32.0759302812312));
#20804=CARTESIAN_POINT('Ctrl Pts',(-2.71905502894969,1.73094461396924,32.0793639337899));
#20805=CARTESIAN_POINT('Ctrl Pts',(-2.8811429292694,1.46600240786322,32.0975864920437));
#20806=CARTESIAN_POINT('Ctrl Pts',(-2.9873285869846,1.23533075697919,32.1113206172386));
#20807=CARTESIAN_POINT('Ctrl Pts',(-3.11588232448205,0.839114198316271,
32.1348517909764));
#20808=CARTESIAN_POINT('Ctrl Pts',(-3.15441968612414,0.680045115225367,
32.1442721065176));
#20809=CARTESIAN_POINT('Ctrl Pts',(-3.1842497645424,0.497142249588672,32.1554186119938));
#20810=CARTESIAN_POINT('Ctrl Pts',(-3.18755381343815,0.475497244479642,
32.1567423090101));
#20811=CARTESIAN_POINT('Ctrl Pts',(-3.19248036675914,0.440860558960777,
32.1588685520131));
#20812=CARTESIAN_POINT('Ctrl Pts',(-3.19424474433226,0.427889506718449,
32.1596666013287));
#20813=CARTESIAN_POINT('Ctrl Pts',(-3.19722759199732,0.404913407159634,
32.1610835334345));
#20814=CARTESIAN_POINT('Ctrl Pts',(-3.19847825210967,0.394912660524777,
32.1617013880439));
#20815=CARTESIAN_POINT('Ctrl Pts',(-3.20097771890057,0.374134879547901,
32.1629874302397));
#20816=CARTESIAN_POINT('Ctrl Pts',(-3.20221905637688,0.363357090697862,
32.1636558459299));
#20817=CARTESIAN_POINT('Ctrl Pts',(-3.20528499900597,0.335500592200841,
32.1653869608449));
#20818=CARTESIAN_POINT('Ctrl Pts',(-3.20702751516114,0.31841336468411,32.1664522388526));
#20819=CARTESIAN_POINT('Ctrl Pts',(-3.2138810478703,0.245431274437439,32.1710172718786));
#20820=CARTESIAN_POINT('Ctrl Pts',(-3.21766771403154,0.189424769271709,
32.1745584075382));
#20821=CARTESIAN_POINT('Ctrl Pts',(-3.22379684662015,0.0414259104642137,
32.1840219221749));
#20822=CARTESIAN_POINT('Ctrl Pts',(-3.22366532132784,-0.0506120853055336,
32.1900160767371));
#20823=CARTESIAN_POINT('Ctrl Pts',(-3.20889753582343,-0.384242628219668,
32.2121092770526));
#20824=CARTESIAN_POINT('Ctrl Pts',(-3.17101047327491,-0.623973968916234,
32.228749640117));
#20825=CARTESIAN_POINT('Ctrl Pts',(-3.08200055192469,-0.94656489273503,
32.2510192745402));
#20826=CARTESIAN_POINT('Ctrl Pts',(-3.05349410165831,-1.03483803166881,
32.2570894886258));
#20827=CARTESIAN_POINT('Ctrl Pts',(-3.01636191059413,-1.13484492181403,
32.2638467849155));
#20828=CARTESIAN_POINT('Ctrl Pts',(-3.01142116997953,-1.14789142596748,
32.2647258998003));
#20829=CARTESIAN_POINT('Ctrl Pts',(-3.00384559654875,-1.16750987703003,
32.2660437598006));
#20830=CARTESIAN_POINT('Ctrl Pts',(-3.00127364536192,-1.1741056974553,32.2664861297846));
#20831=CARTESIAN_POINT('Ctrl Pts',(-2.99663512387307,-1.18588644032712,
32.2672749184583));
#20832=CARTESIAN_POINT('Ctrl Pts',(-2.99457680639064,-1.19107450110663,
32.2676218239455));
#20833=CARTESIAN_POINT('Ctrl Pts',(-2.99009201281197,-1.20229346454582,
32.2683709751067));
#20834=CARTESIAN_POINT('Ctrl Pts',(-2.98766077210108,-1.20832236285817,
32.2687729279583));
#20835=CARTESIAN_POINT('Ctrl Pts',(-2.98082103074559,-1.22513644049199,
32.2698922904996));
#20836=CARTESIAN_POINT('Ctrl Pts',(-2.97637220712789,-1.23590525909468,
32.2706073026539));
#20837=CARTESIAN_POINT('Ctrl Pts',(-2.95020250469586,-1.2982907150566,32.2747397485273));
#20838=CARTESIAN_POINT('Ctrl Pts',(-2.92719613655321,-1.34936179668311,
32.2780839514318));
#20839=CARTESIAN_POINT('Ctrl Pts',(-2.79246879816565,-1.628753695155,32.2963009923558));
#20840=CARTESIAN_POINT('Ctrl Pts',(-2.65536268545062,-1.84385383607882,
32.3100938861088));
#20841=CARTESIAN_POINT('Ctrl Pts',(-2.39053701552614,-2.16756793231108,
32.3337171517172));
#20842=CARTESIAN_POINT('Ctrl Pts',(-2.27715943863118,-2.28638413007821,
32.3431679597455));
#20843=CARTESIAN_POINT('Ctrl Pts',(-2.13895533847233,-2.41069855614808,
32.3543485735389));
#20844=CARTESIAN_POINT('Ctrl Pts',(-2.1225194768875,-2.42518215862843,32.3556729365911));
#20845=CARTESIAN_POINT('Ctrl Pts',(-2.09602604277873,-2.44805307089488,
32.3578000473681));
#20846=CARTESIAN_POINT('Ctrl Pts',(-2.08606261272699,-2.45654875338665,
32.3585982925504));
#20847=CARTESIAN_POINT('Ctrl Pts',(-2.06833853309669,-2.47147625218798,
32.3600154513119));
#20848=CARTESIAN_POINT('Ctrl Pts',(-2.06059891875293,-2.4779328572401,32.3606333356133));
#20849=CARTESIAN_POINT('Ctrl Pts',(-2.04446697060567,-2.49126274012229,
32.3619193188305));
#20850=CARTESIAN_POINT('Ctrl Pts',(-2.0360699780651,-2.49813015554321,32.3625876452498));
#20851=CARTESIAN_POINT('Ctrl Pts',(-2.01429324732095,-2.51575735412601,
32.364318269295));
#20852=CARTESIAN_POINT('Ctrl Pts',(-2.00086204017969,-2.52645273631248,
32.3653831429305));
#20853=CARTESIAN_POINT('Ctrl Pts',(-1.94320690599002,-2.57161588211964,
32.3699440969464));
#20854=CARTESIAN_POINT('Ctrl Pts',(-1.89817521076367,-2.60503196845777,
32.3734814660727));
#20855=CARTESIAN_POINT('Ctrl Pts',(-1.77711819326298,-2.69005733091694,
32.3829323612883));
#20856=CARTESIAN_POINT('Ctrl Pts',(-1.69972217332263,-2.739616676277,32.3889174252026));
#20857=CARTESIAN_POINT('Ctrl Pts',(-1.57263946449086,-2.81353253129002,
32.3986427283713));
#20858=CARTESIAN_POINT('Ctrl Pts',(-1.52426796674987,-2.84002883744678,
32.4023216146312));
#20859=CARTESIAN_POINT('Ctrl Pts',(-1.47525529429555,-2.86526427736657,
32.4060211118892));
#20860=CARTESIAN_POINT('Origin',(0.,0.,4.68922655072688));
#20861=CARTESIAN_POINT('',(-1.47525541125577,-2.86526421714657,33.905101584668));
#20862=CARTESIAN_POINT('',(-1.47525540501188,-2.8652642203614,33.660216611122));
#20863=CARTESIAN_POINT('',(-1.47525540501186,-2.86526422036142,4.68922655072688));
#20864=CARTESIAN_POINT('Ctrl Pts',(-1.47525541125578,-2.86526421714657,
33.905101584668));
#20865=CARTESIAN_POINT('Ctrl Pts',(-1.69531057939917,-2.75196312064189,
33.8885652916234));
#20866=CARTESIAN_POINT('Ctrl Pts',(-1.90159038241384,-2.61368528888915,
33.8714955802727));
#20867=CARTESIAN_POINT('Ctrl Pts',(-2.13267762831647,-2.41680448803221,
33.8516382700764));
#20868=CARTESIAN_POINT('Ctrl Pts',(-2.17438145576787,-2.37935369134562,
33.8480249354861));
#20869=CARTESIAN_POINT('Ctrl Pts',(-2.22355671916634,-2.3328199566314,33.843749694358));
#20870=CARTESIAN_POINT('Ctrl Pts',(-2.23197990031346,-2.32476217446094,
33.8430168632812));
#20871=CARTESIAN_POINT('Ctrl Pts',(-2.2450340267972,-2.31213798699392,33.8418805711419));
#20872=CARTESIAN_POINT('Ctrl Pts',(-2.2496950809723,-2.30760306309399,33.841474738603));
#20873=CARTESIAN_POINT('Ctrl Pts',(-2.25833249464318,-2.29914833821134,
33.8407225351419));
#20874=CARTESIAN_POINT('Ctrl Pts',(-2.26231235584596,-2.29523235049462,
33.8403758875435));
#20875=CARTESIAN_POINT('Ctrl Pts',(-2.27131713211602,-2.28632591725271,
33.8395914196449));
#20876=CARTESIAN_POINT('Ctrl Pts',(-2.27633577540863,-2.28132925164277,
33.8391540993561));
#20877=CARTESIAN_POINT('Ctrl Pts',(-2.29119454430668,-2.26643770179881,
33.8378588336379));
#20878=CARTESIAN_POINT('Ctrl Pts',(-2.30098706692023,-2.25649525374923,
33.8370045653312));
#20879=CARTESIAN_POINT('Ctrl Pts',(-2.37536362752936,-2.17999231793096,
33.8305082990117));
#20880=CARTESIAN_POINT('Ctrl Pts',(-2.43711849971667,-2.11072872725382,
33.8250681649327));
#20881=CARTESIAN_POINT('Ctrl Pts',(-2.64884877933328,-1.85154983181771,
33.805833806235));
#20882=CARTESIAN_POINT('Ctrl Pts',(-2.78031828541351,-1.64756778863008,
33.7926799463854));
#20883=CARTESIAN_POINT('Ctrl Pts',(-2.92856712725885,-1.34835968307134,
33.7736701677506));
#20884=CARTESIAN_POINT('Ctrl Pts',(-2.9658558378288,-1.26422959548301,33.7683608390868));
#20885=CARTESIAN_POINT('Ctrl Pts',(-3.02001976497589,-1.12638724235393,
33.759627878908));
#20886=CARTESIAN_POINT('Ctrl Pts',(-3.03917676958496,-1.07362544056749,
33.7562778596431));
#20887=CARTESIAN_POINT('Ctrl Pts',(-3.06238494401519,-1.00409717961567,
33.7518423181365));
#20888=CARTESIAN_POINT('Ctrl Pts',(-3.06769382018977,-0.987758725213661,
33.750798540593));
#20889=CARTESIAN_POINT('Ctrl Pts',(-3.07614276474595,-0.96103123062179,
33.7490883531957));
#20890=CARTESIAN_POINT('Ctrl Pts',(-3.07936147513867,-0.950667258406022,
33.7484245430008));
#20891=CARTESIAN_POINT('Ctrl Pts',(-3.08546945383179,-0.930643577050133,
33.7471406748097));
#20892=CARTESIAN_POINT('Ctrl Pts',(-3.08836586201137,-0.920986165319195,
33.7465208601634));
#20893=CARTESIAN_POINT('Ctrl Pts',(-3.09492024947608,-0.898753431200608,
33.745092496014));
#20894=CARTESIAN_POINT('Ctrl Pts',(-3.0985469678971,-0.886169148813521,
33.7442829338374));
#20895=CARTESIAN_POINT('Ctrl Pts',(-3.1080352656065,-0.852475403032485,
33.7421123505938));
#20896=CARTESIAN_POINT('Ctrl Pts',(-3.11375838516319,-0.83132797713795,
33.7407468490101));
#20897=CARTESIAN_POINT('Ctrl Pts',(-3.16045129693933,-0.651543728185929,
33.7291094096636));
#20898=CARTESIAN_POINT('Ctrl Pts',(-3.18947801955127,-0.490078475075718,
33.7184503186501));
#20899=CARTESIAN_POINT('Ctrl Pts',(-3.23190277618421,-0.0742830768988021,
33.6905743230458));
#20900=CARTESIAN_POINT('Ctrl Pts',(-3.22770070291164,0.180712163993436,
33.6730301942253));
#20901=CARTESIAN_POINT('Ctrl Pts',(-3.18604612106548,0.488247502101714,
33.6527289717567));
#20902=CARTESIAN_POINT('Ctrl Pts',(-3.17704768323688,0.543731954564406,
33.649105216305));
#20903=CARTESIAN_POINT('Ctrl Pts',(-3.16443393072998,0.610419163202396,
33.6448193489147));
#20904=CARTESIAN_POINT('Ctrl Pts',(-3.16220352100297,0.6218702102047,33.6440859086618));
#20905=CARTESIAN_POINT('Ctrl Pts',(-3.15863259880329,0.639687412197749,
33.6429488797428));
#20906=CARTESIAN_POINT('Ctrl Pts',(-3.15733493503664,0.64606190827203,33.6425429147233));
#20907=CARTESIAN_POINT('Ctrl Pts',(-3.15488766311264,0.6579001201662,33.6417905917697));
#20908=CARTESIAN_POINT('Ctrl Pts',(-3.15374316922362,0.663364724915909,
33.6414439563693));
#20909=CARTESIAN_POINT('Ctrl Pts',(-3.15111534014424,0.67575127595778,33.6406596765853));
#20910=CARTESIAN_POINT('Ctrl Pts',(-3.14962339958502,0.682671309559527,
33.6402225312141));
#20911=CARTESIAN_POINT('Ctrl Pts',(-3.14512558941835,0.70320476860301,33.638928263838));
#20912=CARTESIAN_POINT('Ctrl Pts',(-3.14205412789166,0.716803873792837,
33.6380748105598));
#20913=CARTESIAN_POINT('Ctrl Pts',(-3.11796838207419,0.820314804306374,
33.6316041442122));
#20914=CARTESIAN_POINT('Ctrl Pts',(-3.09318485771091,0.90931516952203,33.6261870017195));
#20915=CARTESIAN_POINT('Ctrl Pts',(-2.98960636892076,1.22765446023291,33.6069432922198));
#20916=CARTESIAN_POINT('Ctrl Pts',(-2.88883154327705,1.44898135043722,33.5937634997309));
#20917=CARTESIAN_POINT('Ctrl Pts',(-2.71691602821771,1.73578157202477,33.5747272151386));
#20918=CARTESIAN_POINT('Ctrl Pts',(-2.66629737136026,1.81257462390482,33.5694205565016));
#20919=CARTESIAN_POINT('Ctrl Pts',(-2.57961614449665,1.93257490994135,33.5606915871537));
#20920=CARTESIAN_POINT('Ctrl Pts',(-2.54558375648294,1.97718688992095,33.5573428006244));
#20921=CARTESIAN_POINT('Ctrl Pts',(-2.4996346696397,2.03426623877532,33.552908664357));
#20922=CARTESIAN_POINT('Ctrl Pts',(-2.48875687277528,2.04755996794475,33.5518650257321));
#20923=CARTESIAN_POINT('Ctrl Pts',(-2.47083436820923,2.06910919217336,33.5501550087713));
#20924=CARTESIAN_POINT('Ctrl Pts',(-2.46385322311762,2.07741729429547,33.5494912290946));
#20925=CARTESIAN_POINT('Ctrl Pts',(-2.45030507612276,2.09337628143266,33.5482073797634));
#20926=CARTESIAN_POINT('Ctrl Pts',(-2.44374386012715,2.10103192839646,33.5475875532427));
#20927=CARTESIAN_POINT('Ctrl Pts',(-2.42857703578079,2.11856146776315,33.5461591041454));
#20928=CARTESIAN_POINT('Ctrl Pts',(-2.41994698695365,2.12841388916854,33.5453494685017));
#20929=CARTESIAN_POINT('Ctrl Pts',(-2.39671911886759,2.15460789154794,33.5431785601508));
#20930=CARTESIAN_POINT('Ctrl Pts',(-2.3820144899698,2.17085343409826,33.5418128048172));
#20931=CARTESIAN_POINT('Ctrl Pts',(-2.25582664871502,2.30743879070337,33.5301624610827));
#20932=CARTESIAN_POINT('Ctrl Pts',(-2.13548825528763,2.41923599937711,33.5194897257598));
#20933=CARTESIAN_POINT('Ctrl Pts',(-1.8080037731613,2.6799351616483,33.4915704096102));
#20934=CARTESIAN_POINT('Ctrl Pts',(-1.59075110143172,2.81432697847393,33.4739956753835));
#20935=CARTESIAN_POINT('Ctrl Pts',(-1.30952439907176,2.94522622309955,33.4537104289571));
#20936=CARTESIAN_POINT('Ctrl Pts',(-1.25849202675051,2.96739117090903,33.4501243800596));
#20937=CARTESIAN_POINT('Ctrl Pts',(-1.196123234236,2.99258116920105,33.4458769776246));
#20938=CARTESIAN_POINT('Ctrl Pts',(-1.18531482125331,2.99687864785867,33.445145751741));
#20939=CARTESIAN_POINT('Ctrl Pts',(-1.1684324706784,3.00348553222065,33.4440114012174));
#20940=CARTESIAN_POINT('Ctrl Pts',(-1.16237454416993,3.00583519202732,33.4436059179311));
#20941=CARTESIAN_POINT('Ctrl Pts',(-1.15109724614366,3.01017007394198,33.4428540288283));
#20942=CARTESIAN_POINT('Ctrl Pts',(-1.14587987259306,3.01216003267126,33.4425073484203));
#20943=CARTESIAN_POINT('Ctrl Pts',(-1.13402671092958,3.01664569370343,33.4417223816341));
#20944=CARTESIAN_POINT('Ctrl Pts',(-1.1273878591714,3.01913306094684,33.4412845979136));
#20945=CARTESIAN_POINT('Ctrl Pts',(-1.10762355498596,3.02646383684378,33.4399866853785));
#20946=CARTESIAN_POINT('Ctrl Pts',(-1.09447451287261,3.03124377977235,33.4391302559923));
#20947=CARTESIAN_POINT('Ctrl Pts',(-0.992885538735602,3.0674262037669,33.4325647818383));
#20948=CARTESIAN_POINT('Ctrl Pts',(-0.903134053152203,3.09504081957385,
33.4270624925609));
#20949=CARTESIAN_POINT('Ctrl Pts',(-0.579511025181729,3.17933165576605,
33.4078525535622));
#20950=CARTESIAN_POINT('Ctrl Pts',(-0.340662388143395,3.2137119089271,33.3947681847463));
#20951=CARTESIAN_POINT('Ctrl Pts',(-0.0081356523373253,3.22405577500048,
33.3758297082113));
#20952=CARTESIAN_POINT('Ctrl Pts',(0.0840042197246141,3.22297117284149,
33.3705136011199));
#20953=CARTESIAN_POINT('Ctrl Pts',(0.232061255261061,3.21487498674679,33.3617705103617));
#20954=CARTESIAN_POINT('Ctrl Pts',(0.288063533020512,3.21034148164816,33.3584173627918));
#20955=CARTESIAN_POINT('Ctrl Pts',(0.361003346803763,3.20251299401827,33.3539782553722));
#20956=CARTESIAN_POINT('Ctrl Pts',(0.378075196832905,3.20054245730381,33.3529341255126));
#20957=CARTESIAN_POINT('Ctrl Pts',(0.405901942940358,3.19710478028528,33.3512235058603));
#20958=CARTESIAN_POINT('Ctrl Pts',(0.416666771839865,3.19571966231283,33.3505596182623));
#20959=CARTESIAN_POINT('Ctrl Pts',(0.437417203064515,3.19294306230467,33.3492757021845));
#20960=CARTESIAN_POINT('Ctrl Pts',(0.447403689089852,3.19155904597713,33.3486559176027));
#20961=CARTESIAN_POINT('Ctrl Pts',(0.470344416225842,3.18826992788678,33.3472277686543));
#20962=CARTESIAN_POINT('Ctrl Pts',(0.483293803830338,3.18633270296559,33.3464183926119));
#20963=CARTESIAN_POINT('Ctrl Pts',(0.51786759911378,3.18094486418892,33.3442486329774));
#20964=CARTESIAN_POINT('Ctrl Pts',(0.539468950392259,3.17735271768103,33.3428837742108));
#20965=CARTESIAN_POINT('Ctrl Pts',(0.721871183864628,3.14510690047236,33.3312788992833));
#20966=CARTESIAN_POINT('Ctrl Pts',(0.880291141178254,3.1044916454797,33.3206542310558));
#20967=CARTESIAN_POINT('Ctrl Pts',(1.27465914894822,2.97076405636814,33.2928840606322));
#20968=CARTESIAN_POINT('Ctrl Pts',(1.50396205133326,2.86151849308659,33.2754134187567));
#20969=CARTESIAN_POINT('Ctrl Pts',(1.76684169685521,2.69586812064414,33.255071961419));
#20970=CARTESIAN_POINT('Ctrl Pts',(1.81473942900712,2.6638611611531,33.2513558726949));
#20971=CARTESIAN_POINT('Ctrl Pts',(1.87134729900661,2.62379780019707,33.2469759900922));
#20972=CARTESIAN_POINT('Ctrl Pts',(1.88090075121767,2.6169577726662,33.2462372439097));
#20973=CARTESIAN_POINT('Ctrl Pts',(1.89569991469763,2.60623904308241,33.2450937992664));
#20974=CARTESIAN_POINT('Ctrl Pts',(1.90097150091154,2.60239648608435,33.2446866817957));
#20975=CARTESIAN_POINT('Ctrl Pts',(1.91073177118265,2.59523656204553,33.2439333137136));
#20976=CARTESIAN_POINT('Ctrl Pts',(1.9152234632616,2.59192357157722,33.2435867787757));
#20977=CARTESIAN_POINT('Ctrl Pts',(1.92537281045458,2.58439680891437,33.2428041097164));
#20978=CARTESIAN_POINT('Ctrl Pts',(1.93102523661592,2.58017613021912,33.2423684660254));
#20979=CARTESIAN_POINT('Ctrl Pts',(1.94771465926231,2.56762853974097,33.2410827544212));
#20980=CARTESIAN_POINT('Ctrl Pts',(1.95871214737732,2.55924900148646,33.2402362836725));
#20981=CARTESIAN_POINT('Ctrl Pts',(2.04009586749581,2.49640676504022,33.2339749825782));
#20982=CARTESIAN_POINT('Ctrl Pts',(2.10825996911913,2.43911477734735,33.2287458794735));
#20983=CARTESIAN_POINT('Ctrl Pts',(2.35608028398883,2.21265889393444,33.2094167756447));
#20984=CARTESIAN_POINT('Ctrl Pts',(2.51848755508962,2.02588463223565,33.1960181108751));
#20985=CARTESIAN_POINT('Ctrl Pts',(2.7097195090643,1.74696940995367,33.1767612676353));
#20986=CARTESIAN_POINT('Ctrl Pts',(2.75819883300765,1.66937689846189,33.1714812702249));
#20987=CARTESIAN_POINT('Ctrl Pts',(2.83088391091098,1.54121313355475,33.1627921629424));
#20988=CARTESIAN_POINT('Ctrl Pts',(2.85718615166249,1.49188751739117,33.1594557010843));
#20989=CARTESIAN_POINT('Ctrl Pts',(2.88986626982433,1.42656396915544,33.1550356160375));
#20990=CARTESIAN_POINT('Ctrl Pts',(2.89741840600205,1.41116206667512,33.1539933689585));
#20991=CARTESIAN_POINT('Ctrl Pts',(2.90954457508609,1.38592408847538,33.1522850591905));
#20992=CARTESIAN_POINT('Ctrl Pts',(2.91419260448723,1.37612378543218,33.1516215851556));
#20993=CARTESIAN_POINT('Ctrl Pts',(2.92306638619555,1.35716696133607,33.1503379240567));
#20994=CARTESIAN_POINT('Ctrl Pts',(2.92729881354909,1.34801369115939,33.1497179779593));
#20995=CARTESIAN_POINT('Ctrl Pts',(2.93693428517259,1.32691613323543,33.1482886750025));
#20996=CARTESIAN_POINT('Ctrl Pts',(2.94230752113732,1.31495850237124,33.1474783011181));
#20997=CARTESIAN_POINT('Ctrl Pts',(2.95648303512143,1.28289030530972,33.1453041249689));
#20998=CARTESIAN_POINT('Ctrl Pts',(2.96515291693345,1.26272230244952,33.1439358188462));
#20999=CARTESIAN_POINT('Ctrl Pts',(3.03764845674439,1.08921767808597,33.1321543217278));
#21000=CARTESIAN_POINT('Ctrl Pts',(3.08972834569552,0.931271594622281,33.1213428036412));
#21001=CARTESIAN_POINT('Ctrl Pts',(3.19149484625394,0.517696489777949,33.0929191056644));
#21002=CARTESIAN_POINT('Ctrl Pts',(3.22283672148331,0.258783790515589,33.0749644616394));
#21003=CARTESIAN_POINT('Ctrl Pts',(3.22273372058091,-0.0492191042587242,
33.0549003123629));
#21004=CARTESIAN_POINT('Ctrl Pts',(3.22163891785126,-0.0973572008384966,
33.0518049848874));
#21005=CARTESIAN_POINT('Ctrl Pts',(3.21894454657732,-0.156993514469821,
33.0480350902363));
#21006=CARTESIAN_POINT('Ctrl Pts',(3.21836123360326,-0.168528742632896,
33.0473089059134));
#21007=CARTESIAN_POINT('Ctrl Pts',(3.21734997899298,-0.186600028739783,
33.0461762373029));
#21008=CARTESIAN_POINT('Ctrl Pts',(3.21696411126131,-0.19313820626645,33.0457674616939));
#21009=CARTESIAN_POINT('Ctrl Pts',(3.21621264563369,-0.205243528497641,
33.0450125726018));
#21010=CARTESIAN_POINT('Ctrl Pts',(3.21585252668228,-0.210810852038877,
33.044666164964));
#21011=CARTESIAN_POINT('Ctrl Pts',(3.21500663215855,-0.223381276763552,
33.0438857350055));
#21012=CARTESIAN_POINT('Ctrl Pts',(3.21451243296257,-0.230383723740913,
33.0434521910989));
#21013=CARTESIAN_POINT('Ctrl Pts',(3.21295572147802,-0.25146033922258,33.0421507348878));
#21014=CARTESIAN_POINT('Ctrl Pts',(3.21182361217343,-0.265529417527553,
33.0412866388439));
#21015=CARTESIAN_POINT('Ctrl Pts',(3.19904455428085,-0.412273933941461,
33.0323182273948));
#21016=CARTESIAN_POINT('Ctrl Pts',(3.17927452020103,-0.544130897736348,
33.0246362002165));
#21017=CARTESIAN_POINT('Ctrl Pts',(3.10313446795583,-0.899924678833476,
33.0040428507792));
#21018=CARTESIAN_POINT('Ctrl Pts',(3.03080510532378,-1.11961172746976,32.9914320538523));
#21019=CARTESIAN_POINT('Ctrl Pts',(2.89049461495532,-1.42938224049477,32.9718833329992));
#21020=CARTESIAN_POINT('Ctrl Pts',(2.84030004951245,-1.52669072770253,32.9654699017901));
#21021=CARTESIAN_POINT('Ctrl Pts',(2.77513067424075,-1.63864961379603,32.9576661513925));
#21022=CARTESIAN_POINT('Ctrl Pts',(2.76484091562407,-1.65595214271126,32.9564477532775));
#21023=CARTESIAN_POINT('Ctrl Pts',(2.74779316749824,-1.6840165442531,32.9544506857886));
#21024=CARTESIAN_POINT('Ctrl Pts',(2.74113233740833,-1.69483701700616,32.9536755793747));
#21025=CARTESIAN_POINT('Ctrl Pts',(2.72911488678863,-1.71410312240555,32.9522861707441));
#21026=CARTESIAN_POINT('Ctrl Pts',(2.72378258546942,-1.72256378780028,32.9516727747768));
#21027=CARTESIAN_POINT('Ctrl Pts',(2.71241854528443,-1.74041020177461,32.9503719712198));
#21028=CARTESIAN_POINT('Ctrl Pts',(2.70637728709467,-1.74978970454354,32.9496842137768));
#21029=CARTESIAN_POINT('Ctrl Pts',(2.69015916161012,-1.77468463189595,32.9478477257405));
#21030=CARTESIAN_POINT('Ctrl Pts',(2.67989691012695,-1.79014367729256,32.9466957972543));
#21031=CARTESIAN_POINT('Ctrl Pts',(2.63020288933737,-1.8636176895258,32.9411647669136));
#21032=CARTESIAN_POINT('Ctrl Pts',(2.58902001193395,-1.92041981612103,32.9367193943096));
#21033=CARTESIAN_POINT('Ctrl Pts',(2.38118906282716,-2.18822709486243,32.9149068709048));
#21034=CARTESIAN_POINT('Ctrl Pts',(2.19044650969267,-2.37913801747994,32.8965735669121));
#21035=CARTESIAN_POINT('Ctrl Pts',(1.86788299037469,-2.62995918748407,32.8690426065043));
#21036=CARTESIAN_POINT('Ctrl Pts',(1.75200738177078,-2.70853313399905,32.8597365172584));
#21037=CARTESIAN_POINT('Ctrl Pts',(1.61844249412796,-2.78693138080748,32.8499163928834));
#21038=CARTESIAN_POINT('Ctrl Pts',(1.60545126594163,-2.7944353421264,32.8489703493416));
#21039=CARTESIAN_POINT('Ctrl Pts',(1.58615162590132,-2.80540413573197,32.8475788888995));
#21040=CARTESIAN_POINT('Ctrl Pts',(1.57988346991535,-2.80893886886205,32.847129132862));
#21041=CARTESIAN_POINT('Ctrl Pts',(1.568722103029,-2.81518379735845,32.8463321876864));
#21042=CARTESIAN_POINT('Ctrl Pts',(1.56383363175756,-2.81790227355953,32.8459844710727));
#21043=CARTESIAN_POINT('Ctrl Pts',(1.55331518497217,-2.82371577400936,32.8452391639311));
#21044=CARTESIAN_POINT('Ctrl Pts',(1.54768304064095,-2.82680668664678,32.8448418366374));
#21045=CARTESIAN_POINT('Ctrl Pts',(1.532121307783,-2.83528649265728,32.8437487282991));
#21046=CARTESIAN_POINT('Ctrl Pts',(1.52217245422814,-2.84064010843147,32.8430551646226));
#21047=CARTESIAN_POINT('Ctrl Pts',(1.4676109664777,-2.86963144170824,32.839279166703));
#21048=CARTESIAN_POINT('Ctrl Pts',(1.4224730007517,-2.89227207938064,32.8362559736934));
#21049=CARTESIAN_POINT('Ctrl Pts',(1.14300628456107,-3.02432273839991,32.8180339684018));
#21050=CARTESIAN_POINT('Ctrl Pts',(0.896722641424523,-3.10626955590679,
32.8040112962091));
#21051=CARTESIAN_POINT('Ctrl Pts',(0.480927071639537,-3.19096773218185,
32.7800536650873));
#21052=CARTESIAN_POINT('Ctrl Pts',(0.316298426956155,-3.21146547745588,
32.7705121173458));
#21053=CARTESIAN_POINT('Ctrl Pts',(0.128916173166071,-3.22024529389398,
32.7592296494377));
#21054=CARTESIAN_POINT('Ctrl Pts',(0.106986027989452,-3.22104844513118,
32.7579030245892));
#21055=CARTESIAN_POINT('Ctrl Pts',(0.0719471716861846,-3.22197345821536,
32.7557728256951));
#21056=CARTESIAN_POINT('Ctrl Pts',(0.0588427122529572,-3.22223942130419,
32.7549737732803));
#21057=CARTESIAN_POINT('Ctrl Pts',(0.0356540445916773,-3.22256854713764,
32.7535555064266));
#21058=CARTESIAN_POINT('Ctrl Pts',(0.0255704203228948,-3.22266433278892,
32.7529373249543));
#21059=CARTESIAN_POINT('Ctrl Pts',(0.00463905159577563,-3.22276491754879,
32.7516510463084));
#21060=CARTESIAN_POINT('Ctrl Pts',(-0.00620858570992438,-3.22276227535319,
32.7509827230848));
#21061=CARTESIAN_POINT('Ctrl Pts',(-0.0342138956032114,-3.22261405957662,
32.7492527988418));
#21062=CARTESIAN_POINT('Ctrl Pts',(-0.0513706203514442,-3.22238622896835,
32.7481886274113));
#21063=CARTESIAN_POINT('Ctrl Pts',(-0.124445632281463,-3.22083210378685,
32.743636855234));
#21064=CARTESIAN_POINT('Ctrl Pts',(-0.180323326982917,-3.21818722595246,
32.7401081796733));
#21065=CARTESIAN_POINT('Ctrl Pts',(-0.32740542293295,-3.20738284186303,
32.7306869690326));
#21066=CARTESIAN_POINT('Ctrl Pts',(-0.418374846235888,-3.19678885765793,
32.7247234667327));
#21067=CARTESIAN_POINT('Ctrl Pts',(-0.751736903474163,-3.14349393027239,
32.7023943564808));
#21068=CARTESIAN_POINT('Ctrl Pts',(-0.98943642851421,-3.07695669882826,
32.6854611413806));
#21069=CARTESIAN_POINT('Ctrl Pts',(-1.30009905826486,-2.95023187124312,
32.6631601046024));
#21070=CARTESIAN_POINT('Ctrl Pts',(-1.38152323385195,-2.91299199914829,
32.6573077871076));
#21071=CARTESIAN_POINT('Ctrl Pts',(-1.46595678380419,-2.87003755765287,
32.6513079616142));
#21072=CARTESIAN_POINT('Ctrl Pts',(-1.47060898770064,-2.86765654851168,
32.6509776062806));
#21073=CARTESIAN_POINT('Ctrl Pts',(-1.47525540501479,-2.8652642203599,32.6506479065737));
#21074=CARTESIAN_POINT('',(3.22274859474753,0.00298732763886637,32.814161792891));
#21075=CARTESIAN_POINT('Ctrl Pts',(-1.47525529429555,-2.86526427736657,
32.4060211118892));
#21076=CARTESIAN_POINT('Ctrl Pts',(-1.39484804649379,-2.90666402501159,
32.41209028498));
#21077=CARTESIAN_POINT('Ctrl Pts',(-1.31271522488961,-2.9446702933697,32.418215933755));
#21078=CARTESIAN_POINT('Ctrl Pts',(-1.05498043027862,-3.05099990093074,
32.4370884081259));
#21079=CARTESIAN_POINT('Ctrl Pts',(-0.874906521245708,-3.10743291387524,
32.449807403356));
#21080=CARTESIAN_POINT('Ctrl Pts',(-0.676634677132355,-3.15095174123194,
32.4626729572916));
#21081=CARTESIAN_POINT('Ctrl Pts',(-0.662331285902206,-3.1539893228438,
32.4635947268513));
#21082=CARTESIAN_POINT('Ctrl Pts',(-0.641033050275847,-3.15836110696402,
32.4649573327813));
#21083=CARTESIAN_POINT('Ctrl Pts',(-0.634053894286388,-3.15976959840119,
32.4654022583912));
#21084=CARTESIAN_POINT('Ctrl Pts',(-0.621592058936658,-3.16224162011029,
32.4661938154477));
#21085=CARTESIAN_POINT('Ctrl Pts',(-0.616111243562462,-3.16331403576564,
32.4665409479681));
#21086=CARTESIAN_POINT('Ctrl Pts',(-0.604272908015296,-3.16559847424139,
32.4672885693926));
#21087=CARTESIAN_POINT('Ctrl Pts',(-0.597914535005387,-3.16680559208341,
32.4676887762993));
#21088=CARTESIAN_POINT('Ctrl Pts',(-0.581024869463102,-3.16995936235909,
32.4687483870502));
#21089=CARTESIAN_POINT('Ctrl Pts',(-0.57048732975085,-3.17187270741842,
32.4694059227346));
#21090=CARTESIAN_POINT('Ctrl Pts',(-0.515161565583093,-3.18163380533274,
32.4728404833274));
#21091=CARTESIAN_POINT('Ctrl Pts',(-0.470217993924355,-3.18858599350661,
32.4755696656836));
#21092=CARTESIAN_POINT('Ctrl Pts',(-0.335618083148154,-3.20649873356882,
32.4836023584478));
#21093=CARTESIAN_POINT('Ctrl Pts',(-0.245628345288927,-3.21464504109731,
32.4887878617375));
#21094=CARTESIAN_POINT('Ctrl Pts',(0.104682712549077,-3.23155760944982,
32.5086537179753));
#21095=CARTESIAN_POINT('Ctrl Pts',(0.365327829932817,-3.21254741585919,
32.5228349408671));
#21096=CARTESIAN_POINT('Ctrl Pts',(0.704460088561196,-3.14596785493337,
32.5429085629154));
#21097=CARTESIAN_POINT('Ctrl Pts',(0.787380738413174,-3.12624494289355,
32.5479411687893));
#21098=CARTESIAN_POINT('Ctrl Pts',(0.889103026786777,-3.09774616452662,
32.5543135848249));
#21099=CARTESIAN_POINT('Ctrl Pts',(0.90873509933982,-3.09204398118237,32.5555526942832));
#21100=CARTESIAN_POINT('Ctrl Pts',(0.939508698094618,-3.08278732580966,
32.5575101415069));
#21101=CARTESIAN_POINT('Ctrl Pts',(0.950687614269772,-3.07935826826967,
32.5582243655098));
#21102=CARTESIAN_POINT('Ctrl Pts',(0.970389176276476,-3.07319743974693,
32.5594887819215));
#21103=CARTESIAN_POINT('Ctrl Pts',(0.978919613098458,-3.0704908476692,32.5600381397819));
#21104=CARTESIAN_POINT('Ctrl Pts',(0.998438938031406,-3.06420802067885,
32.5612995611318));
#21105=CARTESIAN_POINT('Ctrl Pts',(1.00942003744565,-3.0606081567876,32.5620123995555));
#21106=CARTESIAN_POINT('Ctrl Pts',(1.03820735768362,-3.05099921548932,32.5638896454268));
#21107=CARTESIAN_POINT('Ctrl Pts',(1.05598059159825,-3.04489338015105,32.5650572465812));
#21108=CARTESIAN_POINT('Ctrl Pts',(1.14987903089594,-3.01171441926257,32.5712723458542));
#21109=CARTESIAN_POINT('Ctrl Pts',(1.22501364585072,-2.98194319429782,32.576409257774));
#21110=CARTESIAN_POINT('Ctrl Pts',(1.55350542802854,-2.83727126819555,32.5996236041743));
#21111=CARTESIAN_POINT('Ctrl Pts',(1.79245679538935,-2.69268278754898,32.6186954563068));
#21112=CARTESIAN_POINT('Ctrl Pts',(2.10243759296631,-2.44538510752028,32.6452926506345));
#21113=CARTESIAN_POINT('Ctrl Pts',(2.19091231493155,-2.36644497206343,32.6531208637461));
#21114=CARTESIAN_POINT('Ctrl Pts',(2.28531546148905,-2.27237083728936,32.6615692412041));
#21115=CARTESIAN_POINT('Ctrl Pts',(2.29571235696151,-2.26186665707975,32.6625010365024));
#21116=CARTESIAN_POINT('Ctrl Pts',(2.31103211423161,-2.24617436167468,32.6638755305101));
#21117=CARTESIAN_POINT('Ctrl Pts',(2.3160103871061,-2.24104096018165,32.6643224210818));
#21118=CARTESIAN_POINT('Ctrl Pts',(2.32484807794097,-2.23186697558647,32.6651161191681));
#21119=CARTESIAN_POINT('Ctrl Pts',(2.32871410500528,-2.22783289342548,32.6654634387173));
#21120=CARTESIAN_POINT('Ctrl Pts',(2.33702074847036,-2.21911991402158,32.6662099410067));
#21121=CARTESIAN_POINT('Ctrl Pts',(2.34145780222227,-2.21443774663565,32.666608849857));
#21122=CARTESIAN_POINT('Ctrl Pts',(2.35055030056911,-2.20478507446713,32.6674267097068));
#21123=CARTESIAN_POINT('Ctrl Pts',(2.35520411191296,-2.19981306780473,32.6678455366032));
#21124=CARTESIAN_POINT('Ctrl Pts',(2.37699462063653,-2.17638426085354,32.6698078668024));
#21125=CARTESIAN_POINT('Ctrl Pts',(2.39393090330502,-2.15774113325243,32.6713367334204));
#21126=CARTESIAN_POINT('Ctrl Pts',(2.49796256946775,-2.04049227147627,32.6807653659123));
#21127=CARTESIAN_POINT('Ctrl Pts',(2.57918012713303,-1.93681784657678,32.6882954021693));
#21128=CARTESIAN_POINT('Ctrl Pts',(2.71718240244353,-1.73652014046452,32.7020071237146));
#21129=CARTESIAN_POINT('Ctrl Pts',(2.77570634492024,-1.64135230951347,32.7082109445752));
#21130=CARTESIAN_POINT('Ctrl Pts',(2.86103061052913,-1.48493993474693,32.7181891857034));
#21131=CARTESIAN_POINT('Ctrl Pts',(2.8910708539342,-1.42557066091932,32.7219289446648));
#21132=CARTESIAN_POINT('Ctrl Pts',(2.9806195008897,-1.23410208416092,32.7339312444352));
#21133=CARTESIAN_POINT('Ctrl Pts',(3.03306388312251,-1.09891595040438,32.7423280633316));
#21134=CARTESIAN_POINT('Ctrl Pts',(3.08263348383184,-0.940185612816217,
32.7523337165343));
#21135=CARTESIAN_POINT('Ctrl Pts',(3.08882619650378,-0.919636273651769,
32.7536315586163));
#21136=CARTESIAN_POINT('Ctrl Pts',(3.09842944465002,-0.886578024626569,
32.7557240922569));
#21137=CARTESIAN_POINT('Ctrl Pts',(3.10197061356489,-0.874107500308189,
32.7565145123079));
#21138=CARTESIAN_POINT('Ctrl Pts',(3.10812579449117,-0.851922999431207,
32.7579226460436));
#21139=CARTESIAN_POINT('Ctrl Pts',(3.11076976037074,-0.842217457465309,
32.7585393741851));
#21140=CARTESIAN_POINT('Ctrl Pts',(3.11618551295834,-0.821963720052884,
32.7598278621795));
#21141=CARTESIAN_POINT('Ctrl Pts',(3.11894927622815,-0.811413529519908,
32.7604998740183));
#21142=CARTESIAN_POINT('Ctrl Pts',(3.12443655062962,-0.790024492918964,
32.7618640536353));
#21143=CARTESIAN_POINT('Ctrl Pts',(3.12715733847663,-0.779185108730077,
32.7625562994536));
#21144=CARTESIAN_POINT('Ctrl Pts',(3.13370547461799,-0.752511091504904,
32.764262145044));
#21145=CARTESIAN_POINT('Ctrl Pts',(3.13746921185679,-0.736661301681656,
32.7652777837164));
#21146=CARTESIAN_POINT('Ctrl Pts',(3.15412750157559,-0.664065945541543,
32.7699392589516));
#21147=CARTESIAN_POINT('Ctrl Pts',(3.16560312076216,-0.607009102859284,
32.7736301123873));
#21148=CARTESIAN_POINT('Ctrl Pts',(3.20712647278227,-0.367124868945356,
32.7892681278082));
#21149=CARTESIAN_POINT('Ctrl Pts',(3.22292030341193,-0.182219354745417,
32.801640427985));
#21150=CARTESIAN_POINT('Ctrl Pts',(3.22274861527754,0.00298751178999402,
32.8141617710204));
#21151=CARTESIAN_POINT('Ctrl Pts',(3.22274861544609,0.00298732996773646,
32.8141617587279));
#21152=CARTESIAN_POINT('Ctrl Pts',(3.22254821683741,0.219178492523581,32.82877786743));
#21153=CARTESIAN_POINT('Ctrl Pts',(3.20059451488405,0.434825313060781,32.8435351721082));
#21154=CARTESIAN_POINT('Ctrl Pts',(3.15408936426525,0.661875181097467,32.8583473192536));
#21155=CARTESIAN_POINT('Ctrl Pts',(3.15086501835497,0.677058439667333,32.8593340847704));
#21156=CARTESIAN_POINT('Ctrl Pts',(3.14562904415603,0.70086652878365,32.8608748524812));
#21157=CARTESIAN_POINT('Ctrl Pts',(3.14369139333282,0.709507154534677,32.8614326852729));
#21158=CARTESIAN_POINT('Ctrl Pts',(3.13995805039784,0.725839783878309,32.8624843996454));
#21159=CARTESIAN_POINT('Ctrl Pts',(3.13816964987695,0.733533367913012,32.8629786759137));
#21160=CARTESIAN_POINT('Ctrl Pts',(3.1350438339135,0.746759747290711,32.8638263518822));
#21161=CARTESIAN_POINT('Ctrl Pts',(3.13372001865912,0.752295691454266,32.8641805273361));
#21162=CARTESIAN_POINT('Ctrl Pts',(3.13112769980832,0.763010694757067,32.8648648069713));
#21163=CARTESIAN_POINT('Ctrl Pts',(3.12986100981597,0.768190115164842,32.8651950172635));
#21164=CARTESIAN_POINT('Ctrl Pts',(3.12641332444486,0.78213740374081,32.8660827740626));
#21165=CARTESIAN_POINT('Ctrl Pts',(3.12420828330465,0.790899361946299,32.8666389418758));
#21166=CARTESIAN_POINT('Ctrl Pts',(3.11591133141757,0.823291956719157,32.8686897652535));
#21167=CARTESIAN_POINT('Ctrl Pts',(3.10958774924866,0.846863143310266,32.8701716232201));
#21168=CARTESIAN_POINT('Ctrl Pts',(3.05224328908114,1.05130666770391,32.8829512843741));
#21169=CARTESIAN_POINT('Ctrl Pts',(2.9857523953139,1.22749198326639,32.8934769757778));
#21170=CARTESIAN_POINT('Ctrl Pts',(2.85690170263137,1.49538435153591,32.9100933422932));
#21171=CARTESIAN_POINT('Ctrl Pts',(2.80455186790844,1.59139869031303,32.916182351003));
#21172=CARTESIAN_POINT('Ctrl Pts',(2.67304713907188,1.80587507789757,32.930415745757));
#21173=CARTESIAN_POINT('Ctrl Pts',(2.5907229696946,1.92211170615877,32.9386139946019));
#21174=CARTESIAN_POINT('Ctrl Pts',(2.47952014550147,2.05894556251995,32.9491446161738));
#21175=CARTESIAN_POINT('Ctrl Pts',(2.45762858796366,2.085027235062,32.951194098938));
#21176=CARTESIAN_POINT('Ctrl Pts',(2.42806696076517,2.11913456861155,32.9539333114126));
#21177=CARTESIAN_POINT('Ctrl Pts',(2.4207623075483,2.12747510711607,32.9546079398342));
#21178=CARTESIAN_POINT('Ctrl Pts',(2.40622730457362,2.14389956536553,32.9559460528837));
#21179=CARTESIAN_POINT('Ctrl Pts',(2.39899889462704,2.15198501079376,32.9566094515741));
#21180=CARTESIAN_POINT('Ctrl Pts',(2.38497382522173,2.16751448005937,32.957892758171));
#21181=CARTESIAN_POINT('Ctrl Pts',(2.3781827741766,2.17496341513716,32.9585124241679));
#21182=CARTESIAN_POINT('Ctrl Pts',(2.36248675336626,2.19201858559234,32.9599407805972));
#21183=CARTESIAN_POINT('Ctrl Pts',(2.35355798497797,2.20160258507677,32.9607504852929));
#21184=CARTESIAN_POINT('Ctrl Pts',(2.32952925950451,2.22708141768664,32.9629221910417));
#21185=CARTESIAN_POINT('Ctrl Pts',(2.31432532477309,2.24287682779098,32.9642886817434));
#21186=CARTESIAN_POINT('Ctrl Pts',(2.18341077532949,2.37613583205806,32.9759925231601));
#21187=CARTESIAN_POINT('Ctrl Pts',(2.05902228151188,2.4846964403543,32.9867221900102));
#21188=CARTESIAN_POINT('Ctrl Pts',(1.76922500931947,2.70086120576445,33.0108420739501));
#21189=CARTESIAN_POINT('Ctrl Pts',(1.60112989837387,2.80378071718617,33.0243037573606));
#21190=CARTESIAN_POINT('Ctrl Pts',(1.35795709729627,2.92362921898249,33.0424335399758));
#21191=CARTESIAN_POINT('Ctrl Pts',(1.29008363437771,2.95420733859527,33.047356494781));
#21192=CARTESIAN_POINT('Ctrl Pts',(1.18415103180865,2.99758358768472,33.0547710194766));
#21193=CARTESIAN_POINT('Ctrl Pts',(1.14681231389973,3.01206621750124,33.057334478464));
#21194=CARTESIAN_POINT('Ctrl Pts',(1.09939746123825,3.02944748105969,33.0605185647441));
#21195=CARTESIAN_POINT('Ctrl Pts',(1.08956592616303,3.03299734881753,33.0611749712198));
#21196=CARTESIAN_POINT('Ctrl Pts',(1.07379673868955,3.03860454967796,33.0622215054983));
#21197=CARTESIAN_POINT('Ctrl Pts',(1.06787013768976,3.04069242377124,33.0626134091202));
#21198=CARTESIAN_POINT('Ctrl Pts',(1.05663236657261,3.0446144543874,33.0633537819896));
#21199=CARTESIAN_POINT('Ctrl Pts',(1.05132257400911,3.04645203142315,33.0637024433731));
#21200=CARTESIAN_POINT('Ctrl Pts',(1.03910012166671,3.05064613410803,33.0645023873519));
#21201=CARTESIAN_POINT('Ctrl Pts',(1.03218424126177,3.05299305484908,33.0649530975991));
#21202=CARTESIAN_POINT('Ctrl Pts',(1.01364752562713,3.05921334658098,33.0661561430386));
#21203=CARTESIAN_POINT('Ctrl Pts',(1.00201235182477,3.06304405191075,33.0669060276449));
#21204=CARTESIAN_POINT('Ctrl Pts',(0.915072190078493,3.09111938239442,33.0724722238561));
#21205=CARTESIAN_POINT('Ctrl Pts',(0.838912354402849,3.11265232139756,33.0771414306856));
#21206=CARTESIAN_POINT('Ctrl Pts',(0.74199109393293,3.13623853415201,33.0829144391046));
#21207=CARTESIAN_POINT('Ctrl Pts',(0.721904909761096,3.14092283494992,33.084101812259));
#21208=CARTESIAN_POINT('Ctrl Pts',(0.454419000164066,3.20060174343823,33.0998101881616));
#21209=CARTESIAN_POINT('Ctrl Pts',(0.20141314845607,3.22642107870538,33.1135645299833));
#21210=CARTESIAN_POINT('Ctrl Pts',(-0.132664001225616,3.22102836787693,
33.1326942396608));
#21211=CARTESIAN_POINT('Ctrl Pts',(-0.213230584116318,3.21669936634752,
33.1373746806528));
#21212=CARTESIAN_POINT('Ctrl Pts',(-0.344158407653682,3.20472395039108,
33.1451489266051));
#21213=CARTESIAN_POINT('Ctrl Pts',(-0.394651927594301,3.19889825270692,
33.1481879731844));
#21214=CARTESIAN_POINT('Ctrl Pts',(-0.46101225057508,3.18964686862244,33.1522443825089));
#21215=CARTESIAN_POINT('Ctrl Pts',(-0.477022638378892,3.18729177034332,
33.1532278479773));
#21216=CARTESIAN_POINT('Ctrl Pts',(-0.503734737244689,3.18315669688949,
33.1548769780555));
#21217=CARTESIAN_POINT('Ctrl Pts',(-0.514446535684941,3.18144306877094,
33.1555405279324));
#21218=CARTESIAN_POINT('Ctrl Pts',(-0.535093716633112,3.17803301812316,
33.1568239277939));
#21219=CARTESIAN_POINT('Ctrl Pts',(-0.545030206689636,3.17634400214676,
33.1574435347979));
#21220=CARTESIAN_POINT('Ctrl Pts',(-0.567855859021335,3.17235381230553,
33.1588714696059));
#21221=CARTESIAN_POINT('Ctrl Pts',(-0.580739181956499,3.17002065947254,
33.1596808097193));
#21222=CARTESIAN_POINT('Ctrl Pts',(-0.615136785905561,3.1635745720031,33.1618509018918));
#21223=CARTESIAN_POINT('Ctrl Pts',(-0.636623658660753,3.15932075246752,
33.1632161331257));
#21224=CARTESIAN_POINT('Ctrl Pts',(-0.818491299351512,3.12138525397779,
33.1748556051346));
#21225=CARTESIAN_POINT('Ctrl Pts',(-0.97610611102545,3.07573992396352,33.1855171897619));
#21226=CARTESIAN_POINT('Ctrl Pts',(-1.36735229938579,2.92932350690405,33.2133794792506));
#21227=CARTESIAN_POINT('Ctrl Pts',(-1.59379437568799,2.8125438999033,33.2309059472695));
#21228=CARTESIAN_POINT('Ctrl Pts',(-1.85090986964421,2.63883130783127,33.2512063647467));
#21229=CARTESIAN_POINT('Ctrl Pts',(-1.8968064756676,2.6060360954482,33.254843313869));
#21230=CARTESIAN_POINT('Ctrl Pts',(-1.95113970410506,2.56501612638892,33.2591424493099));
#21231=CARTESIAN_POINT('Ctrl Pts',(-1.96041948655533,2.55793067149038,33.2598764805809));
#21232=CARTESIAN_POINT('Ctrl Pts',(-1.97481003762952,2.54681864355279,33.261014137641));
#21233=CARTESIAN_POINT('Ctrl Pts',(-1.97994735291098,2.54282684611979,33.2614201449728));
#21234=CARTESIAN_POINT('Ctrl Pts',(-1.98946915422156,2.53538186350542,33.262172369432));
#21235=CARTESIAN_POINT('Ctrl Pts',(-1.99385671619039,2.53193287932558,33.2625188649474));
#21236=CARTESIAN_POINT('Ctrl Pts',(-2.00378408823138,2.5240873414287,33.2633025954733));
#21237=CARTESIAN_POINT('Ctrl Pts',(-2.00931838567896,2.51968394975133,33.2637393332713));
#21238=CARTESIAN_POINT('Ctrl Pts',(-2.0256997282627,2.50656175786473,33.2650316931065));
#21239=CARTESIAN_POINT('Ctrl Pts',(-2.03650500789702,2.49779074465531,33.2658836611756));
#21240=CARTESIAN_POINT('Ctrl Pts',(-2.11807225260702,2.43069866689546,33.2723142811886));
#21241=CARTESIAN_POINT('Ctrl Pts',(-2.18638002951525,2.36944546507828,33.2776956308852));
#21242=CARTESIAN_POINT('Ctrl Pts',(-2.42595840876775,2.13541320832331,33.2969539229055));
#21243=CARTESIAN_POINT('Ctrl Pts',(-2.58013914309783,1.94631934001491,33.3101740128229));
#21244=CARTESIAN_POINT('Ctrl Pts',(-2.76123876379042,1.66436750957209,33.3292521348975));
#21245=CARTESIAN_POINT('Ctrl Pts',(-2.80755951247119,1.58498150596806,33.3345553115394));
#21246=CARTESIAN_POINT('Ctrl Pts',(-2.87658702718598,1.45413505750464,33.3432788514775));
#21247=CARTESIAN_POINT('Ctrl Pts',(-2.90145027763158,1.40386872650688,33.3466257985369));
#21248=CARTESIAN_POINT('Ctrl Pts',(-2.93219686171064,1.33739819360027,33.3510576133749));
#21249=CARTESIAN_POINT('Ctrl Pts',(-2.93928035569805,1.32175766951851,33.3521008182964));
#21250=CARTESIAN_POINT('Ctrl Pts',(-2.95063461634486,1.29614451234264,33.3538101517333));
#21251=CARTESIAN_POINT('Ctrl Pts',(-2.95498066420527,1.28620546790602,33.354473683928));
#21252=CARTESIAN_POINT('Ctrl Pts',(-2.96326786817708,1.26698961851998,33.3557570728668));
#21253=CARTESIAN_POINT('Ctrl Pts',(-2.96721585127729,1.25771588216632,33.3563766867554));
#21254=CARTESIAN_POINT('Ctrl Pts',(-2.97619240891793,1.23635259936775,33.3578046708032));
#21255=CARTESIAN_POINT('Ctrl Pts',(-2.98119091300347,1.22425068387007,33.3586140535));
#21256=CARTESIAN_POINT('Ctrl Pts',(-2.99435464763178,1.19182116285148,33.3607843341181));
#21257=CARTESIAN_POINT('Ctrl Pts',(-3.00238648521609,1.17144047869872,33.3621497124367));
#21258=CARTESIAN_POINT('Ctrl Pts',(-3.06877958779751,0.997799595134482,
33.3737966676907));
#21259=CARTESIAN_POINT('Ctrl Pts',(-3.11556275071706,0.840396463538818,
33.3844661647027));
#21260=CARTESIAN_POINT('Ctrl Pts',(-3.20380085196605,0.431708309118718,
33.4123533144407));
#21261=CARTESIAN_POINT('Ctrl Pts',(-3.22786115138708,0.177818998295027,
33.4298972485246));
#21262=CARTESIAN_POINT('Ctrl Pts',(-3.22052108757301,-0.132306711781043,
33.4501884075272));
#21263=CARTESIAN_POINT('Ctrl Pts',(-3.21773183101023,-0.1883186410448,33.4538037002444));
#21264=CARTESIAN_POINT('Ctrl Pts',(-3.21259889385944,-0.255854954542151,
33.4580807577507));
#21265=CARTESIAN_POINT('Ctrl Pts',(-3.21165254418778,-0.267472158926023,
33.4588135267291));
#21266=CARTESIAN_POINT('Ctrl Pts',(-3.21008015760449,-0.28556122520582,
33.4599496571486));
#21267=CARTESIAN_POINT('Ctrl Pts',(-3.20949753802068,-0.292036618935335,
33.4603553900228));
#21268=CARTESIAN_POINT('Ctrl Pts',(-3.20837833855174,-0.304067675371715,
33.4611073666807));
#21269=CARTESIAN_POINT('Ctrl Pts',(-3.207846927222,-0.309623653353343,33.4614538872164));
#21270=CARTESIAN_POINT('Ctrl Pts',(-3.20660883806567,-0.322222629696172,
33.4622380063206));
#21271=CARTESIAN_POINT('Ctrl Pts',(-3.20589339118047,-0.329264680906096,
33.4626751056123));
#21272=CARTESIAN_POINT('Ctrl Pts',(-3.20369958877302,-0.350172751837709,
33.4639695279551));
#21273=CARTESIAN_POINT('Ctrl Pts',(-3.20215441087964,-0.364031806872042,
33.4648231797169));
#21274=CARTESIAN_POINT('Ctrl Pts',(-3.18966937048855,-0.469775800286934,
33.4713061363506));
#21275=CARTESIAN_POINT('Ctrl Pts',(-3.17486552036997,-0.561170539849794,
33.4767344907806));
#21276=CARTESIAN_POINT('Ctrl Pts',(-3.10716912956218,-0.888965110141979,
33.4959732949462));
#21277=CARTESIAN_POINT('Ctrl Pts',(-3.03161728829047,-1.11985196555058,
33.5091401015489));
#21278=CARTESIAN_POINT('Ctrl Pts',(-2.89266269291002,-1.42375561537799,
33.5281638821857));
#21279=CARTESIAN_POINT('Ctrl Pts',(-2.85085485522526,-1.50572313829151,
33.5334727086058));
#21280=CARTESIAN_POINT('Ctrl Pts',(-2.77798835726111,-1.63463983206211,
33.5422046933284));
#21281=CARTESIAN_POINT('Ctrl Pts',(-2.74910544859249,-1.68276122763449,
33.5455542491201));
#21282=CARTESIAN_POINT('Ctrl Pts',(-2.70976221439132,-1.74459200784426,
33.5499890377277));
#21283=CARTESIAN_POINT('Ctrl Pts',(-2.70042661011467,-1.75900785615045,
33.55103253664));
#21284=CARTESIAN_POINT('Ctrl Pts',(-2.68500669728452,-1.78240688256158,
33.5527422307683));
#21285=CARTESIAN_POINT('Ctrl Pts',(-2.67899138624992,-1.79143529252744,
33.553405827549));
#21286=CARTESIAN_POINT('Ctrl Pts',(-2.66730001727916,-1.80879234905369,
33.5546892564034));
#21287=CARTESIAN_POINT('Ctrl Pts',(-2.66163024240726,-1.81712509013346,
33.5553088451646));
#21288=CARTESIAN_POINT('Ctrl Pts',(-2.64850644800981,-1.83621963140854,
33.5567366494497));
#21289=CARTESIAN_POINT('Ctrl Pts',(-2.64102579390097,-1.84696282792607,
33.5575458766783));
#21290=CARTESIAN_POINT('Ctrl Pts',(-2.6208577448739,-1.87555371791103,33.5597154693262));
#21291=CARTESIAN_POINT('Ctrl Pts',(-2.60805372459752,-1.89331793395098,
33.5610803106803));
#21292=CARTESIAN_POINT('Ctrl Pts',(-2.49807986736813,-2.04266242620315,
33.572699992241));
#21293=CARTESIAN_POINT('Ctrl Pts',(-2.3912186061171,-2.16677912507858,33.583340654715));
#21294=CARTESIAN_POINT('Ctrl Pts',(-2.09604642557909,-2.46106918579612,
33.6111384574185));
#21295=CARTESIAN_POINT('Ctrl Pts',(-1.89623078275139,-2.61812451795397,
33.6286200839546));
#21296=CARTESIAN_POINT('Ctrl Pts',(-1.63124165278221,-2.78000817298476,
33.6489449574626));
#21297=CARTESIAN_POINT('Ctrl Pts',(-1.58159924147276,-2.80854759089056,
33.6526381635886));
#21298=CARTESIAN_POINT('Ctrl Pts',(-1.52090135742906,-2.84132260140222,
33.6569945872463));
#21299=CARTESIAN_POINT('Ctrl Pts',(-1.51055283545487,-2.84683775539471,
33.6577318552148));
#21300=CARTESIAN_POINT('Ctrl Pts',(-1.49440648798576,-2.85532997758415,
33.6588734260387));
#21301=CARTESIAN_POINT('Ctrl Pts',(-1.4886294712769,-2.85834608318441,33.6592801364429));
#21302=CARTESIAN_POINT('Ctrl Pts',(-1.48031571465441,-2.86265454636422,
33.6598629068856));
#21303=CARTESIAN_POINT('Ctrl Pts',(-1.47778642730061,-2.86396105806136,
33.6600398669396));
#21304=CARTESIAN_POINT('Ctrl Pts',(-1.47525540501188,-2.8652642203614,33.660216611122));
#21305=CARTESIAN_POINT('Origin',(0.,0.,4.68922655072688));
#21306=CARTESIAN_POINT('',(-1.47525552646581,-2.8652641578277,35.1563175586878));
#21307=CARTESIAN_POINT('',(-1.47525540445791,-2.86526422064663,34.9063554765866));
#21308=CARTESIAN_POINT('',(-1.47525540501186,-2.86526422036142,4.68922655072688));
#21309=CARTESIAN_POINT('',(3.22274903069615,-0.00249952936660396,34.3127207581881));
#21310=CARTESIAN_POINT('Ctrl Pts',(-1.47525552646581,-2.8652641578277,35.1563175586878));
#21311=CARTESIAN_POINT('Ctrl Pts',(-1.5179786368742,-2.84326705694414,35.1534900287168));
#21312=CARTESIAN_POINT('Ctrl Pts',(-1.56021632410078,-2.82031103518203,
35.150632229143));
#21313=CARTESIAN_POINT('Ctrl Pts',(-1.62096631363004,-2.78551014190289,
35.146421317202));
#21314=CARTESIAN_POINT('Ctrl Pts',(-1.63988409403924,-2.7744150126229,35.1450954968172));
#21315=CARTESIAN_POINT('Ctrl Pts',(-1.6699213053194,-2.75638387962761,35.1429663459599));
#21316=CARTESIAN_POINT('Ctrl Pts',(-1.68111443427663,-2.74957151366147,
35.1421675300128));
#21317=CARTESIAN_POINT('Ctrl Pts',(-1.70084704537755,-2.73739631176315,
35.1407495369148));
#21318=CARTESIAN_POINT('Ctrl Pts',(-1.70940353540863,-2.73206127107097,
35.1401313914053));
#21319=CARTESIAN_POINT('Ctrl Pts',(-1.72711415399747,-2.72090278595853,
35.1388450421301));
#21320=CARTESIAN_POINT('Ctrl Pts',(-1.73626418293619,-2.71507310288679,
35.1381766115914));
#21321=CARTESIAN_POINT('Ctrl Pts',(-1.75981505434774,-2.69990059222446,
35.1364460971715));
#21322=CARTESIAN_POINT('Ctrl Pts',(-1.77417085675511,-2.6904888005836,35.135381439547));
#21323=CARTESIAN_POINT('Ctrl Pts',(-1.83503964978362,-2.64988367822589,
35.130824774063));
#21324=CARTESIAN_POINT('Ctrl Pts',(-1.88080814757814,-2.61759700897596,
35.1272915814473));
#21325=CARTESIAN_POINT('Ctrl Pts',(-1.99924781255354,-2.52933522155223,
35.1178552546094));
#21326=CARTESIAN_POINT('Ctrl Pts',(-2.07040678604797,-2.47142503715811,
35.1118808696354));
#21327=CARTESIAN_POINT('Ctrl Pts',(-2.32202096135386,-2.24815717635066,
35.0896297664439));
#21328=CARTESIAN_POINT('Ctrl Pts',(-2.48593682768389,-2.06545269928067,
35.0727943646564));
#21329=CARTESIAN_POINT('Ctrl Pts',(-2.68002016186566,-1.7921516345158,35.0505052130097));
#21330=CARTESIAN_POINT('Ctrl Pts',(-2.72931560658516,-1.71614543216571,
35.0445815800732));
#21331=CARTESIAN_POINT('Ctrl Pts',(-2.78240414784869,-1.62620336552493,
35.0379665134103));
#21332=CARTESIAN_POINT('Ctrl Pts',(-2.7893825488052,-1.61420421283992,35.037091854403));
#21333=CARTESIAN_POINT('Ctrl Pts',(-2.79979613030385,-1.59602917237582,
35.0357792620165));
#21334=CARTESIAN_POINT('Ctrl Pts',(-2.80328877516139,-1.58988664239112,
35.0353377469127));
#21335=CARTESIAN_POINT('Ctrl Pts',(-2.80950444728965,-1.57887095232093,
35.0345497698746));
#21336=CARTESIAN_POINT('Ctrl Pts',(-2.81223503144743,-1.574002176899,35.0342028264667));
#21337=CARTESIAN_POINT('Ctrl Pts',(-2.81812494196711,-1.5634359004169,35.0334527747247));
#21338=CARTESIAN_POINT('Ctrl Pts',(-2.82127963779431,-1.55773592447216,
35.0330499638339));
#21339=CARTESIAN_POINT('Ctrl Pts',(-2.83005619289586,-1.54176412620451,
35.0319261826464));
#21340=CARTESIAN_POINT('Ctrl Pts',(-2.83563945374104,-1.53147104902214,
35.0312076395943));
#21341=CARTESIAN_POINT('Ctrl Pts',(-2.86803336675817,-1.47096639833774,
35.0270157530493));
#21342=CARTESIAN_POINT('Ctrl Pts',(-2.89356790136217,-1.42007861040143,
35.0236181149031));
#21343=CARTESIAN_POINT('Ctrl Pts',(-3.02542968025674,-1.138947318291,35.0053923346017));
#21344=CARTESIAN_POINT('Ctrl Pts',(-3.10565204760635,-0.897428543206136,
34.9916298287095));
#21345=CARTESIAN_POINT('Ctrl Pts',(-3.18966930973458,-0.488757482110987,
34.9680616591426));
#21346=CARTESIAN_POINT('Ctrl Pts',(-3.21035909838568,-0.326279391726797,
34.9586348844414));
#21347=CARTESIAN_POINT('Ctrl Pts',(-3.21973544117005,-0.141070877135228,
34.9474808597557));
#21348=CARTESIAN_POINT('Ctrl Pts',(-3.22061982517785,-0.119185606911457,
34.9461567220849));
#21349=CARTESIAN_POINT('Ctrl Pts',(-3.22167637508481,-0.0842043726205361,
34.9440297635706));
#21350=CARTESIAN_POINT('Ctrl Pts',(-3.22199192258901,-0.0711131842581894,
34.9432314424066));
#21351=CARTESIAN_POINT('Ctrl Pts',(-3.22240918699982,-0.0479400138150561,
34.9418140219369));
#21352=CARTESIAN_POINT('Ctrl Pts',(-3.22254339392139,-0.0378587375628033,
34.9411959515001));
#21353=CARTESIAN_POINT('Ctrl Pts',(-3.22272383388549,-0.0169245308703073,
34.9399094535703));
#21354=CARTESIAN_POINT('Ctrl Pts',(-3.22276255398095,-0.00607167879688278,
34.9392407977888));
#21355=CARTESIAN_POINT('Ctrl Pts',(-3.22272096316074,0.0219632680854339,
34.9375090447834));
#21356=CARTESIAN_POINT('Ctrl Pts',(-3.22255806208995,0.0391447259466706,
34.9364433668175));
#21357=CARTESIAN_POINT('Ctrl Pts',(-3.22127641534352,0.112467131535375,
34.931876414891));
#21358=CARTESIAN_POINT('Ctrl Pts',(-3.21882795275129,0.168572151615786,
34.9283337245431));
#21359=CARTESIAN_POINT('Ctrl Pts',(-3.20850071668411,0.316407724861215,
34.9188655845864));
#21360=CARTESIAN_POINT('Ctrl Pts',(-3.19815547125634,0.407908995153394,
34.9128682853862));
#21361=CARTESIAN_POINT('Ctrl Pts',(-3.14655836853488,0.737236912508392,
34.8908150037665));
#21362=CARTESIAN_POINT('Ctrl Pts',(-3.08255485188429,0.970664025651237,
34.8742217351011));
#21363=CARTESIAN_POINT('Ctrl Pts',(-2.95853734549217,1.28135465067181,34.8519555482104));
#21364=CARTESIAN_POINT('Ctrl Pts',(-2.9202214309433,1.36642720062402,34.8458487216998));
#21365=CARTESIAN_POINT('Ctrl Pts',(-2.87198078471137,1.46220351821693,34.8390556949436));
#21366=CARTESIAN_POINT('Ctrl Pts',(-2.86561476281879,1.47464056779452,34.8381752450757));
#21367=CARTESIAN_POINT('Ctrl Pts',(-2.85589862950396,1.49332206248369,34.8368556904724));
#21368=CARTESIAN_POINT('Ctrl Pts',(-2.85260857298831,1.49959731124572,34.836412948579));
#21369=CARTESIAN_POINT('Ctrl Pts',(-2.84668878298526,1.51079836932837,34.8356236486531));
#21370=CARTESIAN_POINT('Ctrl Pts',(-2.84406692746556,1.51572822551384,34.8352766022834));
#21371=CARTESIAN_POINT('Ctrl Pts',(-2.83836494384229,1.52638273865082,34.8345273123887));
#21372=CARTESIAN_POINT('Ctrl Pts',(-2.83528031325231,1.53210488098275,34.8341253610044));
#21373=CARTESIAN_POINT('Ctrl Pts',(-2.82662178978973,1.54805116811146,34.8330064032023));
#21374=CARTESIAN_POINT('Ctrl Pts',(-2.82100969894211,1.55825461646311,34.8322917904595));
#21375=CARTESIAN_POINT('Ctrl Pts',(-2.78816334376455,1.61721413353522,34.828169109464));
#21376=CARTESIAN_POINT('Ctrl Pts',(-2.75971890279074,1.66528941530197,34.8248338584807));
#21377=CARTESIAN_POINT('Ctrl Pts',(-2.59485495346103,1.92809660837726,34.806611540719));
#21378=CARTESIAN_POINT('Ctrl Pts',(-2.43462180274939,2.12684576768699,34.7928077704821));
#21379=CARTESIAN_POINT('Ctrl Pts',(-2.13546398142824,2.41924988661233,34.7691793709168));
#21380=CARTESIAN_POINT('Ctrl Pts',(-2.00971121895142,2.52468350588945,34.7597358335645));
#21381=CARTESIAN_POINT('Ctrl Pts',(-1.85865160309898,2.6328717424318,34.7485606173765));
#21382=CARTESIAN_POINT('Ctrl Pts',(-1.84067598858579,2.64546995112959,34.7472336376699));
#21383=CARTESIAN_POINT('Ctrl Pts',(-1.81176215150119,2.66529685266751,34.7451029764889));
#21384=CARTESIAN_POINT('Ctrl Pts',(-1.80090588407834,2.67264427022651,34.7443038197812));
#21385=CARTESIAN_POINT('Ctrl Pts',(-1.78161939419822,2.68552631557019,34.7428854321714));
#21386=CARTESIAN_POINT('Ctrl Pts',(-1.77320740509473,2.69108802387602,34.7422672348207));
#21387=CARTESIAN_POINT('Ctrl Pts',(-1.75569344848455,2.70254985767915,34.7409809872404));
#21388=CARTESIAN_POINT('Ctrl Pts',(-1.74658753157699,2.70844368747574,34.7403127112793));
#21389=CARTESIAN_POINT('Ctrl Pts',(-1.72300384022498,2.72353990556162,34.7385830469685));
#21390=CARTESIAN_POINT('Ctrl Pts',(-1.70848217389009,2.73267277473435,34.7375190896748));
#21391=CARTESIAN_POINT('Ctrl Pts',(-1.64633024919451,2.77107188781397,34.7329694710051));
#21392=CARTESIAN_POINT('Ctrl Pts',(-1.59801811703694,2.79921063210115,34.7294427831501));
#21393=CARTESIAN_POINT('Ctrl Pts',(-1.46878126175548,2.87004663105121,34.7200282214757));
#21394=CARTESIAN_POINT('Ctrl Pts',(-1.38673240735123,2.91057671298835,34.7140695049439));
#21395=CARTESIAN_POINT('Ctrl Pts',(-1.07752064500466,3.04727510124331,34.6917090704481));
#21396=CARTESIAN_POINT('Ctrl Pts',(-0.841289158798219,3.12076164626857,
34.6747360586032));
#21397=CARTESIAN_POINT('Ctrl Pts',(-0.511487963635961,3.18314790046483,
34.6524296120023));
#21398=CARTESIAN_POINT('Ctrl Pts',(-0.423315214009551,3.19606912650404,
34.6466057424536));
#21399=CARTESIAN_POINT('Ctrl Pts',(-0.320958914875676,3.20675757697304,
34.6400878871736));
#21400=CARTESIAN_POINT('Ctrl Pts',(-0.307196072076568,3.20810526198146,
34.6392165556126));
#21401=CARTESIAN_POINT('Ctrl Pts',(-0.286399184222595,3.21000667291289,
34.6379079656637));
#21402=CARTESIAN_POINT('Ctrl Pts',(-0.279371504714646,3.2106259354637,34.63746715723));
#21403=CARTESIAN_POINT('Ctrl Pts',(-0.266780355377734,3.21169378307977,
34.6366799401552));
#21404=CARTESIAN_POINT('Ctrl Pts',(-0.261217723788742,3.21215099530102,
34.6363330539973));
#21405=CARTESIAN_POINT('Ctrl Pts',(-0.249151434329551,3.21311121403159,
34.6355825540068));
#21406=CARTESIAN_POINT('Ctrl Pts',(-0.2426474483865,3.21360892588635,34.6351792407081));
#21407=CARTESIAN_POINT('Ctrl Pts',(-0.224426021197621,3.21494767094675,
34.6340526372061));
#21408=CARTESIAN_POINT('Ctrl Pts',(-0.212705285095834,3.21574439865924,
34.6333317939887));
#21409=CARTESIAN_POINT('Ctrl Pts',(-0.143531063224039,3.22006672147503,
34.6290986971581));
#21410=CARTESIAN_POINT('Ctrl Pts',(-0.0859918400459616,3.22211688353137,
34.6256638969262));
#21411=CARTESIAN_POINT('Ctrl Pts',(0.224690982271083,3.22485720710771,34.6074355426114));
#21412=CARTESIAN_POINT('Ctrl Pts',(0.477210918067906,3.19726231678148,34.5936972384264));
#21413=CARTESIAN_POINT('Ctrl Pts',(0.882997323517739,3.10372099632879,34.5701722845915));
#21414=CARTESIAN_POINT('Ctrl Pts',(1.03903925025733,3.05502133960133,34.5607635991275));
#21415=CARTESIAN_POINT('Ctrl Pts',(1.21110359190262,2.98660799894657,34.5496268051806));
#21416=CARTESIAN_POINT('Ctrl Pts',(1.23141426288627,2.97829114197304,34.5483000212053));
#21417=CARTESIAN_POINT('Ctrl Pts',(1.26371703297937,2.96467681913491,34.5461696150097));
#21418=CARTESIAN_POINT('Ctrl Pts',(1.27576472674439,2.95951241514302,34.5453705158263));
#21419=CARTESIAN_POINT('Ctrl Pts',(1.29702459954135,2.9502451495681,34.5439521948226));
#21420=CARTESIAN_POINT('Ctrl Pts',(1.30624970885962,2.94617225375542,34.5433340062312));
#21421=CARTESIAN_POINT('Ctrl Pts',(1.31567272496999,2.94195902417196,34.5426997017919));
#21422=CARTESIAN_POINT('Ctrl Pts',(1.31588997109556,2.94186185996344,34.5426850764488));
#21423=CARTESIAN_POINT('Ctrl Pts',(1.31629475420398,2.94168076527172,34.5426578229276));
#21424=CARTESIAN_POINT('Ctrl Pts',(1.31648229330338,2.9415968411957,34.5426451950033));
#21425=CARTESIAN_POINT('Ctrl Pts',(1.31683173916775,2.94144042344731,34.5426216629428));
#21426=CARTESIAN_POINT('Ctrl Pts',(1.31699364873046,2.94136793400149,34.5426107589135));
#21427=CARTESIAN_POINT('Ctrl Pts',(1.31729535455267,2.94123282567668,34.5425904384942));
#21428=CARTESIAN_POINT('Ctrl Pts',(1.31743515342947,2.94117020970759,34.5425810221479));
#21429=CARTESIAN_POINT('Ctrl Pts',(1.31769567254005,2.94105350080004,34.5425634733212));
#21430=CARTESIAN_POINT('Ctrl Pts',(1.31781639534897,2.94099940974958,34.5425553408311));
#21431=CARTESIAN_POINT('Ctrl Pts',(1.31804137848477,2.94089858719322,34.5425401839488));
#21432=CARTESIAN_POINT('Ctrl Pts',(1.31814564144904,2.94085185677228,34.542533159501));
#21433=CARTESIAN_POINT('Ctrl Pts',(1.31833996008483,2.94076475119691,34.5425200671157));
#21434=CARTESIAN_POINT('Ctrl Pts',(1.31843001851718,2.94072437649475,34.5425139990832));
#21435=CARTESIAN_POINT('Ctrl Pts',(1.31862851262776,2.9406353773132,34.5425006241901));
#21436=CARTESIAN_POINT('Ctrl Pts',(1.31873694992053,2.94058674987464,34.5424933171002));
#21437=CARTESIAN_POINT('Ctrl Pts',(1.31895027736526,2.94049107149664,34.5424789411808));
#21438=CARTESIAN_POINT('Ctrl Pts',(1.31905516160011,2.94044402367551,34.5424718727752));
#21439=CARTESIAN_POINT('Ctrl Pts',(1.3192615000385,2.94035145337773,34.5424579664067));
#21440=CARTESIAN_POINT('Ctrl Pts',(1.31936295515624,2.94030593092374,34.5424511284054));
#21441=CARTESIAN_POINT('Ctrl Pts',(1.31956255669724,2.94021635820134,34.5424376747366));
#21442=CARTESIAN_POINT('Ctrl Pts',(1.31966070412971,2.94017230788393,34.5424310590229));
#21443=CARTESIAN_POINT('Ctrl Pts',(1.31985380705667,2.94008562823101,34.5424180421238));
#21444=CARTESIAN_POINT('Ctrl Pts',(1.3199487636481,2.94004299878011,34.5424116408848));
#21445=CARTESIAN_POINT('Ctrl Pts',(1.32013559730026,2.93995911151546,34.5423990454179));
#21446=CARTESIAN_POINT('Ctrl Pts',(1.32022747551323,2.93991785353631,34.5423928511312));
#21447=CARTESIAN_POINT('Ctrl Pts',(1.3204082604511,2.93983666174328,34.5423806623413));
#21448=CARTESIAN_POINT('Ctrl Pts',(1.32049716845465,2.93979672768375,34.5423746677694));
#21449=CARTESIAN_POINT('Ctrl Pts',(1.32067211699855,2.93971813798157,34.5423628714479));
#21450=CARTESIAN_POINT('Ctrl Pts',(1.32075815890107,2.93967948203387,34.5423570696229));
#21451=CARTESIAN_POINT('Ctrl Pts',(1.32092747520156,2.93960340455824,34.542345652104));
#21452=CARTESIAN_POINT('Ctrl Pts',(1.3210107511155,2.93956598263577,34.5423400363233));
#21453=CARTESIAN_POINT('Ctrl Pts',(1.32117463172044,2.9394923307955,34.5423289844459));
#21454=CARTESIAN_POINT('Ctrl Pts',(1.32125523799563,2.9394561004335,34.5423235482569));
#21455=CARTESIAN_POINT('Ctrl Pts',(1.32141387197333,2.93938479086568,34.5423128493576));
#21456=CARTESIAN_POINT('Ctrl Pts',(1.3214919013374,2.93934971116318,34.5423075865486));
#21457=CARTESIAN_POINT('Ctrl Pts',(1.3216454634901,2.93928066679447,34.5422972289189));
#21458=CARTESIAN_POINT('Ctrl Pts',(1.3217209981069,2.93924670154207,34.542292133988));
#21459=CARTESIAN_POINT('Ctrl Pts',(1.3218696909511,2.93917983272141,34.5422821040443));
#21460=CARTESIAN_POINT('Ctrl Pts',(1.32194283000676,2.93914693799495,34.542277170337));
#21461=CARTESIAN_POINT('Ctrl Pts',(1.32208678870919,2.9390821852495,34.5422674590326));
#21462=CARTESIAN_POINT('Ctrl Pts',(1.32215760841277,2.93905032740962,34.5422626814427));
#21463=CARTESIAN_POINT('Ctrl Pts',(1.32229700782549,2.93898761332045,34.5422532770486));
#21464=CARTESIAN_POINT('Ctrl Pts',(1.3223655876245,2.93895675722216,34.5422486502487));
#21465=CARTESIAN_POINT('Ctrl Pts',(1.32250058381878,2.93889601272373,34.5422395422978));
#21466=CARTESIAN_POINT('Ctrl Pts',(1.32256700024262,2.9388661244898,34.5422350611546));
#21467=CARTESIAN_POINT('Ctrl Pts',(1.33311176898568,2.93412041483154,34.5415235780819));
#21468=CARTESIAN_POINT('Ctrl Pts',(1.34356471549355,2.92934863871387,34.540814648167));
#21469=CARTESIAN_POINT('Ctrl Pts',(1.37246739732528,2.9159673044564,34.5388441983968));
#21470=CARTESIAN_POINT('Ctrl Pts',(1.39086115781958,2.90723877353556,34.5375785684478));
#21471=CARTESIAN_POINT('Ctrl Pts',(1.43171135774812,2.88737741563289,34.534741268517));
#21472=CARTESIAN_POINT('Ctrl Pts',(1.45412292327897,2.87615580575706,34.5331665602155));
#21473=CARTESIAN_POINT('Ctrl Pts',(1.52313576622269,2.84058784527043,34.5282603735897));
#21474=CARTESIAN_POINT('Ctrl Pts',(1.56927196686695,2.81536264999635,34.5248987128684));
#21475=CARTESIAN_POINT('Ctrl Pts',(1.74957968961034,2.71096932119611,34.5114304655076));
#21476=CARTESIAN_POINT('Ctrl Pts',(1.87853929317941,2.62325443148371,34.5010420051069));
#21477=CARTESIAN_POINT('Ctrl Pts',(2.17973946380182,2.38475215573849,34.4751049975089));
#21478=CARTESIAN_POINT('Ctrl Pts',(2.34326390700389,2.22428327706668,34.4594586098844));
#21479=CARTESIAN_POINT('Ctrl Pts',(2.50360585802273,2.02944428320449,34.443311334839));
#21480=CARTESIAN_POINT('Ctrl Pts',(2.51855678428998,2.01086006328894,34.4417972879391));
#21481=CARTESIAN_POINT('Ctrl Pts',(2.53883459739856,1.98507344998785,34.4397340726004));
#21482=CARTESIAN_POINT('Ctrl Pts',(2.54433939956032,1.97801282583329,34.4391729631644));
#21483=CARTESIAN_POINT('Ctrl Pts',(2.55306660819457,1.96672233149081,34.4382818971493));
#21484=CARTESIAN_POINT('Ctrl Pts',(2.55630804374984,1.96250733030496,34.4379506075629));
#21485=CARTESIAN_POINT('Ctrl Pts',(2.5630058776689,1.95375305104818,34.4372654012395));
#21486=CARTESIAN_POINT('Ctrl Pts',(2.56646065984225,1.94921260907553,34.4369116067553));
#21487=CARTESIAN_POINT('Ctrl Pts',(2.57470967460473,1.93831140353089,34.4360659227143));
#21488=CARTESIAN_POINT('Ctrl Pts',(2.57949245926113,1.9319419404734,34.4355748371941));
#21489=CARTESIAN_POINT('Ctrl Pts',(2.59576009918418,1.91010943970282,34.4339016621769));
#21490=CARTESIAN_POINT('Ctrl Pts',(2.60713018343652,1.89456084951831,34.4327273145807));
#21491=CARTESIAN_POINT('Ctrl Pts',(2.67097802574282,1.8055855418721,34.4260987947794));
#21492=CARTESIAN_POINT('Ctrl Pts',(2.72049729680197,1.73007522473557,34.4208242942289));
#21493=CARTESIAN_POINT('Ctrl Pts',(2.88656355252998,1.45204330706498,34.4022542725769));
#21494=CARTESIAN_POINT('Ctrl Pts',(2.98418871767681,1.23907513865428,34.3895292051052));
#21495=CARTESIAN_POINT('Ctrl Pts',(3.07801820237266,0.957061803149152,34.3726252674123));
#21496=CARTESIAN_POINT('Ctrl Pts',(3.09630667715089,0.896129295454213,34.3689737956609));
#21497=CARTESIAN_POINT('Ctrl Pts',(3.13389207215579,0.755964727717972,34.3605307986982));
#21498=CARTESIAN_POINT('Ctrl Pts',(3.15200826748489,0.676464634466203,34.3557105247701));
#21499=CARTESIAN_POINT('Ctrl Pts',(3.17082219257112,0.576550803667215,34.3495760843915));
#21500=CARTESIAN_POINT('Ctrl Pts',(3.17436763943063,0.556699440708546,34.3483536059036));
#21501=CARTESIAN_POINT('Ctrl Pts',(3.17966402239292,0.525347092388165,34.3464166042813));
#21502=CARTESIAN_POINT('Ctrl Pts',(3.18153942383196,0.513867445738512,34.3457060511851));
#21503=CARTESIAN_POINT('Ctrl Pts',(3.1848887561866,0.492644172432872,34.3443898598164));
#21504=CARTESIAN_POINT('Ctrl Pts',(3.18638022699749,0.482903422517895,34.343784787708));
#21505=CARTESIAN_POINT('Ctrl Pts',(3.18922158457901,0.463760148369837,34.3425936596155));
#21506=CARTESIAN_POINT('Ctrl Pts',(3.19057462295564,0.45435818801226,34.3420077105624));
#21507=CARTESIAN_POINT('Ctrl Pts',(3.19350633385335,0.433327336422162,34.3406948654309));
#21508=CARTESIAN_POINT('Ctrl Pts',(3.19506308599622,0.42169557204803,34.3399672814295));
#21509=CARTESIAN_POINT('Ctrl Pts',(3.1988005096575,0.392560785323828,34.3381410688746));
#21510=CARTESIAN_POINT('Ctrl Pts',(3.20090106324127,0.375048042408418,34.3370399251383));
#21511=CARTESIAN_POINT('Ctrl Pts',(3.2162032193755,0.237962742477789,34.3283928718386));
#21512=CARTESIAN_POINT('Ctrl Pts',(3.22284231002605,0.117769459684636,34.320641953786));
#21513=CARTESIAN_POINT('Ctrl Pts',(3.22274903069615,-0.00249952936660396,
34.3127207581881));
#21514=CARTESIAN_POINT('Ctrl Pts',(3.22274903383091,-0.00249548431075094,
34.3127210246048));
#21515=CARTESIAN_POINT('Ctrl Pts',(3.22268950634448,-0.0793712028058863,
34.3076578131117));
#21516=CARTESIAN_POINT('Ctrl Pts',(3.21987931323977,-0.156217567601901,
34.3025303727163));
#21517=CARTESIAN_POINT('Ctrl Pts',(3.19547714771155,-0.493017212895797,
34.2798330297308));
#21518=CARTESIAN_POINT('Ctrl Pts',(3.14512276324906,-0.749903483919484,
34.2618427002657));
#21519=CARTESIAN_POINT('Ctrl Pts',(3.05768831627768,-1.01839253467862,34.2438188480235));
#21520=CARTESIAN_POINT('Ctrl Pts',(3.05081570427129,-1.03879968789257,34.2424545719402));
#21521=CARTESIAN_POINT('Ctrl Pts',(3.04100169487757,-1.06700310258475,34.2405784727192));
#21522=CARTESIAN_POINT('Ctrl Pts',(3.03823401117646,-1.07485860752131,34.2400569377746));
#21523=CARTESIAN_POINT('Ctrl Pts',(3.03349591789615,-1.08814218853226,34.2391768560884));
#21524=CARTESIAN_POINT('Ctrl Pts',(3.03154132825663,-1.09357582415768,34.2388173795929));
#21525=CARTESIAN_POINT('Ctrl Pts',(3.02778667665852,-1.10392609148478,34.2381336619764));
#21526=CARTESIAN_POINT('Ctrl Pts',(3.02598922875553,-1.10884361530394,34.2378092631707));
#21527=CARTESIAN_POINT('Ctrl Pts',(3.02123293376603,-1.1217583660426,34.2369584146775));
#21528=CARTESIAN_POINT('Ctrl Pts',(3.01825429336274,-1.12974833318804,34.2364331420981));
#21529=CARTESIAN_POINT('Ctrl Pts',(3.00775757135357,-1.15756712588858,34.2346078981426));
#21530=CARTESIAN_POINT('Ctrl Pts',(3.00007532909418,-1.17733399413061,34.2333173609062));
#21531=CARTESIAN_POINT('Ctrl Pts',(2.89878571381708,-1.43052738545369,34.2168519096544));
#21532=CARTESIAN_POINT('Ctrl Pts',(2.77834642053627,-1.65233126494079,34.2030944086737));
#21533=CARTESIAN_POINT('Ctrl Pts',(2.56374626208711,-1.95649825046023,34.1822393187374));
#21534=CARTESIAN_POINT('Ctrl Pts',(2.4886974495452,-2.05111249664109,34.1754271339013));
#21535=CARTESIAN_POINT('Ctrl Pts',(2.36751379097276,-2.18741988250985,34.1648665552193));
#21536=CARTESIAN_POINT('Ctrl Pts',(2.32518847037112,-2.23235866016078,34.161250204236));
#21537=CARTESIAN_POINT('Ctrl Pts',(2.25222757386477,-2.30549740826488,34.1551086869342));
#21538=CARTESIAN_POINT('Ctrl Pts',(2.22228822264614,-2.3343697561343,34.1526129566688));
#21539=CARTESIAN_POINT('Ctrl Pts',(2.18071636178537,-2.37293536823143,34.1491756555924));
#21540=CARTESIAN_POINT('Ctrl Pts',(2.16956113449442,-2.38313880919625,34.1482559879938));
#21541=CARTESIAN_POINT('Ctrl Pts',(2.15141039797253,-2.39950782501703,34.1467636921517));
#21542=CARTESIAN_POINT('Ctrl Pts',(2.14445911070324,-2.40572226627519,34.146193138504));
#21543=CARTESIAN_POINT('Ctrl Pts',(2.12993388445581,-2.41859482021741,34.1450028561489));
#21544=CARTESIAN_POINT('Ctrl Pts',(2.12235547675775,-2.4252477158267,34.1443829181036));
#21545=CARTESIAN_POINT('Ctrl Pts',(2.10485433732945,-2.44046668035701,34.1429536725555));
#21546=CARTESIAN_POINT('Ctrl Pts',(2.09491036727475,-2.44900795103457,34.1421433482938));
#21547=CARTESIAN_POINT('Ctrl Pts',(2.06817704819276,-2.47168829963303,34.1399693918505));
#21548=CARTESIAN_POINT('Ctrl Pts',(2.051295125002,-2.48571672256823,34.1386012572402));
#21549=CARTESIAN_POINT('Ctrl Pts',(1.90719021310976,-2.6029962413126,34.1269603572193));
#21550=CARTESIAN_POINT('Ctrl Pts',(1.77242687335144,-2.69656304193151,34.116300449036));
#21551=CARTESIAN_POINT('Ctrl Pts',(1.41181132049793,-2.90819308711693,34.0884122781505));
#21552=CARTESIAN_POINT('Ctrl Pts',(1.1780151099184,-3.01049395687655,34.0708561732097));
#21553=CARTESIAN_POINT('Ctrl Pts',(0.881064106395242,-3.10048002765734,
34.0505612559151));
#21554=CARTESIAN_POINT('Ctrl Pts',(0.827080387910012,-3.11531528010423,
34.0469523067093));
#21555=CARTESIAN_POINT('Ctrl Pts',(0.761421516496155,-3.1315316721138,34.0426815383601));
#21556=CARTESIAN_POINT('Ctrl Pts',(0.750093829549569,-3.1342642830331,34.041948964279));
#21557=CARTESIAN_POINT('Ctrl Pts',(0.732422321404646,-3.13842594050333,
34.0408129829799));
#21558=CARTESIAN_POINT('Ctrl Pts',(0.726088711568406,-3.13989729539397,
34.0404072063414));
#21559=CARTESIAN_POINT('Ctrl Pts',(0.714308106891325,-3.14259648490657,
34.0396550532596));
#21560=CARTESIAN_POINT('Ctrl Pts',(0.708862427310016,-3.14382932080825,
34.0393084004734));
#21561=CARTESIAN_POINT('Ctrl Pts',(0.696501187692453,-3.1465940042048,34.0385238530142));
#21562=CARTESIAN_POINT('Ctrl Pts',(0.689583781090896,-3.14811720602539,
34.0380864587749));
#21563=CARTESIAN_POINT('Ctrl Pts',(0.669017730390513,-3.1525747781179,34.0367907708732));
#21564=CARTESIAN_POINT('Ctrl Pts',(0.655354772481322,-3.15544332760685,
34.0359361578871));
#21565=CARTESIAN_POINT('Ctrl Pts',(0.550616301565407,-3.17672361120095,
34.0294289845426));
#21566=CARTESIAN_POINT('Ctrl Pts',(0.458792277435907,-3.19127942205414,
34.0239790548164));
#21567=CARTESIAN_POINT('Ctrl Pts',(0.126334080150407,-3.22933003436166,
34.0047486253465));
#21568=CARTESIAN_POINT('Ctrl Pts',(-0.116127361853904,-3.22971513974557,
33.9916057746218));
#21569=CARTESIAN_POINT('Ctrl Pts',(-0.447806915516332,-3.19281253952173,
33.9726072663028));
#21570=CARTESIAN_POINT('Ctrl Pts',(-0.538766487281882,-3.1787279978541,
33.9672968283315));
#21571=CARTESIAN_POINT('Ctrl Pts',(-0.684048714342601,-3.14981681050214,
33.9585622101595));
#21572=CARTESIAN_POINT('Ctrl Pts',(-0.738804759303616,-3.13742498452496,
33.9552116788161));
#21573=CARTESIAN_POINT('Ctrl Pts',(-0.809858678038751,-3.11938161277064,
33.9507755535829));
#21574=CARTESIAN_POINT('Ctrl Pts',(-0.826476112126096,-3.11502005495813,
33.9497317183468));
#21575=CARTESIAN_POINT('Ctrl Pts',(-0.853532251035079,-3.10768692701975,
33.9480214601672));
#21576=CARTESIAN_POINT('Ctrl Pts',(-0.863992360011152,-3.1047950877977,
33.9473576372978));
#21577=CARTESIAN_POINT('Ctrl Pts',(-0.884141689813732,-3.09911482343423,
33.9460737612706));
#21578=CARTESIAN_POINT('Ctrl Pts',(-0.893832836294111,-3.09633365023407,
33.9454539515525));
#21579=CARTESIAN_POINT('Ctrl Pts',(-0.916081501794201,-3.08983555388284,
33.9440256226661));
#21580=CARTESIAN_POINT('Ctrl Pts',(-0.928629669906202,-3.08608749001063,
33.9432160909879));
#21581=CARTESIAN_POINT('Ctrl Pts',(-0.962105929169504,-3.07586567213532,
33.9410456427013));
#21582=CARTESIAN_POINT('Ctrl Pts',(-0.982991155717204,-3.0692549261134,
33.9396802464519));
#21583=CARTESIAN_POINT('Ctrl Pts',(-1.15955612529272,-3.01138028586811,
33.9280391039708));
#21584=CARTESIAN_POINT('Ctrl Pts',(-1.31115926822677,-2.94852985574958,
33.9173759002481));
#21585=CARTESIAN_POINT('Ctrl Pts',(-1.46330007080683,-2.87139610820017,
33.9059988892074));
#21586=CARTESIAN_POINT('Ctrl Pts',(-1.46928281327957,-2.86833936373547,
33.9055504022586));
#21587=CARTESIAN_POINT('Ctrl Pts',(-1.47525541125577,-2.86526421714657,
33.905101584668));
#21588=CARTESIAN_POINT('Ctrl Pts',(-1.47525540501188,-2.8652642203614,33.660216611122));
#21589=CARTESIAN_POINT('Ctrl Pts',(-1.4728255803023,-2.86651527846996,33.6603862885616));
#21590=CARTESIAN_POINT('Ctrl Pts',(-1.47039415665903,-2.8677632496416,33.6605557677759));
#21591=CARTESIAN_POINT('Ctrl Pts',(-1.46167854320598,-2.8722226938255,33.6611621794057));
#21592=CARTESIAN_POINT('Ctrl Pts',(-1.45538535560231,-2.87541663686004,
33.661598000429));
#21593=CARTESIAN_POINT('Ctrl Pts',(-1.43671419720623,-2.88481569470146,
33.6628851366076));
#21594=CARTESIAN_POINT('Ctrl Pts',(-1.42430648638582,-2.89096183400143,
33.6637328414822));
#21595=CARTESIAN_POINT('Ctrl Pts',(-1.33126250157591,-2.93630658633081,
33.6700355573838));
#21596=CARTESIAN_POINT('Ctrl Pts',(-1.24905349074832,-2.97220873530523,
33.6753020303906));
#21597=CARTESIAN_POINT('Ctrl Pts',(-0.936276528111629,-3.09352942048674,
33.6946120711626));
#21598=CARTESIAN_POINT('Ctrl Pts',(-0.6976818284038,-3.15591384426281,33.7079655080248));
#21599=CARTESIAN_POINT('Ctrl Pts',(-0.363631015283433,-3.20347904668118,
33.7271781807225));
#21600=CARTESIAN_POINT('Ctrl Pts',(-0.272456666410673,-3.21251785526814,
33.7324653244585));
#21601=CARTESIAN_POINT('Ctrl Pts',(-0.125168380193548,-3.22080430612031,
33.7411648944585));
#21602=CARTESIAN_POINT('Ctrl Pts',(-0.0692412687039754,-3.22249167207284,
33.7445044316557));
#21603=CARTESIAN_POINT('Ctrl Pts',(0.00385470494090011,-3.22279335776465,
33.7489277989379));
#21604=CARTESIAN_POINT('Ctrl Pts',(0.0210104335126121,-3.22272717268788,
33.7499701676234));
#21605=CARTESIAN_POINT('Ctrl Pts',(0.0490084758830552,-3.22239559004677,
33.7516784751288));
#21606=CARTESIAN_POINT('Ctrl Pts',(0.0598515659565342,-3.22221243169464,
33.7523418236397));
#21607=CARTESIAN_POINT('Ctrl Pts',(0.0807712680053874,-3.22175343200752,
33.7536250993456));
#21608=CARTESIAN_POINT('Ctrl Pts',(0.090847929069417,-3.22148503403112,
33.7542447849867));
#21609=CARTESIAN_POINT('Ctrl Pts',(0.114017320656081,-3.22075910938433,
33.7556732816598));
#21610=CARTESIAN_POINT('Ctrl Pts',(0.127108784992515,-3.22026901651443,
33.7564831076047));
#21611=CARTESIAN_POINT('Ctrl Pts',(0.162106333256662,-3.21874510321659,
33.7586553500724));
#21612=CARTESIAN_POINT('Ctrl Pts',(0.184005162566524,-3.21756749183474,
33.7600222597301));
#21613=CARTESIAN_POINT('Ctrl Pts',(0.370772083119689,-3.20561120434231,
33.7717476540309));
#21614=CARTESIAN_POINT('Ctrl Pts',(0.534572270148137,-3.1823941588063,33.7825001276244));
#21615=CARTESIAN_POINT('Ctrl Pts',(0.946774793484743,-3.09124199611811,
33.8106669531751));
#21616=CARTESIAN_POINT('Ctrl Pts',(1.19014951736551,-3.00594405680605,33.8284144525443));
#21617=CARTESIAN_POINT('Ctrl Pts',(1.46783231030705,-2.86955237620585,33.8486081438843));
#21618=CARTESIAN_POINT('Ctrl Pts',(1.51429135732856,-2.84530929170618,33.8519810455534));
#21619=CARTESIAN_POINT('Ctrl Pts',(1.5701368502739,-2.81441260636867,33.8560100276764));
#21620=CARTESIAN_POINT('Ctrl Pts',(1.58010281171686,-2.8088295001861,33.8567280166059));
#21621=CARTESIAN_POINT('Ctrl Pts',(1.59564990909331,-2.80001081084744,33.857846259732));
#21622=CARTESIAN_POINT('Ctrl Pts',(1.60125125696268,-2.79681132489487,33.8582487683439));
#21623=CARTESIAN_POINT('Ctrl Pts',(1.61168646774392,-2.79080911428948,33.8589978790069));
#21624=CARTESIAN_POINT('Ctrl Pts',(1.61652259638009,-2.78801066689778,33.859344738483));
#21625=CARTESIAN_POINT('Ctrl Pts',(1.62753129229085,-2.7816021616959,33.8601336273992));
#21626=CARTESIAN_POINT('Ctrl Pts',(1.6336991261263,-2.77798413619602,33.8605751324405));
#21627=CARTESIAN_POINT('Ctrl Pts',(1.652576780305,-2.76682596804097,33.8619251009243));
#21628=CARTESIAN_POINT('Ctrl Pts',(1.66524703277727,-2.75921878280522,33.8628293142991));
#21629=CARTESIAN_POINT('Ctrl Pts',(1.78032396427632,-2.68904549225664,33.8710290424274));
#21630=CARTESIAN_POINT('Ctrl Pts',(1.8792260589973,-2.62088445911598,33.877985041915));
#21631=CARTESIAN_POINT('Ctrl Pts',(2.13890018400492,-2.41964683188631,33.8966527980937));
#21632=CARTESIAN_POINT('Ctrl Pts',(2.29091481011329,-2.27624657864255,33.9080743785994));
#21633=CARTESIAN_POINT('Ctrl Pts',(2.49068672697253,-2.04735945558316,33.9253434938951));
#21634=CARTESIAN_POINT('Ctrl Pts',(2.55013727647008,-1.97281496236439,33.9308361593201));
#21635=CARTESIAN_POINT('Ctrl Pts',(2.64005201187934,-1.84920409278532,33.9398423962547));
#21636=CARTESIAN_POINT('Ctrl Pts',(2.67265475293496,-1.8017620134296,33.943276159383));
#21637=CARTESIAN_POINT('Ctrl Pts',(2.71339795707468,-1.73893342349925,33.9478068573847));
#21638=CARTESIAN_POINT('Ctrl Pts',(2.72271001024555,-1.72431670718651,33.9488597311167));
#21639=CARTESIAN_POINT('Ctrl Pts',(2.73767700771383,-1.70040013220511,33.9505809297217));
#21640=CARTESIAN_POINT('Ctrl Pts',(2.74340361270457,-1.69114535784873,33.9512465883831));
#21641=CARTESIAN_POINT('Ctrl Pts',(2.75433675098675,-1.67327462332636,33.9525313185665));
#21642=CARTESIAN_POINT('Ctrl Pts',(2.75955001443458,-1.66466291394646,33.9531501322929));
#21643=CARTESIAN_POINT('Ctrl Pts',(2.77140988974836,-1.64486295434334,33.9545723266797));
#21644=CARTESIAN_POINT('Ctrl Pts',(2.77802921936733,-1.6336586436349,33.9553766930355));
#21645=CARTESIAN_POINT('Ctrl Pts',(2.7954707304801,-1.60372345436638,33.9575248130437));
#21646=CARTESIAN_POINT('Ctrl Pts',(2.80617233955122,-1.58492343251606,33.9588729044331));
#21647=CARTESIAN_POINT('Ctrl Pts',(2.89030821426618,-1.43359424892217,33.9697182053102));
#21648=CARTESIAN_POINT('Ctrl Pts',(2.95449189606819,-1.2961635487674,33.9795443543741));
#21649=CARTESIAN_POINT('Ctrl Pts',(3.08934605135885,-0.94479209763422,34.0045591141958));
#21650=CARTESIAN_POINT('Ctrl Pts',(3.1477224592756,-0.72699748881505,34.0200010606175));
#21651=CARTESIAN_POINT('Ctrl Pts',(3.19306994939233,-0.441126339361872,
34.039271776157));
#21652=CARTESIAN_POINT('Ctrl Pts',(3.20126891046095,-0.377049827926129,
34.0435240463447));
#21653=CARTESIAN_POINT('Ctrl Pts',(3.20989118319928,-0.288625181510789,
34.0492637700471));
#21654=CARTESIAN_POINT('Ctrl Pts',(3.21197264882183,-0.264457337145626,
34.0508193773346));
#21655=CARTESIAN_POINT('Ctrl Pts',(3.21509141407373,-0.222741217698234,
34.053479262443));
#21656=CARTESIAN_POINT('Ctrl Pts',(3.21625835328021,-0.205204016598402,
34.0545897819485));
#21657=CARTESIAN_POINT('Ctrl Pts',(3.21772861712967,-0.179997199387764,
34.056174099854));
#21658=CARTESIAN_POINT('Ctrl Pts',(3.21814808256899,-0.172335042338471,
34.0566541133346));
#21659=CARTESIAN_POINT('Ctrl Pts',(3.21882909996629,-0.159024398863697,
34.0574851697711));
#21660=CARTESIAN_POINT('Ctrl Pts',(3.21910315915259,-0.153376618015321,
34.0578369088213));
#21661=CARTESIAN_POINT('Ctrl Pts',(3.21964498638606,-0.141568850803734,
34.0585704110216));
#21662=CARTESIAN_POINT('Ctrl Pts',(3.219909941799,-0.135408810999306,34.058952015179));
#21663=CARTESIAN_POINT('Ctrl Pts',(3.22056378964949,-0.119118477070685,
34.0599584622756));
#21664=CARTESIAN_POINT('Ctrl Pts',(3.2209225676546,-0.108986945972917,34.0605816349504));
#21665=CARTESIAN_POINT('Ctrl Pts',(3.22223308702053,-0.0662825499948332,
34.0631972589008));
#21666=CARTESIAN_POINT('Ctrl Pts',(3.22273861344313,-0.0336966216181623,
34.0651660519612));
#21667=CARTESIAN_POINT('Ctrl Pts',(3.22284085997709,0.263913886241149,34.0829454412723));
#21668=CARTESIAN_POINT('Ctrl Pts',(3.19024154128433,0.527970392858009,34.0973245963946));
#21669=CARTESIAN_POINT('Ctrl Pts',(3.08206581443839,0.958653158441696,34.1223202205985));
#21670=CARTESIAN_POINT('Ctrl Pts',(3.024093633427,1.12826883321634,34.1325838388579));
#21671=CARTESIAN_POINT('Ctrl Pts',(2.94346373664055,1.31249003732423,34.1446763593646));
#21672=CARTESIAN_POINT('Ctrl Pts',(2.93436729250897,1.33270305097177,34.1460161419005));
#21673=CARTESIAN_POINT('Ctrl Pts',(2.91953522437539,1.36477289721287,34.1481633342022));
#21674=CARTESIAN_POINT('Ctrl Pts',(2.91393406513983,1.37669141178235,34.148966104497));
#21675=CARTESIAN_POINT('Ctrl Pts',(2.90391213803772,1.39768154042701,34.1503885099551));
#21676=CARTESIAN_POINT('Ctrl Pts',(2.89952148989016,1.40676740077379,34.1510070904597));
#21677=CARTESIAN_POINT('Ctrl Pts',(2.8903367502876,1.42554831850029,34.1522917617754));
#21678=CARTESIAN_POINT('Ctrl Pts',(2.88553638730329,1.43524015113331,34.1529580663957));
#21679=CARTESIAN_POINT('Ctrl Pts',(2.87305498665674,1.46012410543961,34.1546775653687));
#21680=CARTESIAN_POINT('Ctrl Pts',(2.86530227172579,1.47527971359988,34.1557332731608));
#21681=CARTESIAN_POINT('Ctrl Pts',(2.83210772836556,1.53892222832228,34.16020274183));
#21682=CARTESIAN_POINT('Ctrl Pts',(2.80555364506525,1.58681566690869,34.1636557592413));
#21683=CARTESIAN_POINT('Ctrl Pts',(2.73272738552284,1.71061948323202,34.1728256631441));
#21684=CARTESIAN_POINT('Ctrl Pts',(2.68451450764142,1.7853284128188,34.1786089104205));
#21685=CARTESIAN_POINT('Ctrl Pts',(2.48782569302961,2.06409703362566,34.2011452485164));
#21686=CARTESIAN_POINT('Ctrl Pts',(2.31868502308203,2.25243322258226,34.2185207336602));
#21687=CARTESIAN_POINT('Ctrl Pts',(2.06364001592,2.47692648334788,34.2410876256664));
#21688=CARTESIAN_POINT('Ctrl Pts',(1.99562036087461,2.53205001763297,34.2468060703505));
#21689=CARTESIAN_POINT('Ctrl Pts',(1.91439438169414,2.59256654014724,34.2532207524362));
#21690=CARTESIAN_POINT('Ctrl Pts',(1.90330110770706,2.60072144280946,34.2540882268972));
#21691=CARTESIAN_POINT('Ctrl Pts',(1.88645647656314,2.61293878463141,34.2553920859953));
#21692=CARTESIAN_POINT('Ctrl Pts',(1.88074367525935,2.617053755735,34.2558319846327));
#21693=CARTESIAN_POINT('Ctrl Pts',(1.87048017380436,2.62439566420057,34.2566181146173));
#21694=CARTESIAN_POINT('Ctrl Pts',(1.86593455715238,2.62762952351049,34.2569648189313));
#21695=CARTESIAN_POINT('Ctrl Pts',(1.85605025136268,2.6346228686724,34.2577155332949));
#21696=CARTESIAN_POINT('Ctrl Pts',(1.85070854347813,2.63837792679481,34.2581192397352));
#21697=CARTESIAN_POINT('Ctrl Pts',(1.83569472308831,2.64886415320818,34.2592484518159));
#21698=CARTESIAN_POINT('Ctrl Pts',(1.82599693378279,2.65555862792185,34.2599714910957));
#21699=CARTESIAN_POINT('Ctrl Pts',(1.76816082889255,2.69501680216037,34.2642474219768));
#21700=CARTESIAN_POINT('Ctrl Pts',(1.71917506605233,2.72652642660301,34.2677210106777));
#21701=CARTESIAN_POINT('Ctrl Pts',(1.45333332568138,2.88751105619469,34.2859467393601));
#21702=CARTESIAN_POINT('Ctrl Pts',(1.22266080426761,2.99249470690328,34.2996551499078));
#21703=CARTESIAN_POINT('Ctrl Pts',(0.826639648367929,3.11920150073874,34.3231453481257));
#21704=CARTESIAN_POINT('Ctrl Pts',(0.667670942802012,3.15704866566824,34.332551571068));
#21705=CARTESIAN_POINT('Ctrl Pts',(0.484914441452332,3.18613476437704,34.3436823160037));
#21706=CARTESIAN_POINT('Ctrl Pts',(0.463262042801261,3.18935494979522,34.3450057038783));
#21707=CARTESIAN_POINT('Ctrl Pts',(0.428613349125122,3.19414769256769,34.3471315440924));
#21708=CARTESIAN_POINT('Ctrl Pts',(0.41563712568302,3.19586211479855,34.3479295024848));
#21709=CARTESIAN_POINT('Ctrl Pts',(0.392651493811022,3.19875662437138,34.3493463293875));
#21710=CARTESIAN_POINT('Ctrl Pts',(0.382646260562462,3.19996890190581,34.3499641702262));
#21711=CARTESIAN_POINT('Ctrl Pts',(0.361858629613905,3.20238873522098,34.3512502398636));
#21712=CARTESIAN_POINT('Ctrl Pts',(0.351075505047797,3.20358881013814,34.3519186970447));
#21713=CARTESIAN_POINT('Ctrl Pts',(0.3232038226825,3.20654829435708,34.3536500400945));
#21714=CARTESIAN_POINT('Ctrl Pts',(0.306107057752536,3.20822554160638,34.3547155060354));
#21715=CARTESIAN_POINT('Ctrl Pts',(0.233069075445021,3.21480166838262,34.3592824360435));
#21716=CARTESIAN_POINT('Ctrl Pts',(0.177021192189369,3.21837440618064,34.3628253235261));
#21717=CARTESIAN_POINT('Ctrl Pts',(0.0289100688562121,3.22393516175409,
34.3722947096103));
#21718=CARTESIAN_POINT('Ctrl Pts',(-0.0631892968643576,3.22344509803694,
34.3782930945743));
#21719=CARTESIAN_POINT('Ctrl Pts',(-0.396139889156062,3.20739911314354,
34.4003459230898));
#21720=CARTESIAN_POINT('Ctrl Pts',(-0.635052964436707,3.1687582514174,34.416937439632));
#21721=CARTESIAN_POINT('Ctrl Pts',(-0.957227151273777,3.07872246075456,
34.4392030718179));
#21722=CARTESIAN_POINT('Ctrl Pts',(-1.04592751058867,3.04973031407694,34.445310912867));
#21723=CARTESIAN_POINT('Ctrl Pts',(-1.1463295606484,3.01201613809305,34.4521047022913));
#21724=CARTESIAN_POINT('Ctrl Pts',(-1.15937404031762,3.00701920995031,34.4529849721801));
#21725=CARTESIAN_POINT('Ctrl Pts',(-1.1789838577939,2.99936073164673,34.4543042204606));
#21726=CARTESIAN_POINT('Ctrl Pts',(-1.18557338442597,2.99676216739007,34.4547468348062));
#21727=CARTESIAN_POINT('Ctrl Pts',(-1.1973401612175,2.99207708067093,34.4555358873653));
#21728=CARTESIAN_POINT('Ctrl Pts',(-1.20252059043243,2.98999882098789,34.4558828137425));
#21729=CARTESIAN_POINT('Ctrl Pts',(-1.21372000588447,2.98547207841237,34.4566318148952));
#21730=CARTESIAN_POINT('Ctrl Pts',(-1.2197369765306,2.98301885570794,34.4570335978975));
#21731=CARTESIAN_POINT('Ctrl Pts',(-1.23651036056334,2.97612082167146,34.4581520078113));
#21732=CARTESIAN_POINT('Ctrl Pts',(-1.24725030549444,2.97163586296246,34.4588662437971));
#21733=CARTESIAN_POINT('Ctrl Pts',(-1.30933042849502,2.94531559422303,34.4629851525495));
#21734=CARTESIAN_POINT('Ctrl Pts',(-1.3601244415025,2.92220678523587,34.4663171541771));
#21735=CARTESIAN_POINT('Ctrl Pts',(-1.6389793450722,2.7864936606291,34.4845336149946));
#21736=CARTESIAN_POINT('Ctrl Pts',(-1.85370559745061,2.6485096302318,34.4983346524173));
#21737=CARTESIAN_POINT('Ctrl Pts',(-2.17659955859563,2.38232168211621,34.5219705142417));
#21738=CARTESIAN_POINT('Ctrl Pts',(-2.29503818044432,2.26844252967868,34.5314253652527));
#21739=CARTESIAN_POINT('Ctrl Pts',(-2.41887269397027,2.12970712156491,34.5426105021688));
#21740=CARTESIAN_POINT('Ctrl Pts',(-2.43329421195046,2.11321479624367,34.543934953249));
#21741=CARTESIAN_POINT('Ctrl Pts',(-2.45606470765608,2.0866324959153,34.5460621787147));
#21742=CARTESIAN_POINT('Ctrl Pts',(-2.46452243674701,2.0766362637765,34.5468604497816));
#21743=CARTESIAN_POINT('Ctrl Pts',(-2.4793822421309,2.05885474266377,34.5482776384994));
#21744=CARTESIAN_POINT('Ctrl Pts',(-2.4858091911122,2.05109039676444,34.5488955267275));
#21745=CARTESIAN_POINT('Ctrl Pts',(-2.49907709557057,2.03490759017481,34.5501815021643));
#21746=CARTESIAN_POINT('Ctrl Pts',(-2.50591217278991,2.02648449483665,34.5508498167971));
#21747=CARTESIAN_POINT('Ctrl Pts',(-2.52345516515957,2.00464120262812,34.5525803760308));
#21748=CARTESIAN_POINT('Ctrl Pts',(-2.5340984917923,1.99116979119174,34.5536451962752));
#21749=CARTESIAN_POINT('Ctrl Pts',(-2.57903520613856,1.93334887253686,34.5582056119943));
#21750=CARTESIAN_POINT('Ctrl Pts',(-2.61227414128307,1.88819586676661,34.561742484096));
#21751=CARTESIAN_POINT('Ctrl Pts',(-2.6968215291213,1.76683556149029,34.5711917145426));
#21752=CARTESIAN_POINT('Ctrl Pts',(-2.74607575513466,1.68926602187381,34.5771755793808));
#21753=CARTESIAN_POINT('Ctrl Pts',(-2.91358124290104,1.39873667276134,34.5993598767689));
#21754=CARTESIAN_POINT('Ctrl Pts',(-3.01090014482924,1.17468513655043,34.6161114129974));
#21755=CARTESIAN_POINT('Ctrl Pts',(-3.10878701675985,0.854357027892131,
34.6383912175558));
#21756=CARTESIAN_POINT('Ctrl Pts',(-3.13178297586233,0.76578156239024,34.6443769437342));
#21757=CARTESIAN_POINT('Ctrl Pts',(-3.15390009751464,0.662740663365961,
34.6510521895322));
#21758=CARTESIAN_POINT('Ctrl Pts',(-3.1567310133967,0.649122744523126,34.6519286477451));
#21759=CARTESIAN_POINT('Ctrl Pts',(-3.16086796299769,0.628554910666711,
34.6532433138618));
#21760=CARTESIAN_POINT('Ctrl Pts',(-3.16223938941499,0.621618533769253,
34.6536851211943));
#21761=CARTESIAN_POINT('Ctrl Pts',(-3.16465241468779,0.609199311869242,
34.6544733029363));
#21762=CARTESIAN_POINT('Ctrl Pts',(-3.16570260643867,0.60371824266424,34.6548201609968));
#21763=CARTESIAN_POINT('Ctrl Pts',(-3.16794647384673,0.591840386406922,
34.6555696606333));
#21764=CARTESIAN_POINT('Ctrl Pts',(-3.1691350119311,0.585442723125801,34.6559720069591));
#21765=CARTESIAN_POINT('Ctrl Pts',(-3.17240293322075,0.567550558853649,
34.657093577287));
#21766=CARTESIAN_POINT('Ctrl Pts',(-3.17443923746657,0.556048149832419,
34.6578103884036));
#21767=CARTESIAN_POINT('Ctrl Pts',(-3.18595801147179,0.488856137763672,
34.6619744338813));
#21768=CARTESIAN_POINT('Ctrl Pts',(-3.19403809728417,0.43293222306134,34.665347122134));
#21769=CARTESIAN_POINT('Ctrl Pts',(-3.23032081244044,0.12475387467685,34.6835656797003));
#21770=CARTESIAN_POINT('Ctrl Pts',(-3.23011976760302,-0.129959484163719,
34.6973396808747));
#21771=CARTESIAN_POINT('Ctrl Pts',(-3.18060479565052,-0.544714443388395,
34.7209335717263));
#21772=CARTESIAN_POINT('Ctrl Pts',(-3.14880858468423,-0.705659088372832,
34.7303748316575));
#21773=CARTESIAN_POINT('Ctrl Pts',(-3.09905095561747,-0.884579272956763,
34.7415447641064));
#21774=CARTESIAN_POINT('Ctrl Pts',(-3.09296751080527,-0.905620923168818,
34.742868919011));
#21775=CARTESIAN_POINT('Ctrl Pts',(-3.08290575764763,-0.939138473665273,
34.7449957585969));
#21776=CARTESIAN_POINT('Ctrl Pts',(-3.07906501170587,-0.951655204895223,
34.7457939425712));
#21777=CARTESIAN_POINT('Ctrl Pts',(-3.07213280761211,-0.973765455228551,
34.747211030499));
#21778=CARTESIAN_POINT('Ctrl Pts',(-3.06907239689361,-0.98336858215175,
34.7478289055177));
#21779=CARTESIAN_POINT('Ctrl Pts',(-3.0626246217544,-1.00327746414113,34.7491149071457));
#21780=CARTESIAN_POINT('Ctrl Pts',(-3.05923017317437,-1.01358077466077,
34.7497832614461));
#21781=CARTESIAN_POINT('Ctrl Pts',(-3.05032844770001,-1.0401484419375,34.7515140388028));
#21782=CARTESIAN_POINT('Ctrl Pts',(-3.04474313928114,-1.05638611194859,
34.7525790387347));
#21783=CARTESIAN_POINT('Ctrl Pts',(-3.02036166261241,-1.12546825988132,
34.7571412663421));
#21784=CARTESIAN_POINT('Ctrl Pts',(-3.00031839562588,-1.17785918683693,
34.7606798114443));
#21785=CARTESIAN_POINT('Ctrl Pts',(-2.94384900810734,-1.31465517888829,
34.7701346459885));
#21786=CARTESIAN_POINT('Ctrl Pts',(-2.90516325351745,-1.39806622594099,
34.7761225474268));
#21787=CARTESIAN_POINT('Ctrl Pts',(-2.75142987754299,-1.69551340725513,
34.7982722767553));
#21788=CARTESIAN_POINT('Ctrl Pts',(-2.61586033812479,-1.89799678043436,
34.8149814582973));
#21789=CARTESIAN_POINT('Ctrl Pts',(-2.3994112719973,-2.15346113835054,34.8372572014884));
#21790=CARTESIAN_POINT('Ctrl Pts',(-2.33700121942408,-2.22103535195844,
34.8432749163128));
#21791=CARTESIAN_POINT('Ctrl Pts',(-2.26190437589437,-2.2956698477108,34.8499812455905));
#21792=CARTESIAN_POINT('Ctrl Pts',(-2.25196415784003,-2.30542163251187,
34.8508587199754));
#21793=CARTESIAN_POINT('Ctrl Pts',(-2.23687916253723,-2.3200300031454,34.8521746078523));
#21794=CARTESIAN_POINT('Ctrl Pts',(-2.23178124087571,-2.32493442884553,
34.8526166304943));
#21795=CARTESIAN_POINT('Ctrl Pts',(-2.22263247016308,-2.33367812965707,
34.853405044379));
#21796=CARTESIAN_POINT('Ctrl Pts',(-2.21858777281354,-2.33752369103636,
34.8537519204768));
#21797=CARTESIAN_POINT('Ctrl Pts',(-2.20980738000018,-2.34582847095305,
34.8545012862538));
#21798=CARTESIAN_POINT('Ctrl Pts',(-2.20506818236936,-2.35028385194338,
34.8549034816138));
#21799=CARTESIAN_POINT('Ctrl Pts',(-2.19178901696946,-2.36269224545409,
34.8560242047182));
#21800=CARTESIAN_POINT('Ctrl Pts',(-2.1832191914672,-2.37061336226623,34.8567403254728));
#21801=CARTESIAN_POINT('Ctrl Pts',(-2.13305380186929,-2.4164786266356,34.8608922072046));
#21802=CARTESIAN_POINT('Ctrl Pts',(-2.09050983496426,-2.45337665240373,
34.8642539298408));
#21803=CARTESIAN_POINT('Ctrl Pts',(-1.87028138285107,-2.63448778882551,
34.8809967045372));
#21804=CARTESIAN_POINT('Ctrl Pts',(-1.67860838796915,-2.76056267662292,
34.8935046039807));
#21805=CARTESIAN_POINT('Ctrl Pts',(-1.4752554044579,-2.86526422064663,34.9063554765866));
#21806=CARTESIAN_POINT('Origin',(0.,0.,4.68922655072688));
#21807=CARTESIAN_POINT('',(-1.47525545662511,-2.865264193787,36.4017031386693));
#21808=CARTESIAN_POINT('',(-1.47525533429856,-2.86526425676998,36.1542047394732));
#21809=CARTESIAN_POINT('',(-1.47525540501186,-2.86526422036142,4.68922655072688));
#21810=CARTESIAN_POINT('Ctrl Pts',(-1.4752554566251,-2.865264193787,36.4017031386693));
#21811=CARTESIAN_POINT('Ctrl Pts',(-1.66869427635609,-2.76566720899584,
36.3893221826344));
#21812=CARTESIAN_POINT('Ctrl Pts',(-1.85161275111611,-2.64670560438004,
36.3774197811539));
#21813=CARTESIAN_POINT('Ctrl Pts',(-2.09281079697536,-2.45249159555157,
36.3597902555439));
#21814=CARTESIAN_POINT('Ctrl Pts',(-2.16192269046745,-2.39179020980833,
36.3544830894472));
#21815=CARTESIAN_POINT('Ctrl Pts',(-2.26887596446572,-2.28942515554214,
36.3457533615933));
#21816=CARTESIAN_POINT('Ctrl Pts',(-2.30838825200233,-2.24957969103573,
36.3424043407513));
#21817=CARTESIAN_POINT('Ctrl Pts',(-2.35861129851129,-2.19621614818392,
36.3379699373801));
#21818=CARTESIAN_POINT('Ctrl Pts',(-2.37028355000504,-2.183613633822,36.3369262723467));
#21819=CARTESIAN_POINT('Ctrl Pts',(-2.38916441559391,-2.16289822266887,
36.3352162229861));
#21820=CARTESIAN_POINT('Ctrl Pts',(-2.39643388059001,-2.15484105626593,
36.3345524375081));
#21821=CARTESIAN_POINT('Ctrl Pts',(-2.41037868396717,-2.13922738878082,
36.3332685845929));
#21822=CARTESIAN_POINT('Ctrl Pts',(-2.4170595355309,-2.13167596483264,36.3326487603306));
#21823=CARTESIAN_POINT('Ctrl Pts',(-2.43233722136632,-2.11424330367405,
36.3312203273868));
#21824=CARTESIAN_POINT('Ctrl Pts',(-2.44090943012627,-2.10434081159747,
36.330410705713));
#21825=CARTESIAN_POINT('Ctrl Pts',(-2.46366055643201,-2.077732978578,36.3282398591823));
#21826=CARTESIAN_POINT('Ctrl Pts',(-2.47772967263198,-2.06093505444706,
36.3268741521003));
#21827=CARTESIAN_POINT('Ctrl Pts',(-2.59564432521869,-1.91719733185216,
36.3152262642827));
#21828=CARTESIAN_POINT('Ctrl Pts',(-2.68981555077983,-1.78266448109943,
36.3045561258471));
#21829=CARTESIAN_POINT('Ctrl Pts',(-2.90296655650853,-1.42255880187577,
36.2766451192449));
#21830=CARTESIAN_POINT('Ctrl Pts',(-3.00619697526368,-1.1889757742665,36.2590762793693));
#21831=CARTESIAN_POINT('Ctrl Pts',(-3.09723001100283,-0.892406918471076,
36.2387879909886));
#21832=CARTESIAN_POINT('Ctrl Pts',(-3.11220098758202,-0.838707191176308,
36.2351947135659));
#21833=CARTESIAN_POINT('Ctrl Pts',(-3.12860596231211,-0.77335485671857,
36.2309399339579));
#21834=CARTESIAN_POINT('Ctrl Pts',(-3.1313783140909,-0.762051747337994,
36.23020828139));
#21835=CARTESIAN_POINT('Ctrl Pts',(-3.13560336091536,-0.744413435422304,
36.2290734147302));
#21836=CARTESIAN_POINT('Ctrl Pts',(-3.13709819101134,-0.738088572967554,
36.2286678385843));
#21837=CARTESIAN_POINT('Ctrl Pts',(-3.13984177468579,-0.72632112201274,
36.2279158659925));
#21838=CARTESIAN_POINT('Ctrl Pts',(-3.14109550405649,-0.720879863391161,
36.2275691944005));
#21839=CARTESIAN_POINT('Ctrl Pts',(-3.14390848360291,-0.708524692862517,
36.2267843606805));
#21840=CARTESIAN_POINT('Ctrl Pts',(-3.14545906890058,-0.7016088951856,36.2263467005048));
#21841=CARTESIAN_POINT('Ctrl Pts',(-3.15000053601545,-0.681035719783496,
36.2250494938298));
#21842=CARTESIAN_POINT('Ctrl Pts',(-3.15292541978737,-0.667363725563551,
36.2241936408038));
#21843=CARTESIAN_POINT('Ctrl Pts',(-3.17473630572985,-0.562066480390239,
36.217646818863));
#21844=CARTESIAN_POINT('Ctrl Pts',(-3.18971552183379,-0.469667736758124,
36.2121612808798));
#21845=CARTESIAN_POINT('Ctrl Pts',(-3.22881685393737,-0.137475661207952,
36.1929448764684));
#21846=CARTESIAN_POINT('Ctrl Pts',(-3.23006391976129,0.104198470726065,
36.1798418610527));
#21847=CARTESIAN_POINT('Ctrl Pts',(-3.19454133368619,0.435317819656115,
36.160884215462));
#21848=CARTESIAN_POINT('Ctrl Pts',(-3.18080107331359,0.526401492349101,
36.1555698766831));
#21849=CARTESIAN_POINT('Ctrl Pts',(-3.15243249578763,0.671893889730702,
36.1468294285881));
#21850=CARTESIAN_POINT('Ctrl Pts',(-3.14024503129078,0.726727324839323,
36.1434770969363));
#21851=CARTESIAN_POINT('Ctrl Pts',(-3.12246623469435,0.797883107871334,
36.1390389195492));
#21852=CARTESIAN_POINT('Ctrl Pts',(-3.11816761874797,0.814520425915876,
36.1379948815497));
#21853=CARTESIAN_POINT('Ctrl Pts',(-3.11093724354449,0.841608473586556,
36.1362843746005));
#21854=CARTESIAN_POINT('Ctrl Pts',(-3.10808534167546,0.852080313344894,
36.1356205071843));
#21855=CARTESIAN_POINT('Ctrl Pts',(-3.10248225175357,0.872251734680528,
36.1343366035991));
#21856=CARTESIAN_POINT('Ctrl Pts',(-3.09973833263651,0.881953216784308,
36.1337168111851));
#21857=CARTESIAN_POINT('Ctrl Pts',(-3.09332614644484,0.904224736958464,
36.1322886061585));
#21858=CARTESIAN_POINT('Ctrl Pts',(-3.08962672060242,0.916785548758172,
36.1314791816102));
#21859=CARTESIAN_POINT('Ctrl Pts',(-3.07953558225134,0.950293529925363,
36.129309207357));
#21860=CARTESIAN_POINT('Ctrl Pts',(-3.07300680849741,0.971198389648268,
36.1279441810858));
#21861=CARTESIAN_POINT('Ctrl Pts',(-3.0159472071808,1.14756308465134,36.1163308383265));
#21862=CARTESIAN_POINT('Ctrl Pts',(-2.95387687150754,1.29901325345948,36.105697220258));
#21863=CARTESIAN_POINT('Ctrl Pts',(-2.76697646274527,1.67157634412449,36.0778999850928));
#21864=CARTESIAN_POINT('Ctrl Pts',(-2.62704589908076,1.8838659841783,36.0604107198992));
#21865=CARTESIAN_POINT('Ctrl Pts',(-2.4268025361608,2.12132573757848,36.0400797143045));
#21866=CARTESIAN_POINT('Ctrl Pts',(-2.38874354333528,2.16409303804695,36.0363872694324));
#21867=CARTESIAN_POINT('Ctrl Pts',(-2.34153542950344,2.2143773270336,36.0320314379602));
#21868=CARTESIAN_POINT('Ctrl Pts',(-2.33346121713322,2.22288413378063,36.0312940349814));
#21869=CARTESIAN_POINT('Ctrl Pts',(-2.32082720425748,2.23605034476201,36.0301522142088));
#21870=CARTESIAN_POINT('Ctrl Pts',(-2.31629950050604,2.24074020851906,36.029745388234));
#21871=CARTESIAN_POINT('Ctrl Pts',(-2.30786846486906,2.24942034050592,36.0289922854517));
#21872=CARTESIAN_POINT('Ctrl Pts',(-2.30396903297706,2.2534141685973,36.0286457260504));
#21873=CARTESIAN_POINT('Ctrl Pts',(-2.29511360627042,2.26243694868658,36.0278626538892));
#21874=CARTESIAN_POINT('Ctrl Pts',(-2.290151462035,2.26745974510023,36.0274266337121));
#21875=CARTESIAN_POINT('Ctrl Pts',(-2.27540346167664,2.28229020923059,36.0261387796157));
#21876=CARTESIAN_POINT('Ctrl Pts',(-2.26557067601711,2.29205127353722,36.0252905607156));
#21877=CARTESIAN_POINT('Ctrl Pts',(-2.19153366999279,2.3646062912491,36.0189783980574));
#21878=CARTESIAN_POINT('Ctrl Pts',(-2.12478637581597,2.42476159288578,36.0137036131672));
#21879=CARTESIAN_POINT('Ctrl Pts',(-1.86643674046048,2.63872350758135,35.9943970810265));
#21880=CARTESIAN_POINT('Ctrl Pts',(-1.65997040785983,2.77325803802885,35.981053019721));
#21881=CARTESIAN_POINT('Ctrl Pts',(-1.35827624099663,2.92396860341079,35.961850542876));
#21882=CARTESIAN_POINT('Ctrl Pts',(-1.27463637834816,2.96138598143209,35.9565630524638));
#21883=CARTESIAN_POINT('Ctrl Pts',(-1.1375192048237,3.01584123027732,35.9478627399254));
#21884=CARTESIAN_POINT('Ctrl Pts',(-1.08499093539938,3.03513465362525,35.944522811462));
#21885=CARTESIAN_POINT('Ctrl Pts',(-1.0157326370007,3.05854528327568,35.9400987738295));
#21886=CARTESIAN_POINT('Ctrl Pts',(-0.999432527825012,3.06391035187438,
35.9390561348554));
#21887=CARTESIAN_POINT('Ctrl Pts',(-0.972759502201917,3.07245409982136,
35.9373473443108));
#21888=CARTESIAN_POINT('Ctrl Pts',(-0.962411873305188,3.07571107651609,
35.9366837842103));
#21889=CARTESIAN_POINT('Ctrl Pts',(-0.942414204529635,3.08189466328807,
35.9354000702273));
#21890=CARTESIAN_POINT('Ctrl Pts',(-0.932766472689344,3.08482835053112,
35.9347801579221));
#21891=CARTESIAN_POINT('Ctrl Pts',(-0.910548242818551,3.09147072288122,
35.9333510959763));
#21892=CARTESIAN_POINT('Ctrl Pts',(-0.897968636476481,3.09514808251229,
35.9325409304278));
#21893=CARTESIAN_POINT('Ctrl Pts',(-0.864270272341653,3.10477629925755,
35.9303676766413));
#21894=CARTESIAN_POINT('Ctrl Pts',(-0.84311287625281,3.11058830633781,35.9290000905431));
#21895=CARTESIAN_POINT('Ctrl Pts',(-0.661863218807286,3.15839317942911,
35.917255867631));
#21896=CARTESIAN_POINT('Ctrl Pts',(-0.498840065700016,3.18820543149673,
35.9064838119598));
#21897=CARTESIAN_POINT('Ctrl Pts',(-0.0775209154443138,3.23214251743292,
35.8782184628344));
#21898=CARTESIAN_POINT('Ctrl Pts',(0.181502930681532,3.22797267735349,35.8603879234517));
#21899=CARTESIAN_POINT('Ctrl Pts',(0.487863319199088,3.18601893455163,35.8402195684928));
#21900=CARTESIAN_POINT('Ctrl Pts',(0.538307763061424,3.17788494441735,35.8369327137392));
#21901=CARTESIAN_POINT('Ctrl Pts',(0.599688383849988,3.16648384856296,35.8329920686422));
#21902=CARTESIAN_POINT('Ctrl Pts',(0.610825264923671,3.1643543773893,35.8322794622434));
#21903=CARTESIAN_POINT('Ctrl Pts',(0.628263365765897,3.16092456329657,35.8311676523732));
#21904=CARTESIAN_POINT('Ctrl Pts',(0.634572195913244,3.15966407732031,35.8307662369272));
#21905=CARTESIAN_POINT('Ctrl Pts',(0.646357797563831,3.15727262567872,35.8300179358789));
#21906=CARTESIAN_POINT('Ctrl Pts',(0.651835339067373,3.15614630945402,35.8296708001458));
#21907=CARTESIAN_POINT('Ctrl Pts',(0.664341425809498,3.15354080655823,35.8288796893868));
#21908=CARTESIAN_POINT('Ctrl Pts',(0.671367963211146,3.15205238043466,35.8284362492664));
#21909=CARTESIAN_POINT('Ctrl Pts',(0.692987271204733,3.14739720691011,35.8270749245637));
#21910=CARTESIAN_POINT('Ctrl Pts',(0.707563300445875,3.1441524663894,35.8261613932797));
#21911=CARTESIAN_POINT('Ctrl Pts',(0.850396354165353,3.11131309319946,35.8172470247137));
#21912=CARTESIAN_POINT('Ctrl Pts',(0.976765664063272,3.07398449267316,35.8096553219812));
#21913=CARTESIAN_POINT('Ctrl Pts',(1.28116377243312,2.96339000666203,35.7913234671513));
#21914=CARTESIAN_POINT('Ctrl Pts',(1.45558247647445,2.88172568056682,35.780760304734));
#21915=CARTESIAN_POINT('Ctrl Pts',(1.70654800596999,2.73559036088559,35.7642735856097));
#21916=CARTESIAN_POINT('Ctrl Pts',(1.78910043840985,2.68232698899493,35.7586216402397));
#21917=CARTESIAN_POINT('Ctrl Pts',(1.91698293481149,2.59128356765466,35.7493783783071));
#21918=CARTESIAN_POINT('Ctrl Pts',(1.9639329974732,2.55588353055802,35.745872467841));
#21919=CARTESIAN_POINT('Ctrl Pts',(2.02353954300244,2.508328195338,35.7412594877645));
#21920=CARTESIAN_POINT('Ctrl Pts',(2.03710357511151,2.49732489340492,35.7401985238074));
#21921=CARTESIAN_POINT('Ctrl Pts',(2.05899814435663,2.47926669655605,35.7384672422277));
#21922=CARTESIAN_POINT('Ctrl Pts',(2.06738357303326,2.47227867936313,35.7377996490559));
#21923=CARTESIAN_POINT('Ctrl Pts',(2.0834294887869,2.45876805592077,35.7365133556708));
#21924=CARTESIAN_POINT('Ctrl Pts',(2.09109526081211,2.45225190266198,35.7358949252326));
#21925=CARTESIAN_POINT('Ctrl Pts',(2.10856282331383,2.43726245061999,35.7344766745273));
#21926=CARTESIAN_POINT('Ctrl Pts',(2.11834423121709,2.42876576541529,35.7336758885155));
#21927=CARTESIAN_POINT('Ctrl Pts',(2.14416746548818,2.40605957695487,35.7315440229543));
#21928=CARTESIAN_POINT('Ctrl Pts',(2.16011903659429,2.39174884129328,35.7302087106815));
#21929=CARTESIAN_POINT('Ctrl Pts',(2.28178596952608,2.28038701143607,35.7198793175012));
#21930=CARTESIAN_POINT('Ctrl Pts',(2.38104065298987,2.17654485412815,35.7105913832565));
#21931=CARTESIAN_POINT('Ctrl Pts',(2.60610116272965,1.9072020843764,35.6873192778303));
#21932=CARTESIAN_POINT('Ctrl Pts',(2.72346917200883,1.73547943336091,35.6731209344519));
#21933=CARTESIAN_POINT('Ctrl Pts',(2.86327716762166,1.48140730809603,35.6536685706928));
#21934=CARTESIAN_POINT('Ctrl Pts',(2.90026300488421,1.40762216183968,35.6481915085174));
#21935=CARTESIAN_POINT('Ctrl Pts',(2.95217899339544,1.29329433477463,35.6400426875703));
#21936=CARTESIAN_POINT('Ctrl Pts',(2.96919330260592,1.25373944989675,35.6372828773444));
#21937=CARTESIAN_POINT('Ctrl Pts',(2.9894558456152,1.20390474923328,35.6338900495056));
#21938=CARTESIAN_POINT('Ctrl Pts',(2.99345118547411,1.19393588856406,35.6332155142094));
#21939=CARTESIAN_POINT('Ctrl Pts',(2.99971151516166,1.17808662315959,35.6321498891079));
#21940=CARTESIAN_POINT('Ctrl Pts',(3.00200917756625,1.17221933326814,35.6317568749454));
#21941=CARTESIAN_POINT('Ctrl Pts',(3.00632254169706,1.16110890536614,35.6310154895963));
#21942=CARTESIAN_POINT('Ctrl Pts',(3.00834171820475,1.15586730284646,35.6306669200337));
#21943=CARTESIAN_POINT('Ctrl Pts',(3.01294585228916,1.14382158984963,35.6298685788811));
#21944=CARTESIAN_POINT('Ctrl Pts',(3.01552146961116,1.13701398715773,35.629419370794));
#21945=CARTESIAN_POINT('Ctrl Pts',(3.02233856552016,1.11880964888251,35.6282232474624));
#21946=CARTESIAN_POINT('Ctrl Pts',(3.02653868850251,1.10739740513477,35.6274787377006));
#21947=CARTESIAN_POINT('Ctrl Pts',(3.0568196732153,1.0236610669434,35.6220530591413));
#21948=CARTESIAN_POINT('Ctrl Pts',(3.08037192600609,0.95044167935542,35.6175107525742));
#21949=CARTESIAN_POINT('Ctrl Pts',(3.11097997869764,0.842135496686508,35.6109890728551));
#21950=CARTESIAN_POINT('Ctrl Pts',(3.12010599606352,0.807667834496542,35.6089422944302));
#21951=CARTESIAN_POINT('Ctrl Pts',(3.19099536871426,0.520768915049164,35.5920907939819));
#21952=CARTESIAN_POINT('Ctrl Pts',(3.22258956834844,0.26187146746877,35.5779830578411));
#21953=CARTESIAN_POINT('Ctrl Pts',(3.22277045874783,-0.0322773699741125,
35.5610272103996));
#21954=CARTESIAN_POINT('Ctrl Pts',(3.22224523984713,-0.066533945178146,
35.5590399266099));
#21955=CARTESIAN_POINT('Ctrl Pts',(3.21890748730524,-0.173222058847471,
35.5528027301262));
#21956=CARTESIAN_POINT('Ctrl Pts',(3.21419767276895,-0.245567538508346,
35.5485036776561));
#21957=CARTESIAN_POINT('Ctrl Pts',(3.20514311002084,-0.33697288876932,35.5429577596319));
#21958=CARTESIAN_POINT('Ctrl Pts',(3.20305899040129,-0.356238911551028,
35.541782396898));
#21959=CARTESIAN_POINT('Ctrl Pts',(3.19946716450695,-0.386857263082903,
35.5399037846077));
#21960=CARTESIAN_POINT('Ctrl Pts',(3.1980724597936,-0.398222570088934,35.5392041122974));
#21961=CARTESIAN_POINT('Ctrl Pts',(3.19535127629391,-0.419460375111782,
35.537892182604));
#21962=CARTESIAN_POINT('Ctrl Pts',(3.19403953329945,-0.429334649629104,
35.5372803993823));
#21963=CARTESIAN_POINT('Ctrl Pts',(3.19101107114512,-0.451349357235508,
35.5359123039807));
#21964=CARTESIAN_POINT('Ctrl Pts',(3.18927080993015,-0.463486345758742,
35.5351552527041));
#21965=CARTESIAN_POINT('Ctrl Pts',(3.18396657084568,-0.499034276468238,
35.5329295583531));
#21966=CARTESIAN_POINT('Ctrl Pts',(3.18021382781233,-0.52241582519382,35.5314549444777));
#21967=CARTESIAN_POINT('Ctrl Pts',(3.14448045485697,-0.730378754707215,
35.5182414144364));
#21968=CARTESIAN_POINT('Ctrl Pts',(3.09672586591152,-0.911854036969413,
35.505990195684));
#21969=CARTESIAN_POINT('Ctrl Pts',(2.9656460481618,-1.27727914256669,35.4799597309547));
#21970=CARTESIAN_POINT('Ctrl Pts',(2.88025696302375,-1.45966344587103,35.466189726902));
#21971=CARTESIAN_POINT('Ctrl Pts',(2.73622269328183,-1.70474207114958,35.4473403881831));
#21972=CARTESIAN_POINT('Ctrl Pts',(2.69123067814493,-1.77491978094744,35.4419040066358));
#21973=CARTESIAN_POINT('Ctrl Pts',(2.63578119894601,-1.85444337392499,35.4357656432674));
#21974=CARTESIAN_POINT('Ctrl Pts',(2.62792686323624,-1.86555706765961,35.4349083201578));
#21975=CARTESIAN_POINT('Ctrl Pts',(2.61592162305662,-1.88231791459035,35.4336165957597));
#21976=CARTESIAN_POINT('Ctrl Pts',(2.6118224261631,-1.88800166471346,35.4331787764034));
#21977=CARTESIAN_POINT('Ctrl Pts',(2.6044269530751,-1.89818569295259,35.4323947565128));
#21978=CARTESIAN_POINT('Ctrl Pts',(2.60113751873638,-1.90269080224331,35.4320480952229));
#21979=CARTESIAN_POINT('Ctrl Pts',(2.59395485720042,-1.91247451749451,35.4312956204062));
#21980=CARTESIAN_POINT('Ctrl Pts',(2.5900572199996,-1.91774976996398,35.4308901207858));
#21981=CARTESIAN_POINT('Ctrl Pts',(2.579034956004,-1.93257294270851,35.4297512096261));
#21982=CARTESIAN_POINT('Ctrl Pts',(2.57187336579427,-1.94209342818767,35.4290203320154));
#21983=CARTESIAN_POINT('Ctrl Pts',(2.52804589648987,-1.99968924852045,35.4246010107285));
#21984=CARTESIAN_POINT('Ctrl Pts',(2.49008323391232,-2.04676811675291,35.4209981831955));
#21985=CARTESIAN_POINT('Ctrl Pts',(2.28489354975244,-2.28706488110814,35.40249454867));
#21986=CARTESIAN_POINT('Ctrl Pts',(2.09643850884567,-2.46097052873984,35.3886395806164));
#21987=CARTESIAN_POINT('Ctrl Pts',(1.76143196867848,-2.70341046135735,35.3652458027176));
#21988=CARTESIAN_POINT('Ctrl Pts',(1.62684207387483,-2.78647554838319,35.356126270503));
#21989=CARTESIAN_POINT('Ctrl Pts',(1.467387265963,-2.86938439405468,35.3453154817556));
#21990=CARTESIAN_POINT('Ctrl Pts',(1.44795700712991,-2.87923820809416,35.3439983244115));
#21991=CARTESIAN_POINT('Ctrl Pts',(1.41672087715647,-2.89468307490204,35.3418804623409));
#21992=CARTESIAN_POINT('Ctrl Pts',(1.40497811468858,-2.90040077183462,35.3410841959532));
#21993=CARTESIAN_POINT('Ctrl Pts',(1.38411443619748,-2.91040312218429,35.339669150958));
#21994=CARTESIAN_POINT('Ctrl Pts',(1.37500751912376,-2.91471669717657,35.3390513897142));
#21995=CARTESIAN_POINT('Ctrl Pts',(1.3560369876221,-2.92359357021239,35.3377642617047));
#21996=CARTESIAN_POINT('Ctrl Pts',(1.34617023405761,-2.92814982060188,35.3370946603137));
#21997=CARTESIAN_POINT('Ctrl Pts',(1.32058308736153,-2.93980874357326,35.3353577093626));
#21998=CARTESIAN_POINT('Ctrl Pts',(1.30482853168874,-2.94683518773189,35.3342877496162));
#21999=CARTESIAN_POINT('Ctrl Pts',(1.23698173352815,-2.9764437312877,35.3296773755474));
#22000=CARTESIAN_POINT('Ctrl Pts',(1.18435676770846,-2.99777241964207,35.3260945593449));
#22001=CARTESIAN_POINT('Ctrl Pts',(1.04366031753545,-3.05051313782734,35.3164915764213));
#22002=CARTESIAN_POINT('Ctrl Pts',(0.954743117662606,-3.07949999194473,
35.3103969897814));
#22003=CARTESIAN_POINT('Ctrl Pts',(0.656845778650454,-3.16247139270354,
35.2899247795844));
#22004=CARTESIAN_POINT('Ctrl Pts',(0.443710345811826,-3.199340739048,35.2751505480742));
#22005=CARTESIAN_POINT('Ctrl Pts',(0.113232386153195,-3.22283315364041,
35.2529448366808));
#22006=CARTESIAN_POINT('Ctrl Pts',(-0.00242276030634944,-3.22482174519131,
35.2453152469946));
#22007=CARTESIAN_POINT('Ctrl Pts',(-0.132683918455096,-3.2200512461733,
35.2370526009332));
#22008=CARTESIAN_POINT('Ctrl Pts',(-0.147417957322412,-3.21941035215556,
35.2361228164553));
#22009=CARTESIAN_POINT('Ctrl Pts',(-0.169284399981222,-3.21830878263779,
35.2347506128558));
#22010=CARTESIAN_POINT('Ctrl Pts',(-0.176420262156259,-3.21792549974631,
35.2343040230992));
#22011=CARTESIAN_POINT('Ctrl Pts',(-0.189134577961852,-3.21720016603975,
35.2335105456669));
#22012=CARTESIAN_POINT('Ctrl Pts',(-0.194713460213433,-3.21686733749034,
35.2331631481637));
#22013=CARTESIAN_POINT('Ctrl Pts',(-0.206736929684483,-3.21611864022215,
35.2324161189759));
#22014=CARTESIAN_POINT('Ctrl Pts',(-0.213181122619191,-3.2156979144143,
35.2320167632884));
#22015=CARTESIAN_POINT('Ctrl Pts',(-0.23104695915257,-3.21447755572762,
35.2309123357424));
#22016=CARTESIAN_POINT('Ctrl Pts',(-0.242465805131233,-3.21363641318313,
35.2302095577113));
#22017=CARTESIAN_POINT('Ctrl Pts',(-0.30647150506476,-3.20857848651103,
35.2262865344371));
#22018=CARTESIAN_POINT('Ctrl Pts',(-0.358956472586155,-3.20313154328421,
35.2231311068008));
#22019=CARTESIAN_POINT('Ctrl Pts',(-0.665949292365562,-3.16363011399075,
35.2049125407654));
#22020=CARTESIAN_POINT('Ctrl Pts',(-0.915807722760667,-3.10054341059219,
35.1909852445635));
#22021=CARTESIAN_POINT('Ctrl Pts',(-1.2646773558253,-2.96654253713258,35.1698817324028));
#22022=CARTESIAN_POINT('Ctrl Pts',(-1.37140074843424,-2.91873648247267,
35.1631909462925));
#22023=CARTESIAN_POINT('Ctrl Pts',(-1.4752555264658,-2.86526415782771,35.1563175586878));
#22024=CARTESIAN_POINT('',(3.22274857165764,-0.00244669484556194,35.3125278845694));
#22025=CARTESIAN_POINT('Ctrl Pts',(-1.47525540445791,-2.86526422064663,
34.9063554765866));
#22026=CARTESIAN_POINT('Ctrl Pts',(-1.45292930620259,-2.87675938987894,
34.9077663722593));
#22027=CARTESIAN_POINT('Ctrl Pts',(-1.43046239099383,-2.88799693977385,
34.9091808614218));
#22028=CARTESIAN_POINT('Ctrl Pts',(-1.26043613777036,-2.97056855777938,
34.9198572862357));
#22029=CARTESIAN_POINT('Ctrl Pts',(-1.10778616152534,-3.03080454484676,
34.9293011572805));
#22030=CARTESIAN_POINT('Ctrl Pts',(-0.930291869104101,-3.08563686439293,
34.9404746320225));
#22031=CARTESIAN_POINT('Ctrl Pts',(-0.909288411363604,-3.09189139027313,
34.9417994740626));
#22032=CARTESIAN_POINT('Ctrl Pts',(-0.875634271945152,-3.10154053545866,
34.9439272088911));
#22033=CARTESIAN_POINT('Ctrl Pts',(-0.863023620240147,-3.10507315441357,
34.9447255949124));
#22034=CARTESIAN_POINT('Ctrl Pts',(-0.840669612786261,-3.11118848065654,
34.9461429166753));
#22035=CARTESIAN_POINT('Ctrl Pts',(-0.830934958741308,-3.11380253881126,
34.9467608223501));
#22036=CARTESIAN_POINT('Ctrl Pts',(-0.810699682232674,-3.11913469368569,
34.9480467632726));
#22037=CARTESIAN_POINT('Ctrl Pts',(-0.800197293731507,-3.12184552766872,
34.9487150255927));
#22038=CARTESIAN_POINT('Ctrl Pts',(-0.773040014159932,-3.12870921128487,
34.9504452971621));
#22039=CARTESIAN_POINT('Ctrl Pts',(-0.756365435618884,-3.13278207057212,
34.9515098804302));
#22040=CARTESIAN_POINT('Ctrl Pts',(-0.685127757610212,-3.14958037949171,
34.9560679076935));
#22041=CARTESIAN_POINT('Ctrl Pts',(-0.630273073406979,-3.16101436698318,
34.9596025745661));
#22042=CARTESIAN_POINT('Ctrl Pts',(-0.484851301103759,-3.18739063269344,
34.9690444199729));
#22043=CARTESIAN_POINT('Ctrl Pts',(-0.39390078102764,-3.19990304455322,
34.9750229661058));
#22044=CARTESIAN_POINT('Ctrl Pts',(-0.0691548172338245,-3.23052492976057,
34.9965997093589));
#22045=CARTESIAN_POINT('Ctrl Pts',(0.165917127999895,-3.22700031323257,
35.0126988713293));
#22046=CARTESIAN_POINT('Ctrl Pts',(0.418350219005723,-3.19554380295184,
35.0296712679666));
#22047=CARTESIAN_POINT('Ctrl Pts',(0.438162186753174,-3.19288756849992,
35.0310006946464));
#22048=CARTESIAN_POINT('Ctrl Pts',(0.538410711821889,-3.17849635255725,
35.0377104753343));
#22049=CARTESIAN_POINT('Ctrl Pts',(0.618415001021133,-3.16390431477802,
35.0430099104089));
#22050=CARTESIAN_POINT('Ctrl Pts',(0.710989412689877,-3.14337310041445,
35.0490132261124));
#22051=CARTESIAN_POINT('Ctrl Pts',(0.724171874476634,-3.14036232060865,
35.0498649965779));
#22052=CARTESIAN_POINT('Ctrl Pts',(0.744137358248051,-3.1356699409744,35.0511499399372));
#22053=CARTESIAN_POINT('Ctrl Pts',(0.750934309816619,-3.13404914626411,
35.0515864797157));
#22054=CARTESIAN_POINT('Ctrl Pts',(0.763144882370624,-3.13109542068199,
35.0523690271339));
#22055=CARTESIAN_POINT('Ctrl Pts',(0.768560335508649,-3.12977054383343,
35.0527154888963));
#22056=CARTESIAN_POINT('Ctrl Pts',(0.780350562240213,-3.12685364745952,
35.0534684685532));
#22057=CARTESIAN_POINT('Ctrl Pts',(0.786723894018734,-3.12525618934163,
35.0538746676402));
#22058=CARTESIAN_POINT('Ctrl Pts',(0.80469689099108,-3.12069284333201,35.0550179272153));
#22059=CARTESIAN_POINT('Ctrl Pts',(0.816285121816515,-3.11768175398948,
35.0557524216429));
#22060=CARTESIAN_POINT('Ctrl Pts',(0.887394488285968,-3.09878101651963,
35.060244858625));
#22061=CARTESIAN_POINT('Ctrl Pts',(0.946471035216613,-3.0812508002563,35.063913850737));
#22062=CARTESIAN_POINT('Ctrl Pts',(1.25864133498492,-2.97879114230051,35.0831396542036));
#22063=CARTESIAN_POINT('Ctrl Pts',(1.50096483369849,-2.86435117756486,35.0975670168958));
#22064=CARTESIAN_POINT('Ctrl Pts',(1.84950045737443,-2.64323899408243,35.120997180681));
#22065=CARTESIAN_POINT('Ctrl Pts',(1.96713019752114,-2.55690344213947,35.1294438775362));
#22066=CARTESIAN_POINT('Ctrl Pts',(2.09496623624399,-2.44901979951021,35.1395081131937));
#22067=CARTESIAN_POINT('Ctrl Pts',(2.11128724137151,-2.43496358479719,35.1408105703398));
#22068=CARTESIAN_POINT('Ctrl Pts',(2.13722039559061,-2.41217229639306,35.1429091243416));
#22069=CARTESIAN_POINT('Ctrl Pts',(2.14692294891978,-2.40354073201732,35.1437009098924));
#22070=CARTESIAN_POINT('Ctrl Pts',(2.16405060814628,-2.38811720508672,35.1451106139376));
#22071=CARTESIAN_POINT('Ctrl Pts',(2.1714966111556,-2.38134862713143,35.1457275392704));
#22072=CARTESIAN_POINT('Ctrl Pts',(2.18577929560792,-2.36824266797561,35.14691885616));
#22073=CARTESIAN_POINT('Ctrl Pts',(2.19262042788094,-2.36191026921959,35.1474930313998));
#22074=CARTESIAN_POINT('Ctrl Pts',(2.21046113508075,-2.34525195816643,35.1489998132359));
#22075=CARTESIAN_POINT('Ctrl Pts',(2.22141574557196,-2.33487842292567,35.1499344685525));
#22076=CARTESIAN_POINT('Ctrl Pts',(2.26262368632985,-2.29530380858307,35.1534867380244));
#22077=CARTESIAN_POINT('Ctrl Pts',(2.29237629209639,-2.2655895888391,35.1561267090831));
#22078=CARTESIAN_POINT('Ctrl Pts',(2.36498724047232,-2.19017740471364,35.1627633713943));
#22079=CARTESIAN_POINT('Ctrl Pts',(2.40710902354072,-2.14379733402282,35.1667898613596));
#22080=CARTESIAN_POINT('Ctrl Pts',(2.52683000432368,-2.00399387390788,35.1787689156205));
#22081=CARTESIAN_POINT('Ctrl Pts',(2.60052735404878,-1.9073841069181,35.1868540777386));
#22082=CARTESIAN_POINT('Ctrl Pts',(2.80829628852151,-1.60052450429051,35.2118120830906));
#22083=CARTESIAN_POINT('Ctrl Pts',(2.92360460029175,-1.37867950457497,35.2289539029287));
#22084=CARTESIAN_POINT('Ctrl Pts',(3.01975798738673,-1.12589116364772,35.2462198111673));
#22085=CARTESIAN_POINT('Ctrl Pts',(3.02711712655888,-1.1059526089785,35.2475666645863));
#22086=CARTESIAN_POINT('Ctrl Pts',(3.03715400392429,-1.07790812734312,35.2494387003354));
#22087=CARTESIAN_POINT('Ctrl Pts',(3.03999741382545,-1.06986265586188,35.2499731902159));
#22088=CARTESIAN_POINT('Ctrl Pts',(3.04453383113319,-1.05686267995059,35.250832584171));
#22089=CARTESIAN_POINT('Ctrl Pts',(3.04624675537791,-1.05191524348307,35.2511586578931));
#22090=CARTESIAN_POINT('Ctrl Pts',(3.0498223232361,-1.04150595757504,35.2518426002686));
#22091=CARTESIAN_POINT('Ctrl Pts',(3.05168236362497,-1.03604324970668,35.2522003070227));
#22092=CARTESIAN_POINT('Ctrl Pts',(3.05618729722679,-1.02269542692598,35.2530714324032));
#22093=CARTESIAN_POINT('Ctrl Pts',(3.05881638239471,-1.01480494401201,35.2535839185662));
#22094=CARTESIAN_POINT('Ctrl Pts',(3.06812182888641,-0.98651245021176,35.2554129612008));
#22095=CARTESIAN_POINT('Ctrl Pts',(3.07462502953678,-0.966053495529832,
35.2567196951894));
#22096=CARTESIAN_POINT('Ctrl Pts',(3.11354420921741,-0.839238949451706,
35.264730398011));
#22097=CARTESIAN_POINT('Ctrl Pts',(3.14064605225898,-0.73131878439612,35.2711631847051));
#22098=CARTESIAN_POINT('Ctrl Pts',(3.20228605224234,-0.418056310754366,
35.2892997880465));
#22099=CARTESIAN_POINT('Ctrl Pts',(3.22259086965953,-0.210506202816104,
35.3006989395904));
#22100=CARTESIAN_POINT('Ctrl Pts',(3.2227490683711,-0.00245047203661506,
35.3125268034609));
#22101=CARTESIAN_POINT('Ctrl Pts',(3.22274907127793,-0.00244664611808667,
35.3125270209625));
#22102=CARTESIAN_POINT('Ctrl Pts',(3.222822198994,0.0938779826516697,35.3180030298239));
#22103=CARTESIAN_POINT('Ctrl Pts',(3.2185767818221,0.190152796939803,35.3235561489518));
#22104=CARTESIAN_POINT('Ctrl Pts',(3.20588205807585,0.332591966317148,35.3319873302714));
#22105=CARTESIAN_POINT('Ctrl Pts',(3.20072779093437,0.378996656346596,35.3347679097327));
#22106=CARTESIAN_POINT('Ctrl Pts',(3.19245693920111,0.441125918843006,35.3385432245935));
#22107=CARTESIAN_POINT('Ctrl Pts',(3.19022835540884,0.456964343398726,35.3395102459607));
#22108=CARTESIAN_POINT('Ctrl Pts',(3.18626032428469,0.483719859681448,35.3411518760625));
#22109=CARTESIAN_POINT('Ctrl Pts',(3.18458242116393,0.494645888305743,35.3418245401713));
#22110=CARTESIAN_POINT('Ctrl Pts',(3.18138073222578,0.514802606888697,35.343069798848));
#22111=CARTESIAN_POINT('Ctrl Pts',(3.17987289518586,0.524035738267946,35.3436418822315));
#22112=CARTESIAN_POINT('Ctrl Pts',(3.17667380192803,0.543102830753287,35.3448267903223));
#22113=CARTESIAN_POINT('Ctrl Pts',(3.17497703570969,0.552935753749137,35.3454397847159));
#22114=CARTESIAN_POINT('Ctrl Pts',(3.17104917621089,0.575083752271063,35.3468249504617));
#22115=CARTESIAN_POINT('Ctrl Pts',(3.16879196380773,0.587393976037243,35.347597947873));
#22116=CARTESIAN_POINT('Ctrl Pts',(3.16283206722838,0.61886319151895,35.3495820765352));
#22117=CARTESIAN_POINT('Ctrl Pts',(3.15902701529105,0.63800205714112,35.3507964632919));
#22118=CARTESIAN_POINT('Ctrl Pts',(3.13493297705785,0.753688096794359,35.3581845259994));
#22119=CARTESIAN_POINT('Ctrl Pts',(3.11039519341025,0.849287276382102,35.3644936335693));
#22120=CARTESIAN_POINT('Ctrl Pts',(3.06261102411507,1.00533551957057,35.3751383797574));
#22121=CARTESIAN_POINT('Ctrl Pts',(3.0418578526508,1.06648292520211,35.379399773773));
#22122=CARTESIAN_POINT('Ctrl Pts',(2.94398912463826,1.32868619866432,35.3980416007017));
#22123=CARTESIAN_POINT('Ctrl Pts',(2.84867416605034,1.52234281914099,35.4128122584179));
#22124=CARTESIAN_POINT('Ctrl Pts',(2.68796576556024,1.78010743066332,35.4330477547681));
#22125=CARTESIAN_POINT('Ctrl Pts',(2.63809033463233,1.85322009616731,35.4388531537061));
#22126=CARTESIAN_POINT('Ctrl Pts',(2.5738869008461,1.93948110285755,35.4457007292539));
#22127=CARTESIAN_POINT('Ctrl Pts',(2.5623729990046,1.9546675885902,35.4469061530209));
#22128=CARTESIAN_POINT('Ctrl Pts',(2.54587837315102,1.97602726308972,35.4486003580822));
#22129=CARTESIAN_POINT('Ctrl Pts',(2.54100879890514,1.98228522730869,35.449096577208));
#22130=CARTESIAN_POINT('Ctrl Pts',(2.53260068933571,1.99300872320809,35.4499465348641));
#22131=CARTESIAN_POINT('Ctrl Pts',(2.5290733341092,1.99748293987475,35.4503010600482));
#22132=CARTESIAN_POINT('Ctrl Pts',(2.52222693279569,2.00611993793479,35.4509851924609));
#22133=CARTESIAN_POINT('Ctrl Pts',(2.51890943473924,2.01028385221078,35.4513149097283));
#22134=CARTESIAN_POINT('Ctrl Pts',(2.50996017443316,2.02145946404088,35.4521996216935));
#22135=CARTESIAN_POINT('Ctrl Pts',(2.50430930530922,2.02845590286812,35.4527532546306));
#22136=CARTESIAN_POINT('Ctrl Pts',(2.4833899848165,2.05413581198401,35.454784834301));
#22137=CARTESIAN_POINT('Ctrl Pts',(2.46794069348604,2.07267184186707,35.4562502916358));
#22138=CARTESIAN_POINT('Ctrl Pts',(2.32053141693219,2.24554782791318,35.469927795437));
#22139=CARTESIAN_POINT('Ctrl Pts',(2.17445047837928,2.38728703534737,35.4812353044151));
#22140=CARTESIAN_POINT('Ctrl Pts',(1.88435771502452,2.61988086240072,35.5020094141611));
#22141=CARTESIAN_POINT('Ctrl Pts',(1.74465664835936,2.71491207884529,35.5114319292465));
#22142=CARTESIAN_POINT('Ctrl Pts',(1.5464281871252,2.82811377439754,35.5246682146053));
#22143=CARTESIAN_POINT('Ctrl Pts',(1.4938808924124,2.85621898990891,35.5281632300493));
#22144=CARTESIAN_POINT('Ctrl Pts',(1.41606868102879,2.89510246998893,35.5333379420563));
#22145=CARTESIAN_POINT('Ctrl Pts',(1.3913956644315,2.90704091091488,35.5349786056314));
#22146=CARTESIAN_POINT('Ctrl Pts',(1.34675667191248,2.92794174274711,35.5379484416452));
#22147=CARTESIAN_POINT('Ctrl Pts',(1.32684582374589,2.93701830193329,35.5392736405939));
#22148=CARTESIAN_POINT('Ctrl Pts',(1.29603469935726,2.95068660944577,35.541325790494));
#22149=CARTESIAN_POINT('Ctrl Pts',(1.28519874229726,2.9554224056854,35.5420477859514));
#22150=CARTESIAN_POINT('Ctrl Pts',(1.26608673208441,2.96365022108519,35.5433217974865));
#22151=CARTESIAN_POINT('Ctrl Pts',(1.25782164012358,2.96716749866542,35.5438729422159));
#22152=CARTESIAN_POINT('Ctrl Pts',(1.23917063255296,2.97501265594226,35.5451171384687));
#22153=CARTESIAN_POINT('Ctrl Pts',(1.22877657943962,2.97932077364512,35.5458108548017));
#22154=CARTESIAN_POINT('Ctrl Pts',(1.20077530730874,2.9907552592962,35.5476807175804));
#22155=CARTESIAN_POINT('Ctrl Pts',(1.18312750074961,2.99778045421981,35.5488602712433));
#22156=CARTESIAN_POINT('Ctrl Pts',(1.10360230784894,3.02862604087624,35.5541811551656));
#22157=CARTESIAN_POINT('Ctrl Pts',(1.0410645080087,3.05068801941584,35.5583808882861));
#22158=CARTESIAN_POINT('Ctrl Pts',(0.670324953753376,3.16874962926328,35.5833851699237));
#22159=CARTESIAN_POINT('Ctrl Pts',(0.349804969398493,3.21991791190272,35.6056886694998));
#22160=CARTESIAN_POINT('Ctrl Pts',(-0.0350210707554559,3.22315930273634,
35.6312791652481));
#22161=CARTESIAN_POINT('Ctrl Pts',(-0.0971925808733141,3.22188406580124,
35.6353675708624));
#22162=CARTESIAN_POINT('Ctrl Pts',(-0.182893561452371,3.21764291224097,
35.6409071917649));
#22163=CARTESIAN_POINT('Ctrl Pts',(-0.206482432798357,3.21621532886052,
35.6424218546974));
#22164=CARTESIAN_POINT('Ctrl Pts',(-0.247231118304599,3.21329906704435,
35.6450184917643));
#22165=CARTESIAN_POINT('Ctrl Pts',(-0.264398353381229,3.21193207610899,
35.646106333131));
#22166=CARTESIAN_POINT('Ctrl Pts',(-0.289135386438601,3.20976264022414,
35.6476642406725));
#22167=CARTESIAN_POINT('Ctrl Pts',(-0.296714242463301,3.20907091529585,
35.6481402449312));
#22168=CARTESIAN_POINT('Ctrl Pts',(-0.309910016238329,3.20781938479212,
35.6489666766877));
#22169=CARTESIAN_POINT('Ctrl Pts',(-0.31552801204594,3.2072716597146,35.6493177779765));
#22170=CARTESIAN_POINT('Ctrl Pts',(-0.327307768498945,3.20609194379902,
35.6500523711005));
#22171=CARTESIAN_POINT('Ctrl Pts',(-0.333469149909224,3.20545694948554,
35.6504356918027));
#22172=CARTESIAN_POINT('Ctrl Pts',(-0.349836035200082,3.20372247086048,
35.6514516121746));
#22173=CARTESIAN_POINT('Ctrl Pts',(-0.360038282121318,3.20259197586956,
35.6520824847972));
#22174=CARTESIAN_POINT('Ctrl Pts',(-0.40367289845304,3.19754574518788,35.6547711014066));
#22175=CARTESIAN_POINT('Ctrl Pts',(-0.437049586291402,3.19315493961492,
35.6568035218393));
#22176=CARTESIAN_POINT('Ctrl Pts',(-0.476615547774752,3.18731787825588,
35.6591906079939));
#22177=CARTESIAN_POINT('Ctrl Pts',(-0.482875551191465,3.1863755021517,35.6595676223802));
#22178=CARTESIAN_POINT('Ctrl Pts',(-0.78807014476277,3.13951168803674,35.6779176620613));
#22179=CARTESIAN_POINT('Ctrl Pts',(-1.07909311969837,3.05175323564138,35.6941078273691));
#22180=CARTESIAN_POINT('Ctrl Pts',(-1.43660826328232,2.88628354462794,35.7165410559189));
#22181=CARTESIAN_POINT('Ctrl Pts',(-1.51789998880267,2.84437228964257,35.7218192810321));
#22182=CARTESIAN_POINT('Ctrl Pts',(-1.64582570326363,2.77137102702872,35.7305055138283));
#22183=CARTESIAN_POINT('Ctrl Pts',(-1.69362443773071,2.74242143171488,35.7338409247734));
#22184=CARTESIAN_POINT('Ctrl Pts',(-1.7550761634918,2.70298340343429,35.7382595874149));
#22185=CARTESIAN_POINT('Ctrl Pts',(-1.76943349387717,2.69360663645655,35.7393014896748));
#22186=CARTESIAN_POINT('Ctrl Pts',(-1.79274581969509,2.67811455287119,35.7410092249677));
#22187=CARTESIAN_POINT('Ctrl Pts',(-1.80174611087036,2.67206775358597,35.7416724710425));
#22188=CARTESIAN_POINT('Ctrl Pts',(-1.81905491081398,2.66031171451251,35.7429556837871));
#22189=CARTESIAN_POINT('Ctrl Pts',(-1.82736749378812,2.65460867660189,35.7435754096296));
#22190=CARTESIAN_POINT('Ctrl Pts',(-1.8464241598826,2.64140249025563,35.745004193069));
#22191=CARTESIAN_POINT('Ctrl Pts',(-1.85714945377346,2.63387266053652,35.7458142669076));
#22192=CARTESIAN_POINT('Ctrl Pts',(-1.88571089358673,2.6135595504263,35.7479876068367));
#22193=CARTESIAN_POINT('Ctrl Pts',(-1.90346265497794,2.60065933571649,35.7493553731951));
#22194=CARTESIAN_POINT('Ctrl Pts',(-2.05259145839286,2.48994252587534,35.7609923150584));
#22195=CARTESIAN_POINT('Ctrl Pts',(-2.17644666712245,2.38243797731905,35.7716483608506));
#22196=CARTESIAN_POINT('Ctrl Pts',(-2.47009394478667,2.0854759631843,35.7995028679659));
#22197=CARTESIAN_POINT('Ctrl Pts',(-2.62663991601537,1.8844978151653,35.8170272932151));
#22198=CARTESIAN_POINT('Ctrl Pts',(-2.78717237984905,1.61894177903155,35.8373288032252));
#22199=CARTESIAN_POINT('Ctrl Pts',(-2.81509616944046,1.56988433892823,35.8409682944937));
#22200=CARTESIAN_POINT('Ctrl Pts',(-2.84722706337797,1.50981852463014,35.8452700206613));
#22201=CARTESIAN_POINT('Ctrl Pts',(-2.8526792567236,1.49949157912259,35.8460041995074));
#22202=CARTESIAN_POINT('Ctrl Pts',(-2.86108165915521,1.48336496995739,35.8471420350367));
#22203=CARTESIAN_POINT('Ctrl Pts',(-2.86407057471238,1.47758574685005,35.8475480744458));
#22204=CARTESIAN_POINT('Ctrl Pts',(-2.86959073405829,1.46683254934182,35.8483003279048));
#22205=CARTESIAN_POINT('Ctrl Pts',(-2.87212653543665,1.46186109940702,35.8486468205337));
#22206=CARTESIAN_POINT('Ctrl Pts',(-2.87784626086216,1.45057521985763,35.8494305058163));
#22207=CARTESIAN_POINT('Ctrl Pts',(-2.88102231595407,1.44425689780227,35.8498672014981));
#22208=CARTESIAN_POINT('Ctrl Pts',(-2.89038546486611,1.42547641484685,35.8511593211402));
#22209=CARTESIAN_POINT('Ctrl Pts',(-2.89651277506788,1.41298439653568,35.8520110931471));
#22210=CARTESIAN_POINT('Ctrl Pts',(-2.94236488448253,1.31795195014025,35.8584356891103));
#22211=CARTESIAN_POINT('Ctrl Pts',(-2.97863920195295,1.23378293082401,35.8638116284189));
#22212=CARTESIAN_POINT('Ctrl Pts',(-3.09796907748042,0.920820293972021,
35.8830722180209));
#22213=CARTESIAN_POINT('Ctrl Pts',(-3.15863409748303,0.684372923629414,
35.896298481329));
#22214=CARTESIAN_POINT('Ctrl Pts',(-3.20474754755038,0.352348715279247,
35.9153828810517));
#22215=CARTESIAN_POINT('Ctrl Pts',(-3.21348774603249,0.260865942913228,
35.9206853786294));
#22216=CARTESIAN_POINT('Ctrl Pts',(-3.22125103730935,0.113149652394659,
35.9294079034964));
#22217=CARTESIAN_POINT('Ctrl Pts',(-3.22273185991701,0.0570952960618219,
35.9327545369201));
#22218=CARTESIAN_POINT('Ctrl Pts',(-3.22275533909513,-0.0161359277741507,
35.9371859942254));
#22219=CARTESIAN_POINT('Ctrl Pts',(-3.22262364041845,-0.0333046288324061,
35.9382291637872));
#22220=CARTESIAN_POINT('Ctrl Pts',(-3.22218487970022,-0.0613174874208513,
35.9399384538424));
#22221=CARTESIAN_POINT('Ctrl Pts',(-3.22196023686762,-0.0721627377965504,
35.9406019782694));
#22222=CARTESIAN_POINT('Ctrl Pts',(-3.22142124196038,-0.0930824086395146,
35.9418853624112));
#22223=CARTESIAN_POINT('Ctrl Pts',(-3.2211143726453,-0.10315690769907,35.9425049793255));
#22224=CARTESIAN_POINT('Ctrl Pts',(-3.22030020351147,-0.126315525354007,
35.9439329850104));
#22225=CARTESIAN_POINT('Ctrl Pts',(-3.21976041510896,-0.139398256247839,
35.9447423864189));
#22226=CARTESIAN_POINT('Ctrl Pts',(-3.21810443471131,-0.174359777866476,
35.9469127498439));
#22227=CARTESIAN_POINT('Ctrl Pts',(-3.21684487112074,-0.196230786862113,
35.948278192795));
#22228=CARTESIAN_POINT('Ctrl Pts',(-3.20426121056356,-0.381757946721685,
35.9599284392866));
#22229=CARTESIAN_POINT('Ctrl Pts',(-3.18068132286312,-0.544316657537262,
35.9706014164879));
#22230=CARTESIAN_POINT('Ctrl Pts',(-3.0892667155855,-0.952469482132061,
35.998499587124));
#22231=CARTESIAN_POINT('Ctrl Pts',(-3.00453278854938,-1.19312402986472,
36.0160512963132));
#22232=CARTESIAN_POINT('Ctrl Pts',(-2.86773749741407,-1.47150484730143,
36.0363383813135));
#22233=CARTESIAN_POINT('Ctrl Pts',(-2.84177029808648,-1.52104810623624,
36.0399440790494));
#22234=CARTESIAN_POINT('Ctrl Pts',(-2.80885164644733,-1.58006507235858,
36.0442113504063));
#22235=CARTESIAN_POINT('Ctrl Pts',(-2.8031230808684,-1.59020571245238,36.0449435571804));
#22236=CARTESIAN_POINT('Ctrl Pts',(-2.79411210041919,-1.60595684151635,
36.0460790076063));
#22237=CARTESIAN_POINT('Ctrl Pts',(-2.7908675420878,-1.61158871019074,36.0464846181944));
#22238=CARTESIAN_POINT('Ctrl Pts',(-2.78480502505577,-1.62203874467475,
36.0472364846307));
#22239=CARTESIAN_POINT('Ctrl Pts',(-2.78199161484652,-1.62685935852861,
36.0475830165017));
#22240=CARTESIAN_POINT('Ctrl Pts',(-2.77558059952186,-1.63777899505023,
36.0483673095912));
#22241=CARTESIAN_POINT('Ctrl Pts',(-2.77197541752484,-1.64387347079022,
36.0488045706096));
#22242=CARTESIAN_POINT('Ctrl Pts',(-2.76120457265491,-1.66194514565416,
36.0500999161951));
#22243=CARTESIAN_POINT('Ctrl Pts',(-2.75398105038895,-1.67388791430352,
36.050954321706));
#22244=CARTESIAN_POINT('Ctrl Pts',(-2.69807807434776,-1.76497171935793,
36.0574610713057));
#22245=CARTESIAN_POINT('Ctrl Pts',(-2.64606923707545,-1.84202919295389,
36.0629107944885));
#22246=CARTESIAN_POINT('Ctrl Pts',(-2.44705131726415,-2.11103574983077,
36.0821409989197));
#22247=CARTESIAN_POINT('Ctrl Pts',(-2.28190073615814,-2.28855277342994,
36.0952837718125));
#22248=CARTESIAN_POINT('Ctrl Pts',(-2.02860552848562,-2.50586217024917,
36.1142829562129));
#22249=CARTESIAN_POINT('Ctrl Pts',(-1.95623474136634,-2.56275814472599,
36.119594215877));
#22250=CARTESIAN_POINT('Ctrl Pts',(-1.83595694390226,-2.6492510166241,36.1283298372918));
#22251=CARTESIAN_POINT('Ctrl Pts',(-1.78953488430647,-2.68082695623838,
36.1316805162257));
#22252=CARTESIAN_POINT('Ctrl Pts',(-1.72786376367948,-2.72045941322018,
36.1361165850886));
#22253=CARTESIAN_POINT('Ctrl Pts',(-1.71333981160578,-2.7296298791251,36.1371602105065));
#22254=CARTESIAN_POINT('Ctrl Pts',(-1.68952376613095,-2.74440243281156,
36.1388700598438));
#22255=CARTESIAN_POINT('Ctrl Pts',(-1.68027534400173,-2.75007455050425,
36.1395336844176));
#22256=CARTESIAN_POINT('Ctrl Pts',(-1.66238055990656,-2.7609255721317,36.140817130465));
#22257=CARTESIAN_POINT('Ctrl Pts',(-1.65373818681447,-2.76611083411253,
36.1414367084293));
#22258=CARTESIAN_POINT('Ctrl Pts',(-1.63381552198751,-2.77793731968781,
36.1428644354347));
#22259=CARTESIAN_POINT('Ctrl Pts',(-1.62251886347597,-2.784550491828,36.1436735958224));
#22260=CARTESIAN_POINT('Ctrl Pts',(-1.59222088829513,-2.80204024783262,
36.145842892712));
#22261=CARTESIAN_POINT('Ctrl Pts',(-1.57314875726316,-2.81279218160706,
36.1472075032309));
#22262=CARTESIAN_POINT('Ctrl Pts',(-1.52791931900792,-2.83768642883583,
36.1504420200467));
#22263=CARTESIAN_POINT('Ctrl Pts',(-1.50167885936097,-2.85165942216976,
36.1523172954271));
#22264=CARTESIAN_POINT('Ctrl Pts',(-1.47525533429856,-2.86526425676998,
36.1542047394732));
#22265=CARTESIAN_POINT('Origin',(0.,0.,4.68922655072688));
#22266=CARTESIAN_POINT('',(-1.47642198135621,-2.8675770180324,37.6538374877124));
#22267=CARTESIAN_POINT('',(-1.47525540431025,-2.86526422072265,37.4085260041042));
#22268=CARTESIAN_POINT('',(-1.47525540501186,-2.86526422036142,4.68922655072688));
#22269=CARTESIAN_POINT('',(3.22710931890567,0.00161487490920624,36.8107734492731));
#22270=CARTESIAN_POINT('Ctrl Pts',(3.22710931890567,0.00161487490920624,
36.8107734492731));
#22271=CARTESIAN_POINT('Ctrl Pts',(3.22766820945557,0.092902302212634,36.8164301670323));
#22272=CARTESIAN_POINT('Ctrl Pts',(3.18268013141034,1.25374923679401,36.8883978642459));
#22273=CARTESIAN_POINT('Ctrl Pts',(1.77912732379145,3.37157490318388,37.0266765409141));
#22274=CARTESIAN_POINT('Ctrl Pts',(-1.875636683147,3.31885498005365,37.2256094792775));
#22275=CARTESIAN_POINT('Ctrl Pts',(-3.806119388409,0.2150966389413,37.4245424176409));
#22276=CARTESIAN_POINT('Ctrl Pts',(-2.68065523427354,-2.1538654548464,37.5672850871192));
#22277=CARTESIAN_POINT('Ctrl Pts',(-1.62254331928945,-2.79407246625599,
37.6437167771431));
#22278=CARTESIAN_POINT('Ctrl Pts',(-1.47642198135613,-2.86757701803244,
37.6538374877124));
#22279=CARTESIAN_POINT('Ctrl Pts',(3.22274952067548,0.00175769336351857,
36.8082682062519));
#22280=CARTESIAN_POINT('Ctrl Pts',(3.22276605484594,-0.0285578844381251,
36.80650283569));
#22281=CARTESIAN_POINT('Ctrl Pts',(3.22235483219543,-0.05887312616645,36.8047522247304));
#22282=CARTESIAN_POINT('Ctrl Pts',(3.21327137318411,-0.387005561556071,
36.7859214086916));
#22283=CARTESIAN_POINT('Ctrl Pts',(3.16376992247395,-0.68224905193963,36.7698842931772));
#22284=CARTESIAN_POINT('Ctrl Pts',(3.04938585646319,-1.04609995332455,36.7476979918744));
#22285=CARTESIAN_POINT('Ctrl Pts',(3.02128342954484,-1.1246883395346,36.742763256182));
#22286=CARTESIAN_POINT('Ctrl Pts',(2.98285032186027,-1.22028936190716,36.7365420512188));
#22287=CARTESIAN_POINT('Ctrl Pts',(2.9753694133729,-1.23841794118675,36.7353524918587));
#22288=CARTESIAN_POINT('Ctrl Pts',(2.96328290429647,-1.266965558166,36.7334631611481));
#22289=CARTESIAN_POINT('Ctrl Pts',(2.95878664247503,-1.27743058344845,36.7327671204464));
#22290=CARTESIAN_POINT('Ctrl Pts',(2.95025209269912,-1.2970078992249,36.7314584368492));
#22291=CARTESIAN_POINT('Ctrl Pts',(2.94622681528071,-1.30612574068935,36.7308462461957));
#22292=CARTESIAN_POINT('Ctrl Pts',(2.93712178009111,-1.32649371637484,36.7294725934711));
#22293=CARTESIAN_POINT('Ctrl Pts',(2.93201957254121,-1.33773358711513,36.7287103643352));
#22294=CARTESIAN_POINT('Ctrl Pts',(2.91892192023341,-1.36615204620692,36.7267723867528));
#22295=CARTESIAN_POINT('Ctrl Pts',(2.91083939729689,-1.38328976290622,36.7255936367331));
#22296=CARTESIAN_POINT('Ctrl Pts',(2.86351639764259,-1.48137920989517,36.7187880237311));
#22297=CARTESIAN_POINT('Ctrl Pts',(2.82105450547159,-1.56072400536159,36.7130492195396));
#22298=CARTESIAN_POINT('Ctrl Pts',(2.63326649012482,-1.87886563895286,36.6890430908086));
#22299=CARTESIAN_POINT('Ctrl Pts',(2.46050134454939,-2.10002863479042,36.669822646677));
#22300=CARTESIAN_POINT('Ctrl Pts',(2.20945924073325,-2.34728117032595,36.6462732745994));
#22301=CARTESIAN_POINT('Ctrl Pts',(2.1557594856927,-2.39669386755196,36.6414506258617));
#22302=CARTESIAN_POINT('Ctrl Pts',(2.0804396760161,-2.46141884193578,36.6350203875209));
#22303=CARTESIAN_POINT('Ctrl Pts',(2.0602432364287,-2.47834821289421,36.6333272889481));
#22304=CARTESIAN_POINT('Ctrl Pts',(2.02986562523331,-2.50318379611761,36.6308294108307));
#22305=CARTESIAN_POINT('Ctrl Pts',(2.01984151149068,-2.51127932629666,36.6300128964112));
#22306=CARTESIAN_POINT('Ctrl Pts',(2.00160723725369,-2.52582561469292,36.6285419920877));
#22307=CARTESIAN_POINT('Ctrl Pts',(1.99341382175586,-2.5322969633083,36.6278862401827));
#22308=CARTESIAN_POINT('Ctrl Pts',(1.98027247466594,-2.54257299615543,36.6268429385855));
#22309=CARTESIAN_POINT('Ctrl Pts',(1.97534477213949,-2.54640325703751,36.62645360774));
#22310=CARTESIAN_POINT('Ctrl Pts',(1.96619282674201,-2.5534744324519,36.6257340567563));
#22311=CARTESIAN_POINT('Ctrl Pts',(1.96197172778946,-2.55671915723209,36.6254035717015));
#22312=CARTESIAN_POINT('Ctrl Pts',(1.95207787242992,-2.56428555302981,36.624632163286));
#22313=CARTESIAN_POINT('Ctrl Pts',(1.94639880479212,-2.56859886173743,36.624191832511));
#22314=CARTESIAN_POINT('Ctrl Pts',(1.92899148777409,-2.58172901126351,36.6228494776079));
#22315=CARTESIAN_POINT('Ctrl Pts',(1.91721711122963,-2.59048478375062,36.6219516327591));
#22316=CARTESIAN_POINT('Ctrl Pts',(1.75489781846419,-2.70947723984751,36.6097061108786));
#22317=CARTESIAN_POINT('Ctrl Pts',(1.59509190662659,-2.80653453996464,36.5991877727189));
#22318=CARTESIAN_POINT('Ctrl Pts',(1.2958759370638,-2.95439752107189,36.5805075949685));
#22319=CARTESIAN_POINT('Ctrl Pts',(1.15968358011756,-3.01046368765049,36.5723406741485));
#22320=CARTESIAN_POINT('Ctrl Pts',(0.932892404282599,-3.08614478306714,
36.5587297343269));
#22321=CARTESIAN_POINT('Ctrl Pts',(0.844441674176579,-3.111509952806,36.5534208244709));
#22322=CARTESIAN_POINT('Ctrl Pts',(0.700471980442569,-3.14620505278839,
36.5446884902619));
#22323=CARTESIAN_POINT('Ctrl Pts',(0.645580608867946,-3.15792532051728,
36.5413386643411));
#22324=CARTESIAN_POINT('Ctrl Pts',(0.573525407193728,-3.17135322634818,
36.536903343233));
#22325=CARTESIAN_POINT('Ctrl Pts',(0.556612567602607,-3.17436530833754,
36.5358595874755));
#22326=CARTESIAN_POINT('Ctrl Pts',(0.52897770913344,-3.17905928174248,36.5341494268078));
#22327=CARTESIAN_POINT('Ctrl Pts',(0.518269707133551,-3.18082250993434,
36.5334856213996));
#22328=CARTESIAN_POINT('Ctrl Pts',(0.497596464884699,-3.18411949787508,
36.5322017561688));
#22329=CARTESIAN_POINT('Ctrl Pts',(0.487632518424355,-3.18566064449777,
36.5315819396622));
#22330=CARTESIAN_POINT('Ctrl Pts',(0.464709565415272,-3.18909612670047,
36.5301535621975));
#22331=CARTESIAN_POINT('Ctrl Pts',(0.451745981609123,-3.19095826445369,
36.5293439885043));
#22332=CARTESIAN_POINT('Ctrl Pts',(0.417066885607546,-3.19572413789937,
36.5271733542962));
#22333=CARTESIAN_POINT('Ctrl Pts',(0.395332806374885,-3.19848549887924,
36.5258078129339));
#22334=CARTESIAN_POINT('Ctrl Pts',(0.210804253310464,-3.2200207344675,36.5141683524406));
#22335=CARTESIAN_POINT('Ctrl Pts',(0.0468498156986263,-3.22657130235436,
36.5035071245191));
#22336=CARTESIAN_POINT('Ctrl Pts',(-0.370926724992662,-3.21141096296261,
36.4756243991621));
#22337=CARTESIAN_POINT('Ctrl Pts',(-0.622986109466305,-3.17216495732823,
36.4580755360971));
#22338=CARTESIAN_POINT('Ctrl Pts',(-0.921844436026495,-3.08860298168915,
36.4377768145144));
#22339=CARTESIAN_POINT('Ctrl Pts',(-0.975479136866018,-3.07208510679403,
36.4341589201158));
#22340=CARTESIAN_POINT('Ctrl Pts',(-1.03970943635549,-3.05045206800001,
36.4298790289116));
#22341=CARTESIAN_POINT('Ctrl Pts',(-1.05073997555764,-3.04667015687418,
36.4291459310195));
#22342=CARTESIAN_POINT('Ctrl Pts',(-1.06789081565318,-3.04068562500645,
36.4280093161713));
#22343=CARTESIAN_POINT('Ctrl Pts',(-1.07402525303346,-3.03852425066817,
36.4276034256032));
#22344=CARTESIAN_POINT('Ctrl Pts',(-1.0854135811211,-3.03447295164859,36.4268511698193));
#22345=CARTESIAN_POINT('Ctrl Pts',(-1.09066905278063,-3.03258796317373,
36.4265045275812));
#22346=CARTESIAN_POINT('Ctrl Pts',(-1.10257831092685,-3.02828148707774,
36.425720142159));
#22347=CARTESIAN_POINT('Ctrl Pts',(-1.10922901640343,-3.02585172937019,
36.4252828985485));
#22348=CARTESIAN_POINT('Ctrl Pts',(-1.12895768572347,-3.01857030311774,
36.4239880705158));
#22349=CARTESIAN_POINT('Ctrl Pts',(-1.14201241672374,-3.01365555221201,
36.4231341595343));
#22350=CARTESIAN_POINT('Ctrl Pts',(-1.24129942132,-2.9755388743415,36.4166589295455));
#22351=CARTESIAN_POINT('Ctrl Pts',(-1.32610848080994,-2.93872346122117,
36.4112379686349));
#22352=CARTESIAN_POINT('Ctrl Pts',(-1.4313674177628,-2.8875441186618,36.4045101853076));
#22353=CARTESIAN_POINT('Ctrl Pts',(-1.45337870525942,-2.87652800565308,
36.4031033493262));
#22354=CARTESIAN_POINT('Ctrl Pts',(-1.47525545662511,-2.865264193787,36.4017031386693));
#22355=CARTESIAN_POINT('Ctrl Pts',(-1.47525533429857,-2.86526425676998,
36.1542047394732));
#22356=CARTESIAN_POINT('Ctrl Pts',(-1.35648519049259,-2.92641613405012,
36.1626885432144));
#22357=CARTESIAN_POINT('Ctrl Pts',(-1.23401696002696,-2.98012972438504,
36.171426215797));
#22358=CARTESIAN_POINT('Ctrl Pts',(-0.871056753745843,-3.11309363011468,
36.1972043428991));
#22359=CARTESIAN_POINT('Ctrl Pts',(-0.62415665607532,-3.17183152281709,
36.2146603565864));
#22360=CARTESIAN_POINT('Ctrl Pts',(-0.315582863209829,-3.20778098899618,
36.2349996513337));
#22361=CARTESIAN_POINT('Ctrl Pts',(-0.258057652374377,-3.21292057905945,
36.2387254237883));
#22362=CARTESIAN_POINT('Ctrl Pts',(-0.188689003787312,-3.21724295097161,
36.2431149691367));
#22363=CARTESIAN_POINT('Ctrl Pts',(-0.176952494959484,-3.21790981388537,
36.2438540833031));
#22364=CARTESIAN_POINT('Ctrl Pts',(-0.158697769992497,-3.21884686376737,
36.2449978860274));
#22365=CARTESIAN_POINT('Ctrl Pts',(-0.152182082262523,-3.21916149489491,
36.2454049970216));
#22366=CARTESIAN_POINT('Ctrl Pts',(-0.140091921436821,-3.21970851840367,
36.2461582237465));
#22367=CARTESIAN_POINT('Ctrl Pts',(-0.134517851565134,-3.21994621667609,
36.246504624429));
#22368=CARTESIAN_POINT('Ctrl Pts',(-0.121899983884943,-3.22045146537396,
36.2472868186752));
#22369=CARTESIAN_POINT('Ctrl Pts',(-0.114855926478386,-3.22071038208709,
36.2477221232154));
#22370=CARTESIAN_POINT('Ctrl Pts',(-0.0940122937803075,-3.2214080568381,
36.2490063209519));
#22371=CARTESIAN_POINT('Ctrl Pts',(-0.0802104780147182,-3.2217812581072,
36.249851628328));
#22372=CARTESIAN_POINT('Ctrl Pts',(0.0221298499941792,-3.22389048050423,
36.2560850492217));
#22373=CARTESIAN_POINT('Ctrl Pts',(0.110712612917276,-3.22206538514645,
36.2612892835029));
#22374=CARTESIAN_POINT('Ctrl Pts',(0.445915510658712,-3.2013154222992,36.2806307746532));
#22375=CARTESIAN_POINT('Ctrl Pts',(0.690145716217482,-3.15768500635991,
36.2940591626006));
#22376=CARTESIAN_POINT('Ctrl Pts',(1.01452756133985,-3.06026212167359,36.3133462070023));
#22377=CARTESIAN_POINT('Ctrl Pts',(1.10089540739617,-3.03026365611643,36.3186227453361));
#22378=CARTESIAN_POINT('Ctrl Pts',(1.23781003456563,-2.97608206240529,36.327306455389));
#22379=CARTESIAN_POINT('Ctrl Pts',(1.28920685994301,-2.95418063542867,36.3306410855843));
#22380=CARTESIAN_POINT('Ctrl Pts',(1.35560046236527,-2.92382608149794,36.3350588579925));
#22381=CARTESIAN_POINT('Ctrl Pts',(1.37113718712766,-2.91657236577657,36.3361006719362));
#22382=CARTESIAN_POINT('Ctrl Pts',(1.39640277016724,-2.90452998414118,36.337808298884));
#22383=CARTESIAN_POINT('Ctrl Pts',(1.40616678114284,-2.89981552936949,36.3384715255641));
#22384=CARTESIAN_POINT('Ctrl Pts',(1.42496266930354,-2.89062287066295,36.3397547264029));
#22385=CARTESIAN_POINT('Ctrl Pts',(1.43399770170545,-2.88615137806843,36.3403744598718));
#22386=CARTESIAN_POINT('Ctrl Pts',(1.45472976009375,-2.87576957325743,36.341803297677));
#22387=CARTESIAN_POINT('Ctrl Pts',(1.46641195118515,-2.86983018568026,36.342613418507));
#22388=CARTESIAN_POINT('Ctrl Pts',(1.49755967260083,-2.85375441088964,36.3447869664951));
#22389=CARTESIAN_POINT('Ctrl Pts',(1.51695816490364,-2.84349030209702,36.3461548952742));
#22390=CARTESIAN_POINT('Ctrl Pts',(1.68083909316897,-2.75462355953177,36.357835068579));
#22391=CARTESIAN_POINT('Ctrl Pts',(1.81919097537173,-2.66527678924624,36.3685375908901));
#22392=CARTESIAN_POINT('Ctrl Pts',(2.15338260351415,-2.41127628278103,36.3965392768757));
#22393=CARTESIAN_POINT('Ctrl Pts',(2.33757028432234,-2.23317501815466,36.4141675774876));
#22394=CARTESIAN_POINT('Ctrl Pts',(2.53323312048606,-1.99294232868106,36.4344160582179));
#22395=CARTESIAN_POINT('Ctrl Pts',(2.56658298813822,-1.94980557244468,36.4379287022976));
#22396=CARTESIAN_POINT('Ctrl Pts',(2.60566044690566,-1.89651913145639,36.4421009236364));
#22397=CARTESIAN_POINT('Ctrl Pts',(2.61244621916695,-1.88716081510612,36.4428275825417));
#22398=CARTESIAN_POINT('Ctrl Pts',(2.62295753273703,-1.87249922315853,36.4439563210097));
#22399=CARTESIAN_POINT('Ctrl Pts',(2.62671759778278,-1.86722098920448,36.4443607233275));
#22400=CARTESIAN_POINT('Ctrl Pts',(2.63368774521397,-1.85737384537279,36.4451115070263));
#22401=CARTESIAN_POINT('Ctrl Pts',(2.63690184234078,-1.85280798122805,36.4454581572087));
#22402=CARTESIAN_POINT('Ctrl Pts',(2.64418024368227,-1.84241116954627,36.4462441981131));
#22403=CARTESIAN_POINT('Ctrl Pts',(2.64823712627546,-1.83657512888788,36.4466830793902));
#22404=CARTESIAN_POINT('Ctrl Pts',(2.65871239544762,-1.82139902013144,36.447818410412));
#22405=CARTESIAN_POINT('Ctrl Pts',(2.66510094696543,-1.81203833942282,36.4485128787553));
#22406=CARTESIAN_POINT('Ctrl Pts',(2.70510337492795,-1.75275647877739,36.4528757988539));
#22407=CARTESIAN_POINT('Ctrl Pts',(2.73736513833007,-1.70193205234039,36.4564596009306));
#22408=CARTESIAN_POINT('Ctrl Pts',(2.93892976009823,-1.36381649689437,36.4794989374551));
#22409=CARTESIAN_POINT('Ctrl Pts',(3.06420210421427,-1.05262467792409,36.4972114672141));
#22410=CARTESIAN_POINT('Ctrl Pts',(3.15914205093584,-0.643036144895613,
36.521630007708));
#22411=CARTESIAN_POINT('Ctrl Pts',(3.17533518873855,-0.557600584126361,
36.526765492885));
#22412=CARTESIAN_POINT('Ctrl Pts',(3.19095975778362,-0.451981742642096,
36.533210627656));
#22413=CARTESIAN_POINT('Ctrl Pts',(3.19368337042743,-0.43231721414448,36.5344146060057));
#22414=CARTESIAN_POINT('Ctrl Pts',(3.19768988748429,-0.401282733161163,
36.5363215020611));
#22415=CARTESIAN_POINT('Ctrl Pts',(3.19909424851081,-0.389928752815022,
36.5370205673367));
#22416=CARTESIAN_POINT('Ctrl Pts',(3.20160785947631,-0.368678505116161,
36.5383317097633));
#22417=CARTESIAN_POINT('Ctrl Pts',(3.20273175667167,-0.358784081663207,
36.5389433152643));
#22418=CARTESIAN_POINT('Ctrl Pts',(3.2051375239809,-0.336691909387495,36.5403114660003));
#22419=CARTESIAN_POINT('Ctrl Pts',(3.20639565045291,-0.324491780416018,
36.5410687525325));
#22420=CARTESIAN_POINT('Ctrl Pts',(3.20939615766952,-0.293672553523231,
36.5429862892245));
#22421=CARTESIAN_POINT('Ctrl Pts',(3.21104615788522,-0.275045112098162,
36.5441494336786));
#22422=CARTESIAN_POINT('Ctrl Pts',(3.21939660122333,-0.170421113847801,
36.5507066252172));
#22423=CARTESIAN_POINT('Ctrl Pts',(3.2228039392682,-0.0842040481459283,
36.5562032879677));
#22424=CARTESIAN_POINT('Ctrl Pts',(3.22263357550004,0.184970274485804,36.5736660170257));
#22425=CARTESIAN_POINT('Ctrl Pts',(3.20694277966631,0.367538399943799,36.5859673833119));
#22426=CARTESIAN_POINT('Ctrl Pts',(3.15894344069144,0.645829823717705,36.6050828408999));
#22427=CARTESIAN_POINT('Ctrl Pts',(3.13749662835673,0.743058334153712,36.6118258198534));
#22428=CARTESIAN_POINT('Ctrl Pts',(3.10457565432211,0.865131329287124,36.620278234588));
#22429=CARTESIAN_POINT('Ctrl Pts',(3.09724088761861,0.89103375506053,36.6220708041795));
#22430=CARTESIAN_POINT('Ctrl Pts',(3.06654473160006,0.994473963037814,36.6292184191876));
#22431=CARTESIAN_POINT('Ctrl Pts',(3.04058708029015,1.07121786073489,36.6344970946243));
#22432=CARTESIAN_POINT('Ctrl Pts',(3.00695581531393,1.15953299579155,36.6404799419706));
#22433=CARTESIAN_POINT('Ctrl Pts',(3.00206897881807,1.17212708571676,36.6413308873444));
#22434=CARTESIAN_POINT('Ctrl Pts',(2.99453543051912,1.19118592291648,36.6426148360029));
#22435=CARTESIAN_POINT('Ctrl Pts',(2.99194672477672,1.19767322165597,36.6430511985206));
#22436=CARTESIAN_POINT('Ctrl Pts',(2.9872538715903,1.20932334375856,36.6438335579084));
#22437=CARTESIAN_POINT('Ctrl Pts',(2.98515741117633,1.21448914159256,36.6441800079051));
#22438=CARTESIAN_POINT('Ctrl Pts',(2.98056009655472,1.22573336116057,36.6449331118216));
#22439=CARTESIAN_POINT('Ctrl Pts',(2.9780540571047,1.23180956183125,36.6453394461138));
#22440=CARTESIAN_POINT('Ctrl Pts',(2.97092667178849,1.24894189853023,36.6464834692871));
#22441=CARTESIAN_POINT('Ctrl Pts',(2.96626216830768,1.2599801246071,36.6472185866358));
#22442=CARTESIAN_POINT('Ctrl Pts',(2.93716503604649,1.32777928414764,36.651723219759));
#22443=CARTESIAN_POINT('Ctrl Pts',(2.91116378962115,1.38385794959682,36.6554032242125));
#22444=CARTESIAN_POINT('Ctrl Pts',(2.76347261567103,1.67977881225645,36.6747539223773));
#22445=CARTESIAN_POINT('Ctrl Pts',(2.61372736611706,1.90444108728551,36.6892804506745));
#22446=CARTESIAN_POINT('Ctrl Pts',(2.34376095287608,2.21665787511883,36.7127248839091));
#22447=CARTESIAN_POINT('Ctrl Pts',(2.24256419857794,2.31898376879698,36.7210616337054));
#22448=CARTESIAN_POINT('Ctrl Pts',(2.11882836152967,2.4284034428552,36.731000513484));
#22449=CARTESIAN_POINT('Ctrl Pts',(2.10263219673709,2.44244032027682,36.7322965821504));
#22450=CARTESIAN_POINT('Ctrl Pts',(2.07642359732163,2.46470088149511,36.7343868019875));
#22451=CARTESIAN_POINT('Ctrl Pts',(2.0664993079806,2.47302769761647,36.735176696898));
#22452=CARTESIAN_POINT('Ctrl Pts',(2.04878125856672,2.48771262000182,36.7365842272608));
#22453=CARTESIAN_POINT('Ctrl Pts',(2.04100738834421,2.49409453755293,36.7372008800983));
#22454=CARTESIAN_POINT('Ctrl Pts',(2.02473884915917,2.50732311237492,36.7384895474435));
#22455=CARTESIAN_POINT('Ctrl Pts',(2.016239043971,2.51416322262954,36.7391618156184));
#22456=CARTESIAN_POINT('Ctrl Pts',(1.99405204187911,2.53183305872703,36.7409140909781));
#22457=CARTESIAN_POINT('Ctrl Pts',(1.9803114508983,2.54259487947004,36.7419967975236));
#22458=CARTESIAN_POINT('Ctrl Pts',(1.91997054415686,2.58906886700687,36.7467412015817));
#22459=CARTESIAN_POINT('Ctrl Pts',(1.87248916450982,2.62361355511462,36.7504484297529));
#22460=CARTESIAN_POINT('Ctrl Pts',(1.74328790330577,2.71231859679064,36.7604747270384));
#22461=CARTESIAN_POINT('Ctrl Pts',(1.66000072818877,2.76407660133745,36.7668766405699));
#22462=CARTESIAN_POINT('Ctrl Pts',(1.40766936111291,2.90536384818186,36.786061721988));
#22463=CARTESIAN_POINT('Ctrl Pts',(1.232871877232,2.9837377322838,36.7991106145913));
#22464=CARTESIAN_POINT('Ctrl Pts',(0.926532175384797,3.08955104591862,36.8209196403535));
#22465=CARTESIAN_POINT('Ctrl Pts',(0.798307190894622,3.12514024818465,36.8297459469964));
#22466=CARTESIAN_POINT('Ctrl Pts',(0.653620244386708,3.15580756373062,36.8391233165872));
#22467=CARTESIAN_POINT('Ctrl Pts',(0.638982021735399,3.15880401407526,36.8400654689786));
#22468=CARTESIAN_POINT('Ctrl Pts',(0.617276612328088,3.16309006136898,36.8414522305245));
#22469=CARTESIAN_POINT('Ctrl Pts',(0.610225350643649,3.16445795931336,36.8419011387716));
#22470=CARTESIAN_POINT('Ctrl Pts',(0.597677836891366,3.1668485942409,36.8426970460851));
#22471=CARTESIAN_POINT('Ctrl Pts',(0.592183448714921,3.16788061333103,36.8430445684284));
#22472=CARTESIAN_POINT('Ctrl Pts',(0.58036448649849,3.17006876268273,36.8437899708233));
#22473=CARTESIAN_POINT('Ctrl Pts',(0.574039147667095,3.17122026292387,36.8441875851245));
#22474=CARTESIAN_POINT('Ctrl Pts',(0.55656201494484,3.17434789388611,36.8452826853262));
#22475=CARTESIAN_POINT('Ctrl Pts',(0.545403057365658,3.17628420356421,36.8459779394641));
#22476=CARTESIAN_POINT('Ctrl Pts',(0.48400431868569,3.18660504084151,36.8497827884402));
#22477=CARTESIAN_POINT('Ctrl Pts',(0.433578292551593,3.19385697964606,36.8528320604096));
#22478=CARTESIAN_POINT('Ctrl Pts',(0.126694374032891,3.23058801392747,36.8710472475619));
#22479=CARTESIAN_POINT('Ctrl Pts',(-0.132392916066827,3.23036419740347,
36.8850459308302));
#22480=CARTESIAN_POINT('Ctrl Pts',(-0.553144886143904,3.17924354978906,
36.9089761751536));
#22481=CARTESIAN_POINT('Ctrl Pts',(-0.715783007048575,3.14661767538846,
36.9185165948688));
#22482=CARTESIAN_POINT('Ctrl Pts',(-0.896295515390018,3.09568300091237,
36.9297975036102));
#22483=CARTESIAN_POINT('Ctrl Pts',(-0.917348495585595,3.08950976600439,
36.931123803746));
#22484=CARTESIAN_POINT('Ctrl Pts',(-0.950871975286829,3.07930702346509,
36.9332534381652));
#22485=CARTESIAN_POINT('Ctrl Pts',(-0.963384003351651,3.07541550237927,
36.9340522528097));
#22486=CARTESIAN_POINT('Ctrl Pts',(-0.985479219561552,3.06839532825165,
36.9354700707615));
#22487=CARTESIAN_POINT('Ctrl Pts',(-0.995072167840309,3.06529779299603,
36.9360880416007));
#22488=CARTESIAN_POINT('Ctrl Pts',(-1.01495353803362,3.05877499347314,36.9373738543905));
#22489=CARTESIAN_POINT('Ctrl Pts',(-1.02523950770585,3.05534271274126,36.9380419221032));
#22490=CARTESIAN_POINT('Ctrl Pts',(-1.05174915691184,3.04634788252861,36.9397711234567));
#22491=CARTESIAN_POINT('Ctrl Pts',(-1.06794594537064,3.04070767254742,36.940834825075));
#22492=CARTESIAN_POINT('Ctrl Pts',(-1.13673876207206,3.01613450103769,36.9453839773432));
#22493=CARTESIAN_POINT('Ctrl Pts',(-1.18887980529481,2.99596503961827,36.9489104514787));
#22494=CARTESIAN_POINT('Ctrl Pts',(-1.32490043599684,2.93923888201575,36.958324879121));
#22495=CARTESIAN_POINT('Ctrl Pts',(-1.40778887040859,2.90045072006253,36.9642836859241));
#22496=CARTESIAN_POINT('Ctrl Pts',(-1.70772472929498,2.74420604356364,36.9866514534945));
#22497=CARTESIAN_POINT('Ctrl Pts',(-1.91270368009395,2.60548260354482,37.0036323679565));
#22498=CARTESIAN_POINT('Ctrl Pts',(-2.16733902784523,2.38677102064044,37.0259392947688));
#22499=CARTESIAN_POINT('Ctrl Pts',(-2.23241276480209,2.32602036633145,37.0317570263363));
#22500=CARTESIAN_POINT('Ctrl Pts',(-2.30459826389271,2.25280612658301,37.0382686764267));
#22501=CARTESIAN_POINT('Ctrl Pts',(-2.3142390779141,2.24290127029268,37.0391395910877));
#22502=CARTESIAN_POINT('Ctrl Pts',(-2.32870215248365,2.22784954115069,37.0404475897907));
#22503=CARTESIAN_POINT('Ctrl Pts',(-2.33357158612701,2.22274851201286,37.0408882204375));
#22504=CARTESIAN_POINT('Ctrl Pts',(-2.34226356460735,2.2135830876514,37.0416751359755));
#22505=CARTESIAN_POINT('Ctrl Pts',(-2.346092319323,2.20952472780483,37.0420218979329));
#22506=CARTESIAN_POINT('Ctrl Pts',(-2.35437302294139,2.2007016498423,37.0427721404088));
#22507=CARTESIAN_POINT('Ctrl Pts',(-2.3588210427999,2.19593337162044,37.0431753205467));
#22508=CARTESIAN_POINT('Ctrl Pts',(-2.37123931686889,2.18253970971524,37.0443015737209));
#22509=CARTESIAN_POINT('Ctrl Pts',(-2.37917703781714,2.17388410798806,37.0450222011656));
#22510=CARTESIAN_POINT('Ctrl Pts',(-2.42573118851716,2.12255921522773,37.0492543391556));
#22511=CARTESIAN_POINT('Ctrl Pts',(-2.46324908445984,2.07890219088969,37.0526884271842));
#22512=CARTESIAN_POINT('Ctrl Pts',(-2.65930140451222,1.83800460723727,37.0709110177983));
#22513=CARTESIAN_POINT('Ctrl Pts',(-2.79536817759413,1.62360345248578,37.0846448609797));
#22514=CARTESIAN_POINT('Ctrl Pts',(-2.97573333399933,1.24813681637361,37.1081755874179));
#22515=CARTESIAN_POINT('Ctrl Pts',(-3.03518938676924,1.09565021399464,37.1175957507025));
#22516=CARTESIAN_POINT('Ctrl Pts',(-3.08920302742152,0.918379895379297,
37.1287420858921));
#22517=CARTESIAN_POINT('Ctrl Pts',(-3.09537110838261,0.897370961205556,
37.1300657795763));
#22518=CARTESIAN_POINT('Ctrl Pts',(-3.10488397570805,0.863703896920118,
37.1321920182396));
#22519=CARTESIAN_POINT('Ctrl Pts',(-3.10836660299303,0.851085176480857,
37.1329900665771));
#22520=CARTESIAN_POINT('Ctrl Pts',(-3.11439433102335,0.828714120288518,
37.1344069975532));
#22521=CARTESIAN_POINT('Ctrl Pts',(-3.11697075770407,0.818970350030057,
37.1350248520166));
#22522=CARTESIAN_POINT('Ctrl Pts',(-3.12222555820101,0.798713233184525,
37.1363108945144));
#22523=CARTESIAN_POINT('Ctrl Pts',(-3.12489663064067,0.788198140285589,
37.1369793106554));
#22524=CARTESIAN_POINT('Ctrl Pts',(-3.13165917973631,0.761001547505315,
37.1387104280406));
#22525=CARTESIAN_POINT('Ctrl Pts',(-3.13567044260096,0.744300631681173,
37.1397757080816));
#22526=CARTESIAN_POINT('Ctrl Pts',(-3.15221945776199,0.672889607208716,
37.1443407616012));
#22527=CARTESIAN_POINT('Ctrl Pts',(-3.16345965886952,0.617891803538932,
37.1478819161826));
#22528=CARTESIAN_POINT('Ctrl Pts',(-3.18931977790645,0.472039927098291,
37.1573454942228));
#22529=CARTESIAN_POINT('Ctrl Pts',(-3.20149397223313,0.380809869881011,
37.1633396944617));
#22530=CARTESIAN_POINT('Ctrl Pts',(-3.23146072734248,0.0482064408569172,
37.1854324681332));
#22531=CARTESIAN_POINT('Ctrl Pts',(-3.22596406277041,-0.194430714669504,
37.2020723137423));
#22532=CARTESIAN_POINT('Ctrl Pts',(-3.18088225099349,-0.526024420256396,
37.22434190437));
#22533=CARTESIAN_POINT('Ctrl Pts',(-3.16443211676231,-0.617321996036819,
37.2304125155196));
#22534=CARTESIAN_POINT('Ctrl Pts',(-3.14100181686343,-0.721401250402509,
37.2371701970664));
#22535=CARTESIAN_POINT('Ctrl Pts',(-3.13784956707135,-0.734991352746937,
37.238049324232));
#22536=CARTESIAN_POINT('Ctrl Pts',(-3.13296472537972,-0.755446696316358,
37.2393671989953));
#22537=CARTESIAN_POINT('Ctrl Pts',(-3.1312976444493,-0.762327190639459,
37.2398095715792));
#22538=CARTESIAN_POINT('Ctrl Pts',(-3.12827571303548,-0.774622345565591,
37.24059836306));
#22539=CARTESIAN_POINT('Ctrl Pts',(-3.12692946109608,-0.780039013078377,
37.240945268769));
#22540=CARTESIAN_POINT('Ctrl Pts',(-3.12398479059021,-0.791756810987841,
37.2416944183312));
#22541=CARTESIAN_POINT('Ctrl Pts',(-3.1223813824102,-0.798056592057209,
37.242096369373));
#22542=CARTESIAN_POINT('Ctrl Pts',(-3.11785094746984,-0.815633975101017,
37.243215721764));
#22543=CARTESIAN_POINT('Ctrl Pts',(-3.11488177370662,-0.826900754306286,
37.2439307256483));
#22544=CARTESIAN_POINT('Ctrl Pts',(-3.09728790003992,-0.89222251294425,
37.2480630269886));
#22545=CARTESIAN_POINT('Ctrl Pts',(-3.08131642639808,-0.945908721459504,
37.2514070996175));
#22546=CARTESIAN_POINT('Ctrl Pts',(-2.98515110660766,-1.24080389563577,
37.2696241341481));
#22547=CARTESIAN_POINT('Ctrl Pts',(-2.87803202414719,-1.47230447864389,
37.2834171147081));
#22548=CARTESIAN_POINT('Ctrl Pts',(-2.65885976161363,-1.82851934396009,
37.3070405146908));
#22549=CARTESIAN_POINT('Ctrl Pts',(-2.56238400196479,-1.96142702769182,
37.3164913659328));
#22550=CARTESIAN_POINT('Ctrl Pts',(-2.44203953090745,-2.10310256496634,
37.3276720280684));
#22551=CARTESIAN_POINT('Ctrl Pts',(-2.42768750438157,-2.11965346555868,
37.328996392058));
#22552=CARTESIAN_POINT('Ctrl Pts',(-2.40448948106646,-2.14586097999958,
37.3311235040547));
#22553=CARTESIAN_POINT('Ctrl Pts',(-2.39575127014583,-2.15561240804024,
37.3319217495112));
#22554=CARTESIAN_POINT('Ctrl Pts',(-2.3801819403947,-2.17277543323153,37.3333389085882));
#22555=CARTESIAN_POINT('Ctrl Pts',(-2.37337498200137,-2.18020878444696,
37.3339567929294));
#22556=CARTESIAN_POINT('Ctrl Pts',(-2.35916991163932,-2.19557567899414,
37.3352427760587));
#22557=CARTESIAN_POINT('Ctrl Pts',(-2.35176639903119,-2.20350403538454,
37.3359111023494));
#22558=CARTESIAN_POINT('Ctrl Pts',(-2.33254173034325,-2.2238843106004,37.3376417256947));
#22559=CARTESIAN_POINT('Ctrl Pts',(-2.3206609577078,-2.23627928750168,37.3387065987548));
#22560=CARTESIAN_POINT('Ctrl Pts',(-2.26956127909485,-2.28874483413571,
37.3432675469909));
#22561=CARTESIAN_POINT('Ctrl Pts',(-2.22940126084228,-2.32788116026025,
37.3468049107828));
#22562=CARTESIAN_POINT('Ctrl Pts',(-2.12079814275964,-2.4283271441839,37.3562557881338));
#22563=CARTESIAN_POINT('Ctrl Pts',(-2.05072260321249,-2.48778852983414,
37.3622408391819));
#22564=CARTESIAN_POINT('Ctrl Pts',(-1.82076289780361,-2.66659256755328,
37.3815103996241));
#22565=CARTESIAN_POINT('Ctrl Pts',(-1.65238201600226,-2.77406600268191,
37.3951166831969));
#22566=CARTESIAN_POINT('Ctrl Pts',(-1.47525540431025,-2.86526422072266,
37.4085260041042));
#22567=CARTESIAN_POINT('Origin',(0.,0.,4.68922655072688));
#22568=CARTESIAN_POINT('',(-1.47525540693158,-2.86526421937299,38.9066255640146));
#22569=CARTESIAN_POINT('',(-1.47525532932069,-2.86526425933297,38.6590632205222));
#22570=CARTESIAN_POINT('',(-1.47525540501186,-2.86526422036142,4.68922655072688));
#22571=CARTESIAN_POINT('',(3.22389497588569,-0.002876326465697,38.0607734492731));
#22572=CARTESIAN_POINT('Ctrl Pts',(-1.47525540693158,-2.86526421937299,
38.9066255640146));
#22573=CARTESIAN_POINT('Ctrl Pts',(-1.49002538501413,-2.85765951406197,
38.9055720617144));
#22574=CARTESIAN_POINT('Ctrl Pts',(-1.50473664835218,-2.84994055882525,
38.9045146246307));
#22575=CARTESIAN_POINT('Ctrl Pts',(-1.60015608991765,-2.79892942837589,
38.8976026072713));
#22576=CARTESIAN_POINT('Ctrl Pts',(-1.67904034790546,-2.75233109776619,
38.8916367201395));
#22577=CARTESIAN_POINT('Ctrl Pts',(-1.96192576918629,-2.56853496469414,
38.8693234378444));
#22578=CARTESIAN_POINT('Ctrl Pts',(-2.1520078611904,-2.4115080988086,38.8524102832026));
#22579=CARTESIAN_POINT('Ctrl Pts',(-2.38458425665035,-2.16977467697611,
38.8301117544657));
#22580=CARTESIAN_POINT('Ctrl Pts',(-2.4440582674071,-2.10255715944651,38.8242448859708));
#22581=CARTESIAN_POINT('Ctrl Pts',(-2.50939236403878,-2.02219172532073,
38.8176851083325));
#22582=CARTESIAN_POINT('Ctrl Pts',(-2.51806045907684,-2.01138781723053,
38.8168123292109));
#22583=CARTESIAN_POINT('Ctrl Pts',(-2.53104110274388,-1.99499331763225,
38.815501998755));
#22584=CARTESIAN_POINT('Ctrl Pts',(-2.53540524587758,-1.989444053651,38.8150608835902));
#22585=CARTESIAN_POINT('Ctrl Pts',(-2.54318719471073,-1.97948165202396,
38.814273337805));
#22586=CARTESIAN_POINT('Ctrl Pts',(-2.54661178932123,-1.9750739515477,38.8139264279438));
#22587=CARTESIAN_POINT('Ctrl Pts',(-2.55401143125022,-1.9654988355663,38.8131761265784));
#22588=CARTESIAN_POINT('Ctrl Pts',(-2.55798224376486,-1.9603282648401,38.8127730342564));
#22589=CARTESIAN_POINT('Ctrl Pts',(-2.56905412833189,-1.94582015119312,
38.8116476693855));
#22590=CARTESIAN_POINT('Ctrl Pts',(-2.57612003334254,-1.93645572083592,
38.8109278351649));
#22591=CARTESIAN_POINT('Ctrl Pts',(-2.6173852565759,-1.88114139013536,38.8067128592521));
#22592=CARTESIAN_POINT('Ctrl Pts',(-2.65040812344926,-1.83432173516558,
38.8032944000121));
#22593=CARTESIAN_POINT('Ctrl Pts',(-2.82260901710396,-1.57580811490179,
38.7850672734058));
#22594=CARTESIAN_POINT('Ctrl Pts',(-2.93771459729681,-1.34913028081267,
38.771318407596));
#22595=CARTESIAN_POINT('Ctrl Pts',(-3.08144711727346,-0.957870180989853,
38.7477716487388));
#22596=CARTESIAN_POINT('Ctrl Pts',(-3.12604745984707,-0.800405221279804,
38.7383519913786));
#22597=CARTESIAN_POINT('Ctrl Pts',(-3.16286278519733,-0.618786061352153,
38.7272059279998));
#22598=CARTESIAN_POINT('Ctrl Pts',(-3.16699464761004,-0.597278874106064,
38.7258819480685));
#22599=CARTESIAN_POINT('Ctrl Pts',(-3.17324614501426,-0.562848047624855,
38.723755195981));
#22600=CARTESIAN_POINT('Ctrl Pts',(-3.17550680959566,-0.549950466707746,
38.7229569221296));
#22601=CARTESIAN_POINT('Ctrl Pts',(-3.17936886221839,-0.527098518780338,
38.7215395575294));
#22602=CARTESIAN_POINT('Ctrl Pts',(-3.18100226506128,-0.517149684859452,
38.7209214953921));
#22603=CARTESIAN_POINT('Ctrl Pts',(-3.18429701960772,-0.496475424153949,
38.7196349866772));
#22604=CARTESIAN_POINT('Ctrl Pts',(-3.18595092605086,-0.485748955792172,
38.718966311672));
#22605=CARTESIAN_POINT('Ctrl Pts',(-3.19008337726808,-0.458018436020884,
38.7172344485463));
#22606=CARTESIAN_POINT('Ctrl Pts',(-3.19248013724707,-0.441002717117454,
38.7161686790451));
#22607=CARTESIAN_POINT('Ctrl Pts',(-3.20212950782503,-0.368291638137228,
38.7116007895461));
#22608=CARTESIAN_POINT('Ctrl Pts',(-3.20806119123702,-0.312433782447478,
38.708057231879));
#22609=CARTESIAN_POINT('Ctrl Pts',(-3.21985750140243,-0.164663528791871,
38.6985861807442));
#22610=CARTESIAN_POINT('Ctrl Pts',(-3.22324705391988,-0.0726106288567802,
38.6925867825136));
#22611=CARTESIAN_POINT('Ctrl Pts',(-3.22123667371041,0.260413000722466,
38.6705540577715));
#22612=CARTESIAN_POINT('Ctrl Pts',(-3.19276414240804,0.500422874191539,
38.6539855881292));
#22613=CARTESIAN_POINT('Ctrl Pts',(-3.11648348568949,0.826072993055285,
38.6317213447037));
#22614=CARTESIAN_POINT('Ctrl Pts',(-3.0911949938636,0.916178464593166,38.6255953149802));
#22615=CARTESIAN_POINT('Ctrl Pts',(-3.05765950143477,1.01834737921826,38.6187836760114));
#22616=CARTESIAN_POINT('Ctrl Pts',(-3.05321304665781,1.03160221008797,38.6179026440848));
#22617=CARTESIAN_POINT('Ctrl Pts',(-3.04638266787942,1.05153242107241,38.6165823904263));
#22618=CARTESIAN_POINT('Ctrl Pts',(-3.04406281571226,1.05822935510263,38.6161395259339));
#22619=CARTESIAN_POINT('Ctrl Pts',(-3.03987575713399,1.07018882576067,38.6153500937918));
#22620=CARTESIAN_POINT('Ctrl Pts',(-3.03801695461214,1.07545419552328,38.6150030371192));
#22621=CARTESIAN_POINT('Ctrl Pts',(-3.03396502082593,1.08683763895693,38.6142538227467));
#22622=CARTESIAN_POINT('Ctrl Pts',(-3.03176707161883,1.0929538994206,38.6138519566616));
#22623=CARTESIAN_POINT('Ctrl Pts',(-3.02558158421137,1.11000409406797,38.6127334781502));
#22624=CARTESIAN_POINT('Ctrl Pts',(-3.02155325032854,1.12092326973296,38.6120192560698));
#22625=CARTESIAN_POINT('Ctrl Pts',(-2.99788974749306,1.1840108399259,38.6079033788696));
#22626=CARTESIAN_POINT('Ctrl Pts',(-2.9769615901331,1.23568813515905,38.6045742601978));
#22627=CARTESIAN_POINT('Ctrl Pts',(-2.85309831341355,1.52009835128221,38.586352211355));
#22628=CARTESIAN_POINT('Ctrl Pts',(-2.72421241054394,1.74056406550934,38.5725443297351));
#22629=CARTESIAN_POINT('Ctrl Pts',(-2.47181419243833,2.0744027604447,38.5489055120823));
#22630=CARTESIAN_POINT('Ctrl Pts',(-2.36308328025146,2.1974619822985,38.5394557028752));
#22631=CARTESIAN_POINT('Ctrl Pts',(-2.22975330802823,2.32697182181145,38.5282759105367));
#22632=CARTESIAN_POINT('Ctrl Pts',(-2.2138810619597,2.34207777013135,38.5269512683837));
#22633=CARTESIAN_POINT('Ctrl Pts',(-2.18827719496378,2.36595266754435,38.5248236519738));
#22634=CARTESIAN_POINT('Ctrl Pts',(-2.17864383419666,2.37482633950933,38.524025181835));
#22635=CARTESIAN_POINT('Ctrl Pts',(-2.16149936665313,2.39042667936403,38.5226075882277));
#22636=CARTESIAN_POINT('Ctrl Pts',(-2.15401023828681,2.39717732158954,38.5219894944578));
#22637=CARTESIAN_POINT('Ctrl Pts',(-2.138395039001,2.41112048299922,38.5207030390866));
#22638=CARTESIAN_POINT('Ctrl Pts',(-2.13026408108945,2.41830731433588,38.5200344496495));
#22639=CARTESIAN_POINT('Ctrl Pts',(-2.10916928992794,2.43676374150166,38.5183030643864));
#22640=CARTESIAN_POINT('Ctrl Pts',(-2.09615150339521,2.44797089073208,38.5172376899081));
#22641=CARTESIAN_POINT('Ctrl Pts',(-2.04023271260731,2.49533887939783,38.5126738089208));
#22642=CARTESIAN_POINT('Ctrl Pts',(-1.99648305983983,2.53047829429274,38.5091339553454));
#22643=CARTESIAN_POINT('Ctrl Pts',(-1.87867403214216,2.62014426252652,38.4996753229585));
#22644=CARTESIAN_POINT('Ctrl Pts',(-1.80316375613681,2.67267095264063,38.4936848739923));
#22645=CARTESIAN_POINT('Ctrl Pts',(-1.52761556632957,2.8473518822491,38.4721019313201));
#22646=CARTESIAN_POINT('Ctrl Pts',(-1.31664350570897,2.9508401911888,38.4560101564839));
#22647=CARTESIAN_POINT('Ctrl Pts',(-1.07787440617152,3.03721739410839,38.4390702099217));
#22648=CARTESIAN_POINT('Ctrl Pts',(-1.05935822808816,3.04372516868267,38.4377649089865));
#22649=CARTESIAN_POINT('Ctrl Pts',(-0.963686946120721,3.07637140395294,
38.4310671036862));
#22650=CARTESIAN_POINT('Ctrl Pts',(-0.885613101174097,3.09974925806941,
38.425755924003));
#22651=CARTESIAN_POINT('Ctrl Pts',(-0.793629191734922,3.12353219665299,
38.4197408189209));
#22652=CARTESIAN_POINT('Ctrl Pts',(-0.780506543574181,3.1268370965065,38.4188883785942));
#22653=CARTESIAN_POINT('Ctrl Pts',(-0.760573147020587,3.13172395437175,
38.4176025381763));
#22654=CARTESIAN_POINT('Ctrl Pts',(-0.753777619485011,3.1333665187637,38.4171657655021));
#22655=CARTESIAN_POINT('Ctrl Pts',(-0.741551397257901,3.13627967390906,
38.4163828579099));
#22656=CARTESIAN_POINT('Ctrl Pts',(-0.736122729708663,3.13755828567696,
38.416036268118));
#22657=CARTESIAN_POINT('Ctrl Pts',(-0.724289912588004,3.14031286251561,
38.4152830693479));
#22658=CARTESIAN_POINT('Ctrl Pts',(-0.717884579000465,3.14178332878175,
38.4148767790806));
#22659=CARTESIAN_POINT('Ctrl Pts',(-0.699797048209316,3.14587746244971,
38.4137334066453));
#22660=CARTESIAN_POINT('Ctrl Pts',(-0.68810451888155,3.148455668894,38.4129988902638));
#22661=CARTESIAN_POINT('Ctrl Pts',(-0.616210696039781,3.16388864193324,
38.4085093110128));
#22662=CARTESIAN_POINT('Ctrl Pts',(-0.555661266310293,3.17508246562517,
38.4048430562699));
#22663=CARTESIAN_POINT('Ctrl Pts',(-0.231564557482987,3.22544170965631,
38.3856500249424));
#22664=CARTESIAN_POINT('Ctrl Pts',(0.0357720105488799,3.23354991255757,
38.3712487592086));
#22665=CARTESIAN_POINT('Ctrl Pts',(0.335747515699205,3.20540226999132,38.3541485629435));
#22666=CARTESIAN_POINT('Ctrl Pts',(0.3703611802829,3.20158751495943,38.3521625935107));
#22667=CARTESIAN_POINT('Ctrl Pts',(0.517728638621303,3.18292441129463,38.3436376088817));
#22668=CARTESIAN_POINT('Ctrl Pts',(0.629705377457992,3.16267572173402,38.3369814075794));
#22669=CARTESIAN_POINT('Ctrl Pts',(0.760147728569706,3.13188536583983,38.3289090070795));
#22670=CARTESIAN_POINT('Ctrl Pts',(0.779880466194814,3.12703005156854,38.3276792463039));
#22671=CARTESIAN_POINT('Ctrl Pts',(0.811930615872333,3.11882175811995,38.3256672537962));
#22672=CARTESIAN_POINT('Ctrl Pts',(0.8242765408059,3.11558159270845,38.3248886756023));
#22673=CARTESIAN_POINT('Ctrl Pts',(0.846267045892457,3.10967036787665,38.3234954075626));
#22674=CARTESIAN_POINT('Ctrl Pts',(0.855919097407876,3.10702755136079,38.3228816435759));
#22675=CARTESIAN_POINT('Ctrl Pts',(0.876273680228241,3.10135224355523,38.3215825293356));
#22676=CARTESIAN_POINT('Ctrl Pts',(0.886973113623122,3.09830921504044,38.3208968418547));
#22677=CARTESIAN_POINT('Ctrl Pts',(0.91533454125471,3.09008398580277,38.3190716989328));
#22678=CARTESIAN_POINT('Ctrl Pts',(0.93296805959005,3.08480581866096,38.3179291149274));
#22679=CARTESIAN_POINT('Ctrl Pts',(1.01495437683612,3.05949793555752,38.3125794965939));
#22680=CARTESIAN_POINT('Ctrl Pts',(1.07870993518799,3.03760494134279,38.3083115877426));
#22681=CARTESIAN_POINT('Ctrl Pts',(1.39514060098899,2.91772761919292,38.2865662059791));
#22682=CARTESIAN_POINT('Ctrl Pts',(1.63540086326412,2.79015561371561,38.2680929982626));
#22683=CARTESIAN_POINT('Ctrl Pts',(1.97184742513313,2.55298693769739,38.2403534573455));
#22684=CARTESIAN_POINT('Ctrl Pts',(2.08145687877717,2.46444139251656,38.2309847786213));
#22685=CARTESIAN_POINT('Ctrl Pts',(2.19596849412832,2.3588270784302,38.2211071425949));
#22686=CARTESIAN_POINT('Ctrl Pts',(2.20692998150898,2.34857465080232,38.2201607054759));
#22687=CARTESIAN_POINT('Ctrl Pts',(2.22304158683202,2.33329283752219,38.2187687794706));
#22688=CARTESIAN_POINT('Ctrl Pts',(2.22824693498608,2.32832234914491,38.2183189473264));
#22689=CARTESIAN_POINT('Ctrl Pts',(2.23746815948907,2.31945792934599,38.2175219186344));
#22690=CARTESIAN_POINT('Ctrl Pts',(2.2414905861456,2.31557094571986,38.2171741941864));
#22691=CARTESIAN_POINT('Ctrl Pts',(2.25011066063178,2.30719761638016,38.216428927465));
#22692=CARTESIAN_POINT('Ctrl Pts',(2.25470500877019,2.30270800390525,38.2160316481237));
#22693=CARTESIAN_POINT('Ctrl Pts',(2.26679697293695,2.29082080974838,38.21498576637));
#22694=CARTESIAN_POINT('Ctrl Pts',(2.27427187445572,2.28340008476939,38.2143389530659));
#22695=CARTESIAN_POINT('Ctrl Pts',(2.31247691316823,2.24509822751942,38.2110307115671));
#22696=CARTESIAN_POINT('Ctrl Pts',(2.3426166156365,2.21363125917362,38.2084131276354));
#22697=CARTESIAN_POINT('Ctrl Pts',(2.4292636926111,2.11941594719959,38.2008298884893));
#22698=CARTESIAN_POINT('Ctrl Pts',(2.48395675346763,2.05504426523028,38.1959669696715));
#22699=CARTESIAN_POINT('Ctrl Pts',(2.60289988764278,1.903355644638,38.1850190688539));
#22700=CARTESIAN_POINT('Ctrl Pts',(2.66539994914537,1.81479888962503,38.178983303926));
#22701=CARTESIAN_POINT('Ctrl Pts',(2.84071569230094,1.53774190101823,38.1606620164246));
#22702=CARTESIAN_POINT('Ctrl Pts',(2.9388299190723,1.34073820988874,38.1483289833366));
#22703=CARTESIAN_POINT('Ctrl Pts',(3.0291607124404,1.10075680698274,38.1330463134295));
#22704=CARTESIAN_POINT('Ctrl Pts',(3.04156958776108,1.06598988876505,38.1308277508842));
#22705=CARTESIAN_POINT('Ctrl Pts',(3.0582051806485,1.01672331008451,38.1276743916881));
#22706=CARTESIAN_POINT('Ctrl Pts',(3.06293166416047,1.00239454547579,38.1267561460961));
#22707=CARTESIAN_POINT('Ctrl Pts',(3.0704282109749,0.979119938544014,38.1252625989505));
#22708=CARTESIAN_POINT('Ctrl Pts',(3.0732602415944,0.970194175053682,38.1246893490493));
#22709=CARTESIAN_POINT('Ctrl Pts',(3.07909211170209,0.951531989013385,38.1234897319037));
#22710=CARTESIAN_POINT('Ctrl Pts',(3.08208475926499,0.941793444106166,38.1228631356315));
#22711=CARTESIAN_POINT('Ctrl Pts',(3.08906898686195,0.918675833820232,38.1213742172039));
#22712=CARTESIAN_POINT('Ctrl Pts',(3.09301987527039,0.905284780912984,38.1205105721028));
#22713=CARTESIAN_POINT('Ctrl Pts',(3.10116125281201,0.877015036798432,38.1186847087445));
#22714=CARTESIAN_POINT('Ctrl Pts',(3.10533194928208,0.862131058501892,38.1177218675539));
#22715=CARTESIAN_POINT('Ctrl Pts',(3.11640311428866,0.821498500236896,38.1150889848471));
#22716=CARTESIAN_POINT('Ctrl Pts',(3.12309132359014,0.795693830806746,38.1134121383776));
#22717=CARTESIAN_POINT('Ctrl Pts',(3.19166642247518,0.516919861529357,38.0952424557336));
#22718=CARTESIAN_POINT('Ctrl Pts',(3.22297737174026,0.257477409621273,38.0777345230348));
#22719=CARTESIAN_POINT('Ctrl Pts',(3.22274875711747,-0.00283037061280869,
38.0601149330464));
#22720=CARTESIAN_POINT('Ctrl Pts',(-1.47642198135613,-2.86757701803244,
37.6538374877124));
#22721=CARTESIAN_POINT('Ctrl Pts',(-0.665155103199407,-3.27567489814633,
37.7100277565976));
#22722=CARTESIAN_POINT('Ctrl Pts',(1.50747120958243,-3.40811199926236,37.8325290049372));
#22723=CARTESIAN_POINT('Ctrl Pts',(3.10959334693804,-1.49896815034561,37.9681743254574));
#22724=CARTESIAN_POINT('Ctrl Pts',(3.22586433700409,-0.215544722264628,
38.0476293770925));
#22725=CARTESIAN_POINT('Ctrl Pts',(3.22389497588569,-0.002876326465697,
38.0607734492731));
#22726=CARTESIAN_POINT('',(3.22274953375635,0.00173354353987881,37.8165056021994));
#22727=CARTESIAN_POINT('Ctrl Pts',(-1.47525540431025,-2.86526422072265,
37.4085260041042));
#22728=CARTESIAN_POINT('Ctrl Pts',(-1.43625760423782,-2.88534324690704,
37.4114783217196));
#22729=CARTESIAN_POINT('Ctrl Pts',(-1.39683575020098,-2.90463337997842,
37.4144193805815));
#22730=CARTESIAN_POINT('Ctrl Pts',(-1.27393816816533,-2.96168666266681,
37.4234325092417));
#22731=CARTESIAN_POINT('Ctrl Pts',(-1.1892482247323,-2.9966979124969,37.429427020127));
#22732=CARTESIAN_POINT('Ctrl Pts',(-1.09009691860782,-3.03282046492186,
37.4361111154649));
#22733=CARTESIAN_POINT('Ctrl Pts',(-1.0769890306239,-3.03749994383052,37.4369881523242));
#22734=CARTESIAN_POINT('Ctrl Pts',(-1.05717493303045,-3.04442913262363,
37.4383035141713));
#22735=CARTESIAN_POINT('Ctrl Pts',(-1.05049115905415,-3.04674185148841,
37.4387454441221));
#22736=CARTESIAN_POINT('Ctrl Pts',(-1.03851967456026,-3.05084014569193,
37.4395337580483));
#22737=CARTESIAN_POINT('Ctrl Pts',(-1.03323490810244,-3.05263399955876,
37.4398806263606));
#22738=CARTESIAN_POINT('Ctrl Pts',(-1.02177956153736,-3.05648923004023,
37.4406300496742));
#22739=CARTESIAN_POINT('Ctrl Pts',(-1.01560741011654,-3.0585456472008,37.4410323099559));
#22740=CARTESIAN_POINT('Ctrl Pts',(-0.998341982499454,-3.06424005945056,
37.4421533973977));
#22741=CARTESIAN_POINT('Ctrl Pts',(-0.987234969882515,-3.0678365308348,
37.4428698150333));
#22742=CARTESIAN_POINT('Ctrl Pts',(-0.92237377082824,-3.08844997402597,
37.4470269220475));
#22743=CARTESIAN_POINT('Ctrl Pts',(-0.868196327896372,-3.10411543744507,
37.4503933551825));
#22744=CARTESIAN_POINT('Ctrl Pts',(-0.567968942834488,-3.18244995353801,
37.4686115598272));
#22745=CARTESIAN_POINT('Ctrl Pts',(-0.315569757793848,-3.21730000377383,
37.4823896948693));
#22746=CARTESIAN_POINT('Ctrl Pts',(0.102172048858668,-3.22529598914287,
37.505990032542));
#22747=CARTESIAN_POINT('Ctrl Pts',(0.265998739668756,-3.21593028080837,
37.5154334030571));
#22748=CARTESIAN_POINT('Ctrl Pts',(0.450099879470417,-3.19123917122849,
37.5266056965123));
#22749=CARTESIAN_POINT('Ctrl Pts',(0.47177886739132,-3.18810633660193,37.5279298974547));
#22750=CARTESIAN_POINT('Ctrl Pts',(0.506362463765492,-3.1827481905488,37.530056797019));
#22751=CARTESIAN_POINT('Ctrl Pts',(0.519288604395263,-3.18066476173729,
37.5308549945278));
#22752=CARTESIAN_POINT('Ctrl Pts',(0.542142228265927,-3.17683820086012,
37.5322720981139));
#22753=CARTESIAN_POINT('Ctrl Pts',(0.552074959888118,-3.17512714471595,
37.5328899751805));
#22754=CARTESIAN_POINT('Ctrl Pts',(0.572681199104011,-3.17147780788289,
37.534175972722));
#22755=CARTESIAN_POINT('Ctrl Pts',(0.58335325957357,-3.16953217551716,37.5348443208466));
#22756=CARTESIAN_POINT('Ctrl Pts',(0.610891962848549,-3.16436777485636,
37.5365750642616));
#22757=CARTESIAN_POINT('Ctrl Pts',(0.627742901766128,-3.16106805300211,
37.5376400362361));
#22758=CARTESIAN_POINT('Ctrl Pts',(0.699516743483176,-3.14641689040722,
37.5422019819395));
#22759=CARTESIAN_POINT('Ctrl Pts',(0.754161905297265,-3.1337680363353,37.5457402667464));
#22760=CARTESIAN_POINT('Ctrl Pts',(0.897409856562916,-3.09664642239335,
37.555194229315));
#22761=CARTESIAN_POINT('Ctrl Pts',(0.98533890770676,-3.06979937999765,37.5611815026519));
#22762=CARTESIAN_POINT('Ctrl Pts',(1.2095339777098,-2.99072159863251,37.5769081150617));
#22763=CARTESIAN_POINT('Ctrl Pts',(1.34361342306006,-2.93293127891763,37.5867751799219));
#22764=CARTESIAN_POINT('Ctrl Pts',(1.64055446299926,-2.78029852200403,37.6093749174947));
#22765=CARTESIAN_POINT('Ctrl Pts',(1.79997494065692,-2.67984805879226,37.6220741106077));
#22766=CARTESIAN_POINT('Ctrl Pts',(1.9613994561847,-2.55719460177184,37.6349237909817));
#22767=CARTESIAN_POINT('Ctrl Pts',(1.97300052435852,-2.54825450221348,37.6358470784723));
#22768=CARTESIAN_POINT('Ctrl Pts',(1.99015393674327,-2.53484824568232,37.6372114851217));
#22769=CARTESIAN_POINT('Ctrl Pts',(1.99575287536791,-2.53044240862144,37.637656708983));
#22770=CARTESIAN_POINT('Ctrl Pts',(2.00571489348871,-2.5225496074878,37.6384485903369));
#22771=CARTESIAN_POINT('Ctrl Pts',(2.01008355105668,-2.51906984333524,37.6387957505675));
#22772=CARTESIAN_POINT('Ctrl Pts',(2.01446052691476,-2.51556481699289,37.6391434612459));
#22773=CARTESIAN_POINT('Ctrl Pts',(2.01447780796669,-2.51555097825504,37.6391448340657));
#22774=CARTESIAN_POINT('Ctrl Pts',(2.01451209387071,-2.51552352138144,37.6391475577606));
#22775=CARTESIAN_POINT('Ctrl Pts',(2.01452909869127,-2.5155099032802,37.6391489086332));
#22776=CARTESIAN_POINT('Ctrl Pts',(2.0145628373658,-2.51548288351646,37.6391515888495));
#22777=CARTESIAN_POINT('Ctrl Pts',(2.01457957132563,-2.51546948177812,37.6391529182017));
#22778=CARTESIAN_POINT('Ctrl Pts',(2.01461277389525,-2.51544289026868,37.6391555558235));
#22779=CARTESIAN_POINT('Ctrl Pts',(2.01462924241462,-2.51542970057863,37.639156864086));
#22780=CARTESIAN_POINT('Ctrl Pts',(2.0146619193043,-2.51540352902598,37.6391594599418));
#22781=CARTESIAN_POINT('Ctrl Pts',(2.01467812761216,-2.51539054722172,37.6391607475302));
#22782=CARTESIAN_POINT('Ctrl Pts',(2.01471028907978,-2.51536478746003,37.6391633024351));
#22783=CARTESIAN_POINT('Ctrl Pts',(2.01472624225204,-2.51535200950061,37.6391645697527));
#22784=CARTESIAN_POINT('Ctrl Pts',(2.01972807099056,-2.51134563322859,37.6395619138407));
#22785=CARTESIAN_POINT('Ctrl Pts',(2.02470211271556,-2.50733717850673,37.6399569153863));
#22786=CARTESIAN_POINT('Ctrl Pts',(2.03827249452963,-2.49633443583687,37.6410343068212));
#22787=CARTESIAN_POINT('Ctrl Pts',(2.04684482313504,-2.48931047799182,37.6417145931564));
#22788=CARTESIAN_POINT('Ctrl Pts',(2.06606395237776,-2.47339638665036,37.6432395665484));
#22789=CARTESIAN_POINT('Ctrl Pts',(2.07669000471623,-2.4644814019076,37.6440825502383));
#22790=CARTESIAN_POINT('Ctrl Pts',(2.10951810837679,-2.43657637541224,37.6466875629647));
#22791=CARTESIAN_POINT('Ctrl Pts',(2.13152033616147,-2.41735232524608,37.6484345170127));
#22792=CARTESIAN_POINT('Ctrl Pts',(2.21662868366218,-2.34092479432583,37.6552100180404));
#22793=CARTESIAN_POINT('Ctrl Pts',(2.277722411028,-2.28152455949615,37.6601136487935));
#22794=CARTESIAN_POINT('Ctrl Pts',(2.47910493352838,-2.06956152673026,37.6767133184336));
#22795=CARTESIAN_POINT('Ctrl Pts',(2.60699792545665,-1.90594121404209,37.6880679711775));
#22796=CARTESIAN_POINT('Ctrl Pts',(2.79364918059233,-1.61285988383586,37.7078258502478));
#22797=CARTESIAN_POINT('Ctrl Pts',(2.86118440054439,-1.48976823541654,37.7159683100511));
#22798=CARTESIAN_POINT('Ctrl Pts',(2.92950456987935,-1.3433449777783,37.7256914787533));
#22799=CARTESIAN_POINT('Ctrl Pts',(2.93833337958235,-1.32392207894861,37.7269817553788));
#22800=CARTESIAN_POINT('Ctrl Pts',(2.95220046439086,-1.29259315699834,37.7290644168006));
#22801=CARTESIAN_POINT('Ctrl Pts',(2.9573611778658,-1.28074178017141,37.7298525949595));
#22802=CARTESIAN_POINT('Ctrl Pts',(2.96640875182672,-1.25961809982176,37.7312581549325));
#22803=CARTESIAN_POINT('Ctrl Pts',(2.97032380494049,-1.25035800092514,37.7318745637));
#22804=CARTESIAN_POINT('Ctrl Pts',(2.97840216178564,-1.23099855951164,37.7331638276924));
#22805=CARTESIAN_POINT('Ctrl Pts',(2.98255756835005,-1.22089607977979,37.7338369421164));
#22806=CARTESIAN_POINT('Ctrl Pts',(2.99324152136314,-1.19454154661972,37.7355938605544));
#22807=CARTESIAN_POINT('Ctrl Pts',(2.9996890194264,-1.17825722107829,37.7366803906561));
#22808=CARTESIAN_POINT('Ctrl Pts',(3.02738045597171,-1.10661678915694,37.7414651034141));
#22809=CARTESIAN_POINT('Ctrl Pts',(3.04722600175411,-1.05073597301318,37.745209778755));
#22810=CARTESIAN_POINT('Ctrl Pts',(3.09618601212435,-0.899794217254751,
37.7553646995311));
#22811=CARTESIAN_POINT('Ctrl Pts',(3.12246079401988,-0.803886135467158,
37.7618604483947));
#22812=CARTESIAN_POINT('Ctrl Pts',(3.19655906508416,-0.474311713053508,
37.7842838470966));
#22813=CARTESIAN_POINT('Ctrl Pts',(3.22287775861272,-0.236643276283802,
37.8006859445876));
#22814=CARTESIAN_POINT('Ctrl Pts',(3.22274953375635,0.00173354353987881,
37.8165056021994));
#22815=CARTESIAN_POINT('Ctrl Pts',(3.222749531205,0.00173828016955539,37.8165059165414));
#22816=CARTESIAN_POINT('Ctrl Pts',(3.22270305071438,0.0879125241068303,
37.8222247873387));
#22817=CARTESIAN_POINT('Ctrl Pts',(3.21920019789002,0.174060452734954,37.8278510718186));
#22818=CARTESIAN_POINT('Ctrl Pts',(3.2114797988416,0.269454144514142,37.8339081349421));
#22819=CARTESIAN_POINT('Ctrl Pts',(3.21067053001022,0.278931510071132,37.8345079924864));
#22820=CARTESIAN_POINT('Ctrl Pts',(3.2092464328258,0.294781062059853,37.8355078136478));
#22821=CARTESIAN_POINT('Ctrl Pts',(3.20865456251314,0.301155178058178,37.835908996707));
#22822=CARTESIAN_POINT('Ctrl Pts',(3.20754096814088,0.312771891365883,37.8366384362922));
#22823=CARTESIAN_POINT('Ctrl Pts',(3.2070253751692,0.318015034703768,37.836967029785));
#22824=CARTESIAN_POINT('Ctrl Pts',(3.20593683907471,0.328812599313765,37.8376423829336));
#22825=CARTESIAN_POINT('Ctrl Pts',(3.20536232519363,0.334366724584944,37.8379890372753));
#22826=CARTESIAN_POINT('Ctrl Pts',(3.20402360875131,0.346988193085497,37.8387751375784));
#22827=CARTESIAN_POINT('Ctrl Pts',(3.20325045895787,0.354054502934622,37.8392140737816));
#22828=CARTESIAN_POINT('Ctrl Pts',(3.20118373404302,0.372382545982474,37.8403496410081));
#22829=CARTESIAN_POINT('Ctrl Pts',(3.19985409722441,0.383640228532662,37.8410442892656));
#22830=CARTESIAN_POINT('Ctrl Pts',(3.19108503739539,0.454666263385874,37.8454102006503));
#22831=CARTESIAN_POINT('Ctrl Pts',(3.1820302095878,0.514227520546008,37.8489966822654));
#22832=CARTESIAN_POINT('Ctrl Pts',(3.16366679900411,0.615771813209107,37.8550362213012));
#22833=CARTESIAN_POINT('Ctrl Pts',(3.1551785212053,0.657883962557299,37.8575185671406));
#22834=CARTESIAN_POINT('Ctrl Pts',(3.09705571057058,0.919161018413947,37.8728485623131));
#22835=CARTESIAN_POINT('Ctrl Pts',(3.02545318345635,1.13280770928991,37.8851126266627));
#22836=CARTESIAN_POINT('Ctrl Pts',(2.89150874849534,1.42650354757404,37.9034389615986));
#22837=CARTESIAN_POINT('Ctrl Pts',(2.84676610907895,1.51382154709284,37.9090837800931));
#22838=CARTESIAN_POINT('Ctrl Pts',(2.76897445235689,1.64995383043231,37.9183162286303));
#22839=CARTESIAN_POINT('Ctrl Pts',(2.73844702740723,1.70013951790317,37.9218187002717));
#22840=CARTESIAN_POINT('Ctrl Pts',(2.69709104329107,1.76412079276401,37.9264275422393));
#22841=CARTESIAN_POINT('Ctrl Pts',(2.68749641232533,1.7787032586588,37.927487903642));
#22842=CARTESIAN_POINT('Ctrl Pts',(2.67171291233598,1.80227265496957,37.9292182942922));
#22843=CARTESIAN_POINT('Ctrl Pts',(2.66559595145052,1.81130749122718,37.9298856027177));
#22844=CARTESIAN_POINT('Ctrl Pts',(2.65375232712182,1.82861075903095,37.9311714103812));
#22845=CARTESIAN_POINT('Ctrl Pts',(2.64803259611736,1.83688379817252,37.9317896403862));
#22846=CARTESIAN_POINT('Ctrl Pts',(2.63485785912359,1.85575036666307,37.9332075188928));
#22847=CARTESIAN_POINT('Ctrl Pts',(2.62737755804495,1.86632594172695,37.9340081330577));
#22848=CARTESIAN_POINT('Ctrl Pts',(2.60735435208714,1.89427559330572,37.9361397271336));
#22849=CARTESIAN_POINT('Ctrl Pts',(2.59470173952829,1.91156992752261,37.9374749398502));
#22850=CARTESIAN_POINT('Ctrl Pts',(2.49592050226965,2.04380213864549,37.9478116764587));
#22851=CARTESIAN_POINT('Ctrl Pts',(2.402379485937,2.15297679446978,37.9571075650017));
#22852=CARTESIAN_POINT('Ctrl Pts',(2.15626158547292,2.40415153159436,37.9804243513077));
#22853=CARTESIAN_POINT('Ctrl Pts',(1.99659451213777,2.53830831002931,37.9946613115335));
#22854=CARTESIAN_POINT('Ctrl Pts',(1.75751803682042,2.70258726230109,38.0141158726067));
#22855=CARTESIAN_POINT('Ctrl Pts',(1.68815084006837,2.74645156053097,38.0195611130074));
#22856=CARTESIAN_POINT('Ctrl Pts',(1.59252827816446,2.80192496797036,38.0267347183051));
#22857=CARTESIAN_POINT('Ctrl Pts',(1.56768624761195,2.81589946415481,38.0285691710128));
#22858=CARTESIAN_POINT('Ctrl Pts',(1.53069724318931,2.8360657951724,38.0312541993667));
#22859=CARTESIAN_POINT('Ctrl Pts',(1.51869179277238,2.84251270853795,38.0321185477782));
#22860=CARTESIAN_POINT('Ctrl Pts',(1.49690928938378,2.85403248933598,38.0336734742623));
#22861=CARTESIAN_POINT('Ctrl Pts',(1.48714650299652,2.85913171395537,38.0343655820304));
#22862=CARTESIAN_POINT('Ctrl Pts',(1.47173453145196,2.86708127940143,38.0354504067361));
#22863=CARTESIAN_POINT('Ctrl Pts',(1.46610287509791,2.86996514874785,38.0358451866311));
#22864=CARTESIAN_POINT('Ctrl Pts',(1.46044796055885,2.87283993937586,38.0362399436139));
#22865=CARTESIAN_POINT('Ctrl Pts',(1.46043321592104,2.87284743496903,38.0362409728929));
#22866=CARTESIAN_POINT('Ctrl Pts',(1.46040364232788,2.87286246873257,38.0362430373144));
#22867=CARTESIAN_POINT('Ctrl Pts',(1.46038881341484,2.8728700068798,38.0362440724538));
#22868=CARTESIAN_POINT('Ctrl Pts',(1.46035907063203,2.87288512607146,38.0362461486401));
#22869=CARTESIAN_POINT('Ctrl Pts',(1.46034415683728,2.87289270707611,38.0362471896817));
#22870=CARTESIAN_POINT('Ctrl Pts',(1.45534669962921,2.87543297376482,38.0365960280181));
#22871=CARTESIAN_POINT('Ctrl Pts',(1.45035764638453,2.87795265786701,38.0369429881896));
#22872=CARTESIAN_POINT('Ctrl Pts',(1.43895354559918,2.88367502743833,38.0377331616025));
#22873=CARTESIAN_POINT('Ctrl Pts',(1.43253436100289,2.88686928646823,38.0381758437417));
#22874=CARTESIAN_POINT('Ctrl Pts',(1.41276385848193,2.89662513128069,38.0395330002227));
#22875=CARTESIAN_POINT('Ctrl Pts',(1.39937750172517,2.90311582586225,38.0404431584222));
#22876=CARTESIAN_POINT('Ctrl Pts',(1.22848058267346,2.9845225447519,38.0519576953124));
#22877=CARTESIAN_POINT('Ctrl Pts',(1.06516083522188,3.04663577192103,38.0618390428793));
#22878=CARTESIAN_POINT('Ctrl Pts',(0.744803845263201,3.1395370959834,38.0805367676056));
#22879=CARTESIAN_POINT('Ctrl Pts',(0.588945809178976,3.17247024686073,38.0893474671676));
#22880=CARTESIAN_POINT('Ctrl Pts',(0.340216192523598,3.20605943601172,38.1036365166495));
#22881=CARTESIAN_POINT('Ctrl Pts',(0.24865913799094,3.21445654336918,38.1089413318794));
#22882=CARTESIAN_POINT('Ctrl Pts',(0.100854190929152,3.2216597544652,38.1176673211599));
#22883=CARTESIAN_POINT('Ctrl Pts',(0.0447762865463718,3.22292687623243,
38.1210150249678));
#22884=CARTESIAN_POINT('Ctrl Pts',(-0.0284747961101848,3.22266994879571,
38.1254477024342));
#22885=CARTESIAN_POINT('Ctrl Pts',(-0.0456448777774604,3.22247248867469,
38.1264909926292));
#22886=CARTESIAN_POINT('Ctrl Pts',(-0.0736583032493643,3.22192639537209,
38.1282004306651));
#22887=CARTESIAN_POINT('Ctrl Pts',(-0.0845030560364107,3.22166020427402,
38.1288639815716));
#22888=CARTESIAN_POINT('Ctrl Pts',(-0.105420791035026,3.22104107495384,
38.1301473820261));
#22889=CARTESIAN_POINT('Ctrl Pts',(-0.115493880682363,3.22069562510396,
38.1307669885861));
#22890=CARTESIAN_POINT('Ctrl Pts',(-0.138648031389127,3.21979280534953,
38.1321949203655));
#22891=CARTESIAN_POINT('Ctrl Pts',(-0.151727580797547,3.21920296332524,
38.1330042578807));
#22892=CARTESIAN_POINT('Ctrl Pts',(-0.18667799869667,3.21741334873613,38.1351743386246));
#22893=CARTESIAN_POINT('Ctrl Pts',(-0.208540539936081,3.21607029412703,
38.1365395609543));
#22894=CARTESIAN_POINT('Ctrl Pts',(-0.393840039733015,3.2027896641646,38.1481785828982));
#22895=CARTESIAN_POINT('Ctrl Pts',(-0.556135396528536,3.17862711579753,
38.158839691741));
#22896=CARTESIAN_POINT('Ctrl Pts',(-0.963423532403372,3.08583802170708,
38.1867004993818));
#22897=CARTESIAN_POINT('Ctrl Pts',(-1.20343252256089,3.00038773177432,38.2042259311353));
#22898=CARTESIAN_POINT('Ctrl Pts',(-1.48147084860564,2.86261145545658,38.2245269036309));
#22899=CARTESIAN_POINT('Ctrl Pts',(-1.53135739624207,2.83623794245424,38.2281651429803));
#22900=CARTESIAN_POINT('Ctrl Pts',(-1.59070494386854,2.80283993168146,38.23246559334));
#22901=CARTESIAN_POINT('Ctrl Pts',(-1.60084970609599,2.79705812049337,38.2331996995365));
#22902=CARTESIAN_POINT('Ctrl Pts',(-1.61659788811844,2.78796900257939,38.2343374472128));
#22903=CARTESIAN_POINT('Ctrl Pts',(-1.62222297267421,2.78469971808759,38.234743470836));
#22904=CARTESIAN_POINT('Ctrl Pts',(-1.63265481793771,2.77859442066814,38.2354957100871));
#22905=CARTESIAN_POINT('Ctrl Pts',(-1.6374640662122,2.77576298370083,38.2358422041996));
#22906=CARTESIAN_POINT('Ctrl Pts',(-1.64835086985035,2.76931525549814,38.2366259119493));
#22907=CARTESIAN_POINT('Ctrl Pts',(-1.65442387733516,2.76569145257135,38.2370626284957));
#22908=CARTESIAN_POINT('Ctrl Pts',(-1.67241077076626,2.75487811040467,38.2383548667934));
#22909=CARTESIAN_POINT('Ctrl Pts',(-1.68429025628301,2.74763125949393,38.2392067355982));
#22910=CARTESIAN_POINT('Ctrl Pts',(-1.77405206577623,2.6920728820386,38.2456342994269));
#22911=CARTESIAN_POINT('Ctrl Pts',(-1.84989646459654,2.64053092553442,38.2510129042002));
#22912=CARTESIAN_POINT('Ctrl Pts',(-2.11863128812539,2.44063412914987,38.2702723580079));
#22913=CARTESIAN_POINT('Ctrl Pts',(-2.29675611581672,2.27381134942314,38.2834955770402));
#22914=CARTESIAN_POINT('Ctrl Pts',(-2.51395734354943,2.01855791224649,38.3025768798924));
#22915=CARTESIAN_POINT('Ctrl Pts',(-2.57047107878271,1.94608172400177,38.3078797114441));
#22916=CARTESIAN_POINT('Ctrl Pts',(-2.65636616807812,1.82564513694718,38.3166027355812));
#22917=CARTESIAN_POINT('Ctrl Pts',(-2.68772469930393,1.77915619050023,38.3199495233266));
#22918=CARTESIAN_POINT('Ctrl Pts',(-2.72708003359799,1.71739536630857,38.3243811566818));
#22919=CARTESIAN_POINT('Ctrl Pts',(-2.7361907508879,1.70284247976019,38.3254243437838));
#22920=CARTESIAN_POINT('Ctrl Pts',(-2.7508671015084,1.6789774937446,38.3271336554537));
#22921=CARTESIAN_POINT('Ctrl Pts',(-2.75650284633126,1.66970874354773,38.3277971838302));
#22922=CARTESIAN_POINT('Ctrl Pts',(-2.76728459198546,1.65177333175417,38.3290805706059));
#22923=CARTESIAN_POINT('Ctrl Pts',(-2.77243694752018,1.64311062344441,38.3297001861775));
#22924=CARTESIAN_POINT('Ctrl Pts',(-2.78418905852207,1.62313902526471,38.3311281815928));
#22925=CARTESIAN_POINT('Ctrl Pts',(-2.79076066565264,1.61181385644982,38.3319375740255));
#22926=CARTESIAN_POINT('Ctrl Pts',(-2.80814204631419,1.58143470015158,38.3341078974175));
#22927=CARTESIAN_POINT('Ctrl Pts',(-2.81882671262365,1.56231027297562,38.3354733090496));
#22928=CARTESIAN_POINT('Ctrl Pts',(-2.90785048558914,1.39908054498373,38.3471219503244));
#22929=CARTESIAN_POINT('Ctrl Pts',(-2.97526571064352,1.24931983145554,38.3577932298352));
#22930=CARTESIAN_POINT('Ctrl Pts',(-3.11736683285141,0.856016445185154,
38.3856860239903));
#22931=CARTESIAN_POINT('Ctrl Pts',(-3.17515349537329,0.607565359259412,
38.4032339399794));
#22932=CARTESIAN_POINT('Ctrl Pts',(-3.2093141222477,0.29925852843585,38.4235230123581));
#22933=CARTESIAN_POINT('Ctrl Pts',(-3.2140294884054,0.243450512011036,38.4271333905509));
#22934=CARTESIAN_POINT('Ctrl Pts',(-3.21796642475436,0.175913030632564,
38.4314054360352));
#22935=CARTESIAN_POINT('Ctrl Pts',(-3.2185813674084,0.164278106729677,38.4321379173505));
#22936=CARTESIAN_POINT('Ctrl Pts',(-3.21944109407276,0.14614670904612,38.4332736998765));
#22937=CARTESIAN_POINT('Ctrl Pts',(-3.21972933480573,0.13965253715186,38.4336793702184));
#22938=CARTESIAN_POINT('Ctrl Pts',(-3.22022854344607,0.127580733825581,
38.4344312904788));
#22939=CARTESIAN_POINT('Ctrl Pts',(-3.22044466915152,0.122003480728437,
38.4347778167768));
#22940=CARTESIAN_POINT('Ctrl Pts',(-3.22090206691413,0.109350619653088,
38.4355620247485));
#22941=CARTESIAN_POINT('Ctrl Pts',(-3.22113451361212,0.102274777662503,
38.4359992066737));
#22942=CARTESIAN_POINT('Ctrl Pts',(-3.22175574471678,0.0812533720824494,
38.4372941009502));
#22943=CARTESIAN_POINT('Ctrl Pts',(-3.22207730168362,0.0673057752632883,
38.4381481380415));
#22944=CARTESIAN_POINT('Ctrl Pts',(-3.2238434874023,-0.0393583179198146,
38.4446432329982));
#22945=CARTESIAN_POINT('Ctrl Pts',(-3.22137664547639,-0.132105592091975,
38.450082489086));
#22946=CARTESIAN_POINT('Ctrl Pts',(-3.19805036666433,-0.465958016293262,
38.4693168858473));
#22947=CARTESIAN_POINT('Ctrl Pts',(-3.15406885139023,-0.704631435494986,
38.4824714164184));
#22948=CARTESIAN_POINT('Ctrl Pts',(-3.05706370892876,-1.02417925709542,
38.5014826397379));
#22949=CARTESIAN_POINT('Ctrl Pts',(-3.02658375078057,-1.11102229362385,
38.5067927171475));
#22950=CARTESIAN_POINT('Ctrl Pts',(-2.97159564421363,-1.24855401512394,
38.5155265714249));
#22951=CARTESIAN_POINT('Ctrl Pts',(-2.94940177372226,-1.30011399551361,
38.5188767044753));
#22952=CARTESIAN_POINT('Ctrl Pts',(-2.91867338573031,-1.36665951756177,
38.5233121509282));
#22953=CARTESIAN_POINT('Ctrl Pts',(-2.91134839518326,-1.38219502010771,
38.524355714684));
#22954=CARTESIAN_POINT('Ctrl Pts',(-2.89919456199872,-1.40744667972448,
38.5260654882481));
#22955=CARTESIAN_POINT('Ctrl Pts',(-2.89444015800656,-1.4171984447344,38.5267290991531));
#22956=CARTESIAN_POINT('Ctrl Pts',(-2.88517414570637,-1.43596284469021,
38.5280125364984));
#22957=CARTESIAN_POINT('Ctrl Pts',(-2.88066931434218,-1.44497869884218,
38.5286321195248));
#22958=CARTESIAN_POINT('Ctrl Pts',(-2.87021637655335,-1.46565578401377,
38.5300598836095));
#22959=CARTESIAN_POINT('Ctrl Pts',(-2.86423939276216,-1.47730214183485,
38.5308690761878));
#22960=CARTESIAN_POINT('Ctrl Pts',(-2.84807586046103,-1.50833049362682,
38.5330385159032));
#22961=CARTESIAN_POINT('Ctrl Pts',(-2.83776260141139,-1.52764536616261,
38.5344032379863));
#22962=CARTESIAN_POINT('Ctrl Pts',(-2.74878830991491,-1.69026769387256,
38.5460168899577));
#22963=CARTESIAN_POINT('Ctrl Pts',(-2.65953734574309,-1.82748148231766,
38.5566511793456));
#22964=CARTESIAN_POINT('Ctrl Pts',(-2.40655797962761,-2.15839222672096,
38.5844296518019));
#22965=CARTESIAN_POINT('Ctrl Pts',(-2.22969529378452,-2.34064781176811,
38.6018979557191));
#22966=CARTESIAN_POINT('Ctrl Pts',(-1.98872409105201,-2.53661202819307,
38.6222302776015));
#22967=CARTESIAN_POINT('Ctrl Pts',(-1.9431451261639,-2.57169439898932,38.6259403739221));
#22968=CARTESIAN_POINT('Ctrl Pts',(-1.88715595583454,-2.61245053861243,
38.6303139793726));
#22969=CARTESIAN_POINT('Ctrl Pts',(-1.87762552175141,-2.61930865466757,
38.6310522071538));
#22970=CARTESIAN_POINT('Ctrl Pts',(-1.86274457894569,-2.62989404893614,
38.6321949382655));
#22971=CARTESIAN_POINT('Ctrl Pts',(-1.85741999614261,-2.63365734953099,
38.632601856881));
#22972=CARTESIAN_POINT('Ctrl Pts',(-1.8475178844385,-2.64061098230092,38.6333549080475));
#22973=CARTESIAN_POINT('Ctrl Pts',(-1.84294353429229,-2.64380555701761,
38.6337013244089));
#22974=CARTESIAN_POINT('Ctrl Pts',(-1.83256804051393,-2.65101144490501,
38.6344837827721));
#22975=CARTESIAN_POINT('Ctrl Pts',(-1.82676202617466,-2.65501559432157,
38.6349193343374));
#22976=CARTESIAN_POINT('Ctrl Pts',(-1.8095358930443,-2.66681243362961,38.6362049378037));
#22977=CARTESIAN_POINT('Ctrl Pts',(-1.79807855029821,-2.67455084962485,
38.6370513921887));
#22978=CARTESIAN_POINT('Ctrl Pts',(-1.7124328785458,-2.73159776516563,38.6433177517081));
#22979=CARTESIAN_POINT('Ctrl Pts',(-1.63627114840698,-2.77788994748917,
38.6485515707677));
#22980=CARTESIAN_POINT('Ctrl Pts',(-1.53081351430991,-2.83614391159488,
38.6554881361776));
#22981=CARTESIAN_POINT('Ctrl Pts',(-1.5031349093025,-2.85090973729773,38.6572808675935));
#22982=CARTESIAN_POINT('Ctrl Pts',(-1.47525532932069,-2.86526425933297,
38.6590632205222));
#22983=CARTESIAN_POINT('Origin',(0.,0.,4.68922655072688));
#22984=CARTESIAN_POINT('',(-1.47525550050006,-2.86526417119684,40.1544081509837));
#22985=CARTESIAN_POINT('',(-1.47525529542902,-2.86526427678297,39.904468116039));
#22986=CARTESIAN_POINT('',(-1.47525540501186,-2.86526422036142,4.68922655072688));
#22987=CARTESIAN_POINT('Ctrl Pts',(-1.47525550050006,-2.86526417119684,
40.1544081509837));
#22988=CARTESIAN_POINT('Ctrl Pts',(-1.5257082871409,-2.8392872467109,40.1512214838131));
#22989=CARTESIAN_POINT('Ctrl Pts',(-1.57548102869782,-2.81197460503496,
40.1480187586786));
#22990=CARTESIAN_POINT('Ctrl Pts',(-1.70398379898398,-2.73697318973332,
40.1395483182983));
#22991=CARTESIAN_POINT('Ctrl Pts',(-1.78141930899777,-2.6872153505836,40.1342378046197));
#22992=CARTESIAN_POINT('Ctrl Pts',(-1.90249889118442,-2.60187749789188,
40.1255031209275));
#22993=CARTESIAN_POINT('Ctrl Pts',(-1.94752644469264,-2.56834746770252,
40.1221525928023));
#22994=CARTESIAN_POINT('Ctrl Pts',(-2.00516054531332,-2.52304259246607,
40.1177164499752));
#22995=CARTESIAN_POINT('Ctrl Pts',(-2.01858226143142,-2.51231733105785,
40.1166725905314));
#22996=CARTESIAN_POINT('Ctrl Pts',(-2.04034132069919,-2.49464278845382,
40.1149622859871));
#22997=CARTESIAN_POINT('Ctrl Pts',(-2.04873056051132,-2.48775771183767,
40.1142984409028));
#22998=CARTESIAN_POINT('Ctrl Pts',(-2.06484634333585,-2.47439463355507,
40.1130145170621));
#22999=CARTESIAN_POINT('Ctrl Pts',(-2.07257758695582,-2.46792247984304,
40.1123946817282));
#23000=CARTESIAN_POINT('Ctrl Pts',(-2.09028095968121,-2.452960373389,40.1109662868802));
#23001=CARTESIAN_POINT('Ctrl Pts',(-2.10023191145538,-2.44444574367854,
40.1101567147658));
#23002=CARTESIAN_POINT('Ctrl Pts',(-2.12668913652012,-2.42152654799782,
40.1079861441118));
#23003=CARTESIAN_POINT('Ctrl Pts',(-2.14310066686595,-2.40701412531151,
40.1066206654441));
#23004=CARTESIAN_POINT('Ctrl Pts',(-2.28092614532539,-2.2826105235455,40.0949883346007));
#23005=CARTESIAN_POINT('Ctrl Pts',(-2.39393054758166,-2.1637968376173,40.084334731861));
#23006=CARTESIAN_POINT('Ctrl Pts',(-2.65772228599949,-1.84037116950742,
40.0564985965985));
#23007=CARTESIAN_POINT('Ctrl Pts',(-2.79426555286322,-1.62558571381885,
40.03899084047));
#23008=CARTESIAN_POINT('Ctrl Pts',(-2.92884012435285,-1.34582337006906,
40.018675713813));
#23009=CARTESIAN_POINT('Ctrl Pts',(-2.95211062396424,-1.29398176979983,
40.0150113002094));
#23010=CARTESIAN_POINT('Ctrl Pts',(-2.97850814812233,-1.23074925183527,
40.0106840442302));
#23011=CARTESIAN_POINT('Ctrl Pts',(-2.98295767820349,-1.21992541136176,
40.0099482798543));
#23012=CARTESIAN_POINT('Ctrl Pts',(-2.98979164271471,-1.20304027883689,
40.0088084576044));
#23013=CARTESIAN_POINT('Ctrl Pts',(-2.99221677429015,-1.19699572129119,
40.0084020044186));
#23014=CARTESIAN_POINT('Ctrl Pts',(-2.99668629148706,-1.18575713745136,
40.0076492799604));
#23015=CARTESIAN_POINT('Ctrl Pts',(-2.99873548786116,-1.18056520072981,
40.0073027280715));
#23016=CARTESIAN_POINT('Ctrl Pts',(-3.00334855925941,-1.16878780518274,
40.006519274946));
#23017=CARTESIAN_POINT('Ctrl Pts',(-3.00590426267253,-1.16219923758535,
40.0060828687203));
#23018=CARTESIAN_POINT('Ctrl Pts',(-3.01341777011743,-1.14263894015396,
40.0047926628828));
#23019=CARTESIAN_POINT('Ctrl Pts',(-3.01831350196856,-1.1296433174915,40.0039424989481));
#23020=CARTESIAN_POINT('Ctrl Pts',(-3.0545723447766,-1.03147617453332,39.9975704414923));
#23021=CARTESIAN_POINT('Ctrl Pts',(-3.08241199747418,-0.945036964367656,
39.9922418278056));
#23022=CARTESIAN_POINT('Ctrl Pts',(-3.17159661621014,-0.621948371578699,
39.9729602834399));
#23023=CARTESIAN_POINT('Ctrl Pts',(-3.2096208052385,-0.379727239062099,
39.9596794192817));
#23024=CARTESIAN_POINT('Ctrl Pts',(-3.2237571068219,-0.0438641655779862,
39.9405401526686));
#23025=CARTESIAN_POINT('Ctrl Pts',(-3.22369918435547,0.0479123905017251,
39.9352445049471));
#23026=CARTESIAN_POINT('Ctrl Pts',(-3.21730122645842,0.195520289011085,
39.9265320649528));
#23027=CARTESIAN_POINT('Ctrl Pts',(-3.21341697581568,0.251408294879304,
39.9231884468364));
#23028=CARTESIAN_POINT('Ctrl Pts',(-3.20644239769175,0.32425203327463,39.9187602840505));
#23029=CARTESIAN_POINT('Ctrl Pts',(-3.20466981922349,0.341326182438772,
39.9177173160471));
#23030=CARTESIAN_POINT('Ctrl Pts',(-3.2015545501712,0.369166240464658,39.9160081803709));
#23031=CARTESIAN_POINT('Ctrl Pts',(-3.20029373615862,0.379941111980566,
39.9153446071768));
#23032=CARTESIAN_POINT('Ctrl Pts',(-3.19775627028726,0.400716913116977,
39.9140610049007));
#23033=CARTESIAN_POINT('Ctrl Pts',(-3.19648704179784,0.410718634287481,
39.9134412180959));
#23034=CARTESIAN_POINT('Ctrl Pts',(-3.19346072759143,0.433702389973712,
39.9120126428223));
#23035=CARTESIAN_POINT('Ctrl Pts',(-3.19167138261563,0.44667992901306,39.9112028399393));
#23036=CARTESIAN_POINT('Ctrl Pts',(-3.18667602231112,0.481346201813041,
39.9090310010592));
#23037=CARTESIAN_POINT('Ctrl Pts',(-3.18332776837149,0.503013437111399,
39.9076644751009));
#23038=CARTESIAN_POINT('Ctrl Pts',(-3.1529390337906,0.687193131615201,39.8959691767041));
#23039=CARTESIAN_POINT('Ctrl Pts',(-3.11369923127039,0.847420280484252,
39.8852487209386));
#23040=CARTESIAN_POINT('Ctrl Pts',(-2.982657886704,1.24715090349905,39.8571851329669));
#23041=CARTESIAN_POINT('Ctrl Pts',(-2.87423617645597,1.47999848744319,39.8395110927366));
#23042=CARTESIAN_POINT('Ctrl Pts',(-2.71109840758028,1.74325926402472,39.8192791525069));
#23043=CARTESIAN_POINT('Ctrl Pts',(-2.68164099980509,1.78824209509877,39.8158162712529));
#23044=CARTESIAN_POINT('Ctrl Pts',(-2.64452351388311,1.8419406886083,39.811694889188));
#23045=CARTESIAN_POINT('Ctrl Pts',(-2.6379262467113,1.85137658033043,39.810971164671));
#23046=CARTESIAN_POINT('Ctrl Pts',(-2.62754202477367,1.86606064944886,39.8098459257176));
#23047=CARTESIAN_POINT('Ctrl Pts',(-2.62378966730064,1.87133300694688,39.8094421117172));
#23048=CARTESIAN_POINT('Ctrl Pts',(-2.61676823700227,1.88113603144475,39.8086917309303));
#23049=CARTESIAN_POINT('Ctrl Pts',(-2.61350329829536,1.88566945285615,39.8083448994666));
#23050=CARTESIAN_POINT('Ctrl Pts',(-2.60604731567502,1.89596564395544,39.8075575760942));
#23051=CARTESIAN_POINT('Ctrl Pts',(-2.60184894692927,1.90172300671287,39.8071175994328));
#23052=CARTESIAN_POINT('Ctrl Pts',(-2.59089152781911,1.91664507075308,39.8059778363865));
#23053=CARTESIAN_POINT('Ctrl Pts',(-2.58410286833128,1.92578804934161,39.8052800560322));
#23054=CARTESIAN_POINT('Ctrl Pts',(-2.54064840413865,1.98366907269412,39.8008649353722));
#23055=CARTESIAN_POINT('Ctrl Pts',(-2.50265108634127,2.03139753663881,39.7972345456825));
#23056=CARTESIAN_POINT('Ctrl Pts',(-2.44044027409346,2.10514318475714,39.7915905494667));
#23057=CARTESIAN_POINT('Ctrl Pts',(-2.41711427567274,2.13188538445169,39.7895363013204));
#23058=CARTESIAN_POINT('Ctrl Pts',(-2.23235480650211,2.33677208746604,39.7736894504789));
#23059=CARTESIAN_POINT('Ctrl Pts',(-2.05188364839378,2.49673737195673,39.7606126207799));
#23060=CARTESIAN_POINT('Ctrl Pts',(-1.77996205678656,2.68818524884868,39.7416817160656));
#23061=CARTESIAN_POINT('Ctrl Pts',(-1.70239841574455,2.7379632119031,39.7363646873085));
#23062=CARTESIAN_POINT('Ctrl Pts',(-1.57426976687456,2.81264096923382,39.7276201671238));
#23063=CARTESIAN_POINT('Ctrl Pts',(-1.52499706432151,2.8396580596163,39.7242665377114));
#23064=CARTESIAN_POINT('Ctrl Pts',(-1.45976460611466,2.87323863308815,39.7198268408919));
#23065=CARTESIAN_POINT('Ctrl Pts',(-1.44442125890776,2.88098249855008,39.7187826140009));
#23066=CARTESIAN_POINT('Ctrl Pts',(-1.41928793491564,2.89341617104172,39.7170718468481));
#23067=CARTESIAN_POINT('Ctrl Pts',(-1.4095347794069,2.89817996027282,39.7164079091796));
#23068=CARTESIAN_POINT('Ctrl Pts',(-1.39067592923892,2.90727358209375,39.7151239040334));
#23069=CARTESIAN_POINT('Ctrl Pts',(-1.38157360341922,2.91161013804268,39.7145040805141));
#23070=CARTESIAN_POINT('Ctrl Pts',(-1.36060372019867,2.92148019611838,39.7130758525399));
#23071=CARTESIAN_POINT('Ctrl Pts',(-1.34872254904603,2.92698419833303,39.7122664364141));
#23072=CARTESIAN_POINT('Ctrl Pts',(-1.31688253718308,2.94149919157231,39.7100965912793));
#23073=CARTESIAN_POINT('Ctrl Pts',(-1.29686511248134,2.95037928960949,39.7087316871857));
#23074=CARTESIAN_POINT('Ctrl Pts',(-1.12678705061772,3.02376378366411,39.6971265634845));
#23075=CARTESIAN_POINT('Ctrl Pts',(-0.972136342063126,3.07696812766912,
39.6865017053639));
#23076=CARTESIAN_POINT('Ctrl Pts',(-0.569019987400004,3.18221836682201,
39.6587180081901));
#23077=CARTESIAN_POINT('Ctrl Pts',(-0.317221819917639,3.21708917067282,
39.6412330911143));
#23078=CARTESIAN_POINT('Ctrl Pts',(-0.00658281150906346,3.22325392202767,
39.6208953911145));
#23079=CARTESIAN_POINT('Ctrl Pts',(0.0508030176557234,3.2228604061706,39.6171938793897));
#23080=CARTESIAN_POINT('Ctrl Pts',(0.119882245504012,3.22054088160411,39.6128287660732));
#23081=CARTESIAN_POINT('Ctrl Pts',(0.131610745624033,3.2200829095702,39.6120907984698));
#23082=CARTESIAN_POINT('Ctrl Pts',(0.149851292117261,3.21927082999772,39.610948270807));
#23083=CARTESIAN_POINT('Ctrl Pts',(0.15636506478163,3.21896102103265,39.6105412983858));
#23084=CARTESIAN_POINT('Ctrl Pts',(0.16845275427524,3.21834932697459,39.6097880407386));
#23085=CARTESIAN_POINT('Ctrl Pts',(0.174026775514854,3.21805273465272,39.6094414721545));
#23086=CARTESIAN_POINT('Ctrl Pts',(0.186647547058653,3.21734829889903,39.6086585176762));
#23087=CARTESIAN_POINT('Ctrl Pts',(0.193693727429667,3.21693178750267,39.6082226235358));
#23088=CARTESIAN_POINT('Ctrl Pts',(0.214556191184979,3.21562977872989,39.6069355119538));
#23089=CARTESIAN_POINT('Ctrl Pts',(0.228368408307645,3.21467838501386,39.6060879031744));
#23090=CARTESIAN_POINT('Ctrl Pts',(0.331437645587854,3.2069112607229,39.5997939293242));
#23091=CARTESIAN_POINT('Ctrl Pts',(0.42039097614108,3.19646763357667,39.5945354862197));
#23092=CARTESIAN_POINT('Ctrl Pts',(0.75171772543088,3.14349398231313,39.5752210712554));
#23093=CARTESIAN_POINT('Ctrl Pts',(0.989396096321654,3.07696985649079,39.5618576085669));
#23094=CARTESIAN_POINT('Ctrl Pts',(1.30196420350957,2.94947227069157,39.5426359611814));
#23095=CARTESIAN_POINT('Ctrl Pts',(1.38520845091741,2.91130436409413,39.5373512666229));
#23096=CARTESIAN_POINT('Ctrl Pts',(1.51651347907473,2.84419279245851,39.5286551452488));
#23097=CARTESIAN_POINT('Ctrl Pts',(1.56564228290785,2.81744732754238,39.5253165195216));
#23098=CARTESIAN_POINT('Ctrl Pts',(1.62889912782115,2.7808451209106,39.5208939676828));
#23099=CARTESIAN_POINT('Ctrl Pts',(1.64368096504025,2.77213362278265,39.519851476176));
#23100=CARTESIAN_POINT('Ctrl Pts',(1.6676934405881,2.7577225786824,39.5181428666633));
#23101=CARTESIAN_POINT('Ctrl Pts',(1.67696623195043,2.75209365485684,39.5174793390619));
#23102=CARTESIAN_POINT('Ctrl Pts',(1.69480401143186,2.74114184513632,39.5161956452952));
#23103=CARTESIAN_POINT('Ctrl Pts',(1.70337279269542,2.73582535585494,39.5155757204777));
#23104=CARTESIAN_POINT('Ctrl Pts',(1.72302158940155,2.72350619016021,39.5141465684993));
#23105=CARTESIAN_POINT('Ctrl Pts',(1.73408406062812,2.71647599435393,39.5133363250114));
#23106=CARTESIAN_POINT('Ctrl Pts',(1.76355271055686,2.69749531897932,39.5111627261614));
#23107=CARTESIAN_POINT('Ctrl Pts',(1.78187997285332,2.68542415321924,39.5097948706838));
#23108=CARTESIAN_POINT('Ctrl Pts',(1.93754087978799,2.58060375725869,39.4980370896905));
#23109=CARTESIAN_POINT('Ctrl Pts',(2.06763348275666,2.47759097241901,39.4872506874491));
#23110=CARTESIAN_POINT('Ctrl Pts',(2.37903539444383,2.18934086152986,39.4589349897228));
#23111=CARTESIAN_POINT('Ctrl Pts',(2.54700423324933,1.99142877288373,39.4410670920848));
#23112=CARTESIAN_POINT('Ctrl Pts',(2.71730081947909,1.73347579528025,39.420914434034));
#23113=CARTESIAN_POINT('Ctrl Pts',(2.74410215972377,1.69072945418358,39.4176698193342));
#23114=CARTESIAN_POINT('Ctrl Pts',(2.7756638746554,1.63766149748852,39.4137727225801));
#23115=CARTESIAN_POINT('Ctrl Pts',(2.78138623733969,1.62792374916509,39.4130629124998));
#23116=CARTESIAN_POINT('Ctrl Pts',(2.79028275332644,1.61260068922477,39.4119544949185));
#23117=CARTESIAN_POINT('Ctrl Pts',(2.79349153540256,1.6070357400336,39.4115536970625));
#23118=CARTESIAN_POINT('Ctrl Pts',(2.79946324941816,1.59660714180388,39.4108059356572));
#23119=CARTESIAN_POINT('Ctrl Pts',(2.80223012713352,1.59174594872404,39.4104587256807));
#23120=CARTESIAN_POINT('Ctrl Pts',(2.80852812601331,1.58061352732041,39.409666652134));
#23121=CARTESIAN_POINT('Ctrl Pts',(2.81205089982569,1.57433766915333,39.4092223285375));
#23122=CARTESIAN_POINT('Ctrl Pts',(2.82285439261683,1.55493917864139,39.4078555611918));
#23123=CARTESIAN_POINT('Ctrl Pts',(2.8300646219203,1.54177723006927,39.4069375215035));
#23124=CARTESIAN_POINT('Ctrl Pts',(2.90383910878204,1.40484377166515,39.3974776304722));
#23125=CARTESIAN_POINT('Ctrl Pts',(2.96234042603946,1.27687786512601,39.3894027369826));
#23126=CARTESIAN_POINT('Ctrl Pts',(3.1085142463978,0.892481908540035,39.3661852721921));
#23127=CARTESIAN_POINT('Ctrl Pts',(3.17246256163294,0.628382129195524,39.3514208794854));
#23128=CARTESIAN_POINT('Ctrl Pts',(3.21022702807425,0.291854640170197,39.3315753933734));
#23129=CARTESIAN_POINT('Ctrl Pts',(3.21566741099104,0.224095523279758,39.3275352790876));
#23130=CARTESIAN_POINT('Ctrl Pts',(3.21985153338909,0.137879565845321,39.3223177686998));
#23131=CARTESIAN_POINT('Ctrl Pts',(3.22058478502712,0.119533646090907,39.3212031576098));
#23132=CARTESIAN_POINT('Ctrl Pts',(3.22151014477212,0.0900747425718642,
39.3194059659622));
#23133=CARTESIAN_POINT('Ctrl Pts',(3.22180160437277,0.0789651144007929,
39.3187265140089));
#23134=CARTESIAN_POINT('Ctrl Pts',(3.22224633524775,0.0578472412051899,
39.3174316687083));
#23135=CARTESIAN_POINT('Ctrl Pts',(3.22241045532736,0.0478393365818509,
39.3168166241478));
#23136=CARTESIAN_POINT('Ctrl Pts',(3.22267799293404,0.0250498448599227,
39.3154127982733));
#23137=CARTESIAN_POINT('Ctrl Pts',(3.22275199573299,0.0122681419001293,
39.3146231015749));
#23138=CARTESIAN_POINT('Ctrl Pts',(3.22274577406068,-0.0267780763807966,
39.3122033488369));
#23139=CARTESIAN_POINT('Ctrl Pts',(3.22242051587675,-0.0530409511759957,
39.3105656360131));
#23140=CARTESIAN_POINT('Ctrl Pts',(3.21657546869301,-0.29052267298961,39.2956612460516));
#23141=CARTESIAN_POINT('Ctrl Pts',(3.19061820458058,-0.500686094542264,
39.2817366890936));
#23142=CARTESIAN_POINT('Ctrl Pts',(3.09075946592093,-0.944944400017209,
39.2510492829271));
#23143=CARTESIAN_POINT('Ctrl Pts',(3.01033022951578,-1.17628252723634,39.2342736439257));
#23144=CARTESIAN_POINT('Ctrl Pts',(2.89512845967804,-1.41591705781204,39.2172917697573));
#23145=CARTESIAN_POINT('Ctrl Pts',(2.88551367160884,-1.43540963624992,39.2159139564565));
#23146=CARTESIAN_POINT('Ctrl Pts',(2.87181285948336,-1.46249194612545,39.2140061827161));
#23147=CARTESIAN_POINT('Ctrl Pts',(2.86789273040673,-1.47016430486403,39.2134664513934));
#23148=CARTESIAN_POINT('Ctrl Pts',(2.86153335074908,-1.48248845911567,39.2126007785497));
#23149=CARTESIAN_POINT('Ctrl Pts',(2.85911344694395,-1.48715010920516,39.2122736360001));
#23150=CARTESIAN_POINT('Ctrl Pts',(2.85401673085687,-1.49690988973128,39.2115893848141));
#23151=CARTESIAN_POINT('Ctrl Pts',(2.85133763931079,-1.50200678603902,39.2112324302642));
#23152=CARTESIAN_POINT('Ctrl Pts',(2.84478889249885,-1.51438492775443,39.2103664167005));
#23153=CARTESIAN_POINT('Ctrl Pts',(2.84090489133678,-1.52165861946619,39.2098582634325));
#23154=CARTESIAN_POINT('Ctrl Pts',(2.82703185631834,-1.54740082260892,39.2080621990342));
#23155=CARTESIAN_POINT('Ctrl Pts',(2.81689004788105,-1.56578700154801,39.2067836464197));
#23156=CARTESIAN_POINT('Ctrl Pts',(2.75422559740134,-1.67681223100307,39.1990810755065));
#23157=CARTESIAN_POINT('Ctrl Pts',(2.69731210723424,-1.76690972779765,39.1929061646783));
#23158=CARTESIAN_POINT('Ctrl Pts',(2.5162037334278,-2.0244070249798,39.1749889155812));
#23159=CARTESIAN_POINT('Ctrl Pts',(2.38013532283281,-2.18276568316848,39.1635801291983));
#23160=CARTESIAN_POINT('Ctrl Pts',(2.1980573943836,-2.35724114196146,39.14926506881));
#23161=CARTESIAN_POINT('Ctrl Pts',(2.16576695546997,-2.38694269429084,39.1467594420274));
#23162=CARTESIAN_POINT('Ctrl Pts',(2.10017667605733,-2.44484737164205,39.1417207489274));
#23163=CARTESIAN_POINT('Ctrl Pts',(2.06689045827015,-2.47305162762471,39.1391884508847));
#23164=CARTESIAN_POINT('Ctrl Pts',(1.98128089139269,-2.54265490726078,39.1327225860384));
#23165=CARTESIAN_POINT('Ctrl Pts',(1.92822767164798,-2.5831192478746,39.1287580645187));
#23166=CARTESIAN_POINT('Ctrl Pts',(1.85846877584393,-2.63297814814501,39.1235783252825));
#23167=CARTESIAN_POINT('Ctrl Pts',(1.84288025072208,-2.64391234287018,39.1224229381918));
#23168=CARTESIAN_POINT('Ctrl Pts',(1.8179171454286,-2.66109407940087,39.1205756050772));
#23169=CARTESIAN_POINT('Ctrl Pts',(1.80860496339993,-2.66743182262345,39.1198871095989));
#23170=CARTESIAN_POINT('Ctrl Pts',(1.7918059536015,-2.67873658804928,39.1186461149906));
#23171=CARTESIAN_POINT('Ctrl Pts',(1.78433118602807,-2.68372139006235,39.1180942973701));
#23172=CARTESIAN_POINT('Ctrl Pts',(1.76677546701283,-2.6953232500139,39.1167990657712));
#23173=CARTESIAN_POINT('Ctrl Pts',(1.75667807853348,-2.70191507915415,39.1160547127544));
#23174=CARTESIAN_POINT('Ctrl Pts',(1.72745845266876,-2.72075735544246,39.1139023447241));
#23175=CARTESIAN_POINT('Ctrl Pts',(1.70824371547161,-2.73286235636227,39.1124889421898));
#23176=CARTESIAN_POINT('Ctrl Pts',(1.56347904162417,-2.8219387156103,39.1018531150306));
#23177=CARTESIAN_POINT('Ctrl Pts',(1.43293094927243,-2.89041569172864,39.0923210311563));
#23178=CARTESIAN_POINT('Ctrl Pts',(1.12299206918269,-3.02682003572455,39.0698561276923));
#23179=CARTESIAN_POINT('Ctrl Pts',(0.941295114479844,-3.08815576330052,
39.0567926850927));
#23180=CARTESIAN_POINT('Ctrl Pts',(0.626296591991462,-3.16408990104728,
39.0349901274769));
#23181=CARTESIAN_POINT('Ctrl Pts',(0.495532729666177,-3.18718810240982,
39.0261834329234));
#23182=CARTESIAN_POINT('Ctrl Pts',(0.348856801022213,-3.20384765012721,
39.0168239504983));
#23183=CARTESIAN_POINT('Ctrl Pts',(0.333998138707797,-3.20543071933491,
39.015881734465));
#23184=CARTESIAN_POINT('Ctrl Pts',(0.311979624632646,-3.20762184356043,
39.0144948003946));
#23185=CARTESIAN_POINT('Ctrl Pts',(0.30482813779362,-3.20830936573366,39.0140457832456));
#23186=CARTESIAN_POINT('Ctrl Pts',(0.292105850759773,-3.20948952471186,
39.0132496467793));
#23187=CARTESIAN_POINT('Ctrl Pts',(0.286536018534134,-3.2099915808396,39.0129020041156));
#23188=CARTESIAN_POINT('Ctrl Pts',(0.27455706398531,-3.21103991789833,39.0121562976743));
#23189=CARTESIAN_POINT('Ctrl Pts',(0.268147622524599,-3.21158150915796,
39.0117585000821));
#23190=CARTESIAN_POINT('Ctrl Pts',(0.250441275974636,-3.21302430115474,
39.0106627725796));
#23191=CARTESIAN_POINT('Ctrl Pts',(0.239141043331531,-3.21388511973132,
39.0099670776138));
#23192=CARTESIAN_POINT('Ctrl Pts',(0.17696229066587,-3.21829195016714,39.0061577092385));
#23193=CARTESIAN_POINT('Ctrl Pts',(0.126006496722375,-3.22068964190635,
39.0031045191778));
#23194=CARTESIAN_POINT('Ctrl Pts',(-0.1830946739326,-3.22788616433542,38.9848837179768));
#23195=CARTESIAN_POINT('Ctrl Pts',(-0.441014466588179,-3.20285955449788,
38.9708829805337));
#23196=CARTESIAN_POINT('Ctrl Pts',(-0.85485490292943,-3.1117099640274,38.9469569118957));
#23197=CARTESIAN_POINT('Ctrl Pts',(-1.01350044503538,-3.06371049011604,
38.9374236231667));
#23198=CARTESIAN_POINT('Ctrl Pts',(-1.18819681511353,-2.99579494117757,
38.9261504041177));
#23199=CARTESIAN_POINT('Ctrl Pts',(-1.20856532806469,-2.98763599060569,
38.9248239579017));
#23200=CARTESIAN_POINT('Ctrl Pts',(-1.24096468549849,-2.9742723458415,38.9226939920739));
#23201=CARTESIAN_POINT('Ctrl Pts',(-1.25305006745087,-2.96920104714872,
38.9218949925177));
#23202=CARTESIAN_POINT('Ctrl Pts',(-1.27437855958805,-2.96009772403249,
38.9204767872859));
#23203=CARTESIAN_POINT('Ctrl Pts',(-1.28363436311561,-2.95609574728522,
38.9198586142834));
#23204=CARTESIAN_POINT('Ctrl Pts',(-1.30280799442383,-2.94769852125175,
38.918572321186));
#23205=CARTESIAN_POINT('Ctrl Pts',(-1.31272270426616,-2.94329650895409,
38.9179039748818));
#23206=CARTESIAN_POINT('Ctrl Pts',(-1.3382631435736,-2.93180213933663,38.9161739220505));
#23207=CARTESIAN_POINT('Ctrl Pts',(-1.35385463617362,-2.92463495695087,
38.9151096443797));
#23208=CARTESIAN_POINT('Ctrl Pts',(-1.40499449194601,-2.90063014056312,
38.9115915079834));
#23209=CARTESIAN_POINT('Ctrl Pts',(-1.44028948151397,-2.883267330633,38.9091195882205));
#23210=CARTESIAN_POINT('Ctrl Pts',(-1.47525540693158,-2.86526421937299,
38.9066255640146));
#23211=CARTESIAN_POINT('Ctrl Pts',(-1.47525532932068,-2.86526425933297,
38.6590632205222));
#23212=CARTESIAN_POINT('Ctrl Pts',(-1.28407448727895,-2.96369865510202,
38.671285489794));
#23213=CARTESIAN_POINT('Ctrl Pts',(-1.08344525766489,-3.04279164141386,
38.6830572974952));
#23214=CARTESIAN_POINT('Ctrl Pts',(-0.788298988501228,-3.126191380641,38.7005217387652));
#23215=CARTESIAN_POINT('Ctrl Pts',(-0.699243561028461,-3.14730748079575,
38.7058035438473));
#23216=CARTESIAN_POINT('Ctrl Pts',(-0.554520133269385,-3.17517719228224,
38.7144951307614));
#23217=CARTESIAN_POINT('Ctrl Pts',(-0.499362042980586,-3.18431778565124,
38.7178321985447));
#23218=CARTESIAN_POINT('Ctrl Pts',(-0.427008882053403,-3.19438180882905,
38.7222527501882));
#23219=CARTESIAN_POINT('Ctrl Pts',(-0.4100029068956,-3.1966090353024,38.7232948396561));
#23220=CARTESIAN_POINT('Ctrl Pts',(-0.382217487871135,-3.20002264666423,
38.7250028045136));
#23221=CARTESIAN_POINT('Ctrl Pts',(-0.371448260896553,-3.20129057289873,
38.725666091599));
#23222=CARTESIAN_POINT('Ctrl Pts',(-0.35065562984874,-3.20363228400043,
38.7269493293259));
#23223=CARTESIAN_POINT('Ctrl Pts',(-0.340633170662929,-3.20471343823334,
38.7275690388482));
#23224=CARTESIAN_POINT('Ctrl Pts',(-0.317571989813094,-3.20709171731181,
38.7289977066194));
#23225=CARTESIAN_POINT('Ctrl Pts',(-0.304530166870745,-3.20835637379617,
38.7298076805755));
#23226=CARTESIAN_POINT('Ctrl Pts',(-0.269632609653829,-3.21152566765951,
38.7319805786219));
#23227=CARTESIAN_POINT('Ctrl Pts',(-0.247764831074532,-3.2132866987346,
38.7333480001095));
#23228=CARTESIAN_POINT('Ctrl Pts',(-0.060656220350022,-3.22643339498369,
38.7450998303797));
#23229=CARTESIAN_POINT('Ctrl Pts',(0.105191485909992,-3.22528622545785,
38.7558802854321));
#23230=CARTESIAN_POINT('Ctrl Pts',(0.527376311259654,-3.18976522331647,
38.7841513322817));
#23231=CARTESIAN_POINT('Ctrl Pts',(0.781014796840861,-3.1373141480355,38.8019781425205));
#23232=CARTESIAN_POINT('Ctrl Pts',(1.07405394425557,-3.03893561923401,38.8221387662267));
#23233=CARTESIAN_POINT('Ctrl Pts',(1.12204082752715,-3.02154706242529,38.8254219409099));
#23234=CARTESIAN_POINT('Ctrl Pts',(1.1801568336041,-2.99891243998137,38.8293586228693));
#23235=CARTESIAN_POINT('Ctrl Pts',(1.19069455895295,-2.99474413779865,38.8300708189757));
#23236=CARTESIAN_POINT('Ctrl Pts',(1.20717751417929,-2.98812338515305,38.8311820456652));
#23237=CARTESIAN_POINT('Ctrl Pts',(1.2131376407651,-2.98570862307673,38.8315832854799));
#23238=CARTESIAN_POINT('Ctrl Pts',(1.22426546879922,-2.98116133007865,38.8323312928323));
#23239=CARTESIAN_POINT('Ctrl Pts',(1.22943479198025,-2.97903321682104,38.8326783101273));
#23240=CARTESIAN_POINT('Ctrl Pts',(1.24123136243931,-2.97414085520648,38.8334691867301));
#23241=CARTESIAN_POINT('Ctrl Pts',(1.24785491385004,-2.97136790688149,38.8339125112813));
#23242=CARTESIAN_POINT('Ctrl Pts',(1.26822193345918,-2.96276114505854,38.83527359686));
#23243=CARTESIAN_POINT('Ctrl Pts',(1.28193440445722,-2.95685384788623,38.8361870054277));
#23244=CARTESIAN_POINT('Ctrl Pts',(1.41626744121304,-2.89787336426817,38.8451106006821));
#23245=CARTESIAN_POINT('Ctrl Pts',(1.53358211754802,-2.83753733299432,38.8527106759889));
#23246=CARTESIAN_POINT('Ctrl Pts',(1.82009682533644,-2.66720294482605,38.8715769792473));
#23247=CARTESIAN_POINT('Ctrl Pts',(1.98326834980852,-2.54820975285874,38.8826373588631));
#23248=CARTESIAN_POINT('Ctrl Pts',(2.20320026995289,-2.35382483260806,38.8993472110471));
#23249=CARTESIAN_POINT('Ctrl Pts',(2.26949388351596,-2.28997343888693,38.9046576200447));
#23250=CARTESIAN_POINT('Ctrl Pts',(2.37168587292633,-2.18274465202265,38.913391970288));
#23251=CARTESIAN_POINT('Ctrl Pts',(2.4093396660718,-2.14110950022714,38.9167422569918));
#23252=CARTESIAN_POINT('Ctrl Pts',(2.45706978185443,-2.08547852234036,38.9211778796392));
#23253=CARTESIAN_POINT('Ctrl Pts',(2.46814952794719,-2.07235384767475,38.9222214618484));
#23254=CARTESIAN_POINT('Ctrl Pts',(2.48605560647135,-2.05079564751309,38.9239312588243));
#23255=CARTESIAN_POINT('Ctrl Pts',(2.49294529191739,-2.04241500025859,38.9245948745641));
#23256=CARTESIAN_POINT('Ctrl Pts',(2.50615350081707,-2.02618206799042,38.9258783164783));
#23257=CARTESIAN_POINT('Ctrl Pts',(2.51247777182223,-2.01833460672897,38.9264978992126));
#23258=CARTESIAN_POINT('Ctrl Pts',(2.52693132591901,-2.00022673627236,38.9279256557813));
#23259=CARTESIAN_POINT('Ctrl Pts',(2.53503507088338,-1.98994625647866,38.9287348410906));
#23260=CARTESIAN_POINT('Ctrl Pts',(2.55652532792222,-1.96233921977238,38.9309042461241));
#23261=CARTESIAN_POINT('Ctrl Pts',(2.56979809190432,-1.94492536987769,38.9322689405519));
#23262=CARTESIAN_POINT('Ctrl Pts',(2.68064589397213,-1.79637748776523,38.9438811116159));
#23263=CARTESIAN_POINT('Ctrl Pts',(2.7682766615979,-1.65815084661719,38.9545138332772));
#23264=CARTESIAN_POINT('Ctrl Pts',(2.96391275139813,-1.29049491292741,38.9822876383255));
#23265=CARTESIAN_POINT('Ctrl Pts',(3.0560559650172,-1.05388462986568,38.99975275878));
#23266=CARTESIAN_POINT('Ctrl Pts',(3.1340222851665,-0.753216771649467,39.0200869078658));
#23267=CARTESIAN_POINT('Ctrl Pts',(3.14697694837441,-0.69711422990077,39.0238010814912));
#23268=CARTESIAN_POINT('Ctrl Pts',(3.16075742472357,-0.62918042395756,39.0281788341636));
#23269=CARTESIAN_POINT('Ctrl Pts',(3.16302943231293,-0.617657125093158,
39.0289172934967));
#23270=CARTESIAN_POINT('Ctrl Pts',(3.16646486897041,-0.599716865689503,
39.0300603048312));
#23271=CARTESIAN_POINT('Ctrl Pts',(3.16767187543463,-0.593308500516473,
39.0304672739813));
#23272=CARTESIAN_POINT('Ctrl Pts',(3.1698755038158,-0.581410339263496,39.0312203711134));
#23273=CARTESIAN_POINT('Ctrl Pts',(3.17087731134209,-0.575921669543651,
39.031566783207));
#23274=CARTESIAN_POINT('Ctrl Pts',(3.17311304417515,-0.563489927102145,
39.0323491718734));
#23275=CARTESIAN_POINT('Ctrl Pts',(3.17433843522563,-0.556545406900894,
39.032784658381));
#23276=CARTESIAN_POINT('Ctrl Pts',(3.17789792682124,-0.535978855656356,
39.0340698933367));
#23277=CARTESIAN_POINT('Ctrl Pts',(3.18016724296081,-0.5223455653897,39.0349160473253));
#23278=CARTESIAN_POINT('Ctrl Pts',(3.19638794546752,-0.420870913814157,
39.0411737663143));
#23279=CARTESIAN_POINT('Ctrl Pts',(3.20678665715305,-0.332491599773301,
39.0463998251197));
#23280=CARTESIAN_POINT('Ctrl Pts',(3.21959808597111,-0.163615866077885,
39.0561515490697));
#23281=CARTESIAN_POINT('Ctrl Pts',(3.22267806929456,-0.083241512514831,
39.0606928146395));
#23282=CARTESIAN_POINT('Ctrl Pts',(3.22300035142336,0.283371477487148,39.0812650273812));
#23283=CARTESIAN_POINT('Ctrl Pts',(3.18512972088702,0.56830024843683,39.0969964397528));
#23284=CARTESIAN_POINT('Ctrl Pts',(3.10136656492807,0.876791876939508,39.1160906873797));
#23285=CARTESIAN_POINT('Ctrl Pts',(3.09209046345141,0.908963697782091,39.1181059828272));
#23286=CARTESIAN_POINT('Ctrl Pts',(3.0785040457592,0.953467757204457,39.1209296153227));
#23287=CARTESIAN_POINT('Ctrl Pts',(3.07461726803527,0.965927829109165,39.1217240969029));
#23288=CARTESIAN_POINT('Ctrl Pts',(3.06778297368048,0.987377682112405,39.1230987240027));
#23289=CARTESIAN_POINT('Ctrl Pts',(3.06487134467569,0.996378792579462,39.1236776826933));
#23290=CARTESIAN_POINT('Ctrl Pts',(3.05876455609028,1.01497747475644,39.1248784105621));
#23291=CARTESIAN_POINT('Ctrl Pts',(3.05556376100611,1.02457307331343,39.1255003607382));
#23292=CARTESIAN_POINT('Ctrl Pts',(3.04796937799707,1.04698799932642,39.1269590492139));
#23293=CARTESIAN_POINT('Ctrl Pts',(3.04354002876989,1.05979492553884,39.1277969672757));
#23294=CARTESIAN_POINT('Ctrl Pts',(3.02892318728499,1.1012102934382,39.1305214350045));
#23295=CARTESIAN_POINT('Ctrl Pts',(3.01841230847862,1.12970209300049,39.1324187212863));
#23296=CARTESIAN_POINT('Ctrl Pts',(2.96261906407752,1.2746005160825,39.1421885313019));
#23297=CARTESIAN_POINT('Ctrl Pts',(2.91100480269604,1.38843892057456,39.1502725301293));
#23298=CARTESIAN_POINT('Ctrl Pts',(2.73746367588499,1.71872862827424,39.1749469343045));
#23299=CARTESIAN_POINT('Ctrl Pts',(2.59701815017566,1.92437427322692,39.1920356184189));
#23300=CARTESIAN_POINT('Ctrl Pts',(2.37679540635408,2.17822909856052,39.2143594642086));
#23301=CARTESIAN_POINT('Ctrl Pts',(2.31651925375649,2.24222656889907,39.2201023517836));
#23302=CARTESIAN_POINT('Ctrl Pts',(2.24384581848401,2.31332302686861,39.2265409233234));
#23303=CARTESIAN_POINT('Ctrl Pts',(2.2339328241013,2.32289725066601,39.2274092544808));
#23304=CARTESIAN_POINT('Ctrl Pts',(2.21886104938312,2.33726823751822,39.2287141439041));
#23305=CARTESIAN_POINT('Ctrl Pts',(2.21374760868439,2.34211201650658,39.2291542242887));
#23306=CARTESIAN_POINT('Ctrl Pts',(2.20455559765037,2.35076228100756,39.2299405482151));
#23307=CARTESIAN_POINT('Ctrl Pts',(2.20048300260674,2.35457495988372,39.230287265748));
#23308=CARTESIAN_POINT('Ctrl Pts',(2.19162387500514,2.36282562994989,39.2310378589657));
#23309=CARTESIAN_POINT('Ctrl Pts',(2.18683376856828,2.36725964724496,39.2314414318532));
#23310=CARTESIAN_POINT('Ctrl Pts',(2.17336571301225,2.37965074318618,39.2325698967051));
#23311=CARTESIAN_POINT('Ctrl Pts',(2.16465747733956,2.38757496171443,39.233292327543));
#23312=CARTESIAN_POINT('Ctrl Pts',(2.11275200052783,2.43428988165557,39.2375571819236));
#23313=CARTESIAN_POINT('Ctrl Pts',(2.06855335562532,2.47195797546705,39.2410207800469));
#23314=CARTESIAN_POINT('Ctrl Pts',(1.82669438903894,2.66704829677977,39.259245557701));
#23315=CARTESIAN_POINT('Ctrl Pts',(1.61204044770465,2.80201906718346,39.2729602638246));
#23316=CARTESIAN_POINT('Ctrl Pts',(1.23635327855258,2.98063822673124,39.2964607938358));
#23317=CARTESIAN_POINT('Ctrl Pts',(1.0838085218015,3.03942797261869,39.3058707943695));
#23318=CARTESIAN_POINT('Ctrl Pts',(0.906513600552543,3.09270591965345,39.317005765055));
#23319=CARTESIAN_POINT('Ctrl Pts',(0.885484730473467,3.09879227592305,39.3183292362209));
#23320=CARTESIAN_POINT('Ctrl Pts',(0.851786065699515,3.10817460799464,39.3204551846339));
#23321=CARTESIAN_POINT('Ctrl Pts',(0.839155134502183,3.11160851454795,39.3212531671907));
#23322=CARTESIAN_POINT('Ctrl Pts',(0.816762353239068,3.11755006327165,39.3226700216246));
#23323=CARTESIAN_POINT('Ctrl Pts',(0.807008945445506,3.12008905273223,39.3232878656914));
#23324=CARTESIAN_POINT('Ctrl Pts',(0.78673154836555,3.12526618801908,39.3245739266984));
#23325=CARTESIAN_POINT('Ctrl Pts',(0.776205839233688,3.12789701967621,39.3252423719447));
#23326=CARTESIAN_POINT('Ctrl Pts',(0.748980992174118,3.13455580899825,39.32697365105));
#23327=CARTESIAN_POINT('Ctrl Pts',(0.732262739341119,3.13850345045512,39.3280390646258));
#23328=CARTESIAN_POINT('Ctrl Pts',(0.660767690658835,3.15478306322465,39.3326054712275));
#23329=CARTESIAN_POINT('Ctrl Pts',(0.605707975589027,3.16581542820628,39.3361478758941));
#23330=CARTESIAN_POINT('Ctrl Pts',(0.459694296651282,3.19112389498064,39.3456156479761));
#23331=CARTESIAN_POINT('Ctrl Pts',(0.368373377273709,3.2029500595136,39.3516128713068));
#23332=CARTESIAN_POINT('Ctrl Pts',(0.0361003955840009,3.23158191611163,
39.3736765843402));
#23333=CARTESIAN_POINT('Ctrl Pts',(-0.206019566525885,3.22520791140348,
39.3902812914309));
#23334=CARTESIAN_POINT('Ctrl Pts',(-0.537365088622875,3.17899771848399,
39.4125479615176));
#23335=CARTESIAN_POINT('Ctrl Pts',(-0.628995432904767,3.16214420919996,
39.4186455967354));
#23336=CARTESIAN_POINT('Ctrl Pts',(-0.733386359925439,3.13822513357812,
39.4254294925948));
#23337=CARTESIAN_POINT('Ctrl Pts',(-0.746977027195903,3.13501800304144,
39.4263094522589));
#23338=CARTESIAN_POINT('Ctrl Pts',(-0.767428929536656,3.13005120710026,
39.4276283282962));
#23339=CARTESIAN_POINT('Ctrl Pts',(-0.774305703008538,3.12835714098051,
39.428070877633));
#23340=CARTESIAN_POINT('Ctrl Pts',(-0.786592154576694,3.12528742681839,
39.4288598623279));
#23341=CARTESIAN_POINT('Ctrl Pts',(-0.792003876800657,3.12392038608281,
39.4292067854653));
#23342=CARTESIAN_POINT('Ctrl Pts',(-0.803708711335837,3.12093128762173,
39.4299558355472));
#23343=CARTESIAN_POINT('Ctrl Pts',(-0.810000458436784,3.119304257976,39.4303576704154));
#23344=CARTESIAN_POINT('Ctrl Pts',(-0.82754980126605,3.11470936497899,39.4314763551853));
#23345=CARTESIAN_POINT('Ctrl Pts',(-0.838796434810256,3.11169947977874,
39.4321908123323));
#23346=CARTESIAN_POINT('Ctrl Pts',(-0.903897274126563,3.09389823740208,
39.4363134609622));
#23347=CARTESIAN_POINT('Ctrl Pts',(-0.95737965684929,3.07776894068284,39.43964882841));
#23348=CARTESIAN_POINT('Ctrl Pts',(-1.2518885347879,2.98052955051237,39.4578658146912));
#23349=CARTESIAN_POINT('Ctrl Pts',(-1.48309546221237,2.87249658179732,39.4716649417582));
#23350=CARTESIAN_POINT('Ctrl Pts',(-1.8386133958519,2.6518923002712,39.4952971602274));
#23351=CARTESIAN_POINT('Ctrl Pts',(-1.97118680334568,2.55488631984889,39.5047503130499));
#23352=CARTESIAN_POINT('Ctrl Pts',(-2.11243334642095,2.43397265135256,39.5159335508639));
#23353=CARTESIAN_POINT('Ctrl Pts',(-2.12892990574813,2.41955676327569,39.5172579715009));
#23354=CARTESIAN_POINT('Ctrl Pts',(-2.15504938944001,2.39625773823557,39.5193851613114));
#23355=CARTESIAN_POINT('Ctrl Pts',(-2.1647675498707,2.38748203471025,39.5201834275149));
#23356=CARTESIAN_POINT('Ctrl Pts',(-2.18187119911505,2.3718467964462,39.5216006156333));
#23357=CARTESIAN_POINT('Ctrl Pts',(-2.18927853627438,2.36501134083585,39.5222185081888));
#23358=CARTESIAN_POINT('Ctrl Pts',(-2.20459104976112,2.35074744238787,39.5235045006977));
#23359=CARTESIAN_POINT('Ctrl Pts',(-2.21249101923929,2.34331361959059,39.5241728281175));
#23360=CARTESIAN_POINT('Ctrl Pts',(-2.23279739041388,2.32401122113596,39.525903437912));
#23361=CARTESIAN_POINT('Ctrl Pts',(-2.24514662512567,2.31208325021044,39.5269682961416));
#23362=CARTESIAN_POINT('Ctrl Pts',(-2.29741377919766,2.260785459167,39.531529034092));
#23363=CARTESIAN_POINT('Ctrl Pts',(-2.33639397209793,2.22047822220215,39.535066197085));
#23364=CARTESIAN_POINT('Ctrl Pts',(-2.43641663291798,2.1114994904577,39.5445163802376));
#23365=CARTESIAN_POINT('Ctrl Pts',(-2.49560495771744,2.04120295070135,39.5505009238395));
#23366=CARTESIAN_POINT('Ctrl Pts',(-2.70039315703021,1.77573954144471,39.5726797617604));
#23367=CARTESIAN_POINT('Ctrl Pts',(-2.82674938959659,1.56679511673867,39.589424555875));
#23368=CARTESIAN_POINT('Ctrl Pts',(-2.96659722480782,1.26245684601902,39.6117037022118));
#23369=CARTESIAN_POINT('Ctrl Pts',(-3.00126028822044,1.17768265432542,39.6176945061403));
#23370=CARTESIAN_POINT('Ctrl Pts',(-3.03698126438962,1.07845068675902,39.6243746911029));
#23371=CARTESIAN_POINT('Ctrl Pts',(-3.04160826559865,1.06533105610021,39.6252513143447));
#23372=CARTESIAN_POINT('Ctrl Pts',(-3.04845888693301,1.04549795695694,39.6265661801149));
#23373=CARTESIAN_POINT('Ctrl Pts',(-3.05074553083901,1.03880665749362,39.6270080236295));
#23374=CARTESIAN_POINT('Ctrl Pts',(-3.05479744172909,1.02682096667632,39.6277962428935));
#23375=CARTESIAN_POINT('Ctrl Pts',(-3.05657099059342,1.02152948495501,39.628143102517));
#23376=CARTESIAN_POINT('Ctrl Pts',(-3.06038254249641,1.01005870677849,39.6288925726029));
#23377=CARTESIAN_POINT('Ctrl Pts',(-3.06241557425149,1.003877856069,39.629294887994));
#23378=CARTESIAN_POINT('Ctrl Pts',(-3.06804543520717,0.986585611056661,
39.6304163038666));
#23379=CARTESIAN_POINT('Ctrl Pts',(-3.07160064736433,0.975460626208227,
39.631132992443));
#23380=CARTESIAN_POINT('Ctrl Pts',(-3.0919892720848,0.910443617439896,39.6352950129623));
#23381=CARTESIAN_POINT('Ctrl Pts',(-3.10746576956372,0.856132367811441,
39.6386658815996));
#23382=CARTESIAN_POINT('Ctrl Pts',(-3.18462999296485,0.555586948438195,
39.6568839990104));
#23383=CARTESIAN_POINT('Ctrl Pts',(-3.21849228996203,0.303116389506117,
39.6706588904062));
#23384=CARTESIAN_POINT('Ctrl Pts',(-3.22487832653238,-0.114571260589173,
39.6942546760087));
#23385=CARTESIAN_POINT('Ctrl Pts',(-3.21488456870987,-0.278340731235344,
39.7036969409756));
#23386=CARTESIAN_POINT('Ctrl Pts',(-3.18949094369585,-0.462325471573138,
39.7148679913995));
#23387=CARTESIAN_POINT('Ctrl Pts',(-3.18627515336803,-0.483991665559696,
39.7161921534439));
#23388=CARTESIAN_POINT('Ctrl Pts',(-3.18078468245329,-0.518553550875952,
39.7183189952192));
#23389=CARTESIAN_POINT('Ctrl Pts',(-3.17865179173586,-0.531471316450938,
39.7191171740483));
#23390=CARTESIAN_POINT('Ctrl Pts',(-3.17473778144699,-0.554309629524622,
39.7205342471714));
#23391=CARTESIAN_POINT('Ctrl Pts',(-3.17298871556446,-0.564235547945788,
39.7211521124968));
#23392=CARTESIAN_POINT('Ctrl Pts',(-3.16926052130431,-0.584827313269401,
39.7224380882202));
#23393=CARTESIAN_POINT('Ctrl Pts',(-3.1672740466979,-0.595491684871205,
39.7231064262771));
#23394=CARTESIAN_POINT('Ctrl Pts',(-3.16200424339392,-0.623010083338556,
39.7248371490724));
#23395=CARTESIAN_POINT('Ctrl Pts',(-3.15864002288915,-0.6398480964976,39.7259021105103));
#23396=CARTESIAN_POINT('Ctrl Pts',(-3.14371400603114,-0.711565311408102,
39.7304640565655));
#23397=CARTESIAN_POINT('Ctrl Pts',(-3.13085585754201,-0.76616180125175,
39.7340023534215));
#23398=CARTESIAN_POINT('Ctrl Pts',(-3.09318546081508,-0.9092674950203,39.7434563852011));
#23399=CARTESIAN_POINT('Ctrl Pts',(-3.06600146818817,-0.997093852123104,
39.7494437189835));
#23400=CARTESIAN_POINT('Ctrl Pts',(-2.9533884000279,-1.31250740328511,39.7715991691548));
#23401=CARTESIAN_POINT('Ctrl Pts',(-2.84605622288976,-1.53138097428601,
39.7883152533023));
#23402=CARTESIAN_POINT('Ctrl Pts',(-2.6656712648271,-1.81349164490135,39.8105916885811));
#23403=CARTESIAN_POINT('Ctrl Pts',(-2.61289646902171,-1.88873785391463,
39.8166042216249));
#23404=CARTESIAN_POINT('Ctrl Pts',(-2.54849956332873,-1.97267872563566,
39.8233055030797));
#23405=CARTESIAN_POINT('Ctrl Pts',(-2.53995393823379,-1.98366967688043,
39.8241828027881));
#23406=CARTESIAN_POINT('Ctrl Pts',(-2.52695942185555,-2.00016091207473,
39.8254984758337));
#23407=CARTESIAN_POINT('Ctrl Pts',(-2.52256333649863,-2.00570232325646,
39.825940456732));
#23408=CARTESIAN_POINT('Ctrl Pts',(-2.51466612406436,-2.01558998636422,
39.8267288199463));
#23409=CARTESIAN_POINT('Ctrl Pts',(-2.51117193107576,-2.01994164341351,
39.8270756869182));
#23410=CARTESIAN_POINT('Ctrl Pts',(-2.50358053567092,-2.02934580015975,
39.8278250595716));
#23411=CARTESIAN_POINT('Ctrl Pts',(-2.49947934768524,-2.03439496349108,
39.8282272707966));
#23412=CARTESIAN_POINT('Ctrl Pts',(-2.48797711888578,-2.04846860672115,
39.8293481021728));
#23413=CARTESIAN_POINT('Ctrl Pts',(-2.48054221281182,-2.0574654594896,39.8300643144918));
#23414=CARTESIAN_POINT('Ctrl Pts',(-2.4369403243924,-2.10964745583943,39.834217938609));
#23415=CARTESIAN_POINT('Ctrl Pts',(-2.39969252699148,-2.15192174664676,
39.8375812376748));
#23416=CARTESIAN_POINT('Ctrl Pts',(-2.18855363647068,-2.37924862519077,
39.8557986074645));
#23417=CARTESIAN_POINT('Ctrl Pts',(-1.99435678089185,-2.54424040897939,
39.869578214336));
#23418=CARTESIAN_POINT('Ctrl Pts',(-1.68364917784115,-2.75056444302925,
39.8906452045811));
#23419=CARTESIAN_POINT('Ctrl Pts',(-1.58098051405214,-2.81082891809792,
39.8974610527913));
#23420=CARTESIAN_POINT('Ctrl Pts',(-1.47525529542902,-2.86526427678297,
39.904468116039));
#23421=CARTESIAN_POINT('Origin',(0.,0.,4.68922655072688));
#23422=CARTESIAN_POINT('',(-1.47525540501187,-2.86526422036141,41.4036966894132));
#23423=CARTESIAN_POINT('',(-1.47525540498233,-2.86526422037662,41.155741540048));
#23424=CARTESIAN_POINT('',(-1.47525540501186,-2.86526422036142,4.68922655072688));
#23425=CARTESIAN_POINT('',(3.22274859133547,0.00301322837664063,40.5607734493322));
#23426=CARTESIAN_POINT('Ctrl Pts',(3.22274859133547,0.00301322837664063,
40.5607734493322));
#23427=CARTESIAN_POINT('Ctrl Pts',(3.22262419112213,0.136063419793571,40.5689887246145));
#23428=CARTESIAN_POINT('Ctrl Pts',(3.21425677216936,0.26874543348901,40.5772039998969));
#23429=CARTESIAN_POINT('Ctrl Pts',(3.19780408718992,0.400208173893808,40.5854192751792));
#23430=CARTESIAN_POINT('Ctrl Pts',(3.18308417976128,0.51782541214356,40.5927693272715));
#23431=CARTESIAN_POINT('Ctrl Pts',(3.16189309846113,0.634467395283658,40.6001193793638));
#23432=CARTESIAN_POINT('Ctrl Pts',(3.13437478364467,0.749541378545861,40.607469431456));
#23433=CARTESIAN_POINT('Ctrl Pts',(3.11126200858287,0.846192612763652,40.6136427782556));
#23434=CARTESIAN_POINT('Ctrl Pts',(3.08363389295753,0.941943832720015,40.6198161250552));
#23435=CARTESIAN_POINT('Ctrl Pts',(3.05157570653629,1.03634129020201,40.6259894718547));
#23436=CARTESIAN_POINT('Ctrl Pts',(3.01956099498361,1.13061073304826,40.6321544468319));
#23437=CARTESIAN_POINT('Ctrl Pts',(2.98312829213254,1.22352965490198,40.6383194218092));
#23438=CARTESIAN_POINT('Ctrl Pts',(2.94241358377365,1.31465579697666,40.6444843967864));
#23439=CARTESIAN_POINT('Ctrl Pts',(2.90174207079912,1.40568526075273,40.6506428311675));
#23440=CARTESIAN_POINT('Ctrl Pts',(2.85679776024314,1.49492533189045,40.6568012655486));
#23441=CARTESIAN_POINT('Ctrl Pts',(2.80776570451632,1.58195110892909,40.6629596999297));
#23442=CARTESIAN_POINT('Ctrl Pts',(2.75876964160129,1.66891300322067,40.6691136136077));
#23443=CARTESIAN_POINT('Ctrl Pts',(2.70569201198593,1.75366345796182,40.6752675272856));
#23444=CARTESIAN_POINT('Ctrl Pts',(2.64876461986577,1.83580052049436,40.6814214409636));
#23445=CARTESIAN_POINT('Ctrl Pts',(2.59185893121694,1.91790626841163,40.6875730084724));
#23446=CARTESIAN_POINT('Ctrl Pts',(2.53110664350499,1.99740024740105,40.6937245759812));
#23447=CARTESIAN_POINT('Ctrl Pts',(2.46678337926716,2.07390870634927,40.69987614349));
#23448=CARTESIAN_POINT('Ctrl Pts',(2.40246744708781,2.15040844427716,40.7060270097961));
#23449=CARTESIAN_POINT('Ctrl Pts',(2.33458162708301,2.2239230063942,40.7121778761021));
#23450=CARTESIAN_POINT('Ctrl Pts',(2.26344175423213,2.29411180802039,40.7183287424081));
#23451=CARTESIAN_POINT('Ctrl Pts',(2.19229097773184,2.36431136752475,40.724480551461));
#23452=CARTESIAN_POINT('Ctrl Pts',(2.11788546687482,2.43118384907181,40.7306323605138));
#23453=CARTESIAN_POINT('Ctrl Pts',(2.04057708960769,2.49442632760885,40.7367841695667));
#23454=CARTESIAN_POINT('Ctrl Pts',(1.96318636876915,2.55773616768849,40.7429425311039));
#23455=CARTESIAN_POINT('Ctrl Pts',(1.88288694393398,2.61740800834537,40.749100892641));
#23456=CARTESIAN_POINT('Ctrl Pts',(1.80006277528914,2.67318004771814,40.7552592541782));
#23457=CARTESIAN_POINT('Ctrl Pts',(1.71719262056847,2.72898305313952,40.7614210349936));
#23458=CARTESIAN_POINT('Ctrl Pts',(1.63179530139903,2.78088171955104,40.767582815809));
#23459=CARTESIAN_POINT('Ctrl Pts',(1.54428088665247,2.82865941845601,40.7737445966245));
#23460=CARTESIAN_POINT('Ctrl Pts',(1.45662043951921,2.87651684241452,40.7799166593981));
#23461=CARTESIAN_POINT('Ctrl Pts',(1.3668362307995,2.92023937284788,40.7860887221718));
#23462=CARTESIAN_POINT('Ctrl Pts',(1.27536000463379,2.95965782162069,40.7922607849455));
#23463=CARTESIAN_POINT('Ctrl Pts',(1.20549579749648,2.98976333411861,40.7969746465701));
#23464=CARTESIAN_POINT('Ctrl Pts',(1.13464508386649,3.01735925009222,40.8016885081947));
#23465=CARTESIAN_POINT('Ctrl Pts',(1.06300562506833,3.04238994929531,40.8064023698193));
#23466=CARTESIAN_POINT('Ctrl Pts',(0.969183155822521,3.07517135280645,40.8125758689596));
#23467=CARTESIAN_POINT('Ctrl Pts',(0.873678323558671,3.103666182483,40.8187493680999));
#23468=CARTESIAN_POINT('Ctrl Pts',(0.776919112435889,3.12770111347485,40.8249228672402));
#23469=CARTESIAN_POINT('Ctrl Pts',(0.680290719135704,3.1517035493967,40.83108801985));
#23470=CARTESIAN_POINT('Ctrl Pts',(0.582411735498871,3.17125796782599,40.8372531724597));
#23471=CARTESIAN_POINT('Ctrl Pts',(0.483727864759985,3.18623993373926,40.8434183250694));
#23472=CARTESIAN_POINT('Ctrl Pts',(0.385148292245413,3.20120606532793,40.8495769617767));
#23473=CARTESIAN_POINT('Ctrl Pts',(0.285765950771235,3.21160928734603,40.855735598484));
#23474=CARTESIAN_POINT('Ctrl Pts',(0.186038433928137,3.21737583499372,40.8618942351914));
#23475=CARTESIAN_POINT('Ctrl Pts',(0.0863835406774207,3.22313818332493,
40.868048387055));
#23476=CARTESIAN_POINT('Ctrl Pts',(-0.0136155960424126,3.22427054543994,
40.8742025389187));
#23477=CARTESIAN_POINT('Ctrl Pts',(-0.113495445003531,3.2207508979217,40.8803566907824));
#23478=CARTESIAN_POINT('Ctrl Pts',(-0.213337571237968,3.21723257970765,
40.8865085183395));
#23479=CARTESIAN_POINT('Ctrl Pts',(-0.313060065815396,3.20906575827465,
40.8926603458966));
#23480=CARTESIAN_POINT('Ctrl Pts',(-0.412199467256615,3.19628051986889,
40.8988121734537));
#23481=CARTESIAN_POINT('Ctrl Pts',(-0.511327913499578,3.18349669426994,
40.9049633212156));
#23482=CARTESIAN_POINT('Ctrl Pts',(-0.609872964109097,3.16609552188737,
40.9111144689774));
#23483=CARTESIAN_POINT('Ctrl Pts',(-0.707377352625077,3.14415884514335,
40.9172656167393));
#23484=CARTESIAN_POINT('Ctrl Pts',(-0.804897017418076,3.12221873152068,
40.9234177282182));
#23485=CARTESIAN_POINT('Ctrl Pts',(-0.901375272646106,3.09574179739957,
40.9295698396971));
#23486=CARTESIAN_POINT('Ctrl Pts',(-0.99636708492585,3.06486055059221,40.935721951176));
#23487=CARTESIAN_POINT('Ctrl Pts',(-1.09146053909923,3.03394626063799,40.9418806454566));
#23488=CARTESIAN_POINT('Ctrl Pts',(-1.18506396053084,2.99861838176978,40.9480393397371));
#23489=CARTESIAN_POINT('Ctrl Pts',(-1.27674958943304,2.95905864226828,40.9541980340177));
#23490=CARTESIAN_POINT('Ctrl Pts',(-1.36848637968764,2.91947682809927,40.9603601649015));
#23491=CARTESIAN_POINT('Ctrl Pts',(-1.45830285597916,2.87565864088038,40.9665222957853));
#23492=CARTESIAN_POINT('Ctrl Pts',(-1.54579517455693,2.82783218045493,40.972684426669));
#23493=CARTESIAN_POINT('Ctrl Pts',(-1.63343382772084,2.779925728261,40.9788568639762));
#23494=CARTESIAN_POINT('Ctrl Pts',(-1.71874018738417,2.72799783754466,40.9850293012833));
#23495=CARTESIAN_POINT('Ctrl Pts',(-1.8013386261253,2.67232047414396,40.9912017385904));
#23496=CARTESIAN_POINT('Ctrl Pts',(-1.86438291609249,2.62982403115618,40.9959129284546));
#23497=CARTESIAN_POINT('Ctrl Pts',(-1.92585023631551,2.58514416715511,41.0006241183187));
#23498=CARTESIAN_POINT('Ctrl Pts',(-1.98558722752699,2.53841701152149,41.0053353081829));
#23499=CARTESIAN_POINT('Ctrl Pts',(-2.06373736416863,2.47728682194238,41.0114986606411));
#23500=CARTESIAN_POINT('Ctrl Pts',(-2.13920186822442,2.41243469483613,41.0176620130993));
#23501=CARTESIAN_POINT('Ctrl Pts',(-2.21160414709847,2.34412556383758,41.0238253655576));
#23502=CARTESIAN_POINT('Ctrl Pts',(-2.28390791960727,2.27590937030333,41.0299803325139));
#23503=CARTESIAN_POINT('Ctrl Pts',(-2.35315743316449,2.20424581702229,41.0361352994702));
#23504=CARTESIAN_POINT('Ctrl Pts',(-2.41900756135291,2.12944123671386,41.0422902664265));
#23505=CARTESIAN_POINT('Ctrl Pts',(-2.48478770214377,2.05471616085053,41.048438691708));
#23506=CARTESIAN_POINT('Ctrl Pts',(-2.54717535364372,1.97685701969955,41.0545871169896));
#23507=CARTESIAN_POINT('Ctrl Pts',(-2.60586152789159,1.89620759938213,41.0607355422712));
#23508=CARTESIAN_POINT('Ctrl Pts',(-2.66450491757013,1.81561697571927,41.0668794851047));
#23509=CARTESIAN_POINT('Ctrl Pts',(-2.71945193898403,1.73224046813409,41.0730234279382));
#23510=CARTESIAN_POINT('Ctrl Pts',(-2.77043388081351,1.64645488080926,41.0791673707717));
#23511=CARTESIAN_POINT('Ctrl Pts',(-2.82139657140941,1.56070168688334,41.0853089935979));
#23512=CARTESIAN_POINT('Ctrl Pts',(-2.86839693478945,1.47254159477363,41.0914506164241));
#23513=CARTESIAN_POINT('Ctrl Pts',(-2.91121011325736,1.38237955676726,41.0975922392503));
#23514=CARTESIAN_POINT('Ctrl Pts',(-2.95401866372039,1.29222726506722,41.1037331981813));
#23515=CARTESIAN_POINT('Ctrl Pts',(-2.9926407421395,1.20007385130773,41.1098741571124));
#23516=CARTESIAN_POINT('Ctrl Pts',(-3.02689837238441,1.10634705484158,41.1160151160435));
#23517=CARTESIAN_POINT('Ctrl Pts',(-3.06116153227586,1.01260512959821,41.1221570662087));
#23518=CARTESIAN_POINT('Ctrl Pts',(-3.09105869515395,0.917289726540066,
41.1282990163739));
#23519=CARTESIAN_POINT('Ctrl Pts',(-3.11646112231233,0.820845683192496,
41.1344409665391));
#23520=CARTESIAN_POINT('Ctrl Pts',(-3.14189120989953,0.724296622966874,
41.1405896046075));
#23521=CARTESIAN_POINT('Ctrl Pts',(-3.16281667734122,0.626616890588295,
41.146738242676));
#23522=CARTESIAN_POINT('Ctrl Pts',(-3.17915953521806,0.528263392761672,
41.1528868807444));
#23523=CARTESIAN_POINT('Ctrl Pts',(-3.19551163962405,0.429854248089751,
41.1590389976145));
#23524=CARTESIAN_POINT('Ctrl Pts',(-3.20727592026887,0.330771011595257,
41.1651911144846));
#23525=CARTESIAN_POINT('Ctrl Pts',(-3.21442633426897,0.231475493428943,
41.1713432313547));
#23526=CARTESIAN_POINT('Ctrl Pts',(-3.22158892941005,0.132010819643656,
41.1775058287093));
#23527=CARTESIAN_POINT('Ctrl Pts',(-3.22412194700544,0.0323335776409921,
41.1836684260639));
#23528=CARTESIAN_POINT('Ctrl Pts',(-3.22205150365813,-0.0670944876602563,
41.1898310234185));
#23529=CARTESIAN_POINT('Ctrl Pts',(-3.22043468254313,-0.144738435567149,
41.1946434311278));
#23530=CARTESIAN_POINT('Ctrl Pts',(-3.21601166693476,-0.222230416598312,
41.199455838837));
#23531=CARTESIAN_POINT('Ctrl Pts',(-3.20881670658963,-0.299354148144459,
41.2042682465462));
#23532=CARTESIAN_POINT('Ctrl Pts',(-3.19957127567767,-0.398457144891972,
41.2104521281608));
#23533=CARTESIAN_POINT('Ctrl Pts',(-3.18571439893586,-0.497303199742479,
41.2166360097754));
#23534=CARTESIAN_POINT('Ctrl Pts',(-3.16726709666734,-0.595429845463283,
41.22281989139));
#23535=CARTESIAN_POINT('Ctrl Pts',(-3.14884484621629,-0.693423233172627,
41.2289953751657));
#23536=CARTESIAN_POINT('Ctrl Pts',(-3.12584464111695,-0.790698732252656,
41.2351708589413));
#23537=CARTESIAN_POINT('Ctrl Pts',(-3.09833932604596,-0.886798163719958,
41.241346342717));
#23538=CARTESIAN_POINT('Ctrl Pts',(-3.07086331758082,-0.982795202316867,
41.2475152465836));
#23539=CARTESIAN_POINT('Ctrl Pts',(-3.03889186148929,-1.07761825109776,
41.2536841504503));
#23540=CARTESIAN_POINT('Ctrl Pts',(-3.00254881755478,-1.17081943983708,
41.259853054317));
#23541=CARTESIAN_POINT('Ctrl Pts',(-2.96623300370973,-1.26395079742213,
41.2660173361217));
#23542=CARTESIAN_POINT('Ctrl Pts',(-2.92555227186591,-1.35546230948821,
41.2721816179263));
#23543=CARTESIAN_POINT('Ctrl Pts',(-2.88067999071116,-1.44492226559645,
41.2783458997309));
#23544=CARTESIAN_POINT('Ctrl Pts',(-2.83582526615847,-1.53434721985476,
41.2845077697161));
#23545=CARTESIAN_POINT('Ctrl Pts',(-2.78678244504761,-1.62172182701643,
41.2906696397012));
#23546=CARTESIAN_POINT('Ctrl Pts',(-2.73377225069178,-1.70663611934343,
41.2968315096864));
#23547=CARTESIAN_POINT('Ctrl Pts',(-2.6807687561129,-1.79153967964379,41.3029926008939));
#23548=CARTESIAN_POINT('Ctrl Pts',(-2.62379911439302,-1.87398317641695,
41.3091536921013));
#23549=CARTESIAN_POINT('Ctrl Pts',(-2.5631285449393,-1.95358379001704,41.3153147833088));
#23550=CARTESIAN_POINT('Ctrl Pts',(-2.50244957388124,-2.03319542663648,
41.3214767276985));
#23551=CARTESIAN_POINT('Ctrl Pts',(-2.43806891945372,-2.10996305405005,
41.3276386720882));
#23552=CARTESIAN_POINT('Ctrl Pts',(-2.3702928086302,-2.18353602302686,41.333800616478));
#23553=CARTESIAN_POINT('Ctrl Pts',(-2.30244683475877,-2.25718483040446,
41.3399689125484));
#23554=CARTESIAN_POINT('Ctrl Pts',(-2.23119870873185,-2.32763208442139,
41.3461372086188));
#23555=CARTESIAN_POINT('Ctrl Pts',(-2.15689225476011,-2.39456329293168,
41.3523055046892));
#23556=CARTESIAN_POINT('Ctrl Pts',(-2.08254577089664,-2.46153055818924,
41.3584771237041));
#23557=CARTESIAN_POINT('Ctrl Pts',(-2.00513801200696,-2.52497773072402,
41.3646487427191));
#23558=CARTESIAN_POINT('Ctrl Pts',(-1.92504508718016,-2.58463130345965,
41.370820361734));
#23559=CARTESIAN_POINT('Ctrl Pts',(-1.8448220891684,-2.64438175529187,41.3770020036335));
#23560=CARTESIAN_POINT('Ctrl Pts',(-1.76190557312126,-2.70032605835056,
41.3831836455331));
#23561=CARTESIAN_POINT('Ctrl Pts',(-1.67669985950868,-2.75223457278328,
41.3893652874326));
#23562=CARTESIAN_POINT('Ctrl Pts',(-1.61313004331406,-2.79096219539821,
41.3939772532583));
#23563=CARTESIAN_POINT('Ctrl Pts',(-1.54828657774929,-2.8274443124284,41.398589219084));
#23564=CARTESIAN_POINT('Ctrl Pts',(-1.48234495845957,-2.86160287018124,
41.4032011849096));
#23565=CARTESIAN_POINT('Ctrl Pts',(-1.47998339359638,-2.86282618939352,
41.4033663530775));
#23566=CARTESIAN_POINT('Ctrl Pts',(-1.47762020665672,-2.8640466410598,41.4035315212454));
#23567=CARTESIAN_POINT('Ctrl Pts',(-1.47525540501187,-2.86526422036141,
41.4036966894132));
#23568=CARTESIAN_POINT('Ctrl Pts',(3.22274859312508,0.00301131371402447,
40.5608077201065));
#23569=CARTESIAN_POINT('Ctrl Pts',(3.2229238947785,-0.184598882557479,40.5503261789538));
#23570=CARTESIAN_POINT('Ctrl Pts',(3.20671723420002,-0.371855052433079,
40.5398166588107));
#23571=CARTESIAN_POINT('Ctrl Pts',(3.16427968097729,-0.613862529188434,
40.5254059762392));
#23572=CARTESIAN_POINT('Ctrl Pts',(3.15269954516447,-0.670804038967186,
40.5219562899646));
#23573=CARTESIAN_POINT('Ctrl Pts',(3.13594431233552,-0.743122694444961,
40.5174858727603));
#23574=CARTESIAN_POINT('Ctrl Pts',(3.13218332582174,-0.758818600182063,
40.5165102250996));
#23575=CARTESIAN_POINT('Ctrl Pts',(3.12563446067714,-0.785270804289436,
40.5148565483237));
#23576=CARTESIAN_POINT('Ctrl Pts',(3.12290854167766,-0.796042243429977,
40.5141805149489));
#23577=CARTESIAN_POINT('Ctrl Pts',(3.11740830733502,-0.817313246518816,
40.5128401633219));
#23578=CARTESIAN_POINT('Ctrl Pts',(3.114636513304,-0.827813314099862,40.512175934349));
#23579=CARTESIAN_POINT('Ctrl Pts',(3.10919338784129,-0.848018491750633,
40.51089268907));
#23580=CARTESIAN_POINT('Ctrl Pts',(3.1065295497782,-0.857725502727836,40.5102739235535));
#23581=CARTESIAN_POINT('Ctrl Pts',(3.10031003975935,-0.879980288415187,
40.508850029205));
#23582=CARTESIAN_POINT('Ctrl Pts',(3.09672360645326,-0.892519214259733,
40.5080439027508));
#23583=CARTESIAN_POINT('Ctrl Pts',(3.08695511710534,-0.925904117693024,
40.5058870977307));
#23584=CARTESIAN_POINT('Ctrl Pts',(3.08063811984657,-0.946709600284812,
40.5045320180866));
#23585=CARTESIAN_POINT('Ctrl Pts',(3.02709939589663,-1.11683119106082,40.4933598813228));
#23586=CARTESIAN_POINT('Ctrl Pts',(2.9692690942477,-1.26256516297879,40.4831901049873));
#23587=CARTESIAN_POINT('Ctrl Pts',(2.8788886727882,-1.4493845179116,40.4693751701246));
#23588=CARTESIAN_POINT('Ctrl Pts',(2.85560670142801,-1.49473260860151,40.4659589530262));
#23589=CARTESIAN_POINT('Ctrl Pts',(2.82894744290142,-1.54376078382435,40.4622016806355));
#23590=CARTESIAN_POINT('Ctrl Pts',(2.82662558960878,-1.54800800010078,40.4618756644591));
#23591=CARTESIAN_POINT('Ctrl Pts',(2.77067316662324,-1.64981254609223,40.4540485249987));
#23592=CARTESIAN_POINT('Ctrl Pts',(2.71203355215114,-1.74452998818334,40.4464840362029));
#23593=CARTESIAN_POINT('Ctrl Pts',(2.57377279054074,-1.94398231964742,40.4301162172918));
#23594=CARTESIAN_POINT('Ctrl Pts',(2.49239564248336,-2.04727740802169,40.4213489548755));
#23595=CARTESIAN_POINT('Ctrl Pts',(2.38857458465351,-2.16366189942263,40.4113634291883));
#23596=CARTESIAN_POINT('Ctrl Pts',(2.37200747121731,-2.18181163351335,40.4098030536497));
#23597=CARTESIAN_POINT('Ctrl Pts',(2.35062176127878,-2.20470872284533,40.4078324829267));
#23598=CARTESIAN_POINT('Ctrl Pts',(2.34599414962127,-2.20963224747159,40.4074086314184));
#23599=CARTESIAN_POINT('Ctrl Pts',(2.3369450838761,-2.21919948386372,40.4065848420951));
#23600=CARTESIAN_POINT('Ctrl Pts',(2.33252519119706,-2.22384462325253,40.406184790299));
#23601=CARTESIAN_POINT('Ctrl Pts',(2.32422418162256,-2.23251669513297,40.4054378305655));
#23602=CARTESIAN_POINT('Ctrl Pts',(2.32034649208245,-2.23654666789858,40.4050906798753));
#23603=CARTESIAN_POINT('Ctrl Pts',(2.31144910298076,-2.24574542598431,40.4042981699123));
#23604=CARTESIAN_POINT('Ctrl Pts',(2.30642255426454,-2.25090747867538,40.4038533540029));
#23605=CARTESIAN_POINT('Ctrl Pts',(2.29084613036601,-2.26679684598253,40.402483733832));
#23606=CARTESIAN_POINT('Ctrl Pts',(2.28023823420157,-2.27746735423769,40.4015633590956));
#23607=CARTESIAN_POINT('Ctrl Pts',(2.16157901497012,-2.39516676427382,40.3913990751255));
#23608=CARTESIAN_POINT('Ctrl Pts',(2.04614058331038,-2.4945077582227,40.3827028048404));
#23609=CARTESIAN_POINT('Ctrl Pts',(1.76139459026686,-2.70642641181927,40.3627219482727));
#23610=CARTESIAN_POINT('Ctrl Pts',(1.58762445738144,-2.81188593057071,40.3515638285195));
#23611=CARTESIAN_POINT('Ctrl Pts',(1.3348199865055,-2.93436040257996,40.3354579954833));
#23612=CARTESIAN_POINT('Ctrl Pts',(1.26333425012722,-2.96583894780112,40.3309210088079));
#23613=CARTESIAN_POINT('Ctrl Pts',(1.1446522514414,-3.01303051967691,40.3233636247056));
#23614=CARTESIAN_POINT('Ctrl Pts',(1.09810952530253,-3.03030307985393,40.3203940283747));
#23615=CARTESIAN_POINT('Ctrl Pts',(1.03621933884947,-3.0516582034835,40.3164297265227));
#23616=CARTESIAN_POINT('Ctrl Pts',(1.02121274523473,-3.056712748057,40.315467326557));
#23617=CARTESIAN_POINT('Ctrl Pts',(0.995847650001017,-3.06504862482765,
40.3138383924981));
#23618=CARTESIAN_POINT('Ctrl Pts',(0.985508596637388,-3.06838856990994,
40.3131738042492));
#23619=CARTESIAN_POINT('Ctrl Pts',(0.965541957742636,-3.0747273002856,40.3118890843201));
#23620=CARTESIAN_POINT('Ctrl Pts',(0.955916786186559,-3.07773331162445,
40.3112691996256));
#23621=CARTESIAN_POINT('Ctrl Pts',(0.933771423142863,-3.08453556587378,
40.3098416058582));
#23622=CARTESIAN_POINT('Ctrl Pts',(0.921241969045974,-3.08830081989703,
40.3090328900427));
#23623=CARTESIAN_POINT('Ctrl Pts',(0.88772424444445,-3.09815118407498,40.3068666329172));
#23624=CARTESIAN_POINT('Ctrl Pts',(0.866696709727775,-3.10409920410611,
40.3055046432148));
#23625=CARTESIAN_POINT('Ctrl Pts',(0.690332581046362,-3.15205528645061,
40.2940545449546));
#23626=CARTESIAN_POINT('Ctrl Pts',(0.532134429685544,-3.18258238173379,
40.2835937515043));
#23627=CARTESIAN_POINT('Ctrl Pts',(0.121474423938302,-3.2303476369322,40.2560428507455));
#23628=CARTESIAN_POINT('Ctrl Pts',(-0.131935317308873,-3.22993636240842,
40.2386162665552));
#23629=CARTESIAN_POINT('Ctrl Pts',(-0.442326483535104,-3.19281568102752,
40.2181240203984));
#23630=CARTESIAN_POINT('Ctrl Pts',(-0.501754566968227,-3.18401760979885,
40.2142446132021));
#23631=CARTESIAN_POINT('Ctrl Pts',(-0.572621039016476,-3.1714924296507,
40.2096985134214));
#23632=CARTESIAN_POINT('Ctrl Pts',(-0.584324483269368,-3.16935703168332,
40.2089503718798));
#23633=CARTESIAN_POINT('Ctrl Pts',(-0.602486847658238,-3.16593912054356,
40.2077937293167));
#23634=CARTESIAN_POINT('Ctrl Pts',(-0.608953969538599,-3.16470156277189,
40.2073827460243));
#23635=CARTESIAN_POINT('Ctrl Pts',(-0.620893496299887,-3.16237884387466,
40.2066256509544));
#23636=CARTESIAN_POINT('Ctrl Pts',(-0.626366835800287,-3.16129930152288,
40.2062792327385));
#23637=CARTESIAN_POINT('Ctrl Pts',(-0.638684432494127,-3.15883657585578,
40.2055010772227));
#23638=CARTESIAN_POINT('Ctrl Pts',(-0.645526993645605,-3.15744536293488,
40.2050698045064));
#23639=CARTESIAN_POINT('Ctrl Pts',(-0.663055734370697,-3.15382209858,40.2039674463562));
#23640=CARTESIAN_POINT('Ctrl Pts',(-0.673735293444924,-3.15155794784685,
40.203298154434));
#23641=CARTESIAN_POINT('Ctrl Pts',(-0.736832483135688,-3.13784545457574,
40.1993565220328));
#23642=CARTESIAN_POINT('Ctrl Pts',(-0.788972514573263,-3.12514309308663,
40.1961512341744));
#23643=CARTESIAN_POINT('Ctrl Pts',(-0.86821343675468,-3.10372854417498,
40.1913258912345));
#23644=CARTESIAN_POINT('Ctrl Pts',(-0.895553884671158,-3.09595038304072,
40.1896694958894));
#23645=CARTESIAN_POINT('Ctrl Pts',(-1.01915676344838,-3.05901181679438,
40.1822051765307));
#23646=CARTESIAN_POINT('Ctrl Pts',(-1.11412936226403,-3.02571508266372,
40.1765352057574));
#23647=CARTESIAN_POINT('Ctrl Pts',(-1.29853395032025,-2.95120144988354,
40.1653921006252));
#23648=CARTESIAN_POINT('Ctrl Pts',(-1.38791377808792,-2.91023432009513,
40.1599247739091));
#23649=CARTESIAN_POINT('Ctrl Pts',(-1.47525550050006,-2.86526417119684,
40.1544081509837));
#23650=CARTESIAN_POINT('',(3.22274996944047,-0.000443814660293801,40.3112149259812));
#23651=CARTESIAN_POINT('Ctrl Pts',(-1.47525529542902,-2.86526427678297,
39.904468116039));
#23652=CARTESIAN_POINT('Ctrl Pts',(-1.4354344117846,-2.88576708692202,39.907107291951));
#23653=CARTESIAN_POINT('Ctrl Pts',(-1.39517988412917,-2.90544297473476,
39.9097730047258));
#23654=CARTESIAN_POINT('Ctrl Pts',(-1.33459234943844,-2.9335069438397,39.9137889337923));
#23655=CARTESIAN_POINT('Ctrl Pts',(-1.31457429940772,-2.94253192056124,
39.9151163693994));
#23656=CARTESIAN_POINT('Ctrl Pts',(-1.28246107940106,-2.956616813754,39.9172474830041));
#23657=CARTESIAN_POINT('Ctrl Pts',(-1.27042432850135,-2.96180880901089,
39.9180466313052));
#23658=CARTESIAN_POINT('Ctrl Pts',(-1.24907510149167,-2.970863610293,39.9194648354831));
#23659=CARTESIAN_POINT('Ctrl Pts',(-1.23977549368212,-2.97475644746363,
39.9200828570189));
#23660=CARTESIAN_POINT('Ctrl Pts',(-1.22043800308202,-2.98274473823459,
39.9213685701654));
#23661=CARTESIAN_POINT('Ctrl Pts',(-1.2103974272437,-2.98683329905711,39.9220364865195));
#23662=CARTESIAN_POINT('Ctrl Pts',(-1.1844299082303,-2.99725493218915,39.9237648559926));
#23663=CARTESIAN_POINT('Ctrl Pts',(-1.16847288555892,-3.00351168359012,
39.9248278723957));
#23664=CARTESIAN_POINT('Ctrl Pts',(-1.10035602627271,-3.02959533807511,
39.9293701413526));
#23665=CARTESIAN_POINT('Ctrl Pts',(-1.04773846536925,-3.04819205055329,
39.9328902629578));
#23666=CARTESIAN_POINT('Ctrl Pts',(-0.907866804382616,-3.09357770389227,
39.942283470876));
#23667=CARTESIAN_POINT('Ctrl Pts',(-0.819916423488113,-3.11804100876193,
39.9482270134279));
#23668=CARTESIAN_POINT('Ctrl Pts',(-0.489238441873115,-3.19506019930173,
39.9706807439011));
#23669=CARTESIAN_POINT('Ctrl Pts',(-0.241751965264356,-3.2232443358107,
39.9877734806567));
#23670=CARTESIAN_POINT('Ctrl Pts',(0.0943292490012712,-3.22256623450963,
40.0100979881635));
#23671=CARTESIAN_POINT('Ctrl Pts',(0.18212114491343,-3.21879885323879,40.0158380748646));
#23672=CARTESIAN_POINT('Ctrl Pts',(0.283388872142236,-3.21029565534206,
40.0222739267102));
#23673=CARTESIAN_POINT('Ctrl Pts',(0.2971131830738,-3.20905456793451,40.0231421733362));
#23674=CARTESIAN_POINT('Ctrl Pts',(0.317839679711471,-3.20704616524514,
40.0244469671753));
#23675=CARTESIAN_POINT('Ctrl Pts',(0.324847796302325,-3.20634388041727,
40.0248870356005));
#23676=CARTESIAN_POINT('Ctrl Pts',(0.33740301201393,-3.20504413317905,40.0256733651343));
#23677=CARTESIAN_POINT('Ctrl Pts',(0.342950889905818,-3.20445523869221,
40.0260201000121));
#23678=CARTESIAN_POINT('Ctrl Pts',(0.354987248919614,-3.20314598992632,
40.0267707701308));
#23679=CARTESIAN_POINT('Ctrl Pts',(0.361475059145022,-3.2024203289196,40.027174402342));
#23680=CARTESIAN_POINT('Ctrl Pts',(0.379659965633833,-3.20033038200326,
40.0283030861608));
#23681=CARTESIAN_POINT('Ctrl Pts',(0.391351996466248,-3.19892167273746,
40.0290256756629));
#23682=CARTESIAN_POINT('Ctrl Pts',(0.460668858059748,-3.19018432957703,
40.0332925773403));
#23683=CARTESIAN_POINT('Ctrl Pts',(0.518098742550746,-3.18136236880429,
40.0367579873582));
#23684=CARTESIAN_POINT('Ctrl Pts',(0.8238959272466,-3.12588644084873,40.054985652752));
#23685=CARTESIAN_POINT('Ctrl Pts',(1.06638357635951,-3.05169180061492,40.0687017116454));
#23686=CARTESIAN_POINT('Ctrl Pts',(1.44700665821806,-2.88424778755483,40.0921939520004));
#23687=CARTESIAN_POINT('Ctrl Pts',(1.59106414428608,-2.8073507326046,40.1015935547739));
#23688=CARTESIAN_POINT('Ctrl Pts',(1.74882749913779,-2.70708148875967,40.1128365923115));
#23689=CARTESIAN_POINT('Ctrl Pts',(1.76883783116284,-2.69404908799061,40.1142808564639));
#23690=CARTESIAN_POINT('Ctrl Pts',(1.79915210180886,-2.67382256825838,40.1164976866093));
#23691=CARTESIAN_POINT('Ctrl Pts',(1.80956213660343,-2.66678838281437,40.1172642282786));
#23692=CARTESIAN_POINT('Ctrl Pts',(1.8279854189055,-2.65418200720913,40.1186303575));
#23693=CARTESIAN_POINT('Ctrl Pts',(1.83601502811607,-2.64863391814042,40.119229022317));
#23694=CARTESIAN_POINT('Ctrl Pts',(1.84419128288443,-2.64292945774922,40.1198419819224));
#23695=CARTESIAN_POINT('Ctrl Pts',(1.84436331220659,-2.6428094102842,40.1198548801868));
#23696=CARTESIAN_POINT('Ctrl Pts',(1.84469492315573,-2.64257795360169,40.119879746363));
#23697=CARTESIAN_POINT('Ctrl Pts',(1.84485451146287,-2.64246654319754,40.1198917145635));
#23698=CARTESIAN_POINT('Ctrl Pts',(1.84516256000937,-2.64225144950816,40.1199148189596));
#23699=CARTESIAN_POINT('Ctrl Pts',(1.84531101617009,-2.6421477719631,40.1199259546724));
#23700=CARTESIAN_POINT('Ctrl Pts',(1.84559791493642,-2.64194737407912,40.119947477178));
#23701=CARTESIAN_POINT('Ctrl Pts',(1.84573635868543,-2.64185065536412,40.1199578639086));
#23702=CARTESIAN_POINT('Ctrl Pts',(1.84600420383836,-2.64166350371011,40.1199779608828));
#23703=CARTESIAN_POINT('Ctrl Pts',(1.84613360619568,-2.64157307214807,40.1199876710731));
#23704=CARTESIAN_POINT('Ctrl Pts',(1.84638421423636,-2.64139790977976,40.1200064780607));
#23705=CARTESIAN_POINT('Ctrl Pts',(1.84650542074391,-2.64131318013095,40.1200155748138));
#23706=CARTESIAN_POINT('Ctrl Pts',(1.84674037741264,-2.64114890913022,40.1200332101801));
#23707=CARTESIAN_POINT('Ctrl Pts',(1.8468541282786,-2.64106936876452,40.1200417487558));
#23708=CARTESIAN_POINT('Ctrl Pts',(1.84707482495552,-2.64091502524191,40.1200583163914));
#23709=CARTESIAN_POINT('Ctrl Pts',(1.84718177136025,-2.64084022293802,40.1200663454183));
#23710=CARTESIAN_POINT('Ctrl Pts',(1.84738943469184,-2.64069495667296,40.120081936941));
#23711=CARTESIAN_POINT('Ctrl Pts',(1.84749015211488,-2.64062449345748,40.1200894994073));
#23712=CARTESIAN_POINT('Ctrl Pts',(1.84768586820412,-2.64048755126454,40.1201041959611));
#23713=CARTESIAN_POINT('Ctrl Pts',(1.84778086732807,-2.64042107291253,40.1201113300251));
#23714=CARTESIAN_POINT('Ctrl Pts',(1.84796560191936,-2.64029178475038,40.1201252037812));
#23715=CARTESIAN_POINT('Ctrl Pts',(1.84805533776569,-2.64022897549687,40.1201319434515));
#23716=CARTESIAN_POINT('Ctrl Pts',(1.84822995269071,-2.64010674314742,40.1201450588323));
#23717=CARTESIAN_POINT('Ctrl Pts',(1.84831483212035,-2.64004732052278,40.1201514345254));
#23718=CARTESIAN_POINT('Ctrl Pts',(1.84848009940399,-2.63993160787134,40.1201638492545));
#23719=CARTESIAN_POINT('Ctrl Pts',(1.84856048753421,-2.63987531827889,40.1201698882729));
#23720=CARTESIAN_POINT('Ctrl Pts',(1.84871710084741,-2.63976564342265,40.1201816542276));
#23721=CARTESIAN_POINT('Ctrl Pts',(1.84879332631048,-2.63971225851419,40.1201873811512));
#23722=CARTESIAN_POINT('Ctrl Pts',(1.84894191112628,-2.63960818675532,40.120198545119));
#23723=CARTESIAN_POINT('Ctrl Pts',(1.84901427069464,-2.63955750023988,40.1202039821497));
#23724=CARTESIAN_POINT('Ctrl Pts',(1.84915539244532,-2.63945863845969,40.1202145864359));
#23725=CARTESIAN_POINT('Ctrl Pts',(1.84922415483558,-2.63941046347887,40.1202197536808));
#23726=CARTESIAN_POINT('Ctrl Pts',(1.84935832619262,-2.63931645511126,40.1202298366511));
#23727=CARTESIAN_POINT('Ctrl Pts',(1.84942373536371,-2.63927062196213,40.1202347523686));
#23728=CARTESIAN_POINT('Ctrl Pts',(1.84955142247948,-2.63918114268188,40.1202443489145));
#23729=CARTESIAN_POINT('Ctrl Pts',(1.84961370055251,-2.63913749679928,40.1202490297319));
#23730=CARTESIAN_POINT('Ctrl Pts',(1.84973532810732,-2.63905225103722,40.1202581716465));
#23731=CARTESIAN_POINT('Ctrl Pts',(1.84979467772745,-2.63901065136238,40.1202626327357));
#23732=CARTESIAN_POINT('Ctrl Pts',(1.8499508514083,-2.63890117735688,40.1202743722087));
#23733=CARTESIAN_POINT('Ctrl Pts',(1.85004767312273,-2.63883329970936,40.1202816507196));
#23734=CARTESIAN_POINT('Ctrl Pts',(1.85987454831579,-2.63194328254921,40.1210204291846));
#23735=CARTESIAN_POINT('Ctrl Pts',(1.86956669129953,-2.6250674579411,40.1217539912025));
#23736=CARTESIAN_POINT('Ctrl Pts',(1.88961513268072,-2.61067729289508,40.1232817217677));
#23737=CARTESIAN_POINT('Ctrl Pts',(1.89996513577431,-2.60315457714655,40.1240762073053));
#23738=CARTESIAN_POINT('Ctrl Pts',(1.92652292712574,-2.58360875843707,40.1261299611862));
#23739=CARTESIAN_POINT('Ctrl Pts',(1.94266288720805,-2.5714948341689,40.1273927576013));
#23740=CARTESIAN_POINT('Ctrl Pts',(2.05084929511193,-2.48869517951676,40.1359580608007));
#23741=CARTESIAN_POINT('Ctrl Pts',(2.13912313870307,-2.41324126002501,40.1434487349545));
#23742=CARTESIAN_POINT('Ctrl Pts',(2.3442565878826,-2.21778516637936,40.1621230029332));
#23743=CARTESIAN_POINT('Ctrl Pts',(2.45620502737752,-2.09312174580871,40.1734576634612));
#23744=CARTESIAN_POINT('Ctrl Pts',(2.62171048559569,-1.877161427229,40.1918679186159));
#23745=CARTESIAN_POINT('Ctrl Pts',(2.68136706640819,-1.79091419996341,40.1989376278261));
#23746=CARTESIAN_POINT('Ctrl Pts',(2.77646025055787,-1.63800175924701,40.2108366087151));
#23747=CARTESIAN_POINT('Ctrl Pts',(2.8139561781881,-1.57271546174028,40.2157314151553));
#23748=CARTESIAN_POINT('Ctrl Pts',(2.8547842455235,-1.49548340334282,40.2212603561159));
#23749=CARTESIAN_POINT('Ctrl Pts',(2.86037387661069,-1.48476428935119,40.222022011679));
#23750=CARTESIAN_POINT('Ctrl Pts',(2.86922201243464,-1.46756098992165,40.2232349863979));
#23751=CARTESIAN_POINT('Ctrl Pts',(2.87251909826765,-1.46109693323464,40.2236886411033));
#23752=CARTESIAN_POINT('Ctrl Pts',(2.87832755210492,-1.44961359117345,40.2244907368085));
#23753=CARTESIAN_POINT('Ctrl Pts',(2.88084767429952,-1.44459881637653,40.2248397236261));
#23754=CARTESIAN_POINT('Ctrl Pts',(2.88617297060559,-1.43393268709669,40.2255792429951));
#23755=CARTESIAN_POINT('Ctrl Pts',(2.88897464815871,-1.42827968244749,40.2259695567574));
#23756=CARTESIAN_POINT('Ctrl Pts',(2.8965202531976,-1.41294171382675,40.227024264696));
#23757=CARTESIAN_POINT('Ctrl Pts',(2.90123224814389,-1.40324100349815,40.2276866907242));
#23758=CARTESIAN_POINT('Ctrl Pts',(2.92476807779917,-1.35416181830449,40.2310156858405));
#23759=CARTESIAN_POINT('Ctrl Pts',(2.94284028211441,-1.31442536880162,40.2336383264671));
#23760=CARTESIAN_POINT('Ctrl Pts',(2.99340659042261,-1.19696666549488,40.2412148326157));
#23761=CARTESIAN_POINT('Ctrl Pts',(3.02366914678196,-1.11831978125285,40.2460666869733));
#23762=CARTESIAN_POINT('Ctrl Pts',(3.15302723056023,-0.738329026262928,
40.2688664922471));
#23763=CARTESIAN_POINT('Ctrl Pts',(3.21035471649592,-0.424663076438896,
40.2859978879917));
#23764=CARTESIAN_POINT('Ctrl Pts',(3.2221453506905,-0.071937250536365,40.3069233384524));
#23765=CARTESIAN_POINT('Ctrl Pts',(3.22274504656494,-0.0361911623234127,
40.3090599752032));
#23766=CARTESIAN_POINT('Ctrl Pts',(3.22274996944047,-0.000443814660293801,
40.3112149259812));
#23767=CARTESIAN_POINT('Ctrl Pts',(-1.47525540498233,-2.86526422037662,
41.155741540048));
#23768=CARTESIAN_POINT('Ctrl Pts',(-1.6289715779912,-2.78611947224071,41.1441838822727));
#23769=CARTESIAN_POINT('Ctrl Pts',(-1.77608938213473,-2.69472340804177,
41.1329065881922));
#23770=CARTESIAN_POINT('Ctrl Pts',(-1.93294765727014,-2.57882119718988,
41.1206854600813));
#23771=CARTESIAN_POINT('Ctrl Pts',(-1.95057667855932,-2.56551282847913,
41.1193085513726));
#23772=CARTESIAN_POINT('Ctrl Pts',(-1.97848089032937,-2.54399368052792,
41.1171232728468));
#23773=CARTESIAN_POINT('Ctrl Pts',(-1.98884480585058,-2.53589960890422,
41.1163103308354));
#23774=CARTESIAN_POINT('Ctrl Pts',(-2.00707472009297,-2.52148180279603,
41.1148779535633));
#23775=CARTESIAN_POINT('Ctrl Pts',(-2.01496104506488,-2.51518416908886,
41.1142574885869));
#23776=CARTESIAN_POINT('Ctrl Pts',(-2.03125022220081,-2.50205064480447,
41.1129741619813));
#23777=CARTESIAN_POINT('Ctrl Pts',(-2.0396484637143,-2.49520921835311,41.1123115342925));
#23778=CARTESIAN_POINT('Ctrl Pts',(-2.06120111631275,-2.47747034382921,
41.1106083649862));
#23779=CARTESIAN_POINT('Ctrl Pts',(-2.07430377794486,-2.46651032852507,
41.109570379794));
#23780=CARTESIAN_POINT('Ctrl Pts',(-2.12939504831909,-2.41967850006918,
41.105194343007));
#23781=CARTESIAN_POINT('Ctrl Pts',(-2.17054663580616,-2.38283343274123,
41.1018966080188));
#23782=CARTESIAN_POINT('Ctrl Pts',(-2.27615696560908,-2.28326776552103,
41.0933336033125));
#23783=CARTESIAN_POINT('Ctrl Pts',(-2.33897420853146,-2.21887442229304,
41.0881382289355));
#23784=CARTESIAN_POINT('Ctrl Pts',(-2.56824119044034,-1.96328293183994,
41.0685722358207));
#23785=CARTESIAN_POINT('Ctrl Pts',(-2.71460484173427,-1.75534803790454,
41.0548320395916));
#23786=CARTESIAN_POINT('Ctrl Pts',(-2.8757065343103,-1.4573001929816,41.0352890107141));
#23787=CARTESIAN_POINT('Ctrl Pts',(-2.91331146018282,-1.38058881519907,
41.0302634888056));
#23788=CARTESIAN_POINT('Ctrl Pts',(-2.95335411860204,-1.28996292813186,
41.0242290024043));
#23789=CARTESIAN_POINT('Ctrl Pts',(-2.95880596390388,-1.27740837571555,
41.0233909103942));
#23790=CARTESIAN_POINT('Ctrl Pts',(-2.96693369862355,-1.25836056346688,
41.0221155898173));
#23791=CARTESIAN_POINT('Ctrl Pts',(-2.96966868800489,-1.25189247181759,
41.0216818742675));
#23792=CARTESIAN_POINT('Ctrl Pts',(-2.97453691650705,-1.2402736696007,41.0209015201471));
#23793=CARTESIAN_POINT('Ctrl Pts',(-2.97667795048034,-1.23512631806238,
41.0205553623453));
#23794=CARTESIAN_POINT('Ctrl Pts',(-2.98130019973509,-1.22393194386215,
41.0198015546003));
#23795=CARTESIAN_POINT('Ctrl Pts',(-2.98377634346722,-1.21788300526373,
41.0193936139739));
#23796=CARTESIAN_POINT('Ctrl Pts',(-2.99068274843617,-1.20086395241495,
41.0182442038285));
#23797=CARTESIAN_POINT('Ctrl Pts',(-2.99507097235738,-1.18987705007791,
41.0175002699164));
#23798=CARTESIAN_POINT('Ctrl Pts',(-3.02104641257968,-1.12378754707162,
41.0130148969916));
#23799=CARTESIAN_POINT('Ctrl Pts',(-3.04117147169789,-1.06812682082553,
41.0091942321191));
#23800=CARTESIAN_POINT('Ctrl Pts',(-3.13877048713662,-0.773024012652112,
40.9888273279141));
#23801=CARTESIAN_POINT('Ctrl Pts',(-3.18953323793687,-0.525670336888177,
40.971460806899));
#23802=CARTESIAN_POINT('Ctrl Pts',(-3.22491441168477,-0.112434273603035,
40.9438025902794));
#23803=CARTESIAN_POINT('Ctrl Pts',(-3.22647460986668,0.0508973108841155,
40.9331915046951));
#23804=CARTESIAN_POINT('Ctrl Pts',(-3.21420885422605,0.235494099923247,
40.921601093887));
#23805=CARTESIAN_POINT('Ctrl Pts',(-3.2125364166089,0.257304954853257,40.920237705593));
#23806=CARTESIAN_POINT('Ctrl Pts',(-3.20950946619191,0.292125950915957,
40.9180703983877));
#23807=CARTESIAN_POINT('Ctrl Pts',(-3.20829761615469,0.305147503778617,
40.9172620084051));
#23808=CARTESIAN_POINT('Ctrl Pts',(-3.20601252250869,0.328180808526523,
40.915835673054));
#23809=CARTESIAN_POINT('Ctrl Pts',(-3.20497156509783,0.338195517648916,
40.9152167170135));
#23810=CARTESIAN_POINT('Ctrl Pts',(-3.20271269702035,0.35897966734687,40.9139345949595));
#23811=CARTESIAN_POINT('Ctrl Pts',(-3.20148735818182,0.369748186159671,
40.9132716720292));
#23812=CARTESIAN_POINT('Ctrl Pts',(-3.19818197095117,0.397547492113584,
40.9115637164637));
#23813=CARTESIAN_POINT('Ctrl Pts',(-3.19602018438141,0.414568361742573,
40.9105212797827));
#23814=CARTESIAN_POINT('Ctrl Pts',(-3.18621639073025,0.487118571474866,
40.9060912570909));
#23815=CARTESIAN_POINT('Ctrl Pts',(-3.17726204624829,0.542462769683345,
40.9027453591955));
#23816=CARTESIAN_POINT('Ctrl Pts',(-3.14983773516817,0.687805389879164,
40.8940240733117));
#23817=CARTESIAN_POINT('Ctrl Pts',(-3.1289557240749,0.777297895401345,40.8887221737297));
#23818=CARTESIAN_POINT('Ctrl Pts',(-3.03866194530129,1.10104807574918,40.8695889237014));
#23819=CARTESIAN_POINT('Ctrl Pts',(-2.94652009072388,1.32807344349637,40.8563193420581));
#23820=CARTESIAN_POINT('Ctrl Pts',(-2.78606595135321,1.62241754024192,40.8370379407796));
#23821=CARTESIAN_POINT('Ctrl Pts',(-2.73913942788136,1.700445250369,40.8316961137062));
#23822=CARTESIAN_POINT('Ctrl Pts',(-2.68132677909077,1.78795889917913,40.8253098197635));
#23823=CARTESIAN_POINT('Ctrl Pts',(-2.67359945158529,1.79949333919269,40.8244598891309));
#23824=CARTESIAN_POINT('Ctrl Pts',(-2.66183028410736,1.81681781036051,40.8231702975767));
#23825=CARTESIAN_POINT('Ctrl Pts',(-2.65784343029871,1.82264525215646,40.8227342756508));
#23826=CARTESIAN_POINT('Ctrl Pts',(-2.65067318450503,1.83305219166411,40.8219514943385));
#23827=CARTESIAN_POINT('Ctrl Pts',(-2.64749702730815,1.83763656853331,40.8216052292907));
#23828=CARTESIAN_POINT('Ctrl Pts',(-2.6405881222401,1.84755359884192,40.8208530340072));
#23829=CARTESIAN_POINT('Ctrl Pts',(-2.63685116277833,1.85288312515524,40.8204468226827));
#23830=CARTESIAN_POINT('Ctrl Pts',(-2.62635864002297,1.8677511821824,40.8193081510671));
#23831=CARTESIAN_POINT('Ctrl Pts',(-2.61956737364725,1.87726421944601,40.8185733030149));
#23832=CARTESIAN_POINT('Ctrl Pts',(-2.57958681669459,1.93262859920604,40.8142607198082));
#23833=CARTESIAN_POINT('Ctrl Pts',(-2.54524812887532,1.97763305004437,40.810610633954));
#23834=CARTESIAN_POINT('Ctrl Pts',(-2.35055066220807,2.21933032591839,40.7903038460388));
#23835=CARTESIAN_POINT('Ctrl Pts',(-2.16857512377057,2.39745746428005,40.7727871770924));
#23836=CARTESIAN_POINT('Ctrl Pts',(-1.83790536018683,2.65236344919967,40.7449406447598));
#23837=CARTESIAN_POINT('Ctrl Pts',(-1.70078027280591,2.74231455234003,40.7342852963149));
#23838=CARTESIAN_POINT('Ctrl Pts',(-1.53817387918843,2.83206999741515,40.7226484448609));
#23839=CARTESIAN_POINT('Ctrl Pts',(-1.51884903318719,2.842480783709,40.7212802573875));
#23840=CARTESIAN_POINT('Ctrl Pts',(-1.4878151546486,2.8587926604125,40.7191062013691));
#23841=CARTESIAN_POINT('Ctrl Pts',(-1.47617412966667,2.86482099906657,40.7182958319227));
#23842=CARTESIAN_POINT('Ctrl Pts',(-1.45551310430304,2.87536099805379,40.71686649845));
#23843=CARTESIAN_POINT('Ctrl Pts',(-1.44650816084706,2.87990163203849,40.7162465180284));
#23844=CARTESIAN_POINT('Ctrl Pts',(-1.42777319535233,2.88923847000818,40.7149627483162));
#23845=CARTESIAN_POINT('Ctrl Pts',(-1.41803996138554,2.89402797263671,40.7142992001003));
#23846=CARTESIAN_POINT('Ctrl Pts',(-1.39285094914866,2.90626532485832,40.712590618553));
#23847=CARTESIAN_POINT('Ctrl Pts',(-1.37735941684391,2.91363912651329,40.7115481738426));
#23848=CARTESIAN_POINT('Ctrl Pts',(-1.31113530347301,2.94451487272887,40.7071264797406));
#23849=CARTESIAN_POINT('Ctrl Pts',(-1.25985275211492,2.96681904290607,40.7037886209601));
#23850=CARTESIAN_POINT('Ctrl Pts',(-1.12318041107601,3.02207816115107,40.6950946121609));
#23851=CARTESIAN_POINT('Ctrl Pts',(-1.03692109068343,3.05275076061364,40.689811170639));
#23852=CARTESIAN_POINT('Ctrl Pts',(-0.714752190887211,3.15207465386251,
40.670613102102));
#23853=CARTESIAN_POINT('Ctrl Pts',(-0.472553630327219,3.19736209181319,
40.6572690935814));
#23854=CARTESIAN_POINT('Ctrl Pts',(-0.138080133596984,3.22104043569993,
40.6379683018134));
#23855=CARTESIAN_POINT('Ctrl Pts',(-0.0483650945236136,3.22363540986981,
40.6326990910141));
#23856=CARTESIAN_POINT('Ctrl Pts',(0.0551846605660254,3.22230727058895,
40.6263931471895));
#23857=CARTESIAN_POINT('Ctrl Pts',(0.0690358363103136,3.22204027445034,
40.6255450017194));
#23858=CARTESIAN_POINT('Ctrl Pts',(0.0899438266587515,3.22150237259412,
40.6242571638466));
#23859=CARTESIAN_POINT('Ctrl Pts',(0.097002387667862,3.22129755892398,40.6238210828002));
#23860=CARTESIAN_POINT('Ctrl Pts',(0.109639740196263,3.22088929556887,40.6230379129507));
#23861=CARTESIAN_POINT('Ctrl Pts',(0.115218727679125,3.22069454792429,40.6226913166813));
#23862=CARTESIAN_POINT('Ctrl Pts',(0.127311456721132,3.22024096148563,40.6219381830628));
#23863=CARTESIAN_POINT('Ctrl Pts',(0.13382483501755,3.21997685842438,40.6215313635449));
#23864=CARTESIAN_POINT('Ctrl Pts',(0.152057546553323,3.21918214617044,40.6203893824988));
#23865=CARTESIAN_POINT('Ctrl Pts',(0.163774706545357,3.21860731112061,40.619651811571));
#23866=CARTESIAN_POINT('Ctrl Pts',(0.232715930597485,3.21484767990292,40.6152914587745));
#23867=CARTESIAN_POINT('Ctrl Pts',(0.2898461134694,3.21020101832495,40.6115944905963));
#23868=CARTESIAN_POINT('Ctrl Pts',(0.598644070961123,3.1767754761183,40.5912641572256));
#23869=CARTESIAN_POINT('Ctrl Pts',(0.846375375800036,3.11992482108336,40.5737814987779));
#23870=CARTESIAN_POINT('Ctrl Pts',(1.23869557149647,2.97966904090722,40.5459965942905));
#23871=CARTESIAN_POINT('Ctrl Pts',(1.3881086345207,2.91306767666634,40.5353688691061));
#23872=CARTESIAN_POINT('Ctrl Pts',(1.55284964782652,2.82406539641601,40.5236373674335));
#23873=CARTESIAN_POINT('Ctrl Pts',(1.57372543889928,2.81248567720223,40.5221501073252));
#23874=CARTESIAN_POINT('Ctrl Pts',(1.60538755351386,2.79445990480158,40.5198929319164));
#23875=CARTESIAN_POINT('Ctrl Pts',(1.61626769312528,2.78818114688704,40.5191170238612));
#23876=CARTESIAN_POINT('Ctrl Pts',(1.63549981824309,2.77693218414056,40.5177449258675));
#23877=CARTESIAN_POINT('Ctrl Pts',(1.64386650227094,2.77198754268475,40.5171478177317));
#23878=CARTESIAN_POINT('Ctrl Pts',(1.66158194992431,2.76140944383695,40.515883037531));
#23879=CARTESIAN_POINT('Ctrl Pts',(1.67092473725706,2.7557661765612,40.5152157335385));
#23880=CARTESIAN_POINT('Ctrl Pts',(1.6900071716636,2.74410720717462,40.5138521065015));
#23881=CARTESIAN_POINT('Ctrl Pts',(1.69974380443528,2.73808685203732,40.5131559659387));
#23882=CARTESIAN_POINT('Ctrl Pts',(1.72381559626856,2.72302489695387,40.5114338600625));
#23883=CARTESIAN_POINT('Ctrl Pts',(1.73811200718185,2.71392178712342,40.5104101648386));
#23884=CARTESIAN_POINT('Ctrl Pts',(1.9288783125375,2.59032732965147,40.4967351122949));
#23885=CARTESIAN_POINT('Ctrl Pts',(2.0938075593618,2.45893363841088,40.4847836469251));
#23886=CARTESIAN_POINT('Ctrl Pts',(2.42373322905084,2.13865464140379,40.4590301853454));
#23887=CARTESIAN_POINT('Ctrl Pts',(2.58189321732426,1.94476591908205,40.4453794647995));
#23888=CARTESIAN_POINT('Ctrl Pts',(2.72753903046045,1.71671203891744,40.4290420576392));
#23889=CARTESIAN_POINT('Ctrl Pts',(2.73880217392482,1.69868536933102,40.4277485893435));
#23890=CARTESIAN_POINT('Ctrl Pts',(2.75433566026193,1.67326789575566,40.4259199916886));
#23891=CARTESIAN_POINT('Ctrl Pts',(2.75875649509246,1.66596908052015,40.4253943457105));
#23892=CARTESIAN_POINT('Ctrl Pts',(2.76584271299706,1.65416415703902,40.4245431480926));
#23893=CARTESIAN_POINT('Ctrl Pts',(2.76852622999115,1.64966890144346,40.424218776408));
#23894=CARTESIAN_POINT('Ctrl Pts',(2.77414418653196,1.64020574504123,40.4235353805807));
#23895=CARTESIAN_POINT('Ctrl Pts',(2.77707624410192,1.63523649250323,40.4231762000395));
#23896=CARTESIAN_POINT('Ctrl Pts',(2.78420116619758,1.62308674109628,40.4222972819549));
#23897=CARTESIAN_POINT('Ctrl Pts',(2.78837959741042,1.61589786808539,40.4217766189935));
#23898=CARTESIAN_POINT('Ctrl Pts',(2.80324190456623,1.59009838977428,40.4199060809042));
#23899=CARTESIAN_POINT('Ctrl Pts',(2.81376737717131,1.57139783429284,40.4185465640782));
#23900=CARTESIAN_POINT('Ctrl Pts',(2.87764461137888,1.45520777051212,40.4100836427643));
#23901=CARTESIAN_POINT('Ctrl Pts',(2.92610575809438,1.35512663248414,40.4027272278837));
#23902=CARTESIAN_POINT('Ctrl Pts',(3.09368764517555,0.957921600581406,40.37379496271));
#23903=CARTESIAN_POINT('Ctrl Pts',(3.1735059966434,0.646114547682966,40.351870055001));
#23904=CARTESIAN_POINT('Ctrl Pts',(3.21046813876591,0.284426754869854,40.3287939816476));
#23905=CARTESIAN_POINT('Ctrl Pts',(3.21401014084984,0.241129345005754,40.3260641302216));
#23906=CARTESIAN_POINT('Ctrl Pts',(3.2176651823808,0.181681614284291,40.322358818661));
#23907=CARTESIAN_POINT('Ctrl Pts',(3.21853373206233,0.165584013924313,40.3213597545801));
#23908=CARTESIAN_POINT('Ctrl Pts',(3.21972472178267,0.139934277854415,40.3197745050124));
#23909=CARTESIAN_POINT('Ctrl Pts',(3.22012551373191,0.130386215296407,40.3191858647466));
#23910=CARTESIAN_POINT('Ctrl Pts',(3.22084429607181,0.111229517769128,40.3180077380531));
#23911=CARTESIAN_POINT('Ctrl Pts',(3.22116177312373,0.101620960980645,40.3174182737083));
#23912=CARTESIAN_POINT('Ctrl Pts',(3.22171475437482,0.0822603084688677,
40.3162334156258));
#23913=CARTESIAN_POINT('Ctrl Pts',(3.22194898627566,0.0725082756372689,
40.3156380678866));
#23914=CARTESIAN_POINT('Ctrl Pts',(3.22235110246199,0.0518618064420085,
40.3143806714447));
#23915=CARTESIAN_POINT('Ctrl Pts',(3.22250802367108,0.040967260254133,40.3137189716861));
#23916=CARTESIAN_POINT('Ctrl Pts',(3.22270461541348,0.0198998894239589,
40.3124427752497));
#23917=CARTESIAN_POINT('Ctrl Pts',(3.22275137521086,0.00972729443329853,
40.3118280689229));
#23918=CARTESIAN_POINT('Ctrl Pts',(3.22274996921859,-0.000445422926308301,
40.3112148290304));
#23919=CARTESIAN_POINT('Origin',(0.,0.,32.));
#23920=CARTESIAN_POINT('',(3.93418083709056,-0.00237382471849651,7.40416393604293));
#23921=CARTESIAN_POINT('',(-1.74869731566807,-3.5228605845499,7.00006232951278));
#23922=CARTESIAN_POINT('Ctrl Pts',(3.93299927912326,-0.0023812635191002,
7.40416352203497));
#23923=CARTESIAN_POINT('Ctrl Pts',(3.93292585737052,-0.123647850894427,
7.39799858961059));
#23924=CARTESIAN_POINT('Ctrl Pts',(3.92724440793317,-0.244754597722826,
7.3918336571862));
#23925=CARTESIAN_POINT('Ctrl Pts',(3.91599597959321,-0.36532791819104,7.38566872476181));
#23926=CARTESIAN_POINT('Ctrl Pts',(3.90526101570742,-0.480397348488062,
7.37978520708859));
#23927=CARTESIAN_POINT('Ctrl Pts',(3.88943218768411,-0.595182928816867,
7.37390168941536));
#23928=CARTESIAN_POINT('Ctrl Pts',(3.86853025860236,-0.709198588745032,
7.36801817174214));
#23929=CARTESIAN_POINT('Ctrl Pts',(3.84765547744091,-0.823066162435068,
7.36214229572095));
#23930=CARTESIAN_POINT('Ctrl Pts',(3.82172077314429,-0.936165403225679,
7.35626641969975));
#23931=CARTESIAN_POINT('Ctrl Pts',(3.7907987530201,-1.04801422418841,7.35039054367856));
#23932=CARTESIAN_POINT('Ctrl Pts',(3.75990870699832,-1.15974739081674,7.34452074345258));
#23933=CARTESIAN_POINT('Ctrl Pts',(3.72404171256226,-1.27023231513042,7.33865094322661));
#23934=CARTESIAN_POINT('Ctrl Pts',(3.68332150352764,-1.37899662858577,7.33278114300062));
#23935=CARTESIAN_POINT('Ctrl Pts',(3.64110685382046,-1.49175261638668,7.32669591980886));
#23936=CARTESIAN_POINT('Ctrl Pts',(3.59367600534624,-1.60265883264998,7.32061069661709));
#23937=CARTESIAN_POINT('Ctrl Pts',(3.54122374104448,-1.7112052524063,7.31452547342533));
#23938=CARTESIAN_POINT('Ctrl Pts',(3.49068837256741,-1.81578478566906,7.30866263794331));
#23939=CARTESIAN_POINT('Ctrl Pts',(3.43549237357525,-1.91817357726072,7.30279980246129));
#23940=CARTESIAN_POINT('Ctrl Pts',(3.37585883407791,-2.01793610710997,7.29693696697926));
#23941=CARTESIAN_POINT('Ctrl Pts',(3.31623521582783,-2.11768203944153,7.29107510689868));
#23942=CARTESIAN_POINT('Ctrl Pts',(3.25217573637191,-2.21480222565135,7.2852132468181));
#23943=CARTESIAN_POINT('Ctrl Pts',(3.18394863562698,-2.30888719639767,7.27935138673752));
#23944=CARTESIAN_POINT('Ctrl Pts',(3.11571652777115,-2.40297907193515,7.27348909646156));
#23945=CARTESIAN_POINT('Ctrl Pts',(3.04331643237488,-2.49403495594284,7.26762680618561));
#23946=CARTESIAN_POINT('Ctrl Pts',(2.96705855633027,-2.58167630103143,7.26176451590965));
#23947=CARTESIAN_POINT('Ctrl Pts',(2.8907768004645,-2.66934509062484,7.25590038988307));
#23948=CARTESIAN_POINT('Ctrl Pts',(2.81063513182465,-2.75359690462564,7.25003626385649));
#23949=CARTESIAN_POINT('Ctrl Pts',(2.72698200459874,-2.83408859187476,7.24417213782991));
#23950=CARTESIAN_POINT('Ctrl Pts',(2.64323690311214,-2.91466877747022,7.23830156436169));
#23951=CARTESIAN_POINT('Ctrl Pts',(2.55597293371334,-2.9914802987659,7.23243099089347));
#23952=CARTESIAN_POINT('Ctrl Pts',(2.46557322678828,-3.06421893201919,7.22656041742525));
#23953=CARTESIAN_POINT('Ctrl Pts',(2.37511446262001,-3.13700508470923,7.22068600876887));
#23954=CARTESIAN_POINT('Ctrl Pts',(2.2815162124136,-3.2057128073294,7.2148116001125));
#23955=CARTESIAN_POINT('Ctrl Pts',(2.18519089692271,-3.27008099960936,7.20893719145613));
#23956=CARTESIAN_POINT('Ctrl Pts',(2.08872771426264,-3.33454131990789,7.20305437495714));
#23957=CARTESIAN_POINT('Ctrl Pts',(1.98953002689324,-3.39464950063828,7.19717155845815));
#23958=CARTESIAN_POINT('Ctrl Pts',(1.88803521411711,-3.45019014407232,7.19128874195916));
#23959=CARTESIAN_POINT('Ctrl Pts',(1.8618515330919,-3.46451854620277,7.18977109010557));
#23960=CARTESIAN_POINT('Ctrl Pts',(1.83551507272312,-3.47854321029207,7.18825343825199));
#23961=CARTESIAN_POINT('Ctrl Pts',(1.80903354477158,-3.49226096302828,7.1867357863984));
#23962=CARTESIAN_POINT('Ctrl Pts',(1.70742084100427,-3.54489757628143,7.18091237966361));
#23963=CARTESIAN_POINT('Ctrl Pts',(1.60332732097401,-3.59318953488544,7.17508897292881));
#23964=CARTESIAN_POINT('Ctrl Pts',(1.49716436618334,-3.63689261054418,7.16926556619402));
#23965=CARTESIAN_POINT('Ctrl Pts',(1.39113729163722,-3.68053974969833,7.1634496129625));
#23966=CARTESIAN_POINT('Ctrl Pts',(1.28304643338149,-3.7196095233296,7.15763365973098));
#23967=CARTESIAN_POINT('Ctrl Pts',(1.17332818810424,-3.75390329696971,7.15181770649946));
#23968=CARTESIAN_POINT('Ctrl Pts',(1.06371979961478,-3.78816273353302,7.14600757656505));
#23969=CARTESIAN_POINT('Ctrl Pts',(0.952487663460509,-3.81765555398607,
7.14019744663064));
#23970=CARTESIAN_POINT('Ctrl Pts',(0.840087882685277,-3.84223129826477,
7.13438731669622));
#23971=CARTESIAN_POINT('Ctrl Pts',(0.727766419218824,-3.86678991878984,
7.12858123511259));
#23972=CARTESIAN_POINT('Ctrl Pts',(0.614279338846755,-3.88643818659611,
7.12277515352895));
#23973=CARTESIAN_POINT('Ctrl Pts',(0.500096915293078,-3.90107575872532,
7.11696907194531));
#23974=CARTESIAN_POINT('Ctrl Pts',(0.385955601725311,-3.91570806077561,
7.11116508077038));
#23975=CARTESIAN_POINT('Ctrl Pts',(0.271119859460527,-3.92533319898689,
7.10536108959544));
#23976=CARTESIAN_POINT('Ctrl Pts',(0.156068457457715,-3.92990224262472,
7.09955709842051));
#23977=CARTESIAN_POINT('Ctrl Pts',(0.0410294744845688,-3.93447079306482,
7.09375373374762));
#23978=CARTESIAN_POINT('Ctrl Pts',(-0.0742247014207859,-3.93398431752344,
7.08795036907474));
#23979=CARTESIAN_POINT('Ctrl Pts',(-0.189212714966521,-3.9284459457265,
7.08214700440185));
#23980=CARTESIAN_POINT('Ctrl Pts',(-0.304217305000114,-3.92290677552676,
7.0763428031252));
#23981=CARTESIAN_POINT('Ctrl Pts',(-0.418955236063756,-3.91231428262367,
7.07053860184856));
#23982=CARTESIAN_POINT('Ctrl Pts',(-0.53294851104485,-3.89672360895343,
7.06473440057192));
#23983=CARTESIAN_POINT('Ctrl Pts',(-0.647054491955444,-3.88111752067766,
7.05892446064184));
#23984=CARTESIAN_POINT('Ctrl Pts',(-0.760413929013011,-3.86050344122573,
7.05311452071175));
#23985=CARTESIAN_POINT('Ctrl Pts',(-0.872557250876692,-3.83498798484982,
7.04730458078166));
#23986=CARTESIAN_POINT('Ctrl Pts',(-0.984759398021493,-3.80945914422714,
7.0414915932216));
#23987=CARTESIAN_POINT('Ctrl Pts',(-1.09574375418876,-3.77902391875517,
7.03567860566153));
#23988=CARTESIAN_POINT('Ctrl Pts',(-1.20505597687301,-3.74383881765797,
7.02986561810146));
#23989=CARTESIAN_POINT('Ctrl Pts',(-1.31453623477521,-3.70859962987232,
7.02404369479197));
#23990=CARTESIAN_POINT('Ctrl Pts',(-1.4223388316586,-3.66859613125696,7.01822177148247));
#23991=CARTESIAN_POINT('Ctrl Pts',(-1.52802922734547,-3.62403306833395,
7.01239984817297));
#23992=CARTESIAN_POINT('Ctrl Pts',(-1.60268710010629,-3.59255448922639,
7.00828734195291));
#23993=CARTESIAN_POINT('Ctrl Pts',(-1.67629148578956,-3.55880179689948,
7.00417483573285));
#23994=CARTESIAN_POINT('Ctrl Pts',(-1.74869731566807,-3.5228605845499,7.00006232951278));
#23995=CARTESIAN_POINT('',(1.748694475331,-3.52286199445094,7.));
#23996=CARTESIAN_POINT('Origin',(0.,0.,7.));
#23997=CARTESIAN_POINT('',(3.93500029318814,-0.00400916611326436,7.22083647796505));
#23998=CARTESIAN_POINT('Ctrl Pts',(1.74869447533099,-3.52286199445094,7.));
#23999=CARTESIAN_POINT('Ctrl Pts',(2.9229184098028,-2.93999530530824,7.06631097945448));
#24000=CARTESIAN_POINT('Ctrl Pts',(3.86598732707265,-1.59538332201294,7.13992313877617));
#24001=CARTESIAN_POINT('Ctrl Pts',(3.93807145761699,-0.14775304387093,7.21353529809785));
#24002=CARTESIAN_POINT('Ctrl Pts',(3.93699603905802,-0.00401119947441216,
7.22083647796505));
#24003=CARTESIAN_POINT('',(3.93141612693361,-0.00220398940945714,8.47083644545494));
#24004=CARTESIAN_POINT('Ctrl Pts',(3.9329979586749,-0.00400712603929224,
7.22083647796505));
#24005=CARTESIAN_POINT('Ctrl Pts',(3.93311290453778,0.108812345978177,7.22657287120762));
#24006=CARTESIAN_POINT('Ctrl Pts',(3.92836938073138,0.221859929722491,7.23230926445019));
#24007=CARTESIAN_POINT('Ctrl Pts',(3.91873516811271,0.334669511901911,7.23804565769276));
#24008=CARTESIAN_POINT('Ctrl Pts',(3.90911290769752,0.447339142521888,7.24377493436629));
#24009=CARTESIAN_POINT('Ctrl Pts',(3.89461204877992,0.559770931113545,7.24950421103982));
#24010=CARTESIAN_POINT('Ctrl Pts',(3.87525235530899,0.671496971454175,7.25523348771335));
#24011=CARTESIAN_POINT('Ctrl Pts',(3.85517041850384,0.787391124684349,7.26117650392225));
#24012=CARTESIAN_POINT('Ctrl Pts',(3.82986000999708,0.902525375176162,7.26711952013114));
#24013=CARTESIAN_POINT('Ctrl Pts',(3.79940243032467,1.01638091896837,7.27306253634004));
#24014=CARTESIAN_POINT('Ctrl Pts',(3.7700858418477,1.12597124620641,7.27878291735463));
#24015=CARTESIAN_POINT('Ctrl Pts',(3.7360009146518,1.23437648833816,7.28450329836921));
#24016=CARTESIAN_POINT('Ctrl Pts',(3.69727230456486,1.34114373051425,7.29022367938379));
#24017=CARTESIAN_POINT('Ctrl Pts',(3.65855424625676,1.44788188348923,7.2959425018556));
#24018=CARTESIAN_POINT('Ctrl Pts',(3.61519516540431,1.55298251607409,7.30166132432741));
#24019=CARTESIAN_POINT('Ctrl Pts',(3.56736922138118,1.65600900913679,7.30738014679922));
#24020=CARTESIAN_POINT('Ctrl Pts',(3.51954362641718,1.75903475025746,7.31309892753203));
#24021=CARTESIAN_POINT('Ctrl Pts',(3.46725141621909,1.85998598947352,7.31881770826484));
#24022=CARTESIAN_POINT('Ctrl Pts',(3.410714010603,1.95844809425127,7.32453648899765));
#24023=CARTESIAN_POINT('Ctrl Pts',(3.35416202302715,2.05693559408266,7.3302567447014));
#24024=CARTESIAN_POINT('Ctrl Pts',(3.29336288198745,2.15293230961354,7.33597700040514));
#24025=CARTESIAN_POINT('Ctrl Pts',(3.22858235517417,2.24605097356627,7.34169725610889));
#24026=CARTESIAN_POINT('Ctrl Pts',(3.16373129213117,2.33927102970884,7.34742374030893));
#24027=CARTESIAN_POINT('Ctrl Pts',(3.09489044247763,2.42960642705178,7.35315022450896));
#24028=CARTESIAN_POINT('Ctrl Pts',(3.02236691452957,2.51670165771729,7.35887670870899));
#24029=CARTESIAN_POINT('Ctrl Pts',(2.94979643021604,2.6038532793996,7.36460690060076));
#24030=CARTESIAN_POINT('Ctrl Pts',(2.87353881682546,2.68776024383179,7.37033709249253));
#24031=CARTESIAN_POINT('Ctrl Pts',(2.79393781419547,2.7681041328694,7.37606728438429));
#24032=CARTESIAN_POINT('Ctrl Pts',(2.71421878928923,2.84856714564105,7.38180597227822));
#24033=CARTESIAN_POINT('Ctrl Pts',(2.63114680560452,2.92545625576873,7.38754466017214));
#24034=CARTESIAN_POINT('Ctrl Pts',(2.54509822031751,2.99849362996433,7.39328334806607));
#24035=CARTESIAN_POINT('Ctrl Pts',(2.52219402365628,3.0179345350834,7.39481085761967));
#24036=CARTESIAN_POINT('Ctrl Pts',(2.49907908717383,3.03710278437769,7.39633836717327));
#24037=CARTESIAN_POINT('Ctrl Pts',(2.47576082822077,3.05599367169627,7.39786587672687));
#24038=CARTESIAN_POINT('Ctrl Pts',(2.38599445874981,3.12871635541322,7.40374620369447));
#24039=CARTESIAN_POINT('Ctrl Pts',(2.29287298841318,3.19760055359902,7.40962653066206));
#24040=CARTESIAN_POINT('Ctrl Pts',(2.19675830299184,3.26232155960084,7.41550685762966));
#24041=CARTESIAN_POINT('Ctrl Pts',(2.1007680438308,3.3269587803548,7.42137957215915));
#24042=CARTESIAN_POINT('Ctrl Pts',(2.00179261458001,3.38744329934152,7.42725228668864));
#24043=CARTESIAN_POINT('Ctrl Pts',(1.90022729055141,3.44349027067649,7.43312500121813));
#24044=CARTESIAN_POINT('Ctrl Pts',(1.79876649403358,3.49947956041141,7.4389916717534));
#24045=CARTESIAN_POINT('Ctrl Pts',(1.69472146340341,3.55104018909941,7.44485834228867));
#24046=CARTESIAN_POINT('Ctrl Pts',(1.58851625654027,3.59793066952481,7.45072501282394));
#24047=CARTESIAN_POINT('Ctrl Pts',(1.47833310201707,3.64657744686256,7.45681142125171));
#24048=CARTESIAN_POINT('Ctrl Pts',(1.36582515837295,3.6901971321489,7.46289782967947));
#24049=CARTESIAN_POINT('Ctrl Pts',(1.25149413262529,3.72857230532069,7.46898423810724));
#24050=CARTESIAN_POINT('Ctrl Pts',(1.14141986485899,3.76551869900226,7.47484403816266));
#24051=CARTESIAN_POINT('Ctrl Pts',(1.02965626948239,3.79760398859222,7.48070383821808));
#24052=CARTESIAN_POINT('Ctrl Pts',(0.916670495179452,3.82468354289181,7.48656363827351));
#24053=CARTESIAN_POINT('Ctrl Pts',(0.803702774904854,3.85175877014188,7.49242250198985));
#24054=CARTESIAN_POINT('Ctrl Pts',(0.689513664648633,3.87382975664777,7.4982813657062));
#24055=CARTESIAN_POINT('Ctrl Pts',(0.574583218563554,3.89080237546771,7.50414022942254));
#24056=CARTESIAN_POINT('Ctrl Pts',(0.459643519947996,3.90777636067643,7.5099995648095));
#24057=CARTESIAN_POINT('Ctrl Pts',(0.343962774535669,3.91965110209251,7.51585890019647));
#24058=CARTESIAN_POINT('Ctrl Pts',(0.228028227937334,3.92638410337855,7.52171823558344));
#24059=CARTESIAN_POINT('Ctrl Pts',(0.11205648961027,3.93311926460711,7.52757945064146));
#24060=CARTESIAN_POINT('Ctrl Pts',(-0.00416880063361079,3.93470938181026,
7.53344066569948));
#24061=CARTESIAN_POINT('Ctrl Pts',(-0.120159010774501,3.93116405306745,
7.53930188075751));
#24062=CARTESIAN_POINT('Ctrl Pts',(-0.236278348012045,3.92761477745699,
7.54516962086349));
#24063=CARTESIAN_POINT('Ctrl Pts',(-0.352161670640159,3.91891865709447,
7.55103736096948));
#24064=CARTESIAN_POINT('Ctrl Pts',(-0.467323979016736,3.90513729574723,
7.55690510107546));
#24065=CARTESIAN_POINT('Ctrl Pts',(-0.582562376489921,3.89134682889185,
7.56277671806659));
#24066=CARTESIAN_POINT('Ctrl Pts',(-0.697078405367553,3.87246449701755,
7.56864833505772));
#24067=CARTESIAN_POINT('Ctrl Pts',(-0.810397477410202,3.84860298401994,
7.57451995204886));
#24068=CARTESIAN_POINT('Ctrl Pts',(-0.923880375902674,3.82470697420823,
7.58040005769199));
#24069=CARTESIAN_POINT('Ctrl Pts',(-1.03616246611069,3.79581751833037,7.58628016333511));
#24070=CARTESIAN_POINT('Ctrl Pts',(-1.14678443855703,3.76209708161332,7.59216026897824));
#24071=CARTESIAN_POINT('Ctrl Pts',(-1.17587264157831,3.75323024541884,7.5937064510156));
#24072=CARTESIAN_POINT('Ctrl Pts',(-1.20484616862641,3.74402963576712,7.59525263305295));
#24073=CARTESIAN_POINT('Ctrl Pts',(-1.23369691855059,3.73449874992063,7.59679881509031));
#24074=CARTESIAN_POINT('Ctrl Pts',(-1.34345847125961,3.69823886648773,7.60268120433972));
#24075=CARTESIAN_POINT('Ctrl Pts',(-1.45179681044438,3.65707747085414,7.60856359358913));
#24076=CARTESIAN_POINT('Ctrl Pts',(-1.55824306996784,3.61114490638318,7.61444598283854));
#24077=CARTESIAN_POINT('Ctrl Pts',(-1.66455493795266,3.56527033312808,7.62032094539823));
#24078=CARTESIAN_POINT('Ctrl Pts',(-1.76897910248425,3.51463673299237,7.62619590795792));
#24079=CARTESIAN_POINT('Ctrl Pts',(-1.87106234597096,3.45942404129497,7.6320708705176));
#24080=CARTESIAN_POINT('Ctrl Pts',(-1.97304373632805,3.40426643783001,7.63793997135793));
#24081=CARTESIAN_POINT('Ctrl Pts',(-2.07268849171423,3.34453902597639,7.64380907219826));
#24082=CARTESIAN_POINT('Ctrl Pts',(-2.16956446485834,3.28046933118173,7.64967817303859));
#24083=CARTESIAN_POINT('Ctrl Pts',(-2.2700134313952,3.21403660880917,7.65576373888923));
#24084=CARTESIAN_POINT('Ctrl Pts',(-2.36748502619612,3.14293530214689,7.66184930473986));
#24085=CARTESIAN_POINT('Ctrl Pts',(-2.46152634707033,3.06747078921358,7.66793487059049));
#24086=CARTESIAN_POINT('Ctrl Pts',(-2.55212327068198,2.99477027150441,7.67379754392789));
#24087=CARTESIAN_POINT('Ctrl Pts',(-2.63953643783171,2.91802083391656,7.67966021726529));
#24088=CARTESIAN_POINT('Ctrl Pts',(-2.72339212490094,2.83753842864331,7.68552289060269));
#24089=CARTESIAN_POINT('Ctrl Pts',(-2.80723670136208,2.75706668702919,7.69138478715479));
#24090=CARTESIAN_POINT('Ctrl Pts',(-2.88752443803497,2.67286324626018,7.69724668370688));
#24091=CARTESIAN_POINT('Ctrl Pts',(-2.9639172344716,2.58528211752648,7.70310858025897));
#24092=CARTESIAN_POINT('Ctrl Pts',(-3.04031822508946,2.49769159450858,7.70897110558033));
#24093=CARTESIAN_POINT('Ctrl Pts',(-3.11282317413419,2.40672297343814,7.7148336309017));
#24094=CARTESIAN_POINT('Ctrl Pts',(-3.18113362464812,2.31276411727031,7.72069615622306));
#24095=CARTESIAN_POINT('Ctrl Pts',(-3.24946778044208,2.21877265524232,7.72656071597405));
#24096=CARTESIAN_POINT('Ctrl Pts',(-3.3136043010335,2.12178922731686,7.73242527572503));
#24097=CARTESIAN_POINT('Ctrl Pts',(-3.3732878846183,2.02223090854813,7.73828983547602));
#24098=CARTESIAN_POINT('Ctrl Pts',(-3.43304005453589,1.92255818076484,7.74416113457848));
#24099=CARTESIAN_POINT('Ctrl Pts',(-3.48832886172091,1.8203050093091,7.75003243368094));
#24100=CARTESIAN_POINT('Ctrl Pts',(-3.53894477635643,1.71591342144629,7.7559037327834));
#24101=CARTESIAN_POINT('Ctrl Pts',(-3.58959522811968,1.6114506033068,7.76177903809237));
#24102=CARTESIAN_POINT('Ctrl Pts',(-3.63556627523173,1.50484684023992,7.76765434340135));
#24103=CARTESIAN_POINT('Ctrl Pts',(-3.67669703722869,1.39656288667349,7.77352964871032));
#24104=CARTESIAN_POINT('Ctrl Pts',(-3.71788836184128,1.28811949138651,7.77941360505905));
#24105=CARTESIAN_POINT('Ctrl Pts',(-3.75422504826353,1.17799135740374,7.78529756140779));
#24106=CARTESIAN_POINT('Ctrl Pts',(-3.78559638614092,1.06665317757781,7.79118151775652));
#24107=CARTESIAN_POINT('Ctrl Pts',(-3.7936831774663,1.0379528196167,7.79269826298893));
#24108=CARTESIAN_POINT('Ctrl Pts',(-3.80144029403778,1.00917209940504,7.79421500822134));
#24109=CARTESIAN_POINT('Ctrl Pts',(-3.80886639532414,0.98031922482961,7.79573175345375));
#24110=CARTESIAN_POINT('Ctrl Pts',(-3.83757891436247,0.868761534109808,
7.80159614644847));
#24111=CARTESIAN_POINT('Ctrl Pts',(-3.86143551269301,0.755749566578593,
7.80746053944319));
#24112=CARTESIAN_POINT('Ctrl Pts',(-3.8802903004427,0.641744641029695,7.81332493243792));
#24113=CARTESIAN_POINT('Ctrl Pts',(-3.89912030216079,0.527889583499651,
7.81918161624854));
#24114=CARTESIAN_POINT('Ctrl Pts',(-3.91296150113471,0.413044568746285,
7.82503830005917));
#24115=CARTESIAN_POINT('Ctrl Pts',(-3.92171807829749,0.297684924634476,
7.83089498386979));
#24116=CARTESIAN_POINT('Ctrl Pts',(-3.93046550417522,0.182445840070855,
7.83674554700312));
#24117=CARTESIAN_POINT('Ctrl Pts',(-3.93413884572687,0.0666936067228916,
7.84259611013644));
#24118=CARTESIAN_POINT('Ctrl Pts',(-3.93269365160892,-0.0490881105248623,
7.84844667326977));
#24119=CARTESIAN_POINT('Ctrl Pts',(-3.9311887151358,-0.169656086163691,
7.85453909070925));
#24120=CARTESIAN_POINT('Ctrl Pts',(-3.92413286646031,-0.290255584384087,
7.86063150814872));
#24121=CARTESIAN_POINT('Ctrl Pts',(-3.91153590472006,-0.410336284144846,
7.8667239255882));
#24122=CARTESIAN_POINT('Ctrl Pts',(-3.89945339953288,-0.5255129201987,7.87256753032662));
#24123=CARTESIAN_POINT('Ctrl Pts',(-3.88227352681979,-0.640211846360301,
7.87841113506504));
#24124=CARTESIAN_POINT('Ctrl Pts',(-3.86005803938839,-0.753950218882538,
7.88425473980346));
#24125=CARTESIAN_POINT('Ctrl Pts',(-3.83784612814636,-0.867670282107759,
7.89009740385412));
#24126=CARTESIAN_POINT('Ctrl Pts',(-3.8106002933054,-0.980429692266308,
7.89594006790478));
#24127=CARTESIAN_POINT('Ctrl Pts',(-3.77843359716715,-1.09175480388157,
7.90178273195544));
#24128=CARTESIAN_POINT('Ctrl Pts',(-3.74626423163027,-1.20308915396821,
7.90762588086781));
#24129=CARTESIAN_POINT('Ctrl Pts',(-3.70917330821319,-1.31298857052792,
7.91346902978019));
#24130=CARTESIAN_POINT('Ctrl Pts',(-3.66732384442588,-1.42099430685187,
7.91931217869256));
#24131=CARTESIAN_POINT('Ctrl Pts',(-3.62546069787914,-1.52903535585063,
7.92515723803326));
#24132=CARTESIAN_POINT('Ctrl Pts',(-3.57883606732273,-1.6351811071349,7.93100229737395));
#24133=CARTESIAN_POINT('Ctrl Pts',(-3.52766092273846,-1.73899321855609,
7.93684735671465));
#24134=CARTESIAN_POINT('Ctrl Pts',(-3.4764275273619,-1.84292349550056,7.94269906927226));
#24135=CARTESIAN_POINT('Ctrl Pts',(-3.42063346306906,-1.94451445861301,
7.94855078182987));
#24136=CARTESIAN_POINT('Ctrl Pts',(-3.36053547687665,-2.04335271273793,
7.95440249438748));
#24137=CARTESIAN_POINT('Ctrl Pts',(-3.30039711067037,-2.14225737657679,
7.96025813872799));
#24138=CARTESIAN_POINT('Ctrl Pts',(-3.23594929514515,-2.23840530530489,
7.96611378306849));
#24139=CARTESIAN_POINT('Ctrl Pts',(-3.16749085903314,-2.33141387530002,
7.97196942740899));
#24140=CARTESIAN_POINT('Ctrl Pts',(-3.09893078147948,-2.4245605367515,7.97783376572743));
#24141=CARTESIAN_POINT('Ctrl Pts',(-3.02634845855472,-2.51455821550396,
7.98369810404587));
#24142=CARTESIAN_POINT('Ctrl Pts',(-2.95008158690857,-2.60105894408086,
7.98956244236431));
#24143=CARTESIAN_POINT('Ctrl Pts',(-2.92796300148598,-2.62614550804825,
7.99126319218193));
#24144=CARTESIAN_POINT('Ctrl Pts',(-2.90553473678805,-2.65093819525922,
7.99296394199956));
#24145=CARTESIAN_POINT('Ctrl Pts',(-2.88280556274161,-2.67542914079705,
7.99466469181719));
#24146=CARTESIAN_POINT('Ctrl Pts',(-2.8043081914697,-2.76001095801379,8.00053839358929));
#24147=CARTESIAN_POINT('Ctrl Pts',(-2.72195407090228,-2.84127646596739,
8.00641209536139));
#24148=CARTESIAN_POINT('Ctrl Pts',(-2.63605453258703,-2.91885345662083,
8.0122857971335));
#24149=CARTESIAN_POINT('Ctrl Pts',(-2.55026625588345,-2.9963299654652,8.01815189097733));
#24150=CARTESIAN_POINT('Ctrl Pts',(-2.46094199760085,-3.07012718360594,
8.02401798482117));
#24151=CARTESIAN_POINT('Ctrl Pts',(-2.36843181965343,-3.13990759667433,
8.02988407866501));
#24152=CARTESIAN_POINT('Ctrl Pts',(-2.27601675373697,-3.2096162667523,8.03574414143084));
#24153=CARTESIAN_POINT('Ctrl Pts',(-2.18042261128095,-3.27531609887929,
8.04160420419668));
#24154=CARTESIAN_POINT('Ctrl Pts',(-2.0820341128983,-3.33670840091366,8.04746426696251));
#24155=CARTESIAN_POINT('Ctrl Pts',(-1.97980367936051,-3.40049798766442,
8.0535531570966));
#24156=CARTESIAN_POINT('Ctrl Pts',(-1.87455654824124,-3.45963647775856,
8.05964204723068));
#24157=CARTESIAN_POINT('Ctrl Pts',(-1.76675979720991,-3.51383676612372,
8.06573093736477));
#24158=CARTESIAN_POINT('Ctrl Pts',(-1.66313443646764,-3.56593967628047,
8.07158420688011));
#24159=CARTESIAN_POINT('Ctrl Pts',(-1.55715351553769,-3.61347926252958,
8.07743747639547));
#24160=CARTESIAN_POINT('Ctrl Pts',(-1.44925819231429,-3.65624666728189,
8.08329074591081));
#24161=CARTESIAN_POINT('Ctrl Pts',(-1.34137938292998,-3.69900752630061,
8.0891431195583));
#24162=CARTESIAN_POINT('Ctrl Pts',(-1.23158713783247,-3.7369975039187,8.0949954932058));
#24163=CARTESIAN_POINT('Ctrl Pts',(-1.12034252612701,-3.77005591790776,
8.1008478668533));
#24164=CARTESIAN_POINT('Ctrl Pts',(-1.00908803632947,-3.80311726735637,
8.10670076016899));
#24165=CARTESIAN_POINT('Ctrl Pts',(-0.896381319617469,-3.83124606496304,
8.11255365348467));
#24166=CARTESIAN_POINT('Ctrl Pts',(-0.78269784444515,-3.85433172992426,
8.11840654680035));
#24167=CARTESIAN_POINT('Ctrl Pts',(-0.668976780273355,-3.87742502807092,
8.12426137535248));
#24168=CARTESIAN_POINT('Ctrl Pts',(-0.554278720128107,-3.8954717956566,
8.1301162039046));
#24169=CARTESIAN_POINT('Ctrl Pts',(-0.439087835519406,-3.90841283294113,
8.13597103245673));
#24170=CARTESIAN_POINT('Ctrl Pts',(-0.323766291036385,-3.92136854911548,
8.14183250208263));
#24171=CARTESIAN_POINT('Ctrl Pts',(-0.207951217146528,-3.92920692934892,
8.14769397170852));
#24172=CARTESIAN_POINT('Ctrl Pts',(-0.0921305048125156,-3.93192077362744,
8.15355544133442));
#24173=CARTESIAN_POINT('Ctrl Pts',(0.0237680012788959,-3.93463644072451,
8.15942084795688));
#24174=CARTESIAN_POINT('Ctrl Pts',(0.139671741283028,-3.93222072659018,
8.16528625457934));
#24175=CARTESIAN_POINT('Ctrl Pts',(0.255095976324763,-3.92471846670088,
8.1711516612018));
#24176=CARTESIAN_POINT('Ctrl Pts',(0.370689957236543,-3.91720517379385,
8.17702569364318));
#24177=CARTESIAN_POINT('Ctrl Pts',(0.485802616608141,-3.9045904503839,8.18289972608456));
#24178=CARTESIAN_POINT('Ctrl Pts',(0.59995736727677,-3.88697056297708,8.18877375852594));
#24179=CARTESIAN_POINT('Ctrl Pts',(0.631206080518413,-3.882147296265,8.19038171574416));
#24180=CARTESIAN_POINT('Ctrl Pts',(0.662383093154374,-3.87694926574991,
8.19198967296239));
#24181=CARTESIAN_POINT('Ctrl Pts',(0.693478824783114,-3.87137909788972,
8.19359763018062));
#24182=CARTESIAN_POINT('Ctrl Pts',(0.807061363038884,-3.85103309633476,
8.19947097204096));
#24183=CARTESIAN_POINT('Ctrl Pts',(0.919937230665374,-3.82565031194341,
8.2053443139013));
#24184=CARTESIAN_POINT('Ctrl Pts',(1.03162505281565,-3.79529165551254,8.21121765576164));
#24185=CARTESIAN_POINT('Ctrl Pts',(1.14316854615067,-3.76497223011717,8.21708340778403));
#24186=CARTESIAN_POINT('Ctrl Pts',(1.25352665202299,-3.72968982732742,8.22294915980642));
#24187=CARTESIAN_POINT('Ctrl Pts',(1.36222626986069,-3.68955669284285,8.22881491182881));
#24188=CARTESIAN_POINT('Ctrl Pts',(1.47081446598169,-3.6494646965226,8.23467465120668));
#24189=CARTESIAN_POINT('Ctrl Pts',(1.57774717021002,-3.60453200084474,8.24053439058456));
#24190=CARTESIAN_POINT('Ctrl Pts',(1.68256523073041,-3.55492098988671,8.24639412996243));
#24191=CARTESIAN_POINT('Ctrl Pts',(1.79148459468508,-3.50336880763997,8.25248314823667));
#24192=CARTESIAN_POINT('Ctrl Pts',(1.89812001434187,-3.446764849266,8.2585721665109));
#24193=CARTESIAN_POINT('Ctrl Pts',(2.00197749850025,-3.38534711595409,8.26466118478513));
#24194=CARTESIAN_POINT('Ctrl Pts',(2.10180924051122,-3.32631006767028,8.2705141794574));
#24195=CARTESIAN_POINT('Ctrl Pts',(2.19907400558695,-3.26282570995485,8.27636717412966));
#24196=CARTESIAN_POINT('Ctrl Pts',(2.29335775739799,-3.19515245279196,8.28222016880192));
#24197=CARTESIAN_POINT('Ctrl Pts',(2.38762737583228,-3.12748934002427,8.28807228609524));
#24198=CARTESIAN_POINT('Ctrl Pts',(2.47891653390792,-3.05563881721695,8.29392440338855));
#24199=CARTESIAN_POINT('Ctrl Pts',(2.56684098390339,-2.97990207277922,8.29977652068187));
#24200=CARTESIAN_POINT('Ctrl Pts',(2.65477352494775,-2.90415835883867,8.30562917650306));
#24201=CARTESIAN_POINT('Ctrl Pts',(2.73934042928356,-2.82452798202587,8.31148183232425));
#24202=CARTESIAN_POINT('Ctrl Pts',(2.82019183635457,-2.74135131024082,8.31733448814544));
#24203=CARTESIAN_POINT('Ctrl Pts',(2.9010702435716,-2.6581468617928,8.32318909844791));
#24204=CARTESIAN_POINT('Ctrl Pts',(2.97823039841043,-2.57139405961669,8.32904370875039));
#24205=CARTESIAN_POINT('Ctrl Pts',(3.05136098149761,-2.48146834769133,8.33489831905286));
#24206=CARTESIAN_POINT('Ctrl Pts',(3.12457489228793,-2.3914401710691,8.34075960031581));
#24207=CARTESIAN_POINT('Ctrl Pts',(3.19374980604273,-2.29823218935168,8.34662088157875));
#24208=CARTESIAN_POINT('Ctrl Pts',(3.25861615586611,-2.2022510639635,8.3524821628417));
#24209=CARTESIAN_POINT('Ctrl Pts',(3.32352626626546,-2.10620518713886,8.35834739828188));
#24210=CARTESIAN_POINT('Ctrl Pts',(3.38412180944998,-2.00738279280494,8.36421263372207));
#24211=CARTESIAN_POINT('Ctrl Pts',(3.44017871465808,-1.90621599280183,8.37007786916226));
#24212=CARTESIAN_POINT('Ctrl Pts',(3.49631831661629,-1.8048999486414,8.37595175716554));
#24213=CARTESIAN_POINT('Ctrl Pts',(3.54790573413224,-1.70123296475599,8.38182564516883));
#24214=CARTESIAN_POINT('Ctrl Pts',(3.59476458326332,-1.59566807040679,8.38769953317212));
#24215=CARTESIAN_POINT('Ctrl Pts',(3.60761108615397,-1.56672711804547,8.3893098782961));
#24216=CARTESIAN_POINT('Ctrl Pts',(3.62010247822007,-1.53764360972564,8.39092022342007));
#24217=CARTESIAN_POINT('Ctrl Pts',(3.63223578236975,-1.5084270685959,8.39253056854406));
#24218=CARTESIAN_POINT('Ctrl Pts',(3.68161746855028,-1.38951782116001,8.39908455883176));
#24219=CARTESIAN_POINT('Ctrl Pts',(3.72520412016676,-1.26806629056107,8.40563854911947));
#24220=CARTESIAN_POINT('Ctrl Pts',(3.76275585153874,-1.14462107341731,8.41219253940718));
#24221=CARTESIAN_POINT('Ctrl Pts',(3.80019800167,-1.02153608680251,8.4187274042282));
#24222=CARTESIAN_POINT('Ctrl Pts',(3.83164026942457,-0.896469241021658,
8.42526226904922));
#24223=CARTESIAN_POINT('Ctrl Pts',(3.85689102631617,-0.769987409716397,
8.43179713387024));
#24224=CARTESIAN_POINT('Ctrl Pts',(3.88203237318332,-0.644053616646821,
8.43830368351153));
#24225=CARTESIAN_POINT('Ctrl Pts',(3.90103563430197,-0.516717295157309,
8.4448102331528));
#24226=CARTESIAN_POINT('Ctrl Pts',(3.91375931073664,-0.388557663188167,
8.45131678279408));
#24227=CARTESIAN_POINT('Ctrl Pts',(3.92648298717131,-0.260398031219027,
8.45782333243537));
#24228=CARTESIAN_POINT('Ctrl Pts',(3.93292693640676,-0.131415309978197,
8.46432988207665));
#24229=CARTESIAN_POINT('Ctrl Pts',(3.93299938180971,-0.00220514953339285,
8.47083643171793));
#24230=CARTESIAN_POINT('',(3.93299870264977,0.00319451955702668,9.72083652192225));
#24231=CARTESIAN_POINT('Ctrl Pts',(3.92766918394753,-0.00220124385136065,
8.47083647796505));
#24232=CARTESIAN_POINT('Ctrl Pts',(3.92369425708854,0.795208744126929,8.51104548761253));
#24233=CARTESIAN_POINT('Ctrl Pts',(3.29976413746548,2.91342972784538,8.61756547671448));
#24234=CARTESIAN_POINT('Ctrl Pts',(-0.165076056764658,4.64938694469499,
8.79039644527095));
#24235=CARTESIAN_POINT('Ctrl Pts',(-4.00140116403964,2.37342693484846,8.98932938363437));
#24236=CARTESIAN_POINT('Ctrl Pts',(-4.15924136175396,-2.08449287814342,
9.18826232199783));
#24237=CARTESIAN_POINT('Ctrl Pts',(-0.493461012700928,-4.62609887161364,
9.38719526036124));
#24238=CARTESIAN_POINT('Ctrl Pts',(3.18264251973689,-3.09907510464914,9.56471997901699));
#24239=CARTESIAN_POINT('Ctrl Pts',(3.92290577835605,-0.886171555639169,
9.67593371821826));
#24240=CARTESIAN_POINT('Ctrl Pts',(3.92964724161972,0.00319092675375862,
9.72083647796504));
#24241=CARTESIAN_POINT('',(3.93299988442888,0.000953458131951196,10.9708364779374));
#24242=CARTESIAN_POINT('Ctrl Pts',(3.93299870264977,0.00319451955702668,
9.72083652192224));
#24243=CARTESIAN_POINT('Ctrl Pts',(3.93288780561851,0.139727689034319,9.72772407767723));
#24244=CARTESIAN_POINT('Ctrl Pts',(3.92566347168156,0.275958603419552,9.73461163343222));
#24245=CARTESIAN_POINT('Ctrl Pts',(3.91144310631301,0.411219924221101,9.7414991891872));
#24246=CARTESIAN_POINT('Ctrl Pts',(3.89645310508584,0.553801870061144,9.74875951383735));
#24247=CARTESIAN_POINT('Ctrl Pts',(3.87368900560028,0.695306167485196,9.75601983848751));
#24248=CARTESIAN_POINT('Ctrl Pts',(3.84334558860368,0.834975261047055,9.76328016313766));
#24249=CARTESIAN_POINT('Ctrl Pts',(3.81300217160709,0.974644354608916,9.77054048778781));
#24250=CARTESIAN_POINT('Ctrl Pts',(3.77507959544271,1.11247819590628,9.77780081243797));
#24251=CARTESIAN_POINT('Ctrl Pts',(3.72982868428875,1.24774475989957,9.78506113708812));
#24252=CARTESIAN_POINT('Ctrl Pts',(3.69322985994942,1.35714802026115,9.79093326959863));
#24253=CARTESIAN_POINT('Ctrl Pts',(3.65175207701635,1.4651230498948,9.79680540210914));
#24254=CARTESIAN_POINT('Ctrl Pts',(3.60552515296765,1.57120252396614,9.80267753461965));
#24255=CARTESIAN_POINT('Ctrl Pts',(3.55935816232143,1.67714446555086,9.80854205388554));
#24256=CARTESIAN_POINT('Ctrl Pts',(3.5084544387876,1.78119536335366,9.81440657315142));
#24257=CARTESIAN_POINT('Ctrl Pts',(3.45299339963115,1.88290349782024,9.82027109241731));
#24258=CARTESIAN_POINT('Ctrl Pts',(3.39758942858733,1.98450697699438,9.82612957722998));
#24259=CARTESIAN_POINT('Ctrl Pts',(3.33763766603066,2.08377212695668,9.83198806204266));
#24260=CARTESIAN_POINT('Ctrl Pts',(3.27336512418679,2.18026827793224,9.83784654685533));
#24261=CARTESIAN_POINT('Ctrl Pts',(3.20655836550377,2.28056919784488,9.8439360272135));
#24262=CARTESIAN_POINT('Ctrl Pts',(3.13508326984826,2.37787785054927,9.85002550757168));
#24263=CARTESIAN_POINT('Ctrl Pts',(3.05924697979565,2.47173965388979,9.85611498792985));
#24264=CARTESIAN_POINT('Ctrl Pts',(2.98637200739073,2.56193626455693,9.86196668126499));
#24265=CARTESIAN_POINT('Ctrl Pts',(2.90947033265802,2.64894981354038,9.86781837460013));
#24266=CARTESIAN_POINT('Ctrl Pts',(2.82885746948552,2.73240817180303,9.87367006793527));
#24267=CARTESIAN_POINT('Ctrl Pts',(2.74825690110632,2.81585380128738,9.87952086879051));
#24268=CARTESIAN_POINT('Ctrl Pts',(2.66394655684131,2.8957450208958,9.88537166964574));
#24269=CARTESIAN_POINT('Ctrl Pts',(2.5762799669011,2.97174536798563,9.89122247050098));
#24270=CARTESIAN_POINT('Ctrl Pts',(2.4886055139896,3.04775253168082,9.89707379612488));
#24271=CARTESIAN_POINT('Ctrl Pts',(2.39757452937672,3.11986785830091,9.90292512174879));
#24272=CARTESIAN_POINT('Ctrl Pts',(2.30357433103063,3.18779458268828,9.90877644737269));
#24273=CARTESIAN_POINT('Ctrl Pts',(2.20954293401993,3.2557438519546,9.91462971505149));
#24274=CARTESIAN_POINT('Ctrl Pts',(2.11254069861223,3.31950151266318,9.92048298273028));
#24275=CARTESIAN_POINT('Ctrl Pts',(2.01298406674388,3.3788140148631,9.92633625040908));
#24276=CARTESIAN_POINT('Ctrl Pts',(1.91331417045744,3.43819399620449,9.9321961772822));
#24277=CARTESIAN_POINT('Ctrl Pts',(1.81108443256838,3.49311851327191,9.93805610415533));
#24278=CARTESIAN_POINT('Ctrl Pts',(1.70673613336183,3.54337985136749,9.94391603102845));
#24279=CARTESIAN_POINT('Ctrl Pts',(1.60231757367317,3.59367503175733,9.94977990354601));
#24280=CARTESIAN_POINT('Ctrl Pts',(1.49577799136053,3.63930061878401,9.95564377606358));
#24281=CARTESIAN_POINT('Ctrl Pts',(1.38757725451918,3.68009760233897,9.96150764858114));
#24282=CARTESIAN_POINT('Ctrl Pts',(1.27921689725041,3.72095477062226,9.9673801716298));
#24283=CARTESIAN_POINT('Ctrl Pts',(1.1691908859848,3.75696899057257,9.97325269467845));
#24284=CARTESIAN_POINT('Ctrl Pts',(1.05797287258894,3.78803146777662,9.9791252177271));
#24285=CARTESIAN_POINT('Ctrl Pts',(1.02723624376487,3.79661601090075,9.98074817030192));
#24286=CARTESIAN_POINT('Ctrl Pts',(0.996408622409986,3.80482265792298,9.98237112287675));
#24287=CARTESIAN_POINT('Ctrl Pts',(0.965500099630154,3.81264980789138,9.98399407545157));
#24288=CARTESIAN_POINT('Ctrl Pts',(0.853667681362951,3.84096979960826,9.98986620051131));
#24289=CARTESIAN_POINT('Ctrl Pts',(0.740400701749089,3.86441270438932,9.99573832557106));
#24290=CARTESIAN_POINT('Ctrl Pts',(0.626162532712097,3.88283523763597,10.0016104506308));
#24291=CARTESIAN_POINT('Ctrl Pts',(0.512072474938538,3.90123388583003,10.0074749624045));
#24292=CARTESIAN_POINT('Ctrl Pts',(0.39701413612062,3.91462504127279,10.0133394741781));
#24293=CARTESIAN_POINT('Ctrl Pts',(0.281464558483938,3.92291558694773,10.0192039859518));
#24294=CARTESIAN_POINT('Ctrl Pts',(0.166033879447143,3.9311976017886,10.0250624632401));
#24295=CARTESIAN_POINT('Ctrl Pts',(0.0501133768782267,3.93438941685644,
10.0309209405284));
#24296=CARTESIAN_POINT('Ctrl Pts',(-0.0658119012407749,3.93244933770991,
10.0367794178166));
#24297=CARTESIAN_POINT('Ctrl Pts',(-0.1863082341534,3.93043275921632,10.0428689009832));
#24298=CARTESIAN_POINT('Ctrl Pts',(-0.306809277726285,3.92287117608799,
10.0489583841498));
#24299=CARTESIAN_POINT('Ctrl Pts',(-0.426766562019581,3.90977739795273,
10.0550478673164));
#24300=CARTESIAN_POINT('Ctrl Pts',(-0.542039453875697,3.89719493845586,
10.0608995530949));
#24301=CARTESIAN_POINT('Ctrl Pts',(-0.656809807979611,3.87950429505613,
10.0667512388734));
#24302=CARTESIAN_POINT('Ctrl Pts',(-0.770594013171069,3.85676987476112,
10.0726029246518));
#24303=CARTESIAN_POINT('Ctrl Pts',(-0.884360864389838,3.83403892184111,
10.0784537179515));
#24304=CARTESIAN_POINT('Ctrl Pts',(-0.997141460458635,3.80626580253215,
10.0843045112511));
#24305=CARTESIAN_POINT('Ctrl Pts',(-1.10846165934521,3.77356618462717,10.0901553045507));
#24306=CARTESIAN_POINT('Ctrl Pts',(-1.21979184292451,3.74086363378064,10.0960066226282));
#24307=CARTESIAN_POINT('Ctrl Pts',(-1.32966097225197,3.7032338224534,10.1018579407057));
#24308=CARTESIAN_POINT('Ctrl Pts',(-1.43761005126368,3.66084229932206,10.1077092587831));
#24309=CARTESIAN_POINT('Ctrl Pts',(-1.54559495893886,3.6184367063012,10.1135625189328));
#24310=CARTESIAN_POINT('Ctrl Pts',(-1.65165816452456,3.5712664099305,10.1194157790825));
#24311=CARTESIAN_POINT('Ctrl Pts',(-1.75536129796696,3.51954481625107,10.1252690392322));
#24312=CARTESIAN_POINT('Ctrl Pts',(-1.85918241454032,3.46776437887658,10.1311289586402));
#24313=CARTESIAN_POINT('Ctrl Pts',(-1.96063772949673,3.41142249363674,10.1369888780483));
#24314=CARTESIAN_POINT('Ctrl Pts',(-2.05931401914049,3.35077823357074,10.1428487974563));
#24315=CARTESIAN_POINT('Ctrl Pts',(-2.15805675070839,3.29009313977111,10.1487126625368));
#24316=CARTESIAN_POINT('Ctrl Pts',(-2.25401638956751,3.22510013406245,10.1545765276174));
#24317=CARTESIAN_POINT('Ctrl Pts',(-2.34681065024533,3.15610024744068,10.1604403926979));
#24318=CARTESIAN_POINT('Ctrl Pts',(-2.43974180507728,3.08699856916665,10.1663129084088));
#24319=CARTESIAN_POINT('Ctrl Pts',(-2.5294979425478,3.01387847260215,10.1721854241197));
#24320=CARTESIAN_POINT('Ctrl Pts',(-2.6157315827658,2.93707972089991,10.1780579398306));
#24321=CARTESIAN_POINT('Ctrl Pts',(-2.63956452449162,2.91585435955244,10.1796809644921));
#24322=CARTESIAN_POINT('Ctrl Pts',(-2.66312863249218,2.89434821296909,10.1813039891535));
#24323=CARTESIAN_POINT('Ctrl Pts',(-2.6864171060488,2.87256890819496,10.182927013815));
#24324=CARTESIAN_POINT('Ctrl Pts',(-2.77067505880192,2.79377114464928,10.1887991348413));
#24325=CARTESIAN_POINT('Ctrl Pts',(-2.85160439663599,2.71113096212789,10.1946712558677));
#24326=CARTESIAN_POINT('Ctrl Pts',(-2.92883417188751,2.624960836581,10.200543376894));
#24327=CARTESIAN_POINT('Ctrl Pts',(-3.00596381657239,2.5389024330153,10.206407884551));
#24328=CARTESIAN_POINT('Ctrl Pts',(-3.07940316397512,2.44932349277566,10.2122723922079));
#24329=CARTESIAN_POINT('Ctrl Pts',(-3.14881609273798,2.35657510258306,10.2181368998649));
#24330=CARTESIAN_POINT('Ctrl Pts',(-3.21815759577494,2.26392215024638,10.2239953729585));
#24331=CARTESIAN_POINT('Ctrl Pts',(-3.2834806749253,2.16810656393992,10.2298538460521));
#24332=CARTESIAN_POINT('Ctrl Pts',(-3.34448815197973,2.06951395290469,10.2357123191457));
#24333=CARTESIAN_POINT('Ctrl Pts',(-3.40790127904621,1.96703363289711,10.2418018038554));
#24334=CARTESIAN_POINT('Ctrl Pts',(-3.46665115215085,1.86155311374219,10.2478912885651));
#24335=CARTESIAN_POINT('Ctrl Pts',(-3.52045218427856,1.75354082308008,10.2539807732748));
#24336=CARTESIAN_POINT('Ctrl Pts',(-3.57215220731775,1.64974657053688,10.2598324546894));
#24337=CARTESIAN_POINT('Ctrl Pts',(-3.61928245327851,1.54361497941328,10.265684136104));
#24338=CARTESIAN_POINT('Ctrl Pts',(-3.66163579849187,1.43558778178236,10.2715358175186));
#24339=CARTESIAN_POINT('Ctrl Pts',(-3.70398268371517,1.3275770611173,10.2773866063991));
#24340=CARTESIAN_POINT('Ctrl Pts',(-3.74155396602138,1.21767169360762,10.2832373952797));
#24341=CARTESIAN_POINT('Ctrl Pts',(-3.774190771307,1.10633314231341,10.2890881841602));
#24342=CARTESIAN_POINT('Ctrl Pts',(-3.8068305036193,0.994984605638975,10.2949394977678));
#24343=CARTESIAN_POINT('Ctrl Pts',(-3.83453476286883,0.882203026408219,
10.3007908113754));
#24344=CARTESIAN_POINT('Ctrl Pts',(-3.85719483088805,0.768464076304509,
10.306642124983));
#24345=CARTESIAN_POINT('Ctrl Pts',(-3.87986241968654,0.654687376731623,
10.3124953806165));
#24346=CARTESIAN_POINT('Ctrl Pts',(-3.8974824075923,0.539953079696709,10.3183486362499));
#24347=CARTESIAN_POINT('Ctrl Pts',(-3.90999749083604,0.424745360958616,
10.3242018918834));
#24348=CARTESIAN_POINT('Ctrl Pts',(-3.92252681241093,0.309406571126669,
10.3300618067288));
#24349=CARTESIAN_POINT('Ctrl Pts',(-3.92993959240011,0.193593695783005,
10.3359217215742));
#24350=CARTESIAN_POINT('Ctrl Pts',(-3.93223054093183,0.0777944275827514,
10.3417816364196));
#24351=CARTESIAN_POINT('Ctrl Pts',(-3.93452303202141,-0.0380828114091053,
10.3476454969048));
#24352=CARTESIAN_POINT('Ctrl Pts',(-3.9316868347727,-0.15394601273332,10.35350935739));
#24353=CARTESIAN_POINT('Ctrl Pts',(-3.92376868189452,-0.269310844534226,
10.3593732178752));
#24354=CARTESIAN_POINT('Ctrl Pts',(-3.91583884781867,-0.384845867467452,
10.3652457289781));
#24355=CARTESIAN_POINT('Ctrl Pts',(-3.9028121416016,-0.499880644273067,
10.371118240081));
#24356=CARTESIAN_POINT('Ctrl Pts',(-3.88478669393042,-0.613939201111262,
10.3769907511839));
#24357=CARTESIAN_POINT('Ctrl Pts',(-3.87980475200986,-0.645463139716109,
10.3786138181821));
#24358=CARTESIAN_POINT('Ctrl Pts',(-3.87444126192626,-0.676912588316585,
10.3802368851803));
#24359=CARTESIAN_POINT('Ctrl Pts',(-3.86869896686081,-0.708277702465682,
10.3818599521785));
#24360=CARTESIAN_POINT('Ctrl Pts',(-3.84792380704504,-0.821754152501958,
10.3877320775037));
#24361=CARTESIAN_POINT('Ctrl Pts',(-3.82211685801432,-0.93450600488425,
10.393604202829));
#24362=CARTESIAN_POINT('Ctrl Pts',(-3.79134061016334,-1.04605228250135,
10.3994763281542));
#24363=CARTESIAN_POINT('Ctrl Pts',(-3.76060426424535,-1.15745393845705,
10.4053408401683));
#24364=CARTESIAN_POINT('Ctrl Pts',(-3.72491154079952,-1.26765273314512,
10.4112053521824));
#24365=CARTESIAN_POINT('Ctrl Pts',(-3.68437623724042,-1.37617613060905,
10.4170698641965));
#24366=CARTESIAN_POINT('Ctrl Pts',(-3.64388264400972,-1.48458785883285,
10.4229283416999));
#24367=CARTESIAN_POINT('Ctrl Pts',(-3.59855652578488,-1.59132723393031,
10.4287868192034));
#24368=CARTESIAN_POINT('Ctrl Pts',(-3.54856177149421,-1.69593583424901,
10.4346452967068));
#24369=CARTESIAN_POINT('Ctrl Pts',(-3.49659567450274,-1.80466925533351,
10.4407347797832));
#24370=CARTESIAN_POINT('Ctrl Pts',(-3.43958531012525,-1.91109996885889,
10.4468242628597));
#24371=CARTESIAN_POINT('Ctrl Pts',(-3.37777051672664,-2.01473455728845,
10.4529137459362));
#24372=CARTESIAN_POINT('Ctrl Pts',(-3.31836961977622,-2.11432216681269,
10.4587654318647));
#24373=CARTESIAN_POINT('Ctrl Pts',(-3.25453271454795,-2.21132754472085,
10.4646171177932));
#24374=CARTESIAN_POINT('Ctrl Pts',(-3.18651957473406,-2.30533771925865,
10.4704688037218));
#24375=CARTESIAN_POINT('Ctrl Pts',(-3.1185168083319,-2.39933355529877,10.4763195971471));
#24376=CARTESIAN_POINT('Ctrl Pts',(-3.04633931608047,-2.49033476143605,
10.4821703905724));
#24377=CARTESIAN_POINT('Ctrl Pts',(-2.97028954566743,-2.57795830356094,
10.4880211839977));
#24378=CARTESIAN_POINT('Ctrl Pts',(-2.89423295440869,-2.66558970457424,
10.4938725021762));
#24379=CARTESIAN_POINT('Ctrl Pts',(-2.81430366557959,-2.7498425271212,10.4997238203546));
#24380=CARTESIAN_POINT('Ctrl Pts',(-2.7308431842205,-2.83036826282313,10.5055751385331));
#24381=CARTESIAN_POINT('Ctrl Pts',(-2.64735500240226,-2.91092072494476,
10.5114283987589));
#24382=CARTESIAN_POINT('Ctrl Pts',(-2.56033359496256,-2.98774335359664,
10.5172816589847));
#24383=CARTESIAN_POINT('Ctrl Pts',(-2.47015540426082,-3.0605263074839,10.5231349192104));
#24384=CARTESIAN_POINT('Ctrl Pts',(-2.37987461834705,-3.13339206612173,
10.5289948386569));
#24385=CARTESIAN_POINT('Ctrl Pts',(-2.28643020261903,-3.20220871686826,
10.5348547581033));
#24386=CARTESIAN_POINT('Ctrl Pts',(-2.19022966427678,-3.26670828476037,
10.5407146775498));
#24387=CARTESIAN_POINT('Ctrl Pts',(-2.09396435137341,-3.33125128204772,
10.5465785426468));
#24388=CARTESIAN_POINT('Ctrl Pts',(-1.99493957300605,-3.39147119416107,
10.5524424077439));
#24389=CARTESIAN_POINT('Ctrl Pts',(-1.89358811873438,-3.44714563611519,
10.5583062728409));
#24390=CARTESIAN_POINT('Ctrl Pts',(-1.79208714692477,-3.50290221113338,
10.5641787885358));
#24391=CARTESIAN_POINT('Ctrl Pts',(-1.6882530181765,-3.55409975061671,10.5700513042307));
#24392=CARTESIAN_POINT('Ctrl Pts',(-1.58253926204241,-3.60056363422371,
10.5759238199256));
#24393=CARTESIAN_POINT('Ctrl Pts',(-1.55332249643609,-3.61340514554777,
10.5775468434643));
#24394=CARTESIAN_POINT('Ctrl Pts',(-1.52396224897608,-3.62588537512602,
10.5791698670031));
#24395=CARTESIAN_POINT('Ctrl Pts',(-1.49446828466722,-3.63800131200139,
10.5807928905419));
#24396=CARTESIAN_POINT('Ctrl Pts',(-1.38775867046928,-3.68183695701938,
10.5866650145413));
#24397=CARTESIAN_POINT('Ctrl Pts',(-1.27893984741821,-3.7210471120347,10.5925371385407));
#24398=CARTESIAN_POINT('Ctrl Pts',(-1.16845029605637,-3.75542446411132,
10.5984092625401));
#24399=CARTESIAN_POINT('Ctrl Pts',(-1.05810399651562,-3.78975724529205,
10.6042737732182));
#24400=CARTESIAN_POINT('Ctrl Pts',(-0.946091667411633,-3.81926956229493,
10.6101382838963));
#24401=CARTESIAN_POINT('Ctrl Pts',(-0.832872410197733,-3.84380183520579,
10.6160027945744));
#24402=CARTESIAN_POINT('Ctrl Pts',(-0.719769654396316,-3.86830886466853,
10.6218612707333));
#24403=CARTESIAN_POINT('Ctrl Pts',(-0.605462842319242,-3.88784595571986,
10.6277197468922));
#24404=CARTESIAN_POINT('Ctrl Pts',(-0.490426265907847,-3.90230330416636,
10.6335782230512));
#24405=CARTESIAN_POINT('Ctrl Pts',(-0.370853646025683,-3.91733072487223,
10.6396677066284));
#24406=CARTESIAN_POINT('Ctrl Pts',(-0.25049296118244,-3.92686942434664,
10.6457571902057));
#24407=CARTESIAN_POINT('Ctrl Pts',(-0.129888989929251,-3.93085459541499,
10.6518466737829));
#24408=CARTESIAN_POINT('Ctrl Pts',(-0.0139946962873338,-3.93468414249548,
10.6576983583543));
#24409=CARTESIAN_POINT('Ctrl Pts',(0.102123787176804,-3.93338574595293,
10.6635500429257));
#24410=CARTESIAN_POINT('Ctrl Pts',(0.217978600822607,-3.92695484180598,
10.6694017274971));
#24411=CARTESIAN_POINT('Ctrl Pts',(0.33381574416035,-3.92052491850784,10.6752525195629));
#24412=CARTESIAN_POINT('Ctrl Pts',(0.44938888497686,-3.9089640669948,10.6811033116287));
#24413=CARTESIAN_POINT('Ctrl Pts',(0.564212295612798,-3.89231980770842,
10.6869541036945));
#24414=CARTESIAN_POINT('Ctrl Pts',(0.679046004657021,-3.87567405561342,
10.6928054205125));
#24415=CARTESIAN_POINT('Ctrl Pts',(0.793129440687579,-3.85394404871565,
10.6986567373306));
#24416=CARTESIAN_POINT('Ctrl Pts',(0.905984822881521,-3.82722882784768,
10.7045080541487));
#24417=CARTESIAN_POINT('Ctrl Pts',(1.01887766169491,-3.8005047402173,10.7103613130145));
#24418=CARTESIAN_POINT('Ctrl Pts',(1.13054123412321,-3.7687922437558,10.7162145718804));
#24419=CARTESIAN_POINT('Ctrl Pts',(1.24051141714121,-3.73224067068863,10.7220678307463));
#24420=CARTESIAN_POINT('Ctrl Pts',(1.35060671278147,-3.695647513048,10.7279277488405));
#24421=CARTESIAN_POINT('Ctrl Pts',(1.45900438110027,-3.65420442064697,10.7337876669348));
#24422=CARTESIAN_POINT('Ctrl Pts',(1.56525874133763,-3.6081094873446,10.7396475850291));
#24423=CARTESIAN_POINT('Ctrl Pts',(1.67158464572791,-3.56198351698221,10.7455114487767));
#24424=CARTESIAN_POINT('Ctrl Pts',(1.77576399773429,-3.51119964956191,10.7513753125244));
#24425=CARTESIAN_POINT('Ctrl Pts',(1.87737581664801,-3.45600188701702,10.757239176272));
#24426=CARTESIAN_POINT('Ctrl Pts',(1.97913753748759,-3.40072269446727,10.7631116906321));
#24427=CARTESIAN_POINT('Ctrl Pts',(2.07832381276221,-3.34101682334,10.7689842049923));
#24428=CARTESIAN_POINT('Ctrl Pts',(2.17454264612672,-3.27717153658093,10.7748567193524));
#24429=CARTESIAN_POINT('Ctrl Pts',(2.20113545981049,-3.25952607408671,10.77647975587));
#24430=CARTESIAN_POINT('Ctrl Pts',(2.22750180242423,-3.24156465711916,10.7781027923877));
#24431=CARTESIAN_POINT('Ctrl Pts',(2.25363386373655,-3.22329387555957,10.7797258289053));
#24432=CARTESIAN_POINT('Ctrl Pts',(2.3475878928883,-3.15760393542214,10.7855612208581));
#24433=CARTESIAN_POINT('Ctrl Pts',(2.43883457827334,-3.08768560540386,10.7913966128109));
#24434=CARTESIAN_POINT('Ctrl Pts',(2.52696543690863,-3.01379074931707,10.7972320047637));
#24435=CARTESIAN_POINT('Ctrl Pts',(2.61498173994283,-2.93999194437274,10.803059811668));
#24436=CARTESIAN_POINT('Ctrl Pts',(2.69988995004763,-2.86222715618575,10.8088876185723));
#24437=CARTESIAN_POINT('Ctrl Pts',(2.7813103475408,-2.78079156907929,10.8147154254767));
#24438=CARTESIAN_POINT('Ctrl Pts',(2.86264740219996,-2.69943934035511,10.8205372669723));
#24439=CARTESIAN_POINT('Ctrl Pts',(2.94050344911103,-2.61442407917905,10.826359108468));
#24440=CARTESIAN_POINT('Ctrl Pts',(3.01453226499092,-2.52608080300862,10.8321809499637));
#24441=CARTESIAN_POINT('Ctrl Pts',(3.08850724603668,-2.43780177135654,10.8379985577314));
#24442=CARTESIAN_POINT('Ctrl Pts',(3.15866026295215,-2.34619985805649,10.8438161654991));
#24443=CARTESIAN_POINT('Ctrl Pts',(3.22468287120717,-2.25164592690393,10.8496337732667));
#24444=CARTESIAN_POINT('Ctrl Pts',(3.29068011935583,-2.15712831509433,10.8554491464188));
#24445=CARTESIAN_POINT('Ctrl Pts',(3.35254987236369,-2.05966128217619,10.8612645195708));
#24446=CARTESIAN_POINT('Ctrl Pts',(3.41002522892359,-1.95964714632625,10.8670798927229));
#24447=CARTESIAN_POINT('Ctrl Pts',(3.4674928737749,-1.85964642979055,10.8728944856021));
#24448=CARTESIAN_POINT('Ctrl Pts',(3.5205670856315,-1.75709965315912,10.8787090784812));
#24449=CARTESIAN_POINT('Ctrl Pts',(3.56902582108089,-1.65243568360704,10.8845236713604));
#24450=CARTESIAN_POINT('Ctrl Pts',(3.61749016656738,-1.54775959717354,10.8903389373913));
#24451=CARTESIAN_POINT('Ctrl Pts',(3.66133779794951,-1.44096621124018,10.8961542034221));
#24452=CARTESIAN_POINT('Ctrl Pts',(3.70039424991618,-1.33250568298497,10.901969469453));
#24453=CARTESIAN_POINT('Ctrl Pts',(3.73948958897038,-1.22393716452989,10.9077905255326));
#24454=CARTESIAN_POINT('Ctrl Pts',(3.77378407801915,-1.11369858340012,10.9136115816122));
#24455=CARTESIAN_POINT('Ctrl Pts',(3.80315269796462,-1.00225673156352,10.9194326376918));
#24456=CARTESIAN_POINT('Ctrl Pts',(3.83253583908598,-0.890759777827898,
10.9252565719652));
#24457=CARTESIAN_POINT('Ctrl Pts',(3.85698817143527,-0.778058778113033,
10.9310805062385));
#24458=CARTESIAN_POINT('Ctrl Pts',(3.87643592228907,-0.664630378772178,
10.9369044405119));
#24459=CARTESIAN_POINT('Ctrl Pts',(3.89591544239246,-0.551016686275567,
10.9427378885858));
#24460=CARTESIAN_POINT('Ctrl Pts',(3.91037399450792,-0.436673636291081,
10.9485713366596));
#24461=CARTESIAN_POINT('Ctrl Pts',(3.91978972160551,-0.322083123425976,
10.9544047847335));
#24462=CARTESIAN_POINT('Ctrl Pts',(3.92863048136433,-0.214490031104953,
10.9598820158014));
#24463=CARTESIAN_POINT('Ctrl Pts',(3.93302597726497,-0.106679082682813,
10.9653592468694));
#24464=CARTESIAN_POINT('Ctrl Pts',(3.93299988442888,0.000953458131958574,
10.9708364779374));
#24465=CARTESIAN_POINT('',(3.93299831367774,-0.00364206096290877,12.2208364640931));
#24466=CARTESIAN_POINT('Ctrl Pts',(3.93299988442875,0.000953458676826257,
10.9708364779651));
#24467=CARTESIAN_POINT('Ctrl Pts',(3.93298746295601,0.0521918102145222,
10.973443907733));
#24468=CARTESIAN_POINT('Ctrl Pts',(3.93197379978628,0.103416823419383,10.9760513375009));
#24469=CARTESIAN_POINT('Ctrl Pts',(3.92996019662714,0.154602241013298,10.9786587672688));
#24470=CARTESIAN_POINT('Ctrl Pts',(3.92542541377817,0.269875577156574,10.9845308914447));
#24471=CARTESIAN_POINT('Ctrl Pts',(3.91580694317262,0.385142477321062,10.9904030156205));
#24472=CARTESIAN_POINT('Ctrl Pts',(3.90109869562193,0.499917960286333,10.9962751397964));
#24473=CARTESIAN_POINT('Ctrl Pts',(3.88640951759966,0.614544634610346,11.0021396506493));
#24474=CARTESIAN_POINT('Ctrl Pts',(3.86664373770084,0.728680752490247,11.0080041615022));
#24475=CARTESIAN_POINT('Ctrl Pts',(3.84184725169761,0.841842440497926,11.0138686723551));
#24476=CARTESIAN_POINT('Ctrl Pts',(3.81707628102204,0.954887686298954,11.019727148687));
#24477=CARTESIAN_POINT('Ctrl Pts',(3.78728498859164,1.06696009520279,11.0255856250189));
#24478=CARTESIAN_POINT('Ctrl Pts',(3.75257085333169,1.17758268954901,11.0314441013508));
#24479=CARTESIAN_POINT('Ctrl Pts',(3.71648789552596,1.29256727361729,11.0375335848625));
#24480=CARTESIAN_POINT('Ctrl Pts',(3.67508593781408,1.4059849034682,11.0436230683742));
#24481=CARTESIAN_POINT('Ctrl Pts',(3.62853270265492,1.51731322598988,11.0497125518859));
#24482=CARTESIAN_POINT('Ctrl Pts',(3.58379740528761,1.62429409630713,11.0555642366245));
#24483=CARTESIAN_POINT('Ctrl Pts',(3.53430577746659,1.72934535777942,11.061415921363));
#24484=CARTESIAN_POINT('Ctrl Pts',(3.4802566423204,1.83202148011008,11.0672676061016));
#24485=CARTESIAN_POINT('Ctrl Pts',(3.42621575083215,1.93468194211929,11.0731183983321));
#24486=CARTESIAN_POINT('Ctrl Pts',(3.3676189266489,2.03496761955094,11.0789691905626));
#24487=CARTESIAN_POINT('Ctrl Pts',(3.30471146846356,2.13245659046214,11.0848199827931));
#24488=CARTESIAN_POINT('Ctrl Pts',(3.24179836819332,2.22995430502739,11.0906712997732));
#24489=CARTESIAN_POINT('Ctrl Pts',(3.17457408953004,2.32465446704812,11.0965226167534));
#24490=CARTESIAN_POINT('Ctrl Pts',(3.10332747457054,2.4161638159644,11.1023739337335));
#24491=CARTESIAN_POINT('Ctrl Pts',(3.03205721294617,2.5077035367223,11.1082271927586));
#24492=CARTESIAN_POINT('Ctrl Pts',(2.95676221428615,2.5960500125395,11.1140804517838));
#24493=CARTESIAN_POINT('Ctrl Pts',(2.87777137047377,2.6808433261348,11.1199337108089));
#24494=CARTESIAN_POINT('Ctrl Pts',(2.79869065917546,2.76573310865675,11.1257936290574));
#24495=CARTESIAN_POINT('Ctrl Pts',(2.71590599212807,2.8470613577299,11.1316535473059));
#24496=CARTESIAN_POINT('Ctrl Pts',(2.62978292935532,2.92450521361672,11.1375134655545));
#24497=CARTESIAN_POINT('Ctrl Pts',(2.54360187745987,3.00200121466787,11.1433773294536));
#24498=CARTESIAN_POINT('Ctrl Pts',(2.45407827250996,3.0756073526987,11.1492411933528));
#24499=CARTESIAN_POINT('Ctrl Pts',(2.36160914426483,3.14504232876518,11.1551050572519));
#24500=CARTESIAN_POINT('Ctrl Pts',(2.26900360185219,3.21457973809384,11.1609775717583));
#24501=CARTESIAN_POINT('Ctrl Pts',(2.17344420358745,3.27993347178056,11.1668500862648));
#24502=CARTESIAN_POINT('Ctrl Pts',(2.07535525939748,3.34086658627537,11.1727226007712));
#24503=CARTESIAN_POINT('Ctrl Pts',(2.04824561414862,3.35770717041565,11.1743456357248));
#24504=CARTESIAN_POINT('Ctrl Pts',(2.02094288146688,3.37421036303248,11.1759686706785));
#24505=CARTESIAN_POINT('Ctrl Pts',(1.99345630321953,3.39037180367498,11.1775917056321));
#24506=CARTESIAN_POINT('Ctrl Pts',(1.89401014270427,3.44884373153116,11.1834638295856));
#24507=CARTESIAN_POINT('Ctrl Pts',(1.79182243863439,3.5030345546962,11.189335953539));
#24508=CARTESIAN_POINT('Ctrl Pts',(1.68729798416334,3.55267709096089,11.1952080774924));
#24509=CARTESIAN_POINT('Ctrl Pts',(1.58290904771732,3.60225526469429,11.2010725881208));
#24510=CARTESIAN_POINT('Ctrl Pts',(1.47618975571495,3.6472967026905,11.2069370987492));
#24511=CARTESIAN_POINT('Ctrl Pts',(1.36757205912588,3.68757856365097,11.2128016093776));
#24512=CARTESIAN_POINT('Ctrl Pts',(1.25906612905989,3.72781897497954,11.2186600854833));
#24513=CARTESIAN_POINT('Ctrl Pts',(1.14866606517241,3.76330940786109,11.224518561589));
#24514=CARTESIAN_POINT('Ctrl Pts',(1.03682588888875,3.79387415133002,11.2303770376946));
#24515=CARTESIAN_POINT('Ctrl Pts',(0.920575705981865,3.82564410320985,11.2364665212905));
#24516=CARTESIAN_POINT('Ctrl Pts',(0.80276991414309,3.85209172587159,11.2425560048864));
#24517=CARTESIAN_POINT('Ctrl Pts',(0.683938671616597,3.87307589565029,11.2486454884822));
#24518=CARTESIAN_POINT('Ctrl Pts',(0.569747881842849,3.89324061722376,11.2544971729917));
#24519=CARTESIAN_POINT('Ctrl Pts',(0.454610673223435,3.90836050409038,11.2603488575011));
#24520=CARTESIAN_POINT('Ctrl Pts',(0.339009367172975,3.91836211304787,11.2662005420105));
#24521=CARTESIAN_POINT('Ctrl Pts',(0.223425692827235,3.92836219654322,11.2720513340112));
#24522=CARTESIAN_POINT('Ctrl Pts',(0.107378473553437,3.9332455186781,11.2779021260119));
#24523=CARTESIAN_POINT('Ctrl Pts',(-0.00864472132234088,3.93299049945372,
11.2837529180126));
#24524=CARTESIAN_POINT('Ctrl Pts',(-0.124678322153347,3.93273545735704,
11.2896042347625));
#24525=CARTESIAN_POINT('Ctrl Pts',(-0.240687480866707,3.92734115868139,
11.2954555515124));
#24526=CARTESIAN_POINT('Ctrl Pts',(-0.356185216441638,3.91683814978209,
11.3013068682623));
#24527=CARTESIAN_POINT('Ctrl Pts',(-0.471721285572108,3.90633165494714,
11.307160127057));
#24528=CARTESIAN_POINT('Ctrl Pts',(-0.586745182549625,3.89071311576923,
11.3130133858517));
#24529=CARTESIAN_POINT('Ctrl Pts',(-0.700776341970374,3.87006479513388,
11.3188666446464));
#24530=CARTESIAN_POINT('Ctrl Pts',(-0.814937234090088,3.84939298300393,
11.3247265626653));
#24531=CARTESIAN_POINT('Ctrl Pts',(-0.928102727295191,3.82368004144668,
11.3305864806843));
#24532=CARTESIAN_POINT('Ctrl Pts',(-1.03980362440171,3.79305911141404,11.3364463987032));
#24533=CARTESIAN_POINT('Ctrl Pts',(-1.1515797329261,3.76241756343093,11.342310262373));
#24534=CARTESIAN_POINT('Ctrl Pts',(-1.26188888920827,3.7268615732093,11.3481741260429));
#24535=CARTESIAN_POINT('Ctrl Pts',(-1.37027986245381,3.68657321893294,11.3540379897127));
#24536=CARTESIAN_POINT('Ctrl Pts',(-1.47883073845663,3.64622542964329,11.3599105039919));
#24537=CARTESIAN_POINT('Ctrl Pts',(-1.58545740436847,3.6011315031968,11.3657830182711));
#24538=CARTESIAN_POINT('Ctrl Pts',(-1.68973121110186,3.55152043978748,11.3716555325503));
#24539=CARTESIAN_POINT('Ctrl Pts',(-1.71855025757699,3.53780900460674,11.3732785696987));
#24540=CARTESIAN_POINT('Ctrl Pts',(-1.74718974259254,3.52375278790568,11.3749016068472));
#24541=CARTESIAN_POINT('Ctrl Pts',(-1.77564100322541,3.5093572100407,11.3765246439956));
#24542=CARTESIAN_POINT('Ctrl Pts',(-1.87857723494723,3.45727422651317,11.3823967679117));
#24543=CARTESIAN_POINT('Ctrl Pts',(-1.97939255309076,3.40057110844041,11.3882688918278));
#24544=CARTESIAN_POINT('Ctrl Pts',(-2.07764341031177,3.33944409439477,11.3941410157439));
#24545=CARTESIAN_POINT('Ctrl Pts',(-2.17576688333062,3.27839633274584,11.4000055263338));
#24546=CARTESIAN_POINT('Ctrl Pts',(-2.27133215961957,3.21293629766038,11.4058700369238));
#24547=CARTESIAN_POINT('Ctrl Pts',(-2.3639183274651,3.14330703894396,11.4117345475137));
#24548=CARTESIAN_POINT('Ctrl Pts',(-2.45640922505211,3.07374942805173,11.4175930235798));
#24549=CARTESIAN_POINT('Ctrl Pts',(-2.5459267831523,3.00003137370619,11.4234514996459));
#24550=CARTESIAN_POINT('Ctrl Pts',(-2.63207782176324,2.92243996348634,11.429309975712));
#24551=CARTESIAN_POINT('Ctrl Pts',(-2.72162591101277,2.84178902021982,11.4353994593223));
#24552=CARTESIAN_POINT('Ctrl Pts',(-2.8075361396866,2.75695321396994,11.4414889429326));
#24553=CARTESIAN_POINT('Ctrl Pts',(-2.88940329061361,2.66830238619824,11.4475784265429));
#24554=CARTESIAN_POINT('Ctrl Pts',(-2.96807346465768,2.58311344324641,11.4534301110101));
#24555=CARTESIAN_POINT('Ctrl Pts',(-3.04301009918702,2.49440217892352,11.4592817954774));
#24556=CARTESIAN_POINT('Ctrl Pts',(-3.11389077473526,2.40253475375875,11.4651334799447));
#24557=CARTESIAN_POINT('Ctrl Pts',(-3.18476063943358,2.31068134038124,11.4709842719024));
#24558=CARTESIAN_POINT('Ctrl Pts',(-3.25157552269572,2.21567305052555,11.4768350638601));
#24559=CARTESIAN_POINT('Ctrl Pts',(-3.31405380922571,2.11790848469818,11.4826858558178));
#24560=CARTESIAN_POINT('Ctrl Pts',(-3.37653769933548,2.02013515051985,11.4885371725239));
#24561=CARTESIAN_POINT('Ctrl Pts',(-3.43468399689634,1.91960539732049,11.4943884892299));
#24562=CARTESIAN_POINT('Ctrl Pts',(-3.4882552657953,1.81674549693989,11.500239805936));
#24563=CARTESIAN_POINT('Ctrl Pts',(-3.54184431492509,1.71385145749913,11.5060930646861));
#24564=CARTESIAN_POINT('Ctrl Pts',(-3.59085512519853,1.60862609954607,11.5119463234362));
#24565=CARTESIAN_POINT('Ctrl Pts',(-3.63509724361739,1.50151824146271,11.5177995821863));
#24566=CARTESIAN_POINT('Ctrl Pts',(-3.67938969607372,1.39428852730337,11.5236595001596));
#24567=CARTESIAN_POINT('Ctrl Pts',(-3.71890246996207,1.28517242054227,11.529519418133));
#24568=CARTESIAN_POINT('Ctrl Pts',(-3.75349406600832,1.17463666571425,11.5353793361064));
#24569=CARTESIAN_POINT('Ctrl Pts',(-3.78810895356494,1.06402648400304,11.54124319973));
#24570=CARTESIAN_POINT('Ctrl Pts',(-3.81779595967751,0.951995149506696,
11.5471070633536));
#24571=CARTESIAN_POINT('Ctrl Pts',(-3.84246447100285,0.839020732211552,
11.5529709269773));
#24572=CARTESIAN_POINT('Ctrl Pts',(-3.86716937431399,0.725879650485935,
11.5588434412097));
#24573=CARTESIAN_POINT('Ctrl Pts',(-3.88684093686975,0.611793115112664,
11.5647159554422));
#24574=CARTESIAN_POINT('Ctrl Pts',(-3.90144022944247,0.49724554908803,11.5705884696747));
#24575=CARTESIAN_POINT('Ctrl Pts',(-3.90547516222909,0.465587047316269,
11.5722115072361));
#24576=CARTESIAN_POINT('Ctrl Pts',(-3.90912295560159,0.433893334131203,
11.5738345447976));
#24577=CARTESIAN_POINT('Ctrl Pts',(-3.9123834894835,0.402174627763785,11.5754575823591));
#24578=CARTESIAN_POINT('Ctrl Pts',(-3.92418004903791,0.287416854281089,
11.5813297063567));
#24579=CARTESIAN_POINT('Ctrl Pts',(-3.93094300318938,0.171947226972836,
11.5872018303543));
#24580=CARTESIAN_POINT('Ctrl Pts',(-3.93259780548776,0.0562450022034934,
11.5930739543519));
#24581=CARTESIAN_POINT('Ctrl Pts',(-3.93425046230221,-0.0593072123422889,
11.5989384650246));
#24582=CARTESIAN_POINT('Ctrl Pts',(-3.93080813179207,-0.175091015091824,
11.6048029756972));
#24583=CARTESIAN_POINT('Ctrl Pts',(-3.92224788754817,-0.290620901904727,
11.6106674863699));
#24584=CARTESIAN_POINT('Ctrl Pts',(-3.9136964517099,-0.406031909620679,
11.6165259625198));
#24585=CARTESIAN_POINT('Ctrl Pts',(-3.90003760738736,-0.521189111292248,
11.6223844386697));
#24586=CARTESIAN_POINT('Ctrl Pts',(-3.88130046816268,-0.635606541690823,
11.6282429148196));
#24587=CARTESIAN_POINT('Ctrl Pts',(-3.86182449886414,-0.754535602041985,
11.6343323983989));
#24588=CARTESIAN_POINT('Ctrl Pts',(-3.83686150121785,-0.872664895569536,
11.6404218819781));
#24589=CARTESIAN_POINT('Ctrl Pts',(-3.80650371712151,-0.989453612626731,
11.6465113655574));
#24590=CARTESIAN_POINT('Ctrl Pts',(-3.77733142788604,-1.10168164029242,
11.6523630501108));
#24591=CARTESIAN_POINT('Ctrl Pts',(-3.74317790042519,-1.21267138998945,
11.6582147346641));
#24592=CARTESIAN_POINT('Ctrl Pts',(-3.70417701890166,-1.32195371047582,
11.6640664192174));
#24593=CARTESIAN_POINT('Ctrl Pts',(-3.66518208585912,-1.43121936303624,
11.6699172112618));
#24594=CARTESIAN_POINT('Ctrl Pts',(-3.62134140768428,-1.53877771492978,
11.6757680033062));
#24595=CARTESIAN_POINT('Ctrl Pts',(-3.57283821333391,-1.64417642038224,
11.6816187953506));
#24596=CARTESIAN_POINT('Ctrl Pts',(-3.52433066880314,-1.7495845788901,11.687470112144));
#24597=CARTESIAN_POINT('Ctrl Pts',(-3.47115994964086,-1.85283233033098,
11.6933214289374));
#24598=CARTESIAN_POINT('Ctrl Pts',(-3.41355644074184,-1.95348955100096,
11.6991727457308));
#24599=CARTESIAN_POINT('Ctrl Pts',(-3.35593381331242,-2.0541801796728,11.7050260045686));
#24600=CARTESIAN_POINT('Ctrl Pts',(-3.29387567591725,-2.1522782093075,11.7108792634065));
#24601=CARTESIAN_POINT('Ctrl Pts',(-3.22765677227372,-2.24738086678595,
11.7167325222444));
#24602=CARTESIAN_POINT('Ctrl Pts',(-3.16136253171153,-2.34259172208673,
11.7225924403059));
#24603=CARTESIAN_POINT('Ctrl Pts',(-3.09089831296656,-2.4348000638389,11.7284523583673));
#24604=CARTESIAN_POINT('Ctrl Pts',(-3.01658039560449,-2.52363462427797,
11.7343122764288));
#24605=CARTESIAN_POINT('Ctrl Pts',(-2.94221243786159,-2.61252899956915,
11.7401761401408));
#24606=CARTESIAN_POINT('Ctrl Pts',(-2.86398589309222,-2.69804476592693,
11.7460400038529));
#24607=CARTESIAN_POINT('Ctrl Pts',(-2.78225406666779,-2.77984735345496,
11.7519038675649));
#24608=CARTESIAN_POINT('Ctrl Pts',(-2.70040166615228,-2.86177061946371,
11.7577763818855));
#24609=CARTESIAN_POINT('Ctrl Pts',(-2.61503396706536,-2.93996949570728,
11.763648896206));
#24610=CARTESIAN_POINT('Ctrl Pts',(-2.52653754786125,-3.01414946863079,
11.7695214105266));
#24611=CARTESIAN_POINT('Ctrl Pts',(-2.50207903977182,-3.03465121869187,
11.7711444472586));
#24612=CARTESIAN_POINT('Ctrl Pts',(-2.4773817136686,-3.05484624018212,11.7727674839905));
#24613=CARTESIAN_POINT('Ctrl Pts',(-2.45245410270203,-3.07472891067489,
11.7743905207225));
#24614=CARTESIAN_POINT('Ctrl Pts',(-2.36226635846595,-3.14666413156455,
11.7802626446843));
#24615=CARTESIAN_POINT('Ctrl Pts',(-2.26875973340759,-3.21474851506088,
11.7861347686461));
#24616=CARTESIAN_POINT('Ctrl Pts',(-2.17229721285864,-3.2786603695727,11.7920068926079));
#24617=CARTESIAN_POINT('Ctrl Pts',(-2.07595975788287,-3.34248936109616,
11.7978714032445));
#24618=CARTESIAN_POINT('Ctrl Pts',(-1.97667437007134,-3.40215635547035,
11.803735913881));
#24619=CARTESIAN_POINT('Ctrl Pts',(-1.87483718466834,-3.45737972039302,
11.8096004245175));
#24620=CARTESIAN_POINT('Ctrl Pts',(-1.77310478871571,-3.51254626102273,
11.8154589006309));
#24621=CARTESIAN_POINT('Ctrl Pts',(-1.6688261791917,-3.56327807113751,11.8213173767443));
#24622=CARTESIAN_POINT('Ctrl Pts',(-1.56242599901136,-3.60933705791152,
11.8271758528578));
#24623=CARTESIAN_POINT('Ctrl Pts',(-1.45183031867757,-3.65721221159191,
11.8332653364506));
#24624=CARTESIAN_POINT('Ctrl Pts',(-1.33894269222286,-3.70003819797956,
11.8393548200434));
#24625=CARTESIAN_POINT('Ctrl Pts',(-1.22426802220387,-3.73760040799027,
11.8454443036363));
#24626=CARTESIAN_POINT('Ctrl Pts',(-1.11407148735314,-3.77369578444812,
11.8512959881526));
#24627=CARTESIAN_POINT('Ctrl Pts',(-1.00222529057778,-3.80493063814588,
11.8571476726689));
#24628=CARTESIAN_POINT('Ctrl Pts',(-0.889196539348197,-3.83116412000467,
11.8629993571852));
#24629=CARTESIAN_POINT('Ctrl Pts',(-0.776185027459509,-3.85739360068738,
11.8688501491924));
#24630=CARTESIAN_POINT('Ctrl Pts',(-0.661991722336443,-3.87862313281099,
11.8747009411997));
#24631=CARTESIAN_POINT('Ctrl Pts',(-0.547096253974035,-3.89476246886605,
11.8805517332069));
#24632=CARTESIAN_POINT('Ctrl Pts',(-0.432190480807463,-3.91090325243423,
11.886403049963));
#24633=CARTESIAN_POINT('Ctrl Pts',(-0.316582828628814,-3.92195287487916,
11.8922543667191));
#24634=CARTESIAN_POINT('Ctrl Pts',(-0.200759709458467,-3.92787277531467,
11.8981056834752));
#24635=CARTESIAN_POINT('Ctrl Pts',(-0.0848981487451517,-3.93379464055745,
11.9039589422757));
#24636=CARTESIAN_POINT('Ctrl Pts',(0.0311786085037482,-3.93458337729355,
11.9098122010763));
#24637=CARTESIAN_POINT('Ctrl Pts',(0.146983195004135,-3.9302525288315,11.9156654598768));
#24638=CARTESIAN_POINT('Ctrl Pts',(0.262919531811611,-3.9259167531845,11.921525377901));
#24639=CARTESIAN_POINT('Ctrl Pts',(0.378582666452337,-3.91644978219727,
11.9273852959252));
#24640=CARTESIAN_POINT('Ctrl Pts',(0.493489297763407,-3.90191713302486,
11.9332452139495));
#24641=CARTESIAN_POINT('Ctrl Pts',(0.608473298998659,-3.88737469860376,
11.9391090776242));
#24642=CARTESIAN_POINT('Ctrl Pts',(0.722699376183601,-3.86775986409176,
11.944972941299));
#24643=CARTESIAN_POINT('Ctrl Pts',(0.835695100465841,-3.84318913131495,
11.9508368049738));
#24644=CARTESIAN_POINT('Ctrl Pts',(0.948857520610756,-3.81858215079937,
11.9567093192574));
#24645=CARTESIAN_POINT('Ctrl Pts',(1.0607855671211,-3.78900478556273,11.962581833541));
#24646=CARTESIAN_POINT('Ctrl Pts',(1.17102253719025,-3.75462317914761,11.9684543478246));
#24647=CARTESIAN_POINT('Ctrl Pts',(1.20148967309694,-3.74512084000782,11.9700773849117));
#24648=CARTESIAN_POINT('Ctrl Pts',(1.23182775947559,-3.73525180915616,11.9717004219989));
#24649=CARTESIAN_POINT('Ctrl Pts',(1.26202745450664,-3.7250202286795,11.973323459086));
#24650=CARTESIAN_POINT('Ctrl Pts',(1.3712895004446,-3.68800252320569,11.9791955830458));
#24651=CARTESIAN_POINT('Ctrl Pts',(1.47910464051812,-3.6461113813765,11.9850677070056));
#24652=CARTESIAN_POINT('Ctrl Pts',(1.58500605166983,-3.59947840890455,11.9909398309654));
#24653=CARTESIAN_POINT('Ctrl Pts',(1.69077015953713,-3.55290589700826,11.9968043415998));
#24654=CARTESIAN_POINT('Ctrl Pts',(1.79462509780673,-3.50160394543342,12.0026688522342));
#24655=CARTESIAN_POINT('Ctrl Pts',(1.89611983850175,-3.44575369956126,12.0085333628686));
#24656=CARTESIAN_POINT('Ctrl Pts',(1.99751014211621,-3.38996092303763,12.0143918389798));
#24657=CARTESIAN_POINT('Ctrl Pts',(2.09654471878094,-3.3296293593651,12.020250315091));
#24658=CARTESIAN_POINT('Ctrl Pts',(2.19279377239964,-3.26498766792853,12.0261087912022));
#24659=CARTESIAN_POINT('Ctrl Pts',(2.29283805384609,-3.1977970688721,12.0321982747958));
#24660=CARTESIAN_POINT('Ctrl Pts',(2.38987220270247,-3.12594962440529,12.0382877583894));
#24661=CARTESIAN_POINT('Ctrl Pts',(2.48344281495836,-3.04975421711844,12.0443772419831));
#24662=CARTESIAN_POINT('Ctrl Pts',(2.57335942188605,-2.97653429986524,12.0502289264968));
#24663=CARTESIAN_POINT('Ctrl Pts',(2.66007757281388,-2.89929991563099,12.0560806110106));
#24664=CARTESIAN_POINT('Ctrl Pts',(2.74322635097398,-2.81836800069153,12.0619322955244));
#24665=CARTESIAN_POINT('Ctrl Pts',(2.82636244713697,-2.73744842962932,12.067783087529));
#24666=CARTESIAN_POINT('Ctrl Pts',(2.90592995681614,-2.65283273745029,12.0736338795336));
#24667=CARTESIAN_POINT('Ctrl Pts',(2.98159377500211,-2.56487573984952,12.0794846715382));
#24668=CARTESIAN_POINT('Ctrl Pts',(3.05726437936244,-2.47691085351759,12.0853359882916));
#24669=CARTESIAN_POINT('Ctrl Pts',(3.12903032661077,-2.38560437945964,12.0911873050449));
#24670=CARTESIAN_POINT('Ctrl Pts',(3.19659633837172,-2.2913447688003,12.0970386217983));
#24671=CARTESIAN_POINT('Ctrl Pts',(3.26418477520299,-2.19705387350032,12.102891880596));
#24672=CARTESIAN_POINT('Ctrl Pts',(3.32757026403745,-2.09980822847908,12.1087451393937));
#24673=CARTESIAN_POINT('Ctrl Pts',(3.38650085297318,-2.00002524304368,12.1145983981914));
#24674=CARTESIAN_POINT('Ctrl Pts',(3.44549848694824,-1.90012873499966,12.1204583162126));
#24675=CARTESIAN_POINT('Ctrl Pts',(3.50003089444123,-1.79768948090604,12.1263182342339));
#24676=CARTESIAN_POINT('Ctrl Pts',(3.54989205363726,-1.69314955261578,12.1321781522551));
#24677=CARTESIAN_POINT('Ctrl Pts',(3.59978678577848,-1.58853923460057,12.1380420159268));
#24678=CARTESIAN_POINT('Ctrl Pts',(3.64500384584713,-1.48182580567601,12.1439058795986));
#24679=CARTESIAN_POINT('Ctrl Pts',(3.68538598749074,-1.37346973872995,12.1497697432703));
#24680=CARTESIAN_POINT('Ctrl Pts',(3.72582770250234,-1.2649538205331,12.1556422575508));
#24681=CARTESIAN_POINT('Ctrl Pts',(3.76142013698568,-1.1547908198029,12.1615147718313));
#24682=CARTESIAN_POINT('Ctrl Pts',(3.79205631273742,-1.04345480066378,12.1673872861118));
#24683=CARTESIAN_POINT('Ctrl Pts',(3.80052349525184,-1.01268391065065,12.1690103232243));
#24684=CARTESIAN_POINT('Ctrl Pts',(3.808612396395,-0.981823467267782,12.1706333603369));
#24685=CARTESIAN_POINT('Ctrl Pts',(3.81632145366088,-0.950883569280524,
12.1722563974494));
#24686=CARTESIAN_POINT('Ctrl Pts',(3.8547788322017,-0.796536892654378,12.1803530752234));
#24687=CARTESIAN_POINT('Ctrl Pts',(3.88388803832101,-0.639774846675686,
12.1884497529973));
#24688=CARTESIAN_POINT('Ctrl Pts',(3.90340589677512,-0.481571806713381,
12.1965464307713));
#24689=CARTESIAN_POINT('Ctrl Pts',(3.92170070402504,-0.333282273347502,
12.2041357449159));
#24690=CARTESIAN_POINT('Ctrl Pts',(3.93156890341389,-0.183726492797682,
12.2117250590606));
#24691=CARTESIAN_POINT('Ctrl Pts',(3.93285535666324,-0.03373045456698,12.2193143732052));
#24692=CARTESIAN_POINT('Ctrl Pts',(3.9329413591105,-0.0237028640777174,
12.2198217368345));
#24693=CARTESIAN_POINT('Ctrl Pts',(3.93298902446914,-0.0136733158283392,
12.2203291004638));
#24694=CARTESIAN_POINT('Ctrl Pts',(3.93299831367774,-0.00364206096290877,
12.2208364640931));
#24695=CARTESIAN_POINT('',(3.92657020349652,0.00060237016638537,13.470836477965));
#24696=CARTESIAN_POINT('Ctrl Pts',(3.93255568468074,-0.00364137684070624,
12.220836477965));
#24697=CARTESIAN_POINT('Ctrl Pts',(3.92346996534201,0.987148471629003,12.2709540972476));
#24698=CARTESIAN_POINT('Ctrl Pts',(3.04053014230206,3.3032803818384,12.3873826959847));
#24699=CARTESIAN_POINT('Ctrl Pts',(-0.855351412277205,4.57304180444516,
12.5701222741763));
#24700=CARTESIAN_POINT('Ctrl Pts',(-4.31013578855369,1.75130433299333,12.7690552125397));
#24701=CARTESIAN_POINT('Ctrl Pts',(-3.80259280182653,-2.68041514802392,
12.9679881509031));
#24702=CARTESIAN_POINT('Ctrl Pts',(0.20069098000617,-4.64801683659501,13.1669210892666));
#24703=CARTESIAN_POINT('Ctrl Pts',(3.4183096060697,-2.70559174609466,13.3345371982872));
#24704=CARTESIAN_POINT('Ctrl Pts',(3.925624757664,-0.693867882632318,13.4358423278534));
#24705=CARTESIAN_POINT('Ctrl Pts',(3.92657020349652,0.00060237016638537,
13.470836477965));
#24706=CARTESIAN_POINT('',(3.93319014431769,0.0034425050413224,14.7208363833869));
#24707=CARTESIAN_POINT('Ctrl Pts',(3.92657020349652,0.00060237016638537,
13.470836477965));
#24708=CARTESIAN_POINT('Ctrl Pts',(3.92741629822079,0.622095000252939,13.5021533073078));
#24709=CARTESIAN_POINT('Ctrl Pts',(3.49488999972759,2.55843734936597,13.5997811161051));
#24710=CARTESIAN_POINT('Ctrl Pts',(0.457995462913449,4.62974918743228,13.7637199043569));
#24711=CARTESIAN_POINT('Ctrl Pts',(-3.64818774369287,2.88705101605783,13.9626528427203));
#24712=CARTESIAN_POINT('Ctrl Pts',(-4.40057542481316,-1.5097262377929,14.1615857810838));
#24713=CARTESIAN_POINT('Ctrl Pts',(-1.10749417555734,-4.5186053195277,14.3605187194471));
#24714=CARTESIAN_POINT('Ctrl Pts',(2.93246189479444,-3.44555640217872,14.546935326452));
#24715=CARTESIAN_POINT('Ctrl Pts',(3.92501016529069,-1.05851774818717,14.6670409540021));
#24716=CARTESIAN_POINT('Ctrl Pts',(3.93477334405261,0.00342846837678905,
14.7208356020977));
#24717=CARTESIAN_POINT('',(3.93483603884783,-0.00214359731175201,15.9708371227931));
#24718=CARTESIAN_POINT('Ctrl Pts',(3.93299849192155,0.00344420423336513,
14.720836477965));
#24719=CARTESIAN_POINT('Ctrl Pts',(3.93284829647542,0.174955073829664,14.729528644049));
#24720=CARTESIAN_POINT('Ctrl Pts',(3.92147599299458,0.345993796770016,14.7382208101329));
#24721=CARTESIAN_POINT('Ctrl Pts',(3.89908469475258,0.515390670410515,14.7469129762169));
#24722=CARTESIAN_POINT('Ctrl Pts',(3.88923427460412,0.589912047382934,14.750736849536));
#24723=CARTESIAN_POINT('Ctrl Pts',(3.8772518881715,0.66411615003633,14.754560722855));
#24724=CARTESIAN_POINT('Ctrl Pts',(3.86315739411471,0.737905107921655,14.7583845961741));
#24725=CARTESIAN_POINT('Ctrl Pts',(3.84151321047313,0.851218984159783,14.7642567201401));
#24726=CARTESIAN_POINT('Ctrl Pts',(3.81484294080112,0.963769723562685,14.7701288441062));
#24727=CARTESIAN_POINT('Ctrl Pts',(3.78321275945683,1.07507684222245,14.7760009680722));
#24728=CARTESIAN_POINT('Ctrl Pts',(3.75162358727073,1.1862396489927,14.7818654787129));
#24729=CARTESIAN_POINT('Ctrl Pts',(3.7150874035512,1.29616164746434,14.7877299893536));
#24730=CARTESIAN_POINT('Ctrl Pts',(3.67372162348358,1.40437118780939,14.7935944999943));
#24731=CARTESIAN_POINT('Ctrl Pts',(3.6323984083921,1.51246938161401,14.799452976112));
#24732=CARTESIAN_POINT('Ctrl Pts',(3.58625562846616,1.61885823836361,14.8053114522296));
#24733=CARTESIAN_POINT('Ctrl Pts',(3.53546068077294,1.72308060598121,14.8111699283472));
#24734=CARTESIAN_POINT('Ctrl Pts',(3.48266282100748,1.8314125996104,14.8172594119384));
#24735=CARTESIAN_POINT('Ctrl Pts',(3.42483848772265,1.93740329631429,14.8233488955297));
#24736=CARTESIAN_POINT('Ctrl Pts',(3.36223129361279,2.04056113073116,14.829438379121));
#24737=CARTESIAN_POINT('Ctrl Pts',(3.30206895913103,2.13969057147421,14.8352900636414));
#24738=CARTESIAN_POINT('Ctrl Pts',(3.23749053752719,2.23620386226628,14.8411417481618));
#24739=CARTESIAN_POINT('Ctrl Pts',(3.16875895953531,2.32969003439614,14.8469934326822));
#24740=CARTESIAN_POINT('Ctrl Pts',(3.10003786460307,2.42316194785268,14.8528442246935));
#24741=CARTESIAN_POINT('Ctrl Pts',(3.02716511758818,2.51360732766554,14.8586950167048));
#24742=CARTESIAN_POINT('Ctrl Pts',(2.95044609254254,2.60064546891738,14.8645458087161));
#24743=CARTESIAN_POINT('Ctrl Pts',(2.87372018668186,2.6876914164904,14.8703971254763));
#24744=CARTESIAN_POINT('Ctrl Pts',(2.79314759040793,2.77132920786618,14.8762484422364));
#24745=CARTESIAN_POINT('Ctrl Pts',(2.70907246939167,2.85121296215911,14.8820997589966));
#24746=CARTESIAN_POINT('Ctrl Pts',(2.62496944395245,2.93112322976585,14.8879530178011));
#24747=CARTESIAN_POINT('Ctrl Pts',(2.53736188179197,3.00727669816909,14.8938062766056));
#24748=CARTESIAN_POINT('Ctrl Pts',(2.44662858854818,3.07936642017457,14.8996595354102));
#24749=CARTESIAN_POINT('Ctrl Pts',(2.35579206848544,3.15153815830021,14.9055194534383));
#24750=CARTESIAN_POINT('Ctrl Pts',(2.26182304327764,3.21963666470747,14.9113793714664));
#24751=CARTESIAN_POINT('Ctrl Pts',(2.16513106164585,3.28339709537185,14.9172392894945));
#24752=CARTESIAN_POINT('Ctrl Pts',(2.06837397453576,3.34720045775885,14.9231031531732));
#24753=CARTESIAN_POINT('Ctrl Pts',(1.96889063425004,3.40665971664292,14.9289670168518));
#24754=CARTESIAN_POINT('Ctrl Pts',(1.86711552174194,3.46155581039369,14.9348308805304));
#24755=CARTESIAN_POINT('Ctrl Pts',(1.76519026647323,3.51653288908135,14.9407033948178));
#24756=CARTESIAN_POINT('Ctrl Pts',(1.66096686208982,3.56693318797672,14.9465759091052));
#24757=CARTESIAN_POINT('Ctrl Pts',(1.5549001628775,3.61258556763484,14.9524484233926));
#24758=CARTESIAN_POINT('Ctrl Pts',(1.52558560117776,3.62520290663159,14.9540714604409));
#24759=CARTESIAN_POINT('Ctrl Pts',(1.49613032818587,3.63745786887671,14.9556944974892));
#24760=CARTESIAN_POINT('Ctrl Pts',(1.46654413194279,3.64934751826462,14.9573175345375));
#24761=CARTESIAN_POINT('Ctrl Pts',(1.35950171279001,3.69236409338985,14.9631896585035));
#24762=CARTESIAN_POINT('Ctrl Pts',(1.25038559468209,3.73073915030892,14.9690617824696));
#24763=CARTESIAN_POINT('Ctrl Pts',(1.13963583403457,3.7642687425029,14.9749339064356));
#24764=CARTESIAN_POINT('Ctrl Pts',(1.02902966265078,3.79775486291483,14.9807984170763));
#24765=CARTESIAN_POINT('Ctrl Pts',(0.916794452779745,3.82640789301592,14.986662927717));
#24766=CARTESIAN_POINT('Ctrl Pts',(0.803390515337624,3.85007177593685,14.9925274383577));
#24767=CARTESIAN_POINT('Ctrl Pts',(0.690103269418896,3.87371130895768,14.9983859144753));
#24768=CARTESIAN_POINT('Ctrl Pts',(0.575650090234624,3.89237182219734,15.004244390593));
#24769=CARTESIAN_POINT('Ctrl Pts',(0.460506097283638,3.90594714945871,15.0101028667106));
#24770=CARTESIAN_POINT('Ctrl Pts',(0.340821824166863,3.92005776985634,15.0161923503018));
#24771=CARTESIAN_POINT('Ctrl Pts',(0.220391572605051,3.92867379076967,15.0222818338931));
#24772=CARTESIAN_POINT('Ctrl Pts',(0.0997606018152224,3.93173458187674,
15.0283713174844));
#24773=CARTESIAN_POINT('Ctrl Pts',(-0.0161596357340333,3.93467584671028,
15.0342230020048));
#24774=CARTESIAN_POINT('Ctrl Pts',(-0.132264757993117,3.93248760048722,
15.0400746865252));
#24775=CARTESIAN_POINT('Ctrl Pts',(-0.248066884677823,3.92516901810944,
15.0459263710456));
#24776=CARTESIAN_POINT('Ctrl Pts',(-0.363851349021001,3.91785155197456,
15.0517771630569));
#24777=CARTESIAN_POINT('Ctrl Pts',(-0.479332497200843,3.90540533158387,
15.0576279550682));
#24778=CARTESIAN_POINT('Ctrl Pts',(-0.594024980004118,3.88788159839405,
15.0634787470795));
#24779=CARTESIAN_POINT('Ctrl Pts',(-0.70872774940532,3.87035629352672,15.0693300638397));
#24780=CARTESIAN_POINT('Ctrl Pts',(-0.822641304122427,3.84775263302172,
15.0751813805998));
#24781=CARTESIAN_POINT('Ctrl Pts',(-0.935288636375196,3.82017331631268,
15.0810326973599));
#24782=CARTESIAN_POINT('Ctrl Pts',(-1.04797335613054,3.79258484606442,15.0868859561645));
#24783=CARTESIAN_POINT('Ctrl Pts',(-1.159390616426,3.76001753414329,15.092739214969));
#24784=CARTESIAN_POINT('Ctrl Pts',(-1.26907745228952,3.7226242652315,15.0985924737735));
#24785=CARTESIAN_POINT('Ctrl Pts',(-1.37888907832363,3.68518845418263,15.1044523918016));
#24786=CARTESIAN_POINT('Ctrl Pts',(-1.48696595892933,3.6429158607928,15.1103123098298));
#24787=CARTESIAN_POINT('Ctrl Pts',(-1.59286394454679,3.59600798861221,15.1161722278579));
#24788=CARTESIAN_POINT('Ctrl Pts',(-1.69883323430863,3.54906853201884,15.1220360915365));
#24789=CARTESIAN_POINT('Ctrl Pts',(-1.80262033846515,3.49748776552355,15.1278999552151));
#24790=CARTESIAN_POINT('Ctrl Pts',(-1.90380615860214,3.44151291011214,15.1337638188938));
#24791=CARTESIAN_POINT('Ctrl Pts',(-2.00514125215168,3.38545547833112,15.1396363331812));
#24792=CARTESIAN_POINT('Ctrl Pts',(-2.10386705147764,3.32499123520002,15.1455088474686));
#24793=CARTESIAN_POINT('Ctrl Pts',(-2.19959377321235,3.26041043932286,15.1513813617559));
#24794=CARTESIAN_POINT('Ctrl Pts',(-2.22605058681703,3.24256169188848,15.1530043988043));
#24795=CARTESIAN_POINT('Ctrl Pts',(-2.25227851449835,3.22439873463254,15.1546274358526));
#24796=CARTESIAN_POINT('Ctrl Pts',(-2.27826979674855,3.20592821710395,15.156250472901));
#24797=CARTESIAN_POINT('Ctrl Pts',(-2.37230587039499,3.13910215866305,15.162122596867));
#24798=CARTESIAN_POINT('Ctrl Pts',(-2.46355689507432,3.06802316936622,15.1679947208331));
#24799=CARTESIAN_POINT('Ctrl Pts',(-2.55161347817067,2.99295132904259,15.1738668447991));
#24800=CARTESIAN_POINT('Ctrl Pts',(-2.63955589415856,2.91797682085057,15.1797313554398));
#24801=CARTESIAN_POINT('Ctrl Pts',(-2.72431179312379,2.83902002216063,15.1855958660805));
#24802=CARTESIAN_POINT('Ctrl Pts',(-2.80550113433061,2.75638393284928,15.1914603767212));
#24803=CARTESIAN_POINT('Ctrl Pts',(-2.88660693251308,2.67383287525169,15.1973188528388));
#24804=CARTESIAN_POINT('Ctrl Pts',(-2.96415318465746,2.58761035059531,15.2031773289564));
#24805=CARTESIAN_POINT('Ctrl Pts',(-3.03779382834163,2.49805877762904,15.209035805074));
#24806=CARTESIAN_POINT('Ctrl Pts',(-3.11433822015321,2.4049760675176,15.2151252886653));
#24807=CARTESIAN_POINT('Ctrl Pts',(-3.18666231397037,2.30829666556898,15.2212147722566));
#24808=CARTESIAN_POINT('Ctrl Pts',(-3.25442046332261,2.20844661423071,15.2273042558478));
#24809=CARTESIAN_POINT('Ctrl Pts',(-3.31953260423783,2.11249578506427,15.2331559403682));
#24810=CARTESIAN_POINT('Ctrl Pts',(-3.38042846209905,2.01361766649564,15.2390076248886));
#24811=CARTESIAN_POINT('Ctrl Pts',(-3.4368437176281,1.91222233555626,15.244859309409));
#24812=CARTESIAN_POINT('Ctrl Pts',(-3.49325036860438,1.81084246960889,15.2507101014203));
#24813=CARTESIAN_POINT('Ctrl Pts',(-3.54517757509486,1.70694651582322,15.2565608934316));
#24814=CARTESIAN_POINT('Ctrl Pts',(-3.59240619645619,1.60097055552661,15.262411685443));
#24815=CARTESIAN_POINT('Ctrl Pts',(-3.63963905368221,1.49498509040399,15.2682630022031));
#24816=CARTESIAN_POINT('Ctrl Pts',(-3.68217231976241,1.38691962555487,15.2741143189632));
#24817=CARTESIAN_POINT('Ctrl Pts',(-3.7198346602213,1.27723102867737,15.2799656357233));
#24818=CARTESIAN_POINT('Ctrl Pts',(-3.75750950076182,1.16750602629776,15.2858188945279));
#24819=CARTESIAN_POINT('Ctrl Pts',(-3.79031006688662,1.05615721148869,15.2916721533324));
#24820=CARTESIAN_POINT('Ctrl Pts',(-3.81811484008639,0.943656753227619,
15.2975254121369));
#24821=CARTESIAN_POINT('Ctrl Pts',(-3.8459512466391,0.831028303751601,15.303385330165));
#24822=CARTESIAN_POINT('Ctrl Pts',(-3.86878041652374,0.71724599723719,15.3092452481931));
#24823=CARTESIAN_POINT('Ctrl Pts',(-3.88653190804482,0.60279244168245,15.3151051662213));
#24824=CARTESIAN_POINT('Ctrl Pts',(-3.90429535215317,0.488261821273257,
15.3209690298999));
#24825=CARTESIAN_POINT('Ctrl Pts',(-3.91697426499136,0.373059461789268,
15.3268328935785));
#24826=CARTESIAN_POINT('Ctrl Pts',(-3.92455020975565,0.257671595459889,
15.3326967572571));
#24827=CARTESIAN_POINT('Ctrl Pts',(-3.93213733085994,0.142113504285216,
15.3385692715445));
#24828=CARTESIAN_POINT('Ctrl Pts',(-3.93460645040682,0.0263697718473956,
15.3444417858319));
#24829=CARTESIAN_POINT('Ctrl Pts',(-3.931991185563,-0.0890747812506412,
15.3503143001193));
#24830=CARTESIAN_POINT('Ctrl Pts',(-3.93126838242877,-0.120981180714116,
15.3519373371676));
#24831=CARTESIAN_POINT('Ctrl Pts',(-3.93015751202227,-0.152864768556174,
15.353560374216));
#24832=CARTESIAN_POINT('Ctrl Pts',(-3.92865997671956,-0.184715422533844,
15.3551834112644));
#24833=CARTESIAN_POINT('Ctrl Pts',(-3.92324191620768,-0.299950616176578,
15.3610555352304));
#24834=CARTESIAN_POINT('Ctrl Pts',(-3.91274036694306,-0.415140414715906,
15.3669276591964));
#24835=CARTESIAN_POINT('Ctrl Pts',(-3.89715295659655,-0.529799804540171,
15.3727997831624));
#24836=CARTESIAN_POINT('Ctrl Pts',(-3.88158575563705,-0.644310536188886,
15.3786642938032));
#24837=CARTESIAN_POINT('Ctrl Pts',(-3.86094586168443,-0.758291820821086,
15.3845288044439));
#24838=CARTESIAN_POINT('Ctrl Pts',(-3.83528287735399,-0.871260150974015,
15.3903933150846));
#24839=CARTESIAN_POINT('Ctrl Pts',(-3.80964629997913,-0.984112237839073,
15.3962517912022));
#24840=CARTESIAN_POINT('Ctrl Pts',(-3.77899700406635,-1.09595304273518,
15.4021102673198));
#24841=CARTESIAN_POINT('Ctrl Pts',(-3.7434361210232,-1.20630634907506,15.4079687434374));
#24842=CARTESIAN_POINT('Ctrl Pts',(-3.70647302525648,-1.32101103246172,
15.4140582270287));
#24843=CARTESIAN_POINT('Ctrl Pts',(-3.66420309412753,-1.4341080449332,15.4201477106199));
#24844=CARTESIAN_POINT('Ctrl Pts',(-3.61679804827907,-1.54507633402518,
15.4262371942112));
#24845=CARTESIAN_POINT('Ctrl Pts',(-3.57124420634438,-1.65171122511293,
15.4320888787316));
#24846=CARTESIAN_POINT('Ctrl Pts',(-3.52094896171056,-1.75638011353525,
15.437940563252));
#24847=CARTESIAN_POINT('Ctrl Pts',(-3.46611454601575,-1.85863900580453,
15.4437922477724));
#24848=CARTESIAN_POINT('Ctrl Pts',(-3.4112884937613,-1.96088230136988,15.4496430397837));
#24849=CARTESIAN_POINT('Ctrl Pts',(-3.35192484231415,-2.06071596740399,
15.455493831795));
#24850=CARTESIAN_POINT('Ctrl Pts',(-3.28827211658734,-2.15771997424925,
15.4613446238064));
#24851=CARTESIAN_POINT('Ctrl Pts',(-3.22461368194239,-2.25473268123938,
15.4671959405665));
#24852=CARTESIAN_POINT('Ctrl Pts',(-3.15666563512766,-2.34891487887022,
15.4730472573266));
#24853=CARTESIAN_POINT('Ctrl Pts',(-3.08471982353216,-2.43987553172446,
15.4788985740868));
#24854=CARTESIAN_POINT('Ctrl Pts',(-3.01275013321574,-2.53086637430061,
15.4847518328913));
#24855=CARTESIAN_POINT('Ctrl Pts',(-2.93678029608717,-2.6186332219377,15.4906050916958));
#24856=CARTESIAN_POINT('Ctrl Pts',(-2.85714195261617,-2.70281868844372,
15.4964583505003));
#24857=CARTESIAN_POINT('Ctrl Pts',(-2.77741300499568,-2.78709993233863,
15.5023182685285));
#24858=CARTESIAN_POINT('Ctrl Pts',(-2.69400750482798,-2.86779136196497,
15.5081781865566));
#24859=CARTESIAN_POINT('Ctrl Pts',(-2.60729347565185,-2.94457292859649,
15.5140381045847));
#24860=CARTESIAN_POINT('Ctrl Pts',(-2.52052105943819,-3.02140619445425,
15.5199019682633));
#24861=CARTESIAN_POINT('Ctrl Pts',(-2.43043599892805,-3.09432409578404,
15.525765831942));
#24862=CARTESIAN_POINT('Ctrl Pts',(-2.3374374679654,-3.16304838460487,15.5316296956206));
#24863=CARTESIAN_POINT('Ctrl Pts',(-2.24430174181019,-3.23187405827491,
15.537502209908));
#24864=CARTESIAN_POINT('Ctrl Pts',(-2.14824430878899,-3.29649354226668,
15.5433747241954));
#24865=CARTESIAN_POINT('Ctrl Pts',(-2.04969128218924,-3.35667315175568,
15.5492472384828));
#24866=CARTESIAN_POINT('Ctrl Pts',(-2.02245333851314,-3.37330550562918,
15.5508702755311));
#24867=CARTESIAN_POINT('Ctrl Pts',(-1.99502489821788,-3.38959899726523,
15.5524933125795));
#24868=CARTESIAN_POINT('Ctrl Pts',(-1.9674152363527,-3.40554933715065,15.5541163496278));
#24869=CARTESIAN_POINT('Ctrl Pts',(-1.86752388926439,-3.46325743026134,
15.5599884735938));
#24870=CARTESIAN_POINT('Ctrl Pts',(-1.76492388788527,-3.51666353423357,
15.5658605975599));
#24871=CARTESIAN_POINT('Ctrl Pts',(-1.66002206106583,-3.5655035768843,15.5717327215259));
#24872=CARTESIAN_POINT('Ctrl Pts',(-1.55525624154774,-3.61428029745,15.5775972321666));
#24873=CARTESIAN_POINT('Ctrl Pts',(-1.44819490272289,-3.65850255652633,
15.5834617428073));
#24874=CARTESIAN_POINT('Ctrl Pts',(-1.33927169064858,-3.69795082966598,
15.589326253448));
#24875=CARTESIAN_POINT('Ctrl Pts',(-1.23046055947581,-3.73735851092504,
15.5951847295657));
#24876=CARTESIAN_POINT('Ctrl Pts',(-1.11979175213365,-3.77200183728434,
15.6010432056833));
#24877=CARTESIAN_POINT('Ctrl Pts',(-1.00772062329801,-3.80170858238501,
15.6069016818009));
#24878=CARTESIAN_POINT('Ctrl Pts',(-0.891230381399196,-3.83258670379556,
15.6129911653922));
#24879=CARTESIAN_POINT('Ctrl Pts',(-0.773225364568132,-3.85813073069646,
15.6190806489834));
#24880=CARTESIAN_POINT('Ctrl Pts',(-0.654236796995729,-3.87820360649834,
15.6251701325747));
#24881=CARTESIAN_POINT('Ctrl Pts',(-0.539894825540682,-3.89749262088675,
15.6310218170951));
#24882=CARTESIAN_POINT('Ctrl Pts',(-0.424645124729601,-3.9117296957019,
15.6368735016155));
#24883=CARTESIAN_POINT('Ctrl Pts',(-0.308970564655511,-3.92084508622522,
15.6427251861359));
#24884=CARTESIAN_POINT('Ctrl Pts',(-0.193313647466286,-3.92995908645334,
15.6485759781472));
#24885=CARTESIAN_POINT('Ctrl Pts',(-0.0772324118786128,-3.93395292312858,
15.6544267701585));
#24886=CARTESIAN_POINT('Ctrl Pts',(0.0387854217168801,-3.93280875343084,
15.6602775621698));
#24887=CARTESIAN_POINT('Ctrl Pts',(0.154813660779084,-3.93166448111423,
15.66612887893));
#24888=CARTESIAN_POINT('Ctrl Pts',(0.270778073127861,-3.9253812904337,15.6719801956901));
#24889=CARTESIAN_POINT('Ctrl Pts',(0.386191926136979,-3.91399345888398,
15.6778315124503));
#24890=CARTESIAN_POINT('Ctrl Pts',(0.501644084853312,-3.90260184772783,
15.6836847712548));
#24891=CARTESIAN_POINT('Ctrl Pts',(0.616544909686108,-3.88610226742192,
15.6895380300593));
#24892=CARTESIAN_POINT('Ctrl Pts',(0.730414479773336,-3.86458066130563,
15.6953912888639));
#24893=CARTESIAN_POINT('Ctrl Pts',(0.844413598707175,-3.84303457016451,
15.701251206892));
#24894=CARTESIAN_POINT('Ctrl Pts',(0.957378714649444,-3.81645512597312,
15.7071111249201));
#24895=CARTESIAN_POINT('Ctrl Pts',(1.06884166453412,-3.78497906152147,15.7129710429482));
#24896=CARTESIAN_POINT('Ctrl Pts',(1.18037966561287,-3.75348180333481,15.7188349066269));
#24897=CARTESIAN_POINT('Ctrl Pts',(1.29041309510056,-3.71708148937148,15.7246987703055));
#24898=CARTESIAN_POINT('Ctrl Pts',(1.39849213082922,-3.67596365052876,15.7305626339841));
#24899=CARTESIAN_POINT('Ctrl Pts',(1.50673060912077,-3.63478515298788,15.7364351482715));
#24900=CARTESIAN_POINT('Ctrl Pts',(1.61300856122449,-3.58887540405998,15.7423076625589));
#24901=CARTESIAN_POINT('Ctrl Pts',(1.71689910560843,-3.53846668221717,15.7481801768463));
#24902=CARTESIAN_POINT('Ctrl Pts',(1.74561222476891,-3.52453479221136,15.7498032138946));
#24903=CARTESIAN_POINT('Ctrl Pts',(1.77414314549015,-3.51025950694262,15.751426250943));
#24904=CARTESIAN_POINT('Ctrl Pts',(1.80248324664458,-3.49564631299644,15.7530492879913));
#24905=CARTESIAN_POINT('Ctrl Pts',(1.90501731224751,-3.44277599405928,15.7589214119573));
#24906=CARTESIAN_POINT('Ctrl Pts',(2.00539511951483,-3.38530193005916,15.7647935359233));
#24907=CARTESIAN_POINT('Ctrl Pts',(2.10317463802229,-3.32342375299627,15.7706656598894));
#24908=CARTESIAN_POINT('Ctrl Pts',(2.20082738344259,-3.26162580221853,15.7765301705301));
#24909=CARTESIAN_POINT('Ctrl Pts',(2.29588819318185,-3.19543531256549,15.7823946811708));
#24910=CARTESIAN_POINT('Ctrl Pts',(2.38793803052643,-3.12509855242448,15.7882591918115));
#24911=CARTESIAN_POINT('Ctrl Pts',(2.47989314950407,-3.05483416810996,15.7941176679291));
#24912=CARTESIAN_POINT('Ctrl Pts',(2.56884313216152,-2.98043224901516,15.7999761440467));
#24913=CARTESIAN_POINT('Ctrl Pts',(2.6543970101716,-2.90218288748178,15.8058346201643));
#24914=CARTESIAN_POINT('Ctrl Pts',(2.74332439091927,-2.82084804997131,15.8119241037556));
#24915=CARTESIAN_POINT('Ctrl Pts',(2.82858194670939,-2.73535635161227,15.8180135873469));
#24916=CARTESIAN_POINT('Ctrl Pts',(2.90976730660895,-2.64608072843398,15.8241030709381));
#24917=CARTESIAN_POINT('Ctrl Pts',(2.98778231505551,-2.56029138778261,15.8299547554585));
#24918=CARTESIAN_POINT('Ctrl Pts',(3.06203689980441,-2.47100844159403,15.8358064399789));
#24919=CARTESIAN_POINT('Ctrl Pts',(3.13221145697249,-2.37860051055453,15.8416581244993));
#24920=CARTESIAN_POINT('Ctrl Pts',(3.20237531099515,-2.28620667373328,15.8475089165107));
#24921=CARTESIAN_POINT('Ctrl Pts',(3.26846012479541,-2.19068912889503,15.853359708522));
#24922=CARTESIAN_POINT('Ctrl Pts',(3.33018734607039,-2.09244862304255,15.8592105005333));
#24923=CARTESIAN_POINT('Ctrl Pts',(3.3919201035679,-1.99419930614543,15.8650618172934));
#24924=CARTESIAN_POINT('Ctrl Pts',(3.44929427165568,-1.89322689282006,15.8709131340535));
#24925=CARTESIAN_POINT('Ctrl Pts',(3.50207568797934,-1.78995946201696,15.8767644508137));
#24926=CARTESIAN_POINT('Ctrl Pts',(3.55487462238606,-1.6866577568886,15.8826177096182));
#24927=CARTESIAN_POINT('Ctrl Pts',(3.60307758595123,-1.58105988758726,15.8884709684227));
#24928=CARTESIAN_POINT('Ctrl Pts',(3.64649757084386,-1.47361611888233,15.8943242272272));
#24929=CARTESIAN_POINT('Ctrl Pts',(3.68996695443863,-1.36605011193295,15.9001841452554));
#24930=CARTESIAN_POINT('Ctrl Pts',(3.72864234313907,-1.25663439742065,15.9060440632835));
#24931=CARTESIAN_POINT('Ctrl Pts',(3.76238581878008,-1.1458367905782,15.9119039813116));
#24932=CARTESIAN_POINT('Ctrl Pts',(3.79615201486897,-1.03496458053606,15.9177678449902));
#24933=CARTESIAN_POINT('Ctrl Pts',(3.82497958296128,-0.922709024863492,
15.9236317086689));
#24934=CARTESIAN_POINT('Ctrl Pts',(3.84878157612253,-0.809548873941413,
15.9294955723475));
#24935=CARTESIAN_POINT('Ctrl Pts',(3.87261868294634,-0.696221784589936,
15.9353680866349));
#24936=CARTESIAN_POINT('Ctrl Pts',(3.89141535113761,-0.581987842983668,
15.9412406009223));
#24937=CARTESIAN_POINT('Ctrl Pts',(3.90513636504672,-0.467331756239275,
15.9471131152097));
#24938=CARTESIAN_POINT('Ctrl Pts',(3.90892855912671,-0.435643271972237,
15.948736152258));
#24939=CARTESIAN_POINT('Ctrl Pts',(3.91233335555995,-0.403922544238162,
15.9503591893064));
#24940=CARTESIAN_POINT('Ctrl Pts',(3.91535071258213,-0.372179791878329,
15.9519822263547));
#24941=CARTESIAN_POINT('Ctrl Pts',(3.92703457166852,-0.249264988340128,
15.9582669768915));
#24942=CARTESIAN_POINT('Ctrl Pts',(3.9329316565498,-0.125791461216173,15.9645517274283));
#24943=CARTESIAN_POINT('Ctrl Pts',(3.93299940944748,-0.00215529249517274,
15.9708364779651));
#24944=CARTESIAN_POINT('',(3.93121378987206,-0.00244485579717362,17.2208359355727));
#24945=CARTESIAN_POINT('Ctrl Pts',(3.93806424214966,-0.00212304094380579,
15.9708382561933));
#24946=CARTESIAN_POINT('Ctrl Pts',(3.93025982083623,1.18025118297352,16.0308638923682));
#24947=CARTESIAN_POINT('Ctrl Pts',(2.73404304350042,3.68246309584126,16.1572005079975));
#24948=CARTESIAN_POINT('Ctrl Pts',(-1.52657745030475,4.39475809013145,16.3498481030817));
#24949=CARTESIAN_POINT('Ctrl Pts',(-4.52281588537782,1.09017147712084,16.5487810414449));
#24950=CARTESIAN_POINT('Ctrl Pts',(-3.36120918071239,-3.21661471520144,
16.7477139798085));
#24951=CARTESIAN_POINT('Ctrl Pts',(0.890372355971627,-4.56635242291656,
16.9466469181718));
#24952=CARTESIAN_POINT('Ctrl Pts',(3.61197945872188,-2.30845509392336,17.1043539150494));
#24953=CARTESIAN_POINT('Ctrl Pts',(3.93082923382665,-0.499818402315335,
17.1957499324723));
#24954=CARTESIAN_POINT('Ctrl Pts',(3.92803675183412,-0.00246202408810856,
17.2208349704406));
#24955=CARTESIAN_POINT('',(3.93299884326148,0.00301643894015496,18.4708364780099));
#24956=CARTESIAN_POINT('Ctrl Pts',(3.93299924609258,-0.00243520742926632,
17.220836477965));
#24957=CARTESIAN_POINT('Ctrl Pts',(3.93307175716978,0.114674328524147,17.2267356713988));
#24958=CARTESIAN_POINT('Ctrl Pts',(3.92790932706125,0.231802111248879,17.2326348648325));
#24959=CARTESIAN_POINT('Ctrl Pts',(3.9175336699977,0.348452212554841,17.2385340582663));
#24960=CARTESIAN_POINT('Ctrl Pts',(3.90715675423114,0.465116465044868,17.2444339673494));
#24961=CARTESIAN_POINT('Ctrl Pts',(3.8915653883706,0.581302518492728,17.2503338764325));
#24962=CARTESIAN_POINT('Ctrl Pts',(3.87083318026104,0.696519555066647,17.2562337855156));
#24963=CARTESIAN_POINT('Ctrl Pts',(3.85009374789081,0.811776739699109,17.262135750457));
#24964=CARTESIAN_POINT('Ctrl Pts',(3.82420997992269,0.92606383820719,17.2680377153984));
#24965=CARTESIAN_POINT('Ctrl Pts',(3.79330649308746,1.03890078905566,17.2739396803398));
#24966=CARTESIAN_POINT('Ctrl Pts',(3.76236280702124,1.15188451811969,17.2798493225524));
#24967=CARTESIAN_POINT('Ctrl Pts',(3.72638646557085,1.26341394123064,17.2857589647651));
#24968=CARTESIAN_POINT('Ctrl Pts',(3.68555197737842,1.37302426127219,17.2916686069777));
#24969=CARTESIAN_POINT('Ctrl Pts',(3.64469073810305,1.48270638813419,17.2975821206563));
#24970=CARTESIAN_POINT('Ctrl Pts',(3.59896516826528,1.59046653530643,17.3034956343349));
#24971=CARTESIAN_POINT('Ctrl Pts',(3.54859718350607,1.69586173646697,17.3094091480134));
#24972=CARTESIAN_POINT('Ctrl Pts',(3.49813571336707,1.80145255614304,17.3153336374551));
#24973=CARTESIAN_POINT('Ctrl Pts',(3.44301479848032,1.9046693008178,17.3212581268969));
#24974=CARTESIAN_POINT('Ctrl Pts',(3.38350180090035,2.00509465195638,17.3271826163386));
#24975=CARTESIAN_POINT('Ctrl Pts',(3.32547312265687,2.10301528485475,17.3329593425253));
#24976=CARTESIAN_POINT('Ctrl Pts',(3.26326912317872,2.1982818815763,17.3387360687121));
#24977=CARTESIAN_POINT('Ctrl Pts',(3.19717471782663,2.29053767130999,17.3445127948988));
#24978=CARTESIAN_POINT('Ctrl Pts',(3.12998881890351,2.38431698789665,17.3503849188648));
#24979=CARTESIAN_POINT('Ctrl Pts',(3.05856069220649,2.47529497941671,17.3562570428309));
#24980=CARTESIAN_POINT('Ctrl Pts',(2.98315198438186,2.56306325284386,17.3621291667969));
#24981=CARTESIAN_POINT('Ctrl Pts',(2.90784104544422,2.65071773296182,17.3679936774376));
#24982=CARTESIAN_POINT('Ctrl Pts',(2.82856005546469,2.73517045995525,17.3738581880783));
#24983=CARTESIAN_POINT('Ctrl Pts',(2.74561346835019,2.81604255692524,17.379722698719));
#24984=CARTESIAN_POINT('Ctrl Pts',(2.66275223244848,2.89683143731215,17.3855811748366));
#24985=CARTESIAN_POINT('Ctrl Pts',(2.57623319604919,2.97404672932306,17.3914396509542));
#24986=CARTESIAN_POINT('Ctrl Pts',(2.48640010144279,3.04734368516997,17.3972981270718));
#24987=CARTESIAN_POINT('Ctrl Pts',(2.39302476892017,3.1235308370775,17.4033876106631));
#24988=CARTESIAN_POINT('Ctrl Pts',(2.29606894246767,3.19548394003025,17.4094770942544));
#24989=CARTESIAN_POINT('Ctrl Pts',(2.19595998586665,3.26285898262131,17.4155665778456));
#24990=CARTESIAN_POINT('Ctrl Pts',(2.09976036188927,3.32760297739243,17.421418262366));
#24991=CARTESIAN_POINT('Ctrl Pts',(2.00064962611799,3.388119503162,17.4272699468864));
#24992=CARTESIAN_POINT('Ctrl Pts',(1.89903886540253,3.44414581394149,17.4331216314068));
#24993=CARTESIAN_POINT('Ctrl Pts',(1.79744360253691,3.50016357949068,17.4389724234182));
#24994=CARTESIAN_POINT('Ctrl Pts',(1.69334943481464,3.55169229219669,17.4448232154295));
#24995=CARTESIAN_POINT('Ctrl Pts',(1.58719328007323,3.59851448401842,17.4506740074408));
#24996=CARTESIAN_POINT('Ctrl Pts',(1.48102760434448,3.64534087525277,17.4565253242009));
#24997=CARTESIAN_POINT('Ctrl Pts',(1.37279995223586,3.68745973961954,17.462376640961));
#24998=CARTESIAN_POINT('Ctrl Pts',(1.26296784461751,3.72470149454452,17.4682279577211));
#24999=CARTESIAN_POINT('Ctrl Pts',(1.15309928386611,3.76195560995932,17.4740812165257));
#25000=CARTESIAN_POINT('Ctrl Pts',(1.04162560004094,3.79432926455533,17.4799344753302));
#25001=CARTESIAN_POINT('Ctrl Pts',(0.929019424292374,3.82170274999083,17.4857877341347));
#25002=CARTESIAN_POINT('Ctrl Pts',(0.816285137054489,3.84910737810535,17.4916476521628));
#25003=CARTESIAN_POINT('Ctrl Pts',(0.702416188173637,3.87150038491822,17.4975075701909));
#25004=CARTESIAN_POINT('Ctrl Pts',(0.587895452026045,3.88881317852723,17.503367488219));
#25005=CARTESIAN_POINT('Ctrl Pts',(0.473297605789349,3.90613762933565,17.5092313518977));
#25006=CARTESIAN_POINT('Ctrl Pts',(0.358047508514276,3.91837501220619,17.5150952155763));
#25007=CARTESIAN_POINT('Ctrl Pts',(0.242631459507403,3.92550875363402,17.5209590792549));
#25008=CARTESIAN_POINT('Ctrl Pts',(0.127045144079103,3.9326530190456,17.5268315935423));
#25009=CARTESIAN_POINT('Ctrl Pts',(0.0112928001081183,3.93467860912628,
17.5327041078297));
#25010=CARTESIAN_POINT('Ctrl Pts',(-0.104140884177499,3.93162099855044,
17.5385766221171));
#25011=CARTESIAN_POINT('Ctrl Pts',(-0.136044279734563,3.9307759405393,17.5401996591654));
#25012=CARTESIAN_POINT('Ctrl Pts',(-0.167923376826395,3.92954290551535,
17.5418226962138));
#25013=CARTESIAN_POINT('Ctrl Pts',(-0.19976805865803,3.92792333463116,17.5434457332622));
#25014=CARTESIAN_POINT('Ctrl Pts',(-0.314981645163972,3.92206375119571,
17.5493178572282));
#25015=CARTESIAN_POINT('Ctrl Pts',(-0.430130357789709,3.91112089027479,
17.5551899811943));
#25016=CARTESIAN_POINT('Ctrl Pts',(-0.544729177393933,3.8950942380507,17.5610621051603));
#25017=CARTESIAN_POINT('Ctrl Pts',(-0.659179417353221,3.87908836469941,
17.566926615801));
#25018=CARTESIAN_POINT('Ctrl Pts',(-0.773080776440481,3.85801186435196,
17.5727911264417));
#25019=CARTESIAN_POINT('Ctrl Pts',(-0.885949940811867,3.83191619198221,
17.5786556370825));
#25020=CARTESIAN_POINT('Ctrl Pts',(-0.998702963935857,3.80584737179975,
17.5845141132001));
#25021=CARTESIAN_POINT('Ctrl Pts',(-1.11042550458523,3.77476974494996,17.5903725893177));
#25022=CARTESIAN_POINT('Ctrl Pts',(-1.22064173718814,3.73878626688319,17.5962310654353));
#25023=CARTESIAN_POINT('Ctrl Pts',(-1.33520394183874,3.70138391261131,17.6023205490266));
#25024=CARTESIAN_POINT('Ctrl Pts',(-1.4481381524386,3.65868092227344,17.6084100326178));
#25025=CARTESIAN_POINT('Ctrl Pts',(-1.55892397835458,3.61085101184072,17.6144995162091));
#25026=CARTESIAN_POINT('Ctrl Pts',(-1.66538353159525,3.56488889661426,17.6203512007295));
#25027=CARTESIAN_POINT('Ctrl Pts',(-1.76985892831254,3.51419294690333,17.6262028852499));
#25028=CARTESIAN_POINT('Ctrl Pts',(-1.87190695319748,3.4589670941729,17.6320545697703));
#25029=CARTESIAN_POINT('Ctrl Pts',(-1.97393941354044,3.40374966458544,17.6379053617816));
#25030=CARTESIAN_POINT('Ctrl Pts',(-2.07354487469328,3.3440039024304,17.6437561537929));
#25031=CARTESIAN_POINT('Ctrl Pts',(-2.17030426238952,3.27997994028224,17.6496069458043));
#25032=CARTESIAN_POINT('Ctrl Pts',(-2.26707232829107,3.21595023592031,17.6554582625644));
#25033=CARTESIAN_POINT('Ctrl Pts',(-2.36099346851071,3.14764179693681,17.6613095793245));
#25034=CARTESIAN_POINT('Ctrl Pts',(-2.45167776881409,3.07534796696289,17.6671608960847));
#25035=CARTESIAN_POINT('Ctrl Pts',(-2.54239216711838,3.00303014276115,17.6730141548892));
#25036=CARTESIAN_POINT('Ctrl Pts',(-2.62986726623438,2.92672455494373,17.6788674136937));
#25037=CARTESIAN_POINT('Ctrl Pts',(-2.71374695338671,2.84676421099191,17.6847206724983));
#25038=CARTESIAN_POINT('Ctrl Pts',(-2.79772207004415,2.76671289655234,17.6905805905264));
#25039=CARTESIAN_POINT('Ctrl Pts',(-2.87809331083056,2.68299881214709,17.6964405085545));
#25040=CARTESIAN_POINT('Ctrl Pts',(-2.95454203957627,2.59599120498827,17.7023004265826));
#25041=CARTESIAN_POINT('Ctrl Pts',(-3.03104224343892,2.5089250131175,17.7081642902613));
#25042=CARTESIAN_POINT('Ctrl Pts',(-3.10361441799898,2.41856120431631,17.7140281539399));
#25043=CARTESIAN_POINT('Ctrl Pts',(-3.1719818468881,2.32530001569956,17.7198920176185));
#25044=CARTESIAN_POINT('Ctrl Pts',(-3.24045013417226,2.23190124440701,17.7257645319059));
#25045=CARTESIAN_POINT('Ctrl Pts',(-3.30470106714789,2.13559690513959,17.7316370461933));
#25046=CARTESIAN_POINT('Ctrl Pts',(-3.36450259550358,2.03681400349902,17.7375095604807));
#25047=CARTESIAN_POINT('Ctrl Pts',(-3.38103045585743,2.00951252729004,17.739132597529));
#25048=CARTESIAN_POINT('Ctrl Pts',(-3.39721872650924,1.98202185432595,17.7407556345774));
#25049=CARTESIAN_POINT('Ctrl Pts',(-3.41306315351781,1.95435127602462,17.7423786716257));
#25050=CARTESIAN_POINT('Ctrl Pts',(-3.47038805541138,1.8542395341734,17.7482507955917));
#25051=CARTESIAN_POINT('Ctrl Pts',(-3.5234006206227,1.75143564244643,17.7541229195577));
#25052=CARTESIAN_POINT('Ctrl Pts',(-3.57183833781004,1.64634743858955,17.7599950435238));
#25053=CARTESIAN_POINT('Ctrl Pts',(-3.62021325453528,1.54139548367559,17.7658595541645));
#25054=CARTESIAN_POINT('Ctrl Pts',(-3.66402494714761,1.43416547827029,17.7717240648052));
#25055=CARTESIAN_POINT('Ctrl Pts',(-3.70305555447318,1.32509190642964,17.7775885754459));
#25056=CARTESIAN_POINT('Ctrl Pts',(-3.74204599969215,1.21613057020918,17.7834470515635));
#25057=CARTESIAN_POINT('Ctrl Pts',(-3.77626500667312,1.10532982769805,17.7893055276811));
#25058=CARTESIAN_POINT('Ctrl Pts',(-3.8055420951674,0.993145690172851,17.7951640037988));
#25059=CARTESIAN_POINT('Ctrl Pts',(-3.83597361804242,0.876537983502165,
17.80125348739));
#25060=CARTESIAN_POINT('Ctrl Pts',(-3.86106528119461,0.758435952410947,
17.8073429709813));
#25061=CARTESIAN_POINT('Ctrl Pts',(-3.88068206460635,0.639371342368892,
17.8134324545725));
#25062=CARTESIAN_POINT('Ctrl Pts',(-3.89953279736724,0.524956297961615,
17.819284139093));
#25063=CARTESIAN_POINT('Ctrl Pts',(-3.9133281493711,0.409652889081125,17.8251358236134));
#25064=CARTESIAN_POINT('Ctrl Pts',(-3.92200022669181,0.29394424952595,17.8309875081338));
#25065=CARTESIAN_POINT('Ctrl Pts',(-3.93067098133221,0.178253258053734,
17.8368383001451));
#25066=CARTESIAN_POINT('Ctrl Pts',(-3.93421998408977,0.0621575709402135,
17.8426890921564));
#25067=CARTESIAN_POINT('Ctrl Pts',(-3.93263126114136,-0.0538550266337851,
17.8485398841677));
#25068=CARTESIAN_POINT('Ctrl Pts',(-3.93104239570276,-0.169878029204725,
17.8543912009278));
#25069=CARTESIAN_POINT('Ctrl Pts',(-3.92431489420144,-0.285817514023418,
17.8602425176879));
#25070=CARTESIAN_POINT('Ctrl Pts',(-3.91248489896147,-0.401186883382818,
17.8660938344481));
#25071=CARTESIAN_POINT('Ctrl Pts',(-3.90065097736151,-0.516594543685525,
17.8719470932526));
#25072=CARTESIAN_POINT('Ctrl Pts',(-3.8837112367347,-0.631431301237319,
17.8778003520571));
#25073=CARTESIAN_POINT('Ctrl Pts',(-3.8617534587689,-0.745217568020551,
17.8836536108616));
#25074=CARTESIAN_POINT('Ctrl Pts',(-3.8397706995477,-0.859133288876737,
17.8895135288898));
#25075=CARTESIAN_POINT('Ctrl Pts',(-3.8127585863616,-0.971995727334371,
17.8953734469179));
#25076=CARTESIAN_POINT('Ctrl Pts',(-3.78085564492224,-1.08333724770249,
17.901233364946));
#25077=CARTESIAN_POINT('Ctrl Pts',(-3.7489312223195,-1.19475373750237,17.9070972286246));
#25078=CARTESIAN_POINT('Ctrl Pts',(-3.71210954521198,-1.30464687903708,
17.9129610923032));
#25079=CARTESIAN_POINT('Ctrl Pts',(-3.67057786678098,-1.41256756436554,
17.9188249559819));
#25080=CARTESIAN_POINT('Ctrl Pts',(-3.62898491913876,-1.52064745865242,
17.9246974702693));
#25081=CARTESIAN_POINT('Ctrl Pts',(-3.58266826726465,-1.62674871175149,
17.9305699845567));
#25082=CARTESIAN_POINT('Ctrl Pts',(-3.53186182366675,-1.73044533531846,
17.9364424988441));
#25083=CARTESIAN_POINT('Ctrl Pts',(-3.51782001189447,-1.75910485892281,
17.9380655358924));
#25084=CARTESIAN_POINT('Ctrl Pts',(-3.50343550553537,-1.78758086959021,
17.9396885729407));
#25085=CARTESIAN_POINT('Ctrl Pts',(-3.48871382416943,-1.81586476728007,
17.9413116099891));
#25086=CARTESIAN_POINT('Ctrl Pts',(-3.43545099935727,-1.91819548958095,
17.9471837339551));
#25087=CARTESIAN_POINT('Ctrl Pts',(-3.37759272571528,-2.0183523285669,17.9530558579211));
#25088=CARTESIAN_POINT('Ctrl Pts',(-3.3153403275674,-2.11589402201653,17.9589279818872));
#25089=CARTESIAN_POINT('Ctrl Pts',(-3.25316864088984,-2.21330925072377,
17.9647924925279));
#25090=CARTESIAN_POINT('Ctrl Pts',(-3.18661437946492,-2.30811573127728,
17.9706570031686));
#25091=CARTESIAN_POINT('Ctrl Pts',(-3.11592541555321,-2.39989537370061,
17.9765215138093));
#25092=CARTESIAN_POINT('Ctrl Pts',(-3.04530918988194,-2.49158057578517,
17.9823799899269));
#25093=CARTESIAN_POINT('Ctrl Pts',(-2.97056697500449,-2.58024480924499,
17.9882384660445));
#25094=CARTESIAN_POINT('Ctrl Pts',(-2.8919903592605,-2.6654982202103,17.9940969421621));
#25095=CARTESIAN_POINT('Ctrl Pts',(-2.81031536347259,-2.75411328609943,
18.0001864257534));
#25096=CARTESIAN_POINT('Ctrl Pts',(-2.72449759953192,-2.83904262555192,
18.0062759093447));
#25097=CARTESIAN_POINT('Ctrl Pts',(-2.63491154255046,-2.91988529961955,
18.0123653929359));
#25098=CARTESIAN_POINT('Ctrl Pts',(-2.54882389077738,-2.99757100438251,
18.0182170774563));
#25099=CARTESIAN_POINT('Ctrl Pts',(-2.45925706845335,-3.07148292612135,
18.0240687619767));
#25100=CARTESIAN_POINT('Ctrl Pts',(-2.36658091822905,-3.14130287579439,
18.0299204464971));
#25101=CARTESIAN_POINT('Ctrl Pts',(-2.27391890313226,-3.21111217640736,
18.0357712385085));
#25102=CARTESIAN_POINT('Ctrl Pts',(-2.17814883317635,-3.27683049719832,
18.0416220305198));
#25103=CARTESIAN_POINT('Ctrl Pts',(-2.07967251978953,-3.33818082350736,
18.0474728225311));
#25104=CARTESIAN_POINT('Ctrl Pts',(-1.98118737420892,-3.39953665223574,
18.0533241392912));
#25105=CARTESIAN_POINT('Ctrl Pts',(-1.8799958536043,-3.45652348908617,18.0591754560513));
#25106=CARTESIAN_POINT('Ctrl Pts',(-1.77652693105584,-3.50890881375297,
18.0650267728115));
#25107=CARTESIAN_POINT('Ctrl Pts',(-1.67302366730741,-3.56131152504048,
18.070880031616));
#25108=CARTESIAN_POINT('Ctrl Pts',(-1.56724186726331,-3.60910950069661,
18.0767332904205));
#25109=CARTESIAN_POINT('Ctrl Pts',(-1.45963250897119,-3.65211745960538,
18.082586549225));
#25110=CARTESIAN_POINT('Ctrl Pts',(-1.351900724044,-3.69517434845643,18.0884464672531));
#25111=CARTESIAN_POINT('Ctrl Pts',(-1.24233761494981,-3.73343018982693,
18.0943063852812));
#25112=CARTESIAN_POINT('Ctrl Pts',(-1.13141152196709,-3.76674885915694,
18.1001663033093));
#25113=CARTESIAN_POINT('Ctrl Pts',(-1.02041073927112,-3.80008996290063,
18.106030166988));
#25114=CARTESIAN_POINT('Ctrl Pts',(-0.90804554512757,-3.82848717414714,
18.1118940306666));
#25115=CARTESIAN_POINT('Ctrl Pts',(-0.79479501956925,-3.85185538109466,
18.1177578943453));
#25116=CARTESIAN_POINT('Ctrl Pts',(-0.681377422257287,-3.87525806176577,
18.1236304086327));
#25117=CARTESIAN_POINT('Ctrl Pts',(-0.567072293497158,-3.89361686589707,
18.1295029229201));
#25118=CARTESIAN_POINT('Ctrl Pts',(-0.452364471787731,-3.90689843541705,
18.1353754372075));
#25119=CARTESIAN_POINT('Ctrl Pts',(-0.420661689085492,-3.91056917648912,
18.1369984742558));
#25120=CARTESIAN_POINT('Ctrl Pts',(-0.388928147598308,-3.91385239920676,
18.1386215113041));
#25121=CARTESIAN_POINT('Ctrl Pts',(-0.35717406625248,-3.91674810096292,
18.1402445483525));
#25122=CARTESIAN_POINT('Ctrl Pts',(-0.242288270958812,-3.92722470696411,
18.1461166723185));
#25123=CARTESIAN_POINT('Ctrl Pts',(-0.126748531622461,-3.93265985724264,
18.1519887962845));
#25124=CARTESIAN_POINT('Ctrl Pts',(-0.0110349298696812,-3.93298451946137,
18.1578609202506));
#25125=CARTESIAN_POINT('Ctrl Pts',(0.104528646901102,-3.93330876074908,
18.1637254308913));
#25126=CARTESIAN_POINT('Ctrl Pts',(0.220265228227679,-3.92853568923793,
18.169589941532));
#25127=CARTESIAN_POINT('Ctrl Pts',(0.335689078507512,-3.918647961041,18.1754544521727));
#25128=CARTESIAN_POINT('Ctrl Pts',(0.450994158793534,-3.90877040721803,
18.1813129282904));
#25129=CARTESIAN_POINT('Ctrl Pts',(0.565986738678701,-3.89378870000194,
18.187171404408));
#25130=CARTESIAN_POINT('Ctrl Pts',(0.680181219717037,-3.87373753735901,
18.1930298805256));
#25131=CARTESIAN_POINT('Ctrl Pts',(0.798878540408689,-3.8528957308126,18.1991193641168));
#25132=CARTESIAN_POINT('Ctrl Pts',(0.916713072146176,-3.82657645198841,
18.2052088477081));
#25133=CARTESIAN_POINT('Ctrl Pts',(1.03314510135539,-3.79487815345175,18.2112983312994));
#25134=CARTESIAN_POINT('Ctrl Pts',(1.14503036925909,-3.76441769812899,18.2171500158198));
#25135=CARTESIAN_POINT('Ctrl Pts',(1.2556201802534,-3.72899056812071,18.2230017003402));
#25136=CARTESIAN_POINT('Ctrl Pts',(1.36444695313568,-3.68873603177006,18.2288533848606));
#25137=CARTESIAN_POINT('Ctrl Pts',(1.47325712756938,-3.64848763511128,18.2347041768719));
#25138=CARTESIAN_POINT('Ctrl Pts',(1.58030441092155,-3.60341343945687,18.2405549688833));
#25139=CARTESIAN_POINT('Ctrl Pts',(1.68513859357947,-3.55370186150006,18.2464057608946));
#25140=CARTESIAN_POINT('Ctrl Pts',(1.78998217865871,-3.50398582498605,18.2522570776547));
#25141=CARTESIAN_POINT('Ctrl Pts',(1.89261189489906,-3.44963175650102,18.2581083944148));
#25142=CARTESIAN_POINT('Ctrl Pts',(1.99260029536081,-3.3908749701114,18.2639597111749));
#25143=CARTESIAN_POINT('Ctrl Pts',(2.09262188184213,-3.33209868242109,18.2698129699795));
#25144=CARTESIAN_POINT('Ctrl Pts',(2.19000005314559,-3.26891698055241,18.275666228784));
#25145=CARTESIAN_POINT('Ctrl Pts',(2.28433522102667,-3.2016092200606,18.2815194875885));
#25146=CARTESIAN_POINT('Ctrl Pts',(2.37877771356199,-3.13422488386235,18.2873794056166));
#25147=CARTESIAN_POINT('Ctrl Pts',(2.47016995586057,-3.06270535980759,18.2932393236447));
#25148=CARTESIAN_POINT('Ctrl Pts',(2.55814434041753,-2.98737117439226,18.2990992416729));
#25149=CARTESIAN_POINT('Ctrl Pts',(2.64617796064519,-2.91198626431403,18.3049631053515));
#25150=CARTESIAN_POINT('Ctrl Pts',(2.73078883963628,-2.83278186028382,18.3108269690301));
#25151=CARTESIAN_POINT('Ctrl Pts',(2.8116464909517,-2.75011509030422,18.3166908327087));
#25152=CARTESIAN_POINT('Ctrl Pts',(2.89262342674343,-2.66732636696332,18.3225633469961));
#25153=CARTESIAN_POINT('Ctrl Pts',(2.96983580951722,-2.58106539029127,18.3284358612835));
#25154=CARTESIAN_POINT('Ctrl Pts',(3.04299358901262,-2.49172209871569,18.3343083755709));
#25155=CARTESIAN_POINT('Ctrl Pts',(3.06321283083729,-2.46702952835285,18.3359314126193));
#25156=CARTESIAN_POINT('Ctrl Pts',(3.08312261895461,-2.44210168159748,18.3375544496676));
#25157=CARTESIAN_POINT('Ctrl Pts',(3.10271742939726,-2.41694715567272,18.339177486716));
#25158=CARTESIAN_POINT('Ctrl Pts',(3.17362919680151,-2.32591530329725,18.345051104427));
#25159=CARTESIAN_POINT('Ctrl Pts',(3.2406541608105,-2.23160238625361,18.3509247221381));
#25160=CARTESIAN_POINT('Ctrl Pts',(3.30347337664496,-2.13437406510619,18.3567983398492));
#25161=CARTESIAN_POINT('Ctrl Pts',(3.36621262879894,-2.03726950759229,18.3626644809293));
#25162=CARTESIAN_POINT('Ctrl Pts',(3.42475655384322,-1.93725726609145,18.3685306220095));
#25163=CARTESIAN_POINT('Ctrl Pts',(3.47882638485046,-1.83473594396259,18.3743967630897));
#25164=CARTESIAN_POINT('Ctrl Pts',(3.53284042763407,-1.73232040138471,18.380256851597));
#25165=CARTESIAN_POINT('Ctrl Pts',(3.58238936433424,-1.62740128815385,18.3861169401043));
#25166=CARTESIAN_POINT('Ctrl Pts',(3.62723809044619,-1.52040548381552,18.3919770286117));
#25167=CARTESIAN_POINT('Ctrl Pts',(3.67205135476632,-1.41349428083085,18.3978324835595));
#25168=CARTESIAN_POINT('Ctrl Pts',(3.71217164172726,-1.30451003165297,18.4036879385074));
#25169=CARTESIAN_POINT('Ctrl Pts',(3.74741043586753,-1.1939028541515,18.4095433934553));
#25170=CARTESIAN_POINT('Ctrl Pts',(3.78263174744206,-1.08335055075398,18.4153959434123));
#25171=CARTESIAN_POINT('Ctrl Pts',(3.81297625756179,-0.97117731256335,18.4212484933693));
#25172=CARTESIAN_POINT('Ctrl Pts',(3.83830434792709,-0.857851229925077,
18.4271010433263));
#25173=CARTESIAN_POINT('Ctrl Pts',(3.86362502022341,-0.744558338130938,
18.4329518791935));
#25174=CARTESIAN_POINT('Ctrl Pts',(3.88393210851618,-0.630113676515642,
18.4388027150608));
#25175=CARTESIAN_POINT('Ctrl Pts',(3.89913662050626,-0.514997684098689,
18.4446535509281));
#25176=CARTESIAN_POINT('Ctrl Pts',(3.91434347859188,-0.399863928986253,
18.4505052895945));
#25177=CARTESIAN_POINT('Ctrl Pts',(3.92444613159445,-0.284059044919621,
18.4563570282608));
#25178=CARTESIAN_POINT('Ctrl Pts',(3.92940725097593,-0.168070389949481,
18.4622087669272));
#25179=CARTESIAN_POINT('Ctrl Pts',(3.93184544965431,-0.111066443156551,
18.4650846706065));
#25180=CARTESIAN_POINT('Ctrl Pts',(3.93304258631382,-0.0540181731665422,
18.4679605742858));
#25181=CARTESIAN_POINT('Ctrl Pts',(3.93299884326216,0.00301643805224686,
18.4708364779651));
#25182=CARTESIAN_POINT('',(3.9344286541877,0.00130879145752274,19.720836477965));
#25183=CARTESIAN_POINT('Ctrl Pts',(3.93299884326148,0.00301643894014107,
18.4708364780099));
#25184=CARTESIAN_POINT('Ctrl Pts',(3.93289556899613,0.137671101008563,18.4776262821271));
#25185=CARTESIAN_POINT('Ctrl Pts',(3.92587308724252,0.272039635390568,18.4844160862444));
#25186=CARTESIAN_POINT('Ctrl Pts',(3.91204290149561,0.405474212321595,18.4912058903616));
#25187=CARTESIAN_POINT('Ctrl Pts',(3.89813028468773,0.539704089760308,18.4980361632598));
#25188=CARTESIAN_POINT('Ctrl Pts',(3.87732868566575,0.672988727294203,18.504866436158));
#25189=CARTESIAN_POINT('Ctrl Pts',(3.84980074140044,0.804688294628814,18.5116967090562));
#25190=CARTESIAN_POINT('Ctrl Pts',(3.8220865626637,0.93727884746791,18.5185731907177));
#25191=CARTESIAN_POINT('Ctrl Pts',(3.78755480536809,1.06826269831912,18.5254496723793));
#25192=CARTESIAN_POINT('Ctrl Pts',(3.74641956867559,1.19700852772427,18.5323261540408));
#25193=CARTESIAN_POINT('Ctrl Pts',(3.73488569762663,1.23310745200056,18.534254244387));
#25194=CARTESIAN_POINT('Ctrl Pts',(3.72283295874,1.26903056256492,18.5361823347332));
#25195=CARTESIAN_POINT('Ctrl Pts',(3.71026673143481,1.30476426284905,18.5381104250794));
#25196=CARTESIAN_POINT('Ctrl Pts',(3.67199547269048,1.41359356031859,18.5439825490454));
#25197=CARTESIAN_POINT('Ctrl Pts',(3.62886773218841,1.52092002594415,18.5498546730115));
#25198=CARTESIAN_POINT('Ctrl Pts',(3.58102047321423,1.62627838035822,18.5557267969775));
#25199=CARTESIAN_POINT('Ctrl Pts',(3.53323524916138,1.73150013557375,18.5615913076182));
#25200=CARTESIAN_POINT('Ctrl Pts',(3.48074284437102,1.83475848103836,18.5674558182589));
#25201=CARTESIAN_POINT('Ctrl Pts',(3.42372957695507,1.93560450089449,18.5733203288996));
#25202=CARTESIAN_POINT('Ctrl Pts',(3.36677497562405,2.03634675119955,18.5791788050172));
#25203=CARTESIAN_POINT('Ctrl Pts',(3.30530896679639,2.13468125551295,18.5850372811348));
#25204=CARTESIAN_POINT('Ctrl Pts',(3.23956513538153,2.23018087464233,18.5908957572524));
#25205=CARTESIAN_POINT('Ctrl Pts',(3.17122893760747,2.32944617025604,18.5969852408437));
#25206=CARTESIAN_POINT('Ctrl Pts',(3.09827080447404,2.42564800037014,18.603074724435));
#25207=CARTESIAN_POINT('Ctrl Pts',(3.02100481017409,2.51833654162921,18.6091642080262));
#25208=CARTESIAN_POINT('Ctrl Pts',(2.94675611305191,2.60740552325554,18.6150158925466));
#25209=CARTESIAN_POINT('Ctrl Pts',(2.86852998137564,2.69323011273485,18.620867577067));
#25210=CARTESIAN_POINT('Ctrl Pts',(2.78664759427774,2.77544306108161,18.6267192615874));
#25211=CARTESIAN_POINT('Ctrl Pts',(2.70477769602373,2.85764347016671,18.6325700535987));
#25212=CARTESIAN_POINT('Ctrl Pts',(2.61925294280469,2.93623304055476,18.63842084561));
#25213=CARTESIAN_POINT('Ctrl Pts',(2.53043197900288,3.01088076808757,18.6442716376214));
#25214=CARTESIAN_POINT('Ctrl Pts',(2.4416030489812,3.0855351906638,18.6501229543815));
#25215=CARTESIAN_POINT('Ctrl Pts',(2.3494776371911,3.15624680158455,18.6559742711416));
#25216=CARTESIAN_POINT('Ctrl Pts',(2.25444756340317,3.22272480734324,18.6618255879018));
#25217=CARTESIAN_POINT('Ctrl Pts',(2.15938594925779,3.28922487706526,18.6676788467063));
#25218=CARTESIAN_POINT('Ctrl Pts',(2.06141809473088,3.35148831077146,18.6735321055108));
#25219=CARTESIAN_POINT('Ctrl Pts',(1.96096427781162,3.40926797144882,18.6793853643153));
#25220=CARTESIAN_POINT('Ctrl Pts',(1.86039617508168,3.46711336776036,18.6852452823434));
#25221=CARTESIAN_POINT('Ctrl Pts',(1.75733682338817,3.52046460300261,18.6911052003716));
#25222=CARTESIAN_POINT('Ctrl Pts',(1.65223063365683,3.56912075071802,18.6969651183997));
#25223=CARTESIAN_POINT('Ctrl Pts',(1.54705367291993,3.61780966001016,18.7028289820783));
#25224=CARTESIAN_POINT('Ctrl Pts',(1.43982751143665,3.66179703041352,18.7086928457569));
#25225=CARTESIAN_POINT('Ctrl Pts',(1.33101439926356,3.70093091923547,18.7145567094356));
#25226=CARTESIAN_POINT('Ctrl Pts',(1.22204076158831,3.7401225399523,18.720429223723));
#25227=CARTESIAN_POINT('Ctrl Pts',(1.11147589410163,3.77444626684249,18.7263017380104));
#25228=CARTESIAN_POINT('Ctrl Pts',(0.999795059351643,3.80380057827642,18.7321742522977));
#25229=CARTESIAN_POINT('Ctrl Pts',(0.968928870949349,3.81191348063042,18.7337972893461));
#25230=CARTESIAN_POINT('Ctrl Pts',(0.937977483556097,3.81964709719531,18.7354203263944));
#25231=CARTESIAN_POINT('Ctrl Pts',(0.906951013230218,3.82699998165674,18.7370433634428));
#25232=CARTESIAN_POINT('Ctrl Pts',(0.794697703814234,3.8536026085711,18.7429154874088));
#25233=CARTESIAN_POINT('Ctrl Pts',(0.681084751037489,3.87530673688424,18.7487876113749));
#25234=CARTESIAN_POINT('Ctrl Pts',(0.566577668216009,3.89197620057971,18.7546597353409));
#25235=CARTESIAN_POINT('Ctrl Pts',(0.452219046101044,3.90862405198452,18.7605242459816));
#25236=CARTESIAN_POINT('Ctrl Pts',(0.336969004602777,3.92025016068099,18.7663887566223));
#25237=CARTESIAN_POINT('Ctrl Pts',(0.221305956864285,3.92676873185274,18.772253267263));
#25238=CARTESIAN_POINT('Ctrl Pts',(0.105761925251269,3.93328059547961,18.7781117433806));
#25239=CARTESIAN_POINT('Ctrl Pts',(-0.0101938570255434,3.9346953521082,
18.7839702194983));
#25240=CARTESIAN_POINT('Ctrl Pts',(-0.12607576011278,3.93097874615368,18.7898286956159));
#25241=CARTESIAN_POINT('Ctrl Pts',(-0.246527040139969,3.92711558950323,
18.7959181792071));
#25242=CARTESIAN_POINT('Ctrl Pts',(-0.366898044498936,3.91770800653887,
18.8020076627984));
#25243=CARTESIAN_POINT('Ctrl Pts',(-0.486640563731101,3.90277721138825,
18.8080971463897));
#25244=CARTESIAN_POINT('Ctrl Pts',(-0.601707044447126,3.88842947540199,
18.8139488309101));
#25245=CARTESIAN_POINT('Ctrl Pts',(-0.716192755698779,3.86898185972451,
18.8198005154305));
#25246=CARTESIAN_POINT('Ctrl Pts',(-0.829615130417031,3.84450617575042,
18.8256521999509));
#25247=CARTESIAN_POINT('Ctrl Pts',(-0.943020205757641,3.82003422485018,
18.8315029919622));
#25248=CARTESIAN_POINT('Ctrl Pts',(-1.05536186303409,3.79053581765028,18.8373537839735));
#25249=CARTESIAN_POINT('Ctrl Pts',(-1.16616778882778,3.75613387518344,18.8432045759848));
#25250=CARTESIAN_POINT('Ctrl Pts',(-1.27698365263991,3.72172884725761,18.849055892745));
#25251=CARTESIAN_POINT('Ctrl Pts',(-1.3862631163148,3.68241953238886,18.8549072095051));
#25252=CARTESIAN_POINT('Ctrl Pts',(-1.49354977511157,3.63837849450331,18.8607585262652));
#25253=CARTESIAN_POINT('Ctrl Pts',(-1.6008720422103,3.5943228394548,18.8666117850698));
#25254=CARTESIAN_POINT('Ctrl Pts',(-1.70619980701989,3.54553249555648,18.8724650438743));
#25255=CARTESIAN_POINT('Ctrl Pts',(-1.80909802186465,3.49222756235693,18.8783183026788));
#25256=CARTESIAN_POINT('Ctrl Pts',(-1.9121133034995,3.43886198439853,18.8841782207069));
#25257=CARTESIAN_POINT('Ctrl Pts',(-2.0126931508247,3.3809717556427,18.8900381387351));
#25258=CARTESIAN_POINT('Ctrl Pts',(-2.11042835948061,3.31882225186887,18.8958980567632));
#25259=CARTESIAN_POINT('Ctrl Pts',(-2.20822937604956,3.25663090105552,18.9017619204418));
#25260=CARTESIAN_POINT('Ctrl Pts',(-2.30318160218773,3.19017480116358,18.9076257841204));
#25261=CARTESIAN_POINT('Ctrl Pts',(-2.39490741118955,3.11976080682948,18.9134896477991));
#25262=CARTESIAN_POINT('Ctrl Pts',(-2.48676853781311,3.04924293492424,18.9193621620865));
#25263=CARTESIAN_POINT('Ctrl Pts',(-2.57539343244822,2.97475578032093,18.9252346763739));
#25264=CARTESIAN_POINT('Ctrl Pts',(-2.66043986350973,2.8966443918176,18.9311071906613));
#25265=CARTESIAN_POINT('Ctrl Pts',(-2.6839448737467,2.87505607866349,18.9327302277096));
#25266=CARTESIAN_POINT('Ctrl Pts',(-2.70717677414301,2.85319112929916,18.9343532647579));
#25267=CARTESIAN_POINT('Ctrl Pts',(-2.73012888152008,2.8310572742864,18.9359763018063));
#25268=CARTESIAN_POINT('Ctrl Pts',(-2.81316926555667,2.75097731516654,18.9418484257723));
#25269=CARTESIAN_POINT('Ctrl Pts',(-2.89282252825392,2.66710640265115,18.9477205497383));
#25270=CARTESIAN_POINT('Ctrl Pts',(-2.96872255476643,2.57976266211082,18.9535926737044));
#25271=CARTESIAN_POINT('Ctrl Pts',(-3.04452417538751,2.49253216446437,18.9594571843451));
#25272=CARTESIAN_POINT('Ctrl Pts',(-3.11658196815892,2.40183810198126,18.9653216949858));
#25273=CARTESIAN_POINT('Ctrl Pts',(-3.1845652322769,2.30803667244981,18.9711862056265));
#25274=CARTESIAN_POINT('Ctrl Pts',(-3.25247854229245,2.21433176365613,18.9770446817441));
#25275=CARTESIAN_POINT('Ctrl Pts',(-3.31632542188778,2.11752618041993,18.9829031578617));
#25276=CARTESIAN_POINT('Ctrl Pts',(-3.37581463799054,2.01801004207828,18.9887616339793));
#25277=CARTESIAN_POINT('Ctrl Pts',(-3.43764959268571,1.91456985057931,18.9948511175706));
#25278=CARTESIAN_POINT('Ctrl Pts',(-3.49477585847065,1.80820128818851,19.0009406011619));
#25279=CARTESIAN_POINT('Ctrl Pts',(-3.54691506206068,1.69937710427293,19.0070300847531));
#25280=CARTESIAN_POINT('Ctrl Pts',(-3.59701818919474,1.59480258938669,19.0128817692735));
#25281=CARTESIAN_POINT('Ctrl Pts',(-3.64251624684647,1.48796104977659,19.0187334537939));
#25282=CARTESIAN_POINT('Ctrl Pts',(-3.6832089061037,1.3792973406769,19.0245851383143));
#25283=CARTESIAN_POINT('Ctrl Pts',(-3.72389535884585,1.27065020515491,19.0304359303256));
#25284=CARTESIAN_POINT('Ctrl Pts',(-3.75977772554019,1.16018183978562,19.036286722337));
#25285=CARTESIAN_POINT('Ctrl Pts',(-3.7907042235979,1.04835608893021,19.0421375143483));
#25286=CARTESIAN_POINT('Ctrl Pts',(-3.82163349540714,0.936520308589818,
19.0479888311084));
#25287=CARTESIAN_POINT('Ctrl Pts',(-3.84760590478224,0.823327299230757,
19.0538401478685));
#25288=CARTESIAN_POINT('Ctrl Pts',(-3.86852003695864,0.709254343412531,
19.0596914646287));
#25289=CARTESIAN_POINT('Ctrl Pts',(-3.8894411105082,0.595143526929192,19.0655447234332));
#25290=CARTESIAN_POINT('Ctrl Pts',(-3.90530049409095,0.480152589678168,
19.0713979822377));
#25291=CARTESIAN_POINT('Ctrl Pts',(-3.91604831164449,0.364766529257176,
19.0772512410422));
#25292=CARTESIAN_POINT('Ctrl Pts',(-3.92680835693691,0.249249194685909,
19.0831111590703));
#25293=CARTESIAN_POINT('Ctrl Pts',(-3.93244519044413,0.133336251571786,
19.0889710770985));
#25294=CARTESIAN_POINT('Ctrl Pts',(-3.93296099779482,0.0175154167745557,
19.0948309951266));
#25295=CARTESIAN_POINT('Ctrl Pts',(-3.93347715245336,-0.0983834035053982,
19.1006948588052));
#25296=CARTESIAN_POINT('Ctrl Pts',(-3.928865431457,-0.214189579898975,19.1065587224838));
#25297=CARTESIAN_POINT('Ctrl Pts',(-3.91917998539294,-0.329419553298565,
19.1124225861625));
#25298=CARTESIAN_POINT('Ctrl Pts',(-3.90948025096728,-0.444819518613378,
19.1182951004499));
#25299=CARTESIAN_POINT('Ctrl Pts',(-3.8946919054861,-0.559641175925521,
19.1241676147373));
#25300=CARTESIAN_POINT('Ctrl Pts',(-3.87492036337435,-0.673410110932998,
19.1300401290246));
#25301=CARTESIAN_POINT('Ctrl Pts',(-3.86945593301628,-0.704853405479625,
19.131663166073));
#25302=CARTESIAN_POINT('Ctrl Pts',(-3.8636111551001,-0.736216373735889,
19.1332862031213));
#25303=CARTESIAN_POINT('Ctrl Pts',(-3.85738892320337,-0.767489215004342,
19.1349092401697));
#25304=CARTESIAN_POINT('Ctrl Pts',(-3.83487698049673,-0.880633890836507,
19.1407813641357));
#25305=CARTESIAN_POINT('Ctrl Pts',(-3.80734494774753,-0.992976934222328,
19.1466534881017));
#25306=CARTESIAN_POINT('Ctrl Pts',(-3.77486267961749,-1.10403838249902,
19.1525256120678));
#25307=CARTESIAN_POINT('Ctrl Pts',(-3.74242252539305,-1.21495583740279,
19.1583901227085));
#25308=CARTESIAN_POINT('Ctrl Pts',(-3.70504501399428,-1.32459460842115,
19.1642546333492));
#25309=CARTESIAN_POINT('Ctrl Pts',(-3.66285117170431,-1.43248395940212,
19.1701191439899));
#25310=CARTESIAN_POINT('Ctrl Pts',(-3.62070074645829,-1.54026229331424,
19.1759776201075));
#25311=CARTESIAN_POINT('Ctrl Pts',(-3.57374399762143,-1.64629440504661,
19.1818360962252));
#25312=CARTESIAN_POINT('Ctrl Pts',(-3.52215182078561,-1.75012443881474,
19.1876945723428));
#25313=CARTESIAN_POINT('Ctrl Pts',(-3.46852529607637,-1.85804862835121,
19.193784055934));
#25314=CARTESIAN_POINT('Ctrl Pts',(-3.40989038826873,-1.9635930687259,19.1998735395253));
#25315=CARTESIAN_POINT('Ctrl Pts',(-3.34649447007401,-2.06626807596789,
19.2059630231166));
#25316=CARTESIAN_POINT('Ctrl Pts',(-3.28557421179645,-2.16493354431272,
19.211814707637));
#25317=CARTESIAN_POINT('Ctrl Pts',(-3.22025804526277,-2.2609490963118,19.2176663921574));
#25318=CARTESIAN_POINT('Ctrl Pts',(-3.15081204299447,-2.35390579032403,
19.2235180766778));
#25319=CARTESIAN_POINT('Ctrl Pts',(-3.0813766327511,-2.44684830641979,19.2293688686891));
#25320=CARTESIAN_POINT('Ctrl Pts',(-3.00781288655098,-2.53673256105849,
19.2352196607004));
#25321=CARTESIAN_POINT('Ctrl Pts',(-2.93042908705681,-2.62318020077374,
19.2410704527117));
#25322=CARTESIAN_POINT('Ctrl Pts',(-2.85303834712496,-2.70963559384901,
19.2469217694719));
#25323=CARTESIAN_POINT('Ctrl Pts',(-2.77182714856107,-2.79265345123121,
19.252773086232));
#25324=CARTESIAN_POINT('Ctrl Pts',(-2.68714229762955,-2.87189053974732,
19.2586244029921));
#25325=CARTESIAN_POINT('Ctrl Pts',(-2.60242933990655,-2.95115392694968,
19.2644776617967));
#25326=CARTESIAN_POINT('Ctrl Pts',(-2.51424073906392,-3.02663376782738,
19.2703309206012));
#25327=CARTESIAN_POINT('Ctrl Pts',(-2.42295764194274,-3.09802602722303,
19.2761841794057));
#25328=CARTESIAN_POINT('Ctrl Pts',(-2.33157069249344,-3.16949950923909,
19.2820440974339));
#25329=CARTESIAN_POINT('Ctrl Pts',(-2.23708254559468,-3.23687587281718,
19.287904015462));
#25330=CARTESIAN_POINT('Ctrl Pts',(-2.13990476760512,-3.29989342033662,
19.2937639334901));
#25331=CARTESIAN_POINT('Ctrl Pts',(-2.04266155703657,-3.36295339937426,
19.2996277971687));
#25332=CARTESIAN_POINT('Ctrl Pts',(-1.94272546491684,-3.42164850950514,
19.3054916608474));
#25333=CARTESIAN_POINT('Ctrl Pts',(-1.84053263824569,-3.47576302522948,
19.311355524526));
#25334=CARTESIAN_POINT('Ctrl Pts',(-1.73818905258519,-3.52995737287514,
19.3172280388134));
#25335=CARTESIAN_POINT('Ctrl Pts',(-1.6335824600058,-3.579557462985,19.3231005531008));
#25336=CARTESIAN_POINT('Ctrl Pts',(-1.527169012984,-3.62439564697088,19.3289730673882));
#25337=CARTESIAN_POINT('Ctrl Pts',(-1.49775861762262,-3.63678795973978,
19.3305961044365));
#25338=CARTESIAN_POINT('Ctrl Pts',(-1.46821029221951,-3.64881682804049,
19.3322191414848));
#25339=CARTESIAN_POINT('Ctrl Pts',(-1.43853384702938,-3.66047939086547,
19.3338421785332));
#25340=CARTESIAN_POINT('Ctrl Pts',(-1.3311649085284,-3.70267437017302,19.3397143024992));
#25341=CARTESIAN_POINT('Ctrl Pts',(-1.2217579028076,-3.74021207553306,19.3455864264652));
#25342=CARTESIAN_POINT('Ctrl Pts',(-1.11075443632876,-3.77289193884161,
19.3514585504313));
#25343=CARTESIAN_POINT('Ctrl Pts',(-0.999894888048273,-3.80552943205848,
19.357323061072));
#25344=CARTESIAN_POINT('Ctrl Pts',(-0.887443388094081,-3.83332149255843,
19.3631875717127));
#25345=CARTESIAN_POINT('Ctrl Pts',(-0.773861429825642,-3.85611559570356,
19.3690520823534));
#25346=CARTESIAN_POINT('Ctrl Pts',(-0.660396346262345,-3.87888624394331,
19.374910558471));
#25347=CARTESIAN_POINT('Ctrl Pts',(-0.545803520995739,-3.89666908334434,
19.3807690345886));
#25348=CARTESIAN_POINT('Ctrl Pts',(-0.430558873189867,-3.90936159196325,
19.3866275107062));
#25349=CARTESIAN_POINT('Ctrl Pts',(-0.310769976263919,-3.92255458300996,
19.3927169942975));
#25350=CARTESIAN_POINT('Ctrl Pts',(-0.190277231330525,-3.93024741903014,
19.3988064778888));
#25351=CARTESIAN_POINT('Ctrl Pts',(-0.0696263462424803,-3.93238365014261,
19.40489596148));
#25352=CARTESIAN_POINT('Ctrl Pts',(0.0463130279362404,-3.9344364597685,
19.4107476460004));
#25353=CARTESIAN_POINT('Ctrl Pts',(0.162397970763817,-3.93135849208445,
19.4165993305208));
#25354=CARTESIAN_POINT('Ctrl Pts',(0.27814060995989,-3.92315266094644,19.4224510150412));
#25355=CARTESIAN_POINT('Ctrl Pts',(0.393865595887476,-3.91494808137606,
19.4283018070525));
#25356=CARTESIAN_POINT('Ctrl Pts',(0.509247969727086,-3.90161722266105,
19.4341525990639));
#25357=CARTESIAN_POINT('Ctrl Pts',(0.623802789213381,-3.88321504428606,
19.4400033910752));
#25358=CARTESIAN_POINT('Ctrl Pts',(0.738367882950747,-3.86481121544712,
19.4458547078353));
#25359=CARTESIAN_POINT('Ctrl Pts',(0.852104866584206,-3.84133522834408,
19.4517060245954));
#25360=CARTESIAN_POINT('Ctrl Pts',(0.964537533390909,-3.81289343500185,
19.4575573413556));
#25361=CARTESIAN_POINT('Ctrl Pts',(1.07700751645285,-3.78444220186555,19.4634106001601));
#25362=CARTESIAN_POINT('Ctrl Pts',(1.18817192131659,-3.75102198659465,19.4692638589646));
#25363=CARTESIAN_POINT('Ctrl Pts',(1.29756896825586,-3.71278921737007,19.4751171177691));
#25364=CARTESIAN_POINT('Ctrl Pts',(1.40709047567452,-3.67451295091298,19.4809770357972));
#25365=CARTESIAN_POINT('Ctrl Pts',(1.51484022133774,-3.63141333858427,19.4868369538253));
#25366=CARTESIAN_POINT('Ctrl Pts',(1.62037561297551,-3.58369528181097,19.4926968718535));
#25367=CARTESIAN_POINT('Ctrl Pts',(1.72598206461274,-3.53594509510443,19.4985607355321));
#25368=CARTESIAN_POINT('Ctrl Pts',(1.82937082548394,-3.48357045823726,19.5044245992107));
#25369=CARTESIAN_POINT('Ctrl Pts',(1.93012470409018,-3.42682179674707,19.5102884628893));
#25370=CARTESIAN_POINT('Ctrl Pts',(2.03102721889137,-3.36998941733724,19.5161609771767));
#25371=CARTESIAN_POINT('Ctrl Pts',(2.12928674395889,-3.3087703526312,19.5220334914641));
#25372=CARTESIAN_POINT('Ctrl Pts',(2.22451573180351,-3.24345783986145,19.5279060057515));
#25373=CARTESIAN_POINT('Ctrl Pts',(2.25083498243191,-3.22540686156519,19.5295290427999));
#25374=CARTESIAN_POINT('Ctrl Pts',(2.27692294587325,-3.20704343676956,19.5311520798482));
#25375=CARTESIAN_POINT('Ctrl Pts',(2.30277191380724,-3.18837427429412,19.5327751168966));
#25376=CARTESIAN_POINT('Ctrl Pts',(2.39552458398488,-3.12138457188128,19.5385989865542));
#25377=CARTESIAN_POINT('Ctrl Pts',(2.48551964526767,-3.05022259204407,19.5444228562118));
#25378=CARTESIAN_POINT('Ctrl Pts',(2.5723534079641,-2.97514486110096,19.5502467258694));
#25379=CARTESIAN_POINT('Ctrl Pts',(2.65907424722462,-2.90016476539875,19.5560630218443));
#25380=CARTESIAN_POINT('Ctrl Pts',(2.74264164523572,-2.82127931423445,19.5618793178192));
#25381=CARTESIAN_POINT('Ctrl Pts',(2.82268126028275,-2.73878796237471,19.567695613794));
#25382=CARTESIAN_POINT('Ctrl Pts',(2.90263909582087,-2.65638089505631,19.5735059670388));
#25383=CARTESIAN_POINT('Ctrl Pts',(2.97907602415453,-2.57037555303375,19.5793163202836));
#25384=CARTESIAN_POINT('Ctrl Pts',(3.05165175501386,-2.48111075248987,19.5851266735283));
#25385=CARTESIAN_POINT('Ctrl Pts',(3.12417493538596,-2.39191058662077,19.5909328196244));
#25386=CARTESIAN_POINT('Ctrl Pts',(3.19284221354518,-2.29945598111866,19.5967389657204));
#25387=CARTESIAN_POINT('Ctrl Pts',(3.25735159402052,-2.20412104770405,19.6025451118165));
#25388=CARTESIAN_POINT('Ctrl Pts',(3.32183656168728,-2.10882219266227,19.6083490606455));
#25389=CARTESIAN_POINT('Ctrl Pts',(3.38216652316824,-2.01064552406509,19.6141530094745));
#25390=CARTESIAN_POINT('Ctrl Pts',(3.43808149197777,-1.90999598285439,19.6199569583036));
#25391=CARTESIAN_POINT('Ctrl Pts',(3.49398939829731,-1.80935915445374,19.6257601740493));
#25392=CARTESIAN_POINT('Ctrl Pts',(3.54548321634294,-1.70625044237268,19.631563389795));
#25393=CARTESIAN_POINT('Ctrl Pts',(3.59234822072463,-1.6011006405147,19.6373666055408));
#25394=CARTESIAN_POINT('Ctrl Pts',(3.63921912209722,-1.49593760773028,19.6431705515011));
#25395=CARTESIAN_POINT('Ctrl Pts',(3.68145988153625,-1.38873335948787,19.6489744974614));
#25396=CARTESIAN_POINT('Ctrl Pts',(3.7189036818442,-1.27993921932476,19.6547784434217));
#25397=CARTESIAN_POINT('Ctrl Pts',(3.75638418468743,-1.17103843879034,19.6605880784288));
#25398=CARTESIAN_POINT('Ctrl Pts',(3.78905820137532,-1.06054505287451,19.6663977134359));
#25399=CARTESIAN_POINT('Ctrl Pts',(3.81680863206719,-0.948926164765915,
19.672207348443));
#25400=CARTESIAN_POINT('Ctrl Pts',(3.84457316313211,-0.83725056157499,19.6780199354051));
#25401=CARTESIAN_POINT('Ctrl Pts',(3.86740904317258,-0.724448729830302,
19.6838325223671));
#25402=CARTESIAN_POINT('Ctrl Pts',(3.8852505658126,-0.610996760100171,19.6896451093291));
#25403=CARTESIAN_POINT('Ctrl Pts',(3.90311995945255,-0.497367562231769,
19.69546677638));
#25404=CARTESIAN_POINT('Ctrl Pts',(3.91597936556538,-0.383086616055516,
19.7012884434309));
#25405=CARTESIAN_POINT('Ctrl Pts',(3.92381506326595,-0.268634229552435,
19.7071101104818));
#25406=CARTESIAN_POINT('Ctrl Pts',(3.92997341763335,-0.17868201582306,19.7116855663095));
#25407=CARTESIAN_POINT('Ctrl Pts',(3.93302969846842,-0.0886240110624213,
19.7162610221373));
#25408=CARTESIAN_POINT('Ctrl Pts',(3.9329997823937,0.00130831614195257,
19.720836477965));
#25409=CARTESIAN_POINT('',(3.93299832388421,-0.00363102244798902,20.9708364779651));
#25410=CARTESIAN_POINT('Ctrl Pts',(3.93900201824057,0.00131031279145309,
19.720836477965));
#25411=CARTESIAN_POINT('Ctrl Pts',(3.93931038383691,0.0726474573565517,
19.7244603370634));
#25412=CARTESIAN_POINT('Ctrl Pts',(3.90516583393947,1.44904206919199,19.7943951756155));
#25413=CARTESIAN_POINT('Ctrl Pts',(2.29631571635523,4.04614279448815,19.9306409936241));
#25414=CARTESIAN_POINT('Ctrl Pts',(-2.16378473825673,4.11854015265543,20.1295739319866));
#25415=CARTESIAN_POINT('Ctrl Pts',(-4.6347080772386,0.404744884258939,20.3285068703506));
#25416=CARTESIAN_POINT('Ctrl Pts',(-2.84492327743589,-3.68113419044451,
20.5274398087137));
#25417=CARTESIAN_POINT('Ctrl Pts',(1.56021238382014,-4.3829299218592,20.7263727470772));
#25418=CARTESIAN_POINT('Ctrl Pts',(3.76741191265789,-1.91077193019647,20.8741716368277));
#25419=CARTESIAN_POINT('Ctrl Pts',(3.93595010307849,-0.303549133925586,
20.9556595471236));
#25420=CARTESIAN_POINT('Ctrl Pts',(3.93316774256311,-0.00363117885869044,
20.9708364779651));
#25421=CARTESIAN_POINT('',(3.93299999067832,0.000270784605071274,22.220836477992));
#25422=CARTESIAN_POINT('Ctrl Pts',(3.93299832388421,-0.00363102244798902,
20.9708364779651));
#25423=CARTESIAN_POINT('Ctrl Pts',(3.93310381018972,0.110628106685084,20.9766187057418));
#25424=CARTESIAN_POINT('Ctrl Pts',(3.92822601209407,0.225031196093933,20.9824009335186));
#25425=CARTESIAN_POINT('Ctrl Pts',(3.91835408310254,0.339102166660221,20.9881831612953));
#25426=CARTESIAN_POINT('Ctrl Pts',(3.90848950901343,0.453088150709805,20.9939610811277));
#25427=CARTESIAN_POINT('Ctrl Pts',(3.89363823801213,0.566742085803051,20.9997390009601));
#25428=CARTESIAN_POINT('Ctrl Pts',(3.87384149043578,0.679588924996797,21.0055169207924));
#25429=CARTESIAN_POINT('Ctrl Pts',(3.8540524889173,0.792391609556333,21.0112925798442));
#25430=CARTESIAN_POINT('Ctrl Pts',(3.829321928639,0.904387407412825,21.0170682388961));
#25431=CARTESIAN_POINT('Ctrl Pts',(3.79974267999181,1.0151081547543,21.0228438979479));
#25432=CARTESIAN_POINT('Ctrl Pts',(3.77016739867057,1.12581405164098,21.0286187823377));
#25433=CARTESIAN_POINT('Ctrl Pts',(3.73574483136308,1.23524482716285,21.0343936667274));
#25434=CARTESIAN_POINT('Ctrl Pts',(3.69661838113476,1.34294510098388,21.0401685511172));
#25435=CARTESIAN_POINT('Ctrl Pts',(3.65748711683048,1.45065862612968,21.0459441460425));
#25436=CARTESIAN_POINT('Ctrl Pts',(3.61365096553608,1.55664082706948,21.0517197409677));
#25437=CARTESIAN_POINT('Ctrl Pts',(3.56530205503563,1.66045483418209,21.057495335893));
#25438=CARTESIAN_POINT('Ctrl Pts',(3.51690448632742,1.76437331941999,21.0632767433608));
#25439=CARTESIAN_POINT('Ctrl Pts',(3.46398526895846,1.86611886724229,21.0690581508285));
#25440=CARTESIAN_POINT('Ctrl Pts',(3.40678324459325,1.96527782370805,21.0748395582963));
#25441=CARTESIAN_POINT('Ctrl Pts',(3.34955186696935,2.06448766366148,21.0806239324974));
#25442=CARTESIAN_POINT('Ctrl Pts',(3.2880335359382,2.16110791166841,21.0864083066984));
#25443=CARTESIAN_POINT('Ctrl Pts',(3.2225102417811,2.2547542530431,21.0921926808995));
#25444=CARTESIAN_POINT('Ctrl Pts',(3.15688054523395,2.34855266544335,21.0979864482675));
#25445=CARTESIAN_POINT('Ctrl Pts',(3.08723315492587,2.43936718858691,21.1037802156355));
#25446=CARTESIAN_POINT('Ctrl Pts',(3.01389031731061,2.52684668217551,21.1095739830034));
#25447=CARTESIAN_POINT('Ctrl Pts',(2.95201081239799,2.60065331318786,21.1144621966037));
#25448=CARTESIAN_POINT('Ctrl Pts',(2.88750153904751,2.67208648082503,21.1193504102039));
#25449=CARTESIAN_POINT('Ctrl Pts',(2.82057507590323,2.74095699367821,21.1242386238041));
#25450=CARTESIAN_POINT('Ctrl Pts',(2.74017750731638,2.82368991456763,21.1301107477701));
#25451=CARTESIAN_POINT('Ctrl Pts',(2.65600199206874,2.90302121266157,21.1359828717362));
#25452=CARTESIAN_POINT('Ctrl Pts',(2.56836805608851,2.97858599480762,21.1418549957022));
#25453=CARTESIAN_POINT('Ctrl Pts',(2.48084773924625,3.05405280571329,21.1477195063429));
#25454=CARTESIAN_POINT('Ctrl Pts',(2.38987822874045,3.12576254443211,21.1535840169836));
#25455=CARTESIAN_POINT('Ctrl Pts',(2.29581698693659,3.19338587748073,21.1594485276243));
#25456=CARTESIAN_POINT('Ctrl Pts',(2.20185253321485,3.26093962679235,21.165307003742));
#25457=CARTESIAN_POINT('Ctrl Pts',(2.10480300972062,3.32441509425251,21.1711654798596));
#25458=CARTESIAN_POINT('Ctrl Pts',(2.00505964888514,3.38352254380144,21.1770239559772));
#25459=CARTESIAN_POINT('Ctrl Pts',(1.90138327520834,3.4449606783819,21.1831134395684));
#25460=CARTESIAN_POINT('Ctrl Pts',(1.79479659507585,3.50167893757552,21.1892029231597));
#25461=CARTESIAN_POINT('Ctrl Pts',(1.68577342106561,3.5534007616407,21.195292406751));
#25462=CARTESIAN_POINT('Ctrl Pts',(1.58100768680266,3.60310280824503,21.2011440912714));
#25463=CARTESIAN_POINT('Ctrl Pts',(1.47399259034375,3.64819113230166,21.2069957757918));
#25464=CARTESIAN_POINT('Ctrl Pts',(1.36517375128535,3.68846711098276,21.2128474603122));
#25465=CARTESIAN_POINT('Ctrl Pts',(1.25637150946539,3.7287369467016,21.2186982523235));
#25466=CARTESIAN_POINT('Ctrl Pts',(1.14576645965264,3.76419575298251,21.2245490443348));
#25467=CARTESIAN_POINT('Ctrl Pts',(1.03382302440939,3.79469352572787,21.2303998363461));
#25468=CARTESIAN_POINT('Ctrl Pts',(0.921869549126134,3.82519403377306,21.2362511531063));
#25469=CARTESIAN_POINT('Ctrl Pts',(0.80857784868674,3.85073251509202,21.2421024698664));
#25470=CARTESIAN_POINT('Ctrl Pts',(0.694425590751786,3.87120938453464,21.2479537866265));
#25471=CARTESIAN_POINT('Ctrl Pts',(0.580235445831579,3.89169305022346,21.2538070454311));
#25472=CARTESIAN_POINT('Ctrl Pts',(0.465184582185747,3.90711169062497,21.2596603042356));
#25473=CARTESIAN_POINT('Ctrl Pts',(0.349758184968424,3.91741728847561,21.2655135630401));
#25474=CARTESIAN_POINT('Ctrl Pts',(0.234200467709677,3.92773461095397,21.2713734810682));
#25475=CARTESIAN_POINT('Ctrl Pts',(0.118266776134782,3.93292724335107,21.2772333990964));
#25476=CARTESIAN_POINT('Ctrl Pts',(0.00244481514791298,3.932999240132,21.2830933171245));
#25477=CARTESIAN_POINT('Ctrl Pts',(-0.113455132079537,3.93307128539042,
21.2889571808031));
#25478=CARTESIAN_POINT('Ctrl Pts',(-0.229242786907232,3.92801584763683,
21.2948210444817));
#25479=CARTESIAN_POINT('Ctrl Pts',(-0.344434801273944,3.91788892998147,
21.3006849081603));
#25480=CARTESIAN_POINT('Ctrl Pts',(-0.459796751557577,3.90774707268775,
21.3065574224477));
#25481=CARTESIAN_POINT('Ctrl Pts',(-0.57456089934629,3.89251885767977,21.3124299367351));
#25482=CARTESIAN_POINT('Ctrl Pts',(-0.688253237752109,3.87231151648776,
21.3183024510225));
#25483=CARTESIAN_POINT('Ctrl Pts',(-0.719675362640237,3.86672664060698,
21.3199254880709));
#25484=CARTESIAN_POINT('Ctrl Pts',(-0.751015704397142,3.86076172775783,
21.3215485251192));
#25485=CARTESIAN_POINT('Ctrl Pts',(-0.78226447348505,3.85441970905131,21.3231715621676));
#25486=CARTESIAN_POINT('Ctrl Pts',(-0.895322056524819,3.83147437944374,
21.3290436861336));
#25487=CARTESIAN_POINT('Ctrl Pts',(-1.00755877682702,3.8035120683751,21.3349158100996));
#25488=CARTESIAN_POINT('Ctrl Pts',(-1.11849494292434,3.77060446913392,21.3407879340657));
#25489=CARTESIAN_POINT('Ctrl Pts',(-1.22928727807958,3.73773953524856,21.3466524447064));
#25490=CARTESIAN_POINT('Ctrl Pts',(-1.33878201957949,3.69994218014727,21.3525169553471));
#25491=CARTESIAN_POINT('Ctrl Pts',(-1.44650889848123,3.65733523300977,21.3583814659878));
#25492=CARTESIAN_POINT('Ctrl Pts',(-1.5541249274962,3.61477212799703,21.3642399421054));
#25493=CARTESIAN_POINT('Ctrl Pts',(-1.65997633009354,3.5674094259213,21.370098418223));
#25494=CARTESIAN_POINT('Ctrl Pts',(-1.76360790867981,3.51541976788577,21.3759568943406));
#25495=CARTESIAN_POINT('Ctrl Pts',(-1.87132581768378,3.46138008876656,21.3820463779319));
#25496=CARTESIAN_POINT('Ctrl Pts',(-1.97664480367967,3.40234118213357,21.3881358615232));
#25497=CARTESIAN_POINT('Ctrl Pts',(-2.07907613418394,3.33855229527213,21.3942253451144));
#25498=CARTESIAN_POINT('Ctrl Pts',(-2.17750744155731,3.27725441405987,21.4000770296348));
#25499=CARTESIAN_POINT('Ctrl Pts',(-2.27327200762698,3.21157081091674,21.4059287141552));
#25500=CARTESIAN_POINT('Ctrl Pts',(-2.36596191330116,3.14176912340934,21.4117803986757));
#25501=CARTESIAN_POINT('Ctrl Pts',(-2.45863768174976,3.0719780821767,21.417631190687));
#25502=CARTESIAN_POINT('Ctrl Pts',(-2.5482393920752,2.99807045406087,21.4234819826983));
#25503=CARTESIAN_POINT('Ctrl Pts',(-2.63438987487826,2.92035596925082,21.4293327747096));
#25504=CARTESIAN_POINT('Ctrl Pts',(-2.72054808438972,2.84263451434447,21.4351840914697));
#25505=CARTESIAN_POINT('Ctrl Pts',(-2.80325414406277,2.76110580093713,21.4410354082298));
#25506=CARTESIAN_POINT('Ctrl Pts',(-2.88216615214998,2.67611794796137,21.44688672499));
#25507=CARTESIAN_POINT('Ctrl Pts',(-2.96110435102948,2.59110188762834,21.4527399837945));
#25508=CARTESIAN_POINT('Ctrl Pts',(-3.03624571325674,2.50262470763229,21.458593242599));
#25509=CARTESIAN_POINT('Ctrl Pts',(-3.10728766639976,2.41106871702984,21.4644465014035));
#25510=CARTESIAN_POINT('Ctrl Pts',(-3.17841044362169,2.31940856362947,21.4703064194316));
#25511=CARTESIAN_POINT('Ctrl Pts',(-3.24542424919564,2.22466293504505,21.4761663374597));
#25512=CARTESIAN_POINT('Ctrl Pts',(-3.30806896447818,2.12724439739684,21.4820262554878));
#25513=CARTESIAN_POINT('Ctrl Pts',(-3.37075586024014,2.02976026505954,21.4878901191665));
#25514=CARTESIAN_POINT('Ctrl Pts',(-3.42906760045181,1.9295999964155,21.4937539828451));
#25515=CARTESIAN_POINT('Ctrl Pts',(-3.4827901324422,1.82720056188784,21.4996178465237));
#25516=CARTESIAN_POINT('Ctrl Pts',(-3.5365919180839,1.72465006357414,21.5054903608111));
#25517=CARTESIAN_POINT('Ctrl Pts',(-3.58579080844062,1.61985417941031,21.5113628750985));
#25518=CARTESIAN_POINT('Ctrl Pts',(-3.6302209040578,1.51326970092637,21.5172353893859));
#25519=CARTESIAN_POINT('Ctrl Pts',(-3.64250042995079,1.48381203613512,21.5188584264342));
#25520=CARTESIAN_POINT('Ctrl Pts',(-3.6544159855181,1.45421783497541,21.5204814634826));
#25521=CARTESIAN_POINT('Ctrl Pts',(-3.66596474736453,1.42449691859285,21.522104500531));
#25522=CARTESIAN_POINT('Ctrl Pts',(-3.70774799641897,1.3169670839792,21.527976624497));
#25523=CARTESIAN_POINT('Ctrl Pts',(-3.7448661961721,1.20741704303183,21.533848748463));
#25524=CARTESIAN_POINT('Ctrl Pts',(-3.7771204721572,1.09628916751512,21.5397208724291));
#25525=CARTESIAN_POINT('Ctrl Pts',(-3.80933292983303,0.985305371495616,
21.5455853830698));
#25526=CARTESIAN_POINT('Ctrl Pts',(-3.8366938902624,0.872748202407449,21.5514498937105));
#25527=CARTESIAN_POINT('Ctrl Pts',(-3.8590525982954,0.759079734671854,21.5573144043512));
#25528=CARTESIAN_POINT('Ctrl Pts',(-3.88138829944023,0.645528230658984,
21.5631728804688));
#25529=CARTESIAN_POINT('Ctrl Pts',(-3.89873190703991,0.530868105702198,
21.5690313565864));
#25530=CARTESIAN_POINT('Ctrl Pts',(-3.9109827235493,0.415575668319147,21.574889832704));
#25531=CARTESIAN_POINT('Ctrl Pts',(-3.92371660598155,0.295737097409332,
21.5809793162952));
#25532=CARTESIAN_POINT('Ctrl Pts',(-3.9309476767346,0.175215759367503,21.5870687998865));
#25533=CARTESIAN_POINT('Ctrl Pts',(-3.93262157740627,0.054557574346977,
21.5931582834778));
#25534=CARTESIAN_POINT('Ctrl Pts',(-3.93423011095468,-0.0613888146960827,
21.5990099679982));
#25535=CARTESIAN_POINT('Ctrl Pts',(-3.93070734706526,-0.1774611110071,21.6048616525186));
#25536=CARTESIAN_POINT('Ctrl Pts',(-3.92205806902059,-0.293171457052866,
21.610713337039));
#25537=CARTESIAN_POINT('Ctrl Pts',(-3.91341011017883,-0.408864154755554,
21.6165641290503));
#25538=CARTESIAN_POINT('Ctrl Pts',(-3.89963722266148,-0.524194599809603,
21.6224149210616));
#25539=CARTESIAN_POINT('Ctrl Pts',(-3.88079622377034,-0.638678064105779,
21.6282657130729));
#25540=CARTESIAN_POINT('Ctrl Pts',(-3.86195353505806,-0.753171796253405,
21.634117029833));
#25541=CARTESIAN_POINT('Ctrl Pts',(-3.83804189850357,-0.866817988683255,
21.6399683465931));
#25542=CARTESIAN_POINT('Ctrl Pts',(-3.80916949009844,-0.979140845692379,
21.6458196633533));
#25543=CARTESIAN_POINT('Ctrl Pts',(-3.78028749897864,-1.09150098251116,
21.6516729221578));
#25544=CARTESIAN_POINT('Ctrl Pts',(-3.74644156496945,-1.20253651037752,
21.6575261809623));
#25545=CARTESIAN_POINT('Ctrl Pts',(-3.70778988456892,-1.31178625236292,
21.6633794397669));
#25546=CARTESIAN_POINT('Ctrl Pts',(-3.66909423034274,-1.42116028723954,
21.669239357795));
#25547=CARTESIAN_POINT('Ctrl Pts',(-3.62558205476129,-1.52874409108368,
21.6750992758231));
#25548=CARTESIAN_POINT('Ctrl Pts',(-3.57745995368959,-1.6340958600239,21.6809591938513));
#25549=CARTESIAN_POINT('Ctrl Pts',(-3.52930545062997,-1.73951856532536,
21.6868230575299));
#25550=CARTESIAN_POINT('Ctrl Pts',(-3.476535029194,-1.84270587599386,21.6926869212085));
#25551=CARTESIAN_POINT('Ctrl Pts',(-3.41940071169139,-1.94324156318365,
21.6985507848872));
#25552=CARTESIAN_POINT('Ctrl Pts',(-3.36218210733394,-2.04392556468334,
21.7044232991746));
#25553=CARTESIAN_POINT('Ctrl Pts',(-3.30058697739615,-2.14194978678147,
21.710295813462));
#25554=CARTESIAN_POINT('Ctrl Pts',(-3.23491004197727,-2.23692780847183,
21.7161683277494));
#25555=CARTESIAN_POINT('Ctrl Pts',(-3.21675834507387,-2.26317769743533,
21.7177913647977));
#25556=CARTESIAN_POINT('Ctrl Pts',(-3.19829509022018,-2.2891951036651,21.719414401846));
#25557=CARTESIAN_POINT('Ctrl Pts',(-3.17952701572355,-2.31497234460459,
21.7210374388944));
#25558=CARTESIAN_POINT('Ctrl Pts',(-3.11162440058543,-2.40823401996461,
21.7269095628604));
#25559=CARTESIAN_POINT('Ctrl Pts',(-3.03950115054583,-2.49866194169334,
21.7327816868264));
#25560=CARTESIAN_POINT('Ctrl Pts',(-2.96342203433715,-2.58584973391825,
21.7386538107924));
#25561=CARTESIAN_POINT('Ctrl Pts',(-2.88744155621313,-2.67292448543948,
21.7445183214332));
#25562=CARTESIAN_POINT('Ctrl Pts',(-2.80751568065602,-2.75676715288993,
21.7503828320739));
#25563=CARTESIAN_POINT('Ctrl Pts',(-2.72395175620129,-2.83700120371633,
21.7562473427146));
#25564=CARTESIAN_POINT('Ctrl Pts',(-2.64047381819366,-2.91715269450247,
21.7621058188322));
#25565=CARTESIAN_POINT('Ctrl Pts',(-2.55336557373237,-2.99370266985572,
21.7679642949498));
#25566=CARTESIAN_POINT('Ctrl Pts',(-2.46297339703016,-3.06630902642276,
21.7738227710674));
#25567=CARTESIAN_POINT('Ctrl Pts',(-2.36901693706379,-3.14177834780629,
21.7799122546586));
#25568=CARTESIAN_POINT('Ctrl Pts',(-2.27151253646121,-3.21298630502146,
21.7860017382499));
#25569=CARTESIAN_POINT('Ctrl Pts',(-2.17089018282705,-3.2795921719179,21.7920912218412));
#25570=CARTESIAN_POINT('Ctrl Pts',(-2.07419721036999,-3.34359702790358,
21.7979429063616));
#25571=CARTESIAN_POINT('Ctrl Pts',(-1.97462560932936,-3.4033522293723,21.803794590882));
#25572=CARTESIAN_POINT('Ctrl Pts',(-1.87258846806875,-3.45859818846537,
21.8096462754024));
#25573=CARTESIAN_POINT('Ctrl Pts',(-1.77056688969027,-3.51383572134874,
21.8154970674137));
#25574=CARTESIAN_POINT('Ctrl Pts',(-1.66608088224018,-3.56456518255316,
21.821347859425));
#25575=CARTESIAN_POINT('Ctrl Pts',(-1.55956901731825,-3.61057245879666,
21.8271986514363));
#25576=CARTESIAN_POINT('Ctrl Pts',(-1.45304759950628,-3.65658386136404,
21.8330499681964));
#25577=CARTESIAN_POINT('Ctrl Pts',(-1.34450034257092,-3.69787207309831,
21.8389012849566));
#25578=CARTESIAN_POINT('Ctrl Pts',(-1.23438605356345,-3.73427102267204,
21.8447526017167));
#25579=CARTESIAN_POINT('Ctrl Pts',(-1.12423521776663,-3.7706820530098,21.8506058605212));
#25580=CARTESIAN_POINT('Ctrl Pts',(-1.01251670803692,-3.80220046479243,
21.8564591193257));
#25581=CARTESIAN_POINT('Ctrl Pts',(-0.899704059044844,-3.82871017525984,
21.8623123781303));
#25582=CARTESIAN_POINT('Ctrl Pts',(-0.78676306366016,-3.85525004569369,
21.8681722961584));
#25583=CARTESIAN_POINT('Ctrl Pts',(-0.672725847122139,-3.8767697463796,
21.8740322141865));
#25584=CARTESIAN_POINT('Ctrl Pts',(-0.558075795289308,-3.89320438799612,
21.8798921322146));
#25585=CARTESIAN_POINT('Ctrl Pts',(-0.443348546295274,-3.90965009552719,
21.8857559958932));
#25586=CARTESIAN_POINT('Ctrl Pts',(-0.328008050780501,-3.92100388590197,
21.8916198595719));
#25587=CARTESIAN_POINT('Ctrl Pts',(-0.212540720783978,-3.92725291291618,
21.8974837232505));
#25588=CARTESIAN_POINT('Ctrl Pts',(-0.0969030487144911,-3.93351115874766,
21.9033562375379));
#25589=CARTESIAN_POINT('Ctrl Pts',(0.0188614194313403,-3.93464960718324,
21.9092287518253));
#25590=CARTESIAN_POINT('Ctrl Pts',(0.134268281523294,-3.93070744632271,
21.9151012661127));
#25591=CARTESIAN_POINT('Ctrl Pts',(0.166164264001246,-3.92961791757673,
21.916724303161));
#25592=CARTESIAN_POINT('Ctrl Pts',(0.198032975418511,-3.9281406094255,21.9183473402094));
#25593=CARTESIAN_POINT('Ctrl Pts',(0.229864310321648,-3.92627704051056,
21.9199703772578));
#25594=CARTESIAN_POINT('Ctrl Pts',(0.345029607837563,-3.91953467581919,
21.9258425012238));
#25595=CARTESIAN_POINT('Ctrl Pts',(0.460091077063301,-3.90770968008665,
21.9317146251898));
#25596=CARTESIAN_POINT('Ctrl Pts',(0.574563709162917,-3.89080525651348,
21.9375867491559));
#25597=CARTESIAN_POINT('Ctrl Pts',(0.688887925222219,-3.87392274986111,
21.9434512597966));
#25598=CARTESIAN_POINT('Ctrl Pts',(0.802624417161421,-3.85197397153181,
21.9493157704373));
#25599=CARTESIAN_POINT('Ctrl Pts',(0.915290279661123,-3.82501407892283,
21.955180281078));
#25600=CARTESIAN_POINT('Ctrl Pts',(1.02784021010917,-3.79808192777513,21.9610387571956));
#25601=CARTESIAN_POINT('Ctrl Pts',(1.13932130274485,-3.76614901427635,21.9668972333132));
#25602=CARTESIAN_POINT('Ctrl Pts',(1.24925853498099,-3.72932193740057,21.9727557094309));
#25603=CARTESIAN_POINT('Ctrl Pts',(1.36353073791085,-3.69104272010116,21.9788451930221));
#25604=CARTESIAN_POINT('Ctrl Pts',(1.47613437252864,-3.64747549872448,21.9849346766134));
#25605=CARTESIAN_POINT('Ctrl Pts',(1.58655039477646,-3.5987979722172,21.9910241602047));
#25606=CARTESIAN_POINT('Ctrl Pts',(1.69265458546996,-3.55202134098317,21.9968758447251));
#25607=CARTESIAN_POINT('Ctrl Pts',(1.79673839959062,-3.5005262201031,22.0027275292455));
#25608=CARTESIAN_POINT('Ctrl Pts',(1.89836019769853,-3.44451993168772,22.0085792137659));
#25609=CARTESIAN_POINT('Ctrl Pts',(1.99996649627292,-3.38852218544894,22.0144300057772));
#25610=CARTESIAN_POINT('Ctrl Pts',(2.09911116350122,-3.32801483922488,22.0202807977885));
#25611=CARTESIAN_POINT('Ctrl Pts',(2.19537705434484,-3.26325122987124,22.0261315897998));
#25612=CARTESIAN_POINT('Ctrl Pts',(2.29165157913314,-3.19848181196574,22.0319829065599));
#25613=CARTESIAN_POINT('Ctrl Pts',(2.38504647123927,-3.12945560284899,22.0378342233201));
#25614=CARTESIAN_POINT('Ctrl Pts',(2.4751740759537,-3.05646892569297,22.0436855400802));
#25615=CARTESIAN_POINT('Ctrl Pts',(2.56533159390193,-2.98345802435453,22.0495387988847));
#25616=CARTESIAN_POINT('Ctrl Pts',(2.65221934707578,-2.90648430126819,22.0553920576892));
#25617=CARTESIAN_POINT('Ctrl Pts',(2.73548378520078,-2.82588348324973,22.0612453164937));
#25618=CARTESIAN_POINT('Ctrl Pts',(2.81884295286569,-2.74519096607879,22.0671052345219));
#25619=CARTESIAN_POINT('Ctrl Pts',(2.89857028040793,-2.66086340524392,22.07296515255));
#25620=CARTESIAN_POINT('Ctrl Pts',(2.97434997078581,-2.57327247902091,22.0788250705781));
#25621=CARTESIAN_POINT('Ctrl Pts',(3.05018068579784,-2.48562257532066,22.0846889342567));
#25622=CARTESIAN_POINT('Ctrl Pts',(3.12205821516943,-2.39470525445788,22.0905527979354));
#25623=CARTESIAN_POINT('Ctrl Pts',(3.18970891792406,-2.30092286244362,22.096416661614));
#25624=CARTESIAN_POINT('Ctrl Pts',(3.2574594217304,-2.20700211885319,22.1022891759014));
#25625=CARTESIAN_POINT('Ctrl Pts',(3.3209704279015,-2.11020821282023,22.1081616901888));
#25626=CARTESIAN_POINT('Ctrl Pts',(3.38001316534968,-2.0109699157528,22.1140342044762));
#25627=CARTESIAN_POINT('Ctrl Pts',(3.39633131216481,-1.98354257801035,22.1156572415245));
#25628=CARTESIAN_POINT('Ctrl Pts',(3.41230842931794,-1.95592865155571,22.1172802785729));
#25629=CARTESIAN_POINT('Ctrl Pts',(3.42794033419869,-1.92813746013447,22.1189033156213));
#25630=CARTESIAN_POINT('Ctrl Pts',(3.48709305513061,-1.82297275992373,22.1250450531969));
#25631=CARTESIAN_POINT('Ctrl Pts',(3.54148206867059,-1.71494248824927,22.1311867907725));
#25632=CARTESIAN_POINT('Ctrl Pts',(3.59083306109141,-1.60449584835016,22.1373285283481));
#25633=CARTESIAN_POINT('Ctrl Pts',(3.64009789866522,-1.4942420214604,22.1434595439416));
#25634=CARTESIAN_POINT('Ctrl Pts',(3.68434208599632,-1.38158055357559,22.149590559535));
#25635=CARTESIAN_POINT('Ctrl Pts',(3.7233365365936,-1.26698620168776,22.1557215751284));
#25636=CARTESIAN_POINT('Ctrl Pts',(3.7622449950462,-1.15264455791443,22.1618390703575));
#25637=CARTESIAN_POINT('Ctrl Pts',(3.79592667883969,-1.03637886525183,22.1679565655866));
#25638=CARTESIAN_POINT('Ctrl Pts',(3.82420041927633,-0.918683924539212,
22.1740740608157));
#25639=CARTESIAN_POINT('Ctrl Pts',(3.852436873825,-0.801144193583254,22.1801834886211));
#25640=CARTESIAN_POINT('Ctrl Pts',(3.87527950163816,-0.682179314835842,
22.1862929164266));
#25641=CARTESIAN_POINT('Ctrl Pts',(3.89259646878022,-0.56230039235246,22.192402344232));
#25642=CARTESIAN_POINT('Ctrl Pts',(3.90988544907727,-0.442615212387448,
22.1985018982756));
#25643=CARTESIAN_POINT('Ctrl Pts',(3.92166651738104,-0.322019287346637,
22.2046014523193));
#25644=CARTESIAN_POINT('Ctrl Pts',(3.92785872762779,-0.201034364719644,
22.2107010063629));
#25645=CARTESIAN_POINT('Ctrl Pts',(3.93128853963601,-0.13402185643831,22.214079496897));
#25646=CARTESIAN_POINT('Ctrl Pts',(3.93300461466183,-0.0668902083912315,
22.217457987431));
#25647=CARTESIAN_POINT('Ctrl Pts',(3.93299999067836,0.000270784070820302,
22.2208364779651));
#25648=CARTESIAN_POINT('',(3.93299840446441,0.00354266571990603,23.4708364779354));
#25649=CARTESIAN_POINT('Ctrl Pts',(3.93299999067832,0.000270784605066124,
22.220836477992));
#25650=CARTESIAN_POINT('Ctrl Pts',(3.93299155737701,0.122759926744457,22.2269982155136));
#25651=CARTESIAN_POINT('Ctrl Pts',(3.92725664341562,0.245125961169734,22.2331599530353));
#25652=CARTESIAN_POINT('Ctrl Pts',(3.91585532059348,0.366832534243778,22.2393216905569));
#25653=CARTESIAN_POINT('Ctrl Pts',(3.90443577122667,0.488733671608779,22.245493278443));
#25654=CARTESIAN_POINT('Ctrl Pts',(3.88733176944826,0.609972902103853,22.251664866329));
#25655=CARTESIAN_POINT('Ctrl Pts',(3.86465467047957,0.730022792754059,22.2578364542151));
#25656=CARTESIAN_POINT('Ctrl Pts',(3.84191835401055,0.850386173875383,22.264024158184));
#25657=CARTESIAN_POINT('Ctrl Pts',(3.81357990986124,0.969553667335715,22.270211862153));
#25658=CARTESIAN_POINT('Ctrl Pts',(3.77980128216693,1.08701024251347,22.276399566122));
#25659=CARTESIAN_POINT('Ctrl Pts',(3.74597350573815,1.20463771989833,22.2825962733525));
#25660=CARTESIAN_POINT('Ctrl Pts',(3.70668985931787,1.32054898604482,22.288792980583));
#25661=CARTESIAN_POINT('Ctrl Pts',(3.66216074202684,1.43424813040053,22.2949896878135));
#25662=CARTESIAN_POINT('Ctrl Pts',(3.61753022850095,1.5482061764782,22.3012005054243));
#25663=CARTESIAN_POINT('Ctrl Pts',(3.5676305095443,1.65994171853242,22.3074113230352));
#25664=CARTESIAN_POINT('Ctrl Pts',(3.5127188247905,1.76898147473694,22.313622140646));
#25665=CARTESIAN_POINT('Ctrl Pts',(3.50029941521256,1.79364306358919,22.3150268450923));
#25666=CARTESIAN_POINT('Ctrl Pts',(3.48762380453704,1.81816686972331,22.3164315495385));
#25667=CARTESIAN_POINT('Ctrl Pts',(3.47469527424782,1.84254762519722,22.3178362539847));
#25668=CARTESIAN_POINT('Ctrl Pts',(3.42064978961855,1.9444671563223,22.3237083779507));
#25669=CARTESIAN_POINT('Ctrl Pts',(3.36202565092841,2.04417765018982,22.3295805019168));
#25670=CARTESIAN_POINT('Ctrl Pts',(3.29902755825593,2.14123940040994,22.3354526258828));
#25671=CARTESIAN_POINT('Ctrl Pts',(3.23611114386145,2.2381753081437,22.3413171365235));
#25672=CARTESIAN_POINT('Ctrl Pts',(3.16883227587687,2.33246895793777,22.3471816471642));
#25673=CARTESIAN_POINT('Ctrl Pts',(3.0974420233671,2.42370417169248,22.3530461578049));
#25674=CARTESIAN_POINT('Ctrl Pts',(3.02612523071679,2.51484550532008,22.3589046339226));
#25675=CARTESIAN_POINT('Ctrl Pts',(2.95070572158437,2.6029343390167,22.3647631100402));
#25676=CARTESIAN_POINT('Ctrl Pts',(2.87147806343923,2.68758306498372,22.3706215861578));
#25677=CARTESIAN_POINT('Ctrl Pts',(2.78912635378591,2.77556960234407,22.3767110697491));
#25678=CARTESIAN_POINT('Ctrl Pts',(2.70266024364892,2.85983877289532,22.3828005533403));
#25679=CARTESIAN_POINT('Ctrl Pts',(2.61245726978783,2.93999251929877,22.3888900369316));
#25680=CARTESIAN_POINT('Ctrl Pts',(2.52577679221918,3.01701619955865,22.394741721452));
#25681=CARTESIAN_POINT('Ctrl Pts',(2.43564616711387,3.09023954456871,22.4005934059724));
#25682=CARTESIAN_POINT('Ctrl Pts',(2.34243766474219,3.15934720896535,22.4064450904928));
#25683=CARTESIAN_POINT('Ctrl Pts',(2.24924337869324,3.22844433294094,22.4122958825041));
#25684=CARTESIAN_POINT('Ctrl Pts',(2.15297248077749,3.29342677827385,22.4181466745154));
#25685=CARTESIAN_POINT('Ctrl Pts',(2.05402889355913,3.3540206177697,22.4239974665267));
#25686=CARTESIAN_POINT('Ctrl Pts',(1.95507643223784,3.41461989183674,22.4298487832869));
#25687=CARTESIAN_POINT('Ctrl Pts',(1.85345115766835,3.47082956169151,22.435700100047));
#25688=CARTESIAN_POINT('Ctrl Pts',(1.74958381228125,3.52242040134385,22.4415514168072));
#25689=CARTESIAN_POINT('Ctrl Pts',(1.64568199345774,3.57402836392857,22.4474046756117));
#25690=CARTESIAN_POINT('Ctrl Pts',(1.53953699420137,3.62101426426451,22.4532579344162));
#25691=CARTESIAN_POINT('Ctrl Pts',(1.43160119924072,3.66319628280174,22.4591111932207));
#25692=CARTESIAN_POINT('Ctrl Pts',(1.32354260626005,3.70542629161281,22.4649711112489));
#25693=CARTESIAN_POINT('Ctrl Pts',(1.2136895363021,3.74284135935537,22.470831029277));
#25694=CARTESIAN_POINT('Ctrl Pts',(1.10251135909919,3.77530895464957,22.4766909473051));
#25695=CARTESIAN_POINT('Ctrl Pts',(0.991258322447728,3.80779841130489,22.4825548109837));
#25696=CARTESIAN_POINT('Ctrl Pts',(0.878678802537223,3.83533366431226,22.4884186746624));
#25697=CARTESIAN_POINT('Ctrl Pts',(0.765252517596467,3.85783327585735,22.494282538341));
#25698=CARTESIAN_POINT('Ctrl Pts',(0.651658901614758,3.88036607973897,22.5001550526284));
#25699=CARTESIAN_POINT('Ctrl Pts',(0.537216434609229,3.89784835349401,22.5060275669158));
#25700=CARTESIAN_POINT('Ctrl Pts',(0.422410196484637,3.91025045564933,22.5119000812032));
#25701=CARTESIAN_POINT('Ctrl Pts',(0.390680213595296,3.91367813079668,22.5135231182515));
#25702=CARTESIAN_POINT('Ctrl Pts',(0.358922442618301,3.91671806324577,22.5151461552998));
#25703=CARTESIAN_POINT('Ctrl Pts',(0.327147102199838,3.91937032870361,22.5167691923482));
#25704=CARTESIAN_POINT('Ctrl Pts',(0.212184391896045,3.92896618578848,22.5226413163142));
#25705=CARTESIAN_POINT('Ctrl Pts',(0.0966063925621662,3.93351572361829,
22.5285134402802));
#25706=CARTESIAN_POINT('Ctrl Pts',(-0.0191062992359001,3.932953591047,22.5343855642463));
#25707=CARTESIAN_POINT('Ctrl Pts',(-0.134668967231466,3.93239218729176,
22.540250074887));
#25708=CARTESIAN_POINT('Ctrl Pts',(-0.250365570825991,3.92673229458379,
22.5461145855277));
#25709=CARTESIAN_POINT('Ctrl Pts',(-0.365710255764052,3.91596029203936,
22.5519790961684));
#25710=CARTESIAN_POINT('Ctrl Pts',(-0.480936252168838,3.90519937377838,
22.557837572286));
#25711=CARTESIAN_POINT('Ctrl Pts',(-0.595810641049526,3.88933684689757,
22.5636960484036));
#25712=CARTESIAN_POINT('Ctrl Pts',(-0.709848104132318,3.86841112978698,
22.5695545245212));
#25713=CARTESIAN_POINT('Ctrl Pts',(-0.828382215442429,3.84666028393179,
22.5756440081125));
#25714=CARTESIAN_POINT('Ctrl Pts',(-0.946011585860243,3.8194387387382,22.5817334917038));
#25715=CARTESIAN_POINT('Ctrl Pts',(-1.06219727216408,3.78684908004098,22.587822975295));
#25716=CARTESIAN_POINT('Ctrl Pts',(-1.17384581704424,3.75553207286531,22.5936746598154));
#25717=CARTESIAN_POINT('Ctrl Pts',(-1.28416088034208,3.71925846474694,22.5995263443358));
#25718=CARTESIAN_POINT('Ctrl Pts',(-1.39267596188577,3.67817110330468,22.6053780288562));
#25719=CARTESIAN_POINT('Ctrl Pts',(-1.50117449252069,3.63709000857816,22.6112288208675));
#25720=CARTESIAN_POINT('Ctrl Pts',(-1.60787320074576,3.59119676670049,22.6170796128788));
#25721=CARTESIAN_POINT('Ctrl Pts',(-1.71232333412335,3.54068323906795,22.6229304048902));
#25722=CARTESIAN_POINT('Ctrl Pts',(-1.81678283547781,3.49016518095236,22.6287817216503));
#25723=CARTESIAN_POINT('Ctrl Pts',(-1.91899298888386,3.43502619331911,22.6346330384104));
#25724=CARTESIAN_POINT('Ctrl Pts',(-2.01852816331218,3.37550485911597,22.6404843551705));
#25725=CARTESIAN_POINT('Ctrl Pts',(-2.11809637333493,3.31596376985973,22.6463376139751));
#25726=CARTESIAN_POINT('Ctrl Pts',(-2.2149874843791,3.25203765392801,22.6521908727796));
#25727=CARTESIAN_POINT('Ctrl Pts',(-2.30880406080973,3.1840089209656,22.6580441315841));
#25728=CARTESIAN_POINT('Ctrl Pts',(-2.40272737189537,3.11590279205015,22.6639040496122));
#25729=CARTESIAN_POINT('Ctrl Pts',(-2.49356883180296,3.04368497267559,22.6697639676403));
#25730=CARTESIAN_POINT('Ctrl Pts',(-2.58096330021652,2.96767879713008,22.6756238856685));
#25731=CARTESIAN_POINT('Ctrl Pts',(-2.6684166138268,2.89162144445137,22.6814877493471));
#25732=CARTESIAN_POINT('Ctrl Pts',(-2.75241801555635,2.81177094057748,22.6873516130257));
#25733=CARTESIAN_POINT('Ctrl Pts',(-2.83263976556501,2.72848693574659,22.6932154767043));
#25734=CARTESIAN_POINT('Ctrl Pts',(-2.91297986194246,2.6450800669848,22.6990879909917));
#25735=CARTESIAN_POINT('Ctrl Pts',(-2.9895289058162,2.55822989696775,22.7049605052791));
#25736=CARTESIAN_POINT('Ctrl Pts',(-3.06199984378392,2.46832857550757,22.7108330195665));
#25737=CARTESIAN_POINT('Ctrl Pts',(-3.08202925733558,2.44348177764815,22.7124560566149));
#25738=CARTESIAN_POINT('Ctrl Pts',(-3.10174742319807,2.41840208184142,22.7140790936632));
#25739=CARTESIAN_POINT('Ctrl Pts',(-3.12114888345213,2.39309812739168,22.7157021307116));
#25740=CARTESIAN_POINT('Ctrl Pts',(-3.19134307886485,2.30154879553204,22.7215742546776));
#25741=CARTESIAN_POINT('Ctrl Pts',(-3.25762356028316,2.20675496657971,22.7274463786436));
#25742=CARTESIAN_POINT('Ctrl Pts',(-3.31967564925479,2.10908572223719,22.7333185026096));
#25743=CARTESIAN_POINT('Ctrl Pts',(-3.38164728646099,2.01154310800923,22.7391830132504));
#25744=CARTESIAN_POINT('Ctrl Pts',(-3.43940121367192,1.91113283781489,22.7450475238911));
#25745=CARTESIAN_POINT('Ctrl Pts',(-3.49266343946043,1.80825636972649,22.7509120345318));
#25746=CARTESIAN_POINT('Ctrl Pts',(-3.54587085894847,1.70548576050032,22.7567705106494));
#25747=CARTESIAN_POINT('Ctrl Pts',(-3.59459558129651,1.60025436588892,22.762628986767));
#25748=CARTESIAN_POINT('Ctrl Pts',(-3.63860769271482,1.49299131227094,22.7684874628846));
#25749=CARTESIAN_POINT('Ctrl Pts',(-3.68435525998632,1.38149873436446,22.7745769464759));
#25750=CARTESIAN_POINT('Ctrl Pts',(-3.72501067739193,1.26781136328398,22.7806664300671));
#25751=CARTESIAN_POINT('Ctrl Pts',(-3.76036904819388,1.15243812041491,22.7867559136584));
#25752=CARTESIAN_POINT('Ctrl Pts',(-3.79434664711298,1.0415702924214,22.7926075981788));
#25753=CARTESIAN_POINT('Ctrl Pts',(-3.82343301099241,0.929146223501031,
22.7984592826992));
#25754=CARTESIAN_POINT('Ctrl Pts',(-3.84749626548086,0.815635633791727,
22.8043109672196));
#25755=CARTESIAN_POINT('Ctrl Pts',(-3.87155584979993,0.702142356914769,
22.8101617592309));
#25756=CARTESIAN_POINT('Ctrl Pts',(-3.89059376233024,0.587563293061722,
22.8160125512422));
#25757=CARTESIAN_POINT('Ctrl Pts',(-3.90452896091025,0.472379713168461,
22.8218633432536));
#25758=CARTESIAN_POINT('Ctrl Pts',(-3.91846540931746,0.357185802631517,
22.8277146600137));
#25759=CARTESIAN_POINT('Ctrl Pts',(-3.92729818434212,0.24138767871805,22.8335659767738));
#25760=CARTESIAN_POINT('Ctrl Pts',(-3.9309980508903,0.125472402928658,22.839417293534));
#25761=CARTESIAN_POINT('Ctrl Pts',(-3.93469914541935,0.00951865501057846,
22.8452705523385));
#25762=CARTESIAN_POINT('Ctrl Pts',(-3.93326393078135,-0.106551909115038,
22.851123811143));
#25763=CARTESIAN_POINT('Ctrl Pts',(-3.92671528481529,-0.222252271074949,
22.8569770699475));
#25764=CARTESIAN_POINT('Ctrl Pts',(-3.9201591884871,-0.338084264764432,
22.8628369879757));
#25765=CARTESIAN_POINT('Ctrl Pts',(-3.90847807257971,-0.453544802631376,
22.8686969060038));
#25766=CARTESIAN_POINT('Ctrl Pts',(-3.8917467013407,-0.568151927395994,
22.8745568240319));
#25767=CARTESIAN_POINT('Ctrl Pts',(-3.8750040643906,-0.682836220417626,
22.8804206877105));
#25768=CARTESIAN_POINT('Ctrl Pts',(-3.85320447865518,-0.796665551098302,
22.8862845513892));
#25769=CARTESIAN_POINT('Ctrl Pts',(-3.82647347540322,-0.909169809241145,
22.8921484150678));
#25770=CARTESIAN_POINT('Ctrl Pts',(-3.79970303749459,-1.0218400382139,22.8980209293552));
#25771=CARTESIAN_POINT('Ctrl Pts',(-3.76798677530151,-1.1331808971224,22.9038934436426));
#25772=CARTESIAN_POINT('Ctrl Pts',(-3.73149955141773,-1.24273894996869,
22.90976595793));
#25773=CARTESIAN_POINT('Ctrl Pts',(-3.72141526498499,-1.27301844696287,
22.9113889949783));
#25774=CARTESIAN_POINT('Ctrl Pts',(-3.71096682649742,-1.30316189301501,
22.9130120320267));
#25775=CARTESIAN_POINT('Ctrl Pts',(-3.70015855625258,-1.33316002737512,
22.914635069075));
#25776=CARTESIAN_POINT('Ctrl Pts',(-3.66105439482814,-1.44169283252124,
22.920507193041));
#25777=CARTESIAN_POINT('Ctrl Pts',(-3.61710541139586,-1.54868563171709,
22.9263793170071));
#25778=CARTESIAN_POINT('Ctrl Pts',(-3.56845213094431,-1.65367420889334,
22.9322514409731));
#25779=CARTESIAN_POINT('Ctrl Pts',(-3.51986193043693,-1.75852666629462,
22.9381159516138));
#25780=CARTESIAN_POINT('Ctrl Pts',(-3.46657973425234,-1.86137969755053,
22.9439804622545));
#25781=CARTESIAN_POINT('Ctrl Pts',(-3.40879529535231,-1.96178582785786,
22.9498449728952));
#25782=CARTESIAN_POINT('Ctrl Pts',(-3.35107031606503,-2.06208864125602,
22.9557034490129));
#25783=CARTESIAN_POINT('Ctrl Pts',(-3.28885251381717,-2.15994920564847,
22.9615619251305));
#25784=CARTESIAN_POINT('Ctrl Pts',(-3.22237874009185,-2.25494218449256,
22.9674204012481));
#25785=CARTESIAN_POINT('Ctrl Pts',(-3.15328381741511,-2.35368086232342,
22.9735098848393));
#25786=CARTESIAN_POINT('Ctrl Pts',(-3.07959057234699,-2.44932074385276,
22.9795993684306));
#25787=CARTESIAN_POINT('Ctrl Pts',(-3.00161651713321,-2.54141442588041,
22.9856888520219));
#25788=CARTESIAN_POINT('Ctrl Pts',(-2.92668740942658,-2.62991177799109,
22.9915405365423));
#25789=CARTESIAN_POINT('Ctrl Pts',(-2.8478058477608,-2.7151343516762,22.9973922210627));
#25790=CARTESIAN_POINT('Ctrl Pts',(-2.76529581629384,-2.79671737013016,
23.0032439055831));
#25791=CARTESIAN_POINT('Ctrl Pts',(-2.68279836940026,-2.87828794540039,
23.0090946975944));
#25792=CARTESIAN_POINT('Ctrl Pts',(-2.59667384697142,-2.95621977858399,
23.0149454896057));
#25793=CARTESIAN_POINT('Ctrl Pts',(-2.50728341954824,-3.03018462375785,
23.0207962816171));
#25794=CARTESIAN_POINT('Ctrl Pts',(-2.41788497483077,-3.1041561027285,23.0266475983772));
#25795=CARTESIAN_POINT('Ctrl Pts',(-2.32522036136581,-3.17415962283936,
23.0324989151373));
#25796=CARTESIAN_POINT('Ctrl Pts',(-2.22968361594914,-3.23990740188172,
23.0383502318975));
#25797=CARTESIAN_POINT('Ctrl Pts',(-2.13411516201148,-3.30567700252606,
23.044203490702));
#25798=CARTESIAN_POINT('Ctrl Pts',(-2.03567302101211,-3.36718781924102,
23.0500567495065));
#25799=CARTESIAN_POINT('Ctrl Pts',(-1.93477935256286,-3.42419594312248,
23.055910008311));
#25800=CARTESIAN_POINT('Ctrl Pts',(-1.83377089788595,-3.48126892486457,
23.0617699263392));
#25801=CARTESIAN_POINT('Ctrl Pts',(-1.73030570895322,-3.53382878552347,
23.0676298443673));
#25802=CARTESIAN_POINT('Ctrl Pts',(-1.62482972346416,-3.5816780103392,23.0734897623954));
#25803=CARTESIAN_POINT('Ctrl Pts',(-1.51928271797545,-3.6295594534074,23.079353626074));
#25804=CARTESIAN_POINT('Ctrl Pts',(-1.41172260273204,-3.67272379135303,
23.0852174897527));
#25805=CARTESIAN_POINT('Ctrl Pts',(-1.30261277864739,-3.71102262845493,
23.0910813534313));
#25806=CARTESIAN_POINT('Ctrl Pts',(-1.1933419913392,-3.74937796554964,23.0969538677187));
#25807=CARTESIAN_POINT('Ctrl Pts',(-1.0825173266438,-3.78285335718505,23.1028263820061));
#25808=CARTESIAN_POINT('Ctrl Pts',(-0.970614811176123,-3.81135092694513,
23.1086988962935));
#25809=CARTESIAN_POINT('Ctrl Pts',(-0.939687354976457,-3.81922704426804,
23.1103219333418));
#25810=CARTESIAN_POINT('Ctrl Pts',(-0.908677608990547,-3.82672323400713,
23.1119449703901));
#25811=CARTESIAN_POINT('Ctrl Pts',(-0.877595700063661,-3.83383812741615,
23.1135680074385));
#25812=CARTESIAN_POINT('Ctrl Pts',(-0.765141814610189,-3.85957970623339,
23.1194401314045));
#25813=CARTESIAN_POINT('Ctrl Pts',(-0.651365865962822,-3.88041251050641,
23.1253122553705));
#25814=CARTESIAN_POINT('Ctrl Pts',(-0.53673439729216,-3.89620394573531,
23.1311843793366));
#25815=CARTESIAN_POINT('Ctrl Pts',(-0.422251550596726,-3.91197490705489,
23.1370488899773));
#25816=CARTESIAN_POINT('Ctrl Pts',(-0.306915795431205,-3.92271744163368,
23.142913400618));
#25817=CARTESIAN_POINT('Ctrl Pts',(-0.191206188388605,-3.92834942355207,
23.1487779112587));
#25818=CARTESIAN_POINT('Ctrl Pts',(-0.075615645380534,-3.9339756102171,
23.1546363873763));
#25819=CARTESIAN_POINT('Ctrl Pts',(0.040347573900666,-3.9345016840641,23.1604948634939));
#25820=CARTESIAN_POINT('Ctrl Pts',(0.156197591340774,-3.92989711219764,
23.1663533396115));
#25821=CARTESIAN_POINT('Ctrl Pts',(0.276615728427503,-3.9251109759631,23.1724428232028));
#25822=CARTESIAN_POINT('Ctrl Pts',(0.396911101818212,-3.9147811914345,23.1785323067941));
#25823=CARTESIAN_POINT('Ctrl Pts',(0.516535680730075,-3.89893317338637,
23.1846217903853));
#25824=CARTESIAN_POINT('Ctrl Pts',(0.631488826787063,-3.88370403277019,
23.1904734749057));
#25825=CARTESIAN_POINT('Ctrl Pts',(0.745822136886462,-3.86337961302314,
23.1963251594261));
#25826=CARTESIAN_POINT('Ctrl Pts',(0.859053608465656,-3.83803542164245,
23.2021768439465));
#25827=CARTESIAN_POINT('Ctrl Pts',(0.972267809784067,-3.81269509580186,
23.2080276359578));
#25828=CARTESIAN_POINT('Ctrl Pts',(1.08438010340764,-3.78233661090207,23.2138784279692));
#25829=CARTESIAN_POINT('Ctrl Pts',(1.194919131808,-3.74708650399737,23.2197292199805));
#25830=CARTESIAN_POINT('Ctrl Pts',(1.30546807428901,-3.71183323556314,23.2255805367406));
#25831=CARTESIAN_POINT('Ctrl Pts',(1.41444307715141,-3.67168759859444,23.2314318535007));
#25832=CARTESIAN_POINT('Ctrl Pts',(1.52138907152172,-3.62682564966312,23.2372831702608));
#25833=CARTESIAN_POINT('Ctrl Pts',(1.62837056112805,-3.58194881110946,23.2431364290654));
#25834=CARTESIAN_POINT('Ctrl Pts',(1.73332132215207,-3.53235270785558,23.2489896878699));
#25835=CARTESIAN_POINT('Ctrl Pts',(1.83580800645338,-3.47826076702735,23.2548429466744));
#25836=CARTESIAN_POINT('Ctrl Pts',(1.93841128934854,-3.42410728606556,23.2607028647025));
#25837=CARTESIAN_POINT('Ctrl Pts',(2.03854453424144,-3.3654479514241,23.2665627827306));
#25838=CARTESIAN_POINT('Ctrl Pts',(2.1358005825287,-3.30255126707672,23.2724227007588));
#25839=CARTESIAN_POINT('Ctrl Pts',(2.23312211609666,-3.23961223259172,23.2782865644374));
#25840=CARTESIAN_POINT('Ctrl Pts',(2.32756225946827,-3.17243040631849,23.284150428116));
#25841=CARTESIAN_POINT('Ctrl Pts',(2.41874574864515,-3.10131552787055,23.2900142917947));
#25842=CARTESIAN_POINT('Ctrl Pts',(2.51006375539161,-3.03009573787892,23.2958868060821));
#25843=CARTESIAN_POINT('Ctrl Pts',(2.59811520610417,-2.9549315830084,23.3017593203695));
#25844=CARTESIAN_POINT('Ctrl Pts',(2.68256052357107,-2.87617072465772,23.3076318346568));
#25845=CARTESIAN_POINT('Ctrl Pts',(2.70589939889778,-2.85440291196175,23.3092548717052));
#25846=CARTESIAN_POINT('Ctrl Pts',(2.72896305236874,-2.83236056418971,23.3108779087535));
#25847=CARTESIAN_POINT('Ctrl Pts',(2.75174486024572,-2.81005146289374,23.3125009458019));
#25848=CARTESIAN_POINT('Ctrl Pts',(2.83299241800593,-2.73048973513665,23.31828923956));
#25849=CARTESIAN_POINT('Ctrl Pts',(2.91094157765737,-2.6472492831955,23.324077533318));
#25850=CARTESIAN_POINT('Ctrl Pts',(2.98523330806928,-2.56063880631254,23.3298658270761));
#25851=CARTESIAN_POINT('Ctrl Pts',(3.06062220235696,-2.47274923839251,23.3357396041953));
#25852=CARTESIAN_POINT('Ctrl Pts',(3.13224439973583,-2.38138954781217,23.3416133813144));
#25853=CARTESIAN_POINT('Ctrl Pts',(3.19976052377038,-2.28692404563875,23.3474871584335));
#25854=CARTESIAN_POINT('Ctrl Pts',(3.26612798680753,-2.19406569789692,23.353261004184));
#25855=CARTESIAN_POINT('Ctrl Pts',(3.32852770953646,-2.09820673283369,23.3590348499344));
#25856=CARTESIAN_POINT('Ctrl Pts',(3.38667611170226,-1.99972846017284,23.3648086956848));
#25857=CARTESIAN_POINT('Ctrl Pts',(3.44478728086328,-1.90131324413712,23.3705788443839));
#25858=CARTESIAN_POINT('Ctrl Pts',(3.49865232249158,-1.80028241880843,23.3763489930831));
#25859=CARTESIAN_POINT('Ctrl Pts',(3.54803070385407,-1.69704658878558,23.3821191417822));
#25860=CARTESIAN_POINT('Ctrl Pts',(3.59739022699559,-1.59385018581644,23.3878870867894));
#25861=CARTESIAN_POINT('Ctrl Pts',(3.64226631262948,-1.48845083627596,23.3936550317966));
#25862=CARTESIAN_POINT('Ctrl Pts',(3.68246459138356,-1.38128329216214,23.3994229768038));
#25863=CARTESIAN_POINT('Ctrl Pts',(3.72393949884909,-1.27071228979112,23.4053741018981));
#25864=CARTESIAN_POINT('Ctrl Pts',(3.7604343121092,-1.1582593355855,23.4113252269924));
#25865=CARTESIAN_POINT('Ctrl Pts',(3.79178979392339,-1.04442288307871,23.4172763520867));
#25866=CARTESIAN_POINT('Ctrl Pts',(3.82219121830909,-0.934050147499971,
23.4230464015038));
#25867=CARTESIAN_POINT('Ctrl Pts',(3.84776146736264,-0.822377326441574,
23.4288164509209));
#25868=CARTESIAN_POINT('Ctrl Pts',(3.86840682438445,-0.709871566592036,
23.4345865003379));
#25869=CARTESIAN_POINT('Ctrl Pts',(3.89002402022443,-0.592069823506447,
23.4406281632708));
#25870=CARTESIAN_POINT('Ctrl Pts',(3.90624124665246,-0.473355322211236,
23.4466698262037));
#25871=CARTESIAN_POINT('Ctrl Pts',(3.91701169785944,-0.354271589084256,
23.4527114891366));
#25872=CARTESIAN_POINT('Ctrl Pts',(3.92778214906643,-0.235187855957294,
23.4587531520695));
#25873=CARTESIAN_POINT('Ctrl Pts',(3.93310584473272,-0.11573542519944,23.4647948150024));
#25874=CARTESIAN_POINT('Ctrl Pts',(3.93299840446441,0.00354266571993175,
23.4708364779354));
#25875=CARTESIAN_POINT('',(3.93503799677841,-0.00183665550588484,24.720837107935));
#25876=CARTESIAN_POINT('Ctrl Pts',(3.93299840446388,0.00354266630733597,
23.4708364779651));
#25877=CARTESIAN_POINT('Ctrl Pts',(3.93284996998897,0.16833169872891,23.4791833569372));
#25878=CARTESIAN_POINT('Ctrl Pts',(3.92234140402553,0.33267328203265,23.4875302359094));
#25879=CARTESIAN_POINT('Ctrl Pts',(3.90166060312833,0.495513408492938,23.4958771148815));
#25880=CARTESIAN_POINT('Ctrl Pts',(3.88881242960801,0.596679616283066,23.5010627046428));
#25881=CARTESIAN_POINT('Ctrl Pts',(3.87203901721538,0.697267067072719,23.506248294404));
#25882=CARTESIAN_POINT('Ctrl Pts',(3.85139390028725,0.797028245942498,23.5114338841653));
#25883=CARTESIAN_POINT('Ctrl Pts',(3.82801552068602,0.909997076160445,23.5173060081313));
#25884=CARTESIAN_POINT('Ctrl Pts',(3.79962334186979,1.02212582540236,23.5231781320974));
#25885=CARTESIAN_POINT('Ctrl Pts',(3.76629089470118,1.13293508043973,23.5290502560634));
#25886=CARTESIAN_POINT('Ctrl Pts',(3.73300166371219,1.24360066907769,23.5349147667041));
#25887=CARTESIAN_POINT('Ctrl Pts',(3.69478501988862,1.35294977334302,23.5407792773448));
#25888=CARTESIAN_POINT('Ctrl Pts',(3.65176559350328,1.46051259840702,23.5466437879855));
#25889=CARTESIAN_POINT('Ctrl Pts',(3.60879043367972,1.5679647423941,23.5525022641031));
#25890=CARTESIAN_POINT('Ctrl Pts',(3.5610224737937,1.67363388163574,23.5583607402207));
#25891=CARTESIAN_POINT('Ctrl Pts',(3.50863609792483,1.77706548341326,23.5642192163383));
#25892=CARTESIAN_POINT('Ctrl Pts',(3.45418405786262,1.884575530258,23.5703086999296));
#25893=CARTESIAN_POINT('Ctrl Pts',(3.39474201927512,1.98966751547182,23.5763981835209));
#25894=CARTESIAN_POINT('Ctrl Pts',(3.33056110036195,2.09185366523469,23.5824876671121));
#25895=CARTESIAN_POINT('Ctrl Pts',(3.26888649625462,2.19004936636518,23.5883393516325));
#25896=CARTESIAN_POINT('Ctrl Pts',(3.20283642093742,2.28556154038991,23.5941910361529));
#25897=CARTESIAN_POINT('Ctrl Pts',(3.13268007309236,2.37798329675589,23.6000427206733));
#25898=CARTESIAN_POINT('Ctrl Pts',(3.06253442561533,2.47039095679507,23.6058935126847));
#25899=CARTESIAN_POINT('Ctrl Pts',(2.98828400077268,2.55970880718149,23.611744304696));
#25900=CARTESIAN_POINT('Ctrl Pts',(2.9102399717319,2.64556086812114,23.6175950967073));
#25901=CARTESIAN_POINT('Ctrl Pts',(2.8321889430384,2.73142062900427,23.6234464134674));
#25902=CARTESIAN_POINT('Ctrl Pts',(2.7503439118771,2.81381367659168,23.6292977302276));
#25903=CARTESIAN_POINT('Ctrl Pts',(2.66505430473725,2.89239944558172,23.6351490469877));
#25904=CARTESIAN_POINT('Ctrl Pts',(2.57973639008812,2.97101129708591,23.6410023057923));
#25905=CARTESIAN_POINT('Ctrl Pts',(2.4909719300523,3.04581307735935,23.6468555645968));
#25906=CARTESIAN_POINT('Ctrl Pts',(2.3991443902885,3.11650368113808,23.6527088234013));
#25907=CARTESIAN_POINT('Ctrl Pts',(2.30721237878694,3.18727470926707,23.6585687414295));
#25908=CARTESIAN_POINT('Ctrl Pts',(2.2122106596709,3.25392497287027,23.6644286594576));
#25909=CARTESIAN_POINT('Ctrl Pts',(2.11455279276454,3.31619593610084,23.6702885774857));
#25910=CARTESIAN_POINT('Ctrl Pts',(2.0168291700216,3.37850882815302,23.6761524411644));
#25911=CARTESIAN_POINT('Ctrl Pts',(1.91644619551017,3.43643634225192,23.682016304843));
#25912=CARTESIAN_POINT('Ctrl Pts',(1.81384165666068,3.48976610169829,23.6878801685216));
#25913=CARTESIAN_POINT('Ctrl Pts',(1.71108575144737,3.54317453536181,23.693752682809));
#25914=CARTESIAN_POINT('Ctrl Pts',(1.60610211442179,3.59197150357573,23.6996251970964));
#25915=CARTESIAN_POINT('Ctrl Pts',(1.49934816946042,3.63599285845499,23.7054977113838));
#25916=CARTESIAN_POINT('Ctrl Pts',(1.46984366776866,3.64815941717073,23.7071207484321));
#25917=CARTESIAN_POINT('Ctrl Pts',(1.44020402538649,3.65996148504753,23.7087437854805));
#25918=CARTESIAN_POINT('Ctrl Pts',(1.41043907420621,3.67139627634397,23.7103668225288));
#25919=CARTESIAN_POINT('Ctrl Pts',(1.30274992234508,3.71276718164006,23.7162389464948));
#25920=CARTESIAN_POINT('Ctrl Pts',(1.19305845469911,3.74946533077813,23.7221110704609));
#25921=CARTESIAN_POINT('Ctrl Pts',(1.08180780183994,3.78129354584886,23.7279831944269));
#25922=CARTESIAN_POINT('Ctrl Pts',(0.970701387661194,3.81308049500677,23.7338477050676));
#25923=CARTESIAN_POINT('Ctrl Pts',(0.858040202120724,3.84000995362341,23.7397122157083));
#25924=CARTESIAN_POINT('Ctrl Pts',(0.744286893916885,3.86193293825042,23.745576726349));
#25925=CARTESIAN_POINT('Ctrl Pts',(0.630650636735532,3.88383336434435,23.7514352024666));
#25926=CARTESIAN_POINT('Ctrl Pts',(0.515924895647583,3.90073748548579,23.7572936785843));
#25927=CARTESIAN_POINT('Ctrl Pts',(0.400586361530627,3.91254643000638,23.7631521547019));
#25928=CARTESIAN_POINT('Ctrl Pts',(0.280699876231974,3.92482101685196,23.7692416382931));
#25929=CARTESIAN_POINT('Ctrl Pts',(0.160151714701838,3.93159021616368,23.7753311218844));
#25930=CARTESIAN_POINT('Ctrl Pts',(0.0394880013782968,3.93280176181652,
23.7814206054756));
#25931=CARTESIAN_POINT('Ctrl Pts',(-0.0764637000832616,3.93396599566924,
23.787272289996));
#25932=CARTESIAN_POINT('Ctrl Pts',(-0.192521645583175,3.92999848729928,
23.7931239745164));
#25933=CARTESIAN_POINT('Ctrl Pts',(-0.308197999498619,3.92090588934561,
23.7989756590368));
#25934=CARTESIAN_POINT('Ctrl Pts',(-0.423856710255597,3.91181467821076,
23.8048264510481));
#25935=CARTESIAN_POINT('Ctrl Pts',(-0.53913353312224,3.89759996411889,23.8106772430595));
#25936=CARTESIAN_POINT('Ctrl Pts',(-0.653543961262705,3.87832042135472,
23.8165280350708));
#25937=CARTESIAN_POINT('Ctrl Pts',(-0.76796465070406,3.85903914943707,23.8223793518309));
#25938=CARTESIAN_POINT('Ctrl Pts',(-0.88151838325822,3.83469221452669,23.828230668591));
#25939=CARTESIAN_POINT('Ctrl Pts',(-0.993729781228285,3.80538961499345,
23.8340819853512));
#25940=CARTESIAN_POINT('Ctrl Pts',(-1.10597842201484,3.77607728996567,23.8399352441557));
#25941=CARTESIAN_POINT('Ctrl Pts',(-1.21688344254404,3.74180613417956,23.8457885029602));
#25942=CARTESIAN_POINT('Ctrl Pts',(-1.32598427545659,3.70273611012746,23.8516417617647));
#25943=CARTESIAN_POINT('Ctrl Pts',(-1.43520923184712,3.66362163630224,23.8575016797928));
#25944=CARTESIAN_POINT('Ctrl Pts',(-1.5426255142142,3.61969753635932,23.8633615978209));
#25945=CARTESIAN_POINT('Ctrl Pts',(-1.64779211357196,3.57117209756825,23.8692215158491));
#25946=CARTESIAN_POINT('Ctrl Pts',(-1.75302952461081,3.52261398521051,23.8750853795277));
#25947=CARTESIAN_POINT('Ctrl Pts',(-1.85601386997222,3.46944855403648,23.8809492432063));
#25948=CARTESIAN_POINT('Ctrl Pts',(-1.95632988957507,3.41192941942755,23.8868131068849));
#25949=CARTESIAN_POINT('Ctrl Pts',(-2.05679389942559,3.35432543026586,23.8926856211723));
#25950=CARTESIAN_POINT('Ctrl Pts',(-2.1545813792603,3.29235513950045,23.8985581354597));
#25951=CARTESIAN_POINT('Ctrl Pts',(-2.24930704022988,3.2263147457699,23.9044306497471));
#25952=CARTESIAN_POINT('Ctrl Pts',(-2.27548718210084,3.20806259678109,23.9060536867955));
#25953=CARTESIAN_POINT('Ctrl Pts',(-2.30143364910498,3.18949978296568,23.9076767238438));
#25954=CARTESIAN_POINT('Ctrl Pts',(-2.32713878456223,3.17063307201988,23.9092997608922));
#25955=CARTESIAN_POINT('Ctrl Pts',(-2.42013958335605,3.10237359167248,23.9151718848582));
#25956=CARTESIAN_POINT('Ctrl Pts',(-2.51029047652954,3.02990436589693,23.9210440088242));
#25957=CARTESIAN_POINT('Ctrl Pts',(-2.59718610574472,2.95349171864872,23.9269161327903));
#25958=CARTESIAN_POINT('Ctrl Pts',(-2.68396907305125,2.87717814191489,23.932780643431));
#25959=CARTESIAN_POINT('Ctrl Pts',(-2.76750486188798,2.79693158153872,23.9386451540717));
#25960=CARTESIAN_POINT('Ctrl Pts',(-2.847418120176,2.71306082661141,23.9445096647124));
#25961=CARTESIAN_POINT('Ctrl Pts',(-2.92724914851625,2.62927637385654,23.95036814083));
#25962=CARTESIAN_POINT('Ctrl Pts',(-3.00346477711461,2.541875441727,23.9562266169476));
#25963=CARTESIAN_POINT('Ctrl Pts',(-3.07572423237954,2.45120571277755,23.9620850930652));
#25964=CARTESIAN_POINT('Ctrl Pts',(-3.15083297368294,2.35696075631136,23.9681745766565));
#25965=CARTESIAN_POINT('Ctrl Pts',(-3.22166678696586,2.25918421411733,23.9742640602478));
#25966=CARTESIAN_POINT('Ctrl Pts',(-3.28788659622261,2.15830737625106,23.9803535438391));
#25967=CARTESIAN_POINT('Ctrl Pts',(-3.35152047041967,2.06136985736918,23.9862052283595));
#25968=CARTESIAN_POINT('Ctrl Pts',(-3.41089369085765,1.96157001502884,23.9920569128799));
#25969=CARTESIAN_POINT('Ctrl Pts',(-3.46574825447171,1.85932192925978,23.9979085974003));
#25970=CARTESIAN_POINT('Ctrl Pts',(-3.52059445157244,1.75708943854639,24.0037593894116));
#25971=CARTESIAN_POINT('Ctrl Pts',(-3.57092316679509,1.65240981105857,24.0096101814229));
#25972=CARTESIAN_POINT('Ctrl Pts',(-3.61652196896533,1.54572243562393,24.0154609734342));
#25973=CARTESIAN_POINT('Ctrl Pts',(-3.66212486082419,1.43902549155754,24.0213122901944));
#25974=CARTESIAN_POINT('Ctrl Pts',(-3.70299683383611,1.33032082174698,24.0271636069545));
#25975=CARTESIAN_POINT('Ctrl Pts',(-3.73897357596759,1.22006786623373,24.0330149237146));
#25976=CARTESIAN_POINT('Ctrl Pts',(-3.77496225873282,1.10977831790849,24.0388681825192));
#25977=CARTESIAN_POINT('Ctrl Pts',(-3.80605235178819,0.99793985488568,24.0447214413237));
#25978=CARTESIAN_POINT('Ctrl Pts',(-3.83212958773443,0.885026453169818,
24.0505747001282));
#25979=CARTESIAN_POINT('Ctrl Pts',(-3.85823649162303,0.771984590435271,
24.0564346181563));
#25980=CARTESIAN_POINT('Ctrl Pts',(-3.87931906207649,0.657865751077166,
24.0622945361845));
#25981=CARTESIAN_POINT('Ctrl Pts',(-3.89531426250649,0.543153566050663,
24.0681544542126));
#25982=CARTESIAN_POINT('Ctrl Pts',(-3.91132023296269,0.428364142027082,
24.0740183178912));
#25983=CARTESIAN_POINT('Ctrl Pts',(-3.92223197378313,0.312980987391279,
24.0798821815698));
#25984=CARTESIAN_POINT('Ctrl Pts',(-3.92803850271045,0.197490559835831,
24.0857460452485));
#25985=CARTESIAN_POINT('Ctrl Pts',(-3.93385359766398,0.081829756132633,
24.0916185595359));
#25986=CARTESIAN_POINT('Ctrl Pts',(-3.93454844694656,-0.0339382244770866,
24.0974910738233));
#25987=CARTESIAN_POINT('Ctrl Pts',(-3.93016409452121,-0.149329133581845,
24.1033635881107));
#25988=CARTESIAN_POINT('Ctrl Pts',(-3.92895235350687,-0.181220706995479,
24.104986625159));
#25989=CARTESIAN_POINT('Ctrl Pts',(-3.92735294043249,-0.21308352364042,
24.1066096622073));
#25990=CARTESIAN_POINT('Ctrl Pts',(-3.92536741265095,-0.244907483956606,
24.1082326992557));
#25991=CARTESIAN_POINT('Ctrl Pts',(-3.91818380258912,-0.360046100328655,
24.1141048232217));
#25992=CARTESIAN_POINT('Ctrl Pts',(-3.90591799665363,-0.475061413349325,
24.1199769471878));
#25993=CARTESIAN_POINT('Ctrl Pts',(-3.88857505649726,-0.589468430017523,
24.1258490711538));
#25994=CARTESIAN_POINT('Ctrl Pts',(-3.87125460180716,-0.70372711571697,
24.1317135817945));
#25995=CARTESIAN_POINT('Ctrl Pts',(-3.84887016469844,-0.817378668474101,
24.1375780924352));
#25996=CARTESIAN_POINT('Ctrl Pts',(-3.8214787525788,-0.929940397869027,
24.1434426030759));
#25997=CARTESIAN_POINT('Ctrl Pts',(-3.79411552594972,-1.04238630236423,
24.1493010791935));
#25998=CARTESIAN_POINT('Ctrl Pts',(-3.76175566929711,-1.15374421477812,
24.1551595553111));
#25999=CARTESIAN_POINT('Ctrl Pts',(-3.72450760102247,-1.26353952448105,
24.1610180314288));
#26000=CARTESIAN_POINT('Ctrl Pts',(-3.6857907920757,-1.37766420868421,24.16710751502));
#26001=CARTESIAN_POINT('Ctrl Pts',(-3.64179241155865,-1.49010007404528,
24.1731969986113));
#26002=CARTESIAN_POINT('Ctrl Pts',(-3.59269214600665,-1.60032876123068,
24.1792864822025));
#26003=CARTESIAN_POINT('Ctrl Pts',(-3.54550928401644,-1.7062529324416,24.1851381667229));
#26004=CARTESIAN_POINT('Ctrl Pts',(-3.49361570877868,-1.81013866142006,
24.1909898512433));
#26005=CARTESIAN_POINT('Ctrl Pts',(-3.43722043317324,-1.91154510639334,
24.1968415357637));
#26006=CARTESIAN_POINT('Ctrl Pts',(-3.38083375907323,-2.01293608467945,
24.2026923277751));
#26007=CARTESIAN_POINT('Ctrl Pts',(-3.31994695067006,-2.11184816963082,
24.2085431197864));
#26008=CARTESIAN_POINT('Ctrl Pts',(-3.25481494139214,-2.20786519001738,
24.2143939117977));
#26009=CARTESIAN_POINT('Ctrl Pts',(-3.18967709052134,-2.30389082202744,
24.2202452285578));
#26010=CARTESIAN_POINT('Ctrl Pts',(-3.12029351397924,-2.39702053115799,
24.2260965453179));
#26011=CARTESIAN_POINT('Ctrl Pts',(-3.04696201819274,-2.4868678010081,24.2319478620781));
#26012=CARTESIAN_POINT('Ctrl Pts',(-2.97360618377854,-2.57674489104975,
24.2378011208826));
#26013=CARTESIAN_POINT('Ctrl Pts',(-2.8963000859215,-2.66333705542741,24.2436543796871));
#26014=CARTESIAN_POINT('Ctrl Pts',(-2.81538080372033,-2.7462920329133,24.2495076384916));
#26015=CARTESIAN_POINT('Ctrl Pts',(-2.73436946005198,-2.82934138786683,
24.2553675565198));
#26016=CARTESIAN_POINT('Ctrl Pts',(-2.64973701603279,-2.90874500045913,
24.2612274745479));
#26017=CARTESIAN_POINT('Ctrl Pts',(-2.56185635729329,-2.98418850017823,
24.267087392576));
#26018=CARTESIAN_POINT('Ctrl Pts',(-2.47391652599122,-3.05968279816478,
24.2729512562546));
#26019=CARTESIAN_POINT('Ctrl Pts',(-2.38272444948504,-3.13121141931702,
24.2788151199333));
#26020=CARTESIAN_POINT('Ctrl Pts',(-2.28868351938012,-3.19850226639248,
24.2846789836119));
#26021=CARTESIAN_POINT('Ctrl Pts',(-2.19450385629327,-3.26589238364594,
24.2905514978993));
#26022=CARTESIAN_POINT('Ctrl Pts',(-2.09746729692934,-3.32903202489284,
24.2964240121867));
#26023=CARTESIAN_POINT('Ctrl Pts',(-1.99800348616251,-3.38769406370801,
24.302296526474));
#26024=CARTESIAN_POINT('Ctrl Pts',(-1.97051382126889,-3.40390699358242,
24.3039195635224));
#26025=CARTESIAN_POINT('Ctrl Pts',(-1.94283887580368,-3.41977818132064,
24.3055426005707));
#26026=CARTESIAN_POINT('Ctrl Pts',(-1.91498798947108,-3.43530348007007,
24.3071656376191));
#26027=CARTESIAN_POINT('Ctrl Pts',(-1.81422389583779,-3.49147378065549,
24.3130377615851));
#26028=CARTESIAN_POINT('Ctrl Pts',(-1.71081740177547,-3.54330108243971,
24.3189098855511));
#26029=CARTESIAN_POINT('Ctrl Pts',(-1.6051793357273,-3.5905275796398,24.3247820095172));
#26030=CARTESIAN_POINT('Ctrl Pts',(-1.4996782315293,-3.63769284674855,24.3306465201579));
#26031=CARTESIAN_POINT('Ctrl Pts',(-1.39195168295005,-3.68026900439558,
24.3365110307986));
#26032=CARTESIAN_POINT('Ctrl Pts',(-1.28243664971561,-3.71804320032275,
24.3423755414393));
#26033=CARTESIAN_POINT('Ctrl Pts',(-1.17303430636084,-3.75577852697811,
24.3482340175569));
#26034=CARTESIAN_POINT('Ctrl Pts',(-1.06184752732504,-3.78872158614705,
24.3540924936745));
#26035=CARTESIAN_POINT('Ctrl Pts',(-0.949334253474952,-3.81670715082768,
24.3599509697921));
#26036=CARTESIAN_POINT('Ctrl Pts',(-0.832384432198021,-3.8457962233943,
24.3660404533834));
#26037=CARTESIAN_POINT('Ctrl Pts',(-0.714001768480387,-3.86952861136376,
24.3721299369747));
#26038=CARTESIAN_POINT('Ctrl Pts',(-0.594719524752181,-3.88777541620893,
24.3782194205659));
#26039=CARTESIAN_POINT('Ctrl Pts',(-0.480095345423647,-3.90530966913187,
24.3840711050863));
#26040=CARTESIAN_POINT('Ctrl Pts',(-0.364640973395392,-3.91777866331343,
24.3899227896067));
#26041=CARTESIAN_POINT('Ctrl Pts',(-0.248840291004333,-3.92512006307742,
24.3957744741271));
#26042=CARTESIAN_POINT('Ctrl Pts',(-0.133057270734517,-3.93246034311836,
24.4016252661384));
#26043=CARTESIAN_POINT('Ctrl Pts',(-0.0169284575948743,-3.93467455759177,
24.4074760581498));
#26044=CARTESIAN_POINT('Ctrl Pts',(0.0990582118394604,-3.93175234096289,
24.4133268501611));
#26045=CARTESIAN_POINT('Ctrl Pts',(0.215055283945308,-3.92882986224476,
24.4191781669212));
#26046=CARTESIAN_POINT('Ctrl Pts',(0.330909773696594,-3.92077004705018,
24.4250294836813));
#26047=CARTESIAN_POINT('Ctrl Pts',(0.446135531003836,-3.90761462889778,
24.4308808004415));
#26048=CARTESIAN_POINT('Ctrl Pts',(0.561399531589519,-3.89445484447927,
24.436734059246));
#26049=CARTESIAN_POINT('Ctrl Pts',(0.676033974266391,-3.87619614108461,
24.4425873180505));
#26050=CARTESIAN_POINT('Ctrl Pts',(0.78956031178076,-3.85293180760582,24.448440576855));
#26051=CARTESIAN_POINT('Ctrl Pts',(0.903215807647861,-3.82964100640989,
24.4543004948832));
#26052=CARTESIAN_POINT('Ctrl Pts',(1.01576027681901,-3.80133329134225,24.4601604129113));
#26053=CARTESIAN_POINT('Ctrl Pts',(1.12672770689481,-3.76815255457042,24.4660203309394));
#26054=CARTESIAN_POINT('Ctrl Pts',(1.23776985451707,-3.73494947625891,24.471884194618));
#26055=CARTESIAN_POINT('Ctrl Pts',(1.34723245915725,-3.69686697835184,24.4777480582967));
#26056=CARTESIAN_POINT('Ctrl Pts',(1.45466859507815,-3.6540974642849,24.4836119219753));
#26057=CARTESIAN_POINT('Ctrl Pts',(1.56226322513018,-3.61126485490173,24.4894844362627));
#26058=CARTESIAN_POINT('Ctrl Pts',(1.66782504437113,-3.56373159845388,24.4953569505501));
#26059=CARTESIAN_POINT('Ctrl Pts',(1.77093078149554,-3.51173648885442,24.5012294648375));
#26060=CARTESIAN_POINT('Ctrl Pts',(1.79942699675513,-3.49736615528313,24.5028525018858));
#26061=CARTESIAN_POINT('Ctrl Pts',(1.82773577182878,-3.48265525930262,24.5044755389342));
#26062=CARTESIAN_POINT('Ctrl Pts',(1.85584857069332,-3.46760941898818,24.5060985759825));
#26063=CARTESIAN_POINT('Ctrl Pts',(1.9575602599824,-3.41317379190853,24.5119706999485));
#26064=CARTESIAN_POINT('Ctrl Pts',(2.05704538356677,-3.35416800905721,24.5178428239146));
#26065=CARTESIAN_POINT('Ctrl Pts',(2.15386502266241,-3.29079845389405,24.5237149478806));
#26066=CARTESIAN_POINT('Ctrl Pts',(2.25055913317359,-3.22751105861737,24.5295794585213));
#26067=CARTESIAN_POINT('Ctrl Pts',(2.34459428892378,-3.15987136648445,24.535443969162));
#26068=CARTESIAN_POINT('Ctrl Pts',(2.43555527692493,-3.08813203944442,24.5413084798028));
#26069=CARTESIAN_POINT('Ctrl Pts',(2.52642266697425,-3.01646653145829,24.5471669559204));
#26070=CARTESIAN_POINT('Ctrl Pts',(2.61422185855389,-2.9407100337983,24.553025432038));
#26071=CARTESIAN_POINT('Ctrl Pts',(2.69856637544595,-2.86115859702193,24.5588839081556));
#26072=CARTESIAN_POINT('Ctrl Pts',(2.78623670836476,-2.77847034171686,24.5649733917469));
#26073=CARTESIAN_POINT('Ctrl Pts',(2.87017393604567,-2.69168196048493,24.5710628753381));
#26074=CARTESIAN_POINT('Ctrl Pts',(2.94998145073239,-2.60117251260558,24.5771523589294));
#26075=CARTESIAN_POINT('Ctrl Pts',(3.02667241989339,-2.51419752906747,24.5830040434498));
#26076=CARTESIAN_POINT('Ctrl Pts',(3.09954986129521,-2.42378698559456,24.5888557279702));
#26077=CARTESIAN_POINT('Ctrl Pts',(3.16829985836904,-2.33031435807676,24.5947074124906));
#26078=CARTESIAN_POINT('Ctrl Pts',(3.23703936957381,-2.23685598716659,24.6005582045019));
#26079=CARTESIAN_POINT('Ctrl Pts',(3.30165244326281,-2.14033679376242,24.6064089965132));
#26080=CARTESIAN_POINT('Ctrl Pts',(3.36186670201889,-2.04116174710791,24.6122597885245));
#26081=CARTESIAN_POINT('Ctrl Pts',(3.42208636130212,-1.94197780559124,24.6181111052847));
#26082=CARTESIAN_POINT('Ctrl Pts',(3.47790620680963,-1.84013789070516,24.6239624220448));
#26083=CARTESIAN_POINT('Ctrl Pts',(3.52909866476973,-1.73607362007505,24.6298137388049));
#26084=CARTESIAN_POINT('Ctrl Pts',(3.58030811343977,-1.63197481064944,24.6356669976094));
#26085=CARTESIAN_POINT('Ctrl Pts',(3.62688693828793,-1.52565054825737,24.641520256414));
#26086=CARTESIAN_POINT('Ctrl Pts',(3.66865505456452,-1.41755391100946,24.6473735152185));
#26087=CARTESIAN_POINT('Ctrl Pts',(3.71047069022049,-1.3093342927518,24.6532334332466));
#26088=CARTESIAN_POINT('Ctrl Pts',(3.7474645440102,-1.19933866076966,24.6590933512747));
#26089=CARTESIAN_POINT('Ctrl Pts',(3.77950588407603,-1.08803688918835,24.6649532693028));
#26090=CARTESIAN_POINT('Ctrl Pts',(3.81156879849311,-0.976660174938909,
24.6708171329815));
#26091=CARTESIAN_POINT('Ctrl Pts',(3.83867246276346,-0.863975970879195,
24.6766809966601));
#26092=CARTESIAN_POINT('Ctrl Pts',(3.86073727787361,-0.750464303772734,
24.6825448603387));
#26093=CARTESIAN_POINT('Ctrl Pts',(3.88283464389104,-0.636785179665933,
24.6884173746261));
#26094=CARTESIAN_POINT('Ctrl Pts',(3.89987826420005,-0.522276563585091,
24.6942898889135));
#26095=CARTESIAN_POINT('Ctrl Pts',(3.9118403562932,-0.40742364545509,24.7001624032009));
#26096=CARTESIAN_POINT('Ctrl Pts',(3.91514642209276,-0.375680761212693,
24.7017854402493));
#26097=CARTESIAN_POINT('Ctrl Pts',(3.9180646415612,-0.343911574854212,24.7034084772976));
#26098=CARTESIAN_POINT('Ctrl Pts',(3.92059512956118,-0.312126304660715,
24.705031514346));
#26099=CARTESIAN_POINT('Ctrl Pts',(3.92880900465803,-0.208952434920612,
24.7102998355523));
#26100=CARTESIAN_POINT('Ctrl Pts',(3.93295088356075,-0.105450099946497,
24.7155681567587));
#26101=CARTESIAN_POINT('Ctrl Pts',(3.93299956579126,-0.00184810329566231,
24.7208364779651));
#26102=CARTESIAN_POINT('',(3.93141232006596,-0.00268530749238849,25.9708359449846));
#26103=CARTESIAN_POINT('Ctrl Pts',(3.93846800795475,-0.0018173926281477,
24.7208381679678));
#26104=CARTESIAN_POINT('Ctrl Pts',(3.93147080551259,1.20025348547732,24.7818802628817));
#26105=CARTESIAN_POINT('Ctrl Pts',(2.69981664849856,3.72052139417293,24.90923333725));
#26106=CARTESIAN_POINT('Ctrl Pts',(-1.59375568300688,4.37084433553035,25.1028973910729));
#26107=CARTESIAN_POINT('Ctrl Pts',(-4.53899345815125,1.02072316002629,25.3018303294362));
#26108=CARTESIAN_POINT('Ctrl Pts',(-3.3115139775936,-3.26775344216146,25.5007632677998));
#26109=CARTESIAN_POINT('Ctrl Pts',(0.960255309548966,-4.5521694962993,25.6996962061631));
#26110=CARTESIAN_POINT('Ctrl Pts',(3.62962046299946,-2.2676433969507,25.8563867650922));
#26111=CARTESIAN_POINT('Ctrl Pts',(3.93139694366218,-0.479785797299594,
25.9467663445668));
#26112=CARTESIAN_POINT('Ctrl Pts',(3.92843397312147,-0.0027031107579956,
25.9708349445869));
#26113=CARTESIAN_POINT('',(3.93299899378077,0.00281334665823111,27.2208364780115));
#26114=CARTESIAN_POINT('Ctrl Pts',(3.93299908974997,-0.00267582247178204,
25.9708364779651));
#26115=CARTESIAN_POINT('Ctrl Pts',(3.93307847500203,0.114006852631101,25.9767162588663));
#26116=CARTESIAN_POINT('Ctrl Pts',(3.92796099030741,0.230722709585052,25.9825960397676));
#26117=CARTESIAN_POINT('Ctrl Pts',(3.91766444130927,0.346978854256137,25.9884758206688));
#26118=CARTESIAN_POINT('Ctrl Pts',(3.90736771657427,0.463236983134719,25.9943557019235));
#26119=CARTESIAN_POINT('Ctrl Pts',(3.89189178715577,0.579034978138806,26.0002355831782));
#26120=CARTESIAN_POINT('Ctrl Pts',(3.8713063936447,0.693884577235768,26.0061154644329));
#26121=CARTESIAN_POINT('Ctrl Pts',(3.85071584754484,0.808762923548909,26.0119968174403));
#26122=CARTESIAN_POINT('Ctrl Pts',(3.82501336480267,0.922692000596265,26.0178781704478));
#26123=CARTESIAN_POINT('Ctrl Pts',(3.79431978480095,1.03519388071417,26.0237595234553));
#26124=CARTESIAN_POINT('Ctrl Pts',(3.7622230779227,1.15283867383357,26.0299097367415));
#26125=CARTESIAN_POINT('Ctrl Pts',(3.72466825839089,1.26892221175978,26.0360599500277));
#26126=CARTESIAN_POINT('Ctrl Pts',(3.68185120842645,1.38291745198644,26.042210163314));
#26127=CARTESIAN_POINT('Ctrl Pts',(3.64083112684314,1.49212848025882,26.0481022612274));
#26128=CARTESIAN_POINT('Ctrl Pts',(3.59498179423383,1.59942259743108,26.0539943591409));
#26129=CARTESIAN_POINT('Ctrl Pts',(3.54452368503031,1.70435936535085,26.0598864570543));
#26130=CARTESIAN_POINT('Ctrl Pts',(3.49402528304427,1.8093799294024,26.0657832600395));
#26131=CARTESIAN_POINT('Ctrl Pts',(3.43891096727444,1.91203903764287,26.0716800630246));
#26132=CARTESIAN_POINT('Ctrl Pts',(3.37944587868953,2.01192309818451,26.0775768660097));
#26133=CARTESIAN_POINT('Ctrl Pts',(3.31988876348354,2.11196173669468,26.0834827947334));
#26134=CARTESIAN_POINT('Ctrl Pts',(3.25596766160649,2.20921641858616,26.0893887234571));
#26135=CARTESIAN_POINT('Ctrl Pts',(3.18798953366984,2.30330452463663,26.0952946521808));
#26136=CARTESIAN_POINT('Ctrl Pts',(3.17929004416549,2.31534543420437,26.0960504624172));
#26137=CARTESIAN_POINT('Ctrl Pts',(3.17052416165146,2.32733453073281,26.0968062726536));
#26138=CARTESIAN_POINT('Ctrl Pts',(3.16169257377295,2.33927105504022,26.09756208289));
#26139=CARTESIAN_POINT('Ctrl Pts',(3.09307723047327,2.43200961173293,26.103434206856));
#26140=CARTESIAN_POINT('Ctrl Pts',(3.02026309303068,2.52188215266156,26.1093063308221));
#26141=CARTESIAN_POINT('Ctrl Pts',(2.94351803671329,2.60848434297458,26.1151784547881));
#26142=CARTESIAN_POINT('Ctrl Pts',(2.86687248188506,2.69497425182852,26.1210429654288));
#26143=CARTESIAN_POINT('Ctrl Pts',(2.78630641495341,2.77820193549206,26.1269074760696));
#26144=CARTESIAN_POINT('Ctrl Pts',(2.70213006103127,2.85779322787202,26.1327719867103));
#26145=CARTESIAN_POINT('Ctrl Pts',(2.61804032374003,2.93730262160379,26.1386304628279));
#26146=CARTESIAN_POINT('Ctrl Pts',(2.53034798725404,3.01318278436977,26.1444889389455));
#26147=CARTESIAN_POINT('Ctrl Pts',(2.43940203736505,3.08509427734376,26.1503474150631));
#26148=CARTESIAN_POINT('Ctrl Pts',(2.34486996820184,3.15984133574213,26.1564368986544));
#26149=CARTESIAN_POINT('Ctrl Pts',(2.24682272007359,3.23029996503684,26.1625263822456));
#26150=CARTESIAN_POINT('Ctrl Pts',(2.14569287915421,3.29613274434555,26.1686158658369));
#26151=CARTESIAN_POINT('Ctrl Pts',(2.04851223718516,3.35939470241515,26.1744675503573));
#26152=CARTESIAN_POINT('Ctrl Pts',(1.94848561891036,3.41838507004291,26.1803192348777));
#26153=CARTESIAN_POINT('Ctrl Pts',(1.84602808994577,3.4728474327461,26.1861709193981));
#26154=CARTESIAN_POINT('Ctrl Pts',(1.74358618798152,3.5273014887551,26.1920217114094));
#26155=CARTESIAN_POINT('Ctrl Pts',(1.63871447747145,3.57722871901727,26.1978725034208));
#26156=CARTESIAN_POINT('Ctrl Pts',(1.53185315801943,3.62241837758505,26.2037232954321));
#26157=CARTESIAN_POINT('Ctrl Pts',(1.42498225433505,3.6676120891459,26.2095746121922));
#26158=CARTESIAN_POINT('Ctrl Pts',(1.31612176776525,3.70806722331031,26.2154259289523));
#26159=CARTESIAN_POINT('Ctrl Pts',(1.20573176459576,3.74362122975132,26.2212772457125));
#26160=CARTESIAN_POINT('Ctrl Pts',(1.09530512312868,3.77918703652054,26.227130504517));
#26161=CARTESIAN_POINT('Ctrl Pts',(0.983348348942157,3.80984835435143,26.2329837633215));
#26162=CARTESIAN_POINT('Ctrl Pts',(0.870335852415266,3.8354927328833,26.238837022126));
#26163=CARTESIAN_POINT('Ctrl Pts',(0.757194782129486,3.86116628689792,26.2446969401541));
#26164=CARTESIAN_POINT('Ctrl Pts',(0.642995995563217,3.88181141756269,26.2505568581822));
#26165=CARTESIAN_POINT('Ctrl Pts',(0.528223361667081,3.897366941948,26.2564167762103));
#26166=CARTESIAN_POINT('Ctrl Pts',(0.413373448071933,3.91293294031306,26.262280639889));
#26167=CARTESIAN_POINT('Ctrl Pts',(0.297949328490852,3.92340247136169,26.2681445035676));
#26168=CARTESIAN_POINT('Ctrl Pts',(0.182437499127316,3.92876641694466,26.2740083672462));
#26169=CARTESIAN_POINT('Ctrl Pts',(0.0667552620432346,3.93413827563701,
26.2798808815336));
#26170=CARTESIAN_POINT('Ctrl Pts',(-0.0490145312038706,3.93438951556415,
26.285753395821));
#26171=CARTESIAN_POINT('Ctrl Pts',(-0.164387793031487,3.9295630359497,26.2916259101084));
#26172=CARTESIAN_POINT('Ctrl Pts',(-0.196274489116354,3.92822910045904,
26.2932489471568));
#26173=CARTESIAN_POINT('Ctrl Pts',(-0.228130943146756,3.92650760594574,
26.2948719842051));
#26174=CARTESIAN_POINT('Ctrl Pts',(-0.259947061604304,3.92440014845113,
26.2964950212535));
#26175=CARTESIAN_POINT('Ctrl Pts',(-0.375057306247053,3.9167753984961,26.3023671452195));
#26176=CARTESIAN_POINT('Ctrl Pts',(-0.490024774287691,3.90406896245705,
26.3082392691855));
#26177=CARTESIAN_POINT('Ctrl Pts',(-0.60436449568115,3.88628776036465,26.3141113931516));
#26178=CARTESIAN_POINT('Ctrl Pts',(-0.718555973355574,3.86852961195381,
26.3199759037923));
#26179=CARTESIAN_POINT('Ctrl Pts',(-0.832120918180024,3.84570984473732,
26.325840414433));
#26180=CARTESIAN_POINT('Ctrl Pts',(-0.944576861721489,3.8178873152963,26.3317049250737));
#26181=CARTESIAN_POINT('Ctrl Pts',(-1.0569170892158,3.79009341496129,26.3375634011913));
#26182=CARTESIAN_POINT('Ctrl Pts',(-1.16815018633492,3.75730709029601,26.3434218773089));
#26183=CARTESIAN_POINT('Ctrl Pts',(-1.27780196137539,3.7196385775375,26.3492803534266));
#26184=CARTESIAN_POINT('Ctrl Pts',(-1.39177745115417,3.68048474542393,26.3553698370178));
#26185=CARTESIAN_POINT('Ctrl Pts',(-1.50404389635785,3.63605585179664,26.3614593206091));
#26186=CARTESIAN_POINT('Ctrl Pts',(-1.61408362998824,3.58653356814125,26.3675488042003));
#26187=CARTESIAN_POINT('Ctrl Pts',(-1.71982622642744,3.53894516818284,26.3734004887207));
#26188=CARTESIAN_POINT('Ctrl Pts',(-1.82351234490506,3.48665390054298,26.3792521732412));
#26189=CARTESIAN_POINT('Ctrl Pts',(-1.92470194778854,3.42987046580173,26.3851038577616));
#26190=CARTESIAN_POINT('Ctrl Pts',(-2.02587611705805,3.37309569176857,26.3909546497729));
#26191=CARTESIAN_POINT('Ctrl Pts',(-2.12455416740189,3.31183031519004,26.3968054417842));
#26192=CARTESIAN_POINT('Ctrl Pts',(-2.22032090750913,3.24633086232408,26.4026562337955));
#26193=CARTESIAN_POINT('Ctrl Pts',(-2.31609623679267,3.18082553490974,26.4085075505556));
#26194=CARTESIAN_POINT('Ctrl Pts',(-2.40895939552027,3.11108560970418,26.4143588673158));
#26195=CARTESIAN_POINT('Ctrl Pts',(-2.4985250112749,3.03741037201656,26.4202101840759));
#26196=CARTESIAN_POINT('Ctrl Pts',(-2.5881203537406,2.96371068161362,26.4260634428805));
#26197=CARTESIAN_POINT('Ctrl Pts',(-2.67441565788543,2.88607334407477,26.431916701685));
#26198=CARTESIAN_POINT('Ctrl Pts',(-2.75705995670055,2.80483678583235,26.4377699604895));
#26199=CARTESIAN_POINT('Ctrl Pts',(-2.8397982795255,2.72350780515958,26.4436298785177));
#26200=CARTESIAN_POINT('Ctrl Pts',(-2.91887701128125,2.63857172061785,26.4494897965458));
#26201=CARTESIAN_POINT('Ctrl Pts',(-2.99398321260144,2.55040261971728,26.4553497145739));
#26202=CARTESIAN_POINT('Ctrl Pts',(-3.0691399850766,2.46217415203758,26.4612135782526));
#26203=CARTESIAN_POINT('Ctrl Pts',(-3.14031864775177,2.37070865886504,26.4670774419312));
#26204=CARTESIAN_POINT('Ctrl Pts',(-3.20724865111373,2.27641057147632,26.4729413056098));
#26205=CARTESIAN_POINT('Ctrl Pts',(-3.27427739232229,2.18197337173709,26.4788138198972));
#26206=CARTESIAN_POINT('Ctrl Pts',(-3.3370447415629,2.08469558383415,26.4846863341846));
#26207=CARTESIAN_POINT('Ctrl Pts',(-3.39532522040777,1.98500771979932,26.490558848472));
#26208=CARTESIAN_POINT('Ctrl Pts',(-3.41143269528615,1.95745613138677,26.4921818855203));
#26209=CARTESIAN_POINT('Ctrl Pts',(-3.42719772057195,1.92972057326369,26.4938049225686));
#26210=CARTESIAN_POINT('Ctrl Pts',(-3.44261618523127,1.90181040095581,26.4954279596169));
#26211=CARTESIAN_POINT('Ctrl Pts',(-3.49839996166515,1.80083181154012,26.5013000835829));
#26212=CARTESIAN_POINT('Ctrl Pts',(-3.54983064592923,1.69722748276648,26.507172207549));
#26213=CARTESIAN_POINT('Ctrl Pts',(-3.59665200836169,1.59140922793222,26.513044331515));
#26214=CARTESIAN_POINT('Ctrl Pts',(-3.64341266596814,1.48572816856631,26.5189088421557));
#26215=CARTESIAN_POINT('Ctrl Pts',(-3.68557572025949,1.37783926588556,26.5247733527965));
#26216=CARTESIAN_POINT('Ctrl Pts',(-3.72292999489956,1.26818029202363,26.5306378634372));
#26217=CARTESIAN_POINT('Ctrl Pts',(-3.76024583236257,1.15863415615509,26.5364963395548));
#26218=CARTESIAN_POINT('Ctrl Pts',(-3.7927625998516,1.04732196090309,26.5423548156724));
#26219=CARTESIAN_POINT('Ctrl Pts',(-3.8203168263334,0.934702276895635,26.54821329179));
#26220=CARTESIAN_POINT('Ctrl Pts',(-3.84895755246465,0.817641849567875,
26.5543027753813));
#26221=CARTESIAN_POINT('Ctrl Pts',(-3.87223614290353,0.699169116271193,
26.5603922589725));
#26222=CARTESIAN_POINT('Ctrl Pts',(-3.89002574344495,0.579817829439167,
26.5664817425638));
#26223=CARTESIAN_POINT('Ctrl Pts',(-3.90712064624784,0.465127303193612,
26.5723334270842));
#26224=CARTESIAN_POINT('Ctrl Pts',(-3.91914714633136,0.349625999598826,
26.5781851116046));
#26225=CARTESIAN_POINT('Ctrl Pts',(-3.92604476263612,0.233798036299546,
26.584036796125));
#26226=CARTESIAN_POINT('Ctrl Pts',(-3.93294132690444,0.117987739282589,
26.5898875881363));
#26227=CARTESIAN_POINT('Ctrl Pts',(-3.93471053821578,0.00185129419202212,
26.5957383801477));
#26228=CARTESIAN_POINT('Ctrl Pts',(-3.93134390080584,-0.114123326260163,
26.601589172159));
#26229=CARTESIAN_POINT('Ctrl Pts',(-3.92797696144723,-0.230108348303019,
26.6074404889191));
#26230=CARTESIAN_POINT('Ctrl Pts',(-3.91947326968066,-0.34593110359222,
26.6132918056792));
#26231=CARTESIAN_POINT('Ctrl Pts',(-3.90587642156723,-0.461105605523471,
26.6191431224393));
#26232=CARTESIAN_POINT('Ctrl Pts',(-3.89227506067765,-0.576318333721664,
26.6249963812439));
#26233=CARTESIAN_POINT('Ctrl Pts',(-3.87357723061026,-0.690881970396768,
26.6308496400484));
#26234=CARTESIAN_POINT('Ctrl Pts',(-3.84987805328819,-0.804318329276353,
26.6367028988529));
#26235=CARTESIAN_POINT('Ctrl Pts',(-3.82615191352923,-0.917883744140712,
26.642562816881));
#26236=CARTESIAN_POINT('Ctrl Pts',(-3.79741315400567,-1.03031891645989,
26.6484227349091));
#26237=CARTESIAN_POINT('Ctrl Pts',(-3.76380745151309,-1.14115838862735,
26.6542826529373));
#26238=CARTESIAN_POINT('Ctrl Pts',(-3.7301791213393,-1.25207249218336,26.6601465166159));
#26239=CARTESIAN_POINT('Ctrl Pts',(-3.6916774599466,-1.36138836720362,26.6660103802945));
#26240=CARTESIAN_POINT('Ctrl Pts',(-3.64849658190559,-1.46865982849101,
26.6718742439732));
#26241=CARTESIAN_POINT('Ctrl Pts',(-3.60525200168754,-1.57608954097494,
26.6777467582606));
#26242=CARTESIAN_POINT('Ctrl Pts',(-3.5573145983183,-1.68146844544931,26.683619272548));
#26243=CARTESIAN_POINT('Ctrl Pts',(-3.5049247858653,-1.78437418873596,26.6894917868354));
#26244=CARTESIAN_POINT('Ctrl Pts',(-3.49044536488725,-1.81281512998656,
26.6911148238837));
#26245=CARTESIAN_POINT('Ctrl Pts',(-3.47562610224084,-1.84106732744702,
26.692737860932));
#26246=CARTESIAN_POINT('Ctrl Pts',(-3.46047264866876,-1.8691222666844,26.6943608979804));
#26247=CARTESIAN_POINT('Ctrl Pts',(-3.4056476784195,-1.9706246207001,26.7002330219464));
#26248=CARTESIAN_POINT('Ctrl Pts',(-3.34626111779163,-2.06988291325671,
26.7061051459124));
#26249=CARTESIAN_POINT('Ctrl Pts',(-3.28252103059585,-2.16645901962071,
26.7119772698785));
#26250=CARTESIAN_POINT('Ctrl Pts',(-3.2188635836887,-2.26290991314527,26.7178417805192));
#26251=CARTESIAN_POINT('Ctrl Pts',(-3.15086406056417,-2.35668519412911,
26.7237062911599));
#26252=CARTESIAN_POINT('Ctrl Pts',(-3.07877671234571,-2.44737062079239,
26.7295708018006));
#26253=CARTESIAN_POINT('Ctrl Pts',(-3.00676354129123,-2.53796273305405,
26.7354292779182));
#26254=CARTESIAN_POINT('Ctrl Pts',(-2.93067116743927,-2.62547099335779,
26.7412877540358));
#26255=CARTESIAN_POINT('Ctrl Pts',(-2.85079712008848,-2.70951006274109,
26.7471462301535));
#26256=CARTESIAN_POINT('Ctrl Pts',(-2.76777353324691,-2.79686290395104,
26.7532357137447));
#26257=CARTESIAN_POINT('Ctrl Pts',(-2.6806641552376,-2.88046695630763,26.759325197336));
#26258=CARTESIAN_POINT('Ctrl Pts',(-2.58984956229417,-2.95992706746039,
26.7654146809272));
#26259=CARTESIAN_POINT('Ctrl Pts',(-2.50258134984409,-3.03628419946566,
26.7712663654476));
#26260=CARTESIAN_POINT('Ctrl Pts',(-2.41189221550556,-3.10881466719656,
26.777118049968));
#26261=CARTESIAN_POINT('Ctrl Pts',(-2.31815683530432,-3.17720598748836,
26.7829697344884));
#26262=CARTESIAN_POINT('Ctrl Pts',(-2.22443575178617,-3.24558687661714,
26.7888205264998));
#26263=CARTESIAN_POINT('Ctrl Pts',(-2.127669680089,-3.30982962994569,26.7946713185111));
#26264=CARTESIAN_POINT('Ctrl Pts',(-2.02826463018977,-3.36966342383348,
26.8005221105224));
#26265=CARTESIAN_POINT('Ctrl Pts',(-1.9288506647999,-3.42950258412498,26.8063734272825));
#26266=CARTESIAN_POINT('Ctrl Pts',(-1.8267976049172,-3.48493178567996,26.8122247440426));
#26267=CARTESIAN_POINT('Ctrl Pts',(-1.72253793702434,-3.5357251102867,26.8180760608027));
#26268=CARTESIAN_POINT('Ctrl Pts',(-1.61824366548384,-3.58653529313157,
26.8239293196072));
#26269=CARTESIAN_POINT('Ctrl Pts',(-1.51174170111969,-3.63270635857308,
26.8297825784117));
#26270=CARTESIAN_POINT('Ctrl Pts',(-1.403485808772,-3.674059959306,26.8356358372163));
#26271=CARTESIAN_POINT('Ctrl Pts',(-1.29510675423073,-3.71546060782604,
26.8414957552444));
#26272=CARTESIAN_POINT('Ctrl Pts',(-1.18497017529506,-3.75203270448054,
26.8473556732725));
#26273=CARTESIAN_POINT('Ctrl Pts',(-1.07354644358413,-3.78364731885358,
26.8532155913006));
#26274=CARTESIAN_POINT('Ctrl Pts',(-0.96204768708606,-3.81528322025118,
26.8590794549792));
#26275=CARTESIAN_POINT('Ctrl Pts',(-0.849260453424433,-3.84195489782017,
26.8649433186578));
#26276=CARTESIAN_POINT('Ctrl Pts',(-0.735665070849243,-3.86358459251669,
26.8708071823365));
#26277=CARTESIAN_POINT('Ctrl Pts',(-0.621902107773086,-3.88524619621331,
26.8766796966238));
#26278=CARTESIAN_POINT('Ctrl Pts',(-0.50732902395214,-3.90185091282406,
26.8825522109112));
#26279=CARTESIAN_POINT('Ctrl Pts',(-0.392431112207346,-3.91337281921512,
26.8884247251986));
#26280=CARTESIAN_POINT('Ctrl Pts',(-0.360675792693863,-3.91655722712381,
26.890047762247));
#26281=CARTESIAN_POINT('Ctrl Pts',(-0.328895657422063,-3.91935369076328,
26.8916707992954));
#26282=CARTESIAN_POINT('Ctrl Pts',(-0.297100924157858,-3.92176236415015,
26.8932938363438));
#26283=CARTESIAN_POINT('Ctrl Pts',(-0.182068050828945,-3.93047690873525,
26.8991659603098));
#26284=CARTESIAN_POINT('Ctrl Pts',(-0.0664585796196782,-3.93414056691308,
26.9050380842759));
#26285=CARTESIAN_POINT('Ctrl Pts',(0.0492464061907849,-3.93269167256693,
26.9109102082419));
#26286=CARTESIAN_POINT('Ctrl Pts',(0.164801378189231,-3.93124465674108,
26.9167747188826));
#26287=CARTESIAN_POINT('Ctrl Pts',(0.280451208963498,-3.9246982752529,26.9226392295233));
#26288=CARTESIAN_POINT('Ctrl Pts',(0.395709954140458,-3.91304263102182,
26.928503740164));
#26289=CARTESIAN_POINT('Ctrl Pts',(0.510850099215764,-3.90139898033264,
26.9343622162816));
#26290=CARTESIAN_POINT('Ctrl Pts',(0.625599550294334,-3.88465656542435,
26.9402206923992));
#26291=CARTESIAN_POINT('Ctrl Pts',(0.739473297778224,-3.86285752285442,
26.9460791685168));
#26292=CARTESIAN_POINT('Ctrl Pts',(0.857837237966352,-3.84019891516022,
26.9521686521081));
#26293=CARTESIAN_POINT('Ctrl Pts',(0.975254538461258,-3.8120767023719,26.9582581356994));
#26294=CARTESIAN_POINT('Ctrl Pts',(1.09118705804687,-3.77859759756858,26.9643476192907));
#26295=CARTESIAN_POINT('Ctrl Pts',(1.20259232256616,-3.74642587784908,26.9701993038111));
#26296=CARTESIAN_POINT('Ctrl Pts',(1.31262615914816,-3.70930792204054,26.9760509883315));
#26297=CARTESIAN_POINT('Ctrl Pts',(1.42082317605036,-3.6673901486477,26.9819026728519));
#26298=CARTESIAN_POINT('Ctrl Pts',(1.52900369055571,-3.62547876862642,26.9877534648632));
#26299=CARTESIAN_POINT('Ctrl Pts',(1.63534755702998,-3.57876917592524,26.9936042568745));
#26300=CARTESIAN_POINT('Ctrl Pts',(1.73940750656672,-3.52745666537512,26.9994550488859));
#26301=CARTESIAN_POINT('Ctrl Pts',(1.84347678908511,-3.47613955268247,27.005306365646));
#26302=CARTESIAN_POINT('Ctrl Pts',(1.9452613766542,-3.42021888432176,27.0111576824061));
#26303=CARTESIAN_POINT('Ctrl Pts',(2.04433747915318,-3.35993649810969,27.0170089991663));
#26304=CARTESIAN_POINT('Ctrl Pts',(2.14344646488121,-3.29963410425235,27.0228622579708));
#26305=CARTESIAN_POINT('Ctrl Pts',(2.23984482506121,-3.23496732876364,27.0287155167753));
#26306=CARTESIAN_POINT('Ctrl Pts',(2.33313730000996,-3.16622161879143,27.0345687755799));
#26307=CARTESIAN_POINT('Ctrl Pts',(2.42653591334601,-3.09739769716502,27.040428693608));
#26308=CARTESIAN_POINT('Ctrl Pts',(2.51682125556585,-3.02448582396451,27.0462886116361));
#26309=CARTESIAN_POINT('Ctrl Pts',(2.60363067498782,-2.94781212228027,27.0521485296642));
#26310=CARTESIAN_POINT('Ctrl Pts',(2.6904985456762,-2.87108679399842,27.0580123933428));
#26311=CARTESIAN_POINT('Ctrl Pts',(2.77388553657727,-2.79059488005739,27.0638762570215));
#26312=CARTESIAN_POINT('Ctrl Pts',(2.85346667369858,-2.70669853180799,27.0697401207001));
#26313=CARTESIAN_POINT('Ctrl Pts',(2.9331652121309,-2.62267841627367,27.0756126349875));
#26314=CARTESIAN_POINT('Ctrl Pts',(3.00904642122963,-2.53524415379178,27.0814851492749));
#26315=CARTESIAN_POINT('Ctrl Pts',(3.08082626130985,-2.44479008252724,27.0873576635623));
#26316=CARTESIAN_POINT('Ctrl Pts',(3.10066467022153,-2.41979051647267,27.0889807006106));
#26317=CARTESIAN_POINT('Ctrl Pts',(3.12019005574241,-2.39456044459457,27.090603737659));
#26318=CARTESIAN_POINT('Ctrl Pts',(3.13939702632185,-2.36910854777097,27.0922267747073));
#26319=CARTESIAN_POINT('Ctrl Pts',(3.20911987562503,-2.27671611350491,27.098118529842));
#26320=CARTESIAN_POINT('Ctrl Pts',(3.27487913500775,-2.1810861430357,27.1040102849767));
#26321=CARTESIAN_POINT('Ctrl Pts',(3.33636043504248,-2.08259166604573,27.1099020401115));
#26322=CARTESIAN_POINT('Ctrl Pts',(3.39776198835946,-1.98422494515806,27.1157861531154));
#26323=CARTESIAN_POINT('Ctrl Pts',(3.45489640044684,-1.88300144883806,27.1216702661194));
#26324=CARTESIAN_POINT('Ctrl Pts',(3.50749003621119,-1.77932645848906,27.1275543791234));
#26325=CARTESIAN_POINT('Ctrl Pts',(3.5600278986247,-1.6757614111308,27.1334322522716));
#26326=CARTESIAN_POINT('Ctrl Pts',(3.60803437707639,-1.56975040247509,27.1393101254199));
#26327=CARTESIAN_POINT('Ctrl Pts',(3.65127995366219,-1.46172627395988,27.1451879985681));
#26328=CARTESIAN_POINT('Ctrl Pts',(3.69448990082282,-1.35379114501196,27.151061029019));
#26329=CARTESIAN_POINT('Ctrl Pts',(3.73294659751401,-1.24384657418048,27.1569340594698));
#26330=CARTESIAN_POINT('Ctrl Pts',(3.76646746973821,-1.13234791446968,27.1628070899207));
#26331=CARTESIAN_POINT('Ctrl Pts',(3.79996911840911,-1.02091319702189,27.1686767523054));
#26332=CARTESIAN_POINT('Ctrl Pts',(3.82854045758789,-0.907926555425226,
27.1745464146902));
#26333=CARTESIAN_POINT('Ctrl Pts',(3.85204808511485,-0.793860535587355,
27.1804160770749));
#26334=CARTESIAN_POINT('Ctrl Pts',(3.87554802275477,-0.679831829374881,
27.1862838193577));
#26335=CARTESIAN_POINT('Ctrl Pts',(3.8939874643854,-0.564724848579951,27.1921515616405));
#26336=CARTESIAN_POINT('Ctrl Pts',(3.90728379265852,-0.449023789601447,
27.1980193039234));
#26337=CARTESIAN_POINT('Ctrl Pts',(3.92058067173715,-0.333317937662134,
27.2038872892797));
#26338=CARTESIAN_POINT('Ctrl Pts',(3.92873396285781,-0.217018364804437,
27.209755274636));
#26339=CARTESIAN_POINT('Ctrl Pts',(3.93171279971712,-0.100615409061179,
27.2156232599923));
#26340=CARTESIAN_POINT('Ctrl Pts',(3.93259494949029,-0.0661439539747947,
27.2173609993165));
#26341=CARTESIAN_POINT('Ctrl Pts',(3.93302365566106,-0.0316634505085527,
27.2190987386408));
#26342=CARTESIAN_POINT('Ctrl Pts',(3.93299899378143,0.00281334573800123,
27.2208364779651));
#26343=CARTESIAN_POINT('',(3.93453844469968,0.00164832279441522,28.470836477965));
#26344=CARTESIAN_POINT('Ctrl Pts',(3.93299899378077,0.00281334665823557,
27.2208364780115));
#26345=CARTESIAN_POINT('Ctrl Pts',(3.93290389767504,0.13575568673146,27.2275371914582));
#26346=CARTESIAN_POINT('Ctrl Pts',(3.92606429430853,0.268428158309364,27.2342379049049));
#26347=CARTESIAN_POINT('Ctrl Pts',(3.91258595467795,0.400200134004008,27.2409386183516));
#26348=CARTESIAN_POINT('Ctrl Pts',(3.89903939087984,0.532639108275039,27.247673249225));
#26349=CARTESIAN_POINT('Ctrl Pts',(3.87878683003275,0.664168293236512,27.2544078800984));
#26350=CARTESIAN_POINT('Ctrl Pts',(3.85198507497447,0.794166218227581,27.2611425109719));
#26351=CARTESIAN_POINT('Ctrl Pts',(3.82501742566897,0.9249687885809,27.2679188270453));
#26352=CARTESIAN_POINT('Ctrl Pts',(3.79141935239508,1.05422093329518,27.2746951431186));
#26353=CARTESIAN_POINT('Ctrl Pts',(3.75139889804151,1.18131084299305,27.281471459192));
#26354=CARTESIAN_POINT('Ctrl Pts',(3.73232617878847,1.24187862531122,27.2847008771516));
#26355=CARTESIAN_POINT('Ctrl Pts',(3.71179548391274,1.30195563851191,27.2879302951111));
#26356=CARTESIAN_POINT('Ctrl Pts',(3.68983306351289,1.36147749280225,27.2911597130706));
#26357=CARTESIAN_POINT('Ctrl Pts',(3.64989829607238,1.46970743128063,27.2970318370366));
#26358=CARTESIAN_POINT('Ctrl Pts',(3.60513065091982,1.57636028015,27.3029039610027));
#26359=CARTESIAN_POINT('Ctrl Pts',(3.55567420649342,1.68097291390355,27.3087760849687));
#26360=CARTESIAN_POINT('Ctrl Pts',(3.50628188332928,1.78544991530014,27.3146405956094));
#26361=CARTESIAN_POINT('Ctrl Pts',(3.45221302511836,1.88789159158712,27.3205051062501));
#26362=CARTESIAN_POINT('Ctrl Pts',(3.39366080852772,1.98785193529673,27.3263696168908));
#26363=CARTESIAN_POINT('Ctrl Pts',(3.33516884158535,2.08770942080729,27.3322280930084));
#26364=CARTESIAN_POINT('Ctrl Pts',(3.27220290009074,2.18509029773616,27.338086569126));
#26365=CARTESIAN_POINT('Ctrl Pts',(3.20500308818995,2.27957105717125,27.3439450452436));
#26366=CARTESIAN_POINT('Ctrl Pts',(3.13515349869065,2.37777731810346,27.3500345288349));
#26367=CARTESIAN_POINT('Ctrl Pts',(3.06072946983643,2.47284963393061,27.3561240124261));
#26368=CARTESIAN_POINT('Ctrl Pts',(2.98205193327776,2.56434304788466,27.3622134960174));
#26369=CARTESIAN_POINT('Ctrl Pts',(2.90644681572012,2.65226357285671,27.3680651805378));
#26370=CARTESIAN_POINT('Ctrl Pts',(2.82691445693365,2.73687912545882,27.3739168650582));
#26371=CARTESIAN_POINT('Ctrl Pts',(2.74378162707361,2.81782742248941,27.3797685495786));
#26372=CARTESIAN_POINT('Ctrl Pts',(2.66066147677713,2.89876337314518,27.3856193415899));
#26373=CARTESIAN_POINT('Ctrl Pts',(2.57394224340042,2.97603289203518,27.3914701336012));
#26374=CARTESIAN_POINT('Ctrl Pts',(2.48398760243081,3.04931051074994,27.3973209256125));
#26375=CARTESIAN_POINT('Ctrl Pts',(2.39402489356355,3.12259470162508,27.4031722423727));
#26376=CARTESIAN_POINT('Ctrl Pts',(2.3008265207982,3.19188601948212,27.4090235591328));
#26377=CARTESIAN_POINT('Ctrl Pts',(2.20478871481325,3.25689971031227,27.4148748758929));
#26378=CARTESIAN_POINT('Ctrl Pts',(2.10871903400574,3.32193497910162,27.4207281346974));
#26379=CARTESIAN_POINT('Ctrl Pts',(2.00980838823359,3.38268956617475,27.426581393502));
#26380=CARTESIAN_POINT('Ctrl Pts',(1.90848079393706,3.43892280506169,27.4324346523065));
#26381=CARTESIAN_POINT('Ctrl Pts',(1.80703791973774,3.49522002022634,27.4382945703346));
#26382=CARTESIAN_POINT('Ctrl Pts',(1.70317297027915,3.54698541935836,27.4441544883627));
#26383=CARTESIAN_POINT('Ctrl Pts',(1.59733338384377,3.59402491099578,27.4500144063908));
#26384=CARTESIAN_POINT('Ctrl Pts',(1.49142253258587,3.64109607566911,27.4558782700695));
#26385=CARTESIAN_POINT('Ctrl Pts',(1.38353478079886,3.68343484603094,27.4617421337481));
#26386=CARTESIAN_POINT('Ctrl Pts',(1.27413465303661,3.72089638204711,27.4676059974267));
#26387=CARTESIAN_POINT('Ctrl Pts',(1.16457313378301,3.75841318283573,27.4734785117141));
#26388=CARTESIAN_POINT('Ctrl Pts',(1.05349518082869,3.79103827314113,27.4793510260015));
#26389=CARTESIAN_POINT('Ctrl Pts',(0.941377556897401,3.81867742750941,27.4852235402889));
#26390=CARTESIAN_POINT('Ctrl Pts',(0.910390649328914,3.82631629722186,27.4868465773373));
#26391=CARTESIAN_POINT('Ctrl Pts',(0.879324366011928,3.83357461986963,27.4884696143857));
#26392=CARTESIAN_POINT('Ctrl Pts',(0.848188843983882,3.84045110435497,27.4900926514341));
#26393=CARTESIAN_POINT('Ctrl Pts',(0.735540987129564,3.86533012322183,27.4959647754001));
#26394=CARTESIAN_POINT('Ctrl Pts',(0.621608724895579,3.8852903799034,27.5018368993662));
#26395=CARTESIAN_POINT('Ctrl Pts',(0.506859602906102,3.90020285920385,27.5077090233322));
#26396=CARTESIAN_POINT('Ctrl Pts',(0.392259255431717,3.91509600417878,27.5135735339729));
#26397=CARTESIAN_POINT('Ctrl Pts',(0.276844560493442,3.92495433370982,27.5194380446137));
#26398=CARTESIAN_POINT('Ctrl Pts',(0.161095189998294,3.92969939559751,27.5253025552544));
#26399=CARTESIAN_POINT('Ctrl Pts',(0.0454649244538145,3.93443957486372,
27.531161031372));
#26400=CARTESIAN_POINT('Ctrl Pts',(-0.070498921085112,3.93407693503176,
27.5370195074896));
#26401=CARTESIAN_POINT('Ctrl Pts',(-0.186310248779996,3.9285846676888,27.5428779836072));
#26402=CARTESIAN_POINT('Ctrl Pts',(-0.306688170533229,3.92287583296928,
27.5489674671985));
#26403=CARTESIAN_POINT('Ctrl Pts',(-0.426900847772791,3.91162445356488,
27.5550569507898));
#26404=CARTESIAN_POINT('Ctrl Pts',(-0.546400460578536,3.89486014340433,
27.561146434381));
#26405=CARTESIAN_POINT('Ctrl Pts',(-0.661233520553275,3.8787504925954,27.5669981189014));
#26406=CARTESIAN_POINT('Ctrl Pts',(-0.775407714481389,3.85755046247169,
27.5728498034218));
#26407=CARTESIAN_POINT('Ctrl Pts',(-0.888441632615616,3.83133925219828,
27.5787014879423));
#26408=CARTESIAN_POINT('Ctrl Pts',(-1.00145831062031,3.8051320397042,27.5845522799536));
#26409=CARTESIAN_POINT('Ctrl Pts',(-1.11333465601668,3.77391526011764,27.5904030719649));
#26410=CARTESIAN_POINT('Ctrl Pts',(-1.22360029485032,3.73781905908274,27.5962538639762));
#26411=CARTESIAN_POINT('Ctrl Pts',(-1.33387582324482,3.70171962063336,27.6021051807364));
#26412=CARTESIAN_POINT('Ctrl Pts',(-1.44253996497987,3.66074001939631,27.6079564974965));
#26413=CARTESIAN_POINT('Ctrl Pts',(-1.54913901377649,3.615059794249,27.6138078142567));
#26414=CARTESIAN_POINT('Ctrl Pts',(-1.65577344265825,3.56936440789458,27.6196610730612));
#26415=CARTESIAN_POINT('Ctrl Pts',(-1.76034103593322,3.51896545816114,27.6255143318657));
#26416=CARTESIAN_POINT('Ctrl Pts',(-1.86241017044761,3.46408968662956,27.6313675906703));
#26417=CARTESIAN_POINT('Ctrl Pts',(-1.9645954285115,3.40915148320413,27.6372275086984));
#26418=CARTESIAN_POINT('Ctrl Pts',(-2.0642761899507,3.34972648785435,27.6430874267265));
#26419=CARTESIAN_POINT('Ctrl Pts',(-2.16104736583126,3.28608631697857,27.6489473447546));
#26420=CARTESIAN_POINT('Ctrl Pts',(-2.25788370051402,3.22240329535443,27.6548112084333));
#26421=CARTESIAN_POINT('Ctrl Pts',(-2.35180621446453,3.1544996884199,27.6606750721119));
#26422=CARTESIAN_POINT('Ctrl Pts',(-2.4424420284316,3.08268810257394,27.6665389357906));
#26423=CARTESIAN_POINT('Ctrl Pts',(-2.53321155201563,3.01077057737337,27.672411450078));
#26424=CARTESIAN_POINT('Ctrl Pts',(-2.62068438737155,2.93493383677337,27.6782839643654));
#26425=CARTESIAN_POINT('Ctrl Pts',(-2.70452363160501,2.85552813435449,27.6841564786528));
#26426=CARTESIAN_POINT('Ctrl Pts',(-2.72769500128213,2.83358210058424,27.685779515701));
#26427=CARTESIAN_POINT('Ctrl Pts',(-2.75058905325276,2.81136364899612,27.6874025527493));
#26428=CARTESIAN_POINT('Ctrl Pts',(-2.77319922360805,2.78888061167554,27.6890255897975));
#26429=CARTESIAN_POINT('Ctrl Pts',(-2.85500248457678,2.70753731614063,27.6948977137635));
#26430=CARTESIAN_POINT('Ctrl Pts',(-2.93336091890663,2.62245542621175,27.7007698377296));
#26431=CARTESIAN_POINT('Ctrl Pts',(-3.00791333059858,2.53395864125825,27.7066419616956));
#26432=CARTESIAN_POINT('Ctrl Pts',(-3.08236908360846,2.44557659414363,27.7125064723363));
#26433=CARTESIAN_POINT('Ctrl Pts',(-3.15302836318535,2.35378876990502,27.718370982977));
#26434=CARTESIAN_POINT('Ctrl Pts',(-3.21956596674014,2.25895639307372,27.7242354936178));
#26435=CARTESIAN_POINT('Ctrl Pts',(-3.28603510376284,2.16422159781471,27.7300939697354));
#26436=CARTESIAN_POINT('Ctrl Pts',(-3.34839076462158,2.06644881766277,27.735952445853));
#26437=CARTESIAN_POINT('Ctrl Pts',(-3.40634772973127,1.96603258979973,27.7418109219706));
#26438=CARTESIAN_POINT('Ctrl Pts',(-3.46659001474695,1.86165681705737,27.7479004055619));
#26439=CARTESIAN_POINT('Ctrl Pts',(-3.52207928141067,1.75442518649659,27.7539898891531));
#26440=CARTESIAN_POINT('Ctrl Pts',(-3.57254443486776,1.644814658524,27.7600793727444));
#26441=CARTESIAN_POINT('Ctrl Pts',(-3.62103888482874,1.53948450692773,27.7659310572648));
#26442=CARTESIAN_POINT('Ctrl Pts',(-3.66489406001013,1.43195817784432,27.7717827417852));
#26443=CARTESIAN_POINT('Ctrl Pts',(-3.70391647323494,1.32268354465414,27.7776344263056));
#26444=CARTESIAN_POINT('Ctrl Pts',(-3.7429329346935,1.21342557822086,27.7834852183169));
#26445=CARTESIAN_POINT('Ctrl Pts',(-3.77711796078971,1.10242022709867,27.7893360103283));
#26446=CARTESIAN_POINT('Ctrl Pts',(-3.80632689601003,0.990133607504907,
27.7951868023396));
#26447=CARTESIAN_POINT('Ctrl Pts',(-3.83553845093623,0.877836917091518,
27.8010381190997));
#26448=CARTESIAN_POINT('Ctrl Pts',(-3.85977292370389,0.764259129887349,
27.8068894358599));
#26449=CARTESIAN_POINT('Ctrl Pts',(-3.87893622667187,0.649879026752366,
27.81274075262));
#26450=CARTESIAN_POINT('Ctrl Pts',(-3.89810588991509,0.535460961010476,
27.8185940114245));
#26451=CARTESIAN_POINT('Ctrl Pts',(-3.91220096831981,0.420240457356516,
27.8244472702291));
#26452=CARTESIAN_POINT('Ctrl Pts',(-3.92117902514,0.304703220859408,27.8303005290336));
#26453=CARTESIAN_POINT('Ctrl Pts',(-3.93016729625104,0.189034538219762,
27.8361604470617));
#26454=CARTESIAN_POINT('Ctrl Pts',(-3.93402689395027,0.0730488159131875,
27.8420203650898));
#26455=CARTESIAN_POINT('Ctrl Pts',(-3.93276747874505,-0.0427663199875365,
27.847880283118));
#26456=CARTESIAN_POINT('Ctrl Pts',(-3.93150721553953,-0.158659437533726,
27.8537441467966));
#26457=CARTESIAN_POINT('Ctrl Pts',(-3.92512109894429,-0.274381328186647,
27.8596080104752));
#26458=CARTESIAN_POINT('Ctrl Pts',(-3.91367068459627,-0.389449319593444,
27.8654718741539));
#26459=CARTESIAN_POINT('Ctrl Pts',(-3.90220337813408,-0.504687063953107,
27.8713443884413));
#26460=CARTESIAN_POINT('Ctrl Pts',(-3.88565692194286,-0.619268576150767,
27.8772169027287));
#26461=CARTESIAN_POINT('Ctrl Pts',(-3.86414398931519,-0.732721113275251,
27.8830894170161));
#26462=CARTESIAN_POINT('Ctrl Pts',(-3.85819827595229,-0.764076962229491,
27.8847124540644));
#26463=CARTESIAN_POINT('Ctrl Pts',(-3.85187349085219,-0.795346664820355,
27.8863354911127));
#26464=CARTESIAN_POINT('Ctrl Pts',(-3.84517267746582,-0.826520465850875,
27.887958528161));
#26465=CARTESIAN_POINT('Ctrl Pts',(-3.82092923402807,-0.93930681557368,
27.893830652127));
#26466=CARTESIAN_POINT('Ctrl Pts',(-3.79167857667318,-1.05121468513039,
27.899702776093));
#26467=CARTESIAN_POINT('Ctrl Pts',(-3.75749790814601,-1.16176523888363,
27.905574900059));
#26468=CARTESIAN_POINT('Ctrl Pts',(-3.72336155553428,-1.27217246164886,
27.9114394106997));
#26469=CARTESIAN_POINT('Ctrl Pts',(-3.68430802382435,-1.38122547687397,
27.9173039213404));
#26470=CARTESIAN_POINT('Ctrl Pts',(-3.64046553995892,-1.4884554586455,27.9231684319811));
#26471=CARTESIAN_POINT('Ctrl Pts',(-3.59666816957323,-1.59557510183257,
27.9290269080987));
#26472=CARTESIAN_POINT('Ctrl Pts',(-3.548091804144,-1.70087506242788,27.9348853842163));
#26473=CARTESIAN_POINT('Ctrl Pts',(-3.49491430599666,-1.80390215747415,
27.9407438603339));
#26474=CARTESIAN_POINT('Ctrl Pts',(-3.43963994865642,-1.91099174735172,
27.9468333439252));
#26475=CARTESIAN_POINT('Ctrl Pts',(-3.37939427043638,-2.01562510514671,
27.9529228275164));
#26476=CARTESIAN_POINT('Ctrl Pts',(-3.31443212027581,-2.1173163958379,27.9590123111077));
#26477=CARTESIAN_POINT('Ctrl Pts',(-3.25200679260917,-2.21503656252804,
27.9648639956281));
#26478=CARTESIAN_POINT('Ctrl Pts',(-3.18522668775894,-2.31003974896123,
27.9707156801485));
#26479=CARTESIAN_POINT('Ctrl Pts',(-3.11436411475705,-2.40192113957006,
27.9765673646689));
#26480=CARTESIAN_POINT('Ctrl Pts',(-3.04351234983792,-2.49378851626954,
27.9824181566802));
#26481=CARTESIAN_POINT('Ctrl Pts',(-2.96857960722595,-2.58253471659117,
27.9882689486915));
#26482=CARTESIAN_POINT('Ctrl Pts',(-2.88987993231758,-2.66778615649533,
27.9941197407028));
#26483=CARTESIAN_POINT('Ctrl Pts',(-2.81117319895261,-2.75304524247413,
27.9999710574629));
#26484=CARTESIAN_POINT('Ctrl Pts',(-2.72869914211331,-2.83480864116148,
28.005822374223));
#26485=CARTESIAN_POINT('Ctrl Pts',(-2.64280978799126,-2.91273847512914,
28.0116736909831));
#26486=CARTESIAN_POINT('Ctrl Pts',(-2.55689192730466,-2.99069417390698,
28.0175269497876));
#26487=CARTESIAN_POINT('Ctrl Pts',(-2.46755682138669,-3.06481350032096,
28.0233802085921));
#26488=CARTESIAN_POINT('Ctrl Pts',(-2.37519023219202,-3.13479829668507,
28.0292334673966));
#26489=CARTESIAN_POINT('Ctrl Pts',(-2.2827185579857,-3.20486271440584,28.0350933854247));
#26490=CARTESIAN_POINT('Ctrl Pts',(-2.18720884628985,-3.27078296353361,
28.0409533034528));
#26491=CARTESIAN_POINT('Ctrl Pts',(-2.08907662610493,-3.33230368517967,
28.0468132214809));
#26492=CARTESIAN_POINT('Ctrl Pts',(-1.99087833068777,-3.39386583048825,
28.0526770851595));
#26493=CARTESIAN_POINT('Ctrl Pts',(-1.89005436947373,-3.45102234635887,
28.0585409488382));
#26494=CARTESIAN_POINT('Ctrl Pts',(-1.78704414461185,-3.50356421736615,
28.0644048125168));
#26495=CARTESIAN_POINT('Ctrl Pts',(-1.68388195490171,-3.55618360026573,
28.0702773268041));
#26496=CARTESIAN_POINT('Ctrl Pts',(-1.578527439325,-3.60417458064231,28.0761498410915));
#26497=CARTESIAN_POINT('Ctrl Pts',(-1.47143926629275,-3.64737652095473,
28.0820223553789));
#26498=CARTESIAN_POINT('Ctrl Pts',(-1.44184239112471,-3.65931661105281,
28.0836453924274));
#26499=CARTESIAN_POINT('Ctrl Pts',(-1.41211317255464,-3.6708911853484,28.0852684294759));
#26500=CARTESIAN_POINT('Ctrl Pts',(-1.38226146353499,-3.68209753352978,
28.0868914665243));
#26501=CARTESIAN_POINT('Ctrl Pts',(-1.27425842310814,-3.72264193502029,
28.0927635904904));
#26502=CARTESIAN_POINT('Ctrl Pts',(-1.16428893593136,-3.75849837258234,
28.0986357144564));
#26503=CARTESIAN_POINT('Ctrl Pts',(-1.05279763066019,-3.78947307008195,
28.1045078384225));
#26504=CARTESIAN_POINT('Ctrl Pts',(-0.941450876080078,-3.82040760827121,
28.1103723490632));
#26505=CARTESIAN_POINT('Ctrl Pts',(-0.828586621764973,-3.84647288338478,
28.116236859704));
#26506=CARTESIAN_POINT('Ctrl Pts',(-0.714668644579877,-3.86752346191388,
28.1221013703447));
#26507=CARTESIAN_POINT('Ctrl Pts',(-0.600867887860008,-3.8885523796071,
28.1279598464623));
#26508=CARTESIAN_POINT('Ctrl Pts',(-0.48601596901778,-3.90457678967679,
28.1338183225799));
#26509=CARTESIAN_POINT('Ctrl Pts',(-0.370590322647342,-3.91550147653658,
28.1396767986976));
#26510=CARTESIAN_POINT('Ctrl Pts',(-0.250613290144082,-3.92685693827043,
28.1457662822888));
#26511=CARTESIAN_POINT('Ctrl Pts',(-0.130016792046849,-3.93270210330527,
28.1518557658801));
#26512=CARTESIAN_POINT('Ctrl Pts',(-0.00934733730404496,-3.93298889234197,
28.1579452494714));
#26513=CARTESIAN_POINT('Ctrl Pts',(0.106609881370335,-3.93326448204371,
28.1637969339918));
#26514=CARTESIAN_POINT('Ctrl Pts',(0.222634013232644,-3.92840766600728,
28.1696486185122));
#26515=CARTESIAN_POINT('Ctrl Pts',(0.338237287969133,-3.91842883526386,
28.1755003030326));
#26516=CARTESIAN_POINT('Ctrl Pts',(0.453822930693283,-3.90845152650905,
28.181351095044));
#26517=CARTESIAN_POINT('Ctrl Pts',(0.568987432153757,-3.89335379189814,
28.1872018870553));
#26518=CARTESIAN_POINT('Ctrl Pts',(0.683246749400239,-3.87319801706987,
28.1930526790666));
#26519=CARTESIAN_POINT('Ctrl Pts',(0.797516314394701,-3.85304043450018,
28.1989039958268));
#26520=CARTESIAN_POINT('Ctrl Pts',(0.910880126636748,-3.8278239817254,28.2047553125869));
#26521=CARTESIAN_POINT('Ctrl Pts',(1.02286366537529,-3.79766229699996,28.2106066293471));
#26522=CARTESIAN_POINT('Ctrl Pts',(1.13488437130418,-3.76749060165073,28.2164598881516));
#26523=CARTESIAN_POINT('Ctrl Pts',(1.24552349382999,-3.73237051816125,28.2223131469562));
#26524=CARTESIAN_POINT('Ctrl Pts',(1.35432170501045,-3.69246553394037,28.2281664057607));
#26525=CARTESIAN_POINT('Ctrl Pts',(1.46324369537758,-3.65251515001635,28.2340263237889));
#26526=CARTESIAN_POINT('Ctrl Pts',(1.57032020568019,-3.60776914220727,28.239886241817));
#26527=CARTESIAN_POINT('Ctrl Pts',(1.6751118361179,-3.5584391713921,28.2457461598451));
#26528=CARTESIAN_POINT('Ctrl Pts',(1.77997402575952,-3.50907598529577,28.2516100235238));
#26529=CARTESIAN_POINT('Ctrl Pts',(1.88254790713922,-3.4551228823243,28.2574738872025));
#26530=CARTESIAN_POINT('Ctrl Pts',(1.98242017598273,-3.39683665280752,28.2633377508811));
#26531=CARTESIAN_POINT('Ctrl Pts',(2.08243978043466,-3.33846443708869,28.2692102651685));
#26532=CARTESIAN_POINT('Ctrl Pts',(2.17974947178649,-3.27574655990002,28.2750827794559));
#26533=CARTESIAN_POINT('Ctrl Pts',(2.27396624245754,-3.2089821638899,28.2809552937433));
#26534=CARTESIAN_POINT('Ctrl Pts',(2.3000057379576,-3.19052991619465,28.2825783307915));
#26535=CARTESIAN_POINT('Ctrl Pts',(2.32580918463529,-3.17176880359157,28.2842013678397));
#26536=CARTESIAN_POINT('Ctrl Pts',(2.35136897790047,-3.15270565225606,28.2858244048879));
#26537=CARTESIAN_POINT('Ctrl Pts',(2.44292642898942,-3.08441974994477,28.2916382678411));
#26538=CARTESIAN_POINT('Ctrl Pts',(2.53167513435791,-3.01201639839188,28.2974521307943));
#26539=CARTESIAN_POINT('Ctrl Pts',(2.61721613342261,-2.9357569230017,28.3032659937476));
#26540=CARTESIAN_POINT('Ctrl Pts',(2.70264584827739,-2.85959665706149,28.3090722931797));
#26541=CARTESIAN_POINT('Ctrl Pts',(2.7848758397571,-2.77959051754744,28.3148785926119));
#26542=CARTESIAN_POINT('Ctrl Pts',(2.86353708680282,-2.69604234990937,28.3206848920441));
#26543=CARTESIAN_POINT('Ctrl Pts',(2.94211808810384,-2.61257941337533,28.3264852682188));
#26544=CARTESIAN_POINT('Ctrl Pts',(3.01713729567528,-2.52558193867496,28.3322856443934));
#26545=CARTESIAN_POINT('Ctrl Pts',(3.08826029700842,-2.43539264553408,28.3380860205681));
#26546=CARTESIAN_POINT('Ctrl Pts',(3.15933189784284,-2.34526853207572,28.3438822048186));
#26547=CARTESIAN_POINT('Ctrl Pts',(3.22651263113738,-2.25195751782776,28.3496783890691));
#26548=CARTESIAN_POINT('Ctrl Pts',(3.28950689367905,-2.15583705238545,28.3554745733197));
#26549=CARTESIAN_POINT('Ctrl Pts',(3.35247760017397,-2.0597525301876,28.3612685901476));
#26550=CARTESIAN_POINT('Ctrl Pts',(3.41126471568405,-1.96086099736457,28.3670626069755));
#26551=CARTESIAN_POINT('Ctrl Pts',(3.46561510510418,-1.85957009635929,28.3728566238034));
#26552=CARTESIAN_POINT('Ctrl Pts',(3.51995897317413,-1.75829134896402,28.3786499454236));
#26553=CARTESIAN_POINT('Ctrl Pts',(3.56986697404504,-1.65461417805031,28.3844432670438));
#26554=CARTESIAN_POINT('Ctrl Pts',(3.6151316267666,-1.54897137518803,28.3902365886639));
#26555=CARTESIAN_POINT('Ctrl Pts',(3.66040234371183,-1.4433144190837,28.3960306864305));
#26556=CARTESIAN_POINT('Ctrl Pts',(3.70102831075177,-1.33569169633608,28.4018247841971));
#26557=CARTESIAN_POINT('Ctrl Pts',(3.73685027231346,-1.2265557640445,28.4076188819637));
#26558=CARTESIAN_POINT('Ctrl Pts',(3.77270662462591,-1.11731505617719,28.4134185423338));
#26559=CARTESIAN_POINT('Ctrl Pts',(3.80374963117829,-1.00655864017171,28.419218202704));
#26560=CARTESIAN_POINT('Ctrl Pts',(3.82987000929517,-0.894753995186079,
28.4250178630742));
#26561=CARTESIAN_POINT('Ctrl Pts',(3.8560039587028,-0.7828912601782,28.4308205367575));
#26562=CARTESIAN_POINT('Ctrl Pts',(3.87721010983761,-0.669979626732484,
28.4366232104407));
#26563=CARTESIAN_POINT('Ctrl Pts',(3.89343070412677,-0.556494700929754,
28.442425884124));
#26564=CARTESIAN_POINT('Ctrl Pts',(3.90967540972263,-0.442841084029651,
28.4482371832646));
#26565=CARTESIAN_POINT('Ctrl Pts',(3.92091971988341,-0.328612893091065,
28.4540484824053));
#26566=CARTESIAN_POINT('Ctrl Pts',(3.92715791049324,-0.214288931236205,
28.4598597815459));
#26567=CARTESIAN_POINT('Ctrl Pts',(3.93108558787204,-0.142308501827107,
28.4635186803523));
#26568=CARTESIAN_POINT('Ctrl Pts',(3.93302979224588,-0.0702901060402026,
28.4671775791586));
#26569=CARTESIAN_POINT('Ctrl Pts',(3.93299965486354,0.0016476781387844,
28.470836477965));
#26570=CARTESIAN_POINT('',(3.93378334737471,-0.00358749909980301,29.7208364779651));
#26571=CARTESIAN_POINT('Ctrl Pts',(3.93869061149251,0.00165006228972526,
28.470836477965));
#26572=CARTESIAN_POINT('Ctrl Pts',(3.93917274253189,0.0930152245985141,
28.4754767663938));
#26573=CARTESIAN_POINT('Ctrl Pts',(3.89479594559616,1.48953671629816,28.5464280342761));
#26574=CARTESIAN_POINT('Ctrl Pts',(2.23403159274154,4.08086268149356,28.6836902816154));
#26575=CARTESIAN_POINT('Ctrl Pts',(-2.22665458802441,4.08489249897418,28.8826232199778));
#26576=CARTESIAN_POINT('Ctrl Pts',(-4.64036711535831,0.333662130402121,
29.0815561583418));
#26577=CARTESIAN_POINT('Ctrl Pts',(-2.78816912451703,-3.72430534672374,
29.280489096705));
#26578=CARTESIAN_POINT('Ctrl Pts',(1.62720537780082,-4.35850204095535,29.4794220350685));
#26579=CARTESIAN_POINT('Ctrl Pts',(3.78133859306296,-1.8700370989607,29.6262044954885));
#26580=CARTESIAN_POINT('Ctrl Pts',(3.93638707710448,-0.283307213321637,
29.706675976454));
#26581=CARTESIAN_POINT('Ctrl Pts',(3.93378334737471,-0.00358749909980301,
29.7208364779651));
#26582=CARTESIAN_POINT('',(3.92648812541355,-6.39030992054769E-5,30.9708364779651));
#26583=CARTESIAN_POINT('Ctrl Pts',(3.93378334737471,-0.00358749909980301,
29.7208364779651));
#26584=CARTESIAN_POINT('Ctrl Pts',(3.92419429788116,1.02656787890612,29.7729869559085));
#26585=CARTESIAN_POINT('Ctrl Pts',(2.98160786092303,3.38213034827263,29.8914484133063));
#26586=CARTESIAN_POINT('Ctrl Pts',(-0.995113215119353,4.54467678406942,
30.0762208501589));
#26587=CARTESIAN_POINT('Ctrl Pts',(-4.36178824789613,1.61837593378662,30.2751537885222));
#26588=CARTESIAN_POINT('Ctrl Pts',(-3.7186515778127,-2.79570524651421,30.4740867268857));
#26589=CARTESIAN_POINT('Ctrl Pts',(0.343058339789779,-4.63968192423417,
30.6730196652491));
#26590=CARTESIAN_POINT('Ctrl Pts',(3.46134686146429,-2.6242923161433,30.8386029156089));
#26591=CARTESIAN_POINT('Ctrl Pts',(3.92658248875702,-0.654225497905084,
30.9378751865142));
#26592=CARTESIAN_POINT('Ctrl Pts',(3.92648812541355,-6.39030992054769E-5,
30.9708364779651));
#26593=CARTESIAN_POINT('',(3.93354801992752,0.00360815564889333,32.2208364779651));
#26594=CARTESIAN_POINT('Ctrl Pts',(3.92648812541355,-6.39030992054769E-5,
30.9708364779651));
#26595=CARTESIAN_POINT('Ctrl Pts',(3.9263926501477,0.661805948792916,31.0041861659687));
#26596=CARTESIAN_POINT('Ctrl Pts',(3.45325931545757,2.63983545764988,31.103846833427));
#26597=CARTESIAN_POINT('Ctrl Pts',(0.315878541481514,4.6416115875405,31.2698184803395));
#26598=CARTESIAN_POINT('Ctrl Pts',(-3.73496181963207,2.77387771692204,31.4687514187028));
#26599=CARTESIAN_POINT('Ctrl Pts',(-4.35223485401481,-1.64389450940807,
31.6676843570663));
#26600=CARTESIAN_POINT('Ctrl Pts',(-0.968478663821196,-4.55042706350403,
31.8666172954298));
#26601=CARTESIAN_POINT('Ctrl Pts',(2.99302062995904,-3.36710213391904,32.0510013357293));
#26602=CARTESIAN_POINT('Ctrl Pts',(3.92403177335956,-1.01903183245315,32.1690743965744));
#26603=CARTESIAN_POINT('Ctrl Pts',(3.93354801992752,0.00360815564889333,
32.2208364779651));
#26604=CARTESIAN_POINT('',(3.93449192545046,-0.00152063529977577,33.4708364779651));
#26605=CARTESIAN_POINT('Ctrl Pts',(3.93354801992752,0.00360815564889333,
32.2208364779651));
#26606=CARTESIAN_POINT('Ctrl Pts',(3.93622277522228,0.291044142440767,32.2353853760289));
#26607=CARTESIAN_POINT('Ctrl Pts',(3.77605966658974,1.88560059886485,32.3162452535476));
#26608=CARTESIAN_POINT('Ctrl Pts',(1.60165038246052,4.36795758162834,32.4634161105198));
#26609=CARTESIAN_POINT('Ctrl Pts',(-2.80993399564309,3.7079115850692,32.6623490488836));
#26610=CARTESIAN_POINT('Ctrl Pts',(-4.63833331760885,-0.360834335010101,
32.8612819872469));
#26611=CARTESIAN_POINT('Ctrl Pts',(-2.20269180088781,-4.09786361569582,
33.0602149256104));
#26612=CARTESIAN_POINT('Ctrl Pts',(2.25789427045762,-4.06770830394701,33.2591478639738));
#26613=CARTESIAN_POINT('Ctrl Pts',(3.8987968700746,-1.47405973851723,33.3960217147587));
#26614=CARTESIAN_POINT('Ctrl Pts',(3.93922925932993,-0.0852329913937091,
33.4665845860891));
#26615=CARTESIAN_POINT('Ctrl Pts',(3.93881695897552,-0.00152230687485492,
33.4708364779651));
#26616=CARTESIAN_POINT('',(3.93299893535526,-0.0028938718737489,34.7208364779192));
#26617=CARTESIAN_POINT('Ctrl Pts',(3.93299970625754,-0.00152005857443918,
33.4708364779651));
#26618=CARTESIAN_POINT('Ctrl Pts',(3.9330438950136,0.112813933216348,33.4766524118655));
#26619=CARTESIAN_POINT('Ctrl Pts',(3.92809825171672,0.227351778088693,33.4824683457659));
#26620=CARTESIAN_POINT('Ctrl Pts',(3.91813566485521,0.341616615213035,33.4882842796663));
#26621=CARTESIAN_POINT('Ctrl Pts',(3.90818549564635,0.455739029382667,33.4940929644206));
#26622=CARTESIAN_POINT('Ctrl Pts',(3.89323084998174,0.569588695816249,33.499901649175));
#26623=CARTESIAN_POINT('Ctrl Pts',(3.87329661328719,0.682687589969195,33.5057103339293));
#26624=CARTESIAN_POINT('Ctrl Pts',(3.85338164164078,0.795677181936531,33.5115134049954));
#26625=CARTESIAN_POINT('Ctrl Pts',(3.8284967206146,0.907917031182888,33.5173164760614));
#26626=CARTESIAN_POINT('Ctrl Pts',(3.79871857100013,1.01893386357445,33.5231195471275));
#26627=CARTESIAN_POINT('Ctrl Pts',(3.76895950630716,1.12987954488512,33.5289188989847));
#26628=CARTESIAN_POINT('Ctrl Pts',(3.73431355699685,1.23960336145571,33.534718250842));
#26629=CARTESIAN_POINT('Ctrl Pts',(3.69490845196252,1.34764258303748,33.5405176026993));
#26630=CARTESIAN_POINT('Ctrl Pts',(3.65551615023596,1.45564670106085,33.5463150702604));
#26631=CARTESIAN_POINT('Ctrl Pts',(3.61136791005949,1.56196691584907,33.5521125378216));
#26632=CARTESIAN_POINT('Ctrl Pts',(3.56264098550639,1.666156717836,33.5579100053827));
#26633=CARTESIAN_POINT('Ctrl Pts',(3.51391755067153,1.77033905797193,33.5637070577416));
#26634=CARTESIAN_POINT('Ctrl Pts',(3.46061626229255,1.87239090655358,33.5695041101005));
#26635=CARTESIAN_POINT('Ctrl Pts',(3.40296173666513,1.97188752691249,33.5753011624594));
#26636=CARTESIAN_POINT('Ctrl Pts',(3.34529673573918,2.0714022248948,33.5810992680895));
#26637=CARTESIAN_POINT('Ctrl Pts',(3.28327713764424,2.16836040724858,33.5868973737197));
#26638=CARTESIAN_POINT('Ctrl Pts',(3.21717212097101,2.26236437030972,33.5926954793498));
#26639=CARTESIAN_POINT('Ctrl Pts',(3.15099797860989,2.35646663284854,33.5984996480303));
#26640=CARTESIAN_POINT('Ctrl Pts',(3.08073013102971,2.44760816254515,33.6043038167107));
#26641=CARTESIAN_POINT('Ctrl Pts',(3.0066795021211,2.53542252327395,33.6101079853911));
#26642=CARTESIAN_POINT('Ctrl Pts',(2.93258748986793,2.62328595923682,33.615915397743));
#26643=CARTESIAN_POINT('Ctrl Pts',(2.85470877348838,2.70781821477734,33.6217228100949));
#26644=CARTESIAN_POINT('Ctrl Pts',(2.77339144552847,2.78868945740996,33.6275302224468));
#26645=CARTESIAN_POINT('Ctrl Pts',(2.69194533307536,2.86968877805817,33.6333468321577));
#26646=CARTESIAN_POINT('Ctrl Pts',(2.60705004603519,2.94701522419906,33.6391634418686));
#26647=CARTESIAN_POINT('Ctrl Pts',(2.51908725535366,3.02037885039522,33.6449800515795));
#26648=CARTESIAN_POINT('Ctrl Pts',(2.45842666840782,3.07097161343802,33.6489912812865));
#26649=CARTESIAN_POINT('Ctrl Pts',(2.39630793521481,3.11968064274633,33.6530025109936));
#26650=CARTESIAN_POINT('Ctrl Pts',(2.33286372890622,3.16642319066068,33.6570137407007));
#26651=CARTESIAN_POINT('Ctrl Pts',(2.23998641407312,3.23485059469543,33.6628858646667));
#26652=CARTESIAN_POINT('Ctrl Pts',(2.14394017682272,3.2993028447297,33.6687579886327));
#26653=CARTESIAN_POINT('Ctrl Pts',(2.04510005975058,3.35947239095787,33.6746301125987));
#26654=CARTESIAN_POINT('Ctrl Pts',(1.94638809085282,3.4195639261746,33.6804946232394));
#26655=CARTESIAN_POINT('Ctrl Pts',(1.8448897954779,3.47538358673165,33.6863591338801));
#26656=CARTESIAN_POINT('Ctrl Pts',(1.74101180716422,3.52666512264983,33.6922236445208));
#26657=CARTESIAN_POINT('Ctrl Pts',(1.63724070826689,3.57789389037783,33.6980821206385));
#26658=CARTESIAN_POINT('Ctrl Pts',(1.53109515544159,3.62459363979002,33.7039405967561));
#26659=CARTESIAN_POINT('Ctrl Pts',(1.42300860101261,3.66654272052626,33.7097990728737));
#26660=CARTESIAN_POINT('Ctrl Pts',(1.31066005056724,3.71014590908317,33.7158885564649));
#26661=CARTESIAN_POINT('Ctrl Pts',(1.19621466552446,3.74861583435007,33.7219780400562));
#26662=CARTESIAN_POINT('Ctrl Pts',(1.08018519929194,3.78175738714564,33.7280675236475));
#26663=CARTESIAN_POINT('Ctrl Pts',(0.968686773967879,3.8136047365258,33.7339192081679));
#26664=CARTESIAN_POINT('Ctrl Pts',(0.855726099958207,3.840531933996,33.7397708926883));
#26665=CARTESIAN_POINT('Ctrl Pts',(0.741775337649826,3.86241612833916,33.7456225772087));
#26666=CARTESIAN_POINT('Ctrl Pts',(0.627841955309791,3.88429698486697,33.75147336922));
#26667=CARTESIAN_POINT('Ctrl Pts',(0.512919190807531,3.90113628966456,33.7573241612313));
#26668=CARTESIAN_POINT('Ctrl Pts',(0.397489779361355,3.91286223566627,33.7631749532426));
#26669=CARTESIAN_POINT('Ctrl Pts',(0.282050015223007,3.92458923335063,33.7690262700028));
#26670=CARTESIAN_POINT('Ctrl Pts',(0.166103925129751,3.93120191878137,33.7748775867629));
#26671=CARTESIAN_POINT('Ctrl Pts',(0.0501390412784461,3.93268039338816,
33.780728903523));
#26672=CARTESIAN_POINT('Ctrl Pts',(-0.0658643311663984,3.93415935869875,
33.7865821623276));
#26673=CARTESIAN_POINT('Ctrl Pts',(-0.181886096611841,3.93050071954973,
33.7924354211321));
#26674=CARTESIAN_POINT('Ctrl Pts',(-0.297439764363639,3.92173667991303,
33.7982886799366));
#26675=CARTESIAN_POINT('Ctrl Pts',(-0.413124896951639,3.91296266947179,
33.8041485979647));
#26676=CARTESIAN_POINT('Ctrl Pts',(-0.528340456410724,3.89907169643622,
33.8100085159929));
#26677=CARTESIAN_POINT('Ctrl Pts',(-0.642606006254656,3.88014774470321,
33.815868434021));
#26678=CARTESIAN_POINT('Ctrl Pts',(-0.756948494363085,3.86121105093198,
33.8217322976996));
#26679=CARTESIAN_POINT('Ctrl Pts',(-0.870339295668422,3.83723471591854,
33.8275961613782));
#26680=CARTESIAN_POINT('Ctrl Pts',(-0.982310791191115,3.80835325429633,
33.8334600250568));
#26681=CARTESIAN_POINT('Ctrl Pts',(-1.09444747159112,3.77942918557424,33.8393325393442));
#26682=CARTESIAN_POINT('Ctrl Pts',(-1.20516027346493,3.74558566845188,33.8452050536316));
#26683=CARTESIAN_POINT('Ctrl Pts',(-1.31399919406462,3.7070062203883,33.851077567919));
#26684=CARTESIAN_POINT('Ctrl Pts',(-1.34407993832424,3.69634368804707,33.8527006049674));
#26685=CARTESIAN_POINT('Ctrl Pts',(-1.37401768016128,3.68531967695817,33.8543236420158));
#26686=CARTESIAN_POINT('Ctrl Pts',(-1.40380324329395,3.67393868404433,33.8559466790642));
#26687=CARTESIAN_POINT('Ctrl Pts',(-1.51156696888908,3.63276242050001,33.8618188030302));
#26688=CARTESIAN_POINT('Ctrl Pts',(-1.61769815373918,3.5867717276717,33.8676909269962));
#26689=CARTESIAN_POINT('Ctrl Pts',(-1.72173535916121,3.53611599824073,33.8735630509623));
#26690=CARTESIAN_POINT('Ctrl Pts',(-1.82563767828081,3.4855259449687,33.879427561603));
#26691=CARTESIAN_POINT('Ctrl Pts',(-1.92745104863631,3.43028306229867,33.8852920722437));
#26692=CARTESIAN_POINT('Ctrl Pts',(-2.02673171285118,3.37058564111985,33.8911565828845));
#26693=CARTESIAN_POINT('Ctrl Pts',(-2.12591021824992,3.31094964799374,33.8970150590021));
#26694=CARTESIAN_POINT('Ctrl Pts',(-2.22256084906142,3.24686844526265,33.9028735351197));
#26695=CARTESIAN_POINT('Ctrl Pts',(-2.31626288442334,3.17858698956673,33.9087320112373));
#26696=CARTESIAN_POINT('Ctrl Pts',(-2.41365971516066,3.10761310562465,33.9148214948285));
#26697=CARTESIAN_POINT('Ctrl Pts',(-2.50787022334738,3.03210111018802,33.9209109784198));
#26698=CARTESIAN_POINT('Ctrl Pts',(-2.59845317081807,2.95237702861025,33.9270004620111));
#26699=CARTESIAN_POINT('Ctrl Pts',(-2.6854987837315,2.87576623443023,33.9328521465315));
#26700=CARTESIAN_POINT('Ctrl Pts',(-2.76919449786096,2.79526645012768,33.9387038310519));
#26701=CARTESIAN_POINT('Ctrl Pts',(-2.84918181026032,2.71120858881823,33.9445555155723));
#26702=CARTESIAN_POINT('Ctrl Pts',(-2.92915692285575,2.6271635481599,33.9504063075836));
#26703=CARTESIAN_POINT('Ctrl Pts',(-3.0054244734278,2.53956180892644,33.9562570995949));
#26704=CARTESIAN_POINT('Ctrl Pts',(-3.07766319562749,2.44877076393034,33.9621078916063));
#26705=CARTESIAN_POINT('Ctrl Pts',(-3.14990839681041,2.35797157602085,33.9679592083664));
#26706=CARTESIAN_POINT('Ctrl Pts',(-3.21812379389611,2.26398283724358,33.9738105251265));
#26707=CARTESIAN_POINT('Ctrl Pts',(-3.28202920647759,2.16720402542725,33.9796618418866));
#26708=CARTESIAN_POINT('Ctrl Pts',(-3.34595582918186,2.07039309284995,33.9855151006911));
#26709=CARTESIAN_POINT('Ctrl Pts',(-3.40556939528662,1.97079059070432,33.9913683594956));
#26710=CARTESIAN_POINT('Ctrl Pts',(-3.46063412841611,1.86882327394585,33.9972216183001));
#26711=CARTESIAN_POINT('Ctrl Pts',(-3.51576150842041,1.76673994947491,34.0030815363283));
#26712=CARTESIAN_POINT('Ctrl Pts',(-3.56632952936131,1.66228680432588,34.0089414543564));
#26713=CARTESIAN_POINT('Ctrl Pts',(-3.61214925603459,1.55591347835564,34.0148013723845));
#26714=CARTESIAN_POINT('Ctrl Pts',(-3.65799983444114,1.44946852818077,34.0206652360631));
#26715=CARTESIAN_POINT('Ctrl Pts',(-3.69909560617159,1.34110120834975,34.0265290997418));
#26716=CARTESIAN_POINT('Ctrl Pts',(-3.73529708060709,1.23127767770236,34.0323929634204));
#26717=CARTESIAN_POINT('Ctrl Pts',(-3.7715519609212,1.12129213094271,34.0382654777078));
#26718=CARTESIAN_POINT('Ctrl Pts',(-3.80289802211455,1.00984648231674,34.0441379919952));
#26719=CARTESIAN_POINT('Ctrl Pts',(-3.82924652548556,0.897418546196115,
34.0500105062826));
#26720=CARTESIAN_POINT('Ctrl Pts',(-3.83652868693235,0.866345874992341,
34.0516335433309));
#26721=CARTESIAN_POINT('Ctrl Pts',(-3.84342941401099,0.835198207784189,
34.0532565803793));
#26722=CARTESIAN_POINT('Ctrl Pts',(-3.84994753223726,0.803985695780863,
34.0548796174276));
#26723=CARTESIAN_POINT('Ctrl Pts',(-3.87352998729532,0.691059290334441,
34.0607517413936));
#26724=CARTESIAN_POINT('Ctrl Pts',(-3.89217924055118,0.576905106979158,
34.0666238653597));
#26725=CARTESIAN_POINT('Ctrl Pts',(-3.90577165990679,0.461992143514322,
34.0724959893257));
#26726=CARTESIAN_POINT('Ctrl Pts',(-3.91934645642081,0.347228166988323,
34.0783604999664));
#26727=CARTESIAN_POINT('Ctrl Pts',(-3.92787740899491,0.23170777347713,34.0842250106071));
#26728=CARTESIAN_POINT('Ctrl Pts',(-3.93129158458168,0.115911505025303,
34.0900895212478));
#26729=CARTESIAN_POINT('Ctrl Pts',(-3.93470224701574,0.000234389781788094,
34.0959479973655));
#26730=CARTESIAN_POINT('Ctrl Pts',(-3.93300659291112,-0.1157176250214,34.1018064734831));
#26731=CARTESIAN_POINT('Ctrl Pts',(-3.92618340346277,-0.231458165493218,
34.1076649496007));
#26732=CARTESIAN_POINT('Ctrl Pts',(-3.91909116661625,-0.351762508789647,
34.1137544331919));
#26733=CARTESIAN_POINT('Ctrl Pts',(-3.90645865083155,-0.471837905322594,
34.1198439167832));
#26734=CARTESIAN_POINT('Ctrl Pts',(-3.88832176543053,-0.591136911788797,
34.1259334003745));
#26735=CARTESIAN_POINT('Ctrl Pts',(-3.87089313951194,-0.705777199257459,
34.1317850848949));
#26736=CARTESIAN_POINT('Ctrl Pts',(-3.84838204447286,-0.8197001488176,34.1376367694153));
#26737=CARTESIAN_POINT('Ctrl Pts',(-3.82087320819095,-0.932425292947679,
34.1434884539357));
#26738=CARTESIAN_POINT('Ctrl Pts',(-3.79336856760453,-1.04513324404301,
34.149339245947));
#26739=CARTESIAN_POINT('Ctrl Pts',(-3.760867799379,-1.15664335144015,34.1551900379583));
#26740=CARTESIAN_POINT('Ctrl Pts',(-3.72350644764521,-1.26648676832589,
34.1610408299696));
#26741=CARTESIAN_POINT('Ctrl Pts',(-3.68614174502749,-1.37634003690392,
34.1668921467298));
#26742=CARTESIAN_POINT('Ctrl Pts',(-3.64391572542909,-1.48452592639684,
34.1727434634899));
#26743=CARTESIAN_POINT('Ctrl Pts',(-3.59701313135075,-1.59059282435521,
34.17859478025));
#26744=CARTESIAN_POINT('Ctrl Pts',(-3.55009497036268,-1.6966949257785,34.1844480390545));
#26745=CARTESIAN_POINT('Ctrl Pts',(-3.49849731565263,-1.80067625932397,
34.1903012978591));
#26746=CARTESIAN_POINT('Ctrl Pts',(-3.44245185545404,-1.90210783681711,
34.1961545566636));
#26747=CARTESIAN_POINT('Ctrl Pts',(-3.3863426326125,-2.00365481251442,34.2020144746917));
#26748=CARTESIAN_POINT('Ctrl Pts',(-3.32577570422196,-2.10264588008473,
34.2078743927198));
#26749=CARTESIAN_POINT('Ctrl Pts',(-3.26102732534971,-2.19867909966928,
34.213734310748));
#26750=CARTESIAN_POINT('Ctrl Pts',(-3.19623534954079,-2.29477698116916,
34.2195981744266));
#26751=CARTESIAN_POINT('Ctrl Pts',(-3.12725656250775,-2.38791271760243,
34.2254620381052));
#26752=CARTESIAN_POINT('Ctrl Pts',(-3.05440783635046,-2.47771704785694,
34.2313259017839));
#26753=CARTESIAN_POINT('Ctrl Pts',(-2.98145164080723,-2.56765386109003,
34.2371984160713));
#26754=CARTESIAN_POINT('Ctrl Pts',(-2.90461438521196,-2.65424915139292,
34.2430709303587));
#26755=CARTESIAN_POINT('Ctrl Pts',(-2.82425017279994,-2.73717006439854,
34.2489434446461));
#26756=CARTESIAN_POINT('Ctrl Pts',(-2.80203922741655,-2.76008762701293,
34.2505664816944));
#26757=CARTESIAN_POINT('Ctrl Pts',(-2.77955907006268,-2.78272475872175,
34.2521895187427));
#26758=CARTESIAN_POINT('Ctrl Pts',(-2.75681760776031,-2.80507498608197,
34.253812555791));
#26759=CARTESIAN_POINT('Ctrl Pts',(-2.67453933447679,-2.885937777148,34.259684679757));
#26760=CARTESIAN_POINT('Ctrl Pts',(-2.58856231310679,-2.9633129929522,34.265556803723));
#26761=CARTESIAN_POINT('Ctrl Pts',(-2.49921437368522,-3.03684318237956,
34.271428927689));
#26762=CARTESIAN_POINT('Ctrl Pts',(-2.4099822756412,-3.11027803845631,34.2772934383297));
#26763=CARTESIAN_POINT('Ctrl Pts',(-2.3173882670729,-3.1798775215431,34.2831579489704));
#26764=CARTESIAN_POINT('Ctrl Pts',(-2.22179728694304,-3.24532060291931,
34.2890224596111));
#26765=CARTESIAN_POINT('Ctrl Pts',(-2.12630466898078,-3.31069634401582,
34.2948809357287));
#26766=CARTESIAN_POINT('Ctrl Pts',(-2.02782155246302,-3.37192395821575,
34.3007394118463));
#26767=CARTESIAN_POINT('Ctrl Pts',(-1.92674572718564,-3.4287227800993,34.3065978879639));
#26768=CARTESIAN_POINT('Ctrl Pts',(-1.82168434822858,-3.48776125476767,
34.3126873715551));
#26769=CARTESIAN_POINT('Ctrl Pts',(-1.71382193748083,-3.54201419621172,
34.3187768551464));
#26770=CARTESIAN_POINT('Ctrl Pts',(-1.60363854014919,-3.5912160102879,34.3248663387377));
#26771=CARTESIAN_POINT('Ctrl Pts',(-1.49775789018835,-3.6384964552533,34.3307180232581));
#26772=CARTESIAN_POINT('Ctrl Pts',(-1.38973453766546,-3.68111268626925,
34.3365697077785));
#26773=CARTESIAN_POINT('Ctrl Pts',(-1.2800185505601,-3.71887637737826,34.3424213922989));
#26774=CARTESIAN_POINT('Ctrl Pts',(-1.17031929752784,-3.75663430870344,
34.3482721843101));
#26775=CARTESIAN_POINT('Ctrl Pts',(-1.05892831402063,-3.78954103719723,
34.3541229763214));
#26776=CARTESIAN_POINT('Ctrl Pts',(-0.946313348315403,-3.8174572750458,
34.3599737683327));
#26777=CARTESIAN_POINT('Ctrl Pts',(-0.833688282341747,-3.84537601666013,
34.3658250850928));
#26778=CARTESIAN_POINT('Ctrl Pts',(-0.719839417234603,-3.86830327838563,
34.371676401853));
#26779=CARTESIAN_POINT('Ctrl Pts',(-0.60524658378432,-3.88615048252347,
34.3775277186131));
#26780=CARTESIAN_POINT('Ctrl Pts',(-0.490615717121421,-3.90400361012519,
34.3833809774176));
#26781=CARTESIAN_POINT('Ctrl Pts',(-0.375240799399043,-3.91677326392377,
34.3892342362222));
#26782=CARTESIAN_POINT('Ctrl Pts',(-0.259607991416861,-3.9244225932986,
34.3950874950267));
#26783=CARTESIAN_POINT('Ctrl Pts',(-0.143843628561474,-3.93208062527759,
34.4009474130548));
#26784=CARTESIAN_POINT('Ctrl Pts',(-0.0278212025839399,-3.93460667824842,
34.4068073310829));
#26785=CARTESIAN_POINT('Ctrl Pts',(0.0879718037122605,-3.93201601748411,
34.412667249111));
#26786=CARTESIAN_POINT('Ctrl Pts',(0.203842776753245,-3.92942361235377,
34.4185311127896));
#26787=CARTESIAN_POINT('Ctrl Pts',(0.319483611034425,-3.9217076608176,34.4243949764682));
#26788=CARTESIAN_POINT('Ctrl Pts',(0.434412373694578,-3.90893526290485,
34.4302588401468));
#26789=CARTESIAN_POINT('Ctrl Pts',(0.549510683911981,-3.89614402263432,
34.4361313544342));
#26790=CARTESIAN_POINT('Ctrl Pts',(0.663894419018809,-3.87828151180982,
34.4420038687216));
#26791=CARTESIAN_POINT('Ctrl Pts',(0.777092162551848,-3.85546583059693,
34.447876383009));
#26792=CARTESIAN_POINT('Ctrl Pts',(0.80837759202277,-3.84916006545411,34.4494994200575));
#26793=CARTESIAN_POINT('Ctrl Pts',(0.839572523282062,-3.84247624389803,
34.4511224571059));
#26794=CARTESIAN_POINT('Ctrl Pts',(0.870667236762643,-3.83541752131735,
34.4527454941544));
#26795=CARTESIAN_POINT('Ctrl Pts',(0.983167448893481,-3.80987916772566,
34.4586176181204));
#26796=CARTESIAN_POINT('Ctrl Pts',(1.09473167951738,-3.77934402944444,34.4644897420864));
#26797=CARTESIAN_POINT('Ctrl Pts',(1.20488201210318,-3.74389480847288,34.4703618660525));
#26798=CARTESIAN_POINT('Ctrl Pts',(1.31488953259553,-3.70849154812023,34.4762263766932));
#26799=CARTESIAN_POINT('Ctrl Pts',(1.42348641061621,-3.66818700057308,34.4820908873339));
#26800=CARTESIAN_POINT('Ctrl Pts',(1.53020532523458,-3.62311477359243,34.4879553979747));
#26801=CARTESIAN_POINT('Ctrl Pts',(1.63681442715162,-3.5780889254849,34.4938138740923));
#26802=CARTESIAN_POINT('Ctrl Pts',(1.7415490307667,-3.5283053158788,34.4996723502099));
#26803=CARTESIAN_POINT('Ctrl Pts',(1.84395802764502,-3.47394700481793,34.5055308263276));
#26804=CARTESIAN_POINT('Ctrl Pts',(1.95040514692448,-3.41744527354718,34.5116203099188));
#26805=CARTESIAN_POINT('Ctrl Pts',(2.05433904962835,-3.3560007849713,34.5177097935101));
#26806=CARTESIAN_POINT('Ctrl Pts',(2.15527686239892,-3.28987395600619,34.5237992771013));
#26807=CARTESIAN_POINT('Ctrl Pts',(2.25227297506802,-3.22632943114782,34.5296509616218));
#26808=CARTESIAN_POINT('Ctrl Pts',(2.3465022275652,-3.15846164931986,34.5355026461422));
#26809=CARTESIAN_POINT('Ctrl Pts',(2.43756296134221,-3.08654755503501,34.5413543306626));
#26810=CARTESIAN_POINT('Ctrl Pts',(2.52860980637792,-3.01464442921273,34.547205122674));
#26811=CARTESIAN_POINT('Ctrl Pts',(2.61648876923229,-2.93869647417318,34.5530559146853));
#26812=CARTESIAN_POINT('Ctrl Pts',(2.70082990059299,-2.85902200902037,34.5589067066966));
#26813=CARTESIAN_POINT('Ctrl Pts',(2.78517859638419,-2.7793403979834,34.5647580234568));
#26814=CARTESIAN_POINT('Ctrl Pts',(2.86598852937225,-2.69593189633577,34.570609340217));
#26815=CARTESIAN_POINT('Ctrl Pts',(2.9429258910973,-2.60915239100923,34.5764606569771));
#26816=CARTESIAN_POINT('Ctrl Pts',(3.01988878823249,-2.5223440836779,34.5823139157817));
#26817=CARTESIAN_POINT('Ctrl Pts',(3.09297628425374,-2.4321628571224,34.5881671745863));
#26818=CARTESIAN_POINT('Ctrl Pts',(3.16189467562143,-2.33899787521854,34.5940204333908));
#26819=CARTESIAN_POINT('Ctrl Pts',(3.23089147510185,-2.24572689997592,34.599880351419));
#26820=CARTESIAN_POINT('Ctrl Pts',(3.29570945667985,-2.14946572640307,34.6057402694471));
#26821=CARTESIAN_POINT('Ctrl Pts',(3.35609805496617,-2.05063279147007,34.6116001874753));
#26822=CARTESIAN_POINT('Ctrl Pts',(3.41652731462377,-1.9517333094938,34.6174640511539));
#26823=CARTESIAN_POINT('Ctrl Pts',(3.47252105314246,-1.85025897920198,34.6233279148325));
#26824=CARTESIAN_POINT('Ctrl Pts',(3.52387531996301,-1.7466515764043,34.6291917785112));
#26825=CARTESIAN_POINT('Ctrl Pts',(3.57530534667407,-1.64289132777746,34.6350642927986));
#26826=CARTESIAN_POINT('Ctrl Pts',(3.62208207524941,-1.53699210297488,34.640936807086));
#26827=CARTESIAN_POINT('Ctrl Pts',(3.66405015128883,-1.42941438667739,34.6468093213734));
#26828=CARTESIAN_POINT('Ctrl Pts',(3.67564922775244,-1.3996822122517,34.6484323584216));
#26829=CARTESIAN_POINT('Ctrl Pts',(3.68688129123842,-1.36982190487914,34.6500553954697));
#26830=CARTESIAN_POINT('Ctrl Pts',(3.6977437448767,-1.33984334801695,34.6516784325179));
#26831=CARTESIAN_POINT('Ctrl Pts',(3.74330859657717,-1.21409197147652,34.6584866035691));
#26832=CARTESIAN_POINT('Ctrl Pts',(3.78249192574234,-1.08591200323833,34.6652947746203));
#26833=CARTESIAN_POINT('Ctrl Pts',(3.81506507350435,-0.955911860438615,
34.6721029456715));
#26834=CARTESIAN_POINT('Ctrl Pts',(3.84749838015831,-0.826469826549651,
34.6788818882861));
#26835=CARTESIAN_POINT('Ctrl Pts',(3.873378040257,-0.695223338518079,34.6856608309007));
#26836=CARTESIAN_POINT('Ctrl Pts',(3.89252502226064,-0.562794768165829,
34.6924397735153));
#26837=CARTESIAN_POINT('Ctrl Pts',(3.91152246576056,-0.431400468919896,
34.6991657723848));
#26838=CARTESIAN_POINT('Ctrl Pts',(3.92389189775187,-0.298842620994969,
34.7058917712543));
#26839=CARTESIAN_POINT('Ctrl Pts',(3.92950587279998,-0.165748591639581,
34.7126177701238));
#26840=CARTESIAN_POINT('Ctrl Pts',(3.9317925032017,-0.111538009796322,34.7153573393889));
#26841=CARTESIAN_POINT('Ctrl Pts',(3.9329589488365,-0.0572386882909903,
34.718096908654));
#26842=CARTESIAN_POINT('Ctrl Pts',(3.93299893535526,-0.00289387187375899,
34.7208364779192));
#26843=CARTESIAN_POINT('',(3.93133412486678,0.00259602383233126,35.9708370172092));
#26844=CARTESIAN_POINT('Ctrl Pts',(3.93299893535593,-0.00289387096241059,
34.7208364779651));
#26845=CARTESIAN_POINT('Ctrl Pts',(3.93308449943932,0.113394468515101,34.7266986738786));
#26846=CARTESIAN_POINT('Ctrl Pts',(3.92800824320406,0.229730550276868,34.7325608697921));
#26847=CARTESIAN_POINT('Ctrl Pts',(3.91778417834047,0.345624264115084,34.7384230657055));
#26848=CARTESIAN_POINT('Ctrl Pts',(3.90756092742359,0.461508751553829,34.7442847949245));
#26849=CARTESIAN_POINT('Ctrl Pts',(3.89219071857662,0.576950531920689,34.7501465241435));
#26850=CARTESIAN_POINT('Ctrl Pts',(3.8717395335229,0.691463653821281,34.7560082533624));
#26851=CARTESIAN_POINT('Ctrl Pts',(3.85128510293533,0.805994948566741,34.761870912818));
#26852=CARTESIAN_POINT('Ctrl Pts',(3.825748164523,0.919596887314197,34.7677335722735));
#26853=CARTESIAN_POINT('Ctrl Pts',(3.79524588350174,1.03179343076175,34.7735962317291));
#26854=CARTESIAN_POINT('Ctrl Pts',(3.76473149296649,1.14403451663584,34.7794612186813));
#26855=CARTESIAN_POINT('Ctrl Pts',(3.72924794657055,1.25486870131012,34.7853262056335));
#26856=CARTESIAN_POINT('Ctrl Pts',(3.68896215429787,1.36383548280502,34.7911911925857));
#26857=CARTESIAN_POINT('Ctrl Pts',(3.64862612139279,1.47293815737053,34.7970634937953));
#26858=CARTESIAN_POINT('Ctrl Pts',(3.60347602983005,1.58016839428293,34.8029357950049));
#26859=CARTESIAN_POINT('Ctrl Pts',(3.55372687053111,1.68508585231292,34.8088080962145));
#26860=CARTESIAN_POINT('Ctrl Pts',(3.5039418090126,1.7900790255845,34.8146846352574));
#26861=CARTESIAN_POINT('Ctrl Pts',(3.4495512622404,1.89275573424209,34.8205611743004));
#26862=CARTESIAN_POINT('Ctrl Pts',(3.39081520360784,1.99270199853916,34.8264377133433));
#26863=CARTESIAN_POINT('Ctrl Pts',(3.33198561160341,2.0928074207934,34.8323236103943));
#26864=CARTESIAN_POINT('Ctrl Pts',(3.26879691658386,2.1901733754738,34.8382095074454));
#26865=CARTESIAN_POINT('Ctrl Pts',(3.20155135893729,2.28441631409137,34.8440954044964));
#26866=CARTESIAN_POINT('Ctrl Pts',(3.17673668813112,2.31919344405276,34.8462673932914));
#26867=CARTESIAN_POINT('Ctrl Pts',(3.15136996528233,2.35354564591212,34.8484393820864));
#26868=CARTESIAN_POINT('Ctrl Pts',(3.12546767104165,2.3874548869609,34.8506113708814));
#26869=CARTESIAN_POINT('Ctrl Pts',(3.05543900278248,2.47913089721161,34.8564834948474));
#26870=CARTESIAN_POINT('Ctrl Pts',(2.98125596041048,2.56787687429776,34.8623556188135));
#26871=CARTESIAN_POINT('Ctrl Pts',(2.90319258488516,2.65329263653066,34.8682277427795));
#26872=CARTESIAN_POINT('Ctrl Pts',(2.82523042007632,2.73859765553172,34.8740922534202));
#26873=CARTESIAN_POINT('Ctrl Pts',(2.74339820312646,2.82058074365277,34.8799567640609));
#26874=CARTESIAN_POINT('Ctrl Pts',(2.65801185747507,2.89887253350711,34.8858212747017));
#26875=CARTESIAN_POINT('Ctrl Pts',(2.57271337352382,2.97708376188864,34.8916797508193));
#26876=CARTESIAN_POINT('Ctrl Pts',(2.48386833801903,3.05161096930942,34.8975382269369));
#26877=CARTESIAN_POINT('Ctrl Pts',(2.39183089826845,3.1221201056475,34.9033967030545));
#26878=CARTESIAN_POINT('Ctrl Pts',(2.29616430035269,3.19540951063011,34.9094861866458));
#26879=CARTESIAN_POINT('Ctrl Pts',(2.19704866423798,3.26435711381674,34.915575670237));
#26880=CARTESIAN_POINT('Ctrl Pts',(2.09492169686575,3.32863216411804,34.9216651538283));
#26881=CARTESIAN_POINT('Ctrl Pts',(1.99678286700722,3.39039722370975,34.9275168383487));
#26882=CARTESIAN_POINT('Ctrl Pts',(1.89586386492034,3.44784757492006,34.9333685228691));
#26883=CARTESIAN_POINT('Ctrl Pts',(1.79258363747825,3.50073319501005,34.9392202073895));
#26884=CARTESIAN_POINT('Ctrl Pts',(1.68931916251607,3.55361074889328,34.9450709994008));
#26885=CARTESIAN_POINT('Ctrl Pts',(1.58369454614019,3.60192476758779,34.9509217914122));
#26886=CARTESIAN_POINT('Ctrl Pts',(1.47615316630719,3.6454712767489,34.9567725834235));
#26887=CARTESIAN_POINT('Ctrl Pts',(1.36860214124798,3.68902169153158,34.9626239001836));
#26888=CARTESIAN_POINT('Ctrl Pts',(1.25913439419929,3.72780359159629,34.9684752169438));
#26889=CARTESIAN_POINT('Ctrl Pts',(1.1482124287817,3.76166149705037,34.9743265337039));
#26890=CARTESIAN_POINT('Ctrl Pts',(1.03725364850827,3.79553063989916,34.9801797925084));
#26891=CARTESIAN_POINT('Ctrl Pts',(0.924840085335178,3.824472417874,34.986033051313));
#26892=CARTESIAN_POINT('Ctrl Pts',(0.811447817419639,3.84838166501257,34.9918863101175));
#26893=CARTESIAN_POINT('Ctrl Pts',(0.697926543682018,3.87231811358329,34.9977462281457));
#26894=CARTESIAN_POINT('Ctrl Pts',(0.583424747509723,3.89121051805523,35.0036061461738));
#26895=CARTESIAN_POINT('Ctrl Pts',(0.468427178755177,3.90500511884472,35.0094660642019));
#26896=CARTESIAN_POINT('Ctrl Pts',(0.353352178846265,3.91880900793374,35.0153299278806));
#26897=CARTESIAN_POINT('Ctrl Pts',(0.237781152898853,3.92750822761217,35.0211937915592));
#26898=CARTESIAN_POINT('Ctrl Pts',(0.1222006797235,3.93110111722849,35.0270576552379));
#26899=CARTESIAN_POINT('Ctrl Pts',(0.00644969756160697,3.93469930722082,
35.0329301695253));
#26900=CARTESIAN_POINT('Ctrl Pts',(-0.109310347814557,3.93317613797182,
35.0388026838127));
#26901=CARTESIAN_POINT('Ctrl Pts',(-0.22459608319201,3.92658192317629,35.0446751981001));
#26902=CARTESIAN_POINT('Ctrl Pts',(-0.256458588840009,3.92475942358014,
35.0462982351483));
#26903=CARTESIAN_POINT('Ctrl Pts',(-0.288284915948909,3.92254987399867,
35.0479212721966));
#26904=CARTESIAN_POINT('Ctrl Pts',(-0.320064996648115,3.91995502498698,
35.0495443092448));
#26905=CARTESIAN_POINT('Ctrl Pts',(-0.435044857224395,3.91056689975203,
35.0554164332108));
#26906=CARTESIAN_POINT('Ctrl Pts',(-0.549804072018368,3.89609987364649,
35.0612885571768));
#26907=CARTESIAN_POINT('Ctrl Pts',(-0.663857834012495,3.87656829892371,
35.0671606811429));
#26908=CARTESIAN_POINT('Ctrl Pts',(-0.777763723039442,3.85706204727539,
35.0730251917836));
#26909=CARTESIAN_POINT('Ctrl Pts',(-0.890965574426317,3.83250437410963,
35.0788897024243));
#26910=CARTESIAN_POINT('Ctrl Pts',(-1.00298187849455,3.80296152378795,35.084754213065));
#26911=CARTESIAN_POINT('Ctrl Pts',(-1.11488291890037,3.77344907276532,35.0906126891826));
#26912=CARTESIAN_POINT('Ctrl Pts',(-1.22560044112233,3.73896175259171,35.0964711653002));
#26913=CARTESIAN_POINT('Ctrl Pts',(-1.33466199872459,3.69961705439367,35.1023296414178));
#26914=CARTESIAN_POINT('Ctrl Pts',(-1.44802399800991,3.65872094262829,35.108419125009));
#26915=CARTESIAN_POINT('Ctrl Pts',(-1.55959630369201,3.61257658314203,35.1145086086003));
#26916=CARTESIAN_POINT('Ctrl Pts',(-1.66886409402027,3.56137356025592,35.1205980921916));
#26917=CARTESIAN_POINT('Ctrl Pts',(-1.77386489214357,3.51217005524117,35.126449776712));
#26918=CARTESIAN_POINT('Ctrl Pts',(-1.87673737398393,3.45829575416629,35.1323014612324));
#26919=CARTESIAN_POINT('Ctrl Pts',(-1.97704478296076,3.39996807722773,35.1381531457528));
#26920=CARTESIAN_POINT('Ctrl Pts',(-2.07733689287734,3.34164929652778,35.1440039377641));
#26921=CARTESIAN_POINT('Ctrl Pts',(-2.17506435053188,3.27887869825674,35.1498547297754));
#26922=CARTESIAN_POINT('Ctrl Pts',(-2.26981594510763,3.21191914209171,35.1557055217867));
#26923=CARTESIAN_POINT('Ctrl Pts',(-2.36457603781286,3.14495358042376,35.1615568385468));
#26924=CARTESIAN_POINT('Ctrl Pts',(-2.45635939922802,3.07379855260523,35.167408155307));
#26925=CARTESIAN_POINT('Ctrl Pts',(-2.54478528928676,2.99875921531384,35.1732594720671));
#26926=CARTESIAN_POINT('Ctrl Pts',(-2.63324052778291,2.92369497256443,35.1791127308716));
#26927=CARTESIAN_POINT('Ctrl Pts',(-2.71833576408511,2.84474412420826,35.1849659896761));
#26928=CARTESIAN_POINT('Ctrl Pts',(-2.79972525940178,2.76225043612407,35.1908192484807));
#26929=CARTESIAN_POINT('Ctrl Pts',(-2.88120735114467,2.67966289537901,35.1966791665088));
#26930=CARTESIAN_POINT('Ctrl Pts',(-2.95897499634738,2.59352476425835,35.2025390845369));
#26931=CARTESIAN_POINT('Ctrl Pts',(-3.03272102596396,2.50421488268801,35.208399002565));
#26932=CARTESIAN_POINT('Ctrl Pts',(-3.10651671089285,2.4148448662184,35.2142628662436));
#26933=CARTESIAN_POINT('Ctrl Pts',(-3.1762851400794,2.32229917614978,35.2201267299223));
#26934=CARTESIAN_POINT('Ctrl Pts',(-3.24176199442419,2.22698634290983,35.2259905936009));
#26935=CARTESIAN_POINT('Ctrl Pts',(-3.3073354428715,2.13153290032515,35.2318631078883));
#26936=CARTESIAN_POINT('Ctrl Pts',(-3.36860446279633,2.03330451671135,35.2377356221756));
#26937=CARTESIAN_POINT('Ctrl Pts',(-3.42535020062493,1.93273510939258,35.243608136463));
#26938=CARTESIAN_POINT('Ctrl Pts',(-3.44103350599065,1.90493988131405,35.2452311735114));
#26939=CARTESIAN_POINT('Ctrl Pts',(-3.45637158232295,1.8769659537885,35.2468542105598));
#26940=CARTESIAN_POINT('Ctrl Pts',(-3.47136046246102,1.8488227442517,35.2484772476082));
#26941=CARTESIAN_POINT('Ctrl Pts',(-3.52559000846581,1.74700102960462,35.2543493715742));
#26942=CARTESIAN_POINT('Ctrl Pts',(-3.57542672946076,1.6426206029676,35.2602214955402));
#26943=CARTESIAN_POINT('Ctrl Pts',(-3.62062073765856,1.53609715644447,35.2660936195063));
#26944=CARTESIAN_POINT('Ctrl Pts',(-3.66575615092748,1.4297118196846,35.271958130147));
#26945=CARTESIAN_POINT('Ctrl Pts',(-3.70626066176825,1.32118936546262,35.2778226407877));
#26946=CARTESIAN_POINT('Ctrl Pts',(-3.74192982829283,1.21097075114654,35.2836871514284));
#26947=CARTESIAN_POINT('Ctrl Pts',(-3.77756229159994,1.10086555068798,35.289545627546));
#26948=CARTESIAN_POINT('Ctrl Pts',(-3.80836918061562,0.989068052643565,
35.2954041036637));
#26949=CARTESIAN_POINT('Ctrl Pts',(-3.8341940719254,0.876039279263296,35.3012625797813));
#26950=CARTESIAN_POINT('Ctrl Pts',(-3.86103727290798,0.758553631627159,
35.3073520633725));
#26951=CARTESIAN_POINT('Ctrl Pts',(-3.88249732192508,0.639738028258825,
35.3134415469638));
#26952=CARTESIAN_POINT('Ctrl Pts',(-3.89845556038526,0.52012810316428,35.3195310305551));
#26953=CARTESIAN_POINT('Ctrl Pts',(-3.91379061722067,0.405189038681629,
35.3253827150755));
#26954=CARTESIAN_POINT('Ctrl Pts',(-3.92404544006576,0.289516974445092,
35.3312343995959));
#26955=CARTESIAN_POINT('Ctrl Pts',(-3.92916697493633,0.173596898214589,
35.3370860841163));
#26956=CARTESIAN_POINT('Ctrl Pts',(-3.9342877286615,0.0576945023155024,
35.3429368761276));
#26957=CARTESIAN_POINT('Ctrl Pts',(-3.93427673289576,-0.0584554174693667,
35.3487876681389));
#26958=CARTESIAN_POINT('Ctrl Pts',(-3.92913297192955,-0.174364815533547,
35.3546384601502));
#26959=CARTESIAN_POINT('Ctrl Pts',(-3.92398874962709,-0.290284609338774,
35.3604897769103));
#26960=CARTESIAN_POINT('Ctrl Pts',(-3.91371086531983,-0.405963425509345,
35.3663410936704));
#26961=CARTESIAN_POINT('Ctrl Pts',(-3.89835035856407,-0.520916002713838,
35.3721924104306));
#26962=CARTESIAN_POINT('Ctrl Pts',(-3.88298475367618,-0.635906732528653,
35.3780456692351));
#26963=CARTESIAN_POINT('Ctrl Pts',(-3.86253322674438,-0.750170334535612,
35.3838989280396));
#26964=CARTESIAN_POINT('Ctrl Pts',(-3.8370982175806,-0.863230136545143,
35.3897521868441));
#26965=CARTESIAN_POINT('Ctrl Pts',(-3.81163427113265,-0.976418566132486,
35.3956121048722));
#26966=CARTESIAN_POINT('Ctrl Pts',(-3.78117561670702,-1.08840005854956,
35.4014720229003));
#26967=CARTESIAN_POINT('Ctrl Pts',(-3.74587504796018,-1.19871144362158,
35.4073319409285));
#26968=CARTESIAN_POINT('Ctrl Pts',(-3.71055071033013,-1.3090971045062,35.4131958046071));
#26969=CARTESIAN_POINT('Ctrl Pts',(-3.67037810963136,-1.41781003204734,
35.4190596682857));
#26970=CARTESIAN_POINT('Ctrl Pts',(-3.62555817622155,-1.52440706861163,
35.4249235319644));
#26971=CARTESIAN_POINT('Ctrl Pts',(-3.58067212263409,-1.6311613614335,35.4307960462517));
#26972=CARTESIAN_POINT('Ctrl Pts',(-3.53112522943475,-1.73579316120889,
35.4366685605391));
#26973=CARTESIAN_POINT('Ctrl Pts',(-3.47716435577114,-1.8378838491468,35.4425410748265));
#26974=CARTESIAN_POINT('Ctrl Pts',(-3.46225072715634,-1.86609952657313,
35.4441641118749));
#26975=CARTESIAN_POINT('Ctrl Pts',(-3.44700018962873,-1.89412127369666,
35.4457871489232));
#26976=CARTESIAN_POINT('Ctrl Pts',(-3.43141852376622,-1.92194066369231,
35.4474101859715));
#26977=CARTESIAN_POINT('Ctrl Pts',(-3.37504428780202,-2.0225908040453,35.4532823099376));
#26978=CARTESIAN_POINT('Ctrl Pts',(-3.31414339153919,-2.12092723197976,
35.4591544339036));
#26979=CARTESIAN_POINT('Ctrl Pts',(-3.24893058939597,-2.21651506317623,
35.4650265578697));
#26980=CARTESIAN_POINT('Ctrl Pts',(-3.18380233694565,-2.31197896285149,
35.4708910685104));
#26981=CARTESIAN_POINT('Ctrl Pts',(-3.11437352686747,-2.40470101416566,
35.4767555791511));
#26982=CARTESIAN_POINT('Ctrl Pts',(-3.04090472941805,-2.49427092085101,
35.4826200897918));
#26983=CARTESIAN_POINT('Ctrl Pts',(-2.96751153063028,-2.58374866099349,
35.4884785659094));
#26984=CARTESIAN_POINT('Ctrl Pts',(-2.89008687375796,-2.67008039031691,
35.494337042027));
#26985=CARTESIAN_POINT('Ctrl Pts',(-2.80893415916184,-2.75288537529149,
35.5001955181447));
#26986=CARTESIAN_POINT('Ctrl Pts',(-2.72458148553147,-2.83895547051,35.5062850017359));
#26987=CARTESIAN_POINT('Ctrl Pts',(-2.63620095757036,-2.92121459514035,
35.5123744853272));
#26988=CARTESIAN_POINT('Ctrl Pts',(-2.54417916322711,-2.99927347626071,
35.5184639689185));
#26989=CARTESIAN_POINT('Ctrl Pts',(-2.45575089153084,-3.0742840973563,35.5243156534389));
#26990=CARTESIAN_POINT('Ctrl Pts',(-2.36396075026656,-3.14541607190399,
35.5301673379593));
#26991=CARTESIAN_POINT('Ctrl Pts',(-2.26918816081457,-3.21236269602593,
35.5360190224797));
#26992=CARTESIAN_POINT('Ctrl Pts',(-2.17443002624266,-3.27929910933239,
35.541869814491));
#26993=CARTESIAN_POINT('Ctrl Pts',(-2.07669068551382,-3.34205120300941,
35.5477206065023));
#26994=CARTESIAN_POINT('Ctrl Pts',(-1.97638025177208,-3.40035440805886,
35.5535713985136));
#26995=CARTESIAN_POINT('Ctrl Pts',(-1.87606082133687,-3.45866284223598,
35.5594227152738));
#26996=CARTESIAN_POINT('Ctrl Pts',(-1.77317019692764,-3.51252138682477,
35.5652740320339));
#26997=CARTESIAN_POINT('Ctrl Pts',(-1.66814427682793,-3.5617107787812,35.5711253487941));
#26998=CARTESIAN_POINT('Ctrl Pts',(-1.56308349876298,-3.61091649663237,
35.5769786075986));
#26999=CARTESIAN_POINT('Ctrl Pts',(-1.45588638998729,-3.65544980515002,
35.5828318664031));
#27000=CARTESIAN_POINT('Ctrl Pts',(-1.34700939553298,-3.69513933273779,
35.5886851252076));
#27001=CARTESIAN_POINT('Ctrl Pts',(-1.23800853226013,-3.73487401490496,
35.5945450432357));
#27002=CARTESIAN_POINT('Ctrl Pts',(-1.12732435725081,-3.76975377516615,
35.6004049612638));
#27003=CARTESIAN_POINT('Ctrl Pts',(-1.01542916296309,-3.79965690753837,
35.6062648792919));
#27004=CARTESIAN_POINT('Ctrl Pts',(-0.903458626439311,-3.82958017454527,
35.6121287429706));
#27005=CARTESIAN_POINT('Ctrl Pts',(-0.790275849730697,-3.85452005260933,
35.6179926066492));
#27006=CARTESIAN_POINT('Ctrl Pts',(-0.676362296463616,-3.87440615371214,
35.6238564703278));
#27007=CARTESIAN_POINT('Ctrl Pts',(-0.562280693316787,-3.89432159159536,
35.6297289846152));
#27008=CARTESIAN_POINT('Ctrl Pts',(-0.447466570445664,-3.90916831983273,
35.6356014989026));
#27009=CARTESIAN_POINT('Ctrl Pts',(-0.33240556098613,-3.91892785631804,
35.64147401319));
#27010=CARTESIAN_POINT('Ctrl Pts',(-0.300605164761025,-3.92162518296817,
35.6430970502384));
#27011=CARTESIAN_POINT('Ctrl Pts',(-0.268785901634046,-3.92393423057186,
35.6447200872867));
#27012=CARTESIAN_POINT('Ctrl Pts',(-0.236957985810335,-3.92585530973324,
35.6463431243351));
#27013=CARTESIAN_POINT('Ctrl Pts',(-0.12180505847427,-3.93280574564311,
35.6522152483011));
#27014=CARTESIAN_POINT('Ctrl Pts',(-0.00615301487706181,-3.93469705103759,
35.6580873722671));
#27015=CARTESIAN_POINT('Ctrl Pts',(0.109516173067406,-3.93147494050727,
35.6639594962331));
#27016=CARTESIAN_POINT('Ctrl Pts',(0.225035393613353,-3.92825700750722,
35.6698240068738));
#27017=CARTESIAN_POINT('Ctrl Pts',(0.340571304870519,-3.9199388539467,35.6756885175145));
#27018=CARTESIAN_POINT('Ctrl Pts',(0.455637867855379,-3.90651803187649,
35.6815530281552));
#27019=CARTESIAN_POINT('Ctrl Pts',(0.570586028491408,-3.89311101969871,
35.6874115042727));
#27020=CARTESIAN_POINT('Ctrl Pts',(0.685065393318412,-3.87461183029995,
35.6932699803903));
#27021=CARTESIAN_POINT('Ctrl Pts',(0.798591655527019,-3.85107002892996,
35.6991284565079));
#27022=CARTESIAN_POINT('Ctrl Pts',(0.91659440863619,-3.8265999431475,35.7052179400992));
#27023=CARTESIAN_POINT('Ctrl Pts',(1.03356689370182,-3.79668140298861,35.7113074236904));
#27024=CARTESIAN_POINT('Ctrl Pts',(1.14897266828838,-3.76142935697672,35.7173969072817));
#27025=CARTESIAN_POINT('Ctrl Pts',(1.25987175760961,-3.7275539307822,35.7232485918021));
#27026=CARTESIAN_POINT('Ctrl Pts',(1.36932377014749,-3.68875386908664,35.7291002763224));
#27027=CARTESIAN_POINT('Ctrl Pts',(1.47686561295159,-3.64518270615906,35.7349519608428));
#27028=CARTESIAN_POINT('Ctrl Pts',(1.58439105328696,-3.60161818878097,35.7408027528541));
#27029=CARTESIAN_POINT('Ctrl Pts',(1.69000652011514,-3.55328417225595,35.7466535448653));
#27030=CARTESIAN_POINT('Ctrl Pts',(1.79326779031035,-3.50038278367315,35.7525043368766));
#27031=CARTESIAN_POINT('Ctrl Pts',(1.89653832185472,-3.4474766504438,35.7583556536367));
#27032=CARTESIAN_POINT('Ctrl Pts',(1.99745386907001,-3.39000251933694,35.7642069703967));
#27033=CARTESIAN_POINT('Ctrl Pts',(2.09559439821291,-3.32820869510592,35.7700582871568));
#27034=CARTESIAN_POINT('Ctrl Pts',(2.19376750006895,-3.26639436158554,35.7759115459613));
#27035=CARTESIAN_POINT('Ctrl Pts',(2.28916340279892,-3.2002577042806,35.7817648047657));
#27036=CARTESIAN_POINT('Ctrl Pts',(2.38139126813706,-3.13009019487308,35.7876180635702));
#27037=CARTESIAN_POINT('Ctrl Pts',(2.4737240606623,-3.05984285623649,35.7934779815983));
#27038=CARTESIAN_POINT('Ctrl Pts',(2.56288129257514,-2.98555576266775,35.7993378996263));
#27039=CARTESIAN_POINT('Ctrl Pts',(2.64850535321294,-2.90756055723736,35.8051978176544));
#27040=CARTESIAN_POINT('Ctrl Pts',(2.73418706698117,-2.82951283540307,35.811061681333));
#27041=CARTESIAN_POINT('Ctrl Pts',(2.81633058015491,-2.74775232106522,35.8169255450116));
#27042=CARTESIAN_POINT('Ctrl Pts',(2.89461650753271,-2.66264610384466,35.8227894086902));
#27043=CARTESIAN_POINT('Ctrl Pts',(2.9730179254756,-2.57741433449169,35.8286619229776));
#27044=CARTESIAN_POINT('Ctrl Pts',(3.04755013455306,-2.48882732664115,35.834534437265));
#27045=CARTESIAN_POINT('Ctrl Pts',(3.11793517238354,-2.39728372555558,35.8404069515523));
#27046=CARTESIAN_POINT('Ctrl Pts',(3.13738808786115,-2.37198303681087,35.842029988601));
#27047=CARTESIAN_POINT('Ctrl Pts',(3.15652448380116,-2.34645666696298,35.8436530256498));
#27048=CARTESIAN_POINT('Ctrl Pts',(3.17533910233628,-2.32071337850546,35.8452760626985));
#27049=CARTESIAN_POINT('Ctrl Pts',(3.24386965336691,-2.22694577221349,35.8511878287586));
#27050=CARTESIAN_POINT('Ctrl Pts',(3.30835742877721,-2.12998392340895,35.8570995948188));
#27051=CARTESIAN_POINT('Ctrl Pts',(3.36849264223259,-2.03020844230953,35.8630113608789));
#27052=CARTESIAN_POINT('Ctrl Pts',(3.42854818206181,-1.9305651545445,35.8689152943929));
#27053=CARTESIAN_POINT('Ctrl Pts',(3.48426242031965,-1.82811599172916,35.8748192279068));
#27054=CARTESIAN_POINT('Ctrl Pts',(3.53536685330977,-1.72327311025228,35.8807231614208));
#27055=CARTESIAN_POINT('Ctrl Pts',(3.58641539569186,-1.61854489069514,35.8866206380695));
#27056=CARTESIAN_POINT('Ctrl Pts',(3.63286398405451,-1.51142852206661,35.8925181147183));
#27057=CARTESIAN_POINT('Ctrl Pts',(3.67448867569264,-1.40236299587752,35.898415591367));
#27058=CARTESIAN_POINT('Ctrl Pts',(3.71708453564452,-1.29075280259325,35.9044506652502));
#27059=CARTESIAN_POINT('Ctrl Pts',(3.75462837515732,-1.17710173246275,35.9104857391334));
#27060=CARTESIAN_POINT('Ctrl Pts',(3.78693102001708,-1.06190510387342,35.9165208130165));
#27061=CARTESIAN_POINT('Ctrl Pts',(3.81844890924432,-0.949507044984043,
35.9224092717156));
#27062=CARTESIAN_POINT('Ctrl Pts',(3.84497722627513,-0.835638076692662,
35.9282977304147));
#27063=CARTESIAN_POINT('Ctrl Pts',(3.8663899645524,-0.720775722405051,35.9341861891138));
#27064=CARTESIAN_POINT('Ctrl Pts',(3.88860242803569,-0.601623476803267,
35.940294570589));
#27065=CARTESIAN_POINT('Ctrl Pts',(3.90530960984758,-0.481402630182505,
35.9464029520642));
#27066=CARTESIAN_POINT('Ctrl Pts',(3.91642873442305,-0.360659074730551,
35.9525113335394));
#27067=CARTESIAN_POINT('Ctrl Pts',(3.92754785899851,-0.239915519278558,
35.9586197150147));
#27068=CARTESIAN_POINT('Ctrl Pts',(3.93307887719384,-0.118649740920967,
35.9647280964899));
#27069=CARTESIAN_POINT('Ctrl Pts',(3.93299914955306,0.00258642898096291,
35.9708364779651));
#27070=CARTESIAN_POINT('',(3.93496388660084,0.00195648875352047,37.2208358380349));
#27071=CARTESIAN_POINT('Ctrl Pts',(3.9282775211904,0.00261363778016546,
35.9708380071379));
#27072=CARTESIAN_POINT('Ctrl Pts',(3.93118033843727,0.487443495032958,35.9952950051125));
#27073=CARTESIAN_POINT('Ctrl Pts',(3.62292672813806,2.28323870400638,36.086062982542));
#27074=CARTESIAN_POINT('Ctrl Pts',(0.933577472432809,4.55771548976854,36.2431419394252));
#27075=CARTESIAN_POINT('Ctrl Pts',(-3.3305959172111,3.24830235946759,36.4420748777888));
#27076=CARTESIAN_POINT('Ctrl Pts',(-4.53293738673136,-1.04728985028724,
36.6410078161523));
#27077=CARTESIAN_POINT('Ctrl Pts',(-1.56812897439943,-4.38010375485825,
36.8399407545156));
#27078=CARTESIAN_POINT('Ctrl Pts',(2.7129575081135,-3.70599985813041,37.0332163973897));
#27079=CARTESIAN_POINT('Ctrl Pts',(3.93099554165428,-1.19260423393931,37.1601810608092));
#27080=CARTESIAN_POINT('Ctrl Pts',(3.93831984400274,0.00193663700642166,
37.2208347447742));
#27081=CARTESIAN_POINT('',(3.93300214177874,-0.00350894827663559,38.4708364798097));
#27082=CARTESIAN_POINT('Ctrl Pts',(3.93299950757024,0.00196810879246953,
37.220836477965));
#27083=CARTESIAN_POINT('Ctrl Pts',(3.93294383452817,0.113223161314397,37.2264931957242));
#27084=CARTESIAN_POINT('Ctrl Pts',(3.92816790717577,0.22435667800964,37.2321499134834));
#27085=CARTESIAN_POINT('Ctrl Pts',(3.91869980905131,0.335083282992792,37.2378066312426));
#27086=CARTESIAN_POINT('Ctrl Pts',(3.90887116844884,0.450026325534738,37.2436787552018));
#27087=CARTESIAN_POINT('Ctrl Pts',(3.89396450975248,0.564729262387047,37.249550879161));
#27088=CARTESIAN_POINT('Ctrl Pts',(3.87399604281211,0.678707345087798,37.2554230031202));
#27089=CARTESIAN_POINT('Ctrl Pts',(3.85405346538562,0.79253765294116,37.261287513754));
#27090=CARTESIAN_POINT('Ctrl Pts',(3.82906220129585,0.905644572093272,37.2671520243879));
#27091=CARTESIAN_POINT('Ctrl Pts',(3.79909033948502,1.01754685023913,37.2730165350218));
#27092=CARTESIAN_POINT('Ctrl Pts',(3.76914931842163,1.12933398205476,37.2788750111326));
#27093=CARTESIAN_POINT('Ctrl Pts',(3.73423799979103,1.23991854148262,37.2847334872434));
#27094=CARTESIAN_POINT('Ctrl Pts',(3.69447568419538,1.34882853576318,37.2905919633542));
#27095=CARTESIAN_POINT('Ctrl Pts',(3.65314548775988,1.46203299556326,37.296681446948));
#27096=CARTESIAN_POINT('Ctrl Pts',(3.6065739399445,1.57342766445927,37.3027709305419));
#27097=CARTESIAN_POINT('Ctrl Pts',(3.55495259639291,1.6824984509352,37.3088604141357));
#27098=CARTESIAN_POINT('Ctrl Pts',(3.50534710653775,1.78730993819564,37.3147120986494));
#27099=CARTESIAN_POINT('Ctrl Pts',(3.45107901028721,1.88997522706534,37.3205637831631));
#27100=CARTESIAN_POINT('Ctrl Pts',(3.392367399822,1.99005839729012,37.3264154676768));
#27101=CARTESIAN_POINT('Ctrl Pts',(3.33366474415319,2.09012630265662,37.3322662596814));
#27102=CARTESIAN_POINT('Ctrl Pts',(3.27052013093913,2.1876125159477,37.338117051686));
#27103=CARTESIAN_POINT('Ctrl Pts',(3.20319799362034,2.28210683660223,37.3439678436907));
#27104=CARTESIAN_POINT('Ctrl Pts',(3.13586981827867,2.37660963231256,37.3498191604442));
#27105=CARTESIAN_POINT('Ctrl Pts',(3.06436361390616,2.46811966523383,37.3556704771977));
#27106=CARTESIAN_POINT('Ctrl Pts',(2.98898599387445,2.55625736740696,37.3615217939512));
#27107=CARTESIAN_POINT('Ctrl Pts',(2.91358335610828,2.64442432236928,37.3673750527492));
#27108=CARTESIAN_POINT('Ctrl Pts',(2.83430701626353,2.72921640696602,37.3732283115471));
#27109=CARTESIAN_POINT('Ctrl Pts',(2.75150206251009,2.81028920220014,37.3790815703451));
#27110=CARTESIAN_POINT('Ctrl Pts',(2.66860290196837,2.89145423355433,37.3849414883668));
#27111=CARTESIAN_POINT('Ctrl Pts',(2.58216741028541,2.96889124035578,37.3908014063884));
#27112=CARTESIAN_POINT('Ctrl Pts',(2.49257560162771,3.04229450746805,37.3966613244101));
#27113=CARTESIAN_POINT('Ctrl Pts',(2.4029234682402,3.11574719910163,37.4025251880824));
#27114=CARTESIAN_POINT('Ctrl Pts',(2.31011111636953,3.18516049589827,37.4083890517546));
#27115=CARTESIAN_POINT('Ctrl Pts',(2.21454808627185,3.25027164612278,37.4142529154269));
#27116=CARTESIAN_POINT('Ctrl Pts',(2.11884407772622,3.31547885095014,37.4201254297081));
#27117=CARTESIAN_POINT('Ctrl Pts',(2.02038164240613,3.37637102573865,37.4259979439892));
#27118=CARTESIAN_POINT('Ctrl Pts',(1.91959553306117,3.4327309812235,37.4318704582704));
#27119=CARTESIAN_POINT('Ctrl Pts',(1.89174041207018,3.44830766524553,37.4334934953822));
#27120=CARTESIAN_POINT('Ctrl Pts',(1.86370791579227,3.46353843799419,37.4351165324941));
#27121=CARTESIAN_POINT('Ctrl Pts',(1.83550747679674,3.47841936842343,37.4367395696059));
#27122=CARTESIAN_POINT('Ctrl Pts',(1.73347871087051,3.53225835184389,37.4426116935682));
#27123=CARTESIAN_POINT('Ctrl Pts',(1.62890808433844,3.5816947379408,37.4484838175304));
#27124=CARTESIAN_POINT('Ctrl Pts',(1.52221224378136,3.62648023362628,37.4543559414927));
#27125=CARTESIAN_POINT('Ctrl Pts',(1.41565473650146,3.67120766402677,37.4602204521296));
#27126=CARTESIAN_POINT('Ctrl Pts',(1.30697787232185,3.71129603691539,37.4660849627664));
#27127=CARTESIAN_POINT('Ctrl Pts',(1.19662338876077,3.74654260158225,37.4719494734033));
#27128=CARTESIAN_POINT('Ctrl Pts',(1.0863824588669,3.78175289788424,37.477807949517));
#27129=CARTESIAN_POINT('Ctrl Pts',(0.974467734634347,3.81213117071812,37.4836664256307));
#27130=CARTESIAN_POINT('Ctrl Pts',(0.861340834317039,3.83752276438043,37.4895249017444));
#27131=CARTESIAN_POINT('Ctrl Pts',(0.743753190362223,3.86391558223926,37.4956143853371));
#27132=CARTESIAN_POINT('Ctrl Pts',(0.624856227806823,3.88492019147547,37.5017038689298));
#27133=CARTESIAN_POINT('Ctrl Pts',(0.505186031405749,3.90041998683123,37.5077933525225));
#27134=CARTESIAN_POINT('Ctrl Pts',(0.390189049364761,3.91531450310821,37.5136450370389));
#27135=CARTESIAN_POINT('Ctrl Pts',(0.274478539588281,3.92512601396187,37.5194967215552));
#27136=CARTESIAN_POINT('Ctrl Pts',(0.158539689569357,3.9298033241921,37.5253484060716));
#27137=CARTESIAN_POINT('Ctrl Pts',(0.0426185227462051,3.9344799210308,37.5311991980788));
#27138=CARTESIAN_POINT('Ctrl Pts',(-0.0735305021100036,3.93402385758884,
37.537049990086));
#27139=CARTESIAN_POINT('Ctrl Pts',(-0.189419339084341,3.92843598827585,
37.5429007820933));
#27140=CARTESIAN_POINT('Ctrl Pts',(-0.305318569954967,3.92284761779523,
37.5487520988493));
#27141=CARTESIAN_POINT('Ctrl Pts',(-0.420957153596696,3.91212654639289,
37.5546034156052));
#27142=CARTESIAN_POINT('Ctrl Pts',(-0.535850027816559,3.89632567269331,
37.5604547323612));
#27143=CARTESIAN_POINT('Ctrl Pts',(-0.650781034830726,3.88051955470447,
37.5663079911616));
#27144=CARTESIAN_POINT('Ctrl Pts',(-0.76496543094427,3.85963033825317,37.572161249962));
#27145=CARTESIAN_POINT('Ctrl Pts',(-0.877926940000475,3.83376228892995,
37.5780145087623));
#27146=CARTESIAN_POINT('Ctrl Pts',(-0.991016964806267,3.80786480965508,
37.5838744267862));
#27147=CARTESIAN_POINT('Ctrl Pts',(-1.10288092238968,3.77697728386623,37.5897343448101));
#27148=CARTESIAN_POINT('Ctrl Pts',(-1.21305623145749,3.74125427889126,37.595594262834));
#27149=CARTESIAN_POINT('Ctrl Pts',(-1.3233057247134,3.70550722059488,37.6014581265084));
#27150=CARTESIAN_POINT('Ctrl Pts',(-1.43186391914719,3.66491834447394,37.6073219901828));
#27151=CARTESIAN_POINT('Ctrl Pts',(-1.53828843031218,3.61969027751929,37.6131858538572));
#27152=CARTESIAN_POINT('Ctrl Pts',(-1.64486994321869,3.57439548829174,37.6190583681404));
#27153=CARTESIAN_POINT('Ctrl Pts',(-1.74931111907896,3.52444802672684,37.6249308824235));
#27154=CARTESIAN_POINT('Ctrl Pts',(-1.85119428810024,3.47009635423932,37.6308033967067));
#27155=CARTESIAN_POINT('Ctrl Pts',(-1.87935261244782,3.45507471683406,37.6324264337942));
#27156=CARTESIAN_POINT('Ctrl Pts',(-1.90731571692631,3.43971691608275,37.6340494708818));
#27157=CARTESIAN_POINT('Ctrl Pts',(-1.93507519692215,3.42402876481152,37.6356725079694));
#27158=CARTESIAN_POINT('Ctrl Pts',(-2.03550858192254,3.36726926727036,37.6415446319685));
#27159=CARTESIAN_POINT('Ctrl Pts',(-2.13361092601821,3.30599200839285,37.6474167559676));
#27160=CARTESIAN_POINT('Ctrl Pts',(-2.22894817098408,3.24041340743226,37.6532888799667));
#27161=CARTESIAN_POINT('Ctrl Pts',(-2.32416180932104,3.17491983042843,37.6591533906405));
#27162=CARTESIAN_POINT('Ctrl Pts',(-2.41661714034022,3.10513623365194,37.6650179013144));
#27163=CARTESIAN_POINT('Ctrl Pts',(-2.50590486924698,3.03132475764051,37.6708824119883));
#27164=CARTESIAN_POINT('Ctrl Pts',(-2.59510072197035,2.95758923290243,37.6767408881391));
#27165=CARTESIAN_POINT('Ctrl Pts',(-2.6811351390289,2.87983433464965,37.6825993642899));
#27166=CARTESIAN_POINT('Ctrl Pts',(-2.76362855226727,2.79836491992969,37.6884578404407));
#27167=CARTESIAN_POINT('Ctrl Pts',(-2.84937478940238,2.71368305892279,37.6945473240195));
#27168=CARTESIAN_POINT('Ctrl Pts',(-2.93129464984765,2.62498797621149,37.7006368075984));
#27169=CARTESIAN_POINT('Ctrl Pts',(-3.00900034488857,2.53266774853325,37.7067262911772));
#27170=CARTESIAN_POINT('Ctrl Pts',(-3.08367157267096,2.44395269687256,37.7125779757308));
#27171=CARTESIAN_POINT('Ctrl Pts',(-3.15445130019248,2.3518906626465,37.7184296602843));
#27172=CARTESIAN_POINT('Ctrl Pts',(-3.22103427970653,2.25686223969374,37.7242813448378));
#27173=CARTESIAN_POINT('Ctrl Pts',(-3.28760710386799,2.16184831064238,37.7301321368822));
#27174=CARTESIAN_POINT('Ctrl Pts',(-3.3499842155701,2.06386923093621,37.7359829289266));
#27175=CARTESIAN_POINT('Ctrl Pts',(-3.40790261924258,1.96333612449819,37.741833720971));
#27176=CARTESIAN_POINT('Ctrl Pts',(-3.46582621752925,1.86279400139762,37.747685037764));
#27177=CARTESIAN_POINT('Ctrl Pts',(-3.51929010644619,1.75969775444043,37.7535363545571));
#27178=CARTESIAN_POINT('Ctrl Pts',(-3.5680766948491,1.65448411889468,37.7593876713502));
#27179=CARTESIAN_POINT('Ctrl Pts',(-3.61687947545567,1.54923556308354,37.7652409301875));
#27180=CARTESIAN_POINT('Ctrl Pts',(-3.66100169490512,1.44186859615042,37.7710941890248));
#27181=CARTESIAN_POINT('Ctrl Pts',(-3.700273731881,1.33284031644884,37.7769474478621));
#27182=CARTESIAN_POINT('Ctrl Pts',(-3.73959044845628,1.22368799582058,37.7828073659227));
#27183=CARTESIAN_POINT('Ctrl Pts',(-3.77404582853621,1.11287097908181,37.7886672839832));
#27184=CARTESIAN_POINT('Ctrl Pts',(-3.8035199767779,1.00086202158512,37.7945272020437));
#27185=CARTESIAN_POINT('Ctrl Pts',(-3.83301397080609,0.888777645255686,
37.8003910657546));
#27186=CARTESIAN_POINT('Ctrl Pts',(-3.8575199673137,0.775500133178189,37.8062549294654));
#27187=CARTESIAN_POINT('Ctrl Pts',(-3.87696942368804,0.66151121516421,37.8121187931763));
#27188=CARTESIAN_POINT('Ctrl Pts',(-3.89644757268483,0.547354136101167,
37.8179913074954));
#27189=CARTESIAN_POINT('Ctrl Pts',(-3.91085424229472,0.432483965168393,
37.8238638218144));
#27190=CARTESIAN_POINT('Ctrl Pts',(-3.92017281141305,0.317386402761502,
37.8297363361335));
#27191=CARTESIAN_POINT('Ctrl Pts',(-3.92274826362268,0.285575910435982,
37.8313593728667));
#27192=CARTESIAN_POINT('Ctrl Pts',(-3.92493536749216,0.253748039176991,
37.8329824095998));
#27193=CARTESIAN_POINT('Ctrl Pts',(-3.92673447276226,0.221913001918477,
37.8346054463329));
#27194=CARTESIAN_POINT('Ctrl Pts',(-3.93324361014652,0.106734288036302,
37.8404775702442));
#27195=CARTESIAN_POINT('Ctrl Pts',(-3.93469174171344,-0.00892415268081789,
37.8463496941556));
#27196=CARTESIAN_POINT('Ctrl Pts',(-3.93102642928762,-0.124580143852121,
37.8522218180669));
#27197=CARTESIAN_POINT('Ctrl Pts',(-3.92736586901214,-0.240086184734537,
37.858086328653));
#27198=CARTESIAN_POINT('Ctrl Pts',(-3.91860506174942,-0.355589373000882,
37.8639508392392));
#27199=CARTESIAN_POINT('Ctrl Pts',(-3.90474342198803,-0.470603663862904,
37.8698153498253));
#27200=CARTESIAN_POINT('Ctrl Pts',(-3.89089604571586,-0.585499606165482,
37.8756738258884));
#27201=CARTESIAN_POINT('Ctrl Pts',(-3.87195832603939,-0.699907243723816,
37.8815323019515));
#27202=CARTESIAN_POINT('Ctrl Pts',(-3.84798168362691,-0.813342463216951,
37.8873907780147));
#27203=CARTESIAN_POINT('Ctrl Pts',(-3.82305961012834,-0.93125058516743,
37.8934802616264));
#27204=CARTESIAN_POINT('Ctrl Pts',(-3.792693070022,-1.04810756904737,37.8995697452381));
#27205=CARTESIAN_POINT('Ctrl Pts',(-3.75699906654958,-1.16337741681088,
37.9056592288499));
#27206=CARTESIAN_POINT('Ctrl Pts',(-3.72269894210745,-1.27414588596759,
37.9115109133165));
#27207=CARTESIAN_POINT('Ctrl Pts',(-3.68347976335989,-1.38344841858774,
37.9173625977831));
#27208=CARTESIAN_POINT('Ctrl Pts',(-3.63949683794381,-1.49082251344585,
37.9232142822497));
#27209=CARTESIAN_POINT('Ctrl Pts',(-3.59552062087744,-1.59818023142654,
37.9290650742076));
#27210=CARTESIAN_POINT('Ctrl Pts',(-3.54678225846339,-1.70360971400905,
37.9349158661654));
#27211=CARTESIAN_POINT('Ctrl Pts',(-3.49348557849583,-1.80666751585389,
37.9407666581233));
#27212=CARTESIAN_POINT('Ctrl Pts',(-3.44018411842481,-1.90973456080647,
37.9466179748304));
#27213=CARTESIAN_POINT('Ctrl Pts',(-3.38232371800281,-2.01042913493269,
37.9524692915375));
#27214=CARTESIAN_POINT('Ctrl Pts',(-3.32015428965931,-2.10833215904347,
37.9583206082445));
#27215=CARTESIAN_POINT('Ctrl Pts',(-3.25796422735877,-2.20626767704789,
37.9641738669965));
#27216=CARTESIAN_POINT('Ctrl Pts',(-3.19146251485241,-2.3014094539185,37.9700271257484));
#27217=CARTESIAN_POINT('Ctrl Pts',(-3.12094211930887,-2.39336777113837,
37.9758803845003));
#27218=CARTESIAN_POINT('Ctrl Pts',(-3.05034149304818,-2.48543070889649,
37.9817403024767));
#27219=CARTESIAN_POINT('Ctrl Pts',(-2.97571330981273,-2.57430262972343,
37.9876002204532));
#27220=CARTESIAN_POINT('Ctrl Pts',(-2.89739058054179,-2.65962719639195,
37.9934601384296));
#27221=CARTESIAN_POINT('Ctrl Pts',(-2.81901511432891,-2.74500921454052,
37.999324002057));
#27222=CARTESIAN_POINT('Ctrl Pts',(-2.73694044074398,-2.82683883131214,
38.0051878656845));
#27223=CARTESIAN_POINT('Ctrl Pts',(-2.65153487054218,-2.90479807048595,
38.0110517293119));
#27224=CARTESIAN_POINT('Ctrl Pts',(-2.56600330657343,-2.98287231829664,
38.0169242435492));
#27225=CARTESIAN_POINT('Ctrl Pts',(-2.47713135497954,-3.05706452898509,
38.0227967577865));
#27226=CARTESIAN_POINT('Ctrl Pts',(-2.38531872319976,-3.12709826976266,
38.0286692720237));
#27227=CARTESIAN_POINT('Ctrl Pts',(-2.35994367196755,-3.1464541004993,38.0302923095813));
#27228=CARTESIAN_POINT('Ctrl Pts',(-2.33434415400022,-3.16549254905002,
38.0319153471388));
#27229=CARTESIAN_POINT('Ctrl Pts',(-2.30852895188268,-3.18420839115775,
38.0335383846963));
#27230=CARTESIAN_POINT('Ctrl Pts',(-2.21512996297538,-3.2519220089498,38.0394105086541));
#27231=CARTESIAN_POINT('Ctrl Pts',(-2.11859260879058,-3.31563630408255,
38.045282632612));
#27232=CARTESIAN_POINT('Ctrl Pts',(-2.01929427785179,-3.37504660996482,
38.0511547565698));
#27233=CARTESIAN_POINT('Ctrl Pts',(-1.9201246891795,-3.43437988920061,38.0570192672018));
#27234=CARTESIAN_POINT('Ctrl Pts',(-1.81820159388598,-3.48942006590099,
38.0628837778338));
#27235=CARTESIAN_POINT('Ctrl Pts',(-1.713933654004,-3.53990401418916,38.0687482884658));
#27236=CARTESIAN_POINT('Ctrl Pts',(-1.60977300480372,-3.59033601499247,
38.0746067645742));
#27237=CARTESIAN_POINT('Ctrl Pts',(-1.50327268008492,-3.63622093358974,
38.0804652406826));
#27238=CARTESIAN_POINT('Ctrl Pts',(-1.39486781808445,-3.67734044794228,
38.086323716791));
#27239=CARTESIAN_POINT('Ctrl Pts',(-1.28218840854103,-3.72008135930414,
38.0924132003855));
#27240=CARTESIAN_POINT('Ctrl Pts',(-1.16745156534972,-3.75767308877766,
38.0985026839801));
#27241=CARTESIAN_POINT('Ctrl Pts',(-1.05117152210389,-3.78992446245539,
38.1045921675746));
#27242=CARTESIAN_POINT('Ctrl Pts',(-0.939432305251541,-3.82091639483319,
38.1104438520846));
#27243=CARTESIAN_POINT('Ctrl Pts',(-0.826268588830766,-3.84697711368964,
38.1162955365947));
#27244=CARTESIAN_POINT('Ctrl Pts',(-0.712153460845849,-3.86798738987154,
38.1221472211047));
#27245=CARTESIAN_POINT('Ctrl Pts',(-0.598055737906514,-3.88899446152815,
38.1279980131053));
#27246=CARTESIAN_POINT('Ctrl Pts',(-0.483007298395968,-3.90495254727666,
38.1338488051058));
#27247=CARTESIAN_POINT('Ctrl Pts',(-0.367491413656636,-3.91579354165776,
38.1396995971063));
#27248=CARTESIAN_POINT('Ctrl Pts',(-0.251965168477452,-3.92663550835077,
38.1455509138553));
#27249=CARTESIAN_POINT('Ctrl Pts',(-0.135971806356071,-3.93235943270726,
38.1514022306043));
#27250=CARTESIAN_POINT('Ctrl Pts',(-0.0199989976658834,-3.93294915300114,
38.1572535473532));
#27251=CARTESIAN_POINT('Ctrl Pts',(0.0960123022405029,-3.93353906902237,
38.1631068061462));
#27252=CARTESIAN_POINT('Ctrl Pts',(0.212002621962486,-3.9289913905169,38.1689600649392));
#27253=CARTESIAN_POINT('Ctrl Pts',(0.327485731892573,-3.91934204878916,
38.1748133237322));
#27254=CARTESIAN_POINT('Ctrl Pts',(0.443100226376169,-3.90968172905385,
38.1806732417482));
#27255=CARTESIAN_POINT('Ctrl Pts',(0.558205947068432,-3.89490819563718,
38.1865331597643));
#27256=CARTESIAN_POINT('Ctrl Pts',(0.672323115213581,-3.87510911185085,
38.1923930777804));
#27257=CARTESIAN_POINT('Ctrl Pts',(0.786517121708234,-3.85529669677577,
38.1982569414466));
#27258=CARTESIAN_POINT('Ctrl Pts',(0.899720847457973,-3.83045208183573,
38.2041208051129));
#27259=CARTESIAN_POINT('Ctrl Pts',(1.0114677180855,-3.80071336136664,38.2099846687792));
#27260=CARTESIAN_POINT('Ctrl Pts',(1.12337944220788,-3.77093076913654,38.2158571830539));
#27261=CARTESIAN_POINT('Ctrl Pts',(1.23382962884221,-3.73623978505086,38.2217296973286));
#27262=CARTESIAN_POINT('Ctrl Pts',(1.34236969486437,-3.69682736982804,38.2276022116033));
#27263=CARTESIAN_POINT('Ctrl Pts',(1.37236784410884,-3.68593462250193,38.2292252487554));
#27264=CARTESIAN_POINT('Ctrl Pts',(1.40222022487575,-3.67468150291303,38.2308482859076));
#27265=CARTESIAN_POINT('Ctrl Pts',(1.43191769561372,-3.66307257817645,38.2324713230597));
#27266=CARTESIAN_POINT('Ctrl Pts',(1.53936270135205,-3.62107166180405,38.2383434472439));
#27267=CARTESIAN_POINT('Ctrl Pts',(1.64513831810261,-3.57426896837866,38.244215571428));
#27268=CARTESIAN_POINT('Ctrl Pts',(1.74878426559977,-3.52281742251719,38.2500876956121));
#27269=CARTESIAN_POINT('Ctrl Pts',(1.85229583408655,-3.47143258459735,38.2559522064717));
#27270=CARTESIAN_POINT('Ctrl Pts',(1.95368285738747,-3.41541106253365,38.2618167173313));
#27271=CARTESIAN_POINT('Ctrl Pts',(2.05250311076411,-3.35495454221121,38.2676812281908));
#27272=CARTESIAN_POINT('Ctrl Pts',(2.15122167909573,-3.29456023103903,38.2735397045278));
#27273=CARTESIAN_POINT('Ctrl Pts',(2.24737838040768,-3.22974021321016,38.2793981808648));
#27274=CARTESIAN_POINT('Ctrl Pts',(2.34055438342991,-3.16074266244613,38.2852566572018));
#27275=CARTESIAN_POINT('Ctrl Pts',(2.43740443474394,-3.08902445051076,38.291346140711));
#27276=CARTESIAN_POINT('Ctrl Pts',(2.53103347873433,-3.01279267932383,38.2974356242203));
#27277=CARTESIAN_POINT('Ctrl Pts',(2.62100278877615,-2.93237674612722,38.3035251077295));
#27278=CARTESIAN_POINT('Ctrl Pts',(2.70745873168408,-2.85510111373542,38.3093767924692));
#27279=CARTESIAN_POINT('Ctrl Pts',(2.79053507015703,-2.77396227756016,38.3152284772089));
#27280=CARTESIAN_POINT('Ctrl Pts',(2.86987584775278,-2.68929388845571,38.3210801619486));
#27281=CARTESIAN_POINT('Ctrl Pts',(2.94920452415025,-2.60463841312645,38.3269309541787));
#27282=CARTESIAN_POINT('Ctrl Pts',(3.02479848991697,-2.51645475682456,38.3327817464089));
#27283=CARTESIAN_POINT('Ctrl Pts',(3.09633930368138,-2.42511276366232,38.3386325386391));
#27284=CARTESIAN_POINT('Ctrl Pts',(3.16788653382689,-2.33376257818289,38.3444838556175));
#27285=CARTESIAN_POINT('Ctrl Pts',(3.23537963439635,-2.23925381822338,38.3503351725959));
#27286=CARTESIAN_POINT('Ctrl Pts',(3.2985414946412,-2.14198809710283,38.3561864895743));
#27287=CARTESIAN_POINT('Ctrl Pts',(3.361724318215,-2.04469009363182,38.3620397485962));
#27288=CARTESIAN_POINT('Ctrl Pts',(3.42057281799139,-1.94463365605857,38.3678930076182));
#27289=CARTESIAN_POINT('Ctrl Pts',(3.4748544949905,-1.84224733373245,38.3737462666401));
#27290=CARTESIAN_POINT('Ctrl Pts',(3.52919792796067,-1.73974452703981,38.3796061848832));
#27291=CARTESIAN_POINT('Ctrl Pts',(3.57896397401331,-1.63490691034585,38.3854661031264));
#27292=CARTESIAN_POINT('Ctrl Pts',(3.62396714934554,-1.52818555825672,38.3913260213695));
#27293=CARTESIAN_POINT('Ctrl Pts',(3.66900062659402,-1.42139234764983,38.397189885262));
#27294=CARTESIAN_POINT('Ctrl Pts',(3.70926470413201,-1.3127132627864,38.4030537491546));
#27295=CARTESIAN_POINT('Ctrl Pts',(3.74462346788478,-1.20261551784705,38.4089176130471));
#27296=CARTESIAN_POINT('Ctrl Pts',(3.78003439429353,-1.09235535233121,38.4147901275451));
#27297=CARTESIAN_POINT('Ctrl Pts',(3.81052545570312,-0.980672747095065,
38.4206626420431));
#27298=CARTESIAN_POINT('Ctrl Pts',(3.83601157778903,-0.868046182566633,
38.4265351565411));
#27299=CARTESIAN_POINT('Ctrl Pts',(3.84305538622439,-0.8369186558838,38.4281581915018));
#27300=CARTESIAN_POINT('Ctrl Pts',(3.84971719773295,-0.805719058755463,
38.4297812264625));
#27301=CARTESIAN_POINT('Ctrl Pts',(3.85599591566377,-0.774457551053836,
38.4314042614232));
#27302=CARTESIAN_POINT('Ctrl Pts',(3.88876514262491,-0.611300764539638,
38.4398750354855));
#27303=CARTESIAN_POINT('Ctrl Pts',(3.91118760611058,-0.446001857174323,
38.4483458095477));
#27304=CARTESIAN_POINT('Ctrl Pts',(3.92304612497759,-0.279639234189963,
38.45681658361));
#27305=CARTESIAN_POINT('Ctrl Pts',(3.92958843073383,-0.187857523659283,
38.4614898817283));
#27306=CARTESIAN_POINT('Ctrl Pts',(3.93291613600371,-0.095752414987991,
38.4661631798467));
#27307=CARTESIAN_POINT('Ctrl Pts',(3.93299843466147,-0.00350898139352327,
38.470836477965));
#27308=CARTESIAN_POINT('',(3.93045782683572,-0.000399788568204086,39.7208363664874));
#27309=CARTESIAN_POINT('Ctrl Pts',(3.93439718561015,-0.00349648589506154,
38.4708371739967));
#27310=CARTESIAN_POINT('Ctrl Pts',(3.92467201342099,1.04631151308355,38.52400384926));
#27311=CARTESIAN_POINT('Ctrl Pts',(2.95138670712728,3.42137387922279,38.6434815039779));
#27312=CARTESIAN_POINT('Ctrl Pts',(-1.06465162905695,4.5288909683736,38.82927013815));
#27313=CARTESIAN_POINT('Ctrl Pts',(-4.38608045124232,1.55133378955204,39.0282030765135));
#27314=CARTESIAN_POINT('Ctrl Pts',(-3.67536551296059,-2.85237220456728,
39.2271360148771));
#27315=CARTESIAN_POINT('Ctrl Pts',(0.414129357579048,-4.63387829221155,
39.4260689532403));
#27316=CARTESIAN_POINT('Ctrl Pts',(3.48221100255245,-2.58359817983051,39.5906356795963));
#27317=CARTESIAN_POINT('Ctrl Pts',(3.92709165371068,-0.634376258868161,
39.6888914264977));
#27318=CARTESIAN_POINT('Ctrl Pts',(3.9265231354041,-0.000402814833626348,
39.7208361939446));
#27319=CARTESIAN_POINT('',(3.93299828088553,0.00367730219960298,40.9708364779999));
#27320=CARTESIAN_POINT('Ctrl Pts',(3.93299997987905,-0.000397833337409791,
39.720836477965));
#27321=CARTESIAN_POINT('Ctrl Pts',(3.93301221516407,0.120560797364908,39.7269213266806));
#27322=CARTESIAN_POINT('Ctrl Pts',(3.92744003772526,0.241429729961996,39.7330061753961));
#27323=CARTESIAN_POINT('Ctrl Pts',(3.91633416341394,0.361684559356363,39.7390910241117));
#27324=CARTESIAN_POINT('Ctrl Pts',(3.90521572833616,0.482075397207768,39.7451827548036));
#27325=CARTESIAN_POINT('Ctrl Pts',(3.88855115022812,0.601850385441626,39.7512744854954));
#27326=CARTESIAN_POINT('Ctrl Pts',(3.86644259922617,0.720493321890755,39.7573662161873));
#27327=CARTESIAN_POINT('Ctrl Pts',(3.84428593703237,0.83939444138757,39.7634712033076));
#27328=CARTESIAN_POINT('Ctrl Pts',(3.81666169142604,0.957158227337841,39.7695761904279));
#27329=CARTESIAN_POINT('Ctrl Pts',(3.78372278395199,1.07328043595445,39.7756811775482));
#27330=CARTESIAN_POINT('Ctrl Pts',(3.75074559613254,1.18953759738512,39.7817932596523));
#27331=CARTESIAN_POINT('Ctrl Pts',(3.7124415414633,1.30414903190815,39.7879053417564));
#27332=CARTESIAN_POINT('Ctrl Pts',(3.6690122216127,1.41662920965814,39.7940174238605));
#27333=CARTESIAN_POINT('Ctrl Pts',(3.62548637651813,1.52935938387681,39.800143090571));
#27334=CARTESIAN_POINT('Ctrl Pts',(3.57681264168092,1.6399484994239,39.8062687572815));
#27335=CARTESIAN_POINT('Ctrl Pts',(3.52323976422024,1.74793322636116,39.8123944239921));
#27336=CARTESIAN_POINT('Ctrl Pts',(3.48959701781275,1.81574557761853,39.8162412259838));
#27337=CARTESIAN_POINT('Ctrl Pts',(3.45402314951959,1.88253138719219,39.8200880279755));
#27338=CARTESIAN_POINT('Ctrl Pts',(3.4165884287368,1.94818184690798,39.8239348299672));
#27339=CARTESIAN_POINT('Ctrl Pts',(3.35944435755049,2.04839722089677,39.8298069701157));
#27340=CARTESIAN_POINT('Ctrl Pts',(3.29779147146901,2.14626424612989,39.8356791102642));
#27341=CARTESIAN_POINT('Ctrl Pts',(3.23184785271714,2.24134969535939,39.8415512504126));
#27342=CARTESIAN_POINT('Ctrl Pts',(3.16598973252548,2.3363118624706,39.8474157770946));
#27343=CARTESIAN_POINT('Ctrl Pts',(3.09585217608569,2.42849928888059,39.8532803037766));
#27344=CARTESIAN_POINT('Ctrl Pts',(3.02169889165576,2.51750368582974,39.8591448304587));
#27345=CARTESIAN_POINT('Ctrl Pts',(2.94762191199982,2.60641649600097,39.8650033224601));
#27346=CARTESIAN_POINT('Ctrl Pts',(2.86953768660722,2.69215247589465,39.8708618144616));
#27347=CARTESIAN_POINT('Ctrl Pts',(2.78775252601083,2.77433322687096,39.8767203064631));
#27348=CARTESIAN_POINT('Ctrl Pts',(2.70274278262887,2.85975415776465,39.8828097840409));
#27349=CARTESIAN_POINT('Ctrl Pts',(2.61373452287241,2.94133337134355,39.8888992616187));
#27350=CARTESIAN_POINT('Ctrl Pts',(2.52111730365917,3.01868457133075,39.8949887391965));
#27351=CARTESIAN_POINT('Ctrl Pts',(2.432116536821,3.09301541578056,39.9008404391145));
#27352=CARTESIAN_POINT('Ctrl Pts',(2.33978370955459,3.16344194615921,39.9066921390324));
#27353=CARTESIAN_POINT('Ctrl Pts',(2.2445005837303,3.22966037372885,39.9125438389503));
#27354=CARTESIAN_POINT('Ctrl Pts',(2.14923199393858,3.29586869926612,39.9183946461551));
#27355=CARTESIAN_POINT('Ctrl Pts',(2.05101433988827,3.35786996257495,39.9242454533599));
#27356=CARTESIAN_POINT('Ctrl Pts',(1.95025975148123,3.41540274371155,39.9300962605647));
#27357=CARTESIAN_POINT('Ctrl Pts',(1.84949613034208,3.47294068270952,39.9359475922991));
#27358=CARTESIAN_POINT('Ctrl Pts',(1.74619548174536,3.52600913816299,39.9417989240336));
#27359=CARTESIAN_POINT('Ctrl Pts',(1.6407953728763,3.57439219229615,39.9476502557681));
#27360=CARTESIAN_POINT('Ctrl Pts',(1.53536028615924,3.6227913027231,39.9535035293126));
#27361=CARTESIAN_POINT('Ctrl Pts',(1.42782472930042,3.66650174766016,39.9593568028571));
#27362=CARTESIAN_POINT('Ctrl Pts',(1.31864644875282,3.70535565677461,39.9652100764017));
#27363=CARTESIAN_POINT('Ctrl Pts',(1.20934396475316,3.74425376689327,39.9710700087503));
#27364=CARTESIAN_POINT('Ctrl Pts',(1.0983954167113,3.77828417495523,39.9769299410989));
#27365=CARTESIAN_POINT('Ctrl Pts',(0.986274017562826,3.80732879618775,39.9827898734475));
#27366=CARTESIAN_POINT('Ctrl Pts',(0.874077128378057,3.83639297282653,39.9886537512206));
#27367=CARTESIAN_POINT('Ctrl Pts',(0.760706219113384,3.86046459279032,39.9945176289936));
#27368=CARTESIAN_POINT('Ctrl Pts',(0.646643280547311,3.87947695800903,40.0003815067666));
#27369=CARTESIAN_POINT('Ctrl Pts',(0.532412080682976,3.89851736954405,40.0062540347086));
#27370=CARTESIAN_POINT('Ctrl Pts',(0.417487222934432,3.91248358144626,40.0121265626506));
#27371=CARTESIAN_POINT('Ctrl Pts',(0.302354469892053,3.92136083197355,40.0179990905925));
#27372=CARTESIAN_POINT('Ctrl Pts',(0.270537151625742,3.92381408960783,40.0196219831719));
#27373=CARTESIAN_POINT('Ctrl Pts',(0.238703945366235,3.92587900390329,40.0212448757513));
#27374=CARTESIAN_POINT('Ctrl Pts',(0.206865059890492,3.92755596357283,40.0228677683307));
#27375=CARTESIAN_POINT('Ctrl Pts',(0.0916611675682571,3.93362377274115,
40.0287399444189));
#27376=CARTESIAN_POINT('Ctrl Pts',(-0.0240030362714795,3.93462867850176,
40.0346121205071));
#27377=CARTESIAN_POINT('Ctrl Pts',(-0.139645169554283,3.93052009619849,
40.0404842965954));
#27378=CARTESIAN_POINT('Ctrl Pts',(-0.255137378609357,3.92641684046617,
40.0463488597017));
#27379=CARTESIAN_POINT('Ctrl Pts',(-0.370607164683488,3.91721329465202,
40.0522134228081));
#27380=CARTESIAN_POINT('Ctrl Pts',(-0.485568476785245,3.90291074127406,
40.0580779859144));
#27381=CARTESIAN_POINT('Ctrl Pts',(-0.600411501363643,3.88862290426969,
40.0639365147765));
#27382=CARTESIAN_POINT('Ctrl Pts',(-0.71474668483969,3.86924654605267,40.0697950436385));
#27383=CARTESIAN_POINT('Ctrl Pts',(-0.828090107617243,3.84483494751939,
40.0756535725005));
#27384=CARTESIAN_POINT('Ctrl Pts',(-0.945901370540731,3.81946107771107,
40.0817430364253));
#27385=CARTESIAN_POINT('Ctrl Pts',(-1.06264062231353,3.78864685520957,40.08783250035));
#27386=CARTESIAN_POINT('Ctrl Pts',(-1.1777723297283,3.75251133766793,40.0939219642747));
#27387=CARTESIAN_POINT('Ctrl Pts',(-1.28840941579538,3.71778651290763,40.0997737019017));
#27388=CARTESIAN_POINT('Ctrl Pts',(-1.39756168502639,3.6781482099432,40.1056254395288));
#27389=CARTESIAN_POINT('Ctrl Pts',(-1.50476722862093,3.63375351223339,40.1114771771558));
#27390=CARTESIAN_POINT('Ctrl Pts',(-1.61195642198051,3.58936558529041,40.117328022317));
#27391=CARTESIAN_POINT('Ctrl Pts',(-1.71719909819135,3.54022286407388,40.1231788674782));
#27392=CARTESIAN_POINT('Ctrl Pts',(-1.82005259035601,3.48653087873009,40.1290297126394));
#27393=CARTESIAN_POINT('Ctrl Pts',(-1.92291530698139,3.43283407799695,40.1348810825362));
#27394=CARTESIAN_POINT('Ctrl Pts',(-2.02338804710449,3.37458739338451,40.140732452433));
#27395=CARTESIAN_POINT('Ctrl Pts',(-2.12105268651087,3.31204234590155,40.1465838223298));
#27396=CARTESIAN_POINT('Ctrl Pts',(-2.21874973922562,3.24947654073265,40.1524371342013));
#27397=CARTESIAN_POINT('Ctrl Pts',(-2.31363649012476,3.18260975890633,40.1582904460728));
#27398=CARTESIAN_POINT('Ctrl Pts',(-2.40532434044997,3.11173646333344,40.1641437579443));
#27399=CARTESIAN_POINT('Ctrl Pts',(-2.49711649680897,3.04078254080358,40.1700037286669));
#27400=CARTESIAN_POINT('Ctrl Pts',(-2.58570216169739,2.96581326006773,40.1758636993896));
#27401=CARTESIAN_POINT('Ctrl Pts',(-2.67072627081659,2.88716299961919,40.1817236701122));
#27402=CARTESIAN_POINT('Ctrl Pts',(-2.7558076263903,2.80845978420761,40.1875875863339));
#27403=CARTESIAN_POINT('Ctrl Pts',(-2.8373223612883,2.72607094727657,40.1934515025557));
#27404=CARTESIAN_POINT('Ctrl Pts',(-2.91495390705511,2.64036602003286,40.1993154187774));
#27405=CARTESIAN_POINT('Ctrl Pts',(-2.99269996862671,2.55453466778213,40.2051879849762));
#27406=CARTESIAN_POINT('Ctrl Pts',(-3.06655114597935,2.46537777960961,40.2110605511749));
#27407=CARTESIAN_POINT('Ctrl Pts',(-3.13623253395467,2.37329612416239,40.2169331173736));
#27408=CARTESIAN_POINT('Ctrl Pts',(-3.15548478634672,2.34785490775071,40.2185556471471));
#27409=CARTESIAN_POINT('Ctrl Pts',(-3.17441899725897,2.32219058273379,40.2201781769206));
#27410=CARTESIAN_POINT('Ctrl Pts',(-3.1930299809604,2.29631194324465,40.2218007066941));
#27411=CARTESIAN_POINT('Ctrl Pts',(-3.26038337409214,2.20265680887942,40.2276726631395));
#27412=CARTESIAN_POINT('Ctrl Pts',(-3.32372571208478,2.10587877460033,40.2335446195849));
#27413=CARTESIAN_POINT('Ctrl Pts',(-3.38275377933201,2.00635636625575,40.2394165760303));
#27414=CARTESIAN_POINT('Ctrl Pts',(-3.44170531139888,1.90696299763461,40.2452809189578));
#27415=CARTESIAN_POINT('Ctrl Pts',(-3.49635348786262,1.80483268346802,40.2511452618853));
#27416=CARTESIAN_POINT('Ctrl Pts',(-3.54643675227542,1.70037506512833,40.2570096048129));
#27417=CARTESIAN_POINT('Ctrl Pts',(-3.59646848004553,1.5960249356877,40.2628679132187));
#27418=CARTESIAN_POINT('Ctrl Pts',(-3.64194446140186,1.4893526360771,40.2687262216245));
#27419=CARTESIAN_POINT('Ctrl Pts',(-3.6826480441159,1.38079411324402,40.2745845300303));
#27420=CARTESIAN_POINT('Ctrl Pts',(-3.72495827103363,1.26795058870246,40.2806740764898));
#27421=CARTESIAN_POINT('Ctrl Pts',(-3.76211135809236,1.15306926060779,40.2867636229493));
#27422=CARTESIAN_POINT('Ctrl Pts',(-3.79391808266823,1.03666512529506,40.2928531694087));
#27423=CARTESIAN_POINT('Ctrl Pts',(-3.82448154379396,0.924811002874548,
40.298704687255));
#27424=CARTESIAN_POINT('Ctrl Pts',(-3.8501086301726,0.811551320650944,40.3045562051013));
#27425=CARTESIAN_POINT('Ctrl Pts',(-3.8706819284736,0.697359597759905,40.3104077229476));
#27426=CARTESIAN_POINT('Ctrl Pts',(-3.89125209113257,0.583185279193724,
40.3162583489453));
#27427=CARTESIAN_POINT('Ctrl Pts',(-3.9067699239503,0.46807960918544,40.3221089749431));
#27428=CARTESIAN_POINT('Ctrl Pts',(-3.91716917591749,0.352526094412765,
40.3279596009409));
#27429=CARTESIAN_POINT('Ctrl Pts',(-3.9275693620848,0.236962199075433,40.3338107525203));
#27430=CARTESIAN_POINT('Ctrl Pts',(-3.93285001626266,0.120950790796229,
40.3396619040996));
#27431=CARTESIAN_POINT('Ctrl Pts',(-3.93299684767512,0.00497957604032452,
40.345513055679));
#27432=CARTESIAN_POINT('Ctrl Pts',(-3.93314372784736,-0.111030150432251,
40.3513661503086));
#27433=CARTESIAN_POINT('Ctrl Pts',(-3.92815339477199,-0.226999243621648,
40.3572192449382));
#27434=CARTESIAN_POINT('Ctrl Pts',(-3.91806364478637,-0.34244163795214,
40.3630723395677));
#27435=CARTESIAN_POINT('Ctrl Pts',(-3.90796241143149,-0.458015419843687,
40.3689320957347));
#27436=CARTESIAN_POINT('Ctrl Pts',(-3.89275021303907,-0.57306089428121,
40.3747918519017));
#27437=CARTESIAN_POINT('Ctrl Pts',(-3.87251655278508,-0.687098645323602,
40.3806516080687));
#27438=CARTESIAN_POINT('Ctrl Pts',(-3.85226926429982,-0.801213205644506,
40.3865153110308));
#27439=CARTESIAN_POINT('Ctrl Pts',(-3.82699386935437,-0.914318288559313,
40.3923790139929));
#27440=CARTESIAN_POINT('Ctrl Pts',(-3.79683025086908,-1.0259478768853,40.3982427169551));
#27441=CARTESIAN_POINT('Ctrl Pts',(-3.76662211752302,-1.13774220590991,
40.404115073452));
#27442=CARTESIAN_POINT('Ctrl Pts',(-3.73151148787811,-1.24805630196375,
40.4099874299489));
#27443=CARTESIAN_POINT('Ctrl Pts',(-3.69168704150918,-1.35644232739664,
40.4158597864458));
#27444=CARTESIAN_POINT('Ctrl Pts',(-3.680669390645,-1.38642791403136,40.417484405983));
#27445=CARTESIAN_POINT('Ctrl Pts',(-3.66929122729997,-1.41626606714415,
40.4191090255203));
#27446=CARTESIAN_POINT('Ctrl Pts',(-3.65755716757587,-1.44594763595172,
40.4207336450576));
#27447=CARTESIAN_POINT('Ctrl Pts',(-3.6151437429181,-1.55323335052489,40.4266059245553));
#27448=CARTESIAN_POINT('Ctrl Pts',(-3.56793476664441,-1.65883117085618,
40.432478204053));
#27449=CARTESIAN_POINT('Ctrl Pts',(-3.51608493954222,-1.76228139010897,
40.4383504835507));
#27450=CARTESIAN_POINT('Ctrl Pts',(-3.46430234261555,-1.8655974724362,40.4442151488594));
#27451=CARTESIAN_POINT('Ctrl Pts',(-3.40789104497284,-1.96677112519497,
40.4500798141681));
#27452=CARTESIAN_POINT('Ctrl Pts',(-3.34705443881563,-2.06536088459248,
40.4559444794768));
#27453=CARTESIAN_POINT('Ctrl Pts',(-3.28628044193404,-2.16384918150202,
40.4618031092344));
#27454=CARTESIAN_POINT('Ctrl Pts',(-3.22109041095424,-2.25975852461353,
40.467661738992));
#27455=CARTESIAN_POINT('Ctrl Pts',(-3.15173413566648,-2.35267102206719,
40.4735203687496));
#27456=CARTESIAN_POINT('Ctrl Pts',(-3.07964562751407,-2.4492437301943,40.4796097943609));
#27457=CARTESIAN_POINT('Ctrl Pts',(-3.0030560804933,-2.54257821622054,40.4856992199722));
#27458=CARTESIAN_POINT('Ctrl Pts',(-2.92229654886902,-2.63223704868468,
40.4917886455835));
#27459=CARTESIAN_POINT('Ctrl Pts',(-2.84468800944538,-2.71839766519671,
40.4976404802601));
#27460=CARTESIAN_POINT('Ctrl Pts',(-2.76322908759393,-2.80116374017019,
40.5034923149366));
#27461=CARTESIAN_POINT('Ctrl Pts',(-2.6782548069731,-2.88018058269364,40.5093441496132));
#27462=CARTESIAN_POINT('Ctrl Pts',(-2.59329350864828,-2.95918535309325,
40.5151950902516));
#27463=CARTESIAN_POINT('Ctrl Pts',(-2.50481822207306,-3.03444174853172,
40.52104603089));
#27464=CARTESIAN_POINT('Ctrl Pts',(-2.4132000205352,-3.10563273116589,40.5268969715284));
#27465=CARTESIAN_POINT('Ctrl Pts',(-2.32157362839142,-3.17683007822628,
40.532748435237));
#27466=CARTESIAN_POINT('Ctrl Pts',(-2.22680408918084,-3.24396103632612,
40.5385998989456));
#27467=CARTESIAN_POINT('Ctrl Pts',(-2.12929408747564,-3.30675001913378,
40.5444513626542));
#27468=CARTESIAN_POINT('Ctrl Pts',(-2.03175175363044,-3.3695598213666,40.5503047665775));
#27469=CARTESIAN_POINT('Ctrl Pts',(-1.93146749782905,-3.42802456186416,
40.5561581705008));
#27470=CARTESIAN_POINT('Ctrl Pts',(-1.82887077054162,-3.48191336834484,
40.5620115744242));
#27471=CARTESIAN_POINT('Ctrl Pts',(-1.72615738244759,-3.53586345077259,
40.5678716341429));
#27472=CARTESIAN_POINT('Ctrl Pts',(-1.62112664071319,-3.58522702136902,
40.5737316938616));
#27473=CARTESIAN_POINT('Ctrl Pts',(-1.51423034177429,-3.62982030850704,
40.5795917535803));
#27474=CARTESIAN_POINT('Ctrl Pts',(-1.40726210138794,-3.67444360702669,
40.5854557571323));
#27475=CARTESIAN_POINT('Ctrl Pts',(-1.29842619104318,-3.71429008774057,
40.5913197606842));
#27476=CARTESIAN_POINT('Ctrl Pts',(-1.18819035846714,-3.74922560964871,
40.5971837642362));
#27477=CARTESIAN_POINT('Ctrl Pts',(-1.07779197578118,-3.78421264632109,
40.6030564146537));
#27478=CARTESIAN_POINT('Ctrl Pts',(-0.96598994866209,-3.81427416447574,
40.6089290650712));
#27479=CARTESIAN_POINT('Ctrl Pts',(-0.853263097909405,-3.83932690529812,
40.6148017154887));
#27480=CARTESIAN_POINT('Ctrl Pts',(-0.822135685109074,-3.84624475140267,
40.6164233381328));
#27481=CARTESIAN_POINT('Ctrl Pts',(-0.790937788482818,-3.85278099027465,
40.6180449607769));
#27482=CARTESIAN_POINT('Ctrl Pts',(-0.759679545227435,-3.85893456650447,
40.619666583421));
#27483=CARTESIAN_POINT('Ctrl Pts',(-0.646483380285604,-3.88121864767312,
40.6255390012275));
#27484=CARTESIAN_POINT('Ctrl Pts',(-0.532116263583732,-3.8985551698722,
40.6314114190341));
#27485=CARTESIAN_POINT('Ctrl Pts',(-0.417048635583041,-3.91082592754501,
40.6372838368406));
#27486=CARTESIAN_POINT('Ctrl Pts',(-0.30213013859324,-3.92308078195704,
40.6431486438219));
#27487=CARTESIAN_POINT('Ctrl Pts',(-0.186513342999179,-3.93028288460637,
40.6490134508033));
#27488=CARTESIAN_POINT('Ctrl Pts',(-0.0706796452800259,-3.93236485943803,
40.6548782577846));
#27489=CARTESIAN_POINT('Ctrl Pts',(0.0450349087417255,-3.9344446928015,
40.6607370323695));
#27490=CARTESIAN_POINT('Ctrl Pts',(0.160965510318117,-3.93141486618567,
40.6665958069543));
#27491=CARTESIAN_POINT('Ctrl Pts',(0.276625530107023,-3.92325978187693,
40.6724545815392));
#27492=CARTESIAN_POINT('Ctrl Pts',(0.396837860319034,-3.9147837182413,40.6785439540494));
#27493=CARTESIAN_POINT('Ctrl Pts',(0.516757419054958,-3.90077060884241,
40.6846333265596));
#27494=CARTESIAN_POINT('Ctrl Pts',(0.635837280804501,-3.88126267499884,
40.6907226990699));
#27495=CARTESIAN_POINT('Ctrl Pts',(0.750274971915399,-3.86251523210964,
40.6965746854607));
#27496=CARTESIAN_POINT('Ctrl Pts',(0.86393676234027,-3.83869342962096,40.7024266718516));
#27497=CARTESIAN_POINT('Ctrl Pts',(0.976343152373888,-3.80988753755444,
40.7082786582424));
#27498=CARTESIAN_POINT('Ctrl Pts',(1.08873241304881,-3.78108603515346,40.7141297528622));
#27499=CARTESIAN_POINT('Ctrl Pts',(1.19986625339821,-3.74730205591859,40.7199808474819));
#27500=CARTESIAN_POINT('Ctrl Pts',(1.30927737957966,-3.70867654875981,40.7258319421016));
#27501=CARTESIAN_POINT('Ctrl Pts',(1.41869832591295,-3.6700475747841,40.731683561884));
#27502=CARTESIAN_POINT('Ctrl Pts',(1.52639586089314,-3.62657634665328,40.7375351816664));
#27503=CARTESIAN_POINT('Ctrl Pts',(1.63192049055313,-3.57845280987647,40.7433868014488));
#27504=CARTESIAN_POINT('Ctrl Pts',(1.73748014350494,-3.53031330104956,40.7492403633653));
#27505=CARTESIAN_POINT('Ctrl Pts',(1.84086508121008,-3.47751858467989,40.7550939252818));
#27506=CARTESIAN_POINT('Ctrl Pts',(1.94164897260077,-3.42030528859609,40.7609474871984));
#27507=CARTESIAN_POINT('Ctrl Pts',(2.04254749510528,-3.36302691838422,40.7668077069281));
#27508=CARTESIAN_POINT('Ctrl Pts',(2.14083870667397,-3.30132014153676,40.7726679266578));
#27509=CARTESIAN_POINT('Ctrl Pts',(2.2361238351808,-3.23546583875279,40.7785281463875));
#27510=CARTESIAN_POINT('Ctrl Pts',(2.33147311131144,-3.16956720169435,40.7843923113202));
#27511=CARTESIAN_POINT('Ctrl Pts',(2.4238119461695,-3.09951572811584,40.7902564762529));
#27512=CARTESIAN_POINT('Ctrl Pts',(2.5127747104818,-3.02563253789404,40.7961206411856));
#27513=CARTESIAN_POINT('Ctrl Pts',(2.60186866387217,-2.95164039571144,40.8019934537182));
#27514=CARTESIAN_POINT('Ctrl Pts',(2.68757630562578,-2.87380553649343,40.8078662662508));
#27515=CARTESIAN_POINT('Ctrl Pts',(2.76956883811472,-2.79248589091223,40.8137390787833));
#27516=CARTESIAN_POINT('Ctrl Pts',(2.7921883257094,-2.77005203433296,40.8153592264504));
#27517=CARTESIAN_POINT('Ctrl Pts',(2.81452531070709,-2.74735315744052,40.8169793741174));
#27518=CARTESIAN_POINT('Ctrl Pts',(2.83657344498074,-2.7243971977724,40.8185995217844));
#27519=CARTESIAN_POINT('Ctrl Pts',(2.91546205128647,-2.64226037648168,40.8243964381981));
#27520=CARTESIAN_POINT('Ctrl Pts',(2.99092924005757,-2.55653868550325,40.8301933546118));
#27521=CARTESIAN_POINT('Ctrl Pts',(3.06262502772754,-2.46755282406211,40.8359902710255));
#27522=CARTESIAN_POINT('Ctrl Pts',(3.13420561239945,-2.37870994784167,40.8417778727755));
#27523=CARTESIAN_POINT('Ctrl Pts',(3.20202658929276,-2.28661366453194,40.8475654745255));
#27524=CARTESIAN_POINT('Ctrl Pts',(3.26577467118157,-2.1916214994996,40.8533530762755));
#27525=CARTESIAN_POINT('Ctrl Pts',(3.32946416229371,-2.09671664163891,40.8591353586485));
#27526=CARTESIAN_POINT('Ctrl Pts',(3.38908796031717,-1.99892154033182,40.8649176410214));
#27527=CARTESIAN_POINT('Ctrl Pts',(3.44437310944292,-1.89862657806808,40.8706999233944));
#27528=CARTESIAN_POINT('Ctrl Pts',(3.49962165888698,-1.7983980127256,40.876478377801));
#27529=CARTESIAN_POINT('Ctrl Pts',(3.55053706312625,-1.6956732461639,40.8822568322075));
#27530=CARTESIAN_POINT('Ctrl Pts',(3.59689024853921,-1.59087068612239,40.8880352866141));
#27531=CARTESIAN_POINT('Ctrl Pts',(3.64322465994652,-1.48611057330079,40.8938114006262));
#27532=CARTESIAN_POINT('Ctrl Pts',(3.68500035492406,-1.37927472836459,40.8995875146384));
#27533=CARTESIAN_POINT('Ctrl Pts',(3.72203509766008,-1.27080436408855,40.9053636286506));
#27534=CARTESIAN_POINT('Ctrl Pts',(3.75907629846722,-1.16231508488898,40.9111407498941));
#27535=CARTESIAN_POINT('Ctrl Pts',(3.79137474787259,-1.05219111583276,40.9169178711376));
#27536=CARTESIAN_POINT('Ctrl Pts',(3.81879724499092,-0.940891386744367,
40.9226949923812));
#27537=CARTESIAN_POINT('Ctrl Pts',(3.84622140628905,-0.829584903246992,
40.9284724642189));
#27538=CARTESIAN_POINT('Ctrl Pts',(3.86876893300363,-0.717102932663289,
40.9342499360566));
#27539=CARTESIAN_POINT('Ctrl Pts',(3.8863575033137,-0.603915852116282,40.9400274078944));
#27540=CARTESIAN_POINT('Ctrl Pts',(3.90396114259419,-0.490631798777366,
40.9458098295689));
#27541=CARTESIAN_POINT('Ctrl Pts',(3.91659728308609,-0.376641850685132,
40.9515922512434));
#27542=CARTESIAN_POINT('Ctrl Pts',(3.92423538306663,-0.2624226710631,40.9573746729179));
#27543=CARTESIAN_POINT('Ctrl Pts',(3.93016269280269,-0.173786432058322,
40.961861941267));
#27544=CARTESIAN_POINT('Ctrl Pts',(3.93308120450337,-0.0850123104087433,
40.966349209616));
#27545=CARTESIAN_POINT('Ctrl Pts',(3.93299828088617,0.00367730151040331,
40.970836477965));
#27546=CARTESIAN_POINT('',(1.74869731696171,-3.52286058390776,41.9999376421029));
#27547=CARTESIAN_POINT('Ctrl Pts',(3.93299828088553,0.00367730219960045,
40.9708364779999));
#27548=CARTESIAN_POINT('Ctrl Pts',(3.93285383869511,0.158163078935381,40.9786527162416));
#27549=CARTESIAN_POINT('Ctrl Pts',(3.92360365029584,0.31224237002749,40.9864689544833));
#27550=CARTESIAN_POINT('Ctrl Pts',(3.9054123314799,0.46501991476143,40.9942851927251));
#27551=CARTESIAN_POINT('Ctrl Pts',(3.8873772938139,0.61648495155591,41.002034281866));
#27552=CARTESIAN_POINT('Ctrl Pts',(3.86055430226053,0.766671074542145,41.009783371007));
#27553=CARTESIAN_POINT('Ctrl Pts',(3.82514809528352,0.914730041678332,41.0175324601479));
#27554=CARTESIAN_POINT('Ctrl Pts',(3.79831164379733,1.02695266104069,41.0234059516215));
#27555=CARTESIAN_POINT('Ctrl Pts',(3.76648749677485,1.13818108591094,41.0292794430952));
#27556=CARTESIAN_POINT('Ctrl Pts',(3.72976395877152,1.2479382243721,41.0351529345688));
#27557=CARTESIAN_POINT('Ctrl Pts',(3.69308805402098,1.35755299938448,41.0410188076723));
#27558=CARTESIAN_POINT('Ctrl Pts',(3.65152552588073,1.46569989484038,41.0468846807759));
#27559=CARTESIAN_POINT('Ctrl Pts',(3.60521545744127,1.57191300822485,41.0527505538794));
#27560=CARTESIAN_POINT('Ctrl Pts',(3.55895308211299,1.67801673645841,41.0586103859265));
#27561=CARTESIAN_POINT('Ctrl Pts',(3.50795305583398,1.78219026741922,41.0644702179736));
#27562=CARTESIAN_POINT('Ctrl Pts',(3.45240372207426,1.88398448502311,41.0703300500206));
#27563=CARTESIAN_POINT('Ctrl Pts',(3.39468220674908,1.98975922782837,41.0764190228744));
#27564=CARTESIAN_POINT('Ctrl Pts',(3.33204847832998,2.09296434917749,41.0825079957282));
#27565=CARTESIAN_POINT('Ctrl Pts',(3.26476834986139,2.19312029349585,41.0885969685819));
#27566=CARTESIAN_POINT('Ctrl Pts',(3.20009542808786,2.28939504355196,41.0944499845321));
#27567=CARTESIAN_POINT('Ctrl Pts',(3.13112976417696,2.38285216241336,41.1003030004822));
#27568=CARTESIAN_POINT('Ctrl Pts',(3.05815299369713,2.4730930567088,41.1061560164323));
#27569=CARTESIAN_POINT('Ctrl Pts',(2.98518749119529,2.56332001735927,41.1120081286476));
#27570=CARTESIAN_POINT('Ctrl Pts',(2.90821237333455,2.65033141965462,41.1178602408628));
#27571=CARTESIAN_POINT('Ctrl Pts',(2.82755028482658,2.73376085032636,41.123712353078));
#27572=CARTESIAN_POINT('Ctrl Pts',(2.74688113675843,2.81719758275656,41.1295649774711));
#27573=CARTESIAN_POINT('Ctrl Pts',(2.66252466381531,2.89705142328491,41.1354176018642));
#27574=CARTESIAN_POINT('Ctrl Pts',(2.57484066466697,2.97299252464202,41.1412702262573));
#27575=CARTESIAN_POINT('Ctrl Pts',(2.48712777846706,3.04895864441221,41.1471247787681));
#27576=CARTESIAN_POINT('Ctrl Pts',(2.39608549844132,3.12100919146258,41.1529793312788));
#27577=CARTESIAN_POINT('Ctrl Pts',(2.3021064437128,3.18885479785706,41.1588338837895));
#27578=CARTESIAN_POINT('Ctrl Pts',(2.20802092745584,3.25677726123819,41.1646950684654));
#27579=CARTESIAN_POINT('Ctrl Pts',(2.11099233141337,3.32048503420083,41.1705562531412));
#27580=CARTESIAN_POINT('Ctrl Pts',(2.01144205714743,3.37973221583286,41.176417437817));
#27581=CARTESIAN_POINT('Ctrl Pts',(1.91182500794981,3.43901913845541,41.1822825539758));
#27582=CARTESIAN_POINT('Ctrl Pts',(1.80968327565849,3.49383931701827,41.1881476701346));
#27583=CARTESIAN_POINT('Ctrl Pts',(1.70546107652955,3.54399372409753,41.1940127862934));
#27584=CARTESIAN_POINT('Ctrl Pts',(1.60108569834002,3.59422184488677,41.1998865226213));
#27585=CARTESIAN_POINT('Ctrl Pts',(1.49462412910148,3.63977034598794,41.2057602589493));
#27586=CARTESIAN_POINT('Ctrl Pts',(1.38653874719456,3.6804890031799,41.2116339952772));
#27587=CARTESIAN_POINT('Ctrl Pts',(1.35690377355658,3.69165329118229,41.2132444630219));
#27588=CARTESIAN_POINT('Ctrl Pts',(1.327146803713,3.70245478722107,41.2148549307666));
#27589=CARTESIAN_POINT('Ctrl Pts',(1.29727751869983,3.71289106216113,41.2164653985113));
#27590=CARTESIAN_POINT('Ctrl Pts',(1.18833940384668,3.75095384530303,41.2223390349262));
#27591=CARTESIAN_POINT('Ctrl Pts',(1.07754295601843,3.78428161568497,41.228212671341));
#27592=CARTESIAN_POINT('Ctrl Pts',(0.965337447573294,3.81269099355202,41.2340863077559));
#27593=CARTESIAN_POINT('Ctrl Pts',(0.853277037124245,3.84106363397314,41.239952348707));
#27594=CARTESIAN_POINT('Ctrl Pts',(0.739811586491714,3.86453042970389,41.2458183896581));
#27595=CARTESIAN_POINT('Ctrl Pts',(0.625408373353521,3.88295678144108,41.2516844306092));
#27596=CARTESIAN_POINT('Ctrl Pts',(0.511122540017522,3.90136422740228,41.2575444528943));
#27597=CARTESIAN_POINT('Ctrl Pts',(0.395901263452485,3.91474145074433,41.2634044751794));
#27598=CARTESIAN_POINT('Ctrl Pts',(0.280224296749863,3.92300437719754,41.2692644974645));
#27599=CARTESIAN_POINT('Ctrl Pts',(0.160029082088124,3.93159004681775,41.27535340744));
#27600=CARTESIAN_POINT('Ctrl Pts',(0.0393422945093155,3.93465364349232,
41.2814423174154));
#27601=CARTESIAN_POINT('Ctrl Pts',(-0.0812889261354467,3.93215985311988,
41.2875312273908));
#27602=CARTESIAN_POINT('Ctrl Pts',(-0.197251541468887,3.92976257609544,
41.2933844876124));
#27603=CARTESIAN_POINT('Ctrl Pts',(-0.31316235941206,3.92223008221031,41.299237747834));
#27604=CARTESIAN_POINT('Ctrl Pts',(-0.428533760636677,3.90958409757286,
41.3050910080556));
#27605=CARTESIAN_POINT('Ctrl Pts',(-0.54388773069462,3.89694002358453,41.3109433839232));
#27606=CARTESIAN_POINT('Ctrl Pts',(-0.658702035494459,3.87918404001055,
41.3167957597908));
#27607=CARTESIAN_POINT('Ctrl Pts',(-0.772493990199379,3.85638976701083,
41.3226481356584));
#27608=CARTESIAN_POINT('Ctrl Pts',(-0.886296273008748,3.83359342513345,
41.3285010427055));
#27609=CARTESIAN_POINT('Ctrl Pts',(-0.999075616123448,3.80575796591518,
41.3343539497526));
#27610=CARTESIAN_POINT('Ctrl Pts',(-1.11036004185059,3.77300802774942,41.3402068567997));
#27611=CARTESIAN_POINT('Ctrl Pts',(-1.22168148223857,3.74024719652431,41.3460617106005));
#27612=CARTESIAN_POINT('Ctrl Pts',(-1.33150662037376,3.70256875254571,41.3519165644013));
#27613=CARTESIAN_POINT('Ctrl Pts',(-1.43937981899881,3.66014681900316,41.3577714182021));
#27614=CARTESIAN_POINT('Ctrl Pts',(-1.5473756888414,3.61767664409663,41.3636329300241));
#27615=CARTESIAN_POINT('Ctrl Pts',(-1.65341480395904,3.57045236420457,41.3694944418461));
#27616=CARTESIAN_POINT('Ctrl Pts',(-1.75706256052522,3.51869580361823,41.3753559536681));
#27617=CARTESIAN_POINT('Ctrl Pts',(-1.86078010940055,3.4669043922064,41.3812214124009));
#27618=CARTESIAN_POINT('Ctrl Pts',(-1.96210273312705,3.41057482342103,41.3870868711337));
#27619=CARTESIAN_POINT('Ctrl Pts',(-2.06062295316566,3.34997343943006,41.3929523298664));
#27620=CARTESIAN_POINT('Ctrl Pts',(-2.15928829598066,3.28928278806742,41.3988264285683));
#27621=CARTESIAN_POINT('Ctrl Pts',(-2.25514265560694,3.22430799375315,41.4047005272701));
#27622=CARTESIAN_POINT('Ctrl Pts',(-2.34780981417076,3.15535704421599,41.410574625972));
#27623=CARTESIAN_POINT('Ctrl Pts',(-2.37317538403825,3.13648325813017,41.4121825296062));
#27624=CARTESIAN_POINT('Ctrl Pts',(-2.39830235271441,3.11731177138596,41.4137904332405));
#27625=CARTESIAN_POINT('Ctrl Pts',(-2.4231834817654,3.09784938525089,41.4153983368747));
#27626=CARTESIAN_POINT('Ctrl Pts',(-2.5139243099458,3.02687057104019,41.421262319458));
#27627=CARTESIAN_POINT('Ctrl Pts',(-2.60169853262691,2.95178047655881,41.4271263020412));
#27628=CARTESIAN_POINT('Ctrl Pts',(-2.68610962259956,2.87285643487071,41.4329902846244));
#27629=CARTESIAN_POINT('Ctrl Pts',(-2.77041086511586,2.79403510012819,41.4388466361775));
#27630=CARTESIAN_POINT('Ctrl Pts',(-2.85135737773794,2.71139001988999,41.4447029877306));
#27631=CARTESIAN_POINT('Ctrl Pts',(-2.92858385142488,2.62524010809933,41.4505593392837));
#27632=CARTESIAN_POINT('Ctrl Pts',(-3.00573063919795,2.53917908984638,41.4564096479774));
#27633=CARTESIAN_POINT('Ctrl Pts',(-3.07916474743663,2.44962073974177,41.4622599566711));
#27634=CARTESIAN_POINT('Ctrl Pts',(-3.14855656489229,2.35692183953428,41.4681102653647));
#27635=CARTESIAN_POINT('Ctrl Pts',(-3.22082156659725,2.26038471992616,41.4742028074428));
#27636=CARTESIAN_POINT('Ctrl Pts',(-3.28870197815474,2.16044168279813,41.4802953495208));
#27637=CARTESIAN_POINT('Ctrl Pts',(-3.35187063466801,2.05753547926888,41.4863878915989));
#27638=CARTESIAN_POINT('Ctrl Pts',(-3.41245765236363,1.95883494773385,41.4922314376717));
#27639=CARTESIAN_POINT('Ctrl Pts',(-3.46871023004299,1.85740907706089,41.4980749837446));
#27640=CARTESIAN_POINT('Ctrl Pts',(-3.52038354497778,1.75367861829061,41.5039185298174));
#27641=CARTESIAN_POINT('Ctrl Pts',(-3.57204917985033,1.64996357669225,41.5097612073801));
#27642=CARTESIAN_POINT('Ctrl Pts',(-3.61913672024701,1.54394499904711,41.5156038849428));
#27643=CARTESIAN_POINT('Ctrl Pts',(-3.66144766340146,1.43606755000314,41.5214465625056));
#27644=CARTESIAN_POINT('Ctrl Pts',(-3.70376264035098,1.32817981625524,41.5272897970912));
#27645=CARTESIAN_POINT('Ctrl Pts',(-3.74129996337929,1.21843324488357,41.5331330316768));
#27646=CARTESIAN_POINT('Ctrl Pts',(-3.77390984208486,1.10729106553562,41.5389762662624));
#27647=CARTESIAN_POINT('Ctrl Pts',(-3.8065307854242,0.996111175298837,41.5448214834757));
#27648=CARTESIAN_POINT('Ctrl Pts',(-3.83422084347951,0.883535133223119,
41.5506667006891));
#27649=CARTESIAN_POINT('Ctrl Pts',(-3.85688069745533,0.77003914549617,41.5565119179025));
#27650=CARTESIAN_POINT('Ctrl Pts',(-3.87956675613467,0.656411906759731,
41.5623638947439));
#27651=CARTESIAN_POINT('Ctrl Pts',(-3.89721091892512,0.541863005858298,
41.5682158715852));
#27652=CARTESIAN_POINT('Ctrl Pts',(-3.90976537386394,0.426876705073691,
41.5740678484266));
#27653=CARTESIAN_POINT('Ctrl Pts',(-3.92232839714301,0.311811926827965,
41.5799238192072));
#27654=CARTESIAN_POINT('Ctrl Pts',(-3.92979476977478,0.196309567073772,
41.5857797899877));
#27655=CARTESIAN_POINT('Ctrl Pts',(-3.93216879837236,0.0808550623451563,
41.5916357607682));
#27656=CARTESIAN_POINT('Ctrl Pts',(-3.93454638763816,-0.0347726059187965,
41.5975005145806));
#27657=CARTESIAN_POINT('Ctrl Pts',(-3.9318163996028,-0.150351862985736,
41.6033652683931));
#27658=CARTESIAN_POINT('Ctrl Pts',(-3.92403507123059,-0.26540112990027,
41.6092300222056));
#27659=CARTESIAN_POINT('Ctrl Pts',(-3.92177896488034,-0.298758336955588,
41.6109304398831));
#27660=CARTESIAN_POINT('Ctrl Pts',(-3.91909855040044,-0.332071051361949,
41.6126308575607));
#27661=CARTESIAN_POINT('Ctrl Pts',(-3.91599599938462,-0.36532770604443,
41.6143312752382));
#27662=CARTESIAN_POINT('Ctrl Pts',(-3.90526104620493,-0.480397088983917,
41.6202147898239));
#27663=CARTESIAN_POINT('Ctrl Pts',(-3.88943223306831,-0.595182622947716,
41.6260983044096));
#27664=CARTESIAN_POINT('Ctrl Pts',(-3.86853032292968,-0.709198237852823,
41.6319818189952));
#27665=CARTESIAN_POINT('Ctrl Pts',(-3.84765556061053,-0.823065766994018,
41.6378576919544));
#27666=CARTESIAN_POINT('Ctrl Pts',(-3.82172087916518,-0.936164964568238,
41.6437335649135));
#27667=CARTESIAN_POINT('Ctrl Pts',(-3.79079888577828,-1.04801374398534,
41.6496094378726));
#27668=CARTESIAN_POINT('Ctrl Pts',(-3.75990886633242,-1.15974686959469,
41.6554792350651));
#27669=CARTESIAN_POINT('Ctrl Pts',(-3.72404190230729,-1.27023175454549,
41.6613490322575));
#27670=CARTESIAN_POINT('Ctrl Pts',(-3.68332172739711,-1.37899603062677,
41.66721882945));
#27671=CARTESIAN_POINT('Ctrl Pts',(-3.64110708328714,-1.49175205922383,
41.6733040537897));
#27672=CARTESIAN_POINT('Ctrl Pts',(-3.59367623703547,-1.60265831580807,
41.6793892781293));
#27673=CARTESIAN_POINT('Ctrl Pts',(-3.54122397187539,-1.71120477471723,
41.685474502469));
#27674=CARTESIAN_POINT('Ctrl Pts',(-3.49068863748631,-1.81578427344784,
41.6913373350063));
#27675=CARTESIAN_POINT('Ctrl Pts',(-3.43549267616954,-1.91817303245174,
41.6972001675436));
#27676=CARTESIAN_POINT('Ctrl Pts',(-3.37585917784821,-2.0179355320074,41.703063000081));
#27677=CARTESIAN_POINT('Ctrl Pts',(-3.31623560038966,-2.11768143468218,
41.7089248572545));
#27678=CARTESIAN_POINT('Ctrl Pts',(-3.25217616516896,-2.21480159349513,
41.714786714428));
#27679=CARTESIAN_POINT('Ctrl Pts',(-3.18394911200897,-2.30888653946817,
41.7206485716015));
#27680=CARTESIAN_POINT('Ctrl Pts',(-3.11571705126772,-2.402978390884,41.7265108590108));
#27681=CARTESIAN_POINT('Ctrl Pts',(-3.04331700627884,-2.49403425335169,
41.7323731464202));
#27682=CARTESIAN_POINT('Ctrl Pts',(-2.96705918382821,-2.58167557986295,
41.7382354338296));
#27683=CARTESIAN_POINT('Ctrl Pts',(-2.89077748099677,-2.66934435153568,
41.744099557033));
#27684=CARTESIAN_POINT('Ctrl Pts',(-2.81063586852203,-2.75359615052861,
41.7499636802364));
#27685=CARTESIAN_POINT('Ctrl Pts',(-2.72698280046746,-2.83408782608349,
41.7558278034398));
#27686=CARTESIAN_POINT('Ctrl Pts',(-2.64323775706398,-2.91466800108155,
41.7616983741626));
#27687=CARTESIAN_POINT('Ctrl Pts',(-2.55597384866479,-2.99147951499695,
41.7675689448854));
#27688=CARTESIAN_POINT('Ctrl Pts',(-2.46557420551259,-3.06421814450456,
41.7734395156082));
#27689=CARTESIAN_POINT('Ctrl Pts',(-2.37511550448373,-3.13700429398968,
41.7793139215612));
#27690=CARTESIAN_POINT('Ctrl Pts',(-2.28151732014737,-3.20571201698357,
41.7851883275142));
#27691=CARTESIAN_POINT('Ctrl Pts',(-2.18519207308076,-3.27008021365608,
41.7910627334672));
#27692=CARTESIAN_POINT('Ctrl Pts',(-2.08872895754162,-3.33454053928985,
41.7969455473444));
#27693=CARTESIAN_POINT('Ctrl Pts',(-1.98953133977585,-3.39464872925959,
41.8028283612216));
#27694=CARTESIAN_POINT('Ctrl Pts',(-1.8880365988769,-3.45018938629481,41.8087111750988));
#27695=CARTESIAN_POINT('Ctrl Pts',(-1.86185244773223,-3.46451805934332,
41.8102288545998));
#27696=CARTESIAN_POINT('Ctrl Pts',(-1.83551551169213,-3.47854298330307,
41.8117465341007));
#27697=CARTESIAN_POINT('Ctrl Pts',(-1.80903350294568,-3.4922609846946,41.8132642136017));
#27698=CARTESIAN_POINT('Ctrl Pts',(-1.70742103092262,-3.54489747635787,
41.8190876074124));
#27699=CARTESIAN_POINT('Ctrl Pts',(-1.60332774807853,-3.59318933627977,
41.8249110012232));
#27700=CARTESIAN_POINT('Ctrl Pts',(-1.49716503359537,-3.63689233579706,
41.8307343950339));
#27701=CARTESIAN_POINT('Ctrl Pts',(-1.39113820063262,-3.68053939825537,
41.8365503352711));
#27702=CARTESIAN_POINT('Ctrl Pts',(-1.28304758713599,-3.71960911780812,
41.8423662755082));
#27703=CARTESIAN_POINT('Ctrl Pts',(-1.17332958763058,-3.75390285953042,
41.8481822157454));
#27704=CARTESIAN_POINT('Ctrl Pts',(-1.06372144601052,-3.78816226378791,
41.8539923326272));
#27705=CARTESIAN_POINT('Ctrl Pts',(-0.952489557777298,-3.81765507416629,
41.859802449509));
#27706=CARTESIAN_POINT('Ctrl Pts',(-0.840090023954876,-3.84223083008446,
41.8656125663909));
#27707=CARTESIAN_POINT('Ctrl Pts',(-0.727768808379918,-3.86678946199802,
41.8714186348736));
#27708=CARTESIAN_POINT('Ctrl Pts',(-0.614281974956971,-3.88643776297211,
41.8772247033564));
#27709=CARTESIAN_POINT('Ctrl Pts',(-0.500099795513575,-3.90107538949548,
41.8830307718391));
#27710=CARTESIAN_POINT('Ctrl Pts',(-0.385958726636555,-3.91570774583465,
41.8888347498838));
#27711=CARTESIAN_POINT('Ctrl Pts',(-0.271123226235575,-3.92533295960325,
41.8946387279286));
#27712=CARTESIAN_POINT('Ctrl Pts',(-0.15607206147564,-3.92990209949647,
41.9004427059734));
#27713=CARTESIAN_POINT('Ctrl Pts',(-0.0410333161247926,-3.9344707461655,
41.9062460574971));
#27714=CARTESIAN_POINT('Ctrl Pts',(0.0742206267747902,-3.93398438758145,
41.9120494090208));
#27715=CARTESIAN_POINT('Ctrl Pts',(0.18920841364813,-3.92844615289617,41.9178527605445));
#27716=CARTESIAN_POINT('Ctrl Pts',(0.304212776840347,-3.92290711983442,
41.9236569486632));
#27717=CARTESIAN_POINT('Ctrl Pts',(0.418950487396495,-3.91231478424112,
41.9294611367818));
#27718=CARTESIAN_POINT('Ctrl Pts',(0.532943549870492,-3.89672428748192,
41.9352653249005));
#27719=CARTESIAN_POINT('Ctrl Pts',(0.647049319293432,-3.88111837612393,
41.9410752517222));
#27720=CARTESIAN_POINT('Ctrl Pts',(0.760408552861537,-3.86050449312197,
41.946885178544));
#27721=CARTESIAN_POINT('Ctrl Pts',(0.872551680866595,-3.83498925216445,
41.9526951053657));
#27722=CARTESIAN_POINT('Ctrl Pts',(0.984753634335691,-3.80946062700841,
41.9585080798253));
#27723=CARTESIAN_POINT('Ctrl Pts',(1.0957378064602,-3.77902563596717,41.9643210542848));
#27724=CARTESIAN_POINT('Ctrl Pts',(1.20504985637141,-3.74384078770175,41.9701340287444));
#27725=CARTESIAN_POINT('Ctrl Pts',(1.31452994394932,-3.70860185226286,41.9759559390776));
#27726=CARTESIAN_POINT('Ctrl Pts',(1.42233238172794,-3.66859862421664,41.9817778494108));
#27727=CARTESIAN_POINT('Ctrl Pts',(1.52802263117264,-3.62403584952249,41.987599759744));
#27728=CARTESIAN_POINT('Ctrl Pts',(1.60268276788032,-3.59255647589797,41.991712387197));
#27729=CARTESIAN_POINT('Ctrl Pts',(1.67628935708178,-3.55880285359254,41.99582501465));
#27730=CARTESIAN_POINT('Ctrl Pts',(1.74869731696171,-3.52286058390776,41.9999376421029));
#27731=CARTESIAN_POINT('',(-1.7486944753309,-3.52286199445099,42.));
#27732=CARTESIAN_POINT('Origin',(0.,0.,42.));
#27733=CARTESIAN_POINT('',(3.93228009845805,0.00389650693369247,41.1541638748943));
#27734=CARTESIAN_POINT('Ctrl Pts',(-1.7486944753309,-3.52286199445099,42.));
#27735=CARTESIAN_POINT('Ctrl Pts',(-2.92291840980274,-2.93999530530831,
41.9336890205455));
#27736=CARTESIAN_POINT('Ctrl Pts',(-4.621982019705,-0.51750383458989,41.8010670616367));
#27737=CARTESIAN_POINT('Ctrl Pts',(-2.92991200205014,3.61782035329863,41.602134123273));
#27738=CARTESIAN_POINT('Ctrl Pts',(1.45961866169696,4.41606836987815,41.4032011849098));
#27739=CARTESIAN_POINT('Ctrl Pts',(3.74575420314252,1.97212767892205,41.2538777887601));
#27740=CARTESIAN_POINT('Ctrl Pts',(3.93515403968839,0.334151972648519,41.1708653720651));
#27741=CARTESIAN_POINT('Ctrl Pts',(3.93215815619892,0.00389757136549701,
41.1541639348245));
#27742=CARTESIAN_POINT('',(3.93299992557056,-0.000765154855056892,39.9041635219977));
#27743=CARTESIAN_POINT('Ctrl Pts',(3.93299807602736,0.00389023972029836,
41.1541635220349));
#27744=CARTESIAN_POINT('Ctrl Pts',(3.93311122308255,-0.110500436017224,
41.1483798001704));
#27745=CARTESIAN_POINT('Ctrl Pts',(3.92822960554725,-0.22502150371433,41.142596078306));
#27746=CARTESIAN_POINT('Ctrl Pts',(3.91834595805662,-0.339196039159292,
41.1368123564415));
#27747=CARTESIAN_POINT('Ctrl Pts',(3.90846841189372,-0.453300092906078,
41.1310322049576));
#27748=CARTESIAN_POINT('Ctrl Pts',(3.89359501003231,-0.567057617791912,
41.1252520534736));
#27749=CARTESIAN_POINT('Ctrl Pts',(3.87377055495045,-0.679993152611765,
41.1194719019897));
#27750=CARTESIAN_POINT('Ctrl Pts',(3.85395218492908,-0.792894022188202,
41.113693524707));
#27751=CARTESIAN_POINT('Ctrl Pts',(3.8291858546012,-0.90497298515588,41.1079151474242));
#27752=CARTESIAN_POINT('Ctrl Pts',(3.79956795898915,-1.01576194308659,41.1021367701414));
#27753=CARTESIAN_POINT('Ctrl Pts',(3.76995155801667,-1.1265453101555,41.0963586844591));
#27754=CARTESIAN_POINT('Ctrl Pts',(3.73548418844761,-1.23603839142066,41.0905805987768));
#27755=CARTESIAN_POINT('Ctrl Pts',(3.69631266180428,-1.34378633204291,41.0848025130945));
#27756=CARTESIAN_POINT('Ctrl Pts',(3.65713306433753,-1.45155647283649,41.0790232369069));
#27757=CARTESIAN_POINT('Ctrl Pts',(3.61324752952121,-1.55758035968635,41.0732439607192));
#27758=CARTESIAN_POINT('Ctrl Pts',(3.56485142260143,-1.66142208206602,41.0674646845316));
#27759=CARTESIAN_POINT('Ctrl Pts',(3.51640383488079,-1.76537426488084,41.0616792607056));
#27760=CARTESIAN_POINT('Ctrl Pts',(3.4634362768292,-1.86713926420627,41.0558938368796));
#27761=CARTESIAN_POINT('Ctrl Pts',(3.4061905932739,-1.96630481927202,41.0501084130536));
#27762=CARTESIAN_POINT('Ctrl Pts',(3.34891136462435,-2.06552848383504,41.0443195990577));
#27763=CARTESIAN_POINT('Ctrl Pts',(3.28734924928495,-2.16214931524564,41.0385307850619));
#27764=CARTESIAN_POINT('Ctrl Pts',(3.22178896106807,-2.25578476152755,41.0327419710661));
#27765=CARTESIAN_POINT('Ctrl Pts',(3.15612629068068,-2.34956643352762,41.0269441169736));
#27766=CARTESIAN_POINT('Ctrl Pts',(3.08645324145257,-2.44035307775196,41.0211462628811));
#27767=CARTESIAN_POINT('Ctrl Pts',(3.01309433601815,-2.52779578333681,41.0153484087886));
#27768=CARTESIAN_POINT('Ctrl Pts',(2.97086318815253,-2.57813467276619,41.0120107085867));
#27769=CARTESIAN_POINT('Ctrl Pts',(2.92741121452159,-2.62736604230084,41.0086730083847));
#27770=CARTESIAN_POINT('Ctrl Pts',(2.88280549253714,-2.67542921644317,41.0053353081828));
#27771=CARTESIAN_POINT('Ctrl Pts',(2.80430807862628,-2.76001107515256,40.999461603586));
#27772=CARTESIAN_POINT('Ctrl Pts',(2.72195391264452,-2.84127661989262,40.9935878989893));
#27773=CARTESIAN_POINT('Ctrl Pts',(2.63605432670703,-2.91885364255372,40.9877141943925));
#27774=CARTESIAN_POINT('Ctrl Pts',(2.55026600203703,-2.99633018373084,40.9818480976999));
#27775=CARTESIAN_POINT('Ctrl Pts',(2.46094169355245,-3.07012742940372,40.9759820010073));
#27776=CARTESIAN_POINT('Ctrl Pts',(2.36843146370396,-3.13990786516692,40.9701159043147));
#27777=CARTESIAN_POINT('Ctrl Pts',(2.27601634556961,-3.20961655819562,40.9642558386796));
#27778=CARTESIAN_POINT('Ctrl Pts',(2.18042214917457,-3.27531640841443,40.9583957730444));
#27779=CARTESIAN_POINT('Ctrl Pts',(2.0820335956378,-3.336708723673,40.9525357074093));
#27780=CARTESIAN_POINT('Ctrl Pts',(1.97980317277675,-3.40049828174347,40.9464468183431));
#27781=CARTESIAN_POINT('Ctrl Pts',(1.87455605503832,-3.45963674409439,40.9403579292768));
#27782=CARTESIAN_POINT('Ctrl Pts',(1.76675931968063,-3.51383700622576,40.9342690402106));
#27783=CARTESIAN_POINT('Ctrl Pts',(1.66313390444639,-3.56593992613824,40.9284157677927));
#27784=CARTESIAN_POINT('Ctrl Pts',(1.55715292797622,-3.61347951740685,40.9225624953748));
#27785=CARTESIAN_POINT('Ctrl Pts',(1.44925754859986,-3.65624692243649,40.916709222957));
#27786=CARTESIAN_POINT('Ctrl Pts',(1.34137868292838,-3.69900778178912,40.9108568463997));
#27787=CARTESIAN_POINT('Ctrl Pts',(1.23158638092573,-3.73699775498812,40.9050044698423));
#27788=CARTESIAN_POINT('Ctrl Pts',(1.12034171211492,-3.77005615980656,40.899152093285));
#27789=CARTESIAN_POINT('Ctrl Pts',(1.00908716513153,-3.80311750010616,40.8932991970553));
#27790=CARTESIAN_POINT('Ctrl Pts',(0.89638039103105,-3.83124628380499,40.8874463008256));
#27791=CARTESIAN_POINT('Ctrl Pts',(0.78269685867274,-3.8543319301046,40.8815934045958));
#27792=CARTESIAN_POINT('Ctrl Pts',(0.668975737292473,-3.8774252095842,40.8757385731285));
#27793=CARTESIAN_POINT('Ctrl Pts',(0.554277620140873,-3.89547195374573,
40.8698837416612));
#27794=CARTESIAN_POINT('Ctrl Pts',(0.439086679126237,-3.90841296285511,
40.8640289101939));
#27795=CARTESIAN_POINT('Ctrl Pts',(0.323765078495354,-3.92136865078619,
40.8581674376658));
#27796=CARTESIAN_POINT('Ctrl Pts',(0.207949949061725,-3.92920699804321,
40.8523059651378));
#27797=CARTESIAN_POINT('Ctrl Pts',(0.0921291821830041,-3.93192080461831,
40.8464444926098));
#27798=CARTESIAN_POINT('Ctrl Pts',(-0.0237693783711899,-3.93463643398386,
40.8405790830892));
#27799=CARTESIAN_POINT('Ctrl Pts',(-0.139673171838126,-3.93222067739507,
40.8347136735687));
#27800=CARTESIAN_POINT('Ctrl Pts',(-0.255097458942097,-3.92471837033452,
40.8288482640481));
#27801=CARTESIAN_POINT('Ctrl Pts',(-0.370691491350461,-3.91720503022861,
40.822974228737));
#27802=CARTESIAN_POINT('Ctrl Pts',(-0.485804200819735,-3.90459025494561,
40.817100193426));
#27803=CARTESIAN_POINT('Ctrl Pts',(-0.59995899977985,-3.88697031099842,
40.8112261581149));
#27804=CARTESIAN_POINT('Ctrl Pts',(-0.631207170979042,-3.88214711451437,
40.809618228683));
#27805=CARTESIAN_POINT('Ctrl Pts',(-0.662383643985488,-3.87694916719674,
40.8080102992512));
#27806=CARTESIAN_POINT('Ctrl Pts',(-0.693478838898908,-3.87137909536116,
40.8064023698194));
#27807=CARTESIAN_POINT('Ctrl Pts',(-0.807061393191453,-3.85103309050611,
40.80052902725));
#27808=CARTESIAN_POINT('Ctrl Pts',(-0.919937276006077,-3.82565030150215,
40.7946556846807));
#27809=CARTESIAN_POINT('Ctrl Pts',(-1.03162511240368,-3.79529163931549,
40.7887823421113));
#27810=CARTESIAN_POINT('Ctrl Pts',(-1.14316862030515,-3.76497220808003,
40.7829165893631));
#27811=CARTESIAN_POINT('Ctrl Pts',(-1.25352673979851,-3.72968979828012,
40.7770508366148));
#27812=CARTESIAN_POINT('Ctrl Pts',(-1.36222637023903,-3.68955665578202,
40.7711850838666));
#27813=CARTESIAN_POINT('Ctrl Pts',(-1.47081457925781,-3.64946465134279,
40.765325343747));
#27814=CARTESIAN_POINT('Ctrl Pts',(-1.57774729535856,-3.60453194651736,
40.7594656036273));
#27815=CARTESIAN_POINT('Ctrl Pts',(-1.6825653666707,-3.55492092554536,40.7536058635077));
#27816=CARTESIAN_POINT('Ctrl Pts',(-1.79148472318545,-3.50336874172185,
40.7475168455056));
#27817=CARTESIAN_POINT('Ctrl Pts',(-1.89812013501853,-3.44676478256776,
40.7414278275034));
#27818=CARTESIAN_POINT('Ctrl Pts',(-2.00197761118039,-3.38534704931894,
40.7353388095013));
#27819=CARTESIAN_POINT('Ctrl Pts',(-2.10180936321883,-3.32630999062031,
40.729485814052));
#27820=CARTESIAN_POINT('Ctrl Pts',(-2.1990741372511,-3.26282562168927,40.7236328186027));
#27821=CARTESIAN_POINT('Ctrl Pts',(-2.29335789691542,-3.19515235265169,
40.7177798231534));
#27822=CARTESIAN_POINT('Ctrl Pts',(-2.38762752339369,-3.12748922787338,
40.7119277050713));
#27823=CARTESIAN_POINT('Ctrl Pts',(-2.47891668839842,-3.05563869237956,
40.7060755869892));
#27824=CARTESIAN_POINT('Ctrl Pts',(-2.5668411441862,-2.9799019347141,40.700223468907));
#27825=CARTESIAN_POINT('Ctrl Pts',(-2.65477369118737,-2.90415820740338,
40.6943708122861));
#27826=CARTESIAN_POINT('Ctrl Pts',(-2.7393406003306,-2.82452781666461,40.6885181556651));
#27827=CARTESIAN_POINT('Ctrl Pts',(-2.82019201104604,-2.74135113052526,
40.6826654990441));
#27828=CARTESIAN_POINT('Ctrl Pts',(-2.9010704220475,-2.65814666757537,40.6768108879315));
#27829=CARTESIAN_POINT('Ctrl Pts',(-2.97823057949439,-2.57139385045657,
40.6709562768189));
#27830=CARTESIAN_POINT('Ctrl Pts',(-3.05136116400601,-2.48146812326813,
40.6651016657063));
#27831=CARTESIAN_POINT('Ctrl Pts',(-3.12457507635168,-2.39143993120645,
40.659240383622));
#27832=CARTESIAN_POINT('Ctrl Pts',(-3.19374999046137,-2.29823193371721,
40.6533791015377));
#27833=CARTESIAN_POINT('Ctrl Pts',(-3.2586163394363,-2.20225079233923,40.6475178194533));
#27834=CARTESIAN_POINT('Ctrl Pts',(-3.32352644906473,-2.10620489939843,
40.6416525831841));
#27835=CARTESIAN_POINT('Ctrl Pts',(-3.38412199026311,-2.00738248872334,
40.635787346915));
#27836=CARTESIAN_POINT('Ctrl Pts',(-3.44017889227008,-1.90621567226255,
40.6299221106458));
#27837=CARTESIAN_POINT('Ctrl Pts',(-3.4963184910571,-1.80489961155763,40.6240482218087));
#27838=CARTESIAN_POINT('Ctrl Pts',(-3.54790590417778,-1.70123261100789,
40.6181743329715));
#27839=CARTESIAN_POINT('Ctrl Pts',(-3.59476474769179,-1.59566769997778,
40.6123004441344));
#27840=CARTESIAN_POINT('Ctrl Pts',(-3.60761118687321,-1.56672688310006,
40.6106901065749));
#27841=CARTESIAN_POINT('Ctrl Pts',(-3.62010251857552,-1.53764351164238,
40.6090797690154));
#27842=CARTESIAN_POINT('Ctrl Pts',(-3.63223576574945,-1.50842710861696,
40.6074694314559));
#27843=CARTESIAN_POINT('Ctrl Pts',(-3.67647145818702,-1.40190922434097,
40.6015984229797));
#27844=CARTESIAN_POINT('Ctrl Pts',(-3.71609204453458,-1.29326458447947,
40.5957274145035));
#27845=CARTESIAN_POINT('Ctrl Pts',(-3.75088844203362,-1.18293063846473,
40.5898564060273));
#27846=CARTESIAN_POINT('Ctrl Pts',(-3.78563962999961,-1.07274004482372,
40.5839930255118));
#27847=CARTESIAN_POINT('Ctrl Pts',(-3.81557897026632,-0.960864900513171,
40.5781296449963));
#27848=CARTESIAN_POINT('Ctrl Pts',(-3.84054502427604,-0.847763479107561,
40.5722662644808));
#27849=CARTESIAN_POINT('Ctrl Pts',(-3.86548532727636,-0.734778715134654,
40.5664089316958));
#27850=CARTESIAN_POINT('Ctrl Pts',(-3.88546245842252,-0.620570591278151,
40.5605515989107));
#27851=CARTESIAN_POINT('Ctrl Pts',(-3.90036469004281,-0.505612781352745,
40.5546942661257));
#27852=CARTESIAN_POINT('Ctrl Pts',(-3.91585863773476,-0.386090394427762,
40.548604358916));
#27853=CARTESIAN_POINT('Ctrl Pts',(-3.9258661880868,-0.265757987767407,
40.5425144517063));
#27854=CARTESIAN_POINT('Ctrl Pts',(-3.93032027697842,-0.145160326440494,
40.5364245444966));
#27855=CARTESIAN_POINT('Ctrl Pts',(-3.93459927735498,-0.0293033126295149,
40.5305740291886));
#27856=CARTESIAN_POINT('Ctrl Pts',(-3.93375315879367,0.0867980431762234,
40.5247235138806));
#27857=CARTESIAN_POINT('Ctrl Pts',(-3.92777539071006,0.202656063645884,
40.5188729985725));
#27858=CARTESIAN_POINT('Ctrl Pts',(-3.92179854230237,0.318496259430816,
40.5130233833627));
#27859=CARTESIAN_POINT('Ctrl Pts',(-3.91069163543769,0.43409278138595,40.5071737681528));
#27860=CARTESIAN_POINT('Ctrl Pts',(-3.89450023206756,0.548959873238225,
40.501324152943));
#27861=CARTESIAN_POINT('Ctrl Pts',(-3.87830739385005,0.663837144365366,
40.4954740193528));
#27862=CARTESIAN_POINT('Ctrl Pts',(-3.85702922116871,0.777984447321958,
40.4896238857626));
#27863=CARTESIAN_POINT('Ctrl Pts',(-3.83076282774209,0.890923766429782,
40.4837737521724));
#27864=CARTESIAN_POINT('Ctrl Pts',(-3.80448773790008,1.00390047808009,40.4779216816893));
#27865=CARTESIAN_POINT('Ctrl Pts',(-3.77322123704001,1.11566800799436,40.4720696112062));
#27866=CARTESIAN_POINT('Ctrl Pts',(-3.73711078392592,1.22576179931689,40.4662175407231));
#27867=CARTESIAN_POINT('Ctrl Pts',(-3.70095925018538,1.3359808375285,40.4603588127017));
#27868=CARTESIAN_POINT('Ctrl Pts',(-3.65995289405373,1.44452194337658,40.4545000846804));
#27869=CARTESIAN_POINT('Ctrl Pts',(-3.61428800787736,1.55093881120884,40.4486413566591));
#27870=CARTESIAN_POINT('Ctrl Pts',(-3.56859238718388,1.65742730236746,40.4427786854509));
#27871=CARTESIAN_POINT('Ctrl Pts',(-3.51823217262971,1.76178833713314,40.4369160142428));
#27872=CARTESIAN_POINT('Ctrl Pts',(-3.46344965982526,1.86360013250061,40.4310533430347));
#27873=CARTESIAN_POINT('Ctrl Pts',(-3.40858626068035,1.96556225291017,40.4251820155967));
#27874=CARTESIAN_POINT('Ctrl Pts',(-3.34928774270519,2.06496726793466,40.4193106881588));
#27875=CARTESIAN_POINT('Ctrl Pts',(-3.28583977385381,2.16142221247038,40.4134393607209));
#27876=CARTESIAN_POINT('Ctrl Pts',(-3.26817897534573,2.18827053198937,40.4118050715114));
#27877=CARTESIAN_POINT('Ctrl Pts',(-3.2501969195197,2.21489048117082,40.410170782302));
#27878=CARTESIAN_POINT('Ctrl Pts',(-3.23190030655268,2.24127405921379,40.4085364930925));
#27879=CARTESIAN_POINT('Ctrl Pts',(-3.1661558687843,2.33607704312568,40.4026640714907));
#27880=CARTESIAN_POINT('Ctrl Pts',(-3.09612640254298,2.42814361612027,40.3967916498889));
#27881=CARTESIAN_POINT('Ctrl Pts',(-3.02206731929664,2.51706140521824,40.3909192282871));
#27882=CARTESIAN_POINT('Ctrl Pts',(-2.94810422636286,2.60586394516656,40.3850544181161));
#27883=CARTESIAN_POINT('Ctrl Pts',(-2.8701221650361,2.69152550264971,40.3791896079451));
#27884=CARTESIAN_POINT('Ctrl Pts',(-2.78841979895134,2.77366256506017,40.3733247977741));
#27885=CARTESIAN_POINT('Ctrl Pts',(-2.70680147827903,2.85571513489572,40.3674660206032));
#27886=CARTESIAN_POINT('Ctrl Pts',(-2.62147075470606,2.93425012980326,40.3616072434324));
#27887=CARTESIAN_POINT('Ctrl Pts',(-2.53276609625377,3.00891756312257,40.3557484662616));
#27888=CARTESIAN_POINT('Ctrl Pts',(-2.4405701333704,3.08652381324533,40.3496590949477));
#27889=CARTESIAN_POINT('Ctrl Pts',(-2.34472948487233,3.15995145527803,40.3435697236339));
#27890=CARTESIAN_POINT('Ctrl Pts',(-2.24566615522885,3.228850030469,40.33748035232));
#27891=CARTESIAN_POINT('Ctrl Pts',(-2.15046464221147,3.29506271104948,40.3316283648642));
#27892=CARTESIAN_POINT('Ctrl Pts',(-2.05228737424939,3.35709256806077,40.3257763774084));
#27893=CARTESIAN_POINT('Ctrl Pts',(-1.95154140619407,3.4146705756061,40.3199243899526));
#27894=CARTESIAN_POINT('Ctrl Pts',(-1.85081080027235,3.47223980343486,40.3140732948304));
#27895=CARTESIAN_POINT('Ctrl Pts',(-1.74751263184131,3.52535832648561,40.3082221997082));
#27896=CARTESIAN_POINT('Ctrl Pts',(-1.64208047633481,3.57380199636746,40.3023711045861));
#27897=CARTESIAN_POINT('Ctrl Pts',(-1.53663886795298,3.62225000962984,40.2965194848642));
#27898=CARTESIAN_POINT('Ctrl Pts',(-1.42906326778344,3.66602216391514,40.2906678651424));
#27899=CARTESIAN_POINT('Ctrl Pts',(-1.31980858498105,3.70494187525396,40.2848162454205));
#27900=CARTESIAN_POINT('Ctrl Pts',(-1.21051765142338,3.74387450017135,40.2789626841285));
#27901=CARTESIAN_POINT('Ctrl Pts',(-1.09954691662211,3.7779513420285,40.2731091228364));
#27902=CARTESIAN_POINT('Ctrl Pts',(-0.987367162415443,3.80704545370602,
40.2672555615444));
#27903=CARTESIAN_POINT('Ctrl Pts',(-0.875059831446061,3.83617265274951,
40.2613953432722));
#27904=CARTESIAN_POINT('Ctrl Pts',(-0.761541137049103,3.86030570733626,
40.255535125));
#27905=CARTESIAN_POINT('Ctrl Pts',(-0.647292886608793,3.87936862375125,
40.2496749067278));
#27906=CARTESIAN_POINT('Ctrl Pts',(-0.53296773170299,3.89844437207738,40.2438107437391));
#27907=CARTESIAN_POINT('Ctrl Pts',(-0.417912452234003,3.91244313667986,
40.2379465807504));
#27908=CARTESIAN_POINT('Ctrl Pts',(-0.30261307848539,3.92134088351543,40.2320824177618));
#27909=CARTESIAN_POINT('Ctrl Pts',(-0.187143692032647,3.93025175037023,
40.2262096078727));
#27910=CARTESIAN_POINT('Ctrl Pts',(-0.0714299045538827,3.93404657419229,
40.2203367979835));
#27911=CARTESIAN_POINT('Ctrl Pts',(0.0440430656483174,3.9327533876876,40.2144639880944));
#27912=CARTESIAN_POINT('Ctrl Pts',(0.0758988375731602,3.93239663359807,
40.2128438436393));
#27913=CARTESIAN_POINT('Ctrl Pts',(0.107736319591384,3.93165295775469,40.2112236991842));
#27914=CARTESIAN_POINT('Ctrl Pts',(0.139545428639648,3.9305236385685,40.2096035547291));
#27915=CARTESIAN_POINT('Ctrl Pts',(0.254838451148347,3.92643038898535,40.2037312949672));
#27916=CARTESIAN_POINT('Ctrl Pts',(0.370144396461502,3.91725319001592,40.1978590352052));
#27917=CARTESIAN_POINT('Ctrl Pts',(0.484978287944126,3.90298412246614,40.1919867754433));
#27918=CARTESIAN_POINT('Ctrl Pts',(0.599663355638497,3.88873354751171,40.1861221260821));
#27919=CARTESIAN_POINT('Ctrl Pts',(0.713877179661275,3.86940427755655,40.180257476721));
#27920=CARTESIAN_POINT('Ctrl Pts',(0.827135695542844,3.84504038225333,40.1743928273599));
#27921=CARTESIAN_POINT('Ctrl Pts',(0.940277725286697,3.82070154516355,40.1685342097779));
#27922=CARTESIAN_POINT('Ctrl Pts',(1.05246599948158,3.79133846864503,40.1626755921959));
#27923=CARTESIAN_POINT('Ctrl Pts',(1.16322315497426,3.75704683118693,40.1568169746139));
#27924=CARTESIAN_POINT('Ctrl Pts',(1.27834384896804,3.72140419406069,40.1507275430202));
#27925=CARTESIAN_POINT('Ctrl Pts',(1.39191789019005,3.68043672491118,40.1446381114265));
#27926=CARTESIAN_POINT('Ctrl Pts',(1.50342232422801,3.63431015668901,40.1385486798329));
#27927=CARTESIAN_POINT('Ctrl Pts',(1.61057603848535,3.58998337135894,40.1326968478532));
#27928=CARTESIAN_POINT('Ctrl Pts',(1.71581820483762,3.5408927104959,40.1268450158735));
#27929=CARTESIAN_POINT('Ctrl Pts',(1.81870252352016,3.48723531338816,40.1209931838938));
#27930=CARTESIAN_POINT('Ctrl Pts',(1.92157118512904,3.43358608193511,40.1151422424538));
#27931=CARTESIAN_POINT('Ctrl Pts',(2.02208234608012,3.37537168716856,40.1092913010138));
#27932=CARTESIAN_POINT('Ctrl Pts',(2.11981313868685,3.31283583309687,40.1034403595737));
#27933=CARTESIAN_POINT('Ctrl Pts',(2.21755272678131,3.25029435097978,40.097588891566));
#27934=CARTESIAN_POINT('Ctrl Pts',(2.31251110087847,3.18343085924278,40.0917374235582));
#27935=CARTESIAN_POINT('Ctrl Pts',(2.40429388921138,3.11253271377199,40.0858859555504));
#27936=CARTESIAN_POINT('Ctrl Pts',(2.49610716553233,3.04161101767858,40.0800325438287));
#27937=CARTESIAN_POINT('Ctrl Pts',(2.5847424316022,2.96665225549757,40.0741791321069));
#27938=CARTESIAN_POINT('Ctrl Pts',(2.66983850645237,2.88798395935022,40.0683257203852));
#27939=CARTESIAN_POINT('Ctrl Pts',(2.75503141718546,2.80922614187151,40.0624656477182));
#27940=CARTESIAN_POINT('Ctrl Pts',(2.83667679426988,2.72675064561217,40.0566055750513));
#27941=CARTESIAN_POINT('Ctrl Pts',(2.91445037436277,2.64092181167423,40.0507455023844));
#27942=CARTESIAN_POINT('Ctrl Pts',(2.99227633610857,2.55503517075115,40.0448814828721));
#27943=CARTESIAN_POINT('Ctrl Pts',(3.06622504527783,2.46579101252098,40.0390174633598));
#27944=CARTESIAN_POINT('Ctrl Pts',(3.13601367904373,2.37358530599821,40.0331534438475));
#27945=CARTESIAN_POINT('Ctrl Pts',(3.20590527171927,2.28124356874244,40.0272807731692));
#27946=CARTESIAN_POINT('Ctrl Pts',(3.27162430620553,2.18593190221344,40.0214081024909));
#27947=CARTESIAN_POINT('Ctrl Pts',(3.33293221062449,2.08807372460403,40.0155354318126));
#27948=CARTESIAN_POINT('Ctrl Pts',(3.34986100144671,2.06105240272565,40.0139138266636));
#27949=CARTESIAN_POINT('Ctrl Pts',(3.36645373589272,2.03383705125486,40.0122922215146));
#27950=CARTESIAN_POINT('Ctrl Pts',(3.38270602987505,2.00643687053617,40.0106706163656));
#27951=CARTESIAN_POINT('Ctrl Pts',(3.44369369945361,1.90361611367065,40.0045854496118));
#27952=CARTESIAN_POINT('Ctrl Pts',(3.50007586451126,1.7978671486112,39.998500282858));
#27953=CARTESIAN_POINT('Ctrl Pts',(3.55157138761894,1.68962412348028,39.9924151161042));
#27954=CARTESIAN_POINT('Ctrl Pts',(3.60298325692126,1.58155693773127,39.9863398346244));
#27955=CARTESIAN_POINT('Ctrl Pts',(3.64952413097963,1.47100409189806,39.9802645531446));
#27956=CARTESIAN_POINT('Ctrl Pts',(3.69095737696613,1.35842653147651,39.9741892716648));
#27957=CARTESIAN_POINT('Ctrl Pts',(3.73230921499947,1.24607016320508,39.968125926885));
#27958=CARTESIAN_POINT('Ctrl Pts',(3.76857329834686,1.13169735592075,39.9620625821053));
#27959=CARTESIAN_POINT('Ctrl Pts',(3.79956034111828,1.01579043813237,39.9559992373255));
#27960=CARTESIAN_POINT('Ctrl Pts',(3.8305116112623,0.900017327723231,39.9499428923029));
#27961=CARTESIAN_POINT('Ctrl Pts',(3.85619787215542,0.782713989463498,39.9438865472803));
#27962=CARTESIAN_POINT('Ctrl Pts',(3.876478819681,0.664380132578184,39.9378302022577));
#27963=CARTESIAN_POINT('Ctrl Pts',(3.8967330581697,0.54620211571679,39.9317818331515));
#27964=CARTESIAN_POINT('Ctrl Pts',(3.91159610689816,0.426996649940712,39.9257334640453));
#27965=CARTESIAN_POINT('Ctrl Pts',(3.92097831272722,0.307275236754875,39.9196850949391));
#27966=CARTESIAN_POINT('Ctrl Pts',(3.92900397987927,0.204863902926982,39.9145112373044));
#27967=CARTESIAN_POINT('Ctrl Pts',(3.93301993290991,0.102075387700563,39.9093373796697));
#27968=CARTESIAN_POINT('Ctrl Pts',(3.93299992557071,-0.000765154113278074,
39.904163522035));
#27969=CARTESIAN_POINT('',(3.93299854544019,-0.00338253830022365,38.654163522061));
#27970=CARTESIAN_POINT('Ctrl Pts',(3.93299992557056,-0.000765154855056982,
39.9041635219977));
#27971=CARTESIAN_POINT('Ctrl Pts',(3.93297584444362,-0.124545419536255,
39.897936197091));
#27972=CARTESIAN_POINT('Ctrl Pts',(3.92710405386225,-0.248177403224034,
39.8917088721844));
#27973=CARTESIAN_POINT('Ctrl Pts',(3.91545184109601,-0.371114375978427,
39.8854815472778));
#27974=CARTESIAN_POINT('Ctrl Pts',(3.90376045750328,-0.494464621552789,
39.879233288196));
#27975=CARTESIAN_POINT('Ctrl Pts',(3.88624980653845,-0.617114855074719,
39.8729850291141));
#27976=CARTESIAN_POINT('Ctrl Pts',(3.86303883359203,-0.738525537919935,
39.8667367700323));
#27977=CARTESIAN_POINT('Ctrl Pts',(3.83978886561927,-0.860140193807824,
39.8604780137159));
#27978=CARTESIAN_POINT('Ctrl Pts',(3.81081953373273,-0.980510824637065,
39.8542192573995));
#27979=CARTESIAN_POINT('Ctrl Pts',(3.77629983507415,-1.09911262189958,39.8479605010831));
#27980=CARTESIAN_POINT('Ctrl Pts',(3.74167620520879,-1.21807150304158,39.8416829010305));
#27981=CARTESIAN_POINT('Ctrl Pts',(3.7014688820161,-1.33525058575408,39.8354053009779));
#27982=CARTESIAN_POINT('Ctrl Pts',(3.655896061848,-1.45014240161587,39.8291277009252));
#27983=CARTESIAN_POINT('Ctrl Pts',(3.61381456675723,-1.55623237733661,39.8233310266176));
#27984=CARTESIAN_POINT('Ctrl Pts',(3.56715880258182,-1.66037218740392,39.8175343523099));
#27985=CARTESIAN_POINT('Ctrl Pts',(3.51613468984839,-1.76218212533346,39.8117376780022));
#27986=CARTESIAN_POINT('Ctrl Pts',(3.4644459897974,-1.86531813421112,39.8058655022106));
#27987=CARTESIAN_POINT('Ctrl Pts',(3.40812898834692,-1.9663508802791,39.7999933264189));
#27988=CARTESIAN_POINT('Ctrl Pts',(3.34737823258863,-2.06483606322435,39.7941211506273));
#27989=CARTESIAN_POINT('Ctrl Pts',(3.28670623631199,-2.16319356640888,39.7882565877372));
#27990=CARTESIAN_POINT('Ctrl Pts',(3.22161213161076,-2.25900972585437,39.7823920248471));
#27991=CARTESIAN_POINT('Ctrl Pts',(3.15233736284497,-2.35186269812071,39.776527461957));
#27992=CARTESIAN_POINT('Ctrl Pts',(3.08313387225576,-2.44462013213162,39.7706689332314));
#27993=CARTESIAN_POINT('Ctrl Pts',(3.00975851934864,-2.53442011398401,39.7648104045057));
#27994=CARTESIAN_POINT('Ctrl Pts',(2.93249689180978,-2.62086836363942,39.7589518757801));
#27995=CARTESIAN_POINT('Ctrl Pts',(2.85218971538898,-2.71072428639816,39.7528624117742));
#27996=CARTESIAN_POINT('Ctrl Pts',(2.76768381859389,-2.79695841363815,39.7467729477683));
#27997=CARTESIAN_POINT('Ctrl Pts',(2.6793474830879,-2.87916412607384,39.7406834837624));
#27998=CARTESIAN_POINT('Ctrl Pts',(2.59445970586742,-2.95816061334627,39.7348317460719));
#27999=CARTESIAN_POINT('Ctrl Pts',(2.50603528321026,-3.03343700738436,39.7289800083814));
#28000=CARTESIAN_POINT('Ctrl Pts',(2.41443914510351,-3.10466948556394,39.7231282706908));
#28001=CARTESIAN_POINT('Ctrl Pts',(2.32285697544311,-3.17589110076315,39.7172774253926));
#28002=CARTESIAN_POINT('Ctrl Pts',(2.2281043783036,-3.24306977257902,39.7114265800943));
#28003=CARTESIAN_POINT('Ctrl Pts',(2.13057887950191,-3.30592235816578,39.705575734796));
#28004=CARTESIAN_POINT('Ctrl Pts',(2.03304463285899,-3.36878058150313,39.6997243646886));
#28005=CARTESIAN_POINT('Ctrl Pts',(1.93273733762553,-3.42731172325869,39.6938729945813));
#28006=CARTESIAN_POINT('Ctrl Pts',(1.83008235984536,-3.48127671353238,39.6880216244739));
#28007=CARTESIAN_POINT('Ctrl Pts',(1.72739331125911,-3.53525961458604,39.6821683123186));
#28008=CARTESIAN_POINT('Ctrl Pts',(1.62235539649211,-3.58467315844459,39.6763150001632));
#28009=CARTESIAN_POINT('Ctrl Pts',(1.5154167078962,-3.62932517163026,39.6704616880078));
#28010=CARTESIAN_POINT('Ctrl Pts',(1.40835636163583,-3.67402798270499,39.664601716894));
#28011=CARTESIAN_POINT('Ctrl Pts',(1.29939130717468,-3.71395829172389,39.6587417457802));
#28012=CARTESIAN_POINT('Ctrl Pts',(1.18898775042528,-3.74897280989588,39.6528817746663));
#28013=CARTESIAN_POINT('Ctrl Pts',(1.07850985814193,-3.78401090360277,39.6470178579905));
#28014=CARTESIAN_POINT('Ctrl Pts',(0.966591933218341,-3.81412650876455,
39.6411539413146));
#28015=CARTESIAN_POINT('Ctrl Pts',(0.853711702038665,-3.83922717871738,
39.6352900246387));
#28016=CARTESIAN_POINT('Ctrl Pts',(0.740664957332911,-3.86436487553503,
39.6294174578969));
#28017=CARTESIAN_POINT('Ctrl Pts',(0.626653478846901,-3.88447280116349,
39.6235448911551));
#28018=CARTESIAN_POINT('Ctrl Pts',(0.51216154411238,-3.89951016830735,39.6176723244133));
#28019=CARTESIAN_POINT('Ctrl Pts',(0.480528629986609,-3.90366483426389,
39.6160497961551));
#28020=CARTESIAN_POINT('Ctrl Pts',(0.448859045477699,-3.90743274129828,
39.614427267897));
#28021=CARTESIAN_POINT('Ctrl Pts',(0.417162998552484,-3.91081373024064,
39.6128047396388));
#28022=CARTESIAN_POINT('Ctrl Pts',(0.302450944877489,-3.92304996228389,
39.6069326020476));
#28023=CARTESIAN_POINT('Ctrl Pts',(0.187007763857721,-3.93025532372492,
39.6010604644563));
#28024=CARTESIAN_POINT('Ctrl Pts',(0.0713124254032304,-3.93235343502884,
39.5951883268651));
#28025=CARTESIAN_POINT('Ctrl Pts',(-0.0442329189806668,-3.93444882622096,
39.5893238022498));
#28026=CARTESIAN_POINT('Ctrl Pts',(-0.160029361168823,-3.93145012727812,
39.5834592776345));
#28027=CARTESIAN_POINT('Ctrl Pts',(-0.275591486117182,-3.9233325544465,
39.5775947530191));
#28028=CARTESIAN_POINT('Ctrl Pts',(-0.391034705595154,-3.91522333403845,
39.5717362625959));
#28029=CARTESIAN_POINT('Ctrl Pts',(-0.506243677474003,-3.90200574478828,
39.5658777721726));
#28030=CARTESIAN_POINT('Ctrl Pts',(-0.620732326585401,-3.88370704079644,
39.5600192817493));
#28031=CARTESIAN_POINT('Ctrl Pts',(-0.739735021830795,-3.86468685747323,
39.5539298033963));
#28032=CARTESIAN_POINT('Ctrl Pts',(-0.85795896923823,-3.84017663347876,
39.5478403250432));
#28033=CARTESIAN_POINT('Ctrl Pts',(-0.974863013293591,-3.81026653993026,
39.5417508466901));
#28034=CARTESIAN_POINT('Ctrl Pts',(-1.0872022489953,-3.78152436016946,39.5358991471228));
#28035=CARTESIAN_POINT('Ctrl Pts',(-1.19832228676465,-3.74779621277451,
39.5300474475556));
#28036=CARTESIAN_POINT('Ctrl Pts',(-1.30775346440781,-3.70921418582553,
39.5241957479884));
#28037=CARTESIAN_POINT('Ctrl Pts',(-1.41716795611689,-3.67063804181752,
39.5183449406812));
#28038=CARTESIAN_POINT('Ctrl Pts',(-1.52489370994096,-3.62720962725778,
39.5124941333741));
#28039=CARTESIAN_POINT('Ctrl Pts',(-1.63047768019904,-3.57911043897401,
39.5066433260669));
#28040=CARTESIAN_POINT('Ctrl Pts',(-1.73607112432105,-3.53100693483469,
39.5007919937771));
#28041=CARTESIAN_POINT('Ctrl Pts',(-1.8395220266095,-3.4782319952331,39.4949406614873));
#28042=CARTESIAN_POINT('Ctrl Pts',(-1.94039938280693,-3.42101435764343,
39.4890893291975));
#28043=CARTESIAN_POINT('Ctrl Pts',(-2.04131022375093,-3.36377772750513,
39.4832360546445));
#28044=CARTESIAN_POINT('Ctrl Pts',(-2.13964546057822,-3.30209567091129,
39.4773827800915));
#28045=CARTESIAN_POINT('Ctrl Pts',(-2.23500126961058,-3.2362413885307,39.4715295055385));
#28046=CARTESIAN_POINT('Ctrl Pts',(-2.33046556821409,-3.17031218147665,
39.4656695715145));
#28047=CARTESIAN_POINT('Ctrl Pts',(-2.42294333270254,-3.10020150904889,
39.4598096374905));
#28048=CARTESIAN_POINT('Ctrl Pts',(-2.51206208548798,-3.02622422808585,
39.4539497034664));
#28049=CARTESIAN_POINT('Ctrl Pts',(-2.60124084681026,-2.95219713416817,
39.4480858236279));
#28050=CARTESIAN_POINT('Ctrl Pts',(-2.68705578737379,-2.87429852462632,
39.4422219437894));
#28051=CARTESIAN_POINT('Ctrl Pts',(-2.76917098541532,-2.79288042234786,
39.4363580639509));
#28052=CARTESIAN_POINT('Ctrl Pts',(-2.85140732442288,-2.7113422074983,39.4304855333865));
#28053=CARTESIAN_POINT('Ctrl Pts',(-2.92993274825609,-2.6262744399724,39.4246130028221));
#28054=CARTESIAN_POINT('Ctrl Pts',(-3.00445126377738,-2.53806256888724,
39.4187404722577));
#28055=CARTESIAN_POINT('Ctrl Pts',(-3.02504466499175,-2.51368497037473,
39.4171175819302));
#28056=CARTESIAN_POINT('Ctrl Pts',(-3.04533231008813,-2.48906742438508,
39.4154946916027));
#28057=CARTESIAN_POINT('Ctrl Pts',(-3.06530854553996,-2.46421844012248,
39.4138718012753));
#28058=CARTESIAN_POINT('Ctrl Pts',(-3.13758853511927,-2.37430738916955,
39.4079996990846));
#28059=CARTESIAN_POINT('Ctrl Pts',(-3.2060304752323,-2.28106274119832,39.402127596894));
#28060=CARTESIAN_POINT('Ctrl Pts',(-3.27031128522053,-2.18484624121681,
39.3962554947034));
#28061=CARTESIAN_POINT('Ctrl Pts',(-3.33450875013576,-2.08875449341588,
39.3903910061502));
#28062=CARTESIAN_POINT('Ctrl Pts',(-3.39455558654056,-1.98969889687443,
39.3845265175971));
#28063=CARTESIAN_POINT('Ctrl Pts',(-3.45016864544456,-1.88807450011679,
39.378662029044));
#28064=CARTESIAN_POINT('Ctrl Pts',(-3.50572447615461,-1.78655467916926,
39.3728035752981));
#28065=CARTESIAN_POINT('Ctrl Pts',(-3.55685540721134,-1.68247167634076,
39.3669451215521));
#28066=CARTESIAN_POINT('Ctrl Pts',(-3.60332171931176,-1.5762492147932,39.3610866678062));
#28067=CARTESIAN_POINT('Ctrl Pts',(-3.65162050975432,-1.46583768913797,
39.3549971759356));
#28068=CARTESIAN_POINT('Ctrl Pts',(-3.69487894392114,-1.35311486465532,
39.348907684065));
#28069=CARTESIAN_POINT('Ctrl Pts',(-3.73288047496086,-1.23858482134087,
39.3428181921944));
#28070=CARTESIAN_POINT('Ctrl Pts',(-3.76939782383343,-1.12852784643285,
39.3369665306163));
#28071=CARTESIAN_POINT('Ctrl Pts',(-3.80106104610488,-1.01680259758531,
39.3311148690381));
#28072=CARTESIAN_POINT('Ctrl Pts',(-3.82772750277615,-0.903875635522399,
39.32526320746));
#28073=CARTESIAN_POINT('Ctrl Pts',(-3.85438989143289,-0.790965900664772,
39.3194124385631));
#28074=CARTESIAN_POINT('Ctrl Pts',(-3.87605693512701,-0.676855219335641,
39.3135616696661));
#28075=CARTESIAN_POINT('Ctrl Pts',(-3.89263654801243,-0.562022868821104,
39.3077109007692));
#28076=CARTESIAN_POINT('Ctrl Pts',(-3.90921764748462,-0.447180222031505,
39.3018596072716));
#28077=CARTESIAN_POINT('Ctrl Pts',(-3.92071035026978,-0.331616186621927,
39.296008313774));
#28078=CARTESIAN_POINT('Ctrl Pts',(-3.92707423075191,-0.215817020098731,
39.2901570202764));
#28079=CARTESIAN_POINT('Ctrl Pts',(-3.93344022327085,-0.0999794222908921,
39.2843037848587));
#28080=CARTESIAN_POINT('Ctrl Pts',(-3.9346739862053,0.0160930492229305,
39.2784505494411));
#28081=CARTESIAN_POINT('Ctrl Pts',(-3.93078719408863,0.131912981881411,
39.2725973140234));
#28082=CARTESIAN_POINT('Ctrl Pts',(-3.92689598001484,0.247864681498345,
39.2667374194495));
#28083=CARTESIAN_POINT('Ctrl Pts',(-3.91787259703238,0.36356285536572,39.2608775248756));
#28084=CARTESIAN_POINT('Ctrl Pts',(-3.90378070873002,0.478523957756888,
39.2550176303017));
#28085=CARTESIAN_POINT('Ctrl Pts',(-3.88967933208241,0.593562465716907,
39.2491537901456));
#28086=CARTESIAN_POINT('Ctrl Pts',(-3.87050272295229,0.707862507278183,
39.2432899499895));
#28087=CARTESIAN_POINT('Ctrl Pts',(-3.84636557089953,0.820951213531456,
39.2374261098335));
#28088=CARTESIAN_POINT('Ctrl Pts',(-3.8221928102654,0.934206755059616,39.231553618987));
#28089=CARTESIAN_POINT('Ctrl Pts',(-3.7930450048547,1.04624699608982,39.2256811281406));
#28090=CARTESIAN_POINT('Ctrl Pts',(-3.75908654585292,1.15661460339541,39.2198086372942));
#28091=CARTESIAN_POINT('Ctrl Pts',(-3.7496998399369,1.18712212060575,39.2181853791667));
#28092=CARTESIAN_POINT('Ctrl Pts',(-3.73994585001045,1.21750196016856,39.2165621210393));
#28093=CARTESIAN_POINT('Ctrl Pts',(-3.7298286840558,1.24774476059591,39.2149388629118));
#28094=CARTESIAN_POINT('Ctrl Pts',(-3.69322985954276,1.35714802140888,39.2090667303787));
#28095=CARTESIAN_POINT('Ctrl Pts',(-3.65175207639979,1.46512305146793,39.2031945978455));
#28096=CARTESIAN_POINT('Ctrl Pts',(-3.6055251521091,1.5712025259363,39.1973224653123));
#28097=CARTESIAN_POINT('Ctrl Pts',(-3.55935816121916,1.67714446792224,39.1914579460235));
#28098=CARTESIAN_POINT('Ctrl Pts',(-3.50845443740917,1.7811953660978,39.1855934267348));
#28099=CARTESIAN_POINT('Ctrl Pts',(-3.45299339794814,1.88290350090666,39.179728907446));
#28100=CARTESIAN_POINT('Ctrl Pts',(-3.39758942659797,1.98450698042652,39.1738704226102));
#28101=CARTESIAN_POINT('Ctrl Pts',(-3.33763766370624,2.08377213070397,39.1680119377745));
#28102=CARTESIAN_POINT('Ctrl Pts',(-3.27336512150243,2.18026828196242,39.1621534529387));
#28103=CARTESIAN_POINT('Ctrl Pts',(-3.20655836280267,2.28056920163255,39.1560639725891));
#28104=CARTESIAN_POINT('Ctrl Pts',(-3.13508326715353,2.37787785409162,39.1499744922395));
#28105=CARTESIAN_POINT('Ctrl Pts',(-3.05924697712946,2.4717396571897,39.1438850118899));
#28106=CARTESIAN_POINT('Ctrl Pts',(-2.98637200435748,2.56193626811212,39.1380333185314));
#28107=CARTESIAN_POINT('Ctrl Pts',(-2.90947032923454,2.64894981731903,39.1321816251728));
#28108=CARTESIAN_POINT('Ctrl Pts',(-2.82885746565195,2.73240817577191,39.1263299318142));
#28109=CARTESIAN_POINT('Ctrl Pts',(-2.74825689686142,2.81585380544783,39.1204791309355));
#28110=CARTESIAN_POINT('Ctrl Pts',(-2.6639465521651,2.89574502521451,39.1146283300567));
#28111=CARTESIAN_POINT('Ctrl Pts',(-2.5762799617768,2.97174537242801,39.108777529178));
#28112=CARTESIAN_POINT('Ctrl Pts',(-2.48860550841617,3.04775253624777,39.1029262035305));
#28113=CARTESIAN_POINT('Ctrl Pts',(-2.39757452333728,3.11986786295776,39.097074877883));
#28114=CARTESIAN_POINT('Ctrl Pts',(-2.30357432451143,3.18779458739921,39.0912235522355));
#28115=CARTESIAN_POINT('Ctrl Pts',(-2.20954292702009,3.25574385672014,39.085370284533));
#28116=CARTESIAN_POINT('Ctrl Pts',(-2.11254069111792,3.3195015174474,39.0795170168306));
#28117=CARTESIAN_POINT('Ctrl Pts',(-2.0129840587443,3.37881401962897,39.0736637491282));
#28118=CARTESIAN_POINT('Ctrl Pts',(-1.91331416195372,3.43819400095099,39.0678038222315));
#28119=CARTESIAN_POINT('Ctrl Pts',(-1.81108442354978,3.49311851796205,39.0619438953348));
#28120=CARTESIAN_POINT('Ctrl Pts',(-1.7067361238206,3.54337985596321,39.0560839684381));
#28121=CARTESIAN_POINT('Ctrl Pts',(-1.60231756360945,3.59367503625831,39.050220095897));
#28122=CARTESIAN_POINT('Ctrl Pts',(-1.49577798076658,3.63930062315217,39.0443562233559));
#28123=CARTESIAN_POINT('Ctrl Pts',(-1.38757724339026,3.68009760653511,39.0384923508147));
#28124=CARTESIAN_POINT('Ctrl Pts',(-1.27921688558971,3.72095477464464,39.0326198277427));
#28125=CARTESIAN_POINT('Ctrl Pts',(-1.16919087378767,3.75696899438222,39.0267473046707));
#28126=CARTESIAN_POINT('Ctrl Pts',(-1.05797285985379,3.78803147133347,39.0208747815987));
#28127=CARTESIAN_POINT('Ctrl Pts',(-1.02723623526008,3.79661601316469,39.0192518292486));
#28128=CARTESIAN_POINT('Ctrl Pts',(-0.996408618161356,3.80482265899863,
39.0176288768985));
#28129=CARTESIAN_POINT('Ctrl Pts',(-0.965500099659244,3.81264980788401,
39.0160059245485));
#28130=CARTESIAN_POINT('Ctrl Pts',(-0.853667681370461,3.84096979960727,
39.0101337994881));
#28131=CARTESIAN_POINT('Ctrl Pts',(-0.740400701736088,3.86441270439239,
39.0042616744278));
#28132=CARTESIAN_POINT('Ctrl Pts',(-0.626162532679911,3.88283523764116,
38.9983895493674));
#28133=CARTESIAN_POINT('Ctrl Pts',(-0.512072474885856,3.90123388583755,
38.9925250375931));
#28134=CARTESIAN_POINT('Ctrl Pts',(-0.397014136048743,3.9146250412806,38.9866605258187));
#28135=CARTESIAN_POINT('Ctrl Pts',(-0.281464558394382,3.92291558695415,
38.9807960140444));
#28136=CARTESIAN_POINT('Ctrl Pts',(-0.166033879338691,3.93119760179373,
38.9749375367554));
#28137=CARTESIAN_POINT('Ctrl Pts',(-0.0501133767523756,3.9343894168585,
38.9690790594664));
#28138=CARTESIAN_POINT('Ctrl Pts',(0.0658119013823674,3.93244933770754,
38.9632205821774));
#28139=CARTESIAN_POINT('Ctrl Pts',(0.186308234291358,3.93043275920968,38.957131099011));
#28140=CARTESIAN_POINT('Ctrl Pts',(0.306809277858817,3.92287117607742,38.9510416158447));
#28141=CARTESIAN_POINT('Ctrl Pts',(0.426766562145073,3.90977739793903,38.9449521326783));
#28142=CARTESIAN_POINT('Ctrl Pts',(0.542039454016827,3.89719493843671,38.939100446899));
#28143=CARTESIAN_POINT('Ctrl Pts',(0.656809808134693,3.87950429503028,38.9332487611196));
#28144=CARTESIAN_POINT('Ctrl Pts',(0.770594013338357,3.8567698747277,38.9273970753402));
#28145=CARTESIAN_POINT('Ctrl Pts',(0.884360864570448,3.83403892179989,38.9215462820396));
#28146=CARTESIAN_POINT('Ctrl Pts',(0.997141460650802,3.80626580248217,38.9156954887391));
#28147=CARTESIAN_POINT('Ctrl Pts',(1.10846165954716,3.77356618456785,38.9098446954385));
#28148=CARTESIAN_POINT('Ctrl Pts',(1.21979184313737,3.74086363371164,38.90399337736));
#28149=CARTESIAN_POINT('Ctrl Pts',(1.32966097247394,3.70323382237404,38.8981420592815));
#28150=CARTESIAN_POINT('Ctrl Pts',(1.43761005149298,3.66084229923202,38.892290741203));
#28151=CARTESIAN_POINT('Ctrl Pts',(1.54559495917646,3.61843670620008,38.8864374810523));
#28152=CARTESIAN_POINT('Ctrl Pts',(1.65165816476864,3.57126640981792,38.8805842209015));
#28153=CARTESIAN_POINT('Ctrl Pts',(1.7553612982158,3.51954481612696,38.8747309607508));
#28154=CARTESIAN_POINT('Ctrl Pts',(1.85918241479537,3.46776437874021,38.8688710413416));
#28155=CARTESIAN_POINT('Ctrl Pts',(1.96063772975617,3.41142249348793,38.8630111219324));
#28156=CARTESIAN_POINT('Ctrl Pts',(2.05931401940264,3.35077823340963,38.8571512025232));
#28157=CARTESIAN_POINT('Ctrl Pts',(2.15805675097397,3.29009313959725,38.8512873374415));
#28158=CARTESIAN_POINT('Ctrl Pts',(2.25401638983479,3.22510013387591,38.8454234723598));
#28159=CARTESIAN_POINT('Ctrl Pts',(2.34681065051272,3.15610024724185,38.839559607278));
#28160=CARTESIAN_POINT('Ctrl Pts',(2.4397418053458,3.08699856895476,38.8336870915659));
#28161=CARTESIAN_POINT('Ctrl Pts',(2.52949794281579,3.01387847237749,38.8278145758537));
#28162=CARTESIAN_POINT('Ctrl Pts',(2.61573158303177,2.93707972066304,38.8219420601415));
#28163=CARTESIAN_POINT('Ctrl Pts',(2.63956452461567,2.91585435943809,38.8203190354893));
#28164=CARTESIAN_POINT('Ctrl Pts',(2.66312863247738,2.89434821298065,38.8186960108372));
#28165=CARTESIAN_POINT('Ctrl Pts',(2.68641710589835,2.87256890833566,38.817072986185));
#28166=CARTESIAN_POINT('Ctrl Pts',(2.7694231565749,2.79494191955099,38.811288112952));
#28167=CARTESIAN_POINT('Ctrl Pts',(2.84922079101553,2.71356508602149,38.8055032397191));
#28168=CARTESIAN_POINT('Ctrl Pts',(2.92544421824122,2.62873831446933,38.7997183664862));
#28169=CARTESIAN_POINT('Ctrl Pts',(3.00535585908918,2.53980704032839,38.7936535813018));
#28170=CARTESIAN_POINT('Ctrl Pts',(3.08133832905436,2.44708382391803,38.7875887961174));
#28171=CARTESIAN_POINT('Ctrl Pts',(3.15300921663704,2.35096190522132,38.781524010933));
#28172=CARTESIAN_POINT('Ctrl Pts',(3.22120142124661,2.25950544684177,38.7757535916435));
#28173=CARTESIAN_POINT('Ctrl Pts',(3.28549042961106,2.16497283811683,38.7699831723539));
#28174=CARTESIAN_POINT('Ctrl Pts',(3.34558553305421,2.06773945191805,38.7642127530643));
#28175=CARTESIAN_POINT('Ctrl Pts',(3.40564321843576,1.97056660783711,38.7584459267115));
#28176=CARTESIAN_POINT('Ctrl Pts',(3.46151196362247,1.87069668919483,38.7526791003587));
#28177=CARTESIAN_POINT('Ctrl Pts',(3.51294353285398,1.76853519472456,38.7469122740059));
#28178=CARTESIAN_POINT('Ctrl Pts',(3.56435639504785,1.66641085912284,38.741147545202));
#28179=CARTESIAN_POINT('Ctrl Pts',(3.61133509773127,1.56199698520079,38.7353828163982));
#28180=CARTESIAN_POINT('Ctrl Pts',(3.65367709697633,1.45572410539588,38.7296180875944));
#28181=CARTESIAN_POINT('Ctrl Pts',(3.69601465676428,1.34946236804761,38.7238539632086));
#28182=CARTESIAN_POINT('Ctrl Pts',(3.73371632356553,1.24134240938727,38.7180898388228));
#28183=CARTESIAN_POINT('Ctrl Pts',(3.76662783714237,1.13181435600729,38.712325714437));
#28184=CARTESIAN_POINT('Ctrl Pts',(3.79955765479451,1.02222538747881,38.7065583842744));
#28185=CARTESIAN_POINT('Ctrl Pts',(3.82769187595247,0.911227169405309,38.7007910541117));
#28186=CARTESIAN_POINT('Ctrl Pts',(3.85092633608448,0.799284276118953,38.6950237239491));
#28187=CARTESIAN_POINT('Ctrl Pts',(3.87416835248562,0.68730497696714,38.6892545181458));
#28188=CARTESIAN_POINT('Ctrl Pts',(3.89250736448081,0.574380811676093,38.6834853123425));
#28189=CARTESIAN_POINT('Ctrl Pts',(3.90589074838289,0.460984231505777,38.6777161065392));
#28190=CARTESIAN_POINT('Ctrl Pts',(3.91928825110571,0.347468023444683,38.6719408145037));
#28191=CARTESIAN_POINT('Ctrl Pts',(3.92771965890806,0.233478830777794,38.6661655224681));
#28192=CARTESIAN_POINT('Ctrl Pts',(3.93118439497244,0.119491642909193,38.6603902304326));
#28193=CARTESIAN_POINT('Ctrl Pts',(3.93242957881912,0.0785260390580603,
38.6583146609754));
#28194=CARTESIAN_POINT('Ctrl Pts',(3.93303375826257,0.0375606726600528,
38.6562390915182));
#28195=CARTESIAN_POINT('Ctrl Pts',(3.93299854544019,-0.00338253830016815,
38.654163522061));
#28196=CARTESIAN_POINT('',(3.93463686453598,0.00228919349351085,37.4041629160656));
#28197=CARTESIAN_POINT('Ctrl Pts',(3.93299854543975,-0.00338253881235497,
38.654163522035));
#28198=CARTESIAN_POINT('Ctrl Pts',(3.93284766481448,-0.178816824309476,
38.6452700807004));
#28199=CARTESIAN_POINT('Ctrl Pts',(3.92095564116745,-0.353765040641901,
38.6363766393657));
#28200=CARTESIAN_POINT('Ctrl Pts',(3.89753452592024,-0.526985407065219,
38.6274831980311));
#28201=CARTESIAN_POINT('Ctrl Pts',(3.88933271406081,-0.587645236481059,
38.6243688146279));
#28202=CARTESIAN_POINT('Ctrl Pts',(3.87971743278634,-0.648093501288501,
38.6212544312248));
#28203=CARTESIAN_POINT('Ctrl Pts',(3.8686989668374,-0.708277702593558,38.6181400478216));
#28204=CARTESIAN_POINT('Ctrl Pts',(3.84792380700203,-0.821754152715708,
38.6122679224922));
#28205=CARTESIAN_POINT('Ctrl Pts',(3.82211685794453,-0.934506005180074,
38.6063957971629));
#28206=CARTESIAN_POINT('Ctrl Pts',(3.79134061006027,-1.04605228287492,38.6005236718335));
#28207=CARTESIAN_POINT('Ctrl Pts',(3.76060426410881,-1.15745393890912,38.5946591598153));
#28208=CARTESIAN_POINT('Ctrl Pts',(3.72491154062295,-1.26765273367135,38.5887946477971));
#28209=CARTESIAN_POINT('Ctrl Pts',(3.68437623701796,-1.37617613120463,38.5829301357788));
#28210=CARTESIAN_POINT('Ctrl Pts',(3.64388264374113,-1.48458785949848,38.5770716582712));
#28211=CARTESIAN_POINT('Ctrl Pts',(3.59855652546422,-1.59132723466118,38.5712131807636));
#28212=CARTESIAN_POINT('Ctrl Pts',(3.54856177111622,-1.69593583503991,38.565354703256));
#28213=CARTESIAN_POINT('Ctrl Pts',(3.4965956741155,-1.80466925608148,38.5592652201811));
#28214=CARTESIAN_POINT('Ctrl Pts',(3.43958530973284,-1.91109996956278,38.5531757371062));
#28215=CARTESIAN_POINT('Ctrl Pts',(3.37777051633314,-2.01473455794815,38.5470862540313));
#28216=CARTESIAN_POINT('Ctrl Pts',(3.31836961932331,-2.11432216752779,38.5412345680985));
#28217=CARTESIAN_POINT('Ctrl Pts',(3.25453271403067,-2.21132754548618,38.5353828821657));
#28218=CARTESIAN_POINT('Ctrl Pts',(3.18651957414802,-2.3053377200687,38.5295311962329));
#28219=CARTESIAN_POINT('Ctrl Pts',(3.1185168076769,-2.39933355615382,38.5236804028033));
#28220=CARTESIAN_POINT('Ctrl Pts',(3.04633931535211,-2.49033476233057,38.5178296093737));
#28221=CARTESIAN_POINT('Ctrl Pts',(2.97028954486185,-2.57795830448911,38.5119788159441));
#28222=CARTESIAN_POINT('Ctrl Pts',(2.89423295352562,-2.66558970553639,38.5061274977614));
#28223=CARTESIAN_POINT('Ctrl Pts',(2.81430366461514,-2.74984252811148,38.5002761795786));
#28224=CARTESIAN_POINT('Ctrl Pts',(2.73084318317132,-2.83036826383542,38.4944248613958));
#28225=CARTESIAN_POINT('Ctrl Pts',(2.64735500126829,-2.91092072597909,38.4885716011657));
#28226=CARTESIAN_POINT('Ctrl Pts',(2.56033359374045,-2.9877433546469,38.4827183409357));
#28227=CARTESIAN_POINT('Ctrl Pts',(2.47015540294773,-3.0605263085437,38.4768650807056));
#28228=CARTESIAN_POINT('Ctrl Pts',(2.37987461694304,-3.13339206719093,38.4710051612549));
#28229=CARTESIAN_POINT('Ctrl Pts',(2.28643020112129,-3.20220871794049,38.4651452418041));
#28230=CARTESIAN_POINT('Ctrl Pts',(2.19022966268298,-3.26670828582896,38.4592853223534));
#28231=CARTESIAN_POINT('Ctrl Pts',(2.09396434968354,-3.33125128311264,38.453421457252));
#28232=CARTESIAN_POINT('Ctrl Pts',(1.99493957121781,-3.39147119521567,38.4475575921507));
#28233=CARTESIAN_POINT('Ctrl Pts',(1.89358811684596,-3.44714563715254,38.4416937270494));
#28234=CARTESIAN_POINT('Ctrl Pts',(1.79208714493666,-3.5029022121531,38.4358212113502));
#28235=CARTESIAN_POINT('Ctrl Pts',(1.68825301608693,-3.55409975161193,38.429948695651));
#28236=CARTESIAN_POINT('Ctrl Pts',(1.58253925985012,-3.60056363518728,38.4240761799519));
#28237=CARTESIAN_POINT('Ctrl Pts',(1.55332249497194,-3.61340514617008,38.422453156454));
#28238=CARTESIAN_POINT('Ctrl Pts',(1.52396224824739,-3.62588537542524,38.4208301329561));
#28239=CARTESIAN_POINT('Ctrl Pts',(1.49446828468059,-3.63800131199589,38.4192071094581));
#28240=CARTESIAN_POINT('Ctrl Pts',(1.3877586704853,-3.68183695701326,38.4133349854589));
#28241=CARTESIAN_POINT('Ctrl Pts',(1.27893984743706,-3.72104711202814,38.4074628614597));
#28242=CARTESIAN_POINT('Ctrl Pts',(1.16845029607819,-3.75542446410453,38.4015907374605));
#28243=CARTESIAN_POINT('Ctrl Pts',(1.05810399654019,-3.78975724528511,38.3957262267826));
#28244=CARTESIAN_POINT('Ctrl Pts',(0.946091667439092,-3.81926956228804,
38.3898617161047));
#28245=CARTESIAN_POINT('Ctrl Pts',(0.832872410228218,-3.84380183519919,
38.3839972054268));
#28246=CARTESIAN_POINT('Ctrl Pts',(0.719769654429791,-3.86830886466222,
38.378138729268));
#28247=CARTESIAN_POINT('Ctrl Pts',(0.605462842355839,-3.88784595571407,
38.3722802531093));
#28248=CARTESIAN_POINT('Ctrl Pts',(0.490426265947687,-3.90230330416135,
38.3664217769505));
#28249=CARTESIAN_POINT('Ctrl Pts',(0.370853646063752,-3.91733072486869,
38.3603322933732));
#28250=CARTESIAN_POINT('Ctrl Pts',(0.250492961218796,-3.92686942434437,
38.3542428097959));
#28251=CARTESIAN_POINT('Ctrl Pts',(0.129888989964001,-3.93085459541384,
38.3481533262185));
#28252=CARTESIAN_POINT('Ctrl Pts',(0.013994696325034,-3.93468414249526,
38.3423016416473));
#28253=CARTESIAN_POINT('Ctrl Pts',(-0.102123787136036,-3.9333857459539,
38.3364499570761));
#28254=CARTESIAN_POINT('Ctrl Pts',(-0.217978600778682,-3.92695484180842,
38.3305982725049));
#28255=CARTESIAN_POINT('Ctrl Pts',(-0.333815744113324,-3.92052491851175,
38.3247474804392));
#28256=CARTESIAN_POINT('Ctrl Pts',(-0.449388884926641,-3.90896406700047,
38.3188966883736));
#28257=CARTESIAN_POINT('Ctrl Pts',(-0.564212295559321,-3.89231980771617,
38.313045896308));
#28258=CARTESIAN_POINT('Ctrl Pts',(-0.679046004600494,-3.87567405562323,
38.30719457949));
#28259=CARTESIAN_POINT('Ctrl Pts',(-0.793129440627937,-3.85394404872781,
38.3013432626721));
#28260=CARTESIAN_POINT('Ctrl Pts',(-0.905984822818731,-3.82722882786255,
38.2954919458542));
#28261=CARTESIAN_POINT('Ctrl Pts',(-1.01887766162924,-3.8005047402348,38.2896386869885));
#28262=CARTESIAN_POINT('Ctrl Pts',(-1.13054123405462,-3.76879224377626,
38.2837854281227));
#28263=CARTESIAN_POINT('Ctrl Pts',(-1.2405114170697,-3.7322406707124,38.277932169257));
#28264=CARTESIAN_POINT('Ctrl Pts',(-1.35060671270718,-3.69564751307503,
38.2720722511629));
#28265=CARTESIAN_POINT('Ctrl Pts',(-1.4590043810232,-3.65420442067761,38.2662123330687));
#28266=CARTESIAN_POINT('Ctrl Pts',(-1.56525874125782,-3.60810948737923,
38.2603524149746));
#28267=CARTESIAN_POINT('Ctrl Pts',(-1.67158464564546,-3.56198351702078,
38.2544885512271));
#28268=CARTESIAN_POINT('Ctrl Pts',(-1.77576399764922,-3.51119964960478,
38.2486246874795));
#28269=CARTESIAN_POINT('Ctrl Pts',(-1.87737581656042,-3.4560018870646,38.242760823732));
#28270=CARTESIAN_POINT('Ctrl Pts',(-1.97913753739779,-3.40072269451939,
38.236888309372));
#28271=CARTESIAN_POINT('Ctrl Pts',(-2.07832381267025,-3.34101682339705,
38.2310157950119));
#28272=CARTESIAN_POINT('Ctrl Pts',(-2.17454264603275,-3.27717153664328,
38.2251432806519));
#28273=CARTESIAN_POINT('Ctrl Pts',(-2.20113545973998,-3.25952607413459,
38.2235202441328));
#28274=CARTESIAN_POINT('Ctrl Pts',(-2.22750180237679,-3.24156465715202,
38.2218972076138));
#28275=CARTESIAN_POINT('Ctrl Pts',(-2.25363386371177,-3.2232938755769,38.2202741710947));
#28276=CARTESIAN_POINT('Ctrl Pts',(-2.34817929855874,-3.15719044168124,
38.2144020475182));
#28277=CARTESIAN_POINT('Ctrl Pts',(-2.43997235973993,-3.08681285873257,
38.2085299239417));
#28278=CARTESIAN_POINT('Ctrl Pts',(-2.52860167352299,-3.01241806140129,
38.2026578003652));
#28279=CARTESIAN_POINT('Ctrl Pts',(-2.61711607754092,-2.93811971848587,
38.1967932901201));
#28280=CARTESIAN_POINT('Ctrl Pts',(-2.70247457756168,-2.85981478214543,
38.1909287798751));
#28281=CARTESIAN_POINT('Ctrl Pts',(-2.78429482194088,-2.77780333078373,
38.18506426963));
#28282=CARTESIAN_POINT('Ctrl Pts',(-2.86603087401856,-2.69587626847383,
38.1792057939137));
#28283=CARTESIAN_POINT('Ctrl Pts',(-2.94423562201799,-2.61025056821768,
38.1733473181973));
#28284=CARTESIAN_POINT('Ctrl Pts',(-3.01856038951325,-2.52126598653566,
38.167488842481));
#28285=CARTESIAN_POINT('Ctrl Pts',(-3.09581588821695,-2.42877261633813,
38.1613993587414));
#28286=CARTESIAN_POINT('Ctrl Pts',(-3.16887877651891,-2.3326503167294,38.1553098750019));
#28287=CARTESIAN_POINT('Ctrl Pts',(-3.2374001529709,-2.23332246877695,38.1492203912623));
#28288=CARTESIAN_POINT('Ctrl Pts',(-3.30324571012527,-2.13787345960598,
38.1433687071547));
#28289=CARTESIAN_POINT('Ctrl Pts',(-3.36489754235973,-2.03946493519753,
38.1375170230471));
#28290=CARTESIAN_POINT('Ctrl Pts',(-3.42208819548022,-1.93850493482862,
38.1316653389395));
#28291=CARTESIAN_POINT('Ctrl Pts',(-3.47927012574741,-1.83756033311708,
38.1258145473446));
#28292=CARTESIAN_POINT('Ctrl Pts',(-3.53199202610027,-1.73406538882097,
38.1199637557497));
#28293=CARTESIAN_POINT('Ctrl Pts',(-3.58003142036333,-1.62845449098564,
38.1141129641547));
#28294=CARTESIAN_POINT('Ctrl Pts',(-3.62807512318259,-1.52283412112229,
38.1082616478141));
#28295=CARTESIAN_POINT('Ctrl Pts',(-3.67143531387795,-1.41509779679653,
38.1024103314735));
#28296=CARTESIAN_POINT('Ctrl Pts',(-3.7099371617375,-1.30570105918588,38.0965590151329));
#28297=CARTESIAN_POINT('Ctrl Pts',(-3.74845178829314,-1.19626801298899,
38.0907057567506));
#28298=CARTESIAN_POINT('Ctrl Pts',(-3.78210472853592,-1.08517384746374,
38.0848524983683));
#28299=CARTESIAN_POINT('Ctrl Pts',(-3.81077084899311,-0.972889786391225,
38.0789992399861));
#28300=CARTESIAN_POINT('Ctrl Pts',(-3.8394695827467,-0.860477980325405,
38.0731393223821));
#28301=CARTESIAN_POINT('Ctrl Pts',(-3.86317007027577,-0.746873977490936,
38.0672794047782));
#28302=CARTESIAN_POINT('Ctrl Pts',(-3.88179817342039,-0.632559831818427,
38.0614194871742));
#28303=CARTESIAN_POINT('Ctrl Pts',(-3.90043881939564,-0.51816871518662,
38.0555556239214));
#28304=CARTESIAN_POINT('Ctrl Pts',(-3.91400023203977,-0.403066913178866,
38.0496917606686));
#28305=CARTESIAN_POINT('Ctrl Pts',(-3.92246024878263,-0.2877405023978,38.0438278974157));
#28306=CARTESIAN_POINT('Ctrl Pts',(-3.93093274608636,-0.172243957403642,
38.0379553835533));
#28307=CARTESIAN_POINT('Ctrl Pts',(-3.93428881547625,-0.0565225540109119,
38.0320828696908));
#28308=CARTESIAN_POINT('Ctrl Pts',(-3.9325583576423,0.0589386438399231,
38.0262103558284));
#28309=CARTESIAN_POINT('Ctrl Pts',(-3.93208009498766,0.0908497241956913,
38.024587314796));
#28310=CARTESIAN_POINT('Ctrl Pts',(-3.93121359972497,0.122740967516733,
38.0229642737637));
#28311=CARTESIAN_POINT('Ctrl Pts',(-3.92996019662631,0.154602241034456,
38.0213412327313));
#28312=CARTESIAN_POINT('Ctrl Pts',(-3.92542541377613,0.269875577192431,
38.0154691085548));
#28313=CARTESIAN_POINT('Ctrl Pts',(-3.91580694316811,0.385142477371152,
38.0095969843782));
#28314=CARTESIAN_POINT('Ctrl Pts',(-3.90109869561376,0.499917960350094,
38.0037248602017));
#28315=CARTESIAN_POINT('Ctrl Pts',(-3.88640951758781,0.61454463468791,37.9978603493481));
#28316=CARTESIAN_POINT('Ctrl Pts',(-3.86664373768413,0.72868075258105,37.9919958384945));
#28317=CARTESIAN_POINT('Ctrl Pts',(-3.84184725167496,0.84184244060131,37.9861313276409));
#28318=CARTESIAN_POINT('Ctrl Pts',(-3.81707628099344,0.954887686414946,
37.9802728513083));
#28319=CARTESIAN_POINT('Ctrl Pts',(-3.787284988556,1.06696009533074,37.9744143749757));
#28320=CARTESIAN_POINT('Ctrl Pts',(-3.75257085328802,1.17758268968817,37.9685558986431));
#28321=CARTESIAN_POINT('Ctrl Pts',(-3.71648789547975,1.2925672737496,37.9624664151316));
#28322=CARTESIAN_POINT('Ctrl Pts',(-3.67508593776599,1.40598490359337,37.9563769316202));
#28323=CARTESIAN_POINT('Ctrl Pts',(-3.62853270260561,1.51731322610778,37.9502874481087));
#28324=CARTESIAN_POINT('Ctrl Pts',(-3.58379740522979,1.62429409643563,37.9444357633694));
#28325=CARTESIAN_POINT('Ctrl Pts',(-3.53430577739931,1.72934535791776,37.9385840786302));
#28326=CARTESIAN_POINT('Ctrl Pts',(-3.48025664224282,1.83202148025746,37.9327323938909));
#28327=CARTESIAN_POINT('Ctrl Pts',(-3.42621575074423,1.93468194227577,37.9268816016597));
#28328=CARTESIAN_POINT('Ctrl Pts',(-3.36761892654977,2.0349676197157,37.9210308094285));
#28329=CARTESIAN_POINT('Ctrl Pts',(-3.30471146835246,2.13245659063431,37.9151800171973));
#28330=CARTESIAN_POINT('Ctrl Pts',(-3.24179836807022,2.22995430520701,37.9093287002164));
#28331=CARTESIAN_POINT('Ctrl Pts',(-3.17457408939415,2.32465446723433,37.9034773832355));
#28332=CARTESIAN_POINT('Ctrl Pts',(-3.10332747442117,2.41616381615625,37.8976260662546));
#28333=CARTESIAN_POINT('Ctrl Pts',(-3.03205721278336,2.50770353691974,37.8917728072288));
#28334=CARTESIAN_POINT('Ctrl Pts',(-2.95676221410921,2.59605001274159,37.8859195482029));
#28335=CARTESIAN_POINT('Ctrl Pts',(-2.87777137028209,2.68084332634056,37.8800662891771));
#28336=CARTESIAN_POINT('Ctrl Pts',(-2.79869065896901,2.76573310886619,37.8742063709278));
#28337=CARTESIAN_POINT('Ctrl Pts',(-2.71590599190624,2.84706135794204,37.8683464526786));
#28338=CARTESIAN_POINT('Ctrl Pts',(-2.62978292911757,2.92450521383051,37.8624865344294));
#28339=CARTESIAN_POINT('Ctrl Pts',(-2.54360187720603,3.00200121488346,37.8566226705295));
#28340=CARTESIAN_POINT('Ctrl Pts',(-2.45407827223948,3.07560735291503,37.8507588066296));
#28341=CARTESIAN_POINT('Ctrl Pts',(-2.36160914397724,3.14504232898114,37.8448949427297));
#28342=CARTESIAN_POINT('Ctrl Pts',(-2.26900360154762,3.2145797383093,37.8390224282226));
#28343=CARTESIAN_POINT('Ctrl Pts',(-2.17344420326544,3.27993347199441,37.8331499137154));
#28344=CARTESIAN_POINT('Ctrl Pts',(-2.07535525905765,3.34086658648647,37.8272773992083));
#28345=CARTESIAN_POINT('Ctrl Pts',(-2.04824561392128,3.35770717055305,37.8256543642614));
#28346=CARTESIAN_POINT('Ctrl Pts',(-2.02094288135367,3.37421036309901,37.8240313293146));
#28347=CARTESIAN_POINT('Ctrl Pts',(-1.99345630322199,3.39037180367353,37.8224082943678));
#28348=CARTESIAN_POINT('Ctrl Pts',(-1.89401014270797,3.44884373152909,37.8165361704145));
#28349=CARTESIAN_POINT('Ctrl Pts',(-1.79182243863938,3.5030345546936,37.8106640464611));
#28350=CARTESIAN_POINT('Ctrl Pts',(-1.68729798416966,3.55267709095789,37.8047919225078));
#28351=CARTESIAN_POINT('Ctrl Pts',(-1.58290904772492,3.60225526469091,37.7989274118794));
#28352=CARTESIAN_POINT('Ctrl Pts',(-1.47618975572388,3.64729670268684,37.7930629012511));
#28353=CARTESIAN_POINT('Ctrl Pts',(-1.36757205913616,3.68757856364716,37.7871983906227));
#28354=CARTESIAN_POINT('Ctrl Pts',(-1.25906612907142,3.72781897497561,37.7813399145171));
#28355=CARTESIAN_POINT('Ctrl Pts',(-1.14866606518523,3.76330940785714,37.7754814384116));
#28356=CARTESIAN_POINT('Ctrl Pts',(-1.03682588890287,3.79387415132616,37.769622962306));
#28357=CARTESIAN_POINT('Ctrl Pts',(-0.920575705995505,3.82564410320659,
37.7635334787101));
#28358=CARTESIAN_POINT('Ctrl Pts',(-0.802769914156219,3.85209172586888,
37.7574439951142));
#28359=CARTESIAN_POINT('Ctrl Pts',(-0.683938671629199,3.87307589564807,
37.7513545115183));
#28360=CARTESIAN_POINT('Ctrl Pts',(-0.569747881856857,3.89324061722167,
37.7455028270089));
#28361=CARTESIAN_POINT('Ctrl Pts',(-0.454610673238863,3.90836050408855,
37.7396511424996));
#28362=CARTESIAN_POINT('Ctrl Pts',(-0.339009367189832,3.91836211304641,
37.7337994579902));
#28363=CARTESIAN_POINT('Ctrl Pts',(-0.22342569284546,3.92836219654214,37.7279486659896));
#28364=CARTESIAN_POINT('Ctrl Pts',(-0.107378473573039,3.93324551867752,
37.722097873989));
#28365=CARTESIAN_POINT('Ctrl Pts',(0.00864472130136986,3.93299049945377,
37.7162470819884));
#28366=CARTESIAN_POINT('Ctrl Pts',(0.124678322130959,3.93273545735771,37.7103957652385));
#28367=CARTESIAN_POINT('Ctrl Pts',(0.240687480842907,3.92734115868281,37.7045444484887));
#28368=CARTESIAN_POINT('Ctrl Pts',(0.356185216416442,3.91683814978439,37.6986931317389));
#28369=CARTESIAN_POINT('Ctrl Pts',(0.47172128554553,3.9063316549503,37.6928398729442));
#28370=CARTESIAN_POINT('Ctrl Pts',(0.58674518252168,3.8907131157734,37.6869866141496));
#28371=CARTESIAN_POINT('Ctrl Pts',(0.700776341941089,3.87006479513918,37.681133355355));
#28372=CARTESIAN_POINT('Ctrl Pts',(0.814937234059575,3.84939298301035,37.6752734373361));
#28373=CARTESIAN_POINT('Ctrl Pts',(0.928102727263476,3.82368004145433,37.6694135193172));
#28374=CARTESIAN_POINT('Ctrl Pts',(1.03980362436883,3.79305911142305,37.6635536012984));
#28375=CARTESIAN_POINT('Ctrl Pts',(1.15157973289209,3.76241756344129,37.6576897376286));
#28376=CARTESIAN_POINT('Ctrl Pts',(1.26188888917317,3.72686157322114,37.6518258739589));
#28377=CARTESIAN_POINT('Ctrl Pts',(1.37027986241766,3.68657321894637,37.6459620102891));
#28378=CARTESIAN_POINT('Ctrl Pts',(1.47883073841939,3.64622542965834,37.64008949601));
#28379=CARTESIAN_POINT('Ctrl Pts',(1.5854574043302,3.6011315032136,37.6342169817309));
#28380=CARTESIAN_POINT('Ctrl Pts',(1.68973121106261,3.55152043980615,37.6283444674517));
#28381=CARTESIAN_POINT('Ctrl Pts',(1.7185502575496,3.53780900462016,37.6267214303026));
#28382=CARTESIAN_POINT('Ctrl Pts',(1.74718974257687,3.52375278791357,37.6250983931535));
#28383=CARTESIAN_POINT('Ctrl Pts',(1.7756410032213,3.50935721004278,37.6234753560044));
#28384=CARTESIAN_POINT('Ctrl Pts',(1.87857723493968,3.45727422651714,37.6176032320885));
#28385=CARTESIAN_POINT('Ctrl Pts',(1.97939255308003,3.40057110844653,37.6117311081726));
#28386=CARTESIAN_POINT('Ctrl Pts',(2.07764341029815,3.33944409440324,37.6058589842567));
#28387=CARTESIAN_POINT('Ctrl Pts',(2.17576688331402,3.27839633275672,37.5999944736669));
#28388=CARTESIAN_POINT('Ctrl Pts',(2.27133215960027,3.21293629767389,37.5941299630771));
#28389=CARTESIAN_POINT('Ctrl Pts',(2.36391832744339,3.14330703896028,37.5882654524874));
#28390=CARTESIAN_POINT('Ctrl Pts',(2.45640922502803,3.07374942807084,37.5824069764215));
#28391=CARTESIAN_POINT('Ctrl Pts',(2.54592678312613,3.00003137372826,37.5765485003556));
#28392=CARTESIAN_POINT('Ctrl Pts',(2.63207782173528,2.92243996351152,37.5706900242897));
#28393=CARTESIAN_POINT('Ctrl Pts',(2.72162591098664,2.84178902024491,37.5646005406793));
#28394=CARTESIAN_POINT('Ctrl Pts',(2.8075361396623,2.75695321399475,37.5585110570689));
#28395=CARTESIAN_POINT('Ctrl Pts',(2.88940329059112,2.66830238622259,37.5524215734586));
#28396=CARTESIAN_POINT('Ctrl Pts',(2.96807346463353,2.583113443274,37.5465698889915));
#28397=CARTESIAN_POINT('Ctrl Pts',(3.0430100991615,2.49440217895448,37.5407182045244));
#28398=CARTESIAN_POINT('Ctrl Pts',(3.11389077470868,2.4025347537932,37.5348665200573));
#28399=CARTESIAN_POINT('Ctrl Pts',(3.18476063940591,2.31068134041921,37.5290157280998));
#28400=CARTESIAN_POINT('Ctrl Pts',(3.25157552266725,2.21567305056715,37.5231649361423));
#28401=CARTESIAN_POINT('Ctrl Pts',(3.31405380919675,2.11790848474349,37.5173141441848));
#28402=CARTESIAN_POINT('Ctrl Pts',(3.3765376993061,2.02013515056877,37.5114628274789));
#28403=CARTESIAN_POINT('Ctrl Pts',(3.43468399686684,1.91960539737308,37.505611510773));
#28404=CARTESIAN_POINT('Ctrl Pts',(3.48825526576596,1.81674549699621,37.4997601940671));
#28405=CARTESIAN_POINT('Ctrl Pts',(3.54184431489582,1.71385145755939,37.4939069353172));
#28406=CARTESIAN_POINT('Ctrl Pts',(3.59085512516964,1.60862609961033,37.4880536765674));
#28407=CARTESIAN_POINT('Ctrl Pts',(3.63509724358918,1.501518241531,37.4822004178175));
#28408=CARTESIAN_POINT('Ctrl Pts',(3.67938969604625,1.39428852737559,37.4763404998443));
#28409=CARTESIAN_POINT('Ctrl Pts',(3.71890246993564,1.28517242061843,37.4704805818711));
#28410=CARTESIAN_POINT('Ctrl Pts',(3.75349406598325,1.17463666579437,37.464620663898));
#28411=CARTESIAN_POINT('Ctrl Pts',(3.78810895354121,1.06402648408717,37.4587568002745));
#28412=CARTESIAN_POINT('Ctrl Pts',(3.81779595965542,0.951995149594837,37.4528929366511));
#28413=CARTESIAN_POINT('Ctrl Pts',(3.84246447098273,0.839020732303683,37.4470290730277));
#28414=CARTESIAN_POINT('Ctrl Pts',(3.86716937429586,0.725879650581997,37.4411565587954));
#28415=CARTESIAN_POINT('Ctrl Pts',(3.88684093685391,0.611793115212634,37.4352840445631));
#28416=CARTESIAN_POINT('Ctrl Pts',(3.90144022942924,0.497245549191858,37.4294115303309));
#28417=CARTESIAN_POINT('Ctrl Pts',(3.9054751622212,0.465587047384892,37.4277884927676));
#28418=CARTESIAN_POINT('Ctrl Pts',(3.90912295559818,0.433893334164532,37.4261654552043));
#28419=CARTESIAN_POINT('Ctrl Pts',(3.9123834894837,0.402174627761775,37.424542417641));
#28420=CARTESIAN_POINT('Ctrl Pts',(3.92602993472042,0.269421034300653,37.417749452439));
#28421=CARTESIAN_POINT('Ctrl Pts',(3.93292115709448,0.135961246390276,37.410956487237));
#28422=CARTESIAN_POINT('Ctrl Pts',(3.93299932738369,0.00230017378215415,
37.404163522035));
#28423=CARTESIAN_POINT('',(3.93121085245411,0.00231623353798856,36.1541640353064));
#28424=CARTESIAN_POINT('Ctrl Pts',(3.9378436511043,0.00226769081060172,
37.4041617293967));
#28425=CARTESIAN_POINT('Ctrl Pts',(3.92969352726255,-1.17026837568043,37.3446443126903));
#28426=CARTESIAN_POINT('Ctrl Pts',(2.75095850512379,-3.66336727924014,37.2188159165294));
#28427=CARTESIAN_POINT('Ctrl Pts',(-1.49285278529501,-4.40632793330521,
37.026676540914));
#28428=CARTESIAN_POINT('Ctrl Pts',(-4.51432818846032,-1.12480055766829,
36.8277436025506));
#28429=CARTESIAN_POINT('Ctrl Pts',(-3.38576122948677,3.19076106622442,36.6288106641873));
#28430=CARTESIAN_POINT('Ctrl Pts',(0.855351370873146,4.57304158308359,36.4298777258236));
#28431=CARTESIAN_POINT('Ctrl Pts',(3.60300821559048,2.32885918759836,36.2716625040733));
#28432=CARTESIAN_POINT('Ctrl Pts',(3.93054449524549,0.509825557930273,36.1797582617771));
#28433=CARTESIAN_POINT('Ctrl Pts',(3.92785313095816,0.00233337176097839,
36.1541649989355));
#28434=CARTESIAN_POINT('',(3.93198289809596,-0.0031156214140876,34.9041631193534));
#28435=CARTESIAN_POINT('Ctrl Pts',(3.93299932332396,0.0023071049629667,
36.154163522035));
#28436=CARTESIAN_POINT('Ctrl Pts',(3.93306815257745,-0.11502843536642,36.1482539137099));
#28437=CARTESIAN_POINT('Ctrl Pts',(3.92788182847184,-0.232374625365518,
36.1423443053847));
#28438=CARTESIAN_POINT('Ctrl Pts',(3.91746406086123,-0.349233921406056,
36.1364346970596));
#28439=CARTESIAN_POINT('Ctrl Pts',(3.90704445346722,-0.466113854861418,
36.1305240450945));
#28440=CARTESIAN_POINT('Ctrl Pts',(3.89139159917373,-0.582506322944185,
36.1246133931293));
#28441=CARTESIAN_POINT('Ctrl Pts',(3.87058107839869,-0.697919132523272,
36.1187027411642));
#28442=CARTESIAN_POINT('Ctrl Pts',(3.84976222824505,-0.813378135899996,
36.1127897234698));
#28443=CARTESIAN_POINT('Ctrl Pts',(3.82378167424935,-0.927856305137044,
36.1068767057753));
#28444=CARTESIAN_POINT('Ctrl Pts',(3.79276595892408,-1.04087241332774,36.1009636880809));
#28445=CARTESIAN_POINT('Ctrl Pts',(3.76170851327563,-1.15404057987561,36.0950427146732));
#28446=CARTESIAN_POINT('Ctrl Pts',(3.72560248091587,-1.26574236800933,36.0891217412655));
#28447=CARTESIAN_POINT('Ctrl Pts',(3.68462423432077,-1.37551199626033,36.0832007678578));
#28448=CARTESIAN_POINT('Ctrl Pts',(3.64361753378841,-1.48535784490568,36.0772756831222));
#28449=CARTESIAN_POINT('Ctrl Pts',(3.59773203505403,-1.59326849094606,36.0713505983866));
#28450=CARTESIAN_POINT('Ctrl Pts',(3.54719143757431,-1.69880013692002,36.0654255136511));
#28451=CARTESIAN_POINT('Ctrl Pts',(3.49655766018267,-1.80452634785695,36.0594895050464));
#28452=CARTESIAN_POINT('Ctrl Pts',(3.4412518234525,-1.90786443959993,36.0535534964416));
#28453=CARTESIAN_POINT('Ctrl Pts',(3.38154295267334,-2.00839643975617,36.0476174878369));
#28454=CARTESIAN_POINT('Ctrl Pts',(3.32921850769105,-2.09649526062636,36.0424156082569));
#28455=CARTESIAN_POINT('Ctrl Pts',(3.27351353645545,-2.18243944889097,36.0372137286769));
#28456=CARTESIAN_POINT('Ctrl Pts',(3.21463464360123,-2.26596847024816,36.0320118490969));
#28457=CARTESIAN_POINT('Ctrl Pts',(3.14816940685497,-2.36025992021537,36.026139725131));
#28458=CARTESIAN_POINT('Ctrl Pts',(3.07744059861696,-2.45178263820824,36.0202676011652));
#28459=CARTESIAN_POINT('Ctrl Pts',(3.00270672808036,-2.54012623803246,36.0143954771994));
#28460=CARTESIAN_POINT('Ctrl Pts',(2.92806975149084,-2.62835529862533,36.0085309665588));
#28461=CARTESIAN_POINT('Ctrl Pts',(2.84943830341971,-2.71341312508545,36.0026664559183));
#28462=CARTESIAN_POINT('Ctrl Pts',(2.7671139252641,-2.79491851842044,35.9968019452778));
#28463=CARTESIAN_POINT('Ctrl Pts',(2.68487425807463,-2.87634004351652,35.9909434691604));
#28464=CARTESIAN_POINT('Ctrl Pts',(2.59894951117365,-2.95421611717767,35.985084993043));
#28465=CARTESIAN_POINT('Ctrl Pts',(2.50968077474067,-3.02819936742894,35.9792265169256));
#28466=CARTESIAN_POINT('Ctrl Pts',(2.41689205377746,-3.1050998752419,35.9731370333342));
#28467=CARTESIAN_POINT('Ctrl Pts',(2.32049049587995,-3.17779389798758,35.9670475497429));
#28468=CARTESIAN_POINT('Ctrl Pts',(2.22090081590631,-3.24593415920698,35.9609580661516));
#28469=CARTESIAN_POINT('Ctrl Pts',(2.12520019040444,-3.31141349022082,35.9551063816313));
#28470=CARTESIAN_POINT('Ctrl Pts',(2.02655614087375,-3.37268778603635,35.9492546971111));
#28471=CARTESIAN_POINT('Ctrl Pts',(1.92537772850614,-3.42949115796681,35.9434030125909));
#28472=CARTESIAN_POINT('Ctrl Pts',(1.8242147480458,-3.48628586614828,35.9375522205798));
#28473=CARTESIAN_POINT('Ctrl Pts',(1.72051853370941,-3.53861080397351,35.9317014285687));
#28474=CARTESIAN_POINT('Ctrl Pts',(1.61472432391119,-3.58624516141459,35.9258506365576));
#28475=CARTESIAN_POINT('Ctrl Pts',(1.50892062558798,-3.63388379111019,35.9199993197976));
#28476=CARTESIAN_POINT('Ctrl Pts',(1.40101893473241,-3.67683083438635,35.9141480030377));
#28477=CARTESIAN_POINT('Ctrl Pts',(1.29147545916237,-3.71491320738202,35.9082966862778));
#28478=CARTESIAN_POINT('Ctrl Pts',(1.18189562625586,-3.75300821986755,35.9024434274734));
#28479=CARTESIAN_POINT('Ctrl Pts',(1.07067331540675,-3.78623521590995,35.8965901686691));
#28480=CARTESIAN_POINT('Ctrl Pts',(0.958280226486698,-3.81447086861659,
35.8907369098648));
#28481=CARTESIAN_POINT('Ctrl Pts',(0.845759268505086,-3.84273864488571,
35.8848769918369));
#28482=CARTESIAN_POINT('Ctrl Pts',(0.732065275031789,-3.86600364264212,
35.8790170738089));
#28483=CARTESIAN_POINT('Ctrl Pts',(0.617680580600549,-3.88419357143139,
35.873157155781));
#28484=CARTESIAN_POINT('Ctrl Pts',(0.503218867680946,-3.90239574802031,
35.8672932921026));
#28485=CARTESIAN_POINT('Ctrl Pts',(0.388065937513293,-3.91551600466352,
35.8614294284241));
#28486=CARTESIAN_POINT('Ctrl Pts',(0.272707948110416,-3.92353404152907,
35.8555655647457));
#28487=CARTESIAN_POINT('Ctrl Pts',(0.1571797779379,-3.93156390692675,35.8496930504585));
#28488=CARTESIAN_POINT('Ctrl Pts',(0.0414463565074991,-3.93447651968868,
35.8438205361713));
#28489=CARTESIAN_POINT('Ctrl Pts',(-0.0740073703216252,-3.93230363898035,
35.8379480218841));
#28490=CARTESIAN_POINT('Ctrl Pts',(-0.105916305245342,-3.93170310133619,
35.8363249848339));
#28491=CARTESIAN_POINT('Ctrl Pts',(-0.137803915726344,-3.93071441185742,
35.8347019477837));
#28492=CARTESIAN_POINT('Ctrl Pts',(-0.169660074222265,-3.929338934123,35.8330789107334));
#28493=CARTESIAN_POINT('Ctrl Pts',(-0.284915182996696,-3.92436247608846,
35.8272067867675));
#28494=CARTESIAN_POINT('Ctrl Pts',(-0.400144376111135,-3.91430239267515,
35.8213346628015));
#28495=CARTESIAN_POINT('Ctrl Pts',(-0.514862652605059,-3.89915445307729,
35.8154625388356));
#28496=CARTESIAN_POINT('Ctrl Pts',(-0.62943219457563,-3.8840261530839,35.8095980281949));
#28497=CARTESIAN_POINT('Ctrl Pts',(-0.743491731159177,-3.86382316858314,
35.8037335175543));
#28498=CARTESIAN_POINT('Ctrl Pts',(-0.856557568373406,-3.83859324910341,
35.7978690069137));
#28499=CARTESIAN_POINT('Ctrl Pts',(-0.969507061966085,-3.81338929095979,
35.7920105307961));
#28500=CARTESIAN_POINT('Ctrl Pts',(-1.08146448894426,-3.78316877600975,
35.7861520546786));
#28501=CARTESIAN_POINT('Ctrl Pts',(-1.19195324869756,-3.7480310101331,35.7802935785611));
#28502=CARTESIAN_POINT('Ctrl Pts',(-1.30679872660717,-3.71150771560258,
35.7742040949698));
#28503=CARTESIAN_POINT('Ctrl Pts',(-1.4200568803427,-3.66967146433403,35.7681146113785));
#28504=CARTESIAN_POINT('Ctrl Pts',(-1.5312060032593,-3.62269197912032,35.7620251277872));
#28505=CARTESIAN_POINT('Ctrl Pts',(-1.63801466646809,-3.57754707934744,
35.7561734432669));
#28506=CARTESIAN_POINT('Ctrl Pts',(-1.74287550973644,-3.52765327827911,
35.7503217587465));
#28507=CARTESIAN_POINT('Ctrl Pts',(-1.84534376791724,-3.47321110475724,
35.7444700742262));
#28508=CARTESIAN_POINT('Ctrl Pts',(-1.94779639746115,-3.41877723485033,
35.738619282215));
#28509=CARTESIAN_POINT('Ctrl Pts',(-2.0478568025135,-3.35979656575146,35.7327684902038));
#28510=CARTESIAN_POINT('Ctrl Pts',(-2.14510400419289,-3.29651601106314,
35.7269176981926));
#28511=CARTESIAN_POINT('Ctrl Pts',(-2.24235992782914,-3.233229780836,35.7210663814325));
#28512=CARTESIAN_POINT('Ctrl Pts',(-2.33680179998934,-3.16564312387548,
35.7152150646724));
#28513=CARTESIAN_POINT('Ctrl Pts',(-2.42803746981478,-3.09404638704326,
35.7093637479124));
#28514=CARTESIAN_POINT('Ctrl Pts',(-2.51930342063967,-3.02242588734775,
35.703510489108));
#28515=CARTESIAN_POINT('Ctrl Pts',(-2.60736072811292,-2.94679291637804,
35.6976572303035));
#28516=CARTESIAN_POINT('Ctrl Pts',(-2.69185073787341,-2.86747774272276,
35.6918039714991));
#28517=CARTESIAN_POINT('Ctrl Pts',(-2.77643687150012,-2.78807233258669,
35.6859440534711));
#28518=CARTESIAN_POINT('Ctrl Pts',(-2.85744730517025,-2.70497664130493,
35.680084135443));
#28519=CARTESIAN_POINT('Ctrl Pts',(-2.93456058230027,-2.61855746333921,
35.674224217415));
#28520=CARTESIAN_POINT('Ctrl Pts',(-3.01172578200672,-2.53208009686771,
35.6683603537365));
#28521=CARTESIAN_POINT('Ctrl Pts',(-3.08498833944942,-2.44227510737343,
35.6624964900579));
#28522=CARTESIAN_POINT('Ctrl Pts',(-3.15406847912027,-2.34954059956834,
35.6566326263794));
#28523=CARTESIAN_POINT('Ctrl Pts',(-3.22325052860603,-2.25666928606813,
35.6507601120921));
#28524=CARTESIAN_POINT('Ctrl Pts',(-3.28823761480356,-2.16086016971041,
35.6448875978048));
#28525=CARTESIAN_POINT('Ctrl Pts',(-3.34879442180649,-2.06253846521167,
35.6390150835175));
#28526=CARTESIAN_POINT('Ctrl Pts',(-3.36553102499484,-2.0353644539908,35.6373920464683));
#28527=CARTESIAN_POINT('Ctrl Pts',(-3.38192949838553,-2.00799864908361,
35.6357690094191));
#28528=CARTESIAN_POINT('Ctrl Pts',(-3.39798551695636,-1.9804503090345,35.63414597237));
#28529=CARTESIAN_POINT('Ctrl Pts',(-3.45607595395473,-1.88078082341616,
35.6282738484039));
#28530=CARTESIAN_POINT('Ctrl Pts',(-3.50987481252454,-1.77838621886318,
35.6224017244377));
#28531=CARTESIAN_POINT('Ctrl Pts',(-3.55911646351883,-1.67367230935725,
35.6165296004716));
#28532=CARTESIAN_POINT('Ctrl Pts',(-3.60829427173484,-1.56909416351423,
35.6106650898308));
#28533=CARTESIAN_POINT('Ctrl Pts',(-3.65292644795823,-1.46220306325422,
35.60480057919));
#28534=CARTESIAN_POINT('Ctrl Pts',(-3.69279180769145,-1.35343181026859,
35.5989360685492));
#28535=CARTESIAN_POINT('Ctrl Pts',(-3.73261614636621,-1.24477248181989,
35.5930775924314));
#28536=CARTESIAN_POINT('Ctrl Pts',(-3.76768328343449,-1.13423723459942,
35.5872191163137));
#28537=CARTESIAN_POINT('Ctrl Pts',(-3.79781924895605,-1.02228075999645,
35.581360640196));
#28538=CARTESIAN_POINT('Ctrl Pts',(-3.82914351551647,-0.905909693301426,
35.5752711566048));
#28539=CARTESIAN_POINT('Ctrl Pts',(-3.8551395311012,-0.788003423404034,
35.5691816730135));
#28540=CARTESIAN_POINT('Ctrl Pts',(-3.87566820456159,-0.669092645416404,
35.5630921894223));
#28541=CARTESIAN_POINT('Ctrl Pts',(-3.89539521735587,-0.554825425799626,
35.5572405049018));
#28542=CARTESIAN_POINT('Ctrl Pts',(-3.91007380593832,-0.439631125272265,
35.5513888203813));
#28543=CARTESIAN_POINT('Ctrl Pts',(-3.91963237582199,-0.323992343131811,
35.5455371358608));
#28544=CARTESIAN_POINT('Ctrl Pts',(-3.92918948781598,-0.208371198419347,
35.5396863438494));
#28545=CARTESIAN_POINT('Ctrl Pts',(-3.93362809976647,-0.0923061187816158,
35.533835551838));
#28546=CARTESIAN_POINT('Ctrl Pts',(-3.93292850011839,0.0237152473421576,
35.5279847598265));
#28547=CARTESIAN_POINT('Ctrl Pts',(-3.93222883772426,0.139747019249488,
35.5221334430663));
#28548=CARTESIAN_POINT('Ctrl Pts',(-3.92639005011987,0.255734656419345,
35.5162821263061));
#28549=CARTESIAN_POINT('Ctrl Pts',(-3.91544454946725,0.371191298452989,
35.5104308095458));
#28550=CARTESIAN_POINT('Ctrl Pts',(-3.90449541601719,0.486686260396046,
35.5045775507412));
#28551=CARTESIAN_POINT('Ctrl Pts',(-3.88843623829481,0.601649465418135,
35.4987242919365));
#28552=CARTESIAN_POINT('Ctrl Pts',(-3.86735112002908,0.715600666859522,
35.4928710331318));
#28553=CARTESIAN_POINT('Ctrl Pts',(-3.84624201332869,0.829681510018675,
35.4870111151036));
#28554=CARTESIAN_POINT('Ctrl Pts',(-3.82009562839742,0.942747644775464,
35.4811511970754));
#28555=CARTESIAN_POINT('Ctrl Pts',(-3.78904690309602,1.05433038756286,35.4752912790471));
#28556=CARTESIAN_POINT('Ctrl Pts',(-3.75797727179921,1.16598826220463,35.4694274153684));
#28557=CARTESIAN_POINT('Ctrl Pts',(-3.72199885544546,1.27616036402106,35.4635635516896));
#28558=CARTESIAN_POINT('Ctrl Pts',(-3.68129545992388,1.38439616322202,35.4576996880109));
#28559=CARTESIAN_POINT('Ctrl Pts',(-3.64053201710782,1.49279163624931,35.4518271737234));
#28560=CARTESIAN_POINT('Ctrl Pts',(-3.59502984521864,1.59924472687513,35.4459546594359));
#28561=CARTESIAN_POINT('Ctrl Pts',(-3.54501958528189,1.7033276666478,35.4400821451484));
#28562=CARTESIAN_POINT('Ctrl Pts',(-3.53119782161342,1.73209395974999,35.4384591081011));
#28563=CARTESIAN_POINT('Ctrl Pts',(-3.51703196704843,1.76067937158613,35.4368360710538));
#28564=CARTESIAN_POINT('Ctrl Pts',(-3.50252747509735,1.78907526006822,35.4352130340065));
#28565=CARTESIAN_POINT('Ctrl Pts',(-3.45005043833285,1.89181116346021,35.4293409100405));
#28566=CARTESIAN_POINT('Ctrl Pts',(-3.39296142786934,1.99240846515638,35.4234687860746));
#28567=CARTESIAN_POINT('Ctrl Pts',(-3.331458380452,2.09042437302002,35.4175966621086));
#28568=CARTESIAN_POINT('Ctrl Pts',(-3.27003507295682,2.18831320131295,35.4117321514679));
#28569=CARTESIAN_POINT('Ctrl Pts',(-3.20420932695427,2.28362694445509,35.4058676408272));
#28570=CARTESIAN_POINT('Ctrl Pts',(-3.13422580334255,2.37594562514839,35.4000031301866));
#28571=CARTESIAN_POINT('Ctrl Pts',(-3.06431429208025,2.46816931083786,35.394144654069));
#28572=CARTESIAN_POINT('Ctrl Pts',(-2.99025376121517,2.5574037366363,35.3882861779514));
#28573=CARTESIAN_POINT('Ctrl Pts',(-2.91233280283166,2.64325682549969,35.3824277018339));
#28574=CARTESIAN_POINT('Ctrl Pts',(-2.83133931784156,2.73249521538173,35.3763382182426));
#28575=CARTESIAN_POINT('Ctrl Pts',(-2.74617494034244,2.81807973566952,35.3702487346513));
#28576=CARTESIAN_POINT('Ctrl Pts',(-2.65721106180506,2.89960658935326,35.36415925106));
#28577=CARTESIAN_POINT('Ctrl Pts',(-2.57172129192485,2.97794975598523,35.3583075665397));
#28578=CARTESIAN_POINT('Ctrl Pts',(-2.48272353281795,3.05254591346051,35.3524558820193));
#28579=CARTESIAN_POINT('Ctrl Pts',(-2.39058517779383,3.12307404774726,35.346604197499));
#28580=CARTESIAN_POINT('Ctrl Pts',(-2.29846087587175,3.19359142496039,35.3407534054877));
#28581=CARTESIAN_POINT('Ctrl Pts',(-2.20319725864039,3.26004176144352,35.3349026134764));
#28582=CARTESIAN_POINT('Ctrl Pts',(-2.10519400279285,3.32214497134081,35.3290518214652));
#28583=CARTESIAN_POINT('Ctrl Pts',(-2.00718195717924,3.38425375118251,35.3232005047051));
#28584=CARTESIAN_POINT('Ctrl Pts',(-1.90643013371653,3.44201440808012,35.317349187945));
#28585=CARTESIAN_POINT('Ctrl Pts',(-1.80336571094006,3.49519114106877,35.3114978711849));
#28586=CARTESIAN_POINT('Ctrl Pts',(-1.70026708121687,3.54838552334535,35.3056446123805));
#28587=CARTESIAN_POINT('Ctrl Pts',(-1.59485469315812,3.59699276705317,35.2997913535761));
#28588=CARTESIAN_POINT('Ctrl Pts',(-1.48757809164367,3.64082414039209,35.2939380947716));
#28589=CARTESIAN_POINT('Ctrl Pts',(-1.38017944206958,3.68470538046795,35.2880781767436));
#28590=CARTESIAN_POINT('Ctrl Pts',(-1.27091272869601,3.72379974862621,35.2822182587155));
#28591=CARTESIAN_POINT('Ctrl Pts',(-1.16024523484106,3.75796753512169,35.2763583406874));
#28592=CARTESIAN_POINT('Ctrl Pts',(-1.04950322539493,3.79215832776579,35.2704944770088));
#28593=CARTESIAN_POINT('Ctrl Pts',(-0.937358956447254,3.82141582942803,
35.2646306133302));
#28594=CARTESIAN_POINT('Ctrl Pts',(-0.824290841697528,3.84565125931793,
35.2587667496516));
#28595=CARTESIAN_POINT('Ctrl Pts',(-0.711055924294302,3.86992244229369,
35.2528942353643));
#28596=CARTESIAN_POINT('Ctrl Pts',(-0.596894847145015,3.88915669855326,
35.2470217210769));
#28597=CARTESIAN_POINT('Ctrl Pts',(-0.482292178867151,3.90331695538597,
35.2411492067896));
#28598=CARTESIAN_POINT('Ctrl Pts',(-0.450618458309539,3.90723054679429,
35.2395261697408));
#28599=CARTESIAN_POINT('Ctrl Pts',(-0.418911010076204,3.9107568669515,35.237903132692));
#28600=CARTESIAN_POINT('Ctrl Pts',(-0.387180052773377,3.91389583493664,
35.2362800956432));
#28601=CARTESIAN_POINT('Ctrl Pts',(-0.272377919957184,3.92525257454261,
35.2304079716771));
#28602=CARTESIAN_POINT('Ctrl Pts',(-0.156883226493117,3.93157301805287,
35.2245358477111));
#28603=CARTESIAN_POINT('Ctrl Pts',(-0.0411755108716569,3.93278445599355,
35.2186637237451));
#28604=CARTESIAN_POINT('Ctrl Pts',(0.0743821873989408,3.93399432328088,
35.2127992131043));
#28605=CARTESIAN_POINT('Ctrl Pts',(0.190151949021274,3.93010835329838,35.2069347024636));
#28606=CARTESIAN_POINT('Ctrl Pts',(0.305648185573892,3.92110548017461,35.2010701918229));
#28607=CARTESIAN_POINT('Ctrl Pts',(0.421025577648148,3.91211187091772,35.1952117157053));
#28608=CARTESIAN_POINT('Ctrl Pts',(0.536129594798534,3.89801186327134,35.1893532395877));
#28609=CARTESIAN_POINT('Ctrl Pts',(0.650474386927082,3.87883643274009,35.1834947634701));
#28610=CARTESIAN_POINT('Ctrl Pts',(0.769327945674206,3.85890488958256,35.1774052798788));
#28611=CARTESIAN_POINT('Ctrl Pts',(0.887360718078583,3.83348942291054,35.1713157962875));
#28612=CARTESIAN_POINT('Ctrl Pts',(1.00403225191212,3.80268434623757,35.1652263126963));
#28613=CARTESIAN_POINT('Ctrl Pts',(1.11614767159814,3.77308223176998,35.1593746281758));
#28614=CARTESIAN_POINT('Ctrl Pts',(1.22700573513248,3.73850366057662,35.1535229436554));
#28615=CARTESIAN_POINT('Ctrl Pts',(1.33613780774355,3.69908431354548,35.147671259135));
#28616=CARTESIAN_POINT('Ctrl Pts',(1.44525323534139,3.65967097882162,35.1418204671237));
#28617=CARTESIAN_POINT('Ctrl Pts',(1.55264280672405,3.61541847668629,35.1359696751124));
#28618=CARTESIAN_POINT('Ctrl Pts',(1.65785488154545,3.56651176806357,35.1301188831011));
#28619=CARTESIAN_POINT('Ctrl Pts',(1.76307639268116,3.51760067307098,35.1242675663409));
#28620=CARTESIAN_POINT('Ctrl Pts',(1.86611964411228,3.46403471605469,35.1184162495808));
#28621=CARTESIAN_POINT('Ctrl Pts',(1.9665553980936,3.40604592837926,35.1125649328206));
#28622=CARTESIAN_POINT('Ctrl Pts',(2.06702448656943,3.34803789430154,35.1067116740162));
#28623=CARTESIAN_POINT('Ctrl Pts',(2.16488399892109,3.2856043172812,35.1008584152117));
#28624=CARTESIAN_POINT('Ctrl Pts',(2.25973221776311,3.21902148237682,35.0950051564072));
#28625=CARTESIAN_POINT('Ctrl Pts',(2.35468834495526,3.15236289651,35.0891452383791));
#28626=CARTESIAN_POINT('Ctrl Pts',(2.44662600199921,3.08154586825698,35.083285320351));
#28627=CARTESIAN_POINT('Ctrl Pts',(2.53517513579142,3.00688809749631,35.0774254023229));
#28628=CARTESIAN_POINT('Ctrl Pts',(2.6237838922495,2.93218005752203,35.0715615386443));
#28629=CARTESIAN_POINT('Ctrl Pts',(2.70899927913946,2.85362640516535,35.0656976749657));
#28630=CARTESIAN_POINT('Ctrl Pts',(2.7904880828334,2.77158172521843,35.059833811287));
#28631=CARTESIAN_POINT('Ctrl Pts',(2.87209710210524,2.68941600964248,35.0539612969996));
#28632=CARTESIAN_POINT('Ctrl Pts',(2.94996828894454,2.60374929259172,35.0480887827122));
#28633=CARTESIAN_POINT('Ctrl Pts',(3.02380861326784,2.51496927820743,35.0422162684248));
#28634=CARTESIAN_POINT('Ctrl Pts',(3.04421649585048,2.49043238558347,35.0405932313765));
#28635=CARTESIAN_POINT('Ctrl Pts',(3.06431673688239,2.46565785193998,35.0389701943281));
#28636=CARTESIAN_POINT('Ctrl Pts',(3.08410374667262,2.44065423191404,35.0373471572797));
#28637=CARTESIAN_POINT('Ctrl Pts',(3.1556087869851,2.35029773657354,35.0314819289908));
#28638=CARTESIAN_POINT('Ctrl Pts',(3.22326457165389,2.25663831851123,35.0256167007019));
#28639=CARTESIAN_POINT('Ctrl Pts',(3.28674987154625,2.16003802788068,35.019751472413));
#28640=CARTESIAN_POINT('Ctrl Pts',(3.35015504965811,2.06355965188702,35.0138936463501));
#28641=CARTESIAN_POINT('Ctrl Pts',(3.40939998051885,1.96414812317378,35.0080358202871));
#28642=CARTESIAN_POINT('Ctrl Pts',(3.46420333166326,1.86219877480713,35.0021779942242));
#28643=CARTESIAN_POINT('Ctrl Pts',(3.51895084127202,1.76035330709835,34.9963261369569));
#28644=CARTESIAN_POINT('Ctrl Pts',(3.56926557482931,1.65597552318575,34.9904742796896));
#28645=CARTESIAN_POINT('Ctrl Pts',(3.61490963089598,1.54948938700964,34.9846224224223));
#28646=CARTESIAN_POINT('Ctrl Pts',(3.66051827221708,1.44308587231251,34.9787751055498));
#28647=CARTESIAN_POINT('Ctrl Pts',(3.70146328114283,1.33457763772048,34.9729277886773));
#28648=CARTESIAN_POINT('Ctrl Pts',(3.73755316320159,1.22441224766898,34.9670804718048));
#28649=CARTESIAN_POINT('Ctrl Pts',(3.7736264771196,1.1142974323377,34.9612358393182));
#28650=CARTESIAN_POINT('Ctrl Pts',(3.80484896667096,1.00252736656861,34.9553912068316));
#28651=CARTESIAN_POINT('Ctrl Pts',(3.8310778916543,0.889567978334213,34.949546574345));
#28652=CARTESIAN_POINT('Ctrl Pts',(3.85729952992758,0.77663997157318,34.9437035655674));
#28653=CARTESIAN_POINT('Ctrl Pts',(3.8785302727413,0.662523703250463,34.9378605567898));
#28654=CARTESIAN_POINT('Ctrl Pts',(3.89467792205645,0.54769780303198,34.9320175480122));
#28655=CARTESIAN_POINT('Ctrl Pts',(3.91082899833729,0.432847533667717,34.9261732991909));
#28656=CARTESIAN_POINT('Ctrl Pts',(3.92189476648159,0.317287741314481,34.9203290503697));
#28657=CARTESIAN_POINT('Ctrl Pts',(3.92783464354237,0.201504374613492,34.9144848015484));
#28658=CARTESIAN_POINT('Ctrl Pts',(3.93133136503697,0.133344346566134,34.9110443750439));
#28659=CARTESIAN_POINT('Ctrl Pts',(3.93305268568233,0.0651069405325119,
34.9076039485395));
#28660=CARTESIAN_POINT('Ctrl Pts',(3.93299877161876,-0.00310844740720695,
34.904163522035));
#28661=CARTESIAN_POINT('',(3.9391332139622,-0.00113435864636278,33.654163522035));
#28662=CARTESIAN_POINT('Ctrl Pts',(3.92939779249061,-0.0031338771959184,
34.9041620946445));
#28663=CARTESIAN_POINT('Ctrl Pts',(3.93258331200376,-0.437279526977727,
34.8822461360685));
#28664=CARTESIAN_POINT('Ctrl Pts',(3.66567225937177,-2.18120492678934,34.7940191980378));
#28665=CARTESIAN_POINT('Ctrl Pts',(1.1074941219487,-4.51860510079755,34.6394812805529));
#28666=CARTESIAN_POINT('Ctrl Pts',(-3.20371133310602,-3.37350989049275,
34.4405483421894));
#28667=CARTESIAN_POINT('Ctrl Pts',(-4.5697304411889,0.872868250080218,34.2416154038258));
#28668=CARTESIAN_POINT('Ctrl Pts',(-1.73477564576997,4.31681465272121,34.0426824654626));
#28669=CARTESIAN_POINT('Ctrl Pts',(2.62558860763858,3.80050871419932,33.8468651715321));
#28670=CARTESIAN_POINT('Ctrl Pts',(3.93440149740121,1.24278092515243,33.7173588570563));
#28671=CARTESIAN_POINT('Ctrl Pts',(3.9391332139622,-0.00113435864636278,
33.654163522035));
#28672=CARTESIAN_POINT('',(3.9329983150557,0.00364057262290602,32.404163522035));
#28673=CARTESIAN_POINT('Ctrl Pts',(3.9391332139622,-0.00113435864636278,
33.654163522035));
#28674=CARTESIAN_POINT('Ctrl Pts',(3.93936649615554,-0.0624616342740536,
33.6510478776019));
#28675=CARTESIAN_POINT('Ctrl Pts',(3.91022907276817,-1.42880496523826,33.5816212537148));
#28676=CARTESIAN_POINT('Ctrl Pts',(2.32725627739605,-4.02842568585283,33.4458836503718));
#28677=CARTESIAN_POINT('Ctrl Pts',(-2.13215816018169,-4.13500143495696,
33.2469507120089));
#28678=CARTESIAN_POINT('Ctrl Pts',(-4.63146993867469,-0.44025162607551,
33.0480177736453));
#28679=CARTESIAN_POINT('Ctrl Pts',(-2.8730504138422,3.65922349777118,32.8490848352818));
#28680=CARTESIAN_POINT('Ctrl Pts',(1.52657737641075,4.3947578773988,32.6501518969184));
#28681=CARTESIAN_POINT('Ctrl Pts',(3.76031183336374,1.93114587073444,32.5018448144934));
#28682=CARTESIAN_POINT('Ctrl Pts',(3.93572306029363,0.313664098688633,32.4198487115227));
#28683=CARTESIAN_POINT('Ctrl Pts',(3.93286077649292,0.00364174925168429,
32.4041635880065));
#28684=CARTESIAN_POINT('',(3.93054987827653,-0.000439589250792058,31.1541634039922));
#28685=CARTESIAN_POINT('Ctrl Pts',(3.9329983150557,0.00364057262290602,
32.404163522035));
#28686=CARTESIAN_POINT('Ctrl Pts',(3.93310415105304,-0.110696605159677,
32.3983789491121));
#28687=CARTESIAN_POINT('Ctrl Pts',(3.92821989213574,-0.225172602477814,
32.3925943761891));
#28688=CARTESIAN_POINT('Ctrl Pts',(3.91833602088708,-0.3393108124107,32.3868098032662));
#28689=CARTESIAN_POINT('Ctrl Pts',(3.90845907876316,-0.453369005326499,
32.3810292856396));
#28690=CARTESIAN_POINT('Ctrl Pts',(3.89358952894702,-0.567089459903584,
32.3752487680131));
#28691=CARTESIAN_POINT('Ctrl Pts',(3.87376992155456,-0.679996760918176,
32.3694682503865));
#28692=CARTESIAN_POINT('Ctrl Pts',(3.8539574981122,-0.792863136782181,32.3636898280058));
#28693=CARTESIAN_POINT('Ctrl Pts',(3.82919865527693,-0.904916526835692,
32.3579114056251));
#28694=CARTESIAN_POINT('Ctrl Pts',(3.79958757305406,-1.01568857170551,32.3521329832444));
#28695=CARTESIAN_POINT('Ctrl Pts',(3.76997962428042,-1.12644889466065,32.3463551723372));
#28696=CARTESIAN_POINT('Ctrl Pts',(3.73552056656729,-1.23592773163399,32.3405773614301));
#28697=CARTESIAN_POINT('Ctrl Pts',(3.69635507222063,-1.34366966925238,32.3347995505229));
#28698=CARTESIAN_POINT('Ctrl Pts',(3.65718367016728,-1.4514278586193,32.3290208680931));
#28699=CARTESIAN_POINT('Ctrl Pts',(3.61330456664536,-1.55744822906134,32.3232421856634));
#28700=CARTESIAN_POINT('Ctrl Pts',(3.56491110023304,-1.66129402799,32.3174635032337));
#28701=CARTESIAN_POINT('Ctrl Pts',(3.51646806002748,-1.76524620553847,32.3116789011782));
#28702=CARTESIAN_POINT('Ctrl Pts',(3.46350160308214,-1.86701897811158,32.3058942991228));
#28703=CARTESIAN_POINT('Ctrl Pts',(3.40625170290018,-1.96619895648677,32.3001096970673));
#28704=CARTESIAN_POINT('Ctrl Pts',(3.34897105225448,-2.06543220710031,32.2943219879463));
#28705=CARTESIAN_POINT('Ctrl Pts',(3.28740260695837,-2.16206953360629,32.2885342788252));
#28706=CARTESIAN_POINT('Ctrl Pts',(3.22182939718089,-2.25572700818628,32.2827465697042));
#28707=CARTESIAN_POINT('Ctrl Pts',(3.15615129373913,-2.3495343012017,32.2769496023202));
#28708=CARTESIAN_POINT('Ctrl Pts',(3.08645589152145,-2.4403518869279,32.2711526349362));
#28709=CARTESIAN_POINT('Ctrl Pts',(3.01306632916588,-2.52782916670546,32.2653556675522));
#28710=CARTESIAN_POINT('Ctrl Pts',(2.95791245091571,-2.59357027598109,32.260999118432));
#28711=CARTESIAN_POINT('Ctrl Pts',(2.90067299541346,-2.65742553068555,32.2566425693117));
#28712=CARTESIAN_POINT('Ctrl Pts',(2.84149790413252,-2.71926068276112,32.2522860201915));
#28713=CARTESIAN_POINT('Ctrl Pts',(2.76173673029731,-2.80260731065918,32.2464138962254));
#28714=CARTESIAN_POINT('Ctrl Pts',(2.67817165199454,-2.88258136840731,32.2405417722594));
#28715=CARTESIAN_POINT('Ctrl Pts',(2.59111938936618,-2.95881552484278,32.2346696482934));
#28716=CARTESIAN_POINT('Ctrl Pts',(2.50417999172485,-3.0349508421807,32.2288051376527));
#28717=CARTESIAN_POINT('Ctrl Pts',(2.41376270892944,-3.1073556309769,32.222940627012));
#28718=CARTESIAN_POINT('Ctrl Pts',(2.320222468961,-3.17569782796294,32.2170761163713));
#28719=CARTESIAN_POINT('Ctrl Pts',(2.22677848096878,-3.24396970150827,32.2112176402537));
#28720=CARTESIAN_POINT('Ctrl Pts',(2.13021825939134,-3.30818705577219,32.2053591641361));
#28721=CARTESIAN_POINT('Ctrl Pts',(2.03093080474347,-3.36805716494599,32.1995006880185));
#28722=CARTESIAN_POINT('Ctrl Pts',(1.92772831423915,-3.43028803183059,32.1934112044272));
#28723=CARTESIAN_POINT('Ctrl Pts',(1.82157943140423,-3.48782146541949,32.1873217208359));
#28724=CARTESIAN_POINT('Ctrl Pts',(1.71295583545349,-3.54037728297223,32.1812322372447));
#28725=CARTESIAN_POINT('Ctrl Pts',(1.60857407541615,-3.59088075496964,32.1753805527243));
#28726=CARTESIAN_POINT('Ctrl Pts',(1.50190766141388,-3.63678787816653,32.1695288682039));
#28727=CARTESIAN_POINT('Ctrl Pts',(1.3934006777869,-3.67789662050784,32.1636771836835));
#28728=CARTESIAN_POINT('Ctrl Pts',(1.28491024383368,-3.71899909287232,32.1578263916722));
#28729=CARTESIAN_POINT('Ctrl Pts',(1.17458018491985,-3.75530449311771,32.1519755996609));
#28730=CARTESIAN_POINT('Ctrl Pts',(1.06287376039485,-3.78665926239266,32.1461248076496));
#28731=CARTESIAN_POINT('Ctrl Pts',(0.95115731708683,-3.81801684383021,32.1402734908895));
#28732=CARTESIAN_POINT('Ctrl Pts',(0.838064660825857,-3.8444227999075,32.1344221741293));
#28733=CARTESIAN_POINT('Ctrl Pts',(0.724072682062405,-3.86577388773464,
32.1285708573692));
#28734=CARTESIAN_POINT('Ctrl Pts',(0.610042869510037,-3.88713206195994,
32.1227175985647));
#28735=CARTESIAN_POINT('Ctrl Pts',(0.495113547070775,-3.90343195585995,
32.1168643397602));
#28736=CARTESIAN_POINT('Ctrl Pts',(0.379769517664681,-3.91462183530577,
32.1110110809556));
#28737=CARTESIAN_POINT('Ctrl Pts',(0.264294261927041,-3.92582444542207,
32.1051511629275));
#28738=CARTESIAN_POINT('Ctrl Pts',(0.148403769228592,-3.93190539727357,
32.0992912448994));
#28739=CARTESIAN_POINT('Ctrl Pts',(0.0325857612234615,-3.93286500762046,
32.0934313268713));
#28740=CARTESIAN_POINT('Ctrl Pts',(-0.0833102303607444,-3.93382526410046,
32.0875674631927));
#28741=CARTESIAN_POINT('Ctrl Pts',(-0.199133227932258,-3.92965732757556,
32.0817035995141));
#28742=CARTESIAN_POINT('Ctrl Pts',(-0.314399468437188,-3.9204134953148,
32.0758397358355));
#28743=CARTESIAN_POINT('Ctrl Pts',(-0.429835754360515,-3.91115602617895,
32.0699672215482));
#28744=CARTESIAN_POINT('Ctrl Pts',(-0.544713235264734,-3.89680776736262,
32.0640947072608));
#28745=CARTESIAN_POINT('Ctrl Pts',(-0.658557096399692,-3.87747231463767,
32.0582221929734));
#28746=CARTESIAN_POINT('Ctrl Pts',(-0.69002109892269,-3.87212841003661,
32.056599155925));
#28747=CARTESIAN_POINT('Ctrl Pts',(-0.721406233175616,-3.86640385287236,
32.0549761188766));
#28748=CARTESIAN_POINT('Ctrl Pts',(-0.752702687445247,-3.8603014991465,
32.0533530818282));
#28749=CARTESIAN_POINT('Ctrl Pts',(-0.86593279476183,-3.83822327388462,
32.0474809578621));
#28750=CARTESIAN_POINT('Ctrl Pts',(-0.978380511693693,-3.81112192370885,
32.0416088338961));
#28751=CARTESIAN_POINT('Ctrl Pts',(-1.08956561142989,-3.77906546362846,
32.0357367099301));
#28752=CARTESIAN_POINT('Ctrl Pts',(-1.20060655747657,-3.74705056538509,
32.0298721992893));
#28753=CARTESIAN_POINT('Ctrl Pts',(-1.31038774818272,-3.71009344650441,
32.0240076886486));
#28754=CARTESIAN_POINT('Ctrl Pts',(-1.41843798709904,-3.66831332859591,
32.0181431780079));
#28755=CARTESIAN_POINT('Ctrl Pts',(-1.52637704339427,-3.62657620201317,
32.0122847018903));
#28756=CARTESIAN_POINT('Ctrl Pts',(-1.63258830738749,-3.58002609588318,
32.0064262257727));
#28757=CARTESIAN_POINT('Ctrl Pts',(-1.73661527179651,-3.52883215777729,
32.0005677496551));
#28758=CARTESIAN_POINT('Ctrl Pts',(-1.8447441572099,-3.47561957487862,31.9944782660638));
#28759=CARTESIAN_POINT('Ctrl Pts',(-1.9505125022498,-3.41738952683523,31.9883887824725));
#28760=CARTESIAN_POINT('Ctrl Pts',(-2.05342967864792,-3.35438750815225,
31.9822992988813));
#28761=CARTESIAN_POINT('Ctrl Pts',(-2.1523278592552,-3.29384576730398,31.9764476143609));
#28762=CARTESIAN_POINT('Ctrl Pts',(-2.24859298738348,-3.22889799641962,
31.9705959298404));
#28763=CARTESIAN_POINT('Ctrl Pts',(-2.3418151048469,-3.15980869906881,31.96474424532));
#28764=CARTESIAN_POINT('Ctrl Pts',(-2.43502300391103,-3.09072993933764,
31.9588934533087));
#28765=CARTESIAN_POINT('Ctrl Pts',(-2.52518848308879,-3.01751115519268,
31.9530426612974));
#28766=CARTESIAN_POINT('Ctrl Pts',(-2.61193201040197,-2.94045917724384,
31.947191869286));
#28767=CARTESIAN_POINT('Ctrl Pts',(-2.69868331761289,-2.86340028861788,
31.9413405525259));
#28768=CARTESIAN_POINT('Ctrl Pts',(-2.78201175374955,-2.78250779732479,
31.9354892357657));
#28769=CARTESIAN_POINT('Ctrl Pts',(-2.86157275925305,-2.69812719186863,
31.9296379190056));
#28770=CARTESIAN_POINT('Ctrl Pts',(-2.9411601709504,-2.61371858059968,31.923784660201));
#28771=CARTESIAN_POINT('Ctrl Pts',(-3.01697738220466,-2.52581985378752,
31.9179314013965));
#28772=CARTESIAN_POINT('Ctrl Pts',(-3.0887188995972,-2.43481099046128,31.912078142592));
#28773=CARTESIAN_POINT('Ctrl Pts',(-3.16054203695916,-2.34369858680147,
31.9062182245638));
#28774=CARTESIAN_POINT('Ctrl Pts',(-3.22827996925133,-2.24946930896179,
31.9003583065357));
#28775=CARTESIAN_POINT('Ctrl Pts',(-3.29166942371827,-2.15253371749626,
31.8944983885076));
#28776=CARTESIAN_POINT('Ctrl Pts',(-3.35510156011908,-2.05553285652273,
31.8886345248289));
#28777=CARTESIAN_POINT('Ctrl Pts',(-3.41417917834624,-1.9558224082933,31.8827706611503));
#28778=CARTESIAN_POINT('Ctrl Pts',(-3.46868488323865,-1.85383768998035,
31.8769067974716));
#28779=CARTESIAN_POINT('Ctrl Pts',(-3.52327099715044,-1.75170251968798,
31.8710342831842));
#28780=CARTESIAN_POINT('Ctrl Pts',(-3.57327155873323,-1.64728675463577,
31.8651617688968));
#28781=CARTESIAN_POINT('Ctrl Pts',(-3.61851717272685,-1.54104590154897,
31.8592892546094));
#28782=CARTESIAN_POINT('Ctrl Pts',(-3.63102209041432,-1.5116832074526,31.8576662175612));
#28783=CARTESIAN_POINT('Ctrl Pts',(-3.64316409482757,-1.48218119166648,
31.8560431805129));
#28784=CARTESIAN_POINT('Ctrl Pts',(-3.65494028738876,-1.45254965341036,
31.8544201434647));
#28785=CARTESIAN_POINT('Ctrl Pts',(-3.69754637739869,-1.34534318752482,
31.8485480194986));
#28786=CARTESIAN_POINT('Ctrl Pts',(-3.73550303719789,-1.23608082345837,
31.8426758955326));
#28787=CARTESIAN_POINT('Ctrl Pts',(-3.76860800799001,-1.12520339588607,
31.8368037715666));
#28788=CARTESIAN_POINT('Ctrl Pts',(-3.80167005753017,-1.01446972310021,
31.8309392609258));
#28789=CARTESIAN_POINT('Ctrl Pts',(-3.82989281002862,-0.902125543410319,
31.8250747502851));
#28790=CARTESIAN_POINT('Ctrl Pts',(-3.85312197359904,-0.788631762337931,
31.8192102396444));
#28791=CARTESIAN_POINT('Ctrl Pts',(-3.87632723459117,-0.675254765237539,
31.8133517635268));
#28792=CARTESIAN_POINT('Ctrl Pts',(-3.89454904468726,-0.560730922233132,
31.8074932874092));
#28793=CARTESIAN_POINT('Ctrl Pts',(-3.90768305905102,-0.445535756147207,
31.8016348112916));
#28794=CARTESIAN_POINT('Ctrl Pts',(-3.92133496499895,-0.325798292070669,
31.7955453277004));
#28795=CARTESIAN_POINT('Ctrl Pts',(-3.92948945333206,-0.205335909445877,
31.7894558441091));
#28796=CARTESIAN_POINT('Ctrl Pts',(-3.932087983519,-0.0846940958124628,
31.7833663605178));
#28797=CARTESIAN_POINT('Ctrl Pts',(-3.9345850390809,0.031236561159069,31.7775146759974));
#28798=CARTESIAN_POINT('Ctrl Pts',(-3.93195191279619,0.147332446022961,
31.771662991477));
#28799=CARTESIAN_POINT('Ctrl Pts',(-3.92418964905146,0.263105678915161,
31.7658113069566));
#28800=CARTESIAN_POINT('Ctrl Pts',(-3.91642856922069,0.378861253872504,
31.7599605149453));
#28801=CARTESIAN_POINT('Ctrl Pts',(-3.90353993504566,0.494293862333126,
31.754109722934));
#28802=CARTESIAN_POINT('Ctrl Pts',(-3.88557684738688,0.608918354996007,
31.7482589309227));
#28803=CARTESIAN_POINT('Ctrl Pts',(-3.86761214864552,0.723553128158945,
31.7424076141625));
#28804=CARTESIAN_POINT('Ctrl Pts',(-3.8445721556929,0.837379232991023,31.7365562974024));
#28805=CARTESIAN_POINT('Ctrl Pts',(-3.81656139502567,0.949920058741654,
31.7307049806423));
#28806=CARTESIAN_POINT('Ctrl Pts',(-3.78854133762356,1.0624982366453,31.7248517218377));
#28807=CARTESIAN_POINT('Ctrl Pts',(-3.75554733180139,1.17378988627484,31.7189984630332));
#28808=CARTESIAN_POINT('Ctrl Pts',(-3.71773403512612,1.28333263188655,31.7131452042287));
#28809=CARTESIAN_POINT('Ctrl Pts',(-3.67987771845016,1.3930000037384,31.7072852862006));
#28810=CARTESIAN_POINT('Ctrl Pts',(-3.63719130220763,1.50091410912668,31.7014253681725));
#28811=CARTESIAN_POINT('Ctrl Pts',(-3.58987799037896,1.60663157388142,31.6955654501443));
#28812=CARTESIAN_POINT('Ctrl Pts',(-3.54253282114334,1.7124202212308,31.6897015864657));
#28813=CARTESIAN_POINT('Ctrl Pts',(-3.49055473786379,1.81600891424349,31.6838377227871));
#28814=CARTESIAN_POINT('Ctrl Pts',(-3.43419256562877,1.91697950489307,31.6779738591084));
#28815=CARTESIAN_POINT('Ctrl Pts',(-3.37774724563876,2.01809905143983,31.672101344821));
#28816=CARTESIAN_POINT('Ctrl Pts',(-3.31690514504655,2.11659243672795,31.6662288305336));
#28817=CARTESIAN_POINT('Ctrl Pts',(-3.25195801391227,2.21207099247555,31.6603563162462));
#28818=CARTESIAN_POINT('Ctrl Pts',(-3.23400801926684,2.23845921832157,31.6587332791979));
#28819=CARTESIAN_POINT('Ctrl Pts',(-3.21574469416063,2.26461735592319,31.6571102421496));
#28820=CARTESIAN_POINT('Ctrl Pts',(-3.19717471782691,2.2905376713096,31.6554872051012));
#28821=CARTESIAN_POINT('Ctrl Pts',(-3.12998881890394,2.38431698789608,31.6496150811352));
#28822=CARTESIAN_POINT('Ctrl Pts',(-3.05856069220708,2.47529497941596,31.6437429571692));
#28823=CARTESIAN_POINT('Ctrl Pts',(-2.98315198438263,2.56306325284297,31.6378708332032));
#28824=CARTESIAN_POINT('Ctrl Pts',(-2.90784104544492,2.65071773296107,31.6320063225625));
#28825=CARTESIAN_POINT('Ctrl Pts',(-2.8285600554653,2.73517045995463,31.6261418119217));
#28826=CARTESIAN_POINT('Ctrl Pts',(-2.7456134683507,2.81604255692474,31.620277301281));
#28827=CARTESIAN_POINT('Ctrl Pts',(-2.66275223244944,2.89683143731124,31.6144188251634));
#28828=CARTESIAN_POINT('Ctrl Pts',(-2.57623319605064,2.97404672932177,31.6085603490459));
#28829=CARTESIAN_POINT('Ctrl Pts',(-2.48640010144476,3.04734368516836,31.6027018729283));
#28830=CARTESIAN_POINT('Ctrl Pts',(-2.39302476892212,3.12353083707601,31.596612389337));
#28831=CARTESIAN_POINT('Ctrl Pts',(-2.2960689424696,3.19548394002888,31.5905229057457));
#28832=CARTESIAN_POINT('Ctrl Pts',(-2.19595998586853,3.26285898262004,31.5844334221545));
#28833=CARTESIAN_POINT('Ctrl Pts',(-2.09976036189145,3.32760297739104,31.5785817376341));
#28834=CARTESIAN_POINT('Ctrl Pts',(-2.00064962612047,3.38811950316052,31.5727300531137));
#28835=CARTESIAN_POINT('Ctrl Pts',(-1.89903886540533,3.44414581393994,31.5668783685933));
#28836=CARTESIAN_POINT('Ctrl Pts',(-1.79744360253997,3.5001635794891,31.561027576582));
#28837=CARTESIAN_POINT('Ctrl Pts',(-1.69334943481795,3.55169229219511,31.5551767845707));
#28838=CARTESIAN_POINT('Ctrl Pts',(-1.58719328007681,3.59851448401684,31.5493259925594));
#28839=CARTESIAN_POINT('Ctrl Pts',(-1.48102760434829,3.64534087525122,31.5434746757993));
#28840=CARTESIAN_POINT('Ctrl Pts',(-1.3727999522399,3.68745973961803,31.5376233590392));
#28841=CARTESIAN_POINT('Ctrl Pts',(-1.26296784462179,3.72470149454307,31.5317720422791));
#28842=CARTESIAN_POINT('Ctrl Pts',(-1.15309928387005,3.76195560995812,31.5259187834745));
#28843=CARTESIAN_POINT('Ctrl Pts',(-1.04162560004453,3.79432926455435,31.52006552467));
#28844=CARTESIAN_POINT('Ctrl Pts',(-0.929019424295612,3.82170274999004,
31.5142122658655));
#28845=CARTESIAN_POINT('Ctrl Pts',(-0.816285137058031,3.84910737810459,
31.5083523478374));
#28846=CARTESIAN_POINT('Ctrl Pts',(-0.702416188177486,3.87150038491752,
31.5024924298093));
#28847=CARTESIAN_POINT('Ctrl Pts',(-0.587895452030208,3.8888131785266,31.4966325117812));
#28848=CARTESIAN_POINT('Ctrl Pts',(-0.473297605793603,3.90613762933514,
31.4907686481026));
#28849=CARTESIAN_POINT('Ctrl Pts',(-0.358047508518624,3.91837501220579,
31.4849047844239));
#28850=CARTESIAN_POINT('Ctrl Pts',(-0.242631459511845,3.92550875363374,
31.4790409207453));
#28851=CARTESIAN_POINT('Ctrl Pts',(-0.127045144083723,3.93265301904545,
31.4731684064579));
#28852=CARTESIAN_POINT('Ctrl Pts',(-0.0112928001129308,3.93467860912626,
31.4672958921706));
#28853=CARTESIAN_POINT('Ctrl Pts',(0.104140884172505,3.93162099855057,31.4614233778832));
#28854=CARTESIAN_POINT('Ctrl Pts',(0.136044279731012,3.93077594053943,31.4598003408348));
#28855=CARTESIAN_POINT('Ctrl Pts',(0.167923376824294,3.92954290551545,31.4581773037863));
#28856=CARTESIAN_POINT('Ctrl Pts',(0.199768058657367,3.9279233346312,31.4565542667379));
#28857=CARTESIAN_POINT('Ctrl Pts',(0.31498164516342,3.92206375119576,31.4506821427718));
#28858=CARTESIAN_POINT('Ctrl Pts',(0.430130357789259,3.91112089027485,31.4448100188058));
#28859=CARTESIAN_POINT('Ctrl Pts',(0.544729177393587,3.89509423805074,31.4389378948398));
#28860=CARTESIAN_POINT('Ctrl Pts',(0.65917941735272,3.87908836469949,31.433073384199));
#28861=CARTESIAN_POINT('Ctrl Pts',(0.773080776439822,3.85801186435209,31.4272088735583));
#28862=CARTESIAN_POINT('Ctrl Pts',(0.885949940811049,3.8319161919824,31.4213443629176));
#28863=CARTESIAN_POINT('Ctrl Pts',(0.998702963935036,3.80584737179996,31.4154858868));
#28864=CARTESIAN_POINT('Ctrl Pts',(1.11042550458441,3.7747697449502,31.4096274106824));
#28865=CARTESIAN_POINT('Ctrl Pts',(1.22064173718731,3.73878626688346,31.4037689345648));
#28866=CARTESIAN_POINT('Ctrl Pts',(1.33520394183798,3.70138391261158,31.3976794509735));
#28867=CARTESIAN_POINT('Ctrl Pts',(1.4481381524379,3.65868092227371,31.3915899673823));
#28868=CARTESIAN_POINT('Ctrl Pts',(1.55892397835393,3.610851011841,31.385500483791));
#28869=CARTESIAN_POINT('Ctrl Pts',(1.6653835315949,3.56488889661443,31.3796487992706));
#28870=CARTESIAN_POINT('Ctrl Pts',(1.76985892831247,3.51419294690338,31.3737971147502));
#28871=CARTESIAN_POINT('Ctrl Pts',(1.87190695319767,3.4589670941728,31.3679454302297));
#28872=CARTESIAN_POINT('Ctrl Pts',(1.97393941354089,3.40374966458519,31.3620946382184));
#28873=CARTESIAN_POINT('Ctrl Pts',(2.07354487469399,3.34400390242997,31.3562438462071));
#28874=CARTESIAN_POINT('Ctrl Pts',(2.17030426239046,3.27997994028162,31.3503930541957));
#28875=CARTESIAN_POINT('Ctrl Pts',(2.26707232829195,3.21595023591969,31.3445417374356));
#28876=CARTESIAN_POINT('Ctrl Pts',(2.36099346851151,3.1476417969362,31.3386904206755));
#28877=CARTESIAN_POINT('Ctrl Pts',(2.45167776881482,3.07534796696231,31.3328391039153));
#28878=CARTESIAN_POINT('Ctrl Pts',(2.54239216711855,3.00303014276098,31.3269858451108));
#28879=CARTESIAN_POINT('Ctrl Pts',(2.62986726623403,2.92672455494401,31.3211325863063));
#28880=CARTESIAN_POINT('Ctrl Pts',(2.71374695338587,2.8467642109927,31.3152793275019));
#28881=CARTESIAN_POINT('Ctrl Pts',(2.79772207004357,2.76671289655293,31.3094194094737));
#28882=CARTESIAN_POINT('Ctrl Pts',(2.87809331083021,2.68299881214748,31.3035594914456));
#28883=CARTESIAN_POINT('Ctrl Pts',(2.95454203957614,2.59599120498843,31.2976995734174));
#28884=CARTESIAN_POINT('Ctrl Pts',(3.03104224343875,2.5089250131177,31.2918357097388));
#28885=CARTESIAN_POINT('Ctrl Pts',(3.1036144179988,2.41856120431654,31.2859718460602));
#28886=CARTESIAN_POINT('Ctrl Pts',(3.17198184688789,2.32530001569984,31.2801079823816));
#28887=CARTESIAN_POINT('Ctrl Pts',(3.24045013417226,2.23190124440702,31.2742354680942));
#28888=CARTESIAN_POINT('Ctrl Pts',(3.30470106714808,2.13559690513932,31.2683629538067));
#28889=CARTESIAN_POINT('Ctrl Pts',(3.36450259550393,2.03681400349844,31.2624904395193));
#28890=CARTESIAN_POINT('Ctrl Pts',(3.38103045585764,2.00951252728967,31.260867402471));
#28891=CARTESIAN_POINT('Ctrl Pts',(3.39721872650933,1.9820218543258,31.2592443654227));
#28892=CARTESIAN_POINT('Ctrl Pts',(3.41306315351778,1.95435127602468,31.2576213283744));
#28893=CARTESIAN_POINT('Ctrl Pts',(3.47282941894242,1.84997595678364,31.2514991213061));
#28894=CARTESIAN_POINT('Ctrl Pts',(3.52788579428435,1.74271420706082,31.2453769142378));
#28895=CARTESIAN_POINT('Ctrl Pts',(3.57795569987535,1.63301010705062,31.2392547071696));
#28896=CARTESIAN_POINT('Ctrl Pts',(3.62794038119396,1.52349273501587,31.2331429207449));
#28897=CARTESIAN_POINT('Ctrl Pts',(3.67295534489491,1.41154161984525,31.2270311343203));
#28898=CARTESIAN_POINT('Ctrl Pts',(3.71276900053987,1.29762681408415,31.2209193478957));
#28899=CARTESIAN_POINT('Ctrl Pts',(3.75249823434007,1.18395355605065,31.2148205210518));
#28900=CARTESIAN_POINT('Ctrl Pts',(3.7870480245688,1.06832524865232,31.2087216942079));
#28901=CARTESIAN_POINT('Ctrl Pts',(3.81623451173568,0.951232438175632,31.202622867364));
#28902=CARTESIAN_POINT('Ctrl Pts',(3.84538425142669,0.834287054321492,31.1965317192959));
#28903=CARTESIAN_POINT('Ctrl Pts',(3.86918404490673,0.715881189403285,31.1904405712279));
#28904=CARTESIAN_POINT('Ctrl Pts',(3.88749925303357,0.596522051280121,31.1843494231598));
#28905=CARTESIAN_POINT('Ctrl Pts',(3.90578672503263,0.47734366787643,31.1782674993856));
#28906=CARTESIAN_POINT('Ctrl Pts',(3.91860611103049,0.357215246689481,31.1721855756113));
#28907=CARTESIAN_POINT('Ctrl Pts',(3.92587358486372,0.236655014037924,31.1661036518371));
#28908=CARTESIAN_POINT('Ctrl Pts',(3.93062945839558,0.157759756535824,31.1621236085697));
#28909=CARTESIAN_POINT('Ctrl Pts',(3.93300877692551,0.0786798389978914,
31.1581435653024));
#28910=CARTESIAN_POINT('Ctrl Pts',(3.9329999756645,-0.000437519150454106,
31.154163522035));
#28911=CARTESIAN_POINT('',(3.93299844479652,-0.00349760319678261,29.904163522035));
#28912=CARTESIAN_POINT('Ctrl Pts',(3.92653051012146,-0.000442985236362668,
31.1541632103437));
#28913=CARTESIAN_POINT('Ctrl Pts',(3.92715270988084,-0.632035046566581,
31.1223382702328));
#28914=CARTESIAN_POINT('Ctrl Pts',(3.48464175740125,-2.57879812069702,31.024202350667));
#28915=CARTESIAN_POINT('Ctrl Pts',(0.42250134717443,-4.63312290995347,30.8597554516478));
#28916=CARTESIAN_POINT('Ctrl Pts',(-3.67020569990779,-2.85900776625179,
30.6608225132839));
#28917=CARTESIAN_POINT('Ctrl Pts',(-4.38887601457751,1.54340617330452,30.4618895749206));
#28918=CARTESIAN_POINT('Ctrl Pts',(-1.07283271971807,4.52695982339219,30.2629566365571));
#28919=CARTESIAN_POINT('Ctrl Pts',(2.94779101406056,3.42599118849705,30.0770481958641));
#28920=CARTESIAN_POINT('Ctrl Pts',(3.92473384533602,1.0486395575314,29.9574507346254));
#28921=CARTESIAN_POINT('Ctrl Pts',(3.93446900659642,-0.00348448155303831,
29.9041642528413));
#28922=CARTESIAN_POINT('',(3.93485131529986,0.00199336934087166,28.6541629095192));
#28923=CARTESIAN_POINT('Ctrl Pts',(3.93299844479652,-0.00349760319678261,
29.904163522035));
#28924=CARTESIAN_POINT('Ctrl Pts',(3.93284906009518,-0.171478293121667,
29.8956526164004));
#28925=CARTESIAN_POINT('Ctrl Pts',(3.92193455469223,-0.338999641682638,
29.8871417107657));
#28926=CARTESIAN_POINT('Ctrl Pts',(3.90045004247335,-0.504953924798754,
29.8786308051311));
#28927=CARTESIAN_POINT('Ctrl Pts',(3.88905676733525,-0.592959777043594,
29.8741174566975));
#28928=CARTESIAN_POINT('Ctrl Pts',(3.8746917325344,-0.680525562943774,29.8696041082638));
#28929=CARTESIAN_POINT('Ctrl Pts',(3.85738892320343,-0.76748921500402,29.8650907598302));
#28930=CARTESIAN_POINT('Ctrl Pts',(3.83487698049658,-0.880633890837322,
29.8592186358641));
#28931=CARTESIAN_POINT('Ctrl Pts',(3.80734494774706,-0.992976934224231,
29.853346511898));
#28932=CARTESIAN_POINT('Ctrl Pts',(3.77486267961663,-1.10403838250195,29.8474743879319));
#28933=CARTESIAN_POINT('Ctrl Pts',(3.74242252539182,-1.21495583740668,29.8416098772911));
#28934=CARTESIAN_POINT('Ctrl Pts',(3.7050450139926,-1.32459460842593,29.8357453666504));
#28935=CARTESIAN_POINT('Ctrl Pts',(3.66285117170211,-1.43248395940774,29.8298808560096));
#28936=CARTESIAN_POINT('Ctrl Pts',(3.62070074645552,-1.54026229332085,29.8240223798919));
#28937=CARTESIAN_POINT('Ctrl Pts',(3.57374399761799,-1.64629440505415,29.8181639037743));
#28938=CARTESIAN_POINT('Ctrl Pts',(3.52215182078143,-1.75012443882314,29.8123054276566));
#28939=CARTESIAN_POINT('Ctrl Pts',(3.46852529607209,-1.85804862835917,29.8062159440653));
#28940=CARTESIAN_POINT('Ctrl Pts',(3.4098903882644,-1.96359306873341,29.8001264604741));
#28941=CARTESIAN_POINT('Ctrl Pts',(3.34649447006966,-2.06626807597494,29.7940369768829));
#28942=CARTESIAN_POINT('Ctrl Pts',(3.28557421179136,-2.1649335443205,29.7881852923624));
#28943=CARTESIAN_POINT('Ctrl Pts',(3.22025804525689,-2.26094909632023,29.782333607842));
#28944=CARTESIAN_POINT('Ctrl Pts',(3.15081204298773,-2.35390579033306,29.7764819233215));
#28945=CARTESIAN_POINT('Ctrl Pts',(3.0813766327435,-2.4468483064294,29.7706311313102));
#28946=CARTESIAN_POINT('Ctrl Pts',(3.00781288654246,-2.53673256106863,29.7647803392988));
#28947=CARTESIAN_POINT('Ctrl Pts',(2.93042908704734,-2.62318020078433,29.7589295472875));
#28948=CARTESIAN_POINT('Ctrl Pts',(2.85303834711451,-2.70963559386006,29.7530782305273));
#28949=CARTESIAN_POINT('Ctrl Pts',(2.7718271485496,-2.79265345124264,29.7472269137671));
#28950=CARTESIAN_POINT('Ctrl Pts',(2.68714229761701,-2.87189053975906,29.741375597007));
#28951=CARTESIAN_POINT('Ctrl Pts',(2.60242933989278,-2.95115392696188,29.7355223382024));
#28952=CARTESIAN_POINT('Ctrl Pts',(2.51424073904886,-3.02663376783994,29.7296690793978));
#28953=CARTESIAN_POINT('Ctrl Pts',(2.42295764192634,-3.09802602723585,29.7238158205932));
#28954=CARTESIAN_POINT('Ctrl Pts',(2.33157069247588,-3.16949950925204,29.7179559025651));
#28955=CARTESIAN_POINT('Ctrl Pts',(2.23708254557593,-3.23687587283017,29.7120959845369));
#28956=CARTESIAN_POINT('Ctrl Pts',(2.13990476758515,-3.29989342034957,29.7062360665088));
#28957=CARTESIAN_POINT('Ctrl Pts',(2.0426615570153,-3.36295339938721,29.7003722028301));
#28958=CARTESIAN_POINT('Ctrl Pts',(1.94272546489425,-3.421648509518,29.6945083391514));
#28959=CARTESIAN_POINT('Ctrl Pts',(1.84053263822175,-3.47576302524215,29.6886444754728));
#28960=CARTESIAN_POINT('Ctrl Pts',(1.73818905255997,-3.5299573728876,29.6827719611853));
#28961=CARTESIAN_POINT('Ctrl Pts',(1.63358245997928,-3.57955746299714,29.6768994468979));
#28962=CARTESIAN_POINT('Ctrl Pts',(1.52716901295618,-3.6243956469826,29.6710269326105));
#28963=CARTESIAN_POINT('Ctrl Pts',(1.49775861760391,-3.6367879597474,29.6694038955626));
#28964=CARTESIAN_POINT('Ctrl Pts',(1.46821029221,-3.64881682804423,29.6677808585148));
#28965=CARTESIAN_POINT('Ctrl Pts',(1.43853384702914,-3.66047939086557,29.666157821467));
#28966=CARTESIAN_POINT('Ctrl Pts',(1.33116490852846,-3.70267437017299,29.660285697501));
#28967=CARTESIAN_POINT('Ctrl Pts',(1.22175790280795,-3.74021207553294,29.654413573535));
#28968=CARTESIAN_POINT('Ctrl Pts',(1.11075443632941,-3.77289193884141,29.648541449569));
#28969=CARTESIAN_POINT('Ctrl Pts',(0.999894888049307,-3.8055294320582,29.6426769389283));
#28970=CARTESIAN_POINT('Ctrl Pts',(0.887443388095505,-3.83332149255809,
29.6368124282876));
#28971=CARTESIAN_POINT('Ctrl Pts',(0.77386142982746,-3.85611559570319,29.6309479176469));
#28972=CARTESIAN_POINT('Ctrl Pts',(0.660396346264503,-3.87888624394293,
29.6250894415293));
#28973=CARTESIAN_POINT('Ctrl Pts',(0.545803520998237,-3.89666908334398,
29.6192309654117));
#28974=CARTESIAN_POINT('Ctrl Pts',(0.430558873192705,-3.90936159196294,
29.6133724892941));
#28975=CARTESIAN_POINT('Ctrl Pts',(0.310769976266677,-3.92255458300974,
29.6072830057028));
#28976=CARTESIAN_POINT('Ctrl Pts',(0.190277231333197,-3.93024741903001,
29.6011935221116));
#28977=CARTESIAN_POINT('Ctrl Pts',(0.0696263462450617,-3.93238365014256,
29.5951040385203));
#28978=CARTESIAN_POINT('Ctrl Pts',(-0.0463130279333092,-3.93443645976852,
29.5892523539999));
#28979=CARTESIAN_POINT('Ctrl Pts',(-0.162397970760541,-3.93135849208458,
29.5834006694795));
#28980=CARTESIAN_POINT('Ctrl Pts',(-0.278140609956272,-3.9231526609467,
29.5775489849591));
#28981=CARTESIAN_POINT('Ctrl Pts',(-0.393865595883609,-3.91494808137644,
29.5716981929478));
#28982=CARTESIAN_POINT('Ctrl Pts',(-0.509247969722975,-3.90161722266158,
29.5658474009365));
#28983=CARTESIAN_POINT('Ctrl Pts',(-0.623802789209033,-3.88321504428676,
29.5599966089252));
#28984=CARTESIAN_POINT('Ctrl Pts',(-0.738367882946152,-3.86481121544799,
29.554145292165));
#28985=CARTESIAN_POINT('Ctrl Pts',(-0.85210486657937,-3.84133522834515,
29.5482939754049));
#28986=CARTESIAN_POINT('Ctrl Pts',(-0.964537533385841,-3.81289343500313,
29.5424426586448));
#28987=CARTESIAN_POINT('Ctrl Pts',(-1.07700751644763,-3.78444220186703,
29.5365893998403));
#28988=CARTESIAN_POINT('Ctrl Pts',(-1.18817192131121,-3.75102198659634,
29.5307361410357));
#28989=CARTESIAN_POINT('Ctrl Pts',(-1.29756896825033,-3.712789217372,29.5248828822312));
#28990=CARTESIAN_POINT('Ctrl Pts',(-1.40709047566875,-3.67451295091518,
29.5190229642031));
#28991=CARTESIAN_POINT('Ctrl Pts',(-1.51484022133172,-3.63141333858677,
29.513163046175));
#28992=CARTESIAN_POINT('Ctrl Pts',(-1.62037561296927,-3.5836952818138,29.5073031281469));
#28993=CARTESIAN_POINT('Ctrl Pts',(-1.72598206460632,-3.53594509510755,
29.5014392644682));
#28994=CARTESIAN_POINT('Ctrl Pts',(-1.82937082547736,-3.4835704582407,29.4955754007896));
#28995=CARTESIAN_POINT('Ctrl Pts',(-1.93012470408345,-3.42682179675086,
29.489711537111));
#28996=CARTESIAN_POINT('Ctrl Pts',(-2.03102721888446,-3.36998941734139,
29.4838390228236));
#28997=CARTESIAN_POINT('Ctrl Pts',(-2.12928674395181,-3.30877035263574,
29.4779665085362));
#28998=CARTESIAN_POINT('Ctrl Pts',(-2.22451573179629,-3.2434578398664,29.4720939942488));
#28999=CARTESIAN_POINT('Ctrl Pts',(-2.25083498242682,-3.22540686156877,
29.4704709572004));
#29000=CARTESIAN_POINT('Ctrl Pts',(-2.27692294587023,-3.20704343677172,
29.4688479201519));
#29001=CARTESIAN_POINT('Ctrl Pts',(-2.30277191380627,-3.18837427429481,
29.4672248831034));
#29002=CARTESIAN_POINT('Ctrl Pts',(-2.3962930963675,-3.1208295213829,29.4613527591374));
#29003=CARTESIAN_POINT('Ctrl Pts',(-2.48699671889459,-3.04905330606792,
29.4554806351713));
#29004=CARTESIAN_POINT('Ctrl Pts',(-2.57447539394731,-2.97330883797157,
29.4496085112053));
#29005=CARTESIAN_POINT('Ctrl Pts',(-2.66184065116091,-2.89766257408203,
29.4437440005646));
#29006=CARTESIAN_POINT('Ctrl Pts',(-2.7459889661596,-2.81805855689906,29.4378794899239));
#29007=CARTESIAN_POINT('Ctrl Pts',(-2.82654263144434,-2.73480268988965,
29.4320149792831));
#29008=CARTESIAN_POINT('Ctrl Pts',(-2.90701340780886,-2.65163249233916,
29.4261565031655));
#29009=CARTESIAN_POINT('Ctrl Pts',(-2.98389660593065,-2.56481821455995,
29.4202980270479));
#29010=CARTESIAN_POINT('Ctrl Pts',(-3.05684879771777,-2.4747049173369,29.4144395509303));
#29011=CARTESIAN_POINT('Ctrl Pts',(-3.13267759106207,-2.38103833343712,
29.4083500673391));
#29012=CARTESIAN_POINT('Ctrl Pts',(-3.20425864665995,-2.28380750608733,
29.4022605837478));
#29013=CARTESIAN_POINT('Ctrl Pts',(-3.27124959321922,-2.18344111412766,
29.3961711001565));
#29014=CARTESIAN_POINT('Ctrl Pts',(-3.3356244912073,-2.08699410784274,29.3903194156361));
#29015=CARTESIAN_POINT('Ctrl Pts',(-3.39576079631841,-1.98765221011616,
29.3844677311157));
#29016=CARTESIAN_POINT('Ctrl Pts',(-3.45139733971157,-1.88582751157997,
29.3786160465953));
#29017=CARTESIAN_POINT('Ctrl Pts',(-3.50702539732247,-1.78401834352369,
29.372765254584));
#29018=CARTESIAN_POINT('Ctrl Pts',(-3.55815485964579,-1.67972749028393,
29.3669144625727));
#29019=CARTESIAN_POINT('Ctrl Pts',(-3.60456993443571,-1.57339269979307,
29.3610636705614));
#29020=CARTESIAN_POINT('Ctrl Pts',(-3.65098917212453,-1.4670483722933,29.3552123538013));
#29021=CARTESIAN_POINT('Ctrl Pts',(-3.69269301634483,-1.35866012203639,
29.3493610370412));
#29022=CARTESIAN_POINT('Ctrl Pts',(-3.72951363891366,-1.24868611634668,
29.343509720281));
#29023=CARTESIAN_POINT('Ctrl Pts',(-3.76634648219906,-1.13867561042808,
29.3376564614765));
#29024=CARTESIAN_POINT('Ctrl Pts',(-3.79829274992259,-1.02707869435946,
29.331803202672));
#29025=CARTESIAN_POINT('Ctrl Pts',(-3.82523454566782,-0.914368454524485,
29.3259499438675));
#29026=CARTESIAN_POINT('Ctrl Pts',(-3.85220699296083,-0.801529984807069,
29.3200900258394));
#29027=CARTESIAN_POINT('Ctrl Pts',(-3.87416350790446,-0.687576065502403,
29.3142301078113));
#29028=CARTESIAN_POINT('Ctrl Pts',(-3.8910373493969,-0.572989830274792,
29.3083701897832));
#29029=CARTESIAN_POINT('Ctrl Pts',(-3.90792255252973,-0.458326440855689,
29.3025063261045));
#29030=CARTESIAN_POINT('Ctrl Pts',(-3.91971822575057,-0.343030298011647,
29.2966424624259));
#29031=CARTESIAN_POINT('Ctrl Pts',(-3.92640965909689,-0.227587760986074,
29.2907785987473));
#29032=CARTESIAN_POINT('Ctrl Pts',(-3.9331109639162,-0.111974918462815,
29.2849060844599));
#29033=CARTESIAN_POINT('Ctrl Pts',(-3.93469299478883,0.00378433744485622,
29.2790335701725));
#29034=CARTESIAN_POINT('Ctrl Pts',(-3.93119308337595,0.119205458000484,
29.2731610558851));
#29035=CARTESIAN_POINT('Ctrl Pts',(-3.93022578289592,0.151105381212052,
29.2715380188368));
#29036=CARTESIAN_POINT('Ctrl Pts',(-3.92887060135923,0.182979519471364,
29.2699149817884));
#29037=CARTESIAN_POINT('Ctrl Pts',(-3.92712901867379,0.214817761579978,
29.26829194474));
#29038=CARTESIAN_POINT('Ctrl Pts',(-3.92082799835126,0.330008049263163,
29.262419820774));
#29039=CARTESIAN_POINT('Ctrl Pts',(-3.9094439864485,0.44511398524188,29.2565476968079));
#29040=CARTESIAN_POINT('Ctrl Pts',(-3.89297832766679,0.559650551966735,
29.2506755728419));
#29041=CARTESIAN_POINT('Ctrl Pts',(-3.87653401693863,0.674038619758618,
29.2448110622012));
#29042=CARTESIAN_POINT('Ctrl Pts',(-3.85502121966352,0.787858380882195,
29.2389465515604));
#29043=CARTESIAN_POINT('Ctrl Pts',(-3.82849324241835,0.900626722209053,
29.2330820409197));
#29044=CARTESIAN_POINT('Ctrl Pts',(-3.80199256219786,1.01327902603453,29.2272235648021));
#29045=CARTESIAN_POINT('Ctrl Pts',(-3.77048706072516,1.12488166201034,29.2213650886845));
#29046=CARTESIAN_POINT('Ctrl Pts',(-3.73408151598168,1.23495920256662,29.2155066125669));
#29047=CARTESIAN_POINT('Ctrl Pts',(-3.69624045238501,1.34937724635927,29.2094171289756));
#29048=CARTESIAN_POINT('Ctrl Pts',(-3.65310502984808,1.46214699686952,29.2033276453843));
#29049=CARTESIAN_POINT('Ctrl Pts',(-3.60485095711975,1.57274873293632,29.1972381617931));
#29050=CARTESIAN_POINT('Ctrl Pts',(-3.55848124346512,1.67903138517994,29.1913864772726));
#29051=CARTESIAN_POINT('Ctrl Pts',(-3.50738533304776,1.78331175617564,29.1855347927522));
#29052=CARTESIAN_POINT('Ctrl Pts',(-3.45176885416513,1.88514741530087,29.1796831082318));
#29053=CARTESIAN_POINT('Ctrl Pts',(-3.3961608580045,1.98696754227442,29.1738323162205));
#29054=CARTESIAN_POINT('Ctrl Pts',(-3.33603386239109,2.08634333603473,29.1679815242092));
#29055=CARTESIAN_POINT('Ctrl Pts',(-3.27163960388811,2.18285668385967,29.1621307321978));
#29056=CARTESIAN_POINT('Ctrl Pts',(-3.20723956995999,2.27937868782305,29.1562794154377));
#29057=CARTESIAN_POINT('Ctrl Pts',(-3.13857174178334,2.3730373915834,29.1504280986775));
#29058=CARTESIAN_POINT('Ctrl Pts',(-3.06593095492429,2.46344400781447,29.1445767819174));
#29059=CARTESIAN_POINT('Ctrl Pts',(-2.99326605868294,2.55388062988341,29.1387235231128));
#29060=CARTESIAN_POINT('Ctrl Pts',(-2.91662584057487,2.64106269607758,29.1328702643083));
#29061=CARTESIAN_POINT('Ctrl Pts',(-2.83634467020339,2.72463537226706,29.1270170055037));
#29062=CARTESIAN_POINT('Ctrl Pts',(-2.75597216434142,2.8083031286769,29.1211570874756));
#29063=CARTESIAN_POINT('Ctrl Pts',(-2.67195072487592,2.8883530005291,29.1152971694475));
#29064=CARTESIAN_POINT('Ctrl Pts',(-2.58465081727061,2.96446776888911,29.1094372514193));
#29065=CARTESIAN_POINT('Ctrl Pts',(-2.49729212813907,3.04063378750099,29.1035733877407));
#29066=CARTESIAN_POINT('Ctrl Pts',(-2.40665089786219,3.11285916971107,29.097709524062));
#29067=CARTESIAN_POINT('Ctrl Pts',(-2.31312842094905,3.18086873482666,29.0918456603834));
#29068=CARTESIAN_POINT('Ctrl Pts',(-2.21946797589712,3.24897863040214,29.085973146096));
#29069=CARTESIAN_POINT('Ctrl Pts',(-2.122918144424,3.31286006896241,29.0801006318086));
#29070=CARTESIAN_POINT('Ctrl Pts',(-2.02390681817594,3.37228263811634,29.0742281175212));
#29071=CARTESIAN_POINT('Ctrl Pts',(-1.99654221030443,3.38870576227026,29.072605080473));
#29072=CARTESIAN_POINT('Ctrl Pts',(-1.96898970831987,3.40478857424379,29.0709820434247));
#29073=CARTESIAN_POINT('Ctrl Pts',(-1.94125861987231,3.42052685573019,29.0693590063765));
#29074=CARTESIAN_POINT('Ctrl Pts',(-1.84092795320357,3.47746772470245,29.0634868824105));
#29075=CARTESIAN_POINT('Ctrl Pts',(-1.73792168060312,3.53008597276691,29.0576147584445));
#29076=CARTESIAN_POINT('Ctrl Pts',(-1.63264864272382,3.57812065327765,29.0517426344785));
#29077=CARTESIAN_POINT('Ctrl Pts',(-1.52751209342835,3.62609305587136,29.0458781238377));
#29078=CARTESIAN_POINT('Ctrl Pts',(-1.42011499590566,3.66949353873066,29.0400136131971));
#29079=CARTESIAN_POINT('Ctrl Pts',(-1.31089266583091,3.70810590715405,29.0341491025563));
#29080=CARTESIAN_POINT('Ctrl Pts',(-1.2017827244472,3.74667854383446,29.0282906264388));
#29081=CARTESIAN_POINT('Ctrl Pts',(-1.09085167365963,3.7804727289979,29.0224321503212));
#29082=CARTESIAN_POINT('Ctrl Pts',(-0.978556174649823,3.80931973100903,
29.0165736742036));
#29083=CARTESIAN_POINT('Ctrl Pts',(-0.861832715363183,3.83930420852128,
29.0104841906123));
#29084=CARTESIAN_POINT('Ctrl Pts',(-0.743635404108951,3.86394313950291,
29.004394707021));
#29085=CARTESIAN_POINT('Ctrl Pts',(-0.624496499827956,3.88310354249055,
28.9983052234298));
#29086=CARTESIAN_POINT('Ctrl Pts',(-0.510010062430147,3.90151571683778,
28.9924535389094));
#29087=CARTESIAN_POINT('Ctrl Pts',(-0.394654638485822,3.91486914347265,
28.986601854389));
#29088=CARTESIAN_POINT('Ctrl Pts',(-0.278913618405177,3.92309778025837,
28.9807501698686));
#29089=CARTESIAN_POINT('Ctrl Pts',(-0.16319025134603,3.9313251619981,28.9748993778573));
#29090=CARTESIAN_POINT('Ctrl Pts',(-0.0470818173448765,3.93442927872797,
28.969048585846));
#29091=CARTESIAN_POINT('Ctrl Pts',(0.0689238407894238,3.93239602585635,
28.9631977938347));
#29092=CARTESIAN_POINT('Ctrl Pts',(0.184939903298399,3.93036259062531,28.9573464770746));
#29093=CARTESIAN_POINT('Ctrl Pts',(0.300852758242594,3.92319087708354,28.9514951603145));
#29094=CARTESIAN_POINT('Ctrl Pts',(0.416175949978906,3.91091889185383,28.9456438435544));
#29095=CARTESIAN_POINT('Ctrl Pts',(0.531537417332094,3.89864283356822,28.9397905847499));
#29096=CARTESIAN_POINT('Ctrl Pts',(0.646308421449583,3.88126318134766,28.9339373259454));
#29097=CARTESIAN_POINT('Ctrl Pts',(0.760009714199924,3.85886955393957,28.9280840671409));
#29098=CARTESIAN_POINT('Ctrl Pts',(0.873840364348574,3.83645044941235,28.9222241491128));
#29099=CARTESIAN_POINT('Ctrl Pts',(0.986598468157101,3.80900606385187,28.9163642310847));
#29100=CARTESIAN_POINT('Ctrl Pts',(1.0978169241759,3.77667671385743,28.9105043130566));
#29101=CARTESIAN_POINT('Ctrl Pts',(1.20911026676409,3.74432559558641,28.904640449378));
#29102=CARTESIAN_POINT('Ctrl Pts',(1.31886150678038,3.70708309598909,28.8987765856994));
#29103=CARTESIAN_POINT('Ctrl Pts',(1.42662225710485,3.66513818778134,28.8929127220207));
#29104=CARTESIAN_POINT('Ctrl Pts',(1.5345419804447,3.62313140074927,28.8870402077334));
#29105=CARTESIAN_POINT('Ctrl Pts',(1.64046497664927,3.57640852599884,28.881167693446));
#29106=CARTESIAN_POINT('Ctrl Pts',(1.7439661568167,3.52520510663961,28.8752951791586));
#29107=CARTESIAN_POINT('Ctrl Pts',(1.77257166405825,3.51105357927631,28.8736721421101));
#29108=CARTESIAN_POINT('Ctrl Pts',(1.80099234655962,3.49656006303404,28.8720491050617));
#29109=CARTESIAN_POINT('Ctrl Pts',(1.8292196254935,3.48173011040623,28.8704260680132));
#29110=CARTESIAN_POINT('Ctrl Pts',(1.93134550196597,3.42807556177944,28.8645539440471));
#29111=CARTESIAN_POINT('Ctrl Pts',(2.03127990206342,3.36983392803109,28.8586818200811));
#29112=CARTESIAN_POINT('Ctrl Pts',(2.12858233824638,3.30720822285286,28.8528096961151));
#29113=CARTESIAN_POINT('Ctrl Pts',(2.22575861988876,3.24466371314491,28.8469451854744));
#29114=CARTESIAN_POINT('Ctrl Pts',(2.32030937920909,3.17774665716709,28.8410806748336));
#29115=CARTESIAN_POINT('Ctrl Pts',(2.41181747910689,3.10670652741363,28.8352161641929));
#29116=CARTESIAN_POINT('Ctrl Pts',(2.50323141808017,3.03573949724703,28.8293576880753));
#29117=CARTESIAN_POINT('Ctrl Pts',(2.59160860048117,2.96065808403047,28.8234992119577));
#29118=CARTESIAN_POINT('Ctrl Pts',(2.67656029262184,2.88175536782012,28.8176407358401));
#29119=CARTESIAN_POINT('Ctrl Pts',(2.76486174251365,2.79974141299225,28.8115512522488));
#29120=CARTESIAN_POINT('Ctrl Pts',(2.84946161860741,2.71359884353586,28.8054617686576));
#29121=CARTESIAN_POINT('Ctrl Pts',(2.92996041982669,2.62370366814718,28.7993722850663));
#29122=CARTESIAN_POINT('Ctrl Pts',(3.00731568024349,2.53731896928115,28.7935206005459));
#29123=CARTESIAN_POINT('Ctrl Pts',(3.08088385372034,2.44746958593525,28.7876689160255));
#29124=CARTESIAN_POINT('Ctrl Pts',(3.15034817072902,2.35452657729411,28.7818172315051));
#29125=CARTESIAN_POINT('Ctrl Pts',(3.2198018929194,2.26159774448211,28.7759664394938));
#29126=CARTESIAN_POINT('Ctrl Pts',(3.28515275575619,2.16557655560454,28.7701156474824));
#29127=CARTESIAN_POINT('Ctrl Pts',(3.34612528628986,2.06686588061528,28.7642648554711));
#29128=CARTESIAN_POINT('Ctrl Pts',(3.407103285359,1.96814635241258,28.758413538711));
#29129=CARTESIAN_POINT('Ctrl Pts',(3.46370195423207,1.8667372103279,28.7525622219508));
#29130=CARTESIAN_POINT('Ctrl Pts',(3.51569041806618,1.76306831527246,28.7467109051907));
#29131=CARTESIAN_POINT('Ctrl Pts',(3.5676961368035,1.65936501264622,28.7408576463862));
#29132=CARTESIAN_POINT('Ctrl Pts',(3.61508842273111,1.55340083505744,28.7350043875816));
#29133=CARTESIAN_POINT('Ctrl Pts',(3.6576837241685,1.4456274672103,28.7291511287771));
#29134=CARTESIAN_POINT('Ctrl Pts',(3.70032748606968,1.33773148613555,28.723291210749));
#29135=CARTESIAN_POINT('Ctrl Pts',(3.73816321839806,1.22802259117911,28.7174312927208));
#29136=CARTESIAN_POINT('Ctrl Pts',(3.77105659219758,1.11696964078851,28.7115713746927));
#29137=CARTESIAN_POINT('Ctrl Pts',(3.80397211404706,1.00584191526814,28.7057075110141));
#29138=CARTESIAN_POINT('Ctrl Pts',(3.83193855149017,0.893368732516753,28.6998436473354));
#29139=CARTESIAN_POINT('Ctrl Pts',(3.85487262910747,0.7800294951847,28.6939797836568));
#29140=CARTESIAN_POINT('Ctrl Pts',(3.87784054000324,0.666523055227682,28.6881072693694));
#29141=CARTESIAN_POINT('Ctrl Pts',(3.89576121051136,0.552148417660778,28.682234755082));
#29142=CARTESIAN_POINT('Ctrl Pts',(3.90860314062828,0.437390545246166,28.6763622407945));
#29143=CARTESIAN_POINT('Ctrl Pts',(3.91215237479467,0.405673929602851,28.6747392037462));
#29144=CARTESIAN_POINT('Ctrl Pts',(3.91531397558892,0.373928040308329,28.6731161666979));
#29145=CARTESIAN_POINT('Ctrl Pts',(3.91808797956127,0.342163096223857,28.6714931296496));
#29146=CARTESIAN_POINT('Ctrl Pts',(3.92796091097148,0.229108782920413,28.6657165937781));
#29147=CARTESIAN_POINT('Ctrl Pts',(3.93294158348204,0.115621047768071,28.6599400579065));
#29148=CARTESIAN_POINT('Ctrl Pts',(3.93299948919698,0.00200448904475932,
28.654163522035));
#29149=CARTESIAN_POINT('',(3.9313993161518,0.00256731592070132,27.4041640341379));
#29150=CARTESIAN_POINT('Ctrl Pts',(3.93827238435518,0.00197282676680643,
28.6541617779557));
#29151=CARTESIAN_POINT('Ctrl Pts',(3.93085187581135,-1.19024594622667,28.5936279157326));
#29152=CARTESIAN_POINT('Ctrl Pts',(2.71699568782789,-3.70151452867356,28.466783074055));
#29153=CARTESIAN_POINT('Ctrl Pts',(-1.56021230829742,-4.38292970969908,
28.2736272529227));
#29154=CARTESIAN_POINT('Ctrl Pts',(-4.5310375107926,-1.05547826263657,28.0746943145594));
#29155=CARTESIAN_POINT('Ctrl Pts',(-3.33645939605003,3.24227913444184,27.8757613761959));
#29156=CARTESIAN_POINT('Ctrl Pts',(0.925340961511961,4.55939462999849,27.6768284378326));
#29157=CARTESIAN_POINT('Ctrl Pts',(3.62084980531289,2.28804957005642,27.5196296619495));
#29158=CARTESIAN_POINT('Ctrl Pts',(3.93111323275754,0.489805113098635,27.4287418655209));
#29159=CARTESIAN_POINT('Ctrl Pts',(3.92823021849111,0.00258536452941557,
27.4041650485469));
#29160=CARTESIAN_POINT('',(3.93299891753245,-0.00291799392896185,26.1541635219892));
#29161=CARTESIAN_POINT('Ctrl Pts',(3.93299916801287,0.00255820446269878,
27.404163522035));
#29162=CARTESIAN_POINT('Ctrl Pts',(3.93307519995185,-0.114333762974888,
27.3982742678373));
#29163=CARTESIAN_POINT('Ctrl Pts',(3.9279357123882,-0.231251489364913,27.3923850136396));
#29164=CARTESIAN_POINT('Ctrl Pts',(3.91760045126501,-0.347700595697167,
27.3864957594419));
#29165=CARTESIAN_POINT('Ctrl Pts',(3.90726448546451,-0.46415764174605,27.3806061037039));
#29166=CARTESIAN_POINT('Ctrl Pts',(3.89173207666385,-0.580145599958414,
27.3747164479659));
#29167=CARTESIAN_POINT('Ctrl Pts',(3.87107488587756,-0.695174962098055,
27.3688267922279));
#29168=CARTESIAN_POINT('Ctrl Pts',(3.85041152868984,-0.810238661782951,
27.362935378362));
#29169=CARTESIAN_POINT('Ctrl Pts',(3.82462041725161,-0.924342796774363,
27.3570439644962));
#29170=CARTESIAN_POINT('Ctrl Pts',(3.79382426704607,-1.03700840438847,27.3511525506304));
#29171=CARTESIAN_POINT('Ctrl Pts',(3.76237774431294,-1.15205335537857,27.34513671817));
#29172=CARTESIAN_POINT('Ctrl Pts',(3.72571251901386,-1.26559790615674,27.3391208857096));
#29173=CARTESIAN_POINT('Ctrl Pts',(3.68401224682527,-1.37715023335924,27.3331050532492));
#29174=CARTESIAN_POINT('Ctrl Pts',(3.64309724419288,-1.48660188730765,27.3272025066222));
#29175=CARTESIAN_POINT('Ctrl Pts',(3.59733538762402,-1.59413534420948,27.3212999599951));
#29176=CARTESIAN_POINT('Ctrl Pts',(3.54694774865305,-1.69930887961109,27.3153974133681));
#29177=CARTESIAN_POINT('Ctrl Pts',(3.49510949708227,-1.80751026189607,27.309324937991));
#29178=CARTESIAN_POINT('Ctrl Pts',(3.4383753150512,-1.91321337510273,27.3032524626139));
#29179=CARTESIAN_POINT('Ctrl Pts',(3.37703446391673,-2.01596806262367,27.2971799872368));
#29180=CARTESIAN_POINT('Ctrl Pts',(3.31569361278226,-2.11872275014462,27.2911075118597));
#29181=CARTESIAN_POINT('Ctrl Pts',(3.24974640496889,-2.21852866757598,27.2850350364827));
#29182=CARTESIAN_POINT('Ctrl Pts',(3.17952701572385,-2.31497234460419,27.2789625611056));
#29183=CARTESIAN_POINT('Ctrl Pts',(3.11162440058551,-2.40823401996453,27.2730904371395));
#29184=CARTESIAN_POINT('Ctrl Pts',(3.03950115054566,-2.49866194169357,27.2672183131735));
#29185=CARTESIAN_POINT('Ctrl Pts',(2.9634220343367,-2.58584973391876,27.2613461892074));
#29186=CARTESIAN_POINT('Ctrl Pts',(2.88744155621256,-2.6729244854401,27.2554816785667));
#29187=CARTESIAN_POINT('Ctrl Pts',(2.8075156806553,-2.75676715289067,27.249617167926));
#29188=CARTESIAN_POINT('Ctrl Pts',(2.72395175620044,-2.83700120371714,27.2437526572853));
#29189=CARTESIAN_POINT('Ctrl Pts',(2.64047381819258,-2.91715269450347,27.2378941811677));
#29190=CARTESIAN_POINT('Ctrl Pts',(2.55336557373104,-2.99370266985687,27.23203570505));
#29191=CARTESIAN_POINT('Ctrl Pts',(2.46297339702857,-3.06630902642404,27.2261772289324));
#29192=CARTESIAN_POINT('Ctrl Pts',(2.36901693706222,-3.14177834780746,27.2200877453412));
#29193=CARTESIAN_POINT('Ctrl Pts',(2.27151253645968,-3.21298630502254,27.2139982617499));
#29194=CARTESIAN_POINT('Ctrl Pts',(2.17089018282556,-3.27959217191888,27.2079087781587));
#29195=CARTESIAN_POINT('Ctrl Pts',(2.07419721036827,-3.34359702790466,27.2020570936382));
#29196=CARTESIAN_POINT('Ctrl Pts',(1.9746256093274,-3.40335222937345,27.1962054091178));
#29197=CARTESIAN_POINT('Ctrl Pts',(1.87258846806653,-3.45859818846657,27.1903537245974));
#29198=CARTESIAN_POINT('Ctrl Pts',(1.77056688968782,-3.51383572134998,27.1845029325861));
#29199=CARTESIAN_POINT('Ctrl Pts',(1.66608088223749,-3.56456518255443,27.1786521405748));
#29200=CARTESIAN_POINT('Ctrl Pts',(1.55956901731533,-3.61057245879793,27.1728013485634));
#29201=CARTESIAN_POINT('Ctrl Pts',(1.45304759950266,-3.6565838613655,27.1669500318033));
#29202=CARTESIAN_POINT('Ctrl Pts',(1.34450034256658,-3.69787207309991,27.1610987150432));
#29203=CARTESIAN_POINT('Ctrl Pts',(1.23438605355836,-3.73427102267372,27.155247398283));
#29204=CARTESIAN_POINT('Ctrl Pts',(1.12423521776118,-3.77068205301144,27.1493941394785));
#29205=CARTESIAN_POINT('Ctrl Pts',(1.0125167080311,-3.80220046479399,27.1435408806739));
#29206=CARTESIAN_POINT('Ctrl Pts',(0.899704059038655,-3.82871017526129,
27.1376876218694));
#29207=CARTESIAN_POINT('Ctrl Pts',(0.786763063653723,-3.85525004569501,
27.1318277038413));
#29208=CARTESIAN_POINT('Ctrl Pts',(0.67272584711545,-3.87676974638077,27.1259677858131));
#29209=CARTESIAN_POINT('Ctrl Pts',(0.558075795282372,-3.89320438799711,
27.120107867785));
#29210=CARTESIAN_POINT('Ctrl Pts',(0.443348546288052,-3.90965009552802,
27.1142440041064));
#29211=CARTESIAN_POINT('Ctrl Pts',(0.328008050772991,-3.9210038859026,27.1083801404277));
#29212=CARTESIAN_POINT('Ctrl Pts',(0.212540720776185,-3.9272529129166,27.1025162767491));
#29213=CARTESIAN_POINT('Ctrl Pts',(0.0969030487063048,-3.93351115874788,
27.0966437624617));
#29214=CARTESIAN_POINT('Ctrl Pts',(-0.0188614194399131,-3.93464960718321,
27.0907712481743));
#29215=CARTESIAN_POINT('Ctrl Pts',(-0.134268281532253,-3.9307074463224,
27.0848987338869));
#29216=CARTESIAN_POINT('Ctrl Pts',(-0.166164264007384,-3.92961791757644,
27.0832756968387));
#29217=CARTESIAN_POINT('Ctrl Pts',(-0.198032975421836,-3.92814060942531,
27.0816526597904));
#29218=CARTESIAN_POINT('Ctrl Pts',(-0.229864310322165,-3.92627704051053,
27.0800296227422));
#29219=CARTESIAN_POINT('Ctrl Pts',(-0.345029607838136,-3.91953467581914,
27.0741574987762));
#29220=CARTESIAN_POINT('Ctrl Pts',(-0.460091077063926,-3.90770968008658,
27.0682853748102));
#29221=CARTESIAN_POINT('Ctrl Pts',(-0.574563709163602,-3.89080525651338,
27.0624132508441));
#29222=CARTESIAN_POINT('Ctrl Pts',(-0.688887925223019,-3.87392274986097,
27.0565487402034));
#29223=CARTESIAN_POINT('Ctrl Pts',(-0.802624417162336,-3.85197397153163,
27.0506842295627));
#29224=CARTESIAN_POINT('Ctrl Pts',(-0.915290279662149,-3.82501407892258,
27.044819718922));
#29225=CARTESIAN_POINT('Ctrl Pts',(-1.02784021010985,-3.79808192777493,
27.0389612428044));
#29226=CARTESIAN_POINT('Ctrl Pts',(-1.1393213027452,-3.76614901427624,27.0331027666868));
#29227=CARTESIAN_POINT('Ctrl Pts',(-1.24925853498102,-3.72932193740056,
27.0272442905692));
#29228=CARTESIAN_POINT('Ctrl Pts',(-1.36353073791085,-3.69104272010116,
27.0211548069779));
#29229=CARTESIAN_POINT('Ctrl Pts',(-1.47613437252862,-3.64747549872449,
27.0150653233866));
#29230=CARTESIAN_POINT('Ctrl Pts',(-1.58655039477642,-3.59879797221722,
27.0089758397954));
#29231=CARTESIAN_POINT('Ctrl Pts',(-1.69265458546978,-3.55202134098325,
27.003124155275));
#29232=CARTESIAN_POINT('Ctrl Pts',(-1.79673839959033,-3.50052622010324,
26.9972724707546));
#29233=CARTESIAN_POINT('Ctrl Pts',(-1.89836019769812,-3.44451993168795,
26.9914207862342));
#29234=CARTESIAN_POINT('Ctrl Pts',(-1.99996649627277,-3.38852218544903,
26.9855699942228));
#29235=CARTESIAN_POINT('Ctrl Pts',(-2.09911116350132,-3.32801483922482,
26.9797192022115));
#29236=CARTESIAN_POINT('Ctrl Pts',(-2.19537705434519,-3.26325122987101,
26.9738684102002));
#29237=CARTESIAN_POINT('Ctrl Pts',(-2.29165157913323,-3.19848181196566,
26.9680170934401));
#29238=CARTESIAN_POINT('Ctrl Pts',(-2.38504647123913,-3.12945560284909,
26.9621657766799));
#29239=CARTESIAN_POINT('Ctrl Pts',(-2.47517407595333,-3.05646892569327,
26.9563144599198));
#29240=CARTESIAN_POINT('Ctrl Pts',(-2.5653315939017,-2.98345802435473,26.9504612011153));
#29241=CARTESIAN_POINT('Ctrl Pts',(-2.65221934707568,-2.90648430126828,
26.9446079423108));
#29242=CARTESIAN_POINT('Ctrl Pts',(-2.73548378520081,-2.8258834832497,26.9387546835063));
#29243=CARTESIAN_POINT('Ctrl Pts',(-2.81884295286556,-2.74519096607892,
26.9328947654781));
#29244=CARTESIAN_POINT('Ctrl Pts',(-2.89857028040766,-2.6608634052442,26.92703484745));
#29245=CARTESIAN_POINT('Ctrl Pts',(-2.97434997078541,-2.57327247902137,
26.9211749294219));
#29246=CARTESIAN_POINT('Ctrl Pts',(-3.05018068579772,-2.48562257532082,
26.9153110657433));
#29247=CARTESIAN_POINT('Ctrl Pts',(-3.12205821516957,-2.39470525445772,
26.9094472020646));
#29248=CARTESIAN_POINT('Ctrl Pts',(-3.18970891792442,-2.30092286244311,
26.903583338386));
#29249=CARTESIAN_POINT('Ctrl Pts',(-3.25745942173073,-2.20700211885269,
26.8977108240986));
#29250=CARTESIAN_POINT('Ctrl Pts',(-3.3209704279018,-2.11020821281976,26.8918383098112));
#29251=CARTESIAN_POINT('Ctrl Pts',(-3.38001316534995,-2.01096991575235,
26.8859657955238));
#29252=CARTESIAN_POINT('Ctrl Pts',(-3.39633131216491,-1.98354257801018,
26.8843427584754));
#29253=CARTESIAN_POINT('Ctrl Pts',(-3.41230842931787,-1.95592865155582,
26.8827197214271));
#29254=CARTESIAN_POINT('Ctrl Pts',(-3.42794033419846,-1.92813746013487,
26.8810966843787));
#29255=CARTESIAN_POINT('Ctrl Pts',(-3.48449633418438,-1.82758934180772,
26.8752245604127));
#29256=CARTESIAN_POINT('Ctrl Pts',(-3.53671949250614,-1.72438220077894,
26.8693524364467));
#29257=CARTESIAN_POINT('Ctrl Pts',(-3.58435043104511,-1.61892587460535,
26.8634803124806));
#29258=CARTESIAN_POINT('Ctrl Pts',(-3.63191961512657,-1.51360627465245,
26.8576158018399));
#29259=CARTESIAN_POINT('Ctrl Pts',(-3.67490825098176,-1.40604366192818,
26.8517512911992));
#29260=CARTESIAN_POINT('Ctrl Pts',(-3.71310181355593,-1.2966741773351,26.8458867805585));
#29261=CARTESIAN_POINT('Ctrl Pts',(-3.75125607533416,-1.18741723285364,
26.8400283044409));
#29262=CARTESIAN_POINT('Ctrl Pts',(-3.78462494247863,-1.07635750259455,
26.8341698283233));
#29263=CARTESIAN_POINT('Ctrl Pts',(-3.8130414344448,-0.963952290939315,
26.8283113522057));
#29264=CARTESIAN_POINT('Ctrl Pts',(-3.84257842633071,-0.847114792892496,
26.8222218686144));
#29265=CARTESIAN_POINT('Ctrl Pts',(-3.86676426336712,-0.728823936971667,
26.8161323850232));
#29266=CARTESIAN_POINT('Ctrl Pts',(-3.88546800459745,-0.609612487773617,
26.8100429014319));
#29267=CARTESIAN_POINT('Ctrl Pts',(-3.90344135018425,-0.495056338393972,
26.8041912169115));
#29268=CARTESIAN_POINT('Ctrl Pts',(-3.9163526553811,-0.379650593153888,
26.7983395323911));
#29269=CARTESIAN_POINT('Ctrl Pts',(-3.92413773081026,-0.263878891977561,
26.7924878478707));
#29270=CARTESIAN_POINT('Ctrl Pts',(-3.93192161884617,-0.14812484850251,
26.7866370558594));
#29271=CARTESIAN_POINT('Ctrl Pts',(-3.93458080397028,-0.0320053724387077,
26.7807862638481));
#29272=CARTESIAN_POINT('Ctrl Pts',(-3.93210305102959,0.0839916429399632,
26.7749354718369));
#29273=CARTESIAN_POINT('Ctrl Pts',(-3.92962507586293,0.199999061918414,
26.7690841550767));
#29274=CARTESIAN_POINT('Ctrl Pts',(-3.92200925558307,0.315883585034949,
26.7632328383166));
#29275=CARTESIAN_POINT('Ctrl Pts',(-3.90929546055342,0.431158905853051,
26.7573815215565));
#29276=CARTESIAN_POINT('Ctrl Pts',(-3.89657744583184,0.546472486399326,
26.751528262752));
#29277=CARTESIAN_POINT('Ctrl Pts',(-3.87875813720348,0.661176051894913,
26.7456750039475));
#29278=CARTESIAN_POINT('Ctrl Pts',(-3.85592898915947,0.774790701131377,
26.739821745143));
#29279=CARTESIAN_POINT('Ctrl Pts',(-3.8330738685066,0.88853460919251,26.7339618271149));
#29280=CARTESIAN_POINT('Ctrl Pts',(-3.8051976135385,1.00118672272018,26.7281019090868));
#29281=CARTESIAN_POINT('Ctrl Pts',(-3.77244232968183,1.11228048136462,26.7222419910587));
#29282=CARTESIAN_POINT('Ctrl Pts',(-3.73966499075515,1.22344904261603,26.7163781273801));
#29283=CARTESIAN_POINT('Ctrl Pts',(-3.70200221550103,1.33305676963155,26.7105142637015));
#29284=CARTESIAN_POINT('Ctrl Pts',(-3.65964469339519,1.44065600269614,26.7046504000229));
#29285=CARTESIAN_POINT('Ctrl Pts',(-3.61722468376027,1.54841397049948,26.6987778857355));
#29286=CARTESIAN_POINT('Ctrl Pts',(-3.570096272167,1.65415715453806,26.6929053714481));
#29287=CARTESIAN_POINT('Ctrl Pts',(-3.51849662886788,1.75746137159409,26.6870328571607));
#29288=CARTESIAN_POINT('Ctrl Pts',(-3.50423559370246,1.78601244245387,26.6854098201123));
#29289=CARTESIAN_POINT('Ctrl Pts',(-3.48963328038741,1.81437737948408,26.6837867830638));
#29290=CARTESIAN_POINT('Ctrl Pts',(-3.47469527424812,1.84254762519664,26.6821637460153));
#29291=CARTESIAN_POINT('Ctrl Pts',(-3.42064978961872,1.94446715632202,26.6762916220493));
#29292=CARTESIAN_POINT('Ctrl Pts',(-3.36202565092841,2.04417765018983,26.6704194980833));
#29293=CARTESIAN_POINT('Ctrl Pts',(-3.29902755825575,2.14123940041022,26.6645473741172));
#29294=CARTESIAN_POINT('Ctrl Pts',(-3.23611114386123,2.23817530814402,26.6586828634765));
#29295=CARTESIAN_POINT('Ctrl Pts',(-3.16883227587662,2.33246895793811,26.6528183528358));
#29296=CARTESIAN_POINT('Ctrl Pts',(-3.09744202336682,2.42370417169284,26.6469538421951));
#29297=CARTESIAN_POINT('Ctrl Pts',(-3.02612523071658,2.51484550532033,26.6410953660774));
#29298=CARTESIAN_POINT('Ctrl Pts',(-2.95070572158423,2.60293433901684,26.6352368899598));
#29299=CARTESIAN_POINT('Ctrl Pts',(-2.87147806343919,2.68758306498376,26.6293784138422));
#29300=CARTESIAN_POINT('Ctrl Pts',(-2.78912635378587,2.77556960234411,26.623288930251));
#29301=CARTESIAN_POINT('Ctrl Pts',(-2.70266024364889,2.85983877289536,26.6171994466597));
#29302=CARTESIAN_POINT('Ctrl Pts',(-2.61245726978781,2.93999251929879,26.6111099630684));
#29303=CARTESIAN_POINT('Ctrl Pts',(-2.52577679221898,3.01701619955882,26.605258278548));
#29304=CARTESIAN_POINT('Ctrl Pts',(-2.43564616711349,3.09023954456902,26.5994065940276));
#29305=CARTESIAN_POINT('Ctrl Pts',(-2.34243766474161,3.15934720896578,26.5935549095072));
#29306=CARTESIAN_POINT('Ctrl Pts',(-2.24924337869259,3.2284443329414,26.5877041174958));
#29307=CARTESIAN_POINT('Ctrl Pts',(-2.15297248077676,3.29342677827433,26.5818533254845));
#29308=CARTESIAN_POINT('Ctrl Pts',(-2.05402889355832,3.3540206177702,26.5760025334732));
#29309=CARTESIAN_POINT('Ctrl Pts',(-1.95507643223684,3.41461989183732,26.5701512167131));
#29310=CARTESIAN_POINT('Ctrl Pts',(-1.85345115766715,3.47082956169215,26.5642998999529));
#29311=CARTESIAN_POINT('Ctrl Pts',(-1.74958381227985,3.52242040134455,26.5584485831928));
#29312=CARTESIAN_POINT('Ctrl Pts',(-1.64568199345628,3.57402836392925,26.5525953243882));
#29313=CARTESIAN_POINT('Ctrl Pts',(-1.53953699419985,3.62101426426516,26.5467420655837));
#29314=CARTESIAN_POINT('Ctrl Pts',(-1.43160119923916,3.66319628280236,26.5408888067792));
#29315=CARTESIAN_POINT('Ctrl Pts',(-1.32354260625827,3.70542629161346,26.535028888751));
#29316=CARTESIAN_POINT('Ctrl Pts',(-1.2136895363001,3.74284135935602,26.5291689707229));
#29317=CARTESIAN_POINT('Ctrl Pts',(-1.10251135909697,3.77530895465022,26.5233090526948));
#29318=CARTESIAN_POINT('Ctrl Pts',(-0.991258322445518,3.80779841130546,
26.5174451890161));
#29319=CARTESIAN_POINT('Ctrl Pts',(-0.878678802535022,3.83533366431276,
26.5115813253375));
#29320=CARTESIAN_POINT('Ctrl Pts',(-0.765252517594276,3.85783327585779,
26.5057174616589));
#29321=CARTESIAN_POINT('Ctrl Pts',(-0.651658901612614,3.88036607973933,
26.4998449473715));
#29322=CARTESIAN_POINT('Ctrl Pts',(-0.537216434607124,3.89784835349429,
26.4939724330841));
#29323=CARTESIAN_POINT('Ctrl Pts',(-0.422410196482577,3.91025045564955,
26.4880999187967));
#29324=CARTESIAN_POINT('Ctrl Pts',(-0.390680213593883,3.91367813079682,
26.4864768817484));
#29325=CARTESIAN_POINT('Ctrl Pts',(-0.35892244261754,3.91671806324583,26.4848538447001));
#29326=CARTESIAN_POINT('Ctrl Pts',(-0.327147102199726,3.91937032870362,
26.4832308076518));
#29327=CARTESIAN_POINT('Ctrl Pts',(-0.212184391895869,3.92896618578849,
26.4773586836858));
#29328=CARTESIAN_POINT('Ctrl Pts',(-0.0966063925619334,3.9335157236183,
26.4714865597197));
#29329=CARTESIAN_POINT('Ctrl Pts',(0.019106299236193,3.932953591047,26.4656144357537));
#29330=CARTESIAN_POINT('Ctrl Pts',(0.134668967232153,3.93239218729174,26.459749925113));
#29331=CARTESIAN_POINT('Ctrl Pts',(0.250365570827072,3.92673229458373,26.4538854144722));
#29332=CARTESIAN_POINT('Ctrl Pts',(0.365710255765519,3.91596029203922,26.4480209038315));
#29333=CARTESIAN_POINT('Ctrl Pts',(0.480936252170543,3.90519937377818,26.4421624277139));
#29334=CARTESIAN_POINT('Ctrl Pts',(0.595810641051473,3.88933684689728,26.4363039515963));
#29335=CARTESIAN_POINT('Ctrl Pts',(0.70984810413449,3.86841112978658,26.4304454754786));
#29336=CARTESIAN_POINT('Ctrl Pts',(0.828382215444494,3.84666028393134,26.4243559918874));
#29337=CARTESIAN_POINT('Ctrl Pts',(0.946011585862198,3.81943873873772,26.4182665082961));
#29338=CARTESIAN_POINT('Ctrl Pts',(1.06219727216592,3.78684908004046,26.4121770247049));
#29339=CARTESIAN_POINT('Ctrl Pts',(1.1738458170463,3.75553207286468,26.4063253401845));
#29340=CARTESIAN_POINT('Ctrl Pts',(1.28416088034434,3.71925846474617,26.400473655664));
#29341=CARTESIAN_POINT('Ctrl Pts',(1.39267596188823,3.67817110330374,26.3946219711436));
#29342=CARTESIAN_POINT('Ctrl Pts',(1.50117449252341,3.63709000857705,26.3887711791323));
#29343=CARTESIAN_POINT('Ctrl Pts',(1.60787320074873,3.59119676669917,26.382920387121));
#29344=CARTESIAN_POINT('Ctrl Pts',(1.71232333412656,3.5406832390664,26.3770695951096));
#29345=CARTESIAN_POINT('Ctrl Pts',(1.81678283548105,3.49016518095067,26.3712182783495));
#29346=CARTESIAN_POINT('Ctrl Pts',(1.91899298888713,3.43502619331729,26.3653669615894));
#29347=CARTESIAN_POINT('Ctrl Pts',(2.01852816331547,3.37550485911401,26.3595156448292));
#29348=CARTESIAN_POINT('Ctrl Pts',(2.11809637333762,3.315963769858,26.3536623860248));
#29349=CARTESIAN_POINT('Ctrl Pts',(2.2149874843812,3.25203765392655,26.3478091272203));
#29350=CARTESIAN_POINT('Ctrl Pts',(2.30880406081129,3.18400892096447,26.3419558684158));
#29351=CARTESIAN_POINT('Ctrl Pts',(2.40272737189701,3.11590279204889,26.3360959503876));
#29352=CARTESIAN_POINT('Ctrl Pts',(2.49356883180467,3.04368497267418,26.3302360323595));
#29353=CARTESIAN_POINT('Ctrl Pts',(2.5809633002183,2.96767879712853,26.3243761143314));
#29354=CARTESIAN_POINT('Ctrl Pts',(2.66841661382838,2.8916214444499,26.3185122506528));
#29355=CARTESIAN_POINT('Ctrl Pts',(2.75241801555775,2.8117709405761,26.3126483869742));
#29356=CARTESIAN_POINT('Ctrl Pts',(2.83263976556624,2.72848693574531,26.3067845232955));
#29357=CARTESIAN_POINT('Ctrl Pts',(2.91297986194377,2.64508006698336,26.3009120090081));
#29358=CARTESIAN_POINT('Ctrl Pts',(2.98952890581758,2.55822989696614,26.2950394947207));
#29359=CARTESIAN_POINT('Ctrl Pts',(3.06199984378537,2.46832857550578,26.2891669804333));
#29360=CARTESIAN_POINT('Ctrl Pts',(3.08202925733651,2.44348177764697,26.287543943385));
#29361=CARTESIAN_POINT('Ctrl Pts',(3.1017474231985,2.41840208184086,26.2859209063367));
#29362=CARTESIAN_POINT('Ctrl Pts',(3.12114888345207,2.39309812739175,26.2842978692884));
#29363=CARTESIAN_POINT('Ctrl Pts',(3.19146659825775,2.30138769791101,26.2784154122573));
#29364=CARTESIAN_POINT('Ctrl Pts',(3.25785940517396,2.20641799845255,26.2725329552262));
#29365=CARTESIAN_POINT('Ctrl Pts',(3.32001064603812,2.10855834877614,26.2666504981952));
#29366=CARTESIAN_POINT('Ctrl Pts',(3.3820820487949,2.01082440743814,26.2607755976381));
#29367=CARTESIAN_POINT('Ctrl Pts',(3.43992249984967,1.91020823968535,26.254900697081));
#29368=CARTESIAN_POINT('Ctrl Pts',(3.49325579813117,1.80711176434191,26.2490257965239));
#29369=CARTESIAN_POINT('Ctrl Pts',(3.54653333138522,1.70412308615265,26.2431570387332));
#29370=CARTESIAN_POINT('Ctrl Pts',(3.59531289573926,1.59865962005353,26.2372882809425));
#29371=CARTESIAN_POINT('Ctrl Pts',(3.63936218127963,1.4911512040942,26.2314195231518));
#29372=CARTESIAN_POINT('Ctrl Pts',(3.68337593372531,1.38372951160104,26.2255554994929));
#29373=CARTESIAN_POINT('Ctrl Pts',(3.72266684230552,1.27426652932657,26.2196914758341));
#29374=CARTESIAN_POINT('Ctrl Pts',(3.75704936513723,1.1632149706404,26.2138274521752));
#29375=CARTESIAN_POINT('Ctrl Pts',(3.79141352010128,1.05222273803521,26.2079665612013));
#29376=CARTESIAN_POINT('Ctrl Pts',(3.82087438444825,0.939644009115514,26.2021056702274));
#29377=CARTESIAN_POINT('Ctrl Pts',(3.84529545264423,0.825949079467748,26.1962447792534));
#29378=CARTESIAN_POINT('Ctrl Pts',(3.86970896790326,0.712289313336499,26.1903857009332));
#29379=CARTESIAN_POINT('Ctrl Pts',(3.88908570448811,0.597514435383587,26.184526622613));
#29380=CARTESIAN_POINT('Ctrl Pts',(3.90333986373395,0.482106739410929,26.1786675442928));
#29381=CARTESIAN_POINT('Ctrl Pts',(3.91759541092605,0.366687806038893,26.1728078954664));
#29382=CARTESIAN_POINT('Ctrl Pts',(3.92672733196767,0.250636339225301,26.16694824664));
#29383=CARTESIAN_POINT('Ctrl Pts',(3.93070153722025,0.134441159227153,26.1610885978136));
#29384=CARTESIAN_POINT('Ctrl Pts',(3.93226714142562,0.0886670607880611,
26.1587802392207));
#29385=CARTESIAN_POINT('Ctrl Pts',(3.93303288933878,0.0428706959530158,
26.1564718806279));
#29386=CARTESIAN_POINT('Ctrl Pts',(3.93299891753312,-0.00291799302117128,
26.154163522035));
#29387=CARTESIAN_POINT('',(3.93448863940243,-0.00148071873010509,24.904163522035));
#29388=CARTESIAN_POINT('Ctrl Pts',(3.93299891753245,-0.00291799392893486,
26.1541635219892));
#29389=CARTESIAN_POINT('Ctrl Pts',(3.93289966337747,-0.136697053654407,
26.1474192790553));
#29390=CARTESIAN_POINT('Ctrl Pts',(3.92597081494,-0.270198098326926,26.1406750361215));
#29391=CARTESIAN_POINT('Ctrl Pts',(3.91232098998049,-0.402782163654324,
26.1339307931876));
#29392=CARTESIAN_POINT('Ctrl Pts',(3.89859623802565,-0.536094013086838,
26.1271495295696));
#29393=CARTESIAN_POINT('Ctrl Pts',(3.87807663698307,-0.668478652679353,
26.1203682659515));
#29394=CARTESIAN_POINT('Ctrl Pts',(3.85092187812462,-0.799305754127397,
26.1135870023335));
#29395=CARTESIAN_POINT('Ctrl Pts',(3.8235914984607,-0.930978967339932,26.1067618815417));
#29396=CARTESIAN_POINT('Ctrl Pts',(3.78953995026768,-1.06107429835095,26.0999367607498));
#29397=CARTESIAN_POINT('Ctrl Pts',(3.74897826520204,-1.18897054927476,26.093111639958));
#29398=CARTESIAN_POINT('Ctrl Pts',(3.73363203755879,-1.23735919432781,26.0905294036137));
#29399=CARTESIAN_POINT('Ctrl Pts',(3.71735441033018,-1.28543328393037,26.0879471672693));
#29400=CARTESIAN_POINT('Ctrl Pts',(3.70015855625265,-1.33316002737492,26.085364930925));
#29401=CARTESIAN_POINT('Ctrl Pts',(3.66105439482825,-1.44169283252097,26.079492806959));
#29402=CARTESIAN_POINT('Ctrl Pts',(3.617105411396,-1.54868563171675,26.0736206829929));
#29403=CARTESIAN_POINT('Ctrl Pts',(3.5684521309445,-1.65367420889293,26.0677485590269));
#29404=CARTESIAN_POINT('Ctrl Pts',(3.51986193043716,-1.75852666629416,26.0618840483862));
#29405=CARTESIAN_POINT('Ctrl Pts',(3.46657973425262,-1.86137969755,26.0560195377455));
#29406=CARTESIAN_POINT('Ctrl Pts',(3.40879529535264,-1.96178582785728,26.0501550271048));
#29407=CARTESIAN_POINT('Ctrl Pts',(3.35107031606528,-2.06208864125563,26.0442965509872));
#29408=CARTESIAN_POINT('Ctrl Pts',(3.28885251381732,-2.15994920564826,26.0384380748695));
#29409=CARTESIAN_POINT('Ctrl Pts',(3.22237874009188,-2.25494218449251,26.0325795987519));
#29410=CARTESIAN_POINT('Ctrl Pts',(3.15328381741514,-2.35368086232338,26.0264901151607));
#29411=CARTESIAN_POINT('Ctrl Pts',(3.07959057234702,-2.44932074385272,26.0204006315694));
#29412=CARTESIAN_POINT('Ctrl Pts',(3.00161651713324,-2.54141442588038,26.0143111479781));
#29413=CARTESIAN_POINT('Ctrl Pts',(2.92668740942666,-2.629911777991,26.0084594634577));
#29414=CARTESIAN_POINT('Ctrl Pts',(2.84780584776093,-2.71513435167606,26.0026077789373));
#29415=CARTESIAN_POINT('Ctrl Pts',(2.76529581629403,-2.79671737012998,25.9967560944169));
#29416=CARTESIAN_POINT('Ctrl Pts',(2.68279836940049,-2.87828794540017,25.9909053024056));
#29417=CARTESIAN_POINT('Ctrl Pts',(2.5966738469717,-2.95621977858374,25.9850545103943));
#29418=CARTESIAN_POINT('Ctrl Pts',(2.50728341954857,-3.03018462375757,25.979203718383));
#29419=CARTESIAN_POINT('Ctrl Pts',(2.41788497483111,-3.10415610272824,25.9733524016228));
#29420=CARTESIAN_POINT('Ctrl Pts',(2.32522036136615,-3.1741596228391,25.9675010848627));
#29421=CARTESIAN_POINT('Ctrl Pts',(2.22968361594949,-3.23990740188148,25.9616497681026));
#29422=CARTESIAN_POINT('Ctrl Pts',(2.13411516201201,-3.30567700252571,25.955796509298));
#29423=CARTESIAN_POINT('Ctrl Pts',(2.03567302101281,-3.36718781924058,25.9499432504935));
#29424=CARTESIAN_POINT('Ctrl Pts',(1.93477935256376,-3.42419594312197,25.944089991689));
#29425=CARTESIAN_POINT('Ctrl Pts',(1.83377089788687,-3.48126892486408,25.9382300736609));
#29426=CARTESIAN_POINT('Ctrl Pts',(1.73030570895415,-3.53382878552301,25.9323701556328));
#29427=CARTESIAN_POINT('Ctrl Pts',(1.62482972346511,-3.58167801033877,25.9265102376046));
#29428=CARTESIAN_POINT('Ctrl Pts',(1.51928271797639,-3.62955945340701,25.920646373926));
#29429=CARTESIAN_POINT('Ctrl Pts',(1.41172260273298,-3.67272379135267,25.9147825102474));
#29430=CARTESIAN_POINT('Ctrl Pts',(1.30261277864833,-3.7110226284546,25.9089186465687));
#29431=CARTESIAN_POINT('Ctrl Pts',(1.1933419913402,-3.74937796554932,25.9030461322813));
#29432=CARTESIAN_POINT('Ctrl Pts',(1.08251732664487,-3.78285335718474,25.8971736179939));
#29433=CARTESIAN_POINT('Ctrl Pts',(0.970614811177254,-3.81135092694485,
25.8913011037065));
#29434=CARTESIAN_POINT('Ctrl Pts',(0.939687354977304,-3.81922704426784,
25.8896780666582));
#29435=CARTESIAN_POINT('Ctrl Pts',(0.908677608991107,-3.826723234007,25.8880550296099));
#29436=CARTESIAN_POINT('Ctrl Pts',(0.877595700063934,-3.83383812741609,
25.8864319925615));
#29437=CARTESIAN_POINT('Ctrl Pts',(0.765141814610416,-3.85957970623335,
25.8805598685955));
#29438=CARTESIAN_POINT('Ctrl Pts',(0.651365865963002,-3.88041251050638,
25.8746877446294));
#29439=CARTESIAN_POINT('Ctrl Pts',(0.536734397292292,-3.89620394573529,
25.8688156206634));
#29440=CARTESIAN_POINT('Ctrl Pts',(0.422251550596811,-3.91197490705488,
25.8629511100227));
#29441=CARTESIAN_POINT('Ctrl Pts',(0.306915795431241,-3.92271744163368,
25.857086599382));
#29442=CARTESIAN_POINT('Ctrl Pts',(0.191206188388593,-3.92834942355207,
25.8512220887413));
#29443=CARTESIAN_POINT('Ctrl Pts',(0.0756156453804744,-3.9339756102171,
25.8453636126236));
#29444=CARTESIAN_POINT('Ctrl Pts',(-0.0403475739007709,-3.9345016840641,
25.839505136506));
#29445=CARTESIAN_POINT('Ctrl Pts',(-0.156197591340927,-3.92989711219763,
25.8336466603884));
#29446=CARTESIAN_POINT('Ctrl Pts',(-0.276615728427646,-3.92511097596309,
25.8275571767972));
#29447=CARTESIAN_POINT('Ctrl Pts',(-0.396911101818345,-3.91478119143449,
25.8214676932059));
#29448=CARTESIAN_POINT('Ctrl Pts',(-0.516535680730198,-3.89893317338636,
25.8153782096146));
#29449=CARTESIAN_POINT('Ctrl Pts',(-0.631488826787159,-3.88370403277017,
25.8095265250942));
#29450=CARTESIAN_POINT('Ctrl Pts',(-0.745822136886534,-3.86337961302313,
25.8036748405738));
#29451=CARTESIAN_POINT('Ctrl Pts',(-0.8590536084657,-3.83803542164244,25.7978231560534));
#29452=CARTESIAN_POINT('Ctrl Pts',(-0.972267809784176,-3.81269509580184,
25.7919723640421));
#29453=CARTESIAN_POINT('Ctrl Pts',(-1.08438010340781,-3.78233661090202,
25.7861215720308));
#29454=CARTESIAN_POINT('Ctrl Pts',(-1.19491913180823,-3.74708650399729,
25.7802707800195));
#29455=CARTESIAN_POINT('Ctrl Pts',(-1.3054680742894,-3.71183323556301,25.7744194632594));
#29456=CARTESIAN_POINT('Ctrl Pts',(-1.41444307715194,-3.67168759859424,
25.7685681464992));
#29457=CARTESIAN_POINT('Ctrl Pts',(-1.52138907152239,-3.62682564966283,
25.7627168297391));
#29458=CARTESIAN_POINT('Ctrl Pts',(-1.62837056112883,-3.58194881110911,
25.7568635709346));
#29459=CARTESIAN_POINT('Ctrl Pts',(-1.73332132215295,-3.53235270785515,
25.75101031213));
#29460=CARTESIAN_POINT('Ctrl Pts',(-1.83580800645435,-3.47826076702683,
25.7451570533255));
#29461=CARTESIAN_POINT('Ctrl Pts',(-1.93841128934952,-3.42410728606501,
25.7392971352974));
#29462=CARTESIAN_POINT('Ctrl Pts',(-2.03854453424244,-3.3654479514235,25.7334372172693));
#29463=CARTESIAN_POINT('Ctrl Pts',(-2.13580058252971,-3.30255126707607,
25.7275772992412));
#29464=CARTESIAN_POINT('Ctrl Pts',(-2.23312211609763,-3.23961223259105,
25.7217134355625));
#29465=CARTESIAN_POINT('Ctrl Pts',(-2.3275622594692,-3.1724304063178,25.7158495718839));
#29466=CARTESIAN_POINT('Ctrl Pts',(-2.41874574864605,-3.10131552786985,
25.7099857082053));
#29467=CARTESIAN_POINT('Ctrl Pts',(-2.51006375539251,-3.03009573787817,
25.7041131939179));
#29468=CARTESIAN_POINT('Ctrl Pts',(-2.59811520610508,-2.95493158300759,
25.6982406796305));
#29469=CARTESIAN_POINT('Ctrl Pts',(-2.68256052357199,-2.87617072465686,
25.6923681653431));
#29470=CARTESIAN_POINT('Ctrl Pts',(-2.70589939889837,-2.85440291196118,
25.6907451282948));
#29471=CARTESIAN_POINT('Ctrl Pts',(-2.728963052369,-2.83236056418945,25.6891220912465));
#29472=CARTESIAN_POINT('Ctrl Pts',(-2.75174486024567,-2.81005146289379,
25.6874990541981));
#29473=CARTESIAN_POINT('Ctrl Pts',(-2.83416910321691,-2.72933746532088,
25.6816269302321));
#29474=CARTESIAN_POINT('Ctrl Pts',(-2.91317727188268,-2.6448585832937,25.6757548062661));
#29475=CARTESIAN_POINT('Ctrl Pts',(-2.98840570014136,-2.5569357386064,25.6698826823001));
#29476=CARTESIAN_POINT('Ctrl Pts',(-3.06353659324907,-2.46912688763302,
25.6640181716593));
#29477=CARTESIAN_POINT('Ctrl Pts',(-3.13489722499802,-2.37788326481389,
25.6581536610186));
#29478=CARTESIAN_POINT('Ctrl Pts',(-3.2021596340609,-2.28356359184302,25.6522891503779));
#29479=CARTESIAN_POINT('Ctrl Pts',(-3.26935283077402,-2.18934097287727,
25.6464306742603));
#29480=CARTESIAN_POINT('Ctrl Pts',(-3.33245595408606,-2.09204893410727,
25.6405721981427));
#29481=CARTESIAN_POINT('Ctrl Pts',(-3.39118076920397,-1.99207981531392,
25.6347137220251));
#29482=CARTESIAN_POINT('Ctrl Pts',(-3.45222118157091,-1.888168781744,25.6286242384338));
#29483=CARTESIAN_POINT('Ctrl Pts',(-3.50853060137652,-1.78136554888669,
25.6225347548426));
#29484=CARTESIAN_POINT('Ctrl Pts',(-3.55983428648306,-1.67214498557381,
25.6164452712513));
#29485=CARTESIAN_POINT('Ctrl Pts',(-3.60913452278029,-1.56718957021407,
25.6105935867309));
#29486=CARTESIAN_POINT('Ctrl Pts',(-3.65381245120797,-1.46000248821375,
25.6047419022105));
#29487=CARTESIAN_POINT('Ctrl Pts',(-3.69367115793895,-1.35103011698849,
25.5988902176901));
#29488=CARTESIAN_POINT('Ctrl Pts',(-3.73352378535073,-1.24207436641863,
25.5930394256788));
#29489=CARTESIAN_POINT('Ctrl Pts',(-3.76855851057502,-1.13133425618119,
25.5871886336675));
#29490=CARTESIAN_POINT('Ctrl Pts',(-3.79862711020792,-1.01927478022045,
25.5813378416562));
#29491=CARTESIAN_POINT('Ctrl Pts',(-3.82869840664872,-0.907205253812249,
25.575486524896));
#29492=CARTESIAN_POINT('Ctrl Pts',(-3.85380258492889,-0.793816525759676,
25.5696352081359));
#29493=CARTESIAN_POINT('Ctrl Pts',(-3.87384189097495,-0.679586641810747,
25.5637838913758));
#29494=CARTESIAN_POINT('Ctrl Pts',(-3.89388784804053,-0.565318845112445,
25.5579306325712));
#29495=CARTESIAN_POINT('Ctrl Pts',(-3.90886551886826,-0.450209744368547,
25.5520773737667));
#29496=CARTESIAN_POINT('Ctrl Pts',(-3.91872874569848,-0.334744705165609,
25.5462241149622));
#29497=CARTESIAN_POINT('Ctrl Pts',(-3.92860319387308,-0.219148301958656,
25.5403641969341));
#29498=CARTESIAN_POINT('Ctrl Pts',(-3.93335154891644,-0.103195564182696,
25.5345042789059));
#29499=CARTESIAN_POINT('Ctrl Pts',(-3.93297973407051,0.0126258223746364,
25.5286443608778));
#29500=CARTESIAN_POINT('Ctrl Pts',(-3.93260766887101,0.128525194786199,
25.5227804971992));
#29501=CARTESIAN_POINT('Ctrl Pts',(-3.92710858858938,0.244292627933414,
25.5169166335206));
#29502=CARTESIAN_POINT('Ctrl Pts',(-3.91654034803666,0.359444991898466,
25.5110527698419));
#29503=CARTESIAN_POINT('Ctrl Pts',(-3.90595651678822,0.474767233286212,
25.5051802555545));
#29504=CARTESIAN_POINT('Ctrl Pts',(-3.89028865584999,0.58947218646435,25.4993077412671));
#29505=CARTESIAN_POINT('Ctrl Pts',(-3.86964581228303,0.703086258918789,
25.4934352269798));
#29506=CARTESIAN_POINT('Ctrl Pts',(-3.86394057288252,0.734486752775978,
25.4918121899314));
#29507=CARTESIAN_POINT('Ctrl Pts',(-3.85785561268348,0.765804007861907,
25.4901891528831));
#29508=CARTESIAN_POINT('Ctrl Pts',(-3.85139390028731,0.797028245942219,
25.4885661158347));
#29509=CARTESIAN_POINT('Ctrl Pts',(-3.82801552068608,0.909997076160167,
25.4826939918687));
#29510=CARTESIAN_POINT('Ctrl Pts',(-3.79962334186986,1.02212582540209,25.4768218679026));
#29511=CARTESIAN_POINT('Ctrl Pts',(-3.76629089470126,1.13293508043946,25.4709497439366));
#29512=CARTESIAN_POINT('Ctrl Pts',(-3.73300166371225,1.2436006690775,25.4650852332959));
#29513=CARTESIAN_POINT('Ctrl Pts',(-3.69478501988866,1.3529497733429,25.4592207226552));
#29514=CARTESIAN_POINT('Ctrl Pts',(-3.6517655935033,1.46051259840697,25.4533562120144));
#29515=CARTESIAN_POINT('Ctrl Pts',(-3.60879043367971,1.56796474239413,25.4474977358968));
#29516=CARTESIAN_POINT('Ctrl Pts',(-3.56102247379366,1.67363388163584,25.4416392597792));
#29517=CARTESIAN_POINT('Ctrl Pts',(-3.50863609792475,1.77706548341342,25.4357807836616));
#29518=CARTESIAN_POINT('Ctrl Pts',(-3.45418405786254,1.88457553025815,25.4296913000703));
#29519=CARTESIAN_POINT('Ctrl Pts',(-3.39474201927504,1.98966751547195,25.4236018164791));
#29520=CARTESIAN_POINT('Ctrl Pts',(-3.33056110036188,2.0918536652348,25.4175123328878));
#29521=CARTESIAN_POINT('Ctrl Pts',(-3.26888649625454,2.1900493663653,25.4116606483674));
#29522=CARTESIAN_POINT('Ctrl Pts',(-3.20283642093734,2.28556154039003,25.405808963847));
#29523=CARTESIAN_POINT('Ctrl Pts',(-3.13268007309228,2.37798329675601,25.3999572793266));
#29524=CARTESIAN_POINT('Ctrl Pts',(-3.06253442561529,2.47039095679511,25.3941064873153));
#29525=CARTESIAN_POINT('Ctrl Pts',(-2.9882840007727,2.55970880718147,25.388255695304));
#29526=CARTESIAN_POINT('Ctrl Pts',(-2.91023997173198,2.64556086812105,25.3824049032927));
#29527=CARTESIAN_POINT('Ctrl Pts',(-2.83218894303857,2.73142062900408,25.3765535865325));
#29528=CARTESIAN_POINT('Ctrl Pts',(-2.75034391187737,2.81381367659142,25.3707022697724));
#29529=CARTESIAN_POINT('Ctrl Pts',(-2.66505430473762,2.89239944558138,25.3648509530123));
#29530=CARTESIAN_POINT('Ctrl Pts',(-2.57973639008858,2.97101129708551,25.3589976942077));
#29531=CARTESIAN_POINT('Ctrl Pts',(-2.49097193005286,3.04581307735888,25.3531444354032));
#29532=CARTESIAN_POINT('Ctrl Pts',(-2.39914439028916,3.11650368113757,25.3472911765987));
#29533=CARTESIAN_POINT('Ctrl Pts',(-2.30721237878769,3.18727470926652,25.3414312585706));
#29534=CARTESIAN_POINT('Ctrl Pts',(-2.21221065967174,3.2539249728697,25.3355713405424));
#29535=CARTESIAN_POINT('Ctrl Pts',(-2.11455279276547,3.31619593610024,25.3297114225143));
#29536=CARTESIAN_POINT('Ctrl Pts',(-2.01682917002254,3.37850882815246,25.3238475588357));
#29537=CARTESIAN_POINT('Ctrl Pts',(-1.9164461955111,3.4364363422514,25.3179836951571));
#29538=CARTESIAN_POINT('Ctrl Pts',(-1.81384165666161,3.4897661016978,25.3121198314784));
#29539=CARTESIAN_POINT('Ctrl Pts',(-1.71108575144835,3.54317453536134,25.306247317191));
#29540=CARTESIAN_POINT('Ctrl Pts',(-1.60610211442283,3.59197150357526,25.3003748029036));
#29541=CARTESIAN_POINT('Ctrl Pts',(-1.49934816946151,3.63599285845454,25.2945022886162));
#29542=CARTESIAN_POINT('Ctrl Pts',(-1.46984366776945,3.64815941717041,25.2928792515679));
#29543=CARTESIAN_POINT('Ctrl Pts',(-1.44020402538699,3.65996148504733,25.2912562145196));
#29544=CARTESIAN_POINT('Ctrl Pts',(-1.41043907420642,3.67139627634388,25.2896331774712));
#29545=CARTESIAN_POINT('Ctrl Pts',(-1.30274992234525,3.71276718164,25.2837610535052));
#29546=CARTESIAN_POINT('Ctrl Pts',(-1.19305845469924,3.74946533077809,25.2778889295392));
#29547=CARTESIAN_POINT('Ctrl Pts',(-1.08180780184001,3.78129354584884,25.2720168055731));
#29548=CARTESIAN_POINT('Ctrl Pts',(-0.970701387661206,3.81308049500677,
25.2661522949324));
#29549=CARTESIAN_POINT('Ctrl Pts',(-0.85804020212067,3.84000995362343,25.2602877842917));
#29550=CARTESIAN_POINT('Ctrl Pts',(-0.744286893916767,3.86193293825045,
25.254423273651));
#29551=CARTESIAN_POINT('Ctrl Pts',(-0.630650636735293,3.88383336434439,
25.2485647975334));
#29552=CARTESIAN_POINT('Ctrl Pts',(-0.515924895647223,3.90073748548584,
25.2427063214157));
#29553=CARTESIAN_POINT('Ctrl Pts',(-0.400586361530146,3.91254643000643,
25.2368478452981));
#29554=CARTESIAN_POINT('Ctrl Pts',(-0.280699876231519,3.92482101685199,
25.2307583617069));
#29555=CARTESIAN_POINT('Ctrl Pts',(-0.160151714701411,3.93159021616369,
25.2246688781156));
#29556=CARTESIAN_POINT('Ctrl Pts',(-0.0394880013778991,3.93280176181653,
25.2185793945244));
#29557=CARTESIAN_POINT('Ctrl Pts',(0.0764637000837605,3.93396599566923,
25.2127277100039));
#29558=CARTESIAN_POINT('Ctrl Pts',(0.192521645583772,3.92999848729926,25.2068760254835));
#29559=CARTESIAN_POINT('Ctrl Pts',(0.308197999499315,3.92090588934555,25.2010243409631));
#29560=CARTESIAN_POINT('Ctrl Pts',(0.423856710256336,3.91181467821068,25.1951735489518));
#29561=CARTESIAN_POINT('Ctrl Pts',(0.53913353312302,3.89759996411879,25.1893227569405));
#29562=CARTESIAN_POINT('Ctrl Pts',(0.653543961263525,3.87832042135458,25.1834719649292));
#29563=CARTESIAN_POINT('Ctrl Pts',(0.767964650704958,3.85903914943689,25.1776206481691));
#29564=CARTESIAN_POINT('Ctrl Pts',(0.881518383259193,3.83469221452647,25.1717693314089));
#29565=CARTESIAN_POINT('Ctrl Pts',(0.99372978122933,3.80538961499318,25.1659180146488));
#29566=CARTESIAN_POINT('Ctrl Pts',(1.10597842201578,3.7760772899654,25.1600647558443));
#29567=CARTESIAN_POINT('Ctrl Pts',(1.21688344254487,3.74180613417929,25.1542114970398));
#29568=CARTESIAN_POINT('Ctrl Pts',(1.32598427545732,3.7027361101272,25.1483582382352));
#29569=CARTESIAN_POINT('Ctrl Pts',(1.4352092318479,3.66362163630194,25.1424983202071));
#29570=CARTESIAN_POINT('Ctrl Pts',(1.54262551421503,3.61969753635897,25.136638402179));
#29571=CARTESIAN_POINT('Ctrl Pts',(1.64779211357284,3.57117209756785,25.1307784841509));
#29572=CARTESIAN_POINT('Ctrl Pts',(1.75302952461166,3.52261398521009,25.1249146204722));
#29573=CARTESIAN_POINT('Ctrl Pts',(1.85601386997303,3.46944855403605,25.1190507567936));
#29574=CARTESIAN_POINT('Ctrl Pts',(1.95632988957584,3.4119294194271,25.113186893115));
#29575=CARTESIAN_POINT('Ctrl Pts',(2.05679389942638,3.35432543026538,25.1073143788276));
#29576=CARTESIAN_POINT('Ctrl Pts',(2.1545813792611,3.29235513949992,25.1014418645402));
#29577=CARTESIAN_POINT('Ctrl Pts',(2.24930704023069,3.22631474576933,25.0955693502528));
#29578=CARTESIAN_POINT('Ctrl Pts',(2.27548718210135,3.20806259678073,25.0939463132045));
#29579=CARTESIAN_POINT('Ctrl Pts',(2.30143364910518,3.18949978296553,25.0923232761561));
#29580=CARTESIAN_POINT('Ctrl Pts',(2.32713878456213,3.17063307201995,25.0907002391078));
#29581=CARTESIAN_POINT('Ctrl Pts',(2.41929313316304,3.10299485784508,25.0848815604942));
#29582=CARTESIAN_POINT('Ctrl Pts',(2.50866441508414,3.03121193412896,25.0790628818805));
#29583=CARTESIAN_POINT('Ctrl Pts',(2.59485131254487,2.95554320993352,25.0732442032669));
#29584=CARTESIAN_POINT('Ctrl Pts',(2.68092610598529,2.87997290868223,25.0674330930573));
#29585=CARTESIAN_POINT('Ctrl Pts',(2.76382443478544,2.80052712962886,25.0616219828477));
#29586=CARTESIAN_POINT('Ctrl Pts',(2.8431746241309,2.71750750812175,25.0558108726382));
#29587=CARTESIAN_POINT('Ctrl Pts',(2.92244380484517,2.63457264137019,25.0500056949927));
#29588=CARTESIAN_POINT('Ctrl Pts',(2.9981717587886,2.54807148956562,25.0442005173472));
#29589=CARTESIAN_POINT('Ctrl Pts',(3.07002114095011,2.45834480781671,25.0383953397017));
#29590=CARTESIAN_POINT('Ctrl Pts',(3.14181856355304,2.36868301401307,25.032594360206));
#29591=CARTESIAN_POINT('Ctrl Pts',(3.2097427294854,2.27580065696699,25.0267933807103));
#29592=CARTESIAN_POINT('Ctrl Pts',(3.27349484603802,2.18007350632095,25.0209924012146));
#29593=CARTESIAN_POINT('Ctrl Pts',(3.33722298896874,2.08438235332706,25.0151936031443));
#29594=CARTESIAN_POINT('Ctrl Pts',(3.3967819668782,1.98584888317275,25.0093948050741));
#29595=CARTESIAN_POINT('Ctrl Pts',(3.45191522647188,1.88487937790502,25.0035960070038));
#29596=CARTESIAN_POINT('Ctrl Pts',(3.50704170690549,1.78392228780088,24.9977979219511));
#29597=CARTESIAN_POINT('Ctrl Pts',(3.55774334901334,1.68053012824946,24.9919998368983));
#29598=CARTESIAN_POINT('Ctrl Pts',(3.60380905841642,1.57513468328133,24.9862017518456));
#29599=CARTESIAN_POINT('Ctrl Pts',(3.64988076245597,1.46972552296207,24.9804029122747));
#29600=CARTESIAN_POINT('Ctrl Pts',(3.69131516671325,1.36231294586496,24.9746040727039));
#29601=CARTESIAN_POINT('Ctrl Pts',(3.72794924521417,1.25334888403312,24.968805233133));
#29602=CARTESIAN_POINT('Ctrl Pts',(3.76461888331469,1.14427905405952,24.9630007648028));
#29603=CARTESIAN_POINT('Ctrl Pts',(3.79647875699002,1.0336551325787,24.9571962964725));
#29604=CARTESIAN_POINT('Ctrl Pts',(3.82341568735235,0.92194440272066,24.9513918281423));
#29605=CARTESIAN_POINT('Ctrl Pts',(3.85036646612251,0.810176241829282,24.9455843757065));
#29606=CARTESIAN_POINT('Ctrl Pts',(3.87238918170624,0.697320573739987,24.9397769232706));
#29607=CARTESIAN_POINT('Ctrl Pts',(3.88942211602274,0.583853237888747,24.9339694708348));
#29608=CARTESIAN_POINT('Ctrl Pts',(3.90648102119818,0.470212893434376,24.9281531635226));
#29609=CARTESIAN_POINT('Ctrl Pts',(3.91853490722703,0.355959437785159,24.9223368562104));
#29610=CARTESIAN_POINT('Ctrl Pts',(3.92557406855906,0.241572416175038,24.9165205488981));
#29611=CARTESIAN_POINT('Ctrl Pts',(3.93055908173005,0.160565491852631,24.9124015399438));
#29612=CARTESIAN_POINT('Ctrl Pts',(3.93303019466974,0.0794916235615288,
24.9082825309894));
#29613=CARTESIAN_POINT('Ctrl Pts',(3.93299972147611,-0.00148015838570855,
24.904163522035));
#29614=CARTESIAN_POINT('',(3.93299834039037,0.00361309930207936,23.654163522035));
#29615=CARTESIAN_POINT('Ctrl Pts',(3.93885394375624,-0.00148236158347574,
24.904163522035));
#29616=CARTESIAN_POINT('Ctrl Pts',(3.93924552707134,-0.082832039204855,
24.9000314482714));
#29617=CARTESIAN_POINT('Ctrl Pts',(3.90002134205164,-1.46928590995256,24.8295883950541));
#29618=CARTESIAN_POINT('Ctrl Pts',(2.26524006589229,-4.06362187352642,24.6928343623803));
#29619=CARTESIAN_POINT('Ctrl Pts',(-2.19528402354312,-4.10183658171443,
24.4939014240179));
#29620=CARTESIAN_POINT('Ctrl Pts',(-4.63767356163746,-0.369214331799999,
24.2949684856538));
#29621=CARTESIAN_POINT('Ctrl Pts',(-2.81662877770042,3.70282832652962,24.0960355472907));
#29622=CARTESIAN_POINT('Ctrl Pts',(1.59375560585921,4.37084412395475,23.897102608927));
#29623=CARTESIAN_POINT('Ctrl Pts',(3.77442032009617,1.89040227389705,23.749811933842));
#29624=CARTESIAN_POINT('Ctrl Pts',(3.93617122324185,0.293430403295199,23.6688322382112));
#29625=CARTESIAN_POINT('Ctrl Pts',(3.93347523015726,0.00361353740297166,
23.654163522035));
#29626=CARTESIAN_POINT('',(3.9329999986383,-0.000103494422979276,22.404163521994));
#29627=CARTESIAN_POINT('Ctrl Pts',(3.93299834039037,0.00361309930207936,
23.654163522035));
#29628=CARTESIAN_POINT('Ctrl Pts',(3.93310324074698,-0.110574996279411,
23.6483832801292));
#29629=CARTESIAN_POINT('Ctrl Pts',(3.92823105114043,-0.224912019346994,
23.6426030382233));
#29630=CARTESIAN_POINT('Ctrl Pts',(3.91836963887632,-0.338922370362654,
23.6368227963175));
#29631=CARTESIAN_POINT('Ctrl Pts',(3.90851599762897,-0.452842878633289,
23.6310471093735));
#29632=CARTESIAN_POINT('Ctrl Pts',(3.89368098718194,-0.56643680435109,23.6252714224295));
#29633=CARTESIAN_POINT('Ctrl Pts',(3.87390454030067,-0.679229425627184,
23.6194957354855));
#29634=CARTESIAN_POINT('Ctrl Pts',(3.85413638626874,-0.791974749619789,
23.6137224704579));
#29635=CARTESIAN_POINT('Ctrl Pts',(3.82943098567734,-0.903919018186908,
23.6079492054304));
#29636=CARTESIAN_POINT('Ctrl Pts',(3.79987994024537,-1.01459422417083,23.6021759404028));
#29637=CARTESIAN_POINT('Ctrl Pts',(3.77033367427634,-1.12525153000818,23.5964036091191));
#29638=CARTESIAN_POINT('Ctrl Pts',(3.73594343083082,-1.23463977005716,23.5906312778354));
#29639=CARTESIAN_POINT('Ctrl Pts',(3.69685138311993,-1.34230356146597,23.5848589465517));
#29640=CARTESIAN_POINT('Ctrl Pts',(3.65775558785716,-1.44997767404414,23.5790860619045));
#29641=CARTESIAN_POINT('Ctrl Pts',(3.61395723875769,-1.55592660967396,23.5733131772573));
#29642=CARTESIAN_POINT('Ctrl Pts',(3.56564729055769,-1.65971334854505,23.5675402926101));
#29643=CARTESIAN_POINT('Ctrl Pts',(3.51728957372828,-1.76360271121209,23.5617616997641));
#29644=CARTESIAN_POINT('Ctrl Pts',(3.46441152820581,-1.86532522057124,23.5559831069181));
#29645=CARTESIAN_POINT('Ctrl Pts',(3.40725089991998,-1.96446692641909,23.5502045140722));
#29646=CARTESIAN_POINT('Ctrl Pts',(3.35006228571326,-2.06365717218017,23.5444230920193));
#29647=CARTESIAN_POINT('Ctrl Pts',(3.28858714318448,-2.16026374001438,23.5386416699665));
#29648=CARTESIAN_POINT('Ctrl Pts',(3.22310645749673,-2.25390189751969,23.5328602479136));
#29649=CARTESIAN_POINT('Ctrl Pts',(3.15751781001056,-2.3476944416778,23.5270692936955));
#29650=CARTESIAN_POINT('Ctrl Pts',(3.08791068603683,-2.4385084610394,23.5212783394773));
#29651=CARTESIAN_POINT('Ctrl Pts',(3.01460647383614,-2.52599224224961,23.5154873852591));
#29652=CARTESIAN_POINT('Ctrl Pts',(2.94603738744473,-2.60782496061002,23.5100705009062));
#29653=CARTESIAN_POINT('Ctrl Pts',(2.87423399507358,-2.68674392815123,23.5046536165532));
#29654=CARTESIAN_POINT('Ctrl Pts',(2.79948658977658,-2.76249232282392,23.4992367322003));
#29655=CARTESIAN_POINT('Ctrl Pts',(2.71845734834484,-2.84460667763814,23.4933646082343));
#29656=CARTESIAN_POINT('Ctrl Pts',(2.63367633994529,-2.92329055679529,23.4874924842682));
#29657=CARTESIAN_POINT('Ctrl Pts',(2.54546587752598,-2.99818152658422,23.4816203603022));
#29658=CARTESIAN_POINT('Ctrl Pts',(2.45736978172267,-3.07297539874381,23.4757558496615));
#29659=CARTESIAN_POINT('Ctrl Pts',(2.36585338632428,-3.14398587573166,23.4698913390208));
#29660=CARTESIAN_POINT('Ctrl Pts',(2.27127666708625,-3.21088637319193,23.4640268283801));
#29661=CARTESIAN_POINT('Ctrl Pts',(2.17679726635115,-3.27771803070604,23.4581683522625));
#29662=CARTESIAN_POINT('Ctrl Pts',(2.07926414084847,-3.34044788332413,23.4523098761448));
#29663=CARTESIAN_POINT('Ctrl Pts',(1.97907073194804,-3.3987892017521,23.4464514000272));
#29664=CARTESIAN_POINT('Ctrl Pts',(1.87492656421521,-3.45943099564649,23.4403619164359));
#29665=CARTESIAN_POINT('Ctrl Pts',(1.76790834682957,-3.51533074927043,23.4342724328447));
#29666=CARTESIAN_POINT('Ctrl Pts',(1.6584919979043,-3.56621554212409,23.4281829492534));
#29667=CARTESIAN_POINT('Ctrl Pts',(1.5533484425126,-3.61511324423675,23.422331264733));
#29668=CARTESIAN_POINT('Ctrl Pts',(1.44599094880336,-3.65938012102753,23.4164795802126));
#29669=CARTESIAN_POINT('Ctrl Pts',(1.33686664545719,-3.6988209705613,23.4106278956922));
#29670=CARTESIAN_POINT('Ctrl Pts',(1.22775898593937,-3.73825580450817,23.4047771036809));
#29671=CARTESIAN_POINT('Ctrl Pts',(1.11688544127904,-3.77286593425945,23.3989263116696));
#29672=CARTESIAN_POINT('Ctrl Pts',(1.00471156997488,-3.80250491928132,23.3930755196583));
#29673=CARTESIAN_POINT('Ctrl Pts',(0.892527637963276,-3.83214656257961,
23.3872242028981));
#29674=CARTESIAN_POINT('Ctrl Pts',(0.77904354718896,-3.85681606921526,23.381372886138));
#29675=CARTESIAN_POINT('Ctrl Pts',(0.664737714468218,-3.87641751762675,
23.3755215693778));
#29676=CARTESIAN_POINT('Ctrl Pts',(0.55039394379119,-3.89602547173332,23.3696683105733));
#29677=CARTESIAN_POINT('Ctrl Pts',(0.435228296101503,-3.91056195306942,
23.3638150517688));
#29678=CARTESIAN_POINT('Ctrl Pts',(0.319726310291494,-3.919982664057,23.3579617929643));
#29679=CARTESIAN_POINT('Ctrl Pts',(0.204092918443143,-3.92941409294089,
23.3521018749362));
#29680=CARTESIAN_POINT('Ctrl Pts',(0.0881228370050104,-3.9337181009102,
23.3462419569081));
#29681=CARTESIAN_POINT('Ctrl Pts',(-0.0276962745125356,-3.93290247989676,
23.3403820388799));
#29682=CARTESIAN_POINT('Ctrl Pts',(-0.14359337035263,-3.93208630970236,
23.3345181752013));
#29683=CARTESIAN_POINT('Ctrl Pts',(-0.259338882001057,-3.92614366763592,
23.3286543115227));
#29684=CARTESIAN_POINT('Ctrl Pts',(-0.374449904777226,-3.91513425935974,
23.322790447844));
#29685=CARTESIAN_POINT('Ctrl Pts',(-0.489730743987692,-3.9041086095594,
23.3169179335566));
#29686=CARTESIAN_POINT('Ctrl Pts',(-0.604374818337527,-3.88800133274279,
23.3110454192692));
#29687=CARTESIAN_POINT('Ctrl Pts',(-0.717908956640308,-3.86692328990059,
23.3051729049819));
#29688=CARTESIAN_POINT('Ctrl Pts',(-0.749287358411539,-3.86109777075066,
23.3035498679335));
#29689=CARTESIAN_POINT('Ctrl Pts',(-0.780581066993679,-3.8548928525475,
23.3019268308852));
#29690=CARTESIAN_POINT('Ctrl Pts',(-0.811780315599351,-3.84831154133932,
23.3003037938368));
#29691=CARTESIAN_POINT('Ctrl Pts',(-0.924658734269251,-3.82450045501019,
23.2944316698708));
#29692=CARTESIAN_POINT('Ctrl Pts',(-1.03667786605961,-3.79567882532997,
23.2885595459048));
#29693=CARTESIAN_POINT('Ctrl Pts',(-1.14735858301995,-3.7619220196557,23.2826874219387));
#29694=CARTESIAN_POINT('Ctrl Pts',(-1.25789580023323,-3.72820898035023,
23.276822911298));
#29695=CARTESIAN_POINT('Ctrl Pts',(-1.36709766168658,-3.68957360894093,
23.2709584006573));
#29696=CARTESIAN_POINT('Ctrl Pts',(-1.47449485356344,-3.64614233496375,
23.2650938900166));
#29697=CARTESIAN_POINT('Ctrl Pts',(-1.58178153479815,-3.60275575133548,
23.259235413899));
#29698=CARTESIAN_POINT('Ctrl Pts',(-1.68726685913955,-3.55458323501818,
23.2533769377813));
#29699=CARTESIAN_POINT('Ctrl Pts',(-1.79049696541762,-3.50180091050738,
23.2475184616637));
#29700=CARTESIAN_POINT('Ctrl Pts',(-1.89779757152842,-3.44693730902381,
23.2414289780725));
#29701=CARTESIAN_POINT('Ctrl Pts',(-2.00266101288997,-3.38709301127182,
23.2353394944812));
#29702=CARTESIAN_POINT('Ctrl Pts',(-2.10460048150773,-3.32252100267815,
23.2292500108899));
#29703=CARTESIAN_POINT('Ctrl Pts',(-2.20255913458384,-3.26047058124646,
23.2233983263695));
#29704=CARTESIAN_POINT('Ctrl Pts',(-2.29781751415447,-3.19405500357113,
23.2175466418491));
#29705=CARTESIAN_POINT('Ctrl Pts',(-2.3899697641798,-3.12354502549689,23.2116949573287));
#29706=CARTESIAN_POINT('Ctrl Pts',(-2.48210795898371,-3.05304580172712,
23.2058441653174));
#29707=CARTESIAN_POINT('Ctrl Pts',(-2.57114063797309,-2.97845367037996,
23.1999933733061));
#29708=CARTESIAN_POINT('Ctrl Pts',(-2.65669301647964,-2.90008124303239,
23.1941425812948));
#29709=CARTESIAN_POINT('Ctrl Pts',(-2.74225306805148,-2.82170178657866,
23.1882912645347));
#29710=CARTESIAN_POINT('Ctrl Pts',(-2.82433189377224,-2.73954163939785,
23.1824399477745));
#29711=CARTESIAN_POINT('Ctrl Pts',(-2.90259026978656,-2.65395153040526,
23.1765886310144));
#29712=CARTESIAN_POINT('Ctrl Pts',(-2.98087461965353,-2.56833301416742,
23.1707353722099));
#29713=CARTESIAN_POINT('Ctrl Pts',(-3.05533571965474,-2.47928257742505,
23.1648821134054));
#29714=CARTESIAN_POINT('Ctrl Pts',(-3.12567393611546,-2.38718483680851,
23.1590288546009));
#29715=CARTESIAN_POINT('Ctrl Pts',(-3.19609217601749,-2.29498231704755,
23.1531689365728));
#29716=CARTESIAN_POINT('Ctrl Pts',(-3.2623779190213,-2.19972590231434,23.1473090185447));
#29717=CARTESIAN_POINT('Ctrl Pts',(-3.3242742158727,-2.10183014006459,23.1414491005165));
#29718=CARTESIAN_POINT('Ctrl Pts',(-3.38621218927206,-2.00386846179664,
23.1355852368379));
#29719=CARTESIAN_POINT('Ctrl Pts',(-3.44375462670587,-1.90326425534581,
23.1297213731593));
#29720=CARTESIAN_POINT('Ctrl Pts',(-3.49669083056497,-1.80045611872183,
23.1238575094807));
#29721=CARTESIAN_POINT('Ctrl Pts',(-3.54970512805217,-1.69749631537825,
23.1179849951933));
#29722=CARTESIAN_POINT('Ctrl Pts',(-3.59809945763546,-1.59232646697015,
23.1121124809059));
#29723=CARTESIAN_POINT('Ctrl Pts',(-3.64171142540951,-1.48540462300406,
23.1062399666185));
#29724=CARTESIAN_POINT('Ctrl Pts',(-3.65376483830642,-1.45585371762645,
23.1046169295701));
#29725=CARTESIAN_POINT('Ctrl Pts',(-3.66545324520294,-1.42616906922076,
23.1029938925218));
#29726=CARTESIAN_POINT('Ctrl Pts',(-3.67677389805233,-1.3963605202816,23.1013708554734));
#29727=CARTESIAN_POINT('Ctrl Pts',(-3.71773185213932,-1.28851363237739,
23.0954987315074));
#29728=CARTESIAN_POINT('Ctrl Pts',(-3.75400941182185,-1.1786823486373,23.0896266075413));
#29729=CARTESIAN_POINT('Ctrl Pts',(-3.78541109864318,-1.06731055193371,
23.0837544835753));
#29730=CARTESIAN_POINT('Ctrl Pts',(-3.81677207255405,-0.956083150975862,
23.0778899729346));
#29731=CARTESIAN_POINT('Ctrl Pts',(-3.84326963395159,-0.843319603191997,
23.0720254622938));
#29732=CARTESIAN_POINT('Ctrl Pts',(-3.86475657327649,-0.729483124764508,
23.0661609516531));
#29733=CARTESIAN_POINT('Ctrl Pts',(-3.88622140275456,-0.615763782940909,
23.0603024755355));
#29734=CARTESIAN_POINT('Ctrl Pts',(-3.90268578923377,-0.500974110244972,
23.0544439994179));
#29735=CARTESIAN_POINT('Ctrl Pts',(-3.9140526883743,-0.385591172914964,
23.0485855233003));
#29736=CARTESIAN_POINT('Ctrl Pts',(-3.92586779940491,-0.265658533525941,
23.042496039709));
#29737=CARTESIAN_POINT('Ctrl Pts',(-3.93217502788284,-0.145085318521391,
23.0364065561177));
#29738=CARTESIAN_POINT('Ctrl Pts',(-3.93292420072768,-0.024417848605377,
23.0303170725265));
#29739=CARTESIAN_POINT('Ctrl Pts',(-3.9336441177902,0.0915374627510185,
23.0244653880061));
#29740=CARTESIAN_POINT('Ctrl Pts',(-3.92923192319479,0.207579353356176,
23.0186137034857));
#29741=CARTESIAN_POINT('Ctrl Pts',(-3.91969613883907,0.323220016660573,
23.0127620189652));
#29742=CARTESIAN_POINT('Ctrl Pts',(-3.91016180889777,0.438843042249969,
23.0069112269539));
#29743=CARTESIAN_POINT('Ctrl Pts',(-3.89550547694663,0.554064550314612,
23.0010604349426));
#29744=CARTESIAN_POINT('Ctrl Pts',(-3.87578767339176,0.668400262406079,
22.9952096429313));
#29745=CARTESIAN_POINT('Ctrl Pts',(-3.85606810137642,0.782746229097468,
22.9893583261711));
#29746=CARTESIAN_POINT('Ctrl Pts',(-3.83128622559715,0.896205834461808,
22.983507009411));
#29747=CARTESIAN_POINT('Ctrl Pts',(-3.80155386518703,1.00830412578823,22.9776556926508));
#29748=CARTESIAN_POINT('Ctrl Pts',(-3.7718116366453,1.1204396223912,22.9718024338463));
#29749=CARTESIAN_POINT('Ctrl Pts',(-3.73711576228698,1.23121250716029,22.9659491750418));
#29750=CARTESIAN_POINT('Ctrl Pts',(-3.69762796824997,1.34016282906801,22.9600959162372));
#29751=CARTESIAN_POINT('Ctrl Pts',(-3.65809524914506,1.44923710321792,22.9542359982091));
#29752=CARTESIAN_POINT('Ctrl Pts',(-3.61375986977994,1.55648428691021,22.948376080181));
#29753=CARTESIAN_POINT('Ctrl Pts',(-3.56483180577043,1.66146417252,22.9425161621529));
#29754=CARTESIAN_POINT('Ctrl Pts',(-3.51587079709513,1.7665147440912,22.9366522984742));
#29755=CARTESIAN_POINT('Ctrl Pts',(-3.46231113681302,1.86929461202232,22.9307884347956));
#29756=CARTESIAN_POINT('Ctrl Pts',(-3.40440802965331,1.96938949109415,22.9249245711169));
#29757=CARTESIAN_POINT('Ctrl Pts',(-3.34641950148917,2.06963203417794,22.9190520568296));
#29758=CARTESIAN_POINT('Ctrl Pts',(-3.28407495980851,2.16718133593129,22.9131795425422));
#29759=CARTESIAN_POINT('Ctrl Pts',(-3.21767207744018,2.26165324531896,22.9073070282548));
#29760=CARTESIAN_POINT('Ctrl Pts',(-3.19931974436393,2.28776325569192,22.9056839912065));
#29761=CARTESIAN_POINT('Ctrl Pts',(-3.18065764414631,2.31363840249603,22.9040609541582));
#29762=CARTESIAN_POINT('Ctrl Pts',(-3.16169257377299,2.33927105504016,22.9024379171099));
#29763=CARTESIAN_POINT('Ctrl Pts',(-3.09307723047334,2.43200961173285,22.8965657931439));
#29764=CARTESIAN_POINT('Ctrl Pts',(-3.02026309303075,2.52188215266147,22.8906936691779));
#29765=CARTESIAN_POINT('Ctrl Pts',(-2.94351803671338,2.60848434297449,22.8848215452118));
#29766=CARTESIAN_POINT('Ctrl Pts',(-2.86687248188534,2.6949742518282,22.8789570345711));
#29767=CARTESIAN_POINT('Ctrl Pts',(-2.78630641495392,2.77820193549154,22.8730925239304));
#29768=CARTESIAN_POINT('Ctrl Pts',(-2.70213006103201,2.85779322787131,22.8672280132897));
#29769=CARTESIAN_POINT('Ctrl Pts',(-2.61804032374078,2.93730262160312,22.8613695371721));
#29770=CARTESIAN_POINT('Ctrl Pts',(-2.53034798725479,3.01318278436915,22.8555110610545));
#29771=CARTESIAN_POINT('Ctrl Pts',(-2.4394020373658,3.08509427734317,22.8496525849369));
#29772=CARTESIAN_POINT('Ctrl Pts',(-2.34486996820258,3.15984133574158,22.8435631013456));
#29773=CARTESIAN_POINT('Ctrl Pts',(-2.24682272007433,3.23029996503633,22.8374736177543));
#29774=CARTESIAN_POINT('Ctrl Pts',(-2.14569287915494,3.29613274434507,22.8313841341631));
#29775=CARTESIAN_POINT('Ctrl Pts',(-2.04851223718589,3.3593947024147,22.8255324496427));
#29776=CARTESIAN_POINT('Ctrl Pts',(-1.9484856189111,3.41838507004249,22.8196807651223));
#29777=CARTESIAN_POINT('Ctrl Pts',(-1.84602808994652,3.4728474327457,22.8138290806019));
#29778=CARTESIAN_POINT('Ctrl Pts',(-1.74358618798242,3.52730148875465,22.8079782885906));
#29779=CARTESIAN_POINT('Ctrl Pts',(-1.63871447747251,3.57722871901678,22.8021274965792));
#29780=CARTESIAN_POINT('Ctrl Pts',(-1.53185315802065,3.62241837758453,22.7962767045679));
#29781=CARTESIAN_POINT('Ctrl Pts',(-1.42498225433632,3.66761208914541,22.7904253878078));
#29782=CARTESIAN_POINT('Ctrl Pts',(-1.31612176776655,3.70806722330985,22.7845740710477));
#29783=CARTESIAN_POINT('Ctrl Pts',(-1.20573176459711,3.74362122975089,22.7787227542876));
#29784=CARTESIAN_POINT('Ctrl Pts',(-1.09530512312952,3.77918703652032,22.7728694954831));
#29785=CARTESIAN_POINT('Ctrl Pts',(-0.983348348942471,3.80984835435136,
22.7670162366785));
#29786=CARTESIAN_POINT('Ctrl Pts',(-0.870335852415045,3.83549273288335,
22.761162977874));
#29787=CARTESIAN_POINT('Ctrl Pts',(-0.757194782129312,3.86116628689795,
22.7553030598459));
#29788=CARTESIAN_POINT('Ctrl Pts',(-0.642995995563085,3.88181141756271,
22.7494431418178));
#29789=CARTESIAN_POINT('Ctrl Pts',(-0.528223361666999,3.89736694194801,
22.7435832237896));
#29790=CARTESIAN_POINT('Ctrl Pts',(-0.413373448071697,3.91293294031309,
22.737719360111));
#29791=CARTESIAN_POINT('Ctrl Pts',(-0.297949328490464,3.92340247136172,
22.7318554964324));
#29792=CARTESIAN_POINT('Ctrl Pts',(-0.182437499126775,3.92876641694468,
22.7259916327537));
#29793=CARTESIAN_POINT('Ctrl Pts',(-0.0667552620427459,3.93413827563701,
22.7201191184664));
#29794=CARTESIAN_POINT('Ctrl Pts',(0.0490145312043054,3.93438951556414,
22.714246604179));
#29795=CARTESIAN_POINT('Ctrl Pts',(0.164387793031867,3.92956303594969,22.7083740898916));
#29796=CARTESIAN_POINT('Ctrl Pts',(0.196274489116512,3.92822910045903,22.7067510528432));
#29797=CARTESIAN_POINT('Ctrl Pts',(0.228130943146691,3.92650760594574,22.7051280157949));
#29798=CARTESIAN_POINT('Ctrl Pts',(0.259947061604018,3.92440014845115,22.7035049787465));
#29799=CARTESIAN_POINT('Ctrl Pts',(0.375057306246639,3.91677539849614,22.6976328547805));
#29800=CARTESIAN_POINT('Ctrl Pts',(0.490024774287151,3.90406896245712,22.6917607308145));
#29801=CARTESIAN_POINT('Ctrl Pts',(0.604364495680487,3.88628776036475,22.6858886068485));
#29802=CARTESIAN_POINT('Ctrl Pts',(0.718555973355043,3.86852961195391,22.6800240962077));
#29803=CARTESIAN_POINT('Ctrl Pts',(0.832120918179618,3.84570984473741,22.674159585567));
#29804=CARTESIAN_POINT('Ctrl Pts',(0.944576861721214,3.81788731529637,22.6682950749263));
#29805=CARTESIAN_POINT('Ctrl Pts',(1.05691708921537,3.7900934149614,22.6624365988087));
#29806=CARTESIAN_POINT('Ctrl Pts',(1.16815018633433,3.75730709029619,22.6565781226911));
#29807=CARTESIAN_POINT('Ctrl Pts',(1.27780196137464,3.71963857753776,22.6507196465735));
#29808=CARTESIAN_POINT('Ctrl Pts',(1.39177745115346,3.68048474542421,22.6446301629822));
#29809=CARTESIAN_POINT('Ctrl Pts',(1.50404389635716,3.63605585179692,22.638540679391));
#29810=CARTESIAN_POINT('Ctrl Pts',(1.61408362998758,3.58653356814154,22.6324511957997));
#29811=CARTESIAN_POINT('Ctrl Pts',(1.71982622642691,3.5389451681831,22.6265995112793));
#29812=CARTESIAN_POINT('Ctrl Pts',(1.82351234490465,3.4866539005432,22.6207478267589));
#29813=CARTESIAN_POINT('Ctrl Pts',(1.92470194778825,3.42987046580189,22.6148961422385));
#29814=CARTESIAN_POINT('Ctrl Pts',(2.02587611705769,3.37309569176878,22.6090453502272));
#29815=CARTESIAN_POINT('Ctrl Pts',(2.12455416740145,3.31183031519032,22.6031945582158));
#29816=CARTESIAN_POINT('Ctrl Pts',(2.22032090750863,3.24633086232443,22.5973437662045));
#29817=CARTESIAN_POINT('Ctrl Pts',(2.31609623679193,3.18082553491027,22.5914924494444));
#29818=CARTESIAN_POINT('Ctrl Pts',(2.40895939551932,3.11108560970491,22.5856411326843));
#29819=CARTESIAN_POINT('Ctrl Pts',(2.49852501127375,3.0374103720175,22.5797898159242));
#29820=CARTESIAN_POINT('Ctrl Pts',(2.58812035373882,2.96371068161514,22.5739365571197));
#29821=CARTESIAN_POINT('Ctrl Pts',(2.67441565788307,2.88607334407693,22.5680832983152));
#29822=CARTESIAN_POINT('Ctrl Pts',(2.75705995669766,2.80483678583519,22.5622300395107));
#29823=CARTESIAN_POINT('Ctrl Pts',(2.83979827952272,2.72350780516248,22.5563701214825));
#29824=CARTESIAN_POINT('Ctrl Pts',(2.91887701127858,2.6385717206208,22.5505102034544));
#29825=CARTESIAN_POINT('Ctrl Pts',(2.99398321259888,2.55040261972028,22.5446502854263));
#29826=CARTESIAN_POINT('Ctrl Pts',(3.06913998507393,2.46217415204089,22.5387864217476));
#29827=CARTESIAN_POINT('Ctrl Pts',(3.14031864774902,2.37070865886867,22.532922558069));
#29828=CARTESIAN_POINT('Ctrl Pts',(3.20724865111092,2.27641057148028,22.5270586943904));
#29829=CARTESIAN_POINT('Ctrl Pts',(3.27427739231955,2.18197337174121,22.521186180103));
#29830=CARTESIAN_POINT('Ctrl Pts',(3.33704474156023,2.08469558383841,22.5153136658156));
#29831=CARTESIAN_POINT('Ctrl Pts',(3.3953252204052,1.98500771980373,22.5094411515282));
#29832=CARTESIAN_POINT('Ctrl Pts',(3.41143269528444,1.95745613138978,22.5078181144798));
#29833=CARTESIAN_POINT('Ctrl Pts',(3.42719772057107,1.92972057326528,22.5061950774315));
#29834=CARTESIAN_POINT('Ctrl Pts',(3.44261618523119,1.90181040095595,22.5045720403831));
#29835=CARTESIAN_POINT('Ctrl Pts',(3.50115409939407,1.7958463308018,22.4984099999001));
#29836=CARTESIAN_POINT('Ctrl Pts',(3.55487319665964,1.6870374951563,22.4922479594172));
#29837=CARTESIAN_POINT('Ctrl Pts',(3.60350142191582,1.57583834902272,22.4860859189342));
#29838=CARTESIAN_POINT('Ctrl Pts',(3.65204246483522,1.4648385645018,22.4799349259671));
#29839=CARTESIAN_POINT('Ctrl Pts',(3.69551067384141,1.35145732804514,22.473783933));
#29840=CARTESIAN_POINT('Ctrl Pts',(3.73367945692755,1.23617422433782,22.4676329400329));
#29841=CARTESIAN_POINT('Ctrl Pts',(3.77176063720777,1.1211557118106,22.4614960644727));
#29842=CARTESIAN_POINT('Ctrl Pts',(3.80456652708893,1.00424436862022,22.4553591889125));
#29843=CARTESIAN_POINT('Ctrl Pts',(3.83191863633248,0.885939368426433,22.4492223133524));
#29844=CARTESIAN_POINT('Ctrl Pts',(3.85923289212364,0.767798094278509,22.4430939308091));
#29845=CARTESIAN_POINT('Ctrl Pts',(3.88110831736986,0.64826734729674,22.4369655482658));
#29846=CARTESIAN_POINT('Ctrl Pts',(3.89741586819658,0.527862245599663,22.4308371657226));
#29847=CARTESIAN_POINT('Ctrl Pts',(3.913695364911,0.407664278516497,22.4247193259233));
#29848=CARTESIAN_POINT('Ctrl Pts',(3.92442603206477,0.286595304961994,22.4186014861239));
#29849=CARTESIAN_POINT('Ctrl Pts',(3.92952978485551,0.165180719012368,22.4124836463246));
#29850=CARTESIAN_POINT('Ctrl Pts',(3.93184344779074,0.11014035188924,22.4097102715614));
#29851=CARTESIAN_POINT('Ctrl Pts',(3.93300144940657,0.0550291046220322,
22.4069368967982));
#29852=CARTESIAN_POINT('Ctrl Pts',(3.93299999863833,-0.000103493608108607,
22.404163522035));
#29853=CARTESIAN_POINT('',(3.93299837124471,-0.00357935559718133,21.154163522035));
#29854=CARTESIAN_POINT('Ctrl Pts',(3.9329999986383,-0.000103494422981112,
22.404163521994));
#29855=CARTESIAN_POINT('Ctrl Pts',(3.9329967860024,-0.122190237360205,22.3980221047082));
#29856=CARTESIAN_POINT('Ctrl Pts',(3.92730461696609,-0.244162252495147,
22.3918806874223));
#29857=CARTESIAN_POINT('Ctrl Pts',(3.91598119473771,-0.365486364260817,
22.3857392701364));
#29858=CARTESIAN_POINT('Ctrl Pts',(3.90464111657057,-0.486988935059093,
22.379588819268));
#29859=CARTESIAN_POINT('Ctrl Pts',(3.88765329229108,-0.607841353962135,
22.3734383683995));
#29860=CARTESIAN_POINT('Ctrl Pts',(3.86512675196899,-0.727519203329828,
22.367287917531));
#29861=CARTESIAN_POINT('Ctrl Pts',(3.84254403578185,-0.847495500955385,
22.3611221288924));
#29862=CARTESIAN_POINT('Ctrl Pts',(3.81439505748278,-0.966291029651327,
22.3549563402538));
#29863=CARTESIAN_POINT('Ctrl Pts',(3.78083947401601,-1.08339368270371,22.3487905516151));
#29864=CARTESIAN_POINT('Ctrl Pts',(3.74723768458369,-1.20065758585503,22.342616272699));
#29865=CARTESIAN_POINT('Ctrl Pts',(3.70821454621656,-1.31622363179537,22.3364419937828));
#29866=CARTESIAN_POINT('Ctrl Pts',(3.663978222529,-1.42959874959138,22.3302677148666));
#29867=CARTESIAN_POINT('Ctrl Pts',(3.61964185622934,-1.54323027076782,22.3240794725163));
#29868=CARTESIAN_POINT('Ctrl Pts',(3.57006888036979,-1.65466064076861,22.317891230166));
#29869=CARTESIAN_POINT('Ctrl Pts',(3.51551436855138,-1.76341932747399,22.3117029878157));
#29870=CARTESIAN_POINT('Ctrl Pts',(3.49769496682149,-1.79894369870233,22.3096816925504));
#29871=CARTESIAN_POINT('Ctrl Pts',(3.4793444322737,-1.83418325163946,22.307660397285));
#29872=CARTESIAN_POINT('Ctrl Pts',(3.46047264866889,-1.86912226668416,22.3056391020197));
#29873=CARTESIAN_POINT('Ctrl Pts',(3.40564767841961,-1.97062462069992,22.2997669780537));
#29874=CARTESIAN_POINT('Ctrl Pts',(3.3462611177917,-2.06988291325659,22.2938948540876));
#29875=CARTESIAN_POINT('Ctrl Pts',(3.28252103059589,-2.16645901962065,22.2880227301216));
#29876=CARTESIAN_POINT('Ctrl Pts',(3.21886358368866,-2.26290991314534,22.2821582194809));
#29877=CARTESIAN_POINT('Ctrl Pts',(3.15086406056402,-2.35668519412931,22.2762937088402));
#29878=CARTESIAN_POINT('Ctrl Pts',(3.07877671234546,-2.44737062079271,22.2704291981994));
#29879=CARTESIAN_POINT('Ctrl Pts',(3.00676354129109,-2.5379627330542,22.2645707220818));
#29880=CARTESIAN_POINT('Ctrl Pts',(2.93067116743926,-2.62547099335779,22.2587122459642));
#29881=CARTESIAN_POINT('Ctrl Pts',(2.85079712008861,-2.70951006274095,22.2528537698466));
#29882=CARTESIAN_POINT('Ctrl Pts',(2.76777353324704,-2.79686290395091,22.2467642862553));
#29883=CARTESIAN_POINT('Ctrl Pts',(2.68066415523773,-2.88046695630752,22.2406748026641));
#29884=CARTESIAN_POINT('Ctrl Pts',(2.58984956229429,-2.95992706746029,22.2345853190728));
#29885=CARTESIAN_POINT('Ctrl Pts',(2.50258134984423,-3.03628419946554,22.2287336345524));
#29886=CARTESIAN_POINT('Ctrl Pts',(2.41189221550572,-3.10881466719643,22.222881950032));
#29887=CARTESIAN_POINT('Ctrl Pts',(2.31815683530451,-3.17720598748822,22.2170302655116));
#29888=CARTESIAN_POINT('Ctrl Pts',(2.22443575178628,-3.24558687661706,22.2111794735003));
#29889=CARTESIAN_POINT('Ctrl Pts',(2.12766968008904,-3.30982962994567,22.205328681489));
#29890=CARTESIAN_POINT('Ctrl Pts',(2.02826463018973,-3.3696634238335,22.1994778894777));
#29891=CARTESIAN_POINT('Ctrl Pts',(1.92885066479962,-3.42950258412515,22.1936265727175));
#29892=CARTESIAN_POINT('Ctrl Pts',(1.82679760491666,-3.48493178568025,22.1877752559574));
#29893=CARTESIAN_POINT('Ctrl Pts',(1.72253793702354,-3.53572511028709,22.1819239391972));
#29894=CARTESIAN_POINT('Ctrl Pts',(1.61824366548264,-3.58653529313212,22.1760706803927));
#29895=CARTESIAN_POINT('Ctrl Pts',(1.51174170111808,-3.63270635857377,22.1702174215882));
#29896=CARTESIAN_POINT('Ctrl Pts',(1.40348580876995,-3.67405995930678,22.1643641627836));
#29897=CARTESIAN_POINT('Ctrl Pts',(1.29510675422864,-3.71546060782677,22.1585042447555));
#29898=CARTESIAN_POINT('Ctrl Pts',(1.18497017529292,-3.75203270448121,22.1526443267274));
#29899=CARTESIAN_POINT('Ctrl Pts',(1.07354644358195,-3.7836473188542,22.1467844086993));
#29900=CARTESIAN_POINT('Ctrl Pts',(0.962047687083573,-3.81528322025182,
22.1409205450206));
#29901=CARTESIAN_POINT('Ctrl Pts',(0.849260453421637,-3.8419548978208,22.135056681342));
#29902=CARTESIAN_POINT('Ctrl Pts',(0.735665070846138,-3.86358459251728,
22.1291928176634));
#29903=CARTESIAN_POINT('Ctrl Pts',(0.621902107769854,-3.88524619621383,
22.123320303376));
#29904=CARTESIAN_POINT('Ctrl Pts',(0.507329023948782,-3.9018509128245,22.1174477890886));
#29905=CARTESIAN_POINT('Ctrl Pts',(0.392431112203861,-3.91337281921547,
22.1115752748012));
#29906=CARTESIAN_POINT('Ctrl Pts',(0.360675792691475,-3.91655722712403,
22.1099522377529));
#29907=CARTESIAN_POINT('Ctrl Pts',(0.328895657420771,-3.91935369076338,
22.1083292007045));
#29908=CARTESIAN_POINT('Ctrl Pts',(0.297100924157665,-3.92176236415016,
22.1067061636562));
#29909=CARTESIAN_POINT('Ctrl Pts',(0.18206805082896,-3.93047690873524,22.1008340396902));
#29910=CARTESIAN_POINT('Ctrl Pts',(0.0664585796198982,-3.93414056691307,
22.0949619157242));
#29911=CARTESIAN_POINT('Ctrl Pts',(-0.0492464061903585,-3.93269167256694,
22.0890897917581));
#29912=CARTESIAN_POINT('Ctrl Pts',(-0.164801378189099,-3.93124465674109,
22.0832252811174));
#29913=CARTESIAN_POINT('Ctrl Pts',(-0.280451208963663,-3.9246982752529,
22.0773607704767));
#29914=CARTESIAN_POINT('Ctrl Pts',(-0.395709954140918,-3.91304263102177,
22.071496259836));
#29915=CARTESIAN_POINT('Ctrl Pts',(-0.510850099215983,-3.90139898033261,
22.0656377837184));
#29916=CARTESIAN_POINT('Ctrl Pts',(-0.625599550294319,-3.88465656542435,
22.0597793076008));
#29917=CARTESIAN_POINT('Ctrl Pts',(-0.739473297777974,-3.86285752285447,
22.0539208314832));
#29918=CARTESIAN_POINT('Ctrl Pts',(-0.857837237966087,-3.84019891516028,
22.0478313478919));
#29919=CARTESIAN_POINT('Ctrl Pts',(-0.975254538460975,-3.81207670237197,
22.0417418643006));
#29920=CARTESIAN_POINT('Ctrl Pts',(-1.09118705804657,-3.77859759756866,
22.0356523807094));
#29921=CARTESIAN_POINT('Ctrl Pts',(-1.20259232256574,-3.74642587784921,
22.029800696189));
#29922=CARTESIAN_POINT('Ctrl Pts',(-1.31262615914762,-3.70930792204073,
22.0239490116686));
#29923=CARTESIAN_POINT('Ctrl Pts',(-1.4208231760497,-3.66739014864795,22.0180973271482));
#29924=CARTESIAN_POINT('Ctrl Pts',(-1.52900369055487,-3.62547876862677,
22.0122465351369));
#29925=CARTESIAN_POINT('Ctrl Pts',(-1.63534755702896,-3.5787691759257,22.0063957431256));
#29926=CARTESIAN_POINT('Ctrl Pts',(-1.73940750656553,-3.5274566653757,22.0005449511142));
#29927=CARTESIAN_POINT('Ctrl Pts',(-1.84347678908387,-3.47613955268312,
21.9946936343541));
#29928=CARTESIAN_POINT('Ctrl Pts',(-1.94526137665291,-3.4202188843225,21.988842317594));
#29929=CARTESIAN_POINT('Ctrl Pts',(-2.04433747915184,-3.35993649811051,
21.9829910008339));
#29930=CARTESIAN_POINT('Ctrl Pts',(-2.14344646487984,-3.29963410425324,
21.9771377420293));
#29931=CARTESIAN_POINT('Ctrl Pts',(-2.23984482505981,-3.23496732876461,
21.9712844832248));
#29932=CARTESIAN_POINT('Ctrl Pts',(-2.33313730000854,-3.16622161879248,
21.9654312244203));
#29933=CARTESIAN_POINT('Ctrl Pts',(-2.42653591334463,-3.0973976971661,21.9595713063922));
#29934=CARTESIAN_POINT('Ctrl Pts',(-2.51682125556449,-3.02448582396564,
21.9537113883641));
#29935=CARTESIAN_POINT('Ctrl Pts',(-2.60363067498649,-2.94781212228144,
21.9478514703359));
#29936=CARTESIAN_POINT('Ctrl Pts',(-2.69049854567493,-2.87108679399961,
21.9419876066573));
#29937=CARTESIAN_POINT('Ctrl Pts',(-2.77388553657606,-2.7905948800586,21.9361237429787));
#29938=CARTESIAN_POINT('Ctrl Pts',(-2.85346667369742,-2.70669853180922,
21.9302598793001));
#29939=CARTESIAN_POINT('Ctrl Pts',(-2.9331652121296,-2.62267841627511,21.9243873650127));
#29940=CARTESIAN_POINT('Ctrl Pts',(-3.00904642122821,-2.53524415379346,
21.9185148507253));
#29941=CARTESIAN_POINT('Ctrl Pts',(-3.08082626130832,-2.44479008252917,
21.9126423364379));
#29942=CARTESIAN_POINT('Ctrl Pts',(-3.10066467022034,-2.4197905164742,21.9110192993895));
#29943=CARTESIAN_POINT('Ctrl Pts',(-3.12019005574155,-2.3945604445957,21.9093962623412));
#29944=CARTESIAN_POINT('Ctrl Pts',(-3.13939702632131,-2.3691085477717,21.9077732252928));
#29945=CARTESIAN_POINT('Ctrl Pts',(-3.20888756097712,-2.27702396259676,
21.9019011013268));
#29946=CARTESIAN_POINT('Ctrl Pts',(-3.27443963197061,-2.18172496883002,
21.8960289773608));
#29947=CARTESIAN_POINT('Ctrl Pts',(-3.33574139859285,-2.08358304891209,
21.8901568533947));
#29948=CARTESIAN_POINT('Ctrl Pts',(-3.39696368625746,-1.98556837194203,
21.884292342754));
#29949=CARTESIAN_POINT('Ctrl Pts',(-3.45394641115383,-1.88471844615048,
21.8784278321133));
#29950=CARTESIAN_POINT('Ctrl Pts',(-3.50641866652358,-1.78143681758715,
21.8725633214726));
#29951=CARTESIAN_POINT('Ctrl Pts',(-3.55883692846457,-1.6782614647921,21.866704845355));
#29952=CARTESIAN_POINT('Ctrl Pts',(-3.60675376637638,-1.57265975256975,
21.8608463692374));
#29953=CARTESIAN_POINT('Ctrl Pts',(-3.64994256188307,-1.46506255666932,
21.8549878931197));
#29954=CARTESIAN_POINT('Ctrl Pts',(-3.69483434880596,-1.35322266080759,
21.8488984095285));
#29955=CARTESIAN_POINT('Ctrl Pts',(-3.73461731533458,-1.23922706053372,
21.8428089259372));
#29956=CARTESIAN_POINT('Ctrl Pts',(-3.76909047092907,-1.12358623253923,
21.8367194423459));
#29957=CARTESIAN_POINT('Ctrl Pts',(-3.80221742298311,-1.01246126882759,
21.8308677578255));
#29958=CARTESIAN_POINT('Ctrl Pts',(-3.83044135719184,-0.899817594464047,
21.8250160733051));
#29959=CARTESIAN_POINT('Ctrl Pts',(-3.85363400283394,-0.786125926427865,
21.8191643887847));
#29960=CARTESIAN_POINT('Ctrl Pts',(-3.87682311109344,-0.672451598842391,
21.8133135967734));
#29961=CARTESIAN_POINT('Ctrl Pts',(-3.89498237396998,-0.557730000358334,
21.8074628047621));
#29962=CARTESIAN_POINT('Ctrl Pts',(-3.90803443996023,-0.442443008855035,
21.8016120127508));
#29963=CARTESIAN_POINT('Ctrl Pts',(-3.92108767657085,-0.327145677433238,
21.7957606959906));
#29964=CARTESIAN_POINT('Ctrl Pts',(-3.92903275921059,-0.211283262999728,
21.7899093792305));
#29965=CARTESIAN_POINT('Ctrl Pts',(-3.93184418629909,-0.0953430367987633,
21.7840580624704));
#29966=CARTESIAN_POINT('Ctrl Pts',(-3.93465654649658,0.0206356698118804,
21.7782048036658));
#29967=CARTESIAN_POINT('Ctrl Pts',(-3.93233185312455,0.136691826469843,
21.7723515448613));
#29968=CARTESIAN_POINT('Ctrl Pts',(-3.92489671567469,0.252338604430756,
21.7664982860568));
#29969=CARTESIAN_POINT('Ctrl Pts',(-3.91745311930571,0.368116953159008,
21.7606383680287));
#29970=CARTESIAN_POINT('Ctrl Pts',(-3.90488750055562,0.483484580762219,
21.7547784500005));
#29971=CARTESIAN_POINT('Ctrl Pts',(-3.88727831501467,0.59796011707865,21.7489185319724));
#29972=CARTESIAN_POINT('Ctrl Pts',(-3.86965727270514,0.712512733049828,
21.7430546682938));
#29973=CARTESIAN_POINT('Ctrl Pts',(-3.84698598222039,0.826171657244995,
21.7371908046151));
#29974=CARTESIAN_POINT('Ctrl Pts',(-3.8193935738895,0.938467755296662,21.7313269409365));
#29975=CARTESIAN_POINT('Ctrl Pts',(-3.79176046012235,1.05092951709206,21.7254544266491));
#29976=CARTESIAN_POINT('Ctrl Pts',(-3.75919185509884,1.16202404493571,21.7195819123617));
#29977=CARTESIAN_POINT('Ctrl Pts',(-3.7218660912396,1.27129925622602,21.7137093980743));
#29978=CARTESIAN_POINT('Ctrl Pts',(-3.71155005033509,1.30150058187796,21.712086361026));
#29979=CARTESIAN_POINT('Ctrl Pts',(-3.70087091071236,1.33156306985958,21.7104633239777));
#29980=CARTESIAN_POINT('Ctrl Pts',(-3.68983306351299,1.36147749280197,21.7088402869293));
#29981=CARTESIAN_POINT('Ctrl Pts',(-3.64989829607244,1.46970743128049,21.7029681629633));
#29982=CARTESIAN_POINT('Ctrl Pts',(-3.60513065091982,1.57636028015001,21.6970960389973));
#29983=CARTESIAN_POINT('Ctrl Pts',(-3.55567420649336,1.68097291390368,21.6912239150312));
#29984=CARTESIAN_POINT('Ctrl Pts',(-3.50628188332908,1.78544991530054,21.6853594043905));
#29985=CARTESIAN_POINT('Ctrl Pts',(-3.45221302511802,1.88789159158776,21.6794948937498));
#29986=CARTESIAN_POINT('Ctrl Pts',(-3.39366080852721,1.98785193529762,21.6736303831091));
#29987=CARTESIAN_POINT('Ctrl Pts',(-3.33516884158474,2.08770942080828,21.6677719069915));
#29988=CARTESIAN_POINT('Ctrl Pts',(-3.27220290009002,2.18509029773725,21.6619134308738));
#29989=CARTESIAN_POINT('Ctrl Pts',(-3.20500308818911,2.27957105717244,21.6560549547562));
#29990=CARTESIAN_POINT('Ctrl Pts',(-3.1351534986898,2.37777731810457,21.649965471165));
#29991=CARTESIAN_POINT('Ctrl Pts',(-3.06072946983559,2.47284963393164,21.6438759875737));
#29992=CARTESIAN_POINT('Ctrl Pts',(-2.98205193327693,2.56434304788562,21.6377865039824));
#29993=CARTESIAN_POINT('Ctrl Pts',(-2.90644681571913,2.6522635728578,21.631934819462));
#29994=CARTESIAN_POINT('Ctrl Pts',(-2.82691445693249,2.73687912546003,21.6260831349416));
#29995=CARTESIAN_POINT('Ctrl Pts',(-2.74378162707226,2.81782742249072,21.6202314504212));
#29996=CARTESIAN_POINT('Ctrl Pts',(-2.66066147677571,2.89876337314649,21.6143806584099));
#29997=CARTESIAN_POINT('Ctrl Pts',(-2.57394224339891,2.97603289203649,21.6085298663986));
#29998=CARTESIAN_POINT('Ctrl Pts',(-2.48398760242921,3.04931051075124,21.6026790743873));
#29999=CARTESIAN_POINT('Ctrl Pts',(-2.39402489356179,3.12259470162643,21.5968277576272));
#30000=CARTESIAN_POINT('Ctrl Pts',(-2.30082652079628,3.19188601948351,21.590976440867));
#30001=CARTESIAN_POINT('Ctrl Pts',(-2.20478871481115,3.25689971031369,21.5851251241069));
#30002=CARTESIAN_POINT('Ctrl Pts',(-2.10871903400364,3.32193497910295,21.5792718653024));
#30003=CARTESIAN_POINT('Ctrl Pts',(-2.00980838823148,3.38268956617601,21.5734186064979));
#30004=CARTESIAN_POINT('Ctrl Pts',(-1.90848079393494,3.43892280506287,21.5675653476933));
#30005=CARTESIAN_POINT('Ctrl Pts',(-1.80703791973546,3.49522002022753,21.5617054296652));
#30006=CARTESIAN_POINT('Ctrl Pts',(-1.70317297027669,3.54698541935955,21.5558455116371));
#30007=CARTESIAN_POINT('Ctrl Pts',(-1.59733338384113,3.59402491099695,21.549985593609));
#30008=CARTESIAN_POINT('Ctrl Pts',(-1.49142253258304,3.64109607567028,21.5441217299304));
#30009=CARTESIAN_POINT('Ctrl Pts',(-1.38353478079582,3.68343484603208,21.5382578662517));
#30010=CARTESIAN_POINT('Ctrl Pts',(-1.27413465303335,3.72089638204823,21.5323940025731));
#30011=CARTESIAN_POINT('Ctrl Pts',(-1.16457313377961,3.75841318283679,21.5265214882857));
#30012=CARTESIAN_POINT('Ctrl Pts',(-1.05349518082514,3.79103827314213,21.5206489739983));
#30013=CARTESIAN_POINT('Ctrl Pts',(-0.941377556893697,3.81867742751032,
21.5147764597109));
#30014=CARTESIAN_POINT('Ctrl Pts',(-0.910390649326295,3.82631629722248,
21.5131534226626));
#30015=CARTESIAN_POINT('Ctrl Pts',(-0.879324366010399,3.83357461986997,
21.5115303856142));
#30016=CARTESIAN_POINT('Ctrl Pts',(-0.848188843983448,3.84045110435506,
21.5099073485659));
#30017=CARTESIAN_POINT('Ctrl Pts',(-0.735540987129409,3.86533012322185,
21.5040352245999));
#30018=CARTESIAN_POINT('Ctrl Pts',(-0.621608724895704,3.88529037990338,
21.4981631006338));
#30019=CARTESIAN_POINT('Ctrl Pts',(-0.506859602906506,3.9002028592038,21.4922909766678));
#30020=CARTESIAN_POINT('Ctrl Pts',(-0.392259255432419,3.9150960041787,21.4864264660271));
#30021=CARTESIAN_POINT('Ctrl Pts',(-0.276844560494443,3.92495433370975,
21.4805619553864));
#30022=CARTESIAN_POINT('Ctrl Pts',(-0.161095189999589,3.92969939559745,
21.4746974447457));
#30023=CARTESIAN_POINT('Ctrl Pts',(-0.0454649244554603,3.93443957486369,
21.4688389686281));
#30024=CARTESIAN_POINT('Ctrl Pts',(0.0704989210831195,3.93407693503178,
21.4629804925105));
#30025=CARTESIAN_POINT('Ctrl Pts',(0.186310248777662,3.92858466768891,21.4571220163929));
#30026=CARTESIAN_POINT('Ctrl Pts',(0.306688170530945,3.92287583296946,21.4510325328016));
#30027=CARTESIAN_POINT('Ctrl Pts',(0.426900847770564,3.91162445356513,21.4449430492103));
#30028=CARTESIAN_POINT('Ctrl Pts',(0.546400460576367,3.89486014340463,21.438853565619));
#30029=CARTESIAN_POINT('Ctrl Pts',(0.661233520550923,3.8787504925958,21.4330018810986));
#30030=CARTESIAN_POINT('Ctrl Pts',(0.775407714478856,3.85755046247219,21.4271501965782));
#30031=CARTESIAN_POINT('Ctrl Pts',(0.888441632612912,3.83133925219891,21.4212985120578));
#30032=CARTESIAN_POINT('Ctrl Pts',(1.00145831061734,3.80513203970497,21.4154477200465));
#30033=CARTESIAN_POINT('Ctrl Pts',(1.11333465601346,3.77391526011858,21.4095969280352));
#30034=CARTESIAN_POINT('Ctrl Pts',(1.22360029484686,3.73781905908388,21.4037461360239));
#30035=CARTESIAN_POINT('Ctrl Pts',(1.33387582324108,3.7017196206347,21.3978948192638));
#30036=CARTESIAN_POINT('Ctrl Pts',(1.44253996497586,3.66074001939788,21.3920435025036));
#30037=CARTESIAN_POINT('Ctrl Pts',(1.54913901377223,3.61505979425082,21.3861921857435));
#30038=CARTESIAN_POINT('Ctrl Pts',(1.65577344265372,3.56936440789667,21.380338926939));
#30039=CARTESIAN_POINT('Ctrl Pts',(1.76034103592844,3.51896545816352,21.3744856681345));
#30040=CARTESIAN_POINT('Ctrl Pts',(1.86241017044259,3.46408968663226,21.3686324093299));
#30041=CARTESIAN_POINT('Ctrl Pts',(1.96459542850639,3.40915148320706,21.3627724913018));
#30042=CARTESIAN_POINT('Ctrl Pts',(2.06427618994552,3.34972648785753,21.3569125732737));
#30043=CARTESIAN_POINT('Ctrl Pts',(2.16104736582602,3.28608631698202,21.3510526552456));
#30044=CARTESIAN_POINT('Ctrl Pts',(2.25788370050872,3.22240329535813,21.3451887915669));
#30045=CARTESIAN_POINT('Ctrl Pts',(2.35180621445919,3.15449968842387,21.3393249278883));
#30046=CARTESIAN_POINT('Ctrl Pts',(2.44244202842624,3.08268810257819,21.3334610642097));
#30047=CARTESIAN_POINT('Ctrl Pts',(2.53321155201019,3.01077057737794,21.3275885499223));
#30048=CARTESIAN_POINT('Ctrl Pts',(2.62068438736605,2.93493383677828,21.3217160356349));
#30049=CARTESIAN_POINT('Ctrl Pts',(2.70452363159946,2.85552813435975,21.3158435213475));
#30050=CARTESIAN_POINT('Ctrl Pts',(2.7276950012782,2.83358210058806,21.3142204842991));
#30051=CARTESIAN_POINT('Ctrl Pts',(2.7505890532504,2.81136364899845,21.3125974472508));
#30052=CARTESIAN_POINT('Ctrl Pts',(2.77319922360723,2.78888061167635,21.3109744102024));
#30053=CARTESIAN_POINT('Ctrl Pts',(2.85386063832436,2.70867274199126,21.305184251951));
#30054=CARTESIAN_POINT('Ctrl Pts',(2.93119302544246,2.62480957187567,21.2993940936995));
#30055=CARTESIAN_POINT('Ctrl Pts',(3.00483960642236,2.53760279391309,21.293603935448));
#30056=CARTESIAN_POINT('Ctrl Pts',(3.07873877903787,2.45009691581051,21.2877939182225));
#30057=CARTESIAN_POINT('Ctrl Pts',(3.1489264602448,2.35922470143109,21.281983900997));
#30058=CARTESIAN_POINT('Ctrl Pts',(3.21507690142854,2.26534092752077,21.2761738837714));
#30059=CARTESIAN_POINT('Ctrl Pts',(3.28083667184213,2.17201161168513,21.2703981793012));
#30060=CARTESIAN_POINT('Ctrl Pts',(3.34260648871566,2.07570654588649,21.264622474831));
#30061=CARTESIAN_POINT('Ctrl Pts',(3.40010512745083,1.97680907582968,21.2588467703608));
#30062=CARTESIAN_POINT('Ctrl Pts',(3.45756656704702,1.87797558816991,21.2530748025222));
#30063=CARTESIAN_POINT('Ctrl Pts',(3.51076210601668,1.77655339587996,21.2473028346837));
#30064=CARTESIAN_POINT('Ctrl Pts',(3.55945375553484,1.67295485958495,21.2415308668451));
#30065=CARTESIAN_POINT('Ctrl Pts',(3.60812647113049,1.56939660795228,21.235761143457));
#30066=CARTESIAN_POINT('Ctrl Pts',(3.65229859812937,1.4636640797495,21.2299914200688));
#30067=CARTESIAN_POINT('Ctrl Pts',(3.69177846402697,1.35619348639738,21.2242216966807));
#30068=CARTESIAN_POINT('Ctrl Pts',(3.73172675897349,1.24744775325724,21.2183835154602));
#30069=CARTESIAN_POINT('Ctrl Pts',(3.76687052644689,1.13692284275504,21.2125453342397));
#30070=CARTESIAN_POINT('Ctrl Pts',(3.79706196232525,1.02508997374023,21.2067071530192));
#30071=CARTESIAN_POINT('Ctrl Pts',(3.82690916046214,0.914532204538681,21.2009355377722));
#30072=CARTESIAN_POINT('Ctrl Pts',(3.85191631229563,0.802696579324076,21.1951639225251));
#30073=CARTESIAN_POINT('Ctrl Pts',(3.87199158259496,0.690050856324234,21.189392307278));
#30074=CARTESIAN_POINT('Ctrl Pts',(3.89241415512724,0.575456361997903,21.1835208430708));
#30075=CARTESIAN_POINT('Ctrl Pts',(3.90773252666534,0.460023929919707,21.1776493788637));
#30076=CARTESIAN_POINT('Ctrl Pts',(3.9179049576323,0.344252440746937,21.1717779146565));
#30077=CARTESIAN_POINT('Ctrl Pts',(3.92807738859927,0.228480951574167,21.1659064504493));
#30078=CARTESIAN_POINT('Ctrl Pts',(3.93310389559052,0.11237086755328,21.1600349862422));
#30079=CARTESIAN_POINT('Ctrl Pts',(3.93299837124471,-0.00357935559718133,
21.154163522035));
#30080=CARTESIAN_POINT('',(3.93453862278255,0.00168715760829792,19.904163522035));
#30081=CARTESIAN_POINT('Ctrl Pts',(3.93385572002521,-0.00358013585587236,
21.154163522035));
#30082=CARTESIAN_POINT('Ctrl Pts',(3.9364368881255,-0.280919883983378,21.1401228386363));
#30083=CARTESIAN_POINT('Ctrl Pts',(3.78295630631491,-1.86523628308173,21.0597711757834));
#30084=CARTESIAN_POINT('Ctrl Pts',(1.63507764328188,-4.35555465900237,20.9131085334754));
#30085=CARTESIAN_POINT('Ctrl Pts',(-2.78143531328603,-3.72933678891077,
20.7141755951122));
#30086=CARTESIAN_POINT('Ctrl Pts',(-4.64096218155626,0.325277291681748,
20.5152426567487));
#30087=CARTESIAN_POINT('Ctrl Pts',(-2.23403148460003,4.08086248395284,20.3163097183853));
#30088=CARTESIAN_POINT('Ctrl Pts',(2.22665448024071,4.08489230124149,20.1173767800218));
#30089=CARTESIAN_POINT('Ctrl Pts',(3.8935518733233,1.49431200163386,19.9799947145718));
#30090=CARTESIAN_POINT('Ctrl Pts',(3.93915414306072,0.0954158123487556,
19.9089236285761));
#30091=CARTESIAN_POINT('Ctrl Pts',(3.93864968270786,0.00168892045947167,
19.904163522035));
#30092=CARTESIAN_POINT('',(3.93210890370979,0.00278794103289284,18.6541635611165));
#30093=CARTESIAN_POINT('Ctrl Pts',(3.93299963840903,0.00168649768106297,
19.904163522035));
#30094=CARTESIAN_POINT('Ctrl Pts',(3.9330486303541,-0.112565246857441,19.898352669845));
#30095=CARTESIAN_POINT('Ctrl Pts',(3.92811496827436,-0.227020618325729,
19.892541817655));
#30096=CARTESIAN_POINT('Ctrl Pts',(3.91817167495914,-0.341203349262369,
19.886730965465));
#30097=CARTESIAN_POINT('Ctrl Pts',(3.90824065065424,-0.455245190349012,
19.8809272832743));
#30098=CARTESIAN_POINT('Ctrl Pts',(3.89331231900895,-0.569014642437496,
19.8751236010836));
#30099=CARTESIAN_POINT('Ctrl Pts',(3.87341170273253,-0.682034296157216,
19.8693199188928));
#30100=CARTESIAN_POINT('Ctrl Pts',(3.8535300506206,-0.794946248523693,19.8635217672837));
#30101=CARTESIAN_POINT('Ctrl Pts',(3.8286856079953,-0.907109409310164,19.8577236156747));
#30102=CARTESIAN_POINT('Ctrl Pts',(3.79895523187636,-1.01805115107208,19.8519254640656));
#30103=CARTESIAN_POINT('Ctrl Pts',(3.76924333610225,-1.12892393165994,19.8461309165765));
#30104=CARTESIAN_POINT('Ctrl Pts',(3.73465165362909,-1.23857639555064,19.8403363690873));
#30105=CARTESIAN_POINT('Ctrl Pts',(3.6953080442437,-1.34654649312522,19.8345418215982));
#30106=CARTESIAN_POINT('Ctrl Pts',(3.65597667055693,-1.4544830124492,19.8287490761892));
#30107=CARTESIAN_POINT('Ctrl Pts',(3.61189645120518,-1.56073780846829,19.8229563307802));
#30108=CARTESIAN_POINT('Ctrl Pts',(3.5632447555487,-1.66486510326053,19.8171635853712));
#30109=CARTESIAN_POINT('Ctrl Pts',(3.51459582578694,-1.76898647831797,19.8113711692852));
#30110=CARTESIAN_POINT('Ctrl Pts',(3.46137611556296,-1.87098020983424,19.8055787531992));
#30111=CARTESIAN_POINT('Ctrl Pts',(3.40381032984178,-1.97042235027478,19.7997863371132));
#30112=CARTESIAN_POINT('Ctrl Pts',(3.34623318594587,-2.06988411141871,19.7939927781388));
#30113=CARTESIAN_POINT('Ctrl Pts',(3.28430847461729,-2.16679291556439,19.7881992191643));
#30114=CARTESIAN_POINT('Ctrl Pts',(3.21830542378325,-2.26075191015009,19.7824056601898));
#30115=CARTESIAN_POINT('Ctrl Pts',(3.1522329179153,-2.3548097778193,19.7766060046512));
#30116=CARTESIAN_POINT('Ctrl Pts',(3.08207374807207,-2.4459112927357,19.7708063491126));
#30117=CARTESIAN_POINT('Ctrl Pts',(3.00813882466016,-2.53369094634136,19.7650066935739));
#30118=CARTESIAN_POINT('Ctrl Pts',(2.9341614336904,-2.6215210197939,19.7592037067651));
#30119=CARTESIAN_POINT('Ctrl Pts',(2.85640425805586,-2.70602512345837,19.7534007199562));
#30120=CARTESIAN_POINT('Ctrl Pts',(2.77521530495391,-2.78687441610661,19.7475977331474));
#30121=CARTESIAN_POINT('Ctrl Pts',(2.69389971201757,-2.86784981878142,19.7417856947464));
#30122=CARTESIAN_POINT('Ctrl Pts',(2.60914196606835,-2.94515874444064,19.7359736563455));
#30123=CARTESIAN_POINT('Ctrl Pts',(2.52132351813424,-3.01851233505897,19.7301616179445));
#30124=CARTESIAN_POINT('Ctrl Pts',(2.4676803058116,-3.06331980238201,19.726611379728));
#30125=CARTESIAN_POINT('Ctrl Pts',(2.4128956596014,-3.10665225137229,19.7230611415115));
#30126=CARTESIAN_POINT('Ctrl Pts',(2.3570614911877,-3.14845202071749,19.719510903295));
#30127=CARTESIAN_POINT('Ctrl Pts',(2.26471130551823,-3.21758919190929,19.7136387793289));
#30128=CARTESIAN_POINT('Ctrl Pts',(2.16916182641396,-3.28277561125713,19.7077666553629));
#30129=CARTESIAN_POINT('Ctrl Pts',(2.07078572851163,-3.34370086380234,19.7018945313969));
#30130=CARTESIAN_POINT('Ctrl Pts',(1.97253717717358,-3.40454712554791,19.6960300207562));
#30131=CARTESIAN_POINT('Ctrl Pts',(1.87146964315069,-3.46114299143328,19.6901655101154));
#30132=CARTESIAN_POINT('Ctrl Pts',(1.76798770760113,-3.51321910301241,19.6843009994747));
#30133=CARTESIAN_POINT('Ctrl Pts',(1.6646122539337,-3.56524162879083,19.6784425233571));
#30134=CARTESIAN_POINT('Ctrl Pts',(1.55882770738393,-3.61275346616886,19.6725840472395));
#30135=CARTESIAN_POINT('Ctrl Pts',(1.45106580890289,-3.65552964948077,19.6667255711219));
#30136=CARTESIAN_POINT('Ctrl Pts',(1.3390547160197,-3.69999255436344,19.6606360875306));
#30137=CARTESIAN_POINT('Ctrl Pts',(1.22490751072737,-3.73933841604629,19.6545466039394));
#30138=CARTESIAN_POINT('Ctrl Pts',(1.1091354361331,-3.77336820152948,19.6484571203481));
#30139=CARTESIAN_POINT('Ctrl Pts',(0.997884351103417,-3.80606909741997,
19.6426054358277));
#30140=CARTESIAN_POINT('Ctrl Pts',(0.885133354146109,-3.83386119200615,
19.6367537513073));
#30141=CARTESIAN_POINT('Ctrl Pts',(0.771353650297388,-3.85661801922006,
19.6309020667869));
#30142=CARTESIAN_POINT('Ctrl Pts',(0.657591300326917,-3.87937137552313,
19.6250512747756));
#30143=CARTESIAN_POINT('Ctrl Pts',(0.542800960703745,-3.89709091039657,
19.6192004827643));
#30144=CARTESIAN_POINT('Ctrl Pts',(0.427464802167997,-3.90970111938336,
19.6133496907529));
#30145=CARTESIAN_POINT('Ctrl Pts',(0.312118299304034,-3.922312459361,19.6074983739928));
#30146=CARTESIAN_POINT('Ctrl Pts',(0.196226291200135,-3.92981351756233,
19.6016470572327));
#30147=CARTESIAN_POINT('Ctrl Pts',(0.0802761432412044,-3.93218065973911,
19.5957957404725));
#30148=CARTESIAN_POINT('Ctrl Pts',(-0.0357124884206846,-3.9345485875673,
19.589942481668));
#30149=CARTESIAN_POINT('Ctrl Pts',(-0.151758885199464,-3.93177920276364,
19.5840892228635));
#30150=CARTESIAN_POINT('Ctrl Pts',(-0.267376323888127,-3.92390098007379,
19.5782359640589));
#30151=CARTESIAN_POINT('Ctrl Pts',(-0.383125299964816,-3.91601379436896,
19.5723760460308));
#30152=CARTESIAN_POINT('Ctrl Pts',(-0.498443931167058,-3.90300619770365,
19.5665161280027));
#30153=CARTESIAN_POINT('Ctrl Pts',(-0.61285115149628,-3.88495848962504,
19.5606562099746));
#30154=CARTESIAN_POINT('Ctrl Pts',(-0.727335405481232,-3.86689862950807,
19.554792346296));
#30155=CARTESIAN_POINT('Ctrl Pts',(-0.840906622513694,-3.84379198277531,
19.5489284826173));
#30156=CARTESIAN_POINT('Ctrl Pts',(-0.953096166476963,-3.81576947645516,
19.5430646189387));
#30157=CARTESIAN_POINT('Ctrl Pts',(-1.06545121699102,-3.78770563020081,
19.5371921046513));
#30158=CARTESIAN_POINT('Ctrl Pts',(-1.17642013158342,-3.7547115679444,19.5313195903639));
#30159=CARTESIAN_POINT('Ctrl Pts',(-1.28555151431262,-3.71696735310502,
19.5254470760765));
#30160=CARTESIAN_POINT('Ctrl Pts',(-1.31571308883352,-3.70653566132085,
19.5238240390282));
#30161=CARTESIAN_POINT('Ctrl Pts',(-1.34573443536757,-3.69574140548776,
19.5222010019798));
#30162=CARTESIAN_POINT('Ctrl Pts',(-1.37560634343977,-3.68458901207289,
19.5205779649315));
#30163=CARTESIAN_POINT('Ctrl Pts',(-1.48368246374951,-3.64423981812336,
19.5147058409655));
#30164=CARTESIAN_POINT('Ctrl Pts',(-1.59016298721955,-3.59906382509579,
19.5088337169995));
#30165=CARTESIAN_POINT('Ctrl Pts',(-1.69458534382848,-3.549206884993,19.5029615930334));
#30166=CARTESIAN_POINT('Ctrl Pts',(-1.79887231477886,-3.49941458540291,
19.4970970823927));
#30167=CARTESIAN_POINT('Ctrl Pts',(-1.90110605583298,-3.44495358413687,
19.491232571752));
#30168=CARTESIAN_POINT('Ctrl Pts',(-2.00084130301933,-3.3860187654725,19.4853680611113));
#30169=CARTESIAN_POINT('Ctrl Pts',(-2.10047392362842,-3.32714459015029,
19.4795095849937));
#30170=CARTESIAN_POINT('Ctrl Pts',(-2.19761281028807,-3.26380596308677,
19.473651108876));
#30171=CARTESIAN_POINT('Ctrl Pts',(-2.29183537723579,-3.19624460948321,
19.4677926327584));
#30172=CARTESIAN_POINT('Ctrl Pts',(-2.38977326480867,-3.12601922221301,
19.4617031491672));
#30173=CARTESIAN_POINT('Ctrl Pts',(-2.48455970176964,-3.05123143794407,
19.4556136655759));
#30174=CARTESIAN_POINT('Ctrl Pts',(-2.57575096437571,-2.97220389097343,
19.4495241819846));
#30175=CARTESIAN_POINT('Ctrl Pts',(-2.66338113724523,-2.89626243118241,
19.4436724974642));
#30176=CARTESIAN_POINT('Ctrl Pts',(-2.74769131345249,-2.81640642311625,
19.4378208129438));
#30177=CARTESIAN_POINT('Ctrl Pts',(-2.82832046458625,-2.73296402274208,
19.4319691284234));
#30178=CARTESIAN_POINT('Ctrl Pts',(-2.90893731802168,-2.64953434914792,
19.4261183364121));
#30179=CARTESIAN_POINT('Ctrl Pts',(-2.9858739755019,-2.56251966807222,19.4202675444008));
#30180=CARTESIAN_POINT('Ctrl Pts',(-3.05880636455274,-2.47228489947491,
19.4144167523895));
#30181=CARTESIAN_POINT('Ctrl Pts',(-3.1317452948009,-2.38204203785563,19.4085654356294));
#30182=CARTESIAN_POINT('Ctrl Pts',(-3.20067898280185,-2.2885788361392,19.4027141188692));
#30183=CARTESIAN_POINT('Ctrl Pts',(-3.26532419492947,-2.19229261322667,
19.3968628021091));
#30184=CARTESIAN_POINT('Ctrl Pts',(-3.32999086271838,-2.09597443304278,
19.3910095433046));
#30185=CARTESIAN_POINT('Ctrl Pts',(-3.39036599409769,-1.99683171163408,
19.3851562845001));
#30186=CARTESIAN_POINT('Ctrl Pts',(-3.44621054912699,-1.89528938452307,
19.3793030256956));
#30187=CARTESIAN_POINT('Ctrl Pts',(-3.50211863823058,-1.7936315332083,19.3734431076675));
#30188=CARTESIAN_POINT('Ctrl Pts',(-3.55348566356971,-1.68956898960502,
19.3675831896394));
#30189=CARTESIAN_POINT('Ctrl Pts',(-3.60011924961873,-1.58354993243808,
19.3617232716112));
#30190=CARTESIAN_POINT('Ctrl Pts',(-3.64678423539589,-1.47745948960572,
19.3558594079326));
#30191=CARTESIAN_POINT('Ctrl Pts',(-3.68870928644008,-1.36941029453041,
19.349995544254));
#30192=CARTESIAN_POINT('Ctrl Pts',(-3.7257513437638,-1.2598674233594,19.3441316805753));
#30193=CARTESIAN_POINT('Ctrl Pts',(-3.76284804702802,-1.15016295011623,
19.3382591662879));
#30194=CARTESIAN_POINT('Ctrl Pts',(-3.79504726499192,-1.0389607985519,19.3323866520005));
#30195=CARTESIAN_POINT('Ctrl Pts',(-3.82225659977131,-0.92673808894675,
19.3265141377131));
#30196=CARTESIAN_POINT('Ctrl Pts',(-3.82977667656401,-0.895722137952037,
19.3248911006648));
#30197=CARTESIAN_POINT('Ctrl Pts',(-3.83691590493077,-0.864628269986622,
19.3232680636164));
#30198=CARTESIAN_POINT('Ctrl Pts',(-3.84367303262681,-0.833466626960804,
19.3216450265681));
#30199=CARTESIAN_POINT('Ctrl Pts',(-3.8681202204012,-0.720724264720546,
19.3157729026021));
#30200=CARTESIAN_POINT('Ctrl Pts',(-3.88764376046699,-0.606716354434508,
19.309900778636));
#30201=CARTESIAN_POINT('Ctrl Pts',(-3.90211643013503,-0.49191093265982,
19.30402865467));
#30202=CARTESIAN_POINT('Ctrl Pts',(-3.91657033569951,-0.377254358393829,
19.2981641440293));
#30203=CARTESIAN_POINT('Ctrl Pts',(-3.925986342335,-0.261802735244286,19.2922996333886));
#30204=CARTESIAN_POINT('Ctrl Pts',(-3.93028783644347,-0.146036032212877,
19.2864351227478));
#30205=CARTESIAN_POINT('Ctrl Pts',(-3.93458490435729,-0.0303884519675996,
19.2805766466302));
#30206=CARTESIAN_POINT('Ctrl Pts',(-3.93377791241063,0.0855731526423031,
19.2747181705126));
#30207=CARTESIAN_POINT('Ctrl Pts',(-3.92784191503611,0.20136258462152,19.268859694395));
#30208=CARTESIAN_POINT('Ctrl Pts',(-3.92167185342207,0.321717747282592,
19.2627702108038));
#30209=CARTESIAN_POINT('Ctrl Pts',(-3.90995992100421,0.441886428504692,
19.2566807272125));
#30210=CARTESIAN_POINT('Ctrl Pts',(-3.89273783065155,0.561320925865294,
19.2505912436212));
#30211=CARTESIAN_POINT('Ctrl Pts',(-3.87618827632311,0.676091413203553,
19.2447395591008));
#30212=CARTESIAN_POINT('Ctrl Pts',(-3.85455090471959,0.790183533818666,
19.2388878745804));
#30213=CARTESIAN_POINT('Ctrl Pts',(-3.82790675910924,0.903116184976115,
19.23303619006));
#30214=CARTESIAN_POINT('Ctrl Pts',(-3.80126667731029,1.01603161144929,19.2271853980487));
#30215=CARTESIAN_POINT('Ctrl Pts',(-3.76962143476761,1.12778751783175,19.2213346060374));
#30216=CARTESIAN_POINT('Ctrl Pts',(-3.73310297856709,1.2379140323195,19.2154838140261));
#30217=CARTESIAN_POINT('Ctrl Pts',(-3.69658124708061,1.34805042389035,19.2096324972659));
#30218=CARTESIAN_POINT('Ctrl Pts',(-3.65518556320843,1.45655674063406,19.2037811805058));
#30219=CARTESIAN_POINT('Ctrl Pts',(-3.60909720303922,1.56297996756661,19.1979298637456));
#30220=CARTESIAN_POINT('Ctrl Pts',(-3.56299354620353,1.66943851622901,19.1920766049411));
#30221=CARTESIAN_POINT('Ctrl Pts',(-3.51219428030129,1.77381222116112,19.1862233461366));
#30222=CARTESIAN_POINT('Ctrl Pts',(-3.45692779915915,1.87567033121513,19.1803700873321));
#30223=CARTESIAN_POINT('Ctrl Pts',(-3.40159844161468,1.97764432473732,19.174510169304));
#30224=CARTESIAN_POINT('Ctrl Pts',(-3.34179192191341,2.07709664735771,19.1686502512758));
#30225=CARTESIAN_POINT('Ctrl Pts',(-3.27778140669515,2.17362325390661,19.1627903332477));
#30226=CARTESIAN_POINT('Ctrl Pts',(-3.21372779136531,2.27021485458184,19.1569264695691));
#30227=CARTESIAN_POINT('Ctrl Pts',(-3.14546478700233,2.36387648331367,19.1510626058905));
#30228=CARTESIAN_POINT('Ctrl Pts',(-3.07330642652341,2.45423646144578,19.1451987422119));
#30229=CARTESIAN_POINT('Ctrl Pts',(-3.0010416151137,2.54472974227095,19.1393262279245));
#30230=CARTESIAN_POINT('Ctrl Pts',(-2.92487024945583,2.63191134126862,19.1334537136371));
#30231=CARTESIAN_POINT('Ctrl Pts',(-2.84514387151662,2.71544570013312,19.1275811993497));
#30232=CARTESIAN_POINT('Ctrl Pts',(-2.82310920990589,2.73853280603239,19.1259581623013));
#30233=CARTESIAN_POINT('Ctrl Pts',(-2.80080319511398,2.76134155239987,19.124335125253));
#30234=CARTESIAN_POINT('Ctrl Pts',(-2.77823368432067,2.78386540538618,19.1227120882046));
#30235=CARTESIAN_POINT('Ctrl Pts',(-2.69657752904987,2.86535637138854,19.1168399642386));
#30236=CARTESIAN_POINT('Ctrl Pts',(-2.61119600685286,2.94338821035076,19.1109678402725));
#30237=CARTESIAN_POINT('Ctrl Pts',(-2.52241419876744,3.01760096928941,19.1050957163065));
#30238=CARTESIAN_POINT('Ctrl Pts',(-2.4337474980592,3.09171750991241,19.0992312056658));
#30239=CARTESIAN_POINT('Ctrl Pts',(-2.34168959270523,3.16202455458497,19.0933666950251));
#30240=CARTESIAN_POINT('Ctrl Pts',(-2.24660295070884,3.22819828725968,19.0875021843844));
#30241=CARTESIAN_POINT('Ctrl Pts',(-2.15161415192113,3.29430392782177,19.0816437082668));
#30242=CARTESIAN_POINT('Ctrl Pts',(-2.05360315272201,3.35628448135034,19.0757852321492));
#30243=CARTESIAN_POINT('Ctrl Pts',(-1.95296558031232,3.41385624215715,19.0699267560316));
#30244=CARTESIAN_POINT('Ctrl Pts',(-1.84835973511434,3.47369813375422,19.0638372724403));
#30245=CARTESIAN_POINT('Ctrl Pts',(-1.740916265865,3.52877609870654,19.0577477888491));
#30246=CARTESIAN_POINT('Ctrl Pts',(-1.63111316826112,3.57882087178517,19.0516583052578));
#30247=CARTESIAN_POINT('Ctrl Pts',(-1.52559796702751,3.62691135754844,19.0458066207374));
#30248=CARTESIAN_POINT('Ctrl Pts',(-1.41790438138372,3.67035418719305,19.039954936217));
#30249=CARTESIAN_POINT('Ctrl Pts',(-1.30848102283375,3.7089575911412,19.0341032516966));
#30250=CARTESIAN_POINT('Ctrl Pts',(-1.19907435372463,3.74755510723108,19.0282524596853));
#30251=CARTESIAN_POINT('Ctrl Pts',(-1.08793882603715,3.78131452773204,19.022401667674));
#30252=CARTESIAN_POINT('Ctrl Pts',(-0.975541106863264,3.81009298427479,
19.0165508756627));
#30253=CARTESIAN_POINT('Ctrl Pts',(-0.863133306905562,3.8388740219144,19.0106995589025));
#30254=CARTESIAN_POINT('Ctrl Pts',(-0.74946349093942,3.86267310497829,19.0048482421424));
#30255=CARTESIAN_POINT('Ctrl Pts',(-0.635010796838518,3.88139798112723,
18.9989969253823));
#30256=CARTESIAN_POINT('Ctrl Pts',(-0.520520116037529,3.90012907203816,
18.9931436665778));
#30257=CARTESIAN_POINT('Ctrl Pts',(-0.405246448207288,3.91378254055294,
18.9872904077732));
#30258=CARTESIAN_POINT('Ctrl Pts',(-0.289675657461678,3.92231781138068,
18.9814371489687));
#30259=CARTESIAN_POINT('Ctrl Pts',(-0.173973382399091,3.93086279274382,
18.9755772309406));
#30260=CARTESIAN_POINT('Ctrl Pts',(-0.0579737222475329,3.9342779235025,
18.9697173129125));
#30261=CARTESIAN_POINT('Ctrl Pts',(0.0578357375176416,3.93257473259769,
18.9638573948843));
#30262=CARTESIAN_POINT('Ctrl Pts',(0.173723175106275,3.9308703948857,18.9579935312057));
#30263=CARTESIAN_POINT('Ctrl Pts',(0.289419745614166,3.92404089752945,18.9521296675271));
#30264=CARTESIAN_POINT('Ctrl Pts',(0.404443016103308,3.91214964523665,18.9462658038485));
#30265=CARTESIAN_POINT('Ctrl Pts',(0.51963597357111,3.90024085048774,18.9403932895611));
#30266=CARTESIAN_POINT('Ctrl Pts',(0.634153241211034,3.88325545787445,18.9345207752737));
#30267=CARTESIAN_POINT('Ctrl Pts',(0.747522511328454,3.86130795133685,18.9286482609863));
#30268=CARTESIAN_POINT('Ctrl Pts',(0.778855347068329,3.85524213106183,18.9270252239379));
#30269=CARTESIAN_POINT('Ctrl Pts',(0.810100584535425,3.84879757193155,18.9254021868896));
#30270=CARTESIAN_POINT('Ctrl Pts',(0.841248480266414,3.8419773547549,18.9237791498412));
#30271=CARTESIAN_POINT('Ctrl Pts',(0.953941104996053,3.81730191017589,18.9179070258752));
#30272=CARTESIAN_POINT('Ctrl Pts',(1.06573606917177,3.78762265463477,18.9120349019091));
#30273=CARTESIAN_POINT('Ctrl Pts',(1.17615483650006,3.75301862513064,18.9061627779431));
#30274=CARTESIAN_POINT('Ctrl Pts',(1.28643044370397,3.71845946043789,18.9002982673024));
#30275=CARTESIAN_POINT('Ctrl Pts',(1.39533301147143,3.67898834185165,18.8944337566617));
#30276=CARTESIAN_POINT('Ctrl Pts',(1.50239420867585,3.63473529183863,18.8885692460209));
#30277=CARTESIAN_POINT('Ctrl Pts',(1.60934524097383,3.59052777777366,18.8827107699033));
#30278=CARTESIAN_POINT('Ctrl Pts',(1.71445829170005,3.54154827648078,18.8768522937857));
#30279=CARTESIAN_POINT('Ctrl Pts',(1.81728086276403,3.48797638550373,18.870993817668));
#30280=CARTESIAN_POINT('Ctrl Pts',(1.92415786400686,3.43229208390254,18.8649043340768));
#30281=CARTESIAN_POINT('Ctrl Pts',(2.02855960189874,3.37164590980433,18.8588148504855));
#30282=CARTESIAN_POINT('Ctrl Pts',(2.13000122152532,3.30629457191894,18.8527253668942));
#30283=CARTESIAN_POINT('Ctrl Pts',(2.22748146700065,3.24349525461052,18.8468736823738));
#30284=CARTESIAN_POINT('Ctrl Pts',(2.32222806536106,3.17635160311987,18.8410219978534));
#30285=CARTESIAN_POINT('Ctrl Pts',(2.41383724745544,3.10513747566782,18.835170313333));
#30286=CARTESIAN_POINT('Ctrl Pts',(2.50543245715824,3.0339342099182,18.8293195213217));
#30287=CARTESIAN_POINT('Ctrl Pts',(2.59389087574815,2.95866195628142,18.8234687293104));
#30288=CARTESIAN_POINT('Ctrl Pts',(2.67884012529963,2.87963618936223,18.817617937299));
#30289=CARTESIAN_POINT('Ctrl Pts',(2.76379699382277,2.80060333473973,18.8117666205389));
#30290=CARTESIAN_POINT('Ctrl Pts',(2.84524376494135,2.71781657921138,18.8059153037787));
#30291=CARTESIAN_POINT('Ctrl Pts',(2.92284391261533,2.63162924107624,18.8000639870186));
#30292=CARTESIAN_POINT('Ctrl Pts',(3.00046981567637,2.54541329747681,18.7942107282141));
#30293=CARTESIAN_POINT('Ctrl Pts',(3.0742462802051,2.45579483409477,18.7883574694096));
#30294=CARTESIAN_POINT('Ctrl Pts',(3.14387662888212,2.36316075254494,18.7825042106051));
#30295=CARTESIAN_POINT('Ctrl Pts',(3.21358619566299,2.27042128165798,18.776644292577));
#30296=CARTESIAN_POINT('Ctrl Pts',(3.27913998300501,2.17465967537183,18.7707843745489));
#30297=CARTESIAN_POINT('Ctrl Pts',(3.34028422613442,2.07629243813043,18.7649244565208));
#30298=CARTESIAN_POINT('Ctrl Pts',(3.40146963943263,1.977858967413,18.7590605928421));
#30299=CARTESIAN_POINT('Ctrl Pts',(3.45823939450847,1.8768167318374,18.7531967291635));
#30300=CARTESIAN_POINT('Ctrl Pts',(3.5103861611893,1.77360593124027,18.7473328654849));
#30301=CARTESIAN_POINT('Ctrl Pts',(3.56260985688832,1.67024286989788,18.7414603511975));
#30302=CARTESIAN_POINT('Ctrl Pts',(3.61019678340428,1.56470523407687,18.7355878369101));
#30303=CARTESIAN_POINT('Ctrl Pts',(3.65298806191879,1.45745230435813,18.7297153226227));
#30304=CARTESIAN_POINT('Ctrl Pts',(3.66481465389889,1.42780989397715,18.7280922855744));
#30305=CARTESIAN_POINT('Ctrl Pts',(3.67627522564143,1.39803654176343,18.7264692485261));
#30306=CARTESIAN_POINT('Ctrl Pts',(3.68736710460949,1.36814211098258,18.7248462114777));
#30307=CARTESIAN_POINT('Ctrl Pts',(3.73357286612343,1.24361001473156,18.7180850790313));
#30308=CARTESIAN_POINT('Ctrl Pts',(3.77350486082523,1.11663082843232,18.7113239465848));
#30309=CARTESIAN_POINT('Ctrl Pts',(3.80693270518357,0.987801790949832,18.7045628141384));
#30310=CARTESIAN_POINT('Ctrl Pts',(3.84022696812535,0.859487568755357,18.6978286999358));
#30311=CARTESIAN_POINT('Ctrl Pts',(3.86706885387637,0.72933839269851,18.6910945857331));
#30312=CARTESIAN_POINT('Ctrl Pts',(3.88727736453247,0.59796629603476,18.6843604715305));
#30313=CARTESIAN_POINT('Ctrl Pts',(3.90733771924772,0.467557335987658,18.6776757275681));
#30314=CARTESIAN_POINT('Ctrl Pts',(3.92086151599839,0.335943479056069,18.6709909836057));
#30315=CARTESIAN_POINT('Ctrl Pts',(3.92771916947069,0.203742793179215,18.6643062396433));
#30316=CARTESIAN_POINT('Ctrl Pts',(3.93118751002375,0.136880709549541,18.6609253501503));
#30317=CARTESIAN_POINT('Ctrl Pts',(3.93295144684361,0.0698688121993667,
18.6575444606572));
#30318=CARTESIAN_POINT('Ctrl Pts',(3.93299901128319,0.00278877131541848,
18.6541635711641));
#30319=CARTESIAN_POINT('',(3.92848299207397,-0.00269963646582772,17.404163522035));
#30320=CARTESIAN_POINT('Ctrl Pts',(3.92864672146726,0.00278471154748855,
18.654163522035));
#30321=CARTESIAN_POINT('Ctrl Pts',(3.92313822395883,-0.844483024166633,
18.6114134390614));
#30322=CARTESIAN_POINT('Ctrl Pts',(3.23759721412511,-3.01409901755068,18.5023523766335));
#30323=CARTESIAN_POINT('Ctrl Pts',(-0.34305832318172,-4.63968169964443,
18.3269803347509));
#30324=CARTESIAN_POINT('Ctrl Pts',(-4.08939297301161,-2.2183778757014,18.1280473963876));
#30325=CARTESIAN_POINT('Ctrl Pts',(-4.07633013060909,2.24229078252717,17.929114458024));
#30326=CARTESIAN_POINT('Ctrl Pts',(-0.315878526192679,4.64161136285755,
17.7301815196607));
#30327=CARTESIAN_POINT('Ctrl Pts',(3.24728594800834,2.99873176707587,17.5551978743308));
#30328=CARTESIAN_POINT('Ctrl Pts',(3.92320510227271,0.836958268880239,17.4465252084557));
#30329=CARTESIAN_POINT('Ctrl Pts',(3.92848299207397,-0.00269963646582772,
17.404163522035));
#30330=CARTESIAN_POINT('',(3.9349711294896,-0.00179957505841655,16.1541641208363));
#30331=CARTESIAN_POINT('Ctrl Pts',(3.92848299207397,-0.00269963646582772,
17.404163522035));
#30332=CARTESIAN_POINT('Ctrl Pts',(3.93146686122864,-0.47740248525043,17.3802142290012));
#30333=CARTESIAN_POINT('Ctrl Pts',(3.63168221550235,-2.26282468683885,17.2899539565132));
#30334=CARTESIAN_POINT('Ctrl Pts',(0.968478616941049,-4.55042684323626,
17.1333827045702));
#30335=CARTESIAN_POINT('Ctrl Pts',(-3.30560419092301,-3.27373123821604,
16.9344497662068));
#30336=CARTESIAN_POINT('Ctrl Pts',(-4.54083008587026,1.01252032985696,16.7355168278434));
#30337=CARTESIAN_POINT('Ctrl Pts',(-1.60165030493022,4.36795737019433,16.5365838894799));
#30338=CARTESIAN_POINT('Ctrl Pts',(2.69574705430972,3.72499564046276,16.3428000122829));
#30339=CARTESIAN_POINT('Ctrl Pts',(3.93162038906629,1.20261472713713,16.2153271145402));
#30340=CARTESIAN_POINT('Ctrl Pts',(3.93851192302398,-0.00178002804509826,
16.1541651962521));
#30341=CARTESIAN_POINT('',(3.93299839598119,0.00355207114488244,14.9041635220072));
#30342=CARTESIAN_POINT('Ctrl Pts',(3.93299958330002,-0.0018104590140189,
16.154163522035));
#30343=CARTESIAN_POINT('Ctrl Pts',(3.93295297921618,-0.103052100462509,
16.149015018941));
#30344=CARTESIAN_POINT('Ctrl Pts',(3.92899756056485,-0.204200298766311,
16.143866515847));
#30345=CARTESIAN_POINT('Ctrl Pts',(3.92115268406435,-0.30504201063944,16.138718012753));
#30346=CARTESIAN_POINT('Ctrl Pts',(3.91220521205771,-0.420057000872728,
16.1328458887869));
#30347=CARTESIAN_POINT('Ctrl Pts',(3.8981780309882,-0.53487080847362,16.1269737648208));
#30348=CARTESIAN_POINT('Ctrl Pts',(3.87908363530141,-0.648998574988258,
16.1211016408548));
#30349=CARTESIAN_POINT('Ctrl Pts',(3.86001399587776,-0.762978372587534,
16.115237130214));
#30350=CARTESIAN_POINT('Ctrl Pts',(3.83589027426291,-0.876273493949008,
16.1093726195733));
#30351=CARTESIAN_POINT('Ctrl Pts',(3.80677686926452,-0.988402179091408,
16.1035081089325));
#30352=CARTESIAN_POINT('Ctrl Pts',(3.77769342167025,-1.10041548493225,16.0976496328149));
#30353=CARTESIAN_POINT('Ctrl Pts',(3.74363060639703,-1.21126434417529,16.0917911566972));
#30354=CARTESIAN_POINT('Ctrl Pts',(3.70470410337022,-1.32047586364608,16.0859326805796));
#30355=CARTESIAN_POINT('Ctrl Pts',(3.6642426767658,-1.43399373799459,16.0798431969883));
#30356=CARTESIAN_POINT('Ctrl Pts',(3.61852618315301,-1.54574204231883,16.0737537133971));
#30357=CARTESIAN_POINT('Ctrl Pts',(3.56774223274705,-1.65520523219119,16.0676642298058));
#30358=CARTESIAN_POINT('Ctrl Pts',(3.5189414351059,-1.76039379935491,16.0618125452854));
#30359=CARTESIAN_POINT('Ctrl Pts',(3.46546172033017,-1.86347196359888,16.055960860765));
#30360=CARTESIAN_POINT('Ctrl Pts',(3.40751883343924,-1.96400213842981,16.0501091762446));
#30361=CARTESIAN_POINT('Ctrl Pts',(3.34958478409809,-2.06451698022382,16.0442583842333));
#30362=CARTESIAN_POINT('Ctrl Pts',(3.28718912253459,-2.16248424723207,16.038407592222));
#30363=CARTESIAN_POINT('Ctrl Pts',(3.22059313080242,-2.25749172442077,16.0325568002107));
#30364=CARTESIAN_POINT('Ctrl Pts',(3.15399116617496,-2.35250772268857,16.0267054834505));
#30365=CARTESIAN_POINT('Ctrl Pts',(3.08318835979914,-2.44456306487948,16.0208541666904));
#30366=CARTESIAN_POINT('Ctrl Pts',(3.00848840717777,-2.53327584441114,16.0150028499303));
#30367=CARTESIAN_POINT('Ctrl Pts',(2.93376366173962,-2.62201806759854,16.0091495911258));
#30368=CARTESIAN_POINT('Ctrl Pts',(2.8551394642411,-2.70741520610614,16.0032963323212));
#30369=CARTESIAN_POINT('Ctrl Pts',(2.77295825322183,-2.78912020642513,15.9974430735167));
#30370=CARTESIAN_POINT('Ctrl Pts',(2.69068354504526,-2.87091816211885,15.9915831554886));
#30371=CARTESIAN_POINT('Ctrl Pts',(2.60484403939898,-2.94901530383245,15.9857232374605));
#30372=CARTESIAN_POINT('Ctrl Pts',(2.51581739640533,-3.0231030131215,15.9798633194324));
#30373=CARTESIAN_POINT('Ctrl Pts',(2.42673080922506,-3.09724060778557,15.9739994557537));
#30374=CARTESIAN_POINT('Ctrl Pts',(2.33445313996473,-3.16736314494313,15.9681355920751));
#30375=CARTESIAN_POINT('Ctrl Pts',(2.23939190322457,-3.23320474201252,15.9622717283965));
#30376=CARTESIAN_POINT('Ctrl Pts',(2.14419042830493,-3.29914347126768,15.9563992141091));
#30377=CARTESIAN_POINT('Ctrl Pts',(2.0461975388517,-3.36078843672843,15.9505266998217));
#30378=CARTESIAN_POINT('Ctrl Pts',(1.94584631039175,-3.41791912372643,15.9446541855343));
#30379=CARTESIAN_POINT('Ctrl Pts',(1.91811138227575,-3.43370882078768,15.9430311484861));
#30380=CARTESIAN_POINT('Ctrl Pts',(1.89019643316264,-3.44915397609759,15.9414081114379));
#30381=CARTESIAN_POINT('Ctrl Pts',(1.86211086521754,-3.4642505864384,15.9397850743898));
#30382=CARTESIAN_POINT('Ctrl Pts',(1.7604976969819,-3.5188698987253,15.9339129504237));
#30383=CARTESIAN_POINT('Ctrl Pts',(1.65630900294329,-3.56910622282458,15.9280408264577));
#30384=CARTESIAN_POINT('Ctrl Pts',(1.54995951462399,-3.61470807991829,15.9221687024917));
#30385=CARTESIAN_POINT('Ctrl Pts',(1.44374791052793,-3.66025081329882,15.916304191851));
#30386=CARTESIAN_POINT('Ctrl Pts',(1.33538145978728,-3.70117086733896,15.9104396812103));
#30387=CARTESIAN_POINT('Ctrl Pts',(1.22530033314438,-3.73726211197399,15.9045751705696));
#30388=CARTESIAN_POINT('Ctrl Pts',(1.11533247888564,-3.77331621907734,15.898716694452));
#30389=CARTESIAN_POINT('Ctrl Pts',(1.0036538486417,-3.80455127192809,15.8928582183344));
#30390=CARTESIAN_POINT('Ctrl Pts',(0.890724861888612,-3.83080908169717,
15.8869997422167));
#30391=CARTESIAN_POINT('Ctrl Pts',(0.773342935598185,-3.85810227168745,
15.8809102586255));
#30392=CARTESIAN_POINT('Ctrl Pts',(0.654610435968224,-3.8800174454089,15.8748207750342));
#30393=CARTESIAN_POINT('Ctrl Pts',(0.535062538391735,-3.896433892678,15.8687312914429));
#30394=CARTESIAN_POINT('Ctrl Pts',(0.420183079204392,-3.91220926491191,
15.8628796069225));
#30395=CARTESIAN_POINT('Ctrl Pts',(0.304551159006151,-3.92290724918914,
15.8570279224021));
#30396=CARTESIAN_POINT('Ctrl Pts',(0.188651558702059,-3.92847293352001,
15.8511762378817));
#30397=CARTESIAN_POINT('Ctrl Pts',(0.0727696356063224,-3.93403776896303,
15.8453254458704));
#30398=CARTESIAN_POINT('Ctrl Pts',(-0.0433794735954423,-3.93447184106165,
15.8394746538591));
#30399=CARTESIAN_POINT('Ctrl Pts',(-0.159307730771794,-3.92977226400161,
15.8336238618477));
#30400=CARTESIAN_POINT('Ctrl Pts',(-0.275246385380741,-3.92507226544351,
15.8277725450876));
#30401=CARTESIAN_POINT('Ctrl Pts',(-0.390963735490063,-3.915237719182,15.8219212283275));
#30402=CARTESIAN_POINT('Ctrl Pts',(-0.505974327755538,-3.90031780495543,
15.8160699115673));
#30403=CARTESIAN_POINT('Ctrl Pts',(-0.621023091886366,-3.88539293882882,
15.8102166527628));
#30404=CARTESIAN_POINT('Ctrl Pts',(-0.735364221981617,-3.86537940176006,
15.8043633939583));
#30405=CARTESIAN_POINT('Ctrl Pts',(-0.848520656818351,-3.84037780627799,
15.7985101351537));
#30406=CARTESIAN_POINT('Ctrl Pts',(-0.961805829171468,-3.81534776660437,
15.7926502171256));
#30407=CARTESIAN_POINT('Ctrl Pts',(-1.07390321213151,-3.78531843083299,
15.7867902990975));
#30408=CARTESIAN_POINT('Ctrl Pts',(-1.1843490534434,-3.75044081670511,15.7809303810693));
#30409=CARTESIAN_POINT('Ctrl Pts',(-1.29486926110112,-3.71553971848147,
15.7750665173907));
#30410=CARTESIAN_POINT('Ctrl Pts',(-1.40373532545892,-3.675783983138,15.7692026537121));
#30411=CARTESIAN_POINT('Ctrl Pts',(-1.5105033222041,-3.63137284144859,15.7633387900334));
#30412=CARTESIAN_POINT('Ctrl Pts',(-1.61742882741433,-3.58689618264756,
15.757466275746));
#30413=CARTESIAN_POINT('Ctrl Pts',(-1.72224971474705,-3.53775058540083,
15.7515937614586));
#30414=CARTESIAN_POINT('Ctrl Pts',(-1.82454642256008,-3.4841813029639,15.7457212471712));
#30415=CARTESIAN_POINT('Ctrl Pts',(-1.85281903946332,-3.46937590176869,
15.7440982101229));
#30416=CARTESIAN_POINT('Ctrl Pts',(-1.88089901846817,-3.45423285102442,
15.7424751730745));
#30417=CARTESIAN_POINT('Ctrl Pts',(-1.90877791066121,-3.43875789897629,
15.7408521360261));
#30418=CARTESIAN_POINT('Ctrl Pts',(-2.00964332908048,-3.38276975201031,
15.7349800120601));
#30419=CARTESIAN_POINT('Ctrl Pts',(-2.10821239750051,-3.32224611220501,
15.7291078880941));
#30420=CARTESIAN_POINT('Ctrl Pts',(-2.20404941189026,-3.2574000659953,15.723235764128));
#30421=CARTESIAN_POINT('Ctrl Pts',(-2.2997621716879,-3.19263809397209,15.7173712534873));
#30422=CARTESIAN_POINT('Ctrl Pts',(-2.39274958229793,-3.12356508957238,
15.7115067428466));
#30423=CARTESIAN_POINT('Ctrl Pts',(-2.48260035200154,-3.05044004895062,
15.7056422322059));
#30424=CARTESIAN_POINT('Ctrl Pts',(-2.572358666157,-2.97739025326816,15.6997837560883));
#30425=CARTESIAN_POINT('Ctrl Pts',(-2.65898644048793,-2.90029697409149,
15.6939252799707));
#30426=CARTESIAN_POINT('Ctrl Pts',(-2.7421017816784,-2.81946215064437,15.6880668038531));
#30427=CARTESIAN_POINT('Ctrl Pts',(-2.82849447086952,-2.73543990303206,
15.6819773202618));
#30428=CARTESIAN_POINT('Ctrl Pts',(-2.91109165153983,-2.64737522763415,
15.6758878366705));
#30429=CARTESIAN_POINT('Ctrl Pts',(-2.98950257228258,-2.55565321792997,
15.6697983530793));
#30430=CARTESIAN_POINT('Ctrl Pts',(-3.06485148557938,-2.46751302404955,
15.6639466685589));
#30431=CARTESIAN_POINT('Ctrl Pts',(-3.13633466294613,-2.37599612293355,
15.6580949840385));
#30432=CARTESIAN_POINT('Ctrl Pts',(-3.20364394887505,-2.28148075793689,
15.6522432995181));
#30433=CARTESIAN_POINT('Ctrl Pts',(-3.27094296867473,-2.18697980858791,
15.6463925075068));
#30434=CARTESIAN_POINT('Ctrl Pts',(-3.33406912306604,-2.08948164132976,
15.6405417154955));
#30435=CARTESIAN_POINT('Ctrl Pts',(-3.3927562735057,-1.98939535250983,15.6346909234842));
#30436=CARTESIAN_POINT('Ctrl Pts',(-3.45144868750846,-1.88930008709975,
15.628839606724));
#30437=CARTESIAN_POINT('Ctrl Pts',(-3.50570109699303,-1.78661659533198,
15.6229882899639));
#30438=CARTESIAN_POINT('Ctrl Pts',(-3.55529257023308,-1.68177993210926,
15.6171369732038));
#30439=CARTESIAN_POINT('Ctrl Pts',(-3.60490050281836,-1.57690847373489,
15.6112837143993));
#30440=CARTESIAN_POINT('Ctrl Pts',(-3.64984424644787,-1.46988279641373,
15.6054304555947));
#30441=CARTESIAN_POINT('Ctrl Pts',(-3.68995068175951,-1.36115868515855,
15.5995771967902));
#30442=CARTESIAN_POINT('Ctrl Pts',(-3.73010274596424,-1.25231087901974,
15.5937172787621));
#30443=CARTESIAN_POINT('Ctrl Pts',(-3.76540637408494,-1.1417611702238,15.587857360734));
#30444=CARTESIAN_POINT('Ctrl Pts',(-3.79573805128353,-1.02998138140373,
15.5819974427059));
#30445=CARTESIAN_POINT('Ctrl Pts',(-3.82609015166841,-0.918126328052883,
15.5761335790273));
#30446=CARTESIAN_POINT('Ctrl Pts',(-3.85146354480521,-0.80503994787316,
15.5702697153486));
#30447=CARTESIAN_POINT('Ctrl Pts',(-3.87178599830118,-0.691203431240699,
15.56440585167));
#30448=CARTESIAN_POINT('Ctrl Pts',(-3.89213843230215,-0.577198978376718,
15.5585333373826));
#30449=CARTESIAN_POINT('Ctrl Pts',(-3.90742500076692,-0.462442588687338,
15.5526608230952));
#30450=CARTESIAN_POINT('Ctrl Pts',(-3.91762536085701,-0.34741982092271,
15.5467883088079));
#30451=CARTESIAN_POINT('Ctrl Pts',(-3.92044452170068,-0.315629993882404,
15.5451652717595));
#30452=CARTESIAN_POINT('Ctrl Pts',(-3.92287547864341,-0.283819812255978,
15.5435422347111));
#30453=CARTESIAN_POINT('Ctrl Pts',(-3.92491850314786,-0.251999491363761,
15.5419191976628));
#30454=CARTESIAN_POINT('Ctrl Pts',(-3.93231013550017,-0.136874042375434,
15.5360470736967));
#30455=CARTESIAN_POINT('Ctrl Pts',(-3.93464458701186,-0.0212300950170252,
15.5301749497307));
#30456=CARTESIAN_POINT('Ctrl Pts',(-3.93186572583331,0.0944505903489437,
15.5243028257647));
#30457=CARTESIAN_POINT('Ctrl Pts',(-3.92909046750346,0.209981293409424,
15.5184383151239));
#30458=CARTESIAN_POINT('Ctrl Pts',(-3.92121509001258,0.325548230282245,
15.5125738044832));
#30459=CARTESIAN_POINT('Ctrl Pts',(-3.90823528300636,0.440665374932272,
15.5067092938425));
#30460=CARTESIAN_POINT('Ctrl Pts',(-3.89526883209242,0.555664065185687,
15.5008508177249));
#30461=CARTESIAN_POINT('Ctrl Pts',(-3.87720844499173,0.670213475474608,
15.4949923416073));
#30462=CARTESIAN_POINT('Ctrl Pts',(-3.85410183080451,0.783829112619164,
15.4891338654897));
#30463=CARTESIAN_POINT('Ctrl Pts',(-3.83008409221207,0.901924764835474,
15.4830443818984));
#30464=CARTESIAN_POINT('Ctrl Pts',(-3.80061399142199,1.01901103417153,15.4769548983072));
#30465=CARTESIAN_POINT('Ctrl Pts',(-3.76580442055278,1.13455104166587,15.4708654147159));
#30466=CARTESIAN_POINT('Ctrl Pts',(-3.73235419050217,1.24557912199635,15.4650137301955));
#30467=CARTESIAN_POINT('Ctrl Pts',(-3.69397381613963,1.35517900657719,15.4591620456751));
#30468=CARTESIAN_POINT('Ctrl Pts',(-3.65081505610943,1.46288701753918,15.4533103611547));
#30469=CARTESIAN_POINT('Ctrl Pts',(-3.60766287872829,1.57057860068822,15.4474595691434));
#30470=CARTESIAN_POINT('Ctrl Pts',(-3.55973391850471,1.67637850030463,15.441608777132));
#30471=CARTESIAN_POINT('Ctrl Pts',(-3.50722859885247,1.77984172200545,15.4357579851207));
#30472=CARTESIAN_POINT('Ctrl Pts',(-3.45471857007634,1.88331422316847,15.4299066683606));
#30473=CARTESIAN_POINT('Ctrl Pts',(-3.39763155303805,1.98444926112361,15.4240553516005));
#30474=CARTESIAN_POINT('Ctrl Pts',(-3.33621424116639,2.08282585374739,15.4182040348403));
#30475=CARTESIAN_POINT('Ctrl Pts',(-3.27477654496913,2.18123509743379,15.4123507760358));
#30476=CARTESIAN_POINT('Ctrl Pts',(-3.20900591493992,2.27688372483143,15.4064975172313));
#30477=CARTESIAN_POINT('Ctrl Pts',(-3.13919232299163,2.36937978367134,15.4006442584267));
#30478=CARTESIAN_POINT('Ctrl Pts',(-3.06929930446503,2.46198107481996,15.3947843403986));
#30479=CARTESIAN_POINT('Ctrl Pts',(-2.99535439242745,2.55142230835978,15.3889244223705));
#30480=CARTESIAN_POINT('Ctrl Pts',(-2.91768785720815,2.63734460545074,15.3830645043424));
#30481=CARTESIAN_POINT('Ctrl Pts',(-2.83996902688801,2.72332475648327,15.3772006406638));
#30482=CARTESIAN_POINT('Ctrl Pts',(-2.75852387350708,2.80578095971988,15.3713367769851));
#30483=CARTESIAN_POINT('Ctrl Pts',(-2.67371826015857,2.88439242567557,15.3654729133065));
#30484=CARTESIAN_POINT('Ctrl Pts',(-2.5887875381407,2.96311986244398,15.3596003990191));
#30485=CARTESIAN_POINT('Ctrl Pts',(-2.50048677607265,3.03799097548627,15.3537278847317));
#30486=CARTESIAN_POINT('Ctrl Pts',(-2.40921355118324,3.10872627691713,15.3478553704443));
#30487=CARTESIAN_POINT('Ctrl Pts',(-2.38398758862848,3.12827599774004,15.346232333396));
#30488=CARTESIAN_POINT('Ctrl Pts',(-2.35853473377561,3.14751006612287,15.3446092963477));
#30489=CARTESIAN_POINT('Ctrl Pts',(-2.33286372890652,3.16642319066046,15.3429862592993));
#30490=CARTESIAN_POINT('Ctrl Pts',(-2.23998641407328,3.23485059469533,15.3371141353333));
#30491=CARTESIAN_POINT('Ctrl Pts',(-2.14394017682271,3.29930284472971,15.3312420113673));
#30492=CARTESIAN_POINT('Ctrl Pts',(-2.04510005975041,3.35947239095797,15.3253698874012));
#30493=CARTESIAN_POINT('Ctrl Pts',(-1.94638809085243,3.41956392617484,15.3195053767605));
#30494=CARTESIAN_POINT('Ctrl Pts',(-1.84488979547726,3.475383586732,15.3136408661198));
#30495=CARTESIAN_POINT('Ctrl Pts',(-1.74101180716334,3.52666512265027,15.3077763554791));
#30496=CARTESIAN_POINT('Ctrl Pts',(-1.63724070826596,3.57789389037826,15.3019178793615));
#30497=CARTESIAN_POINT('Ctrl Pts',(-1.53109515544061,3.62459363979043,15.2960594032439));
#30498=CARTESIAN_POINT('Ctrl Pts',(-1.42300860101158,3.66654272052666,15.2902009271263));
#30499=CARTESIAN_POINT('Ctrl Pts',(-1.31066005056624,3.71014590908352,15.284111443535));
#30500=CARTESIAN_POINT('Ctrl Pts',(-1.1962146655235,3.74861583435038,15.2780219599437));
#30501=CARTESIAN_POINT('Ctrl Pts',(-1.08018519929101,3.78175738714591,15.2719324763525));
#30502=CARTESIAN_POINT('Ctrl Pts',(-0.968686773966867,3.81360473652606,
15.2660807918321));
#30503=CARTESIAN_POINT('Ctrl Pts',(-0.855726099957108,3.84053193399624,
15.2602291073117));
#30504=CARTESIAN_POINT('Ctrl Pts',(-0.741775337648642,3.86241612833939,
15.2543774227913));
#30505=CARTESIAN_POINT('Ctrl Pts',(-0.627841955308467,3.88429698486718,
15.24852663078));
#30506=CARTESIAN_POINT('Ctrl Pts',(-0.512919190806072,3.90113628966476,
15.2426758387686));
#30507=CARTESIAN_POINT('Ctrl Pts',(-0.397489779359752,3.91286223566644,
15.2368250467573));
#30508=CARTESIAN_POINT('Ctrl Pts',(-0.282050015221484,3.92458923335074,
15.2309737299972));
#30509=CARTESIAN_POINT('Ctrl Pts',(-0.166103925128302,3.93120191878143,
15.2251224132371));
#30510=CARTESIAN_POINT('Ctrl Pts',(-0.0501390412770755,3.93268039338818,
15.2192710964769));
#30511=CARTESIAN_POINT('Ctrl Pts',(0.0658643311677466,3.93415935869873,
15.2134178376724));
#30512=CARTESIAN_POINT('Ctrl Pts',(0.181886096613168,3.93050071954967,15.2075645788679));
#30513=CARTESIAN_POINT('Ctrl Pts',(0.297439764364947,3.92173667991293,15.2017113200634));
#30514=CARTESIAN_POINT('Ctrl Pts',(0.413124896953059,3.91296266947165,15.1958514020352));
#30515=CARTESIAN_POINT('Ctrl Pts',(0.528340456412262,3.89907169643602,15.1899914840071));
#30516=CARTESIAN_POINT('Ctrl Pts',(0.642606006256308,3.88014774470294,15.184131565979));
#30517=CARTESIAN_POINT('Ctrl Pts',(0.756948494365145,3.86121105093159,15.1782677023004));
#30518=CARTESIAN_POINT('Ctrl Pts',(0.870339295670883,3.83723471591799,15.1724038386218));
#30519=CARTESIAN_POINT('Ctrl Pts',(0.982310791193972,3.8083532542956,15.1665399749431));
#30520=CARTESIAN_POINT('Ctrl Pts',(1.09444747159405,3.7794291855734,15.1606674606557));
#30521=CARTESIAN_POINT('Ctrl Pts',(1.20516027346793,3.74558566845092,15.1547949463683));
#30522=CARTESIAN_POINT('Ctrl Pts',(1.31399919406769,3.70700622038721,15.1489224320809));
#30523=CARTESIAN_POINT('Ctrl Pts',(1.34407993832644,3.69634368804627,15.1472993950326));
#30524=CARTESIAN_POINT('Ctrl Pts',(1.3740176801626,3.68531967695767,15.1456763579843));
#30525=CARTESIAN_POINT('Ctrl Pts',(1.40380324329441,3.67393868404416,15.1440533209359));
#30526=CARTESIAN_POINT('Ctrl Pts',(1.51156696888942,3.63276242049987,15.1381811969699));
#30527=CARTESIAN_POINT('Ctrl Pts',(1.6176981537394,3.5867717276716,15.1323090730038));
#30528=CARTESIAN_POINT('Ctrl Pts',(1.72173535916131,3.53611599824068,15.1264369490378));
#30529=CARTESIAN_POINT('Ctrl Pts',(1.82563767828066,3.48552594496877,15.1205724383971));
#30530=CARTESIAN_POINT('Ctrl Pts',(1.92745104863593,3.43028306229887,15.1147079277564));
#30531=CARTESIAN_POINT('Ctrl Pts',(2.02673171285057,3.37058564112022,15.1088434171157));
#30532=CARTESIAN_POINT('Ctrl Pts',(2.12591021824936,3.3109496479941,15.1029849409981));
#30533=CARTESIAN_POINT('Ctrl Pts',(2.22256084906092,3.246868445263,15.0971264648805));
#30534=CARTESIAN_POINT('Ctrl Pts',(2.31626288442289,3.17858698956706,15.0912679887628));
#30535=CARTESIAN_POINT('Ctrl Pts',(2.41365971516021,3.10761310562499,15.0851785051716));
#30536=CARTESIAN_POINT('Ctrl Pts',(2.50787022334694,3.03210111018839,15.0790890215803));
#30537=CARTESIAN_POINT('Ctrl Pts',(2.59845317081765,2.95237702861063,15.072999537989));
#30538=CARTESIAN_POINT('Ctrl Pts',(2.68549878373087,2.8757662344308,15.0671478534686));
#30539=CARTESIAN_POINT('Ctrl Pts',(2.76919449786016,2.79526645012846,15.0612961689482));
#30540=CARTESIAN_POINT('Ctrl Pts',(2.84918181025936,2.71120858881924,15.0554444844278));
#30541=CARTESIAN_POINT('Ctrl Pts',(2.92915692285471,2.62716354816106,15.0495936924165));
#30542=CARTESIAN_POINT('Ctrl Pts',(3.00542447342669,2.53956180892775,15.0437429004052));
#30543=CARTESIAN_POINT('Ctrl Pts',(3.07766319562631,2.44877076393182,15.0378921083939));
#30544=CARTESIAN_POINT('Ctrl Pts',(3.14990839680929,2.35797157602235,15.0320407916338));
#30545=CARTESIAN_POINT('Ctrl Pts',(3.21812379389503,2.26398283724511,15.0261894748736));
#30546=CARTESIAN_POINT('Ctrl Pts',(3.28202920647656,2.16720402542881,15.0203381581135));
#30547=CARTESIAN_POINT('Ctrl Pts',(3.34595582918103,2.0703930928513,15.014484899309));
#30548=CARTESIAN_POINT('Ctrl Pts',(3.40556939528597,1.97079059070546,15.0086316405044));
#30549=CARTESIAN_POINT('Ctrl Pts',(3.46063412841561,1.86882327394677,15.0027783816999));
#30550=CARTESIAN_POINT('Ctrl Pts',(3.51576150841988,1.76673994947596,14.9969184636718));
#30551=CARTESIAN_POINT('Ctrl Pts',(3.56632952936074,1.66228680432709,14.9910585456437));
#30552=CARTESIAN_POINT('Ctrl Pts',(3.61214925603401,1.55591347835699,14.9851986276156));
#30553=CARTESIAN_POINT('Ctrl Pts',(3.65799983444048,1.4494685281824,14.979334763937));
#30554=CARTESIAN_POINT('Ctrl Pts',(3.69909560617089,1.34110120835168,14.9734709002583));
#30555=CARTESIAN_POINT('Ctrl Pts',(3.73529708060636,1.23127767770459,14.9676070365797));
#30556=CARTESIAN_POINT('Ctrl Pts',(3.77155196092052,1.121292130945,14.9617345222923));
#30557=CARTESIAN_POINT('Ctrl Pts',(3.80289802211392,1.00984648231908,14.9558620080049));
#30558=CARTESIAN_POINT('Ctrl Pts',(3.829246525485,0.897418546198519,14.9499894937175));
#30559=CARTESIAN_POINT('Ctrl Pts',(3.83652868693191,0.866345874994292,14.9483664566692));
#30560=CARTESIAN_POINT('Ctrl Pts',(3.84342941401067,0.835198207785689,14.9467434196208));
#30561=CARTESIAN_POINT('Ctrl Pts',(3.84994753223704,0.803985695781907,14.9451203825724));
#30562=CARTESIAN_POINT('Ctrl Pts',(3.88332231308886,0.644167982788329,14.9368099310093));
#30563=CARTESIAN_POINT('Ctrl Pts',(3.90675505914046,0.482207980055859,14.9284994794461));
#30564=CARTESIAN_POINT('Ctrl Pts',(3.92003124128456,0.319130173053279,14.9201890278829));
#30565=CARTESIAN_POINT('Ctrl Pts',(3.92856497469929,0.214306172018008,14.9148471926003));
#30566=CARTESIAN_POINT('Ctrl Pts',(3.93290314243907,0.10902067104636,14.9095053573176));
#30567=CARTESIAN_POINT('Ctrl Pts',(3.93299839598069,0.00355207169431283,
14.904163522035));
#30568=CARTESIAN_POINT('',(3.93299999319383,0.000231381426135529,13.654163522081));
#30569=CARTESIAN_POINT('Ctrl Pts',(3.93299839598119,0.00355207114488768,
14.9041635220072));
#30570=CARTESIAN_POINT('Ctrl Pts',(3.9331014152117,-0.110515032762491,14.8983861846387));
#30571=CARTESIAN_POINT('Ctrl Pts',(3.92823788678433,-0.224740458271784,
14.8926088472702));
#30572=CARTESIAN_POINT('Ctrl Pts',(3.91839323831547,-0.338649420379848,
14.8868315099017));
#30573=CARTESIAN_POINT('Ctrl Pts',(3.90840744311791,-0.454191541601957,
14.8809713404978));
#30574=CARTESIAN_POINT('Ctrl Pts',(3.89329652357728,-0.569407612697175,
14.875111171094));
#30575=CARTESIAN_POINT('Ctrl Pts',(3.87310012082037,-0.683801472725241,
14.8692510016901));
#30576=CARTESIAN_POINT('Ctrl Pts',(3.85321605094451,-0.796426257126016,
14.8634814585039));
#30577=CARTESIAN_POINT('Ctrl Pts',(3.82840275016944,-0.908253645725761,
14.8577119153178));
#30578=CARTESIAN_POINT('Ctrl Pts',(3.79875019094154,-1.018815972991,14.8519423721317));
#30579=CARTESIAN_POINT('Ctrl Pts',(3.76910388804956,-1.1293549729254,14.8461740462502));
#30580=CARTESIAN_POINT('Ctrl Pts',(3.73462046600092,-1.23862903038604,14.8404057203688));
#30581=CARTESIAN_POINT('Ctrl Pts',(3.69544052012651,-1.34618288586919,14.8346373944874));
#30582=CARTESIAN_POINT('Ctrl Pts',(3.65625872133245,-1.4537418278487,14.8288687958071));
#30583=CARTESIAN_POINT('Ctrl Pts',(3.61238010408342,-1.55958000593681,14.8231001971268));
#30584=CARTESIAN_POINT('Ctrl Pts',(3.5639941217805,-1.66326032235307,14.8173315984465));
#30585=CARTESIAN_POINT('Ctrl Pts',(3.51426540979626,-1.76981780756068,14.8114029189268));
#30586=CARTESIAN_POINT('Ctrl Pts',(3.45977569300044,-1.8740954742395,14.805474239407));
#30587=CARTESIAN_POINT('Ctrl Pts',(3.40078145967277,-1.97564532837904,14.7995455598872));
#30588=CARTESIAN_POINT('Ctrl Pts',(3.34329862424868,-2.07459353439134,14.7937687696842));
#30589=CARTESIAN_POINT('Ctrl Pts',(3.28153957424957,-2.17095167930799,14.7879919794813));
#30590=CARTESIAN_POINT('Ctrl Pts',(3.21578513749197,-2.26433543219324,14.7822151892783));
#30591=CARTESIAN_POINT('Ctrl Pts',(3.14743737568872,-2.36140219777171,14.7762105651001));
#30592=CARTESIAN_POINT('Ctrl Pts',(3.07477291673487,-2.45525472351012,14.7702059409219));
#30593=CARTESIAN_POINT('Ctrl Pts',(2.99815157968798,-2.54550115011061,14.7642013167437));
#30594=CARTESIAN_POINT('Ctrl Pts',(2.92153024264109,-2.63574757671111,14.7581966925655));
#30595=CARTESIAN_POINT('Ctrl Pts',(2.8409524305194,-2.72238758486848,14.7521920683873));
#30596=CARTESIAN_POINT('Ctrl Pts',(2.7568176077604,-2.80507498608187,14.7461874442091));
#30597=CARTESIAN_POINT('Ctrl Pts',(2.67453933447666,-2.88593777714813,14.740315320243));
#30598=CARTESIAN_POINT('Ctrl Pts',(2.58856231310642,-2.96331299295254,14.734443196277));
#30599=CARTESIAN_POINT('Ctrl Pts',(2.4992143736846,-3.03684318238006,14.728571072311));
#30600=CARTESIAN_POINT('Ctrl Pts',(2.40998227564033,-3.11027803845699,14.7227065616703));
#30601=CARTESIAN_POINT('Ctrl Pts',(2.31738826707177,-3.17987752154393,14.7168420510296));
#30602=CARTESIAN_POINT('Ctrl Pts',(2.22179728694164,-3.24532060292027,14.7109775403889));
#30603=CARTESIAN_POINT('Ctrl Pts',(2.12630466897917,-3.31069634401686,14.7051190642713));
#30604=CARTESIAN_POINT('Ctrl Pts',(2.02782155246119,-3.37192395821685,14.6992605881536));
#30605=CARTESIAN_POINT('Ctrl Pts',(1.9267457271836,-3.42872278010045,14.693402112036));
#30606=CARTESIAN_POINT('Ctrl Pts',(1.82168434822659,-3.48776125476871,14.6873126284448));
#30607=CARTESIAN_POINT('Ctrl Pts',(1.71382193747888,-3.54201419621266,14.6812231448535));
#30608=CARTESIAN_POINT('Ctrl Pts',(1.60363854014731,-3.59121601028874,14.6751336612622));
#30609=CARTESIAN_POINT('Ctrl Pts',(1.4977578901862,-3.63849645525419,14.6692819767418));
#30610=CARTESIAN_POINT('Ctrl Pts',(1.38973453766306,-3.68111268627017,14.6634302922214));
#30611=CARTESIAN_POINT('Ctrl Pts',(1.28001855055742,-3.71887637737918,14.657578607701));
#30612=CARTESIAN_POINT('Ctrl Pts',(1.17031929752487,-3.75663430870437,14.6517278156897));
#30613=CARTESIAN_POINT('Ctrl Pts',(1.05892831401735,-3.78954103719815,14.6458770236784));
#30614=CARTESIAN_POINT('Ctrl Pts',(0.946313348311815,-3.81745727504669,
14.6400262316671));
#30615=CARTESIAN_POINT('Ctrl Pts',(0.833688282337644,-3.84537601666104,
14.634174914907));
#30616=CARTESIAN_POINT('Ctrl Pts',(0.719839417229986,-3.86830327838651,
14.6283235981468));
#30617=CARTESIAN_POINT('Ctrl Pts',(0.605246583779176,-3.88615048252427,
14.6224722813867));
#30618=CARTESIAN_POINT('Ctrl Pts',(0.490615717116629,-3.90400361012578,
14.6166190225821));
#30619=CARTESIAN_POINT('Ctrl Pts',(0.375240799394601,-3.91677326392419,
14.6107657637776));
#30620=CARTESIAN_POINT('Ctrl Pts',(0.259607991412779,-3.92442259329887,
14.6049125049731));
#30621=CARTESIAN_POINT('Ctrl Pts',(0.143843628557176,-3.93208062527775,
14.599052586945));
#30622=CARTESIAN_POINT('Ctrl Pts',(0.0278212025794243,-3.93460667824846,
14.5931926689169));
#30623=CARTESIAN_POINT('Ctrl Pts',(-0.0879718037169931,-3.93201601748401,
14.5873327508887));
#30624=CARTESIAN_POINT('Ctrl Pts',(-0.203842776758241,-3.92942361235352,
14.5814688872101));
#30625=CARTESIAN_POINT('Ctrl Pts',(-0.319483611039676,-3.92170766081718,
14.5756050235315));
#30626=CARTESIAN_POINT('Ctrl Pts',(-0.434412373700088,-3.90893526290424,
14.5697411598528));
#30627=CARTESIAN_POINT('Ctrl Pts',(-0.549510683917648,-3.89614402263353,
14.5638686455654));
#30628=CARTESIAN_POINT('Ctrl Pts',(-0.66389441902465,-3.87828151180883,
14.5579961312781));
#30629=CARTESIAN_POINT('Ctrl Pts',(-0.777092162557845,-3.85546583059572,
14.5521236169907));
#30630=CARTESIAN_POINT('Ctrl Pts',(-0.808377592026888,-3.84916006545323,
14.5505005799423));
#30631=CARTESIAN_POINT('Ctrl Pts',(-0.839572523284305,-3.84247624389752,
14.548877542894));
#30632=CARTESIAN_POINT('Ctrl Pts',(-0.870667236763032,-3.83541752131726,
14.5472545058456));
#30633=CARTESIAN_POINT('Ctrl Pts',(-0.983167448893482,-3.80987916772564,
14.5413823818796));
#30634=CARTESIAN_POINT('Ctrl Pts',(-1.09473167951701,-3.77934402944453,
14.5355102579135));
#30635=CARTESIAN_POINT('Ctrl Pts',(-1.20488201210244,-3.74389480847312,
14.5296381339475));
#30636=CARTESIAN_POINT('Ctrl Pts',(-1.31488953259477,-3.7084915481205,14.5237736233068));
#30637=CARTESIAN_POINT('Ctrl Pts',(-1.42348641061541,-3.66818700057338,
14.5179091126661));
#30638=CARTESIAN_POINT('Ctrl Pts',(-1.53020532523377,-3.62311477359277,
14.5120446020253));
#30639=CARTESIAN_POINT('Ctrl Pts',(-1.63681442715081,-3.57808892548527,
14.5061861259077));
#30640=CARTESIAN_POINT('Ctrl Pts',(-1.74154903076589,-3.5283053158792,14.5003276497901));
#30641=CARTESIAN_POINT('Ctrl Pts',(-1.84395802764422,-3.47394700481836,
14.4944691736725));
#30642=CARTESIAN_POINT('Ctrl Pts',(-1.95040514692368,-3.41744527354764,
14.4883796900812));
#30643=CARTESIAN_POINT('Ctrl Pts',(-2.05433904962757,-3.35600078497178,
14.4822902064899));
#30644=CARTESIAN_POINT('Ctrl Pts',(-2.15527686239815,-3.2898739560067,14.4762007228987));
#30645=CARTESIAN_POINT('Ctrl Pts',(-2.25227297506704,-3.2263294311485,14.4703490383783));
#30646=CARTESIAN_POINT('Ctrl Pts',(-2.34650222756403,-3.15846164932073,
14.4644973538579));
#30647=CARTESIAN_POINT('Ctrl Pts',(-2.43756296134085,-3.08654755503608,
14.4586456693374));
#30648=CARTESIAN_POINT('Ctrl Pts',(-2.52860980637626,-3.01464442921411,
14.4527948773261));
#30649=CARTESIAN_POINT('Ctrl Pts',(-2.61648876923034,-2.9386964741749,14.4469440853148));
#30650=CARTESIAN_POINT('Ctrl Pts',(-2.70082990059078,-2.85902200902246,
14.4410932933035));
#30651=CARTESIAN_POINT('Ctrl Pts',(-2.78517859638153,-2.77934039798603,
14.4352419765434));
#30652=CARTESIAN_POINT('Ctrl Pts',(-2.8659885293692,-2.69593189633899,14.4293906597832));
#30653=CARTESIAN_POINT('Ctrl Pts',(-2.94292589109389,-2.60915239101308,
14.4235393430231));
#30654=CARTESIAN_POINT('Ctrl Pts',(-3.01988878822831,-2.52234408368284,
14.4176860842186));
#30655=CARTESIAN_POINT('Ctrl Pts',(-3.09297628424887,-2.43216285712852,
14.4118328254141));
#30656=CARTESIAN_POINT('Ctrl Pts',(-3.16189467561598,-2.33899787522591,
14.4059795666096));
#30657=CARTESIAN_POINT('Ctrl Pts',(-3.23089147509628,-2.2457268999839,14.4001196485815));
#30658=CARTESIAN_POINT('Ctrl Pts',(-3.29570945667423,-2.14946572641166,
14.3942597305534));
#30659=CARTESIAN_POINT('Ctrl Pts',(-3.35609805496052,-2.05063279147931,
14.3883998125253));
#30660=CARTESIAN_POINT('Ctrl Pts',(-3.41652731461829,-1.95173330950337,
14.3825359488466));
#30661=CARTESIAN_POINT('Ctrl Pts',(-3.47252105313717,-1.85025897921189,
14.376672085168));
#30662=CARTESIAN_POINT('Ctrl Pts',(-3.52387531995793,-1.74665157641454,
14.3708082214894));
#30663=CARTESIAN_POINT('Ctrl Pts',(-3.57530534666929,-1.64289132778788,
14.364935707202));
#30664=CARTESIAN_POINT('Ctrl Pts',(-3.62208207524491,-1.53699210298548,
14.3590631929146));
#30665=CARTESIAN_POINT('Ctrl Pts',(-3.66405015128463,-1.42941438668816,
14.3531906786272));
#30666=CARTESIAN_POINT('Ctrl Pts',(-3.67564922774955,-1.39968221225936,
14.3515676415788));
#30667=CARTESIAN_POINT('Ctrl Pts',(-3.68688129123676,-1.36982190488367,
14.3499446045305));
#30668=CARTESIAN_POINT('Ctrl Pts',(-3.6977437448762,-1.33984334801833,14.3483215674821));
#30669=CARTESIAN_POINT('Ctrl Pts',(-3.73704394101808,-1.23138137395919,
14.3424494435161));
#30670=CARTESIAN_POINT('Ctrl Pts',(-3.77163387810056,-1.12100697259218,
14.3365773195501));
#30671=CARTESIAN_POINT('Ctrl Pts',(-3.80132490392914,-1.00916697070807,
14.330705195584));
#30672=CARTESIAN_POINT('Ctrl Pts',(-3.83097743475323,-0.897471971606928,
14.3248406849433));
#30673=CARTESIAN_POINT('Ctrl Pts',(-3.85574358012656,-0.784315546636132,
14.3189761743026));
#30674=CARTESIAN_POINT('Ctrl Pts',(-3.87548324739994,-0.670163113818152,
14.3131116636619));
#30675=CARTESIAN_POINT('Ctrl Pts',(-3.89520260275208,-0.556128142717823,
14.3072531875442));
#30676=CARTESIAN_POINT('Ctrl Pts',(-3.90990569772854,-0.441099607223665,
14.3013947114266));
#30677=CARTESIAN_POINT('Ctrl Pts',(-3.91950281128406,-0.325556004915201,
14.295536235309));
#30678=CARTESIAN_POINT('Ctrl Pts',(-3.92947835173971,-0.205456365315012,
14.2894467517177));
#30679=CARTESIAN_POINT('Ctrl Pts',(-3.93393683864074,-0.0848006435188474,
14.2833572681265));
#30680=CARTESIAN_POINT('Ctrl Pts',(-3.93283647814454,0.0358641349488431,
14.2772677845352));
#30681=CARTESIAN_POINT('Ctrl Pts',(-3.93177908758163,0.151816859959831,
14.2714161000148));
#30682=CARTESIAN_POINT('Ctrl Pts',(-3.92558886120765,0.267777495236413,
14.2655644154944));
#30683=CARTESIAN_POINT('Ctrl Pts',(-3.9142817964293,0.383258422141242,14.259712730974));
#30684=CARTESIAN_POINT('Ctrl Pts',(-3.90297645622411,0.498721735694511,
14.2538619389627));
#30685=CARTESIAN_POINT('Ctrl Pts',(-3.88655586962668,0.613705075021255,
14.2480111469514));
#30686=CARTESIAN_POINT('Ctrl Pts',(-3.86508798236867,0.727725146294467,
14.2421603549401));
#30687=CARTESIAN_POINT('Ctrl Pts',(-3.84361816968779,0.841755443858191,
14.23630903818));
#30688=CARTESIAN_POINT('Ctrl Pts',(-3.81710023294893,0.954821895326569,
14.2304577214198));
#30689=CARTESIAN_POINT('Ctrl Pts',(-3.78565325765257,1.06645131760644,14.2246064046597));
#30690=CARTESIAN_POINT('Ctrl Pts',(-3.75419584514628,1.17811778954537,14.2187531458552));
#30691=CARTESIAN_POINT('Ctrl Pts',(-3.71780625315916,1.28834588620145,14.2128998870507));
#30692=CARTESIAN_POINT('Ctrl Pts',(-3.67665323840663,1.39667818931708,14.2070466282462));
#30693=CARTESIAN_POINT('Ctrl Pts',(-3.6354534040726,1.50513374155858,14.201186710218));
#30694=CARTESIAN_POINT('Ctrl Pts',(-3.58947947704671,1.61168880857652,14.1953267921899));
#30695=CARTESIAN_POINT('Ctrl Pts',(-3.53894815525177,1.71590645270659,14.1894668741618));
#30696=CARTESIAN_POINT('Ctrl Pts',(-3.48838280927194,1.82019426955856,14.1836030104832));
#30697=CARTESIAN_POINT('Ctrl Pts',(-3.43325415445786,1.92214116691071,14.1777391468046));
#30698=CARTESIAN_POINT('Ctrl Pts',(-3.37382371522563,2.0213368196768,14.171875283126));
#30699=CARTESIAN_POINT('Ctrl Pts',(-3.31430560180668,2.12067880988031,14.1660027688386));
#30700=CARTESIAN_POINT('Ctrl Pts',(-3.25047326529065,2.21726111138966,14.1601302545512));
#30701=CARTESIAN_POINT('Ctrl Pts',(-3.18263023134453,2.31070418066265,14.1542577402638));
#30702=CARTESIAN_POINT('Ctrl Pts',(-3.16387987124665,2.33652984168647,14.1526347032155));
#30703=CARTESIAN_POINT('Ctrl Pts',(-3.14482338009861,2.36211591899212,14.1510116661671));
#30704=CARTESIAN_POINT('Ctrl Pts',(-3.12546767104173,2.38745488696079,14.1493886291187));
#30705=CARTESIAN_POINT('Ctrl Pts',(-3.05543900278274,2.47913089721128,14.1435165051527));
#30706=CARTESIAN_POINT('Ctrl Pts',(-2.98125596041094,2.56787687429722,14.1376443811867));
#30707=CARTESIAN_POINT('Ctrl Pts',(-2.90319258488583,2.65329263652993,14.1317722572206));
#30708=CARTESIAN_POINT('Ctrl Pts',(-2.82523042007706,2.73859765553095,14.1259077465799));
#30709=CARTESIAN_POINT('Ctrl Pts',(-2.74339820312727,2.82058074365197,14.1200432359392));
#30710=CARTESIAN_POINT('Ctrl Pts',(-2.65801185747595,2.8988725335063,14.1141787252985));
#30711=CARTESIAN_POINT('Ctrl Pts',(-2.57271337352471,2.97708376188787,14.1083202491809));
#30712=CARTESIAN_POINT('Ctrl Pts',(-2.48386833801991,3.0516109693087,14.1024617730633));
#30713=CARTESIAN_POINT('Ctrl Pts',(-2.39183089826932,3.12212010564683,14.0966032969457));
#30714=CARTESIAN_POINT('Ctrl Pts',(-2.29616430035355,3.19540951062949,14.0905138133544));
#30715=CARTESIAN_POINT('Ctrl Pts',(-2.19704866423883,3.26435711381618,14.0844243297631));
#30716=CARTESIAN_POINT('Ctrl Pts',(-2.09492169686658,3.32863216411751,14.0783348461719));
#30717=CARTESIAN_POINT('Ctrl Pts',(-1.99678286700823,3.39039722370915,14.0724831616515));
#30718=CARTESIAN_POINT('Ctrl Pts',(-1.89586386492152,3.4478475749194,14.0666314771311));
#30719=CARTESIAN_POINT('Ctrl Pts',(-1.79258363747961,3.50073319500935,14.0607797926106));
#30720=CARTESIAN_POINT('Ctrl Pts',(-1.68931916251746,3.55361074889263,14.0549290005993));
#30721=CARTESIAN_POINT('Ctrl Pts',(-1.5836945461416,3.60192476758717,14.049078208588));
#30722=CARTESIAN_POINT('Ctrl Pts',(-1.47615316630862,3.64547127674832,14.0432274165767));
#30723=CARTESIAN_POINT('Ctrl Pts',(-1.36860214124985,3.68902169153087,14.0373760998166));
#30724=CARTESIAN_POINT('Ctrl Pts',(-1.25913439420161,3.7278035915955,14.0315247830565));
#30725=CARTESIAN_POINT('Ctrl Pts',(-1.14821242878449,3.76166149704952,14.0256734662963));
#30726=CARTESIAN_POINT('Ctrl Pts',(-1.03725364851147,3.79553063989828,14.0198202074918));
#30727=CARTESIAN_POINT('Ctrl Pts',(-0.924840085338792,3.82447241787311,
14.0139669486873));
#30728=CARTESIAN_POINT('Ctrl Pts',(-0.811447817423676,3.84838166501172,
14.0081136898828));
#30729=CARTESIAN_POINT('Ctrl Pts',(-0.69792654368625,3.87231811358252,14.0022537718546));
#30730=CARTESIAN_POINT('Ctrl Pts',(-0.583424747514154,3.89121051805456,
13.9963938538265));
#30731=CARTESIAN_POINT('Ctrl Pts',(-0.468427178759808,3.90500511884416,
13.9905339357984));
#30732=CARTESIAN_POINT('Ctrl Pts',(-0.353352178851344,3.91880900793327,
13.9846700721198));
#30733=CARTESIAN_POINT('Ctrl Pts',(-0.23778115290438,3.92750822761183,13.9788062084411));
#30734=CARTESIAN_POINT('Ctrl Pts',(-0.122200679729478,3.93110111722831,
13.9729423447625));
#30735=CARTESIAN_POINT('Ctrl Pts',(-0.00644969756785038,3.93469930722081,
13.9670698304751));
#30736=CARTESIAN_POINT('Ctrl Pts',(0.109310347808056,3.933176137972,13.9611973161877));
#30737=CARTESIAN_POINT('Ctrl Pts',(0.224596083185247,3.92658192317668,13.9553248019003));
#30738=CARTESIAN_POINT('Ctrl Pts',(0.256458588835168,3.92475942358048,13.953701764852));
#30739=CARTESIAN_POINT('Ctrl Pts',(0.28828491594598,3.9225498739989,13.9520787278036));
#30740=CARTESIAN_POINT('Ctrl Pts',(0.320064996647098,3.91995502498706,13.9504556907553));
#30741=CARTESIAN_POINT('Ctrl Pts',(0.435044857223373,3.91056689975214,13.9445835667893));
#30742=CARTESIAN_POINT('Ctrl Pts',(0.549804072017342,3.89609987364663,13.9387114428232));
#30743=CARTESIAN_POINT('Ctrl Pts',(0.663857834011462,3.87656829892388,13.9328393188572));
#30744=CARTESIAN_POINT('Ctrl Pts',(0.777763723038539,3.85706204727557,13.9269748082165));
#30745=CARTESIAN_POINT('Ctrl Pts',(0.890965574425546,3.83250437410981,13.9211102975758));
#30746=CARTESIAN_POINT('Ctrl Pts',(1.0029818784939,3.80296152378812,13.9152457869351));
#30747=CARTESIAN_POINT('Ctrl Pts',(1.11488291889988,3.77344907276547,13.9093873108175));
#30748=CARTESIAN_POINT('Ctrl Pts',(1.22560044112199,3.73896175259183,13.9035288346999));
#30749=CARTESIAN_POINT('Ctrl Pts',(1.33466199872439,3.69961705439374,13.8976703585822));
#30750=CARTESIAN_POINT('Ctrl Pts',(1.44802399800976,3.65872094262836,13.891580874991));
#30751=CARTESIAN_POINT('Ctrl Pts',(1.55959630369189,3.61257658314208,13.8854913913997));
#30752=CARTESIAN_POINT('Ctrl Pts',(1.66886409402017,3.56137356025596,13.8794019078084));
#30753=CARTESIAN_POINT('Ctrl Pts',(1.77386489214363,3.51217005524115,13.873550223288));
#30754=CARTESIAN_POINT('Ctrl Pts',(1.87673737398412,3.45829575416619,13.8676985387676));
#30755=CARTESIAN_POINT('Ctrl Pts',(1.97704478296108,3.39996807722755,13.8618468542472));
#30756=CARTESIAN_POINT('Ctrl Pts',(2.07733689287751,3.34164929652766,13.8559960622359));
#30757=CARTESIAN_POINT('Ctrl Pts',(2.17506435053191,3.27887869825671,13.8501452702246));
#30758=CARTESIAN_POINT('Ctrl Pts',(2.26981594510753,3.21191914209178,13.8442944782133));
#30759=CARTESIAN_POINT('Ctrl Pts',(2.36457603781254,3.14495358042399,13.8384431614532));
#30760=CARTESIAN_POINT('Ctrl Pts',(2.45635939922749,3.07379855260564,13.8325918446931));
#30761=CARTESIAN_POINT('Ctrl Pts',(2.54478528928605,2.99875921531445,13.826740527933));
#30762=CARTESIAN_POINT('Ctrl Pts',(2.63324052778248,2.92369497256483,13.8208872691284));
#30763=CARTESIAN_POINT('Ctrl Pts',(2.71833576408495,2.84474412420843,13.8150340103239));
#30764=CARTESIAN_POINT('Ctrl Pts',(2.79972525940186,2.76225043612399,13.8091807515193));
#30765=CARTESIAN_POINT('Ctrl Pts',(2.8812073511449,2.67966289537878,13.8033208334912));
#30766=CARTESIAN_POINT('Ctrl Pts',(2.95897499634773,2.59352476425796,13.7974609154631));
#30767=CARTESIAN_POINT('Ctrl Pts',(3.03272102596443,2.50421488268744,13.791600997435));
#30768=CARTESIAN_POINT('Ctrl Pts',(3.10651671089327,2.41484486621786,13.7857371337563));
#30769=CARTESIAN_POINT('Ctrl Pts',(3.17628514007976,2.32229917614927,13.7798732700777));
#30770=CARTESIAN_POINT('Ctrl Pts',(3.24176199442451,2.22698634290937,13.7740094063991));
#30771=CARTESIAN_POINT('Ctrl Pts',(3.30733544287201,2.13153290032437,13.7681368921117));
#30772=CARTESIAN_POINT('Ctrl Pts',(3.36860446279701,2.03330451671025,13.7622643778243));
#30773=CARTESIAN_POINT('Ctrl Pts',(3.42535020062575,1.93273510939113,13.7563918635369));
#30774=CARTESIAN_POINT('Ctrl Pts',(3.44103350599118,1.90493988131309,13.7547688264885));
#30775=CARTESIAN_POINT('Ctrl Pts',(3.45637158232319,1.87696595378804,13.7531457894402));
#30776=CARTESIAN_POINT('Ctrl Pts',(3.47136046246101,1.84882274425173,13.7515227523918));
#30777=CARTESIAN_POINT('Ctrl Pts',(3.52866492773603,1.74122754309106,13.7453176677343));
#30778=CARTESIAN_POINT('Ctrl Pts',(3.58103620167279,1.63082901965534,13.7391125830767));
#30779=CARTESIAN_POINT('Ctrl Pts',(3.62820672022146,1.51809255163835,13.7329074984191));
#30780=CARTESIAN_POINT('Ctrl Pts',(3.67528768351236,1.40557011865349,13.7267141943816));
#30781=CARTESIAN_POINT('Ctrl Pts',(3.71718742956168,1.29071889958609,13.720520890344));
#30782=CARTESIAN_POINT('Ctrl Pts',(3.75368432305832,1.17402853578019,13.7143275863065));
#30783=CARTESIAN_POINT('Ctrl Pts',(3.79009025522458,1.0576289997604,13.7081497178614));
#30784=CARTESIAN_POINT('Ctrl Pts',(3.82112007752275,0.939399784372105,13.7019718494164));
#30785=CARTESIAN_POINT('Ctrl Pts',(3.84660061620373,0.819849193096546,13.6957939809713));
#30786=CARTESIAN_POINT('Ctrl Pts',(3.87204208990804,0.70048188841153,13.6896255840013));
#30787=CARTESIAN_POINT('Ctrl Pts',(3.89195115264444,0.579797577402339,13.6834571870313));
#30788=CARTESIAN_POINT('Ctrl Pts',(3.90620429215287,0.45831978788454,13.6772887900613));
#30789=CARTESIAN_POINT('Ctrl Pts',(3.92042982092566,0.337077321337482,13.6711323423168));
#30790=CARTESIAN_POINT('Ctrl Pts',(3.92902122565854,0.215044780944509,13.6649758945723));
#30791=CARTESIAN_POINT('Ctrl Pts',(3.93190608507485,0.0927552594271314,
13.6588194468278));
#30792=CARTESIAN_POINT('Ctrl Pts',(3.93263332741248,0.0619273733287159,
13.6572674719122));
#30793=CARTESIAN_POINT('Ctrl Pts',(3.93299817815724,0.0310832048097634,
13.6557154969966));
#30794=CARTESIAN_POINT('Ctrl Pts',(3.93299999319383,0.000231381426136011,
13.654163522081));
#30795=CARTESIAN_POINT('',(3.93299832708652,-0.00362755215277343,12.404163522035));
#30796=CARTESIAN_POINT('Ctrl Pts',(3.93299999319388,0.000231380512522024,
13.654163522035));
#30797=CARTESIAN_POINT('Ctrl Pts',(3.93300713064364,-0.12109080676601,13.6480605118815));
#30798=CARTESIAN_POINT('Ctrl Pts',(3.92739626933809,-0.242314977188312,
13.641957501728));
#30799=CARTESIAN_POINT('Ctrl Pts',(3.9162204337665,-0.362913921129693,13.6358544915745));
#30800=CARTESIAN_POINT('Ctrl Pts',(3.90503076600943,-0.483662128806295,
13.6297439278052));
#30801=CARTESIAN_POINT('Ctrl Pts',(3.88826242076357,-0.603783209724141,
13.6236333640359));
#30802=CARTESIAN_POINT('Ctrl Pts',(3.86601983502594,-0.722758351861834,
13.6175228002666));
#30803=CARTESIAN_POINT('Ctrl Pts',(3.84372661366624,-0.842004342919838,
13.6113983256957));
#30804=CARTESIAN_POINT('Ctrl Pts',(3.81593430937306,-0.960098827271787,
13.6052738511248));
#30805=CARTESIAN_POINT('Ctrl Pts',(3.78279806763248,-1.07653508048553,13.5991493765539));
#30806=CARTESIAN_POINT('Ctrl Pts',(3.74962104396456,-1.19311463585328,13.5930173643787));
#30807=CARTESIAN_POINT('Ctrl Pts',(3.71108707651018,-1.30803154905568,13.5868853522035));
#30808=CARTESIAN_POINT('Ctrl Pts',(3.66739993048077,-1.42079792719078,13.5807533400283));
#30809=CARTESIAN_POINT('Ctrl Pts',(3.62361518202276,-1.53381623920967,13.5746076281878));
#30810=CARTESIAN_POINT('Ctrl Pts',(3.57465438680126,-1.64467408370087,13.5684619163473));
#30811=CARTESIAN_POINT('Ctrl Pts',(3.52076837296381,-1.75290589135236,13.5623162045067));
#30812=CARTESIAN_POINT('Ctrl Pts',(3.49234115815661,-1.81000287489173,13.5590740743473));
#30813=CARTESIAN_POINT('Ctrl Pts',(3.46254399245362,-1.86636948408595,13.5558319441879));
#30814=CARTESIAN_POINT('Ctrl Pts',(3.43141852376606,-1.9219406636926,13.5525898140285));
#30815=CARTESIAN_POINT('Ctrl Pts',(3.37504428780194,-2.0225908040454,13.5467176900624));
#30816=CARTESIAN_POINT('Ctrl Pts',(3.31414339153923,-2.12092723197968,13.5408455660964));
#30817=CARTESIAN_POINT('Ctrl Pts',(3.24893058939613,-2.216515063176,13.5349734421304));
#30818=CARTESIAN_POINT('Ctrl Pts',(3.18380233694594,-2.31197896285108,13.5291089314897));
#30819=CARTESIAN_POINT('Ctrl Pts',(3.1143735268679,-2.4047010141651,13.523244420849));
#30820=CARTESIAN_POINT('Ctrl Pts',(3.04090472941863,-2.4942709208503,13.5173799102083));
#30821=CARTESIAN_POINT('Ctrl Pts',(2.96751153063104,-2.5837486609926,13.5115214340907));
#30822=CARTESIAN_POINT('Ctrl Pts',(2.89008687375892,-2.67008039031586,13.5056629579731));
#30823=CARTESIAN_POINT('Ctrl Pts',(2.808934159163,-2.7528853752903,13.4998044818555));
#30824=CARTESIAN_POINT('Ctrl Pts',(2.72458148553266,-2.83895547050886,13.4937149982642));
#30825=CARTESIAN_POINT('Ctrl Pts',(2.63620095757157,-2.92121459513927,13.4876255146729));
#30826=CARTESIAN_POINT('Ctrl Pts',(2.54417916322833,-2.99927347625967,13.4815360310817));
#30827=CARTESIAN_POINT('Ctrl Pts',(2.45575089153234,-3.07428409735508,13.4756843465613));
#30828=CARTESIAN_POINT('Ctrl Pts',(2.36396075026837,-3.14541607190262,13.4698326620409));
#30829=CARTESIAN_POINT('Ctrl Pts',(2.2691881608167,-3.21236269602443,13.4639809775205));
#30830=CARTESIAN_POINT('Ctrl Pts',(2.17443002624507,-3.27929910933079,13.4581301855092));
#30831=CARTESIAN_POINT('Ctrl Pts',(2.07669068551652,-3.34205120300772,13.4522793934979));
#30832=CARTESIAN_POINT('Ctrl Pts',(1.97638025177507,-3.40035440805712,13.4464286014866));
#30833=CARTESIAN_POINT('Ctrl Pts',(1.87606082134031,-3.4586628422341,13.4405772847264));
#30834=CARTESIAN_POINT('Ctrl Pts',(1.77317019693155,-3.51252138682279,13.4347259679663));
#30835=CARTESIAN_POINT('Ctrl Pts',(1.66814427683231,-3.56171077877915,13.4288746512062));
#30836=CARTESIAN_POINT('Ctrl Pts',(1.56308349876767,-3.61091649663032,13.4230213924017));
#30837=CARTESIAN_POINT('Ctrl Pts',(1.4558863899923,-3.65544980514802,13.4171681335972));
#30838=CARTESIAN_POINT('Ctrl Pts',(1.34700939553832,-3.69513933273584,13.4113148747927));
#30839=CARTESIAN_POINT('Ctrl Pts',(1.23800853226577,-3.73487401490308,13.4054549567646));
#30840=CARTESIAN_POINT('Ctrl Pts',(1.12732435725675,-3.76975377516436,13.3995950387365));
#30841=CARTESIAN_POINT('Ctrl Pts',(1.01542916296934,-3.7996569075367,13.3937351207084));
#30842=CARTESIAN_POINT('Ctrl Pts',(0.903458626445167,-3.8295801745439,13.3878712570297));
#30843=CARTESIAN_POINT('Ctrl Pts',(0.790275849736148,-3.85452005260822,
13.3820073933511));
#30844=CARTESIAN_POINT('Ctrl Pts',(0.67636229646865,-3.87440615371126,13.3761435296725));
#30845=CARTESIAN_POINT('Ctrl Pts',(0.562280693322265,-3.89432159159456,
13.3702710153851));
#30846=CARTESIAN_POINT('Ctrl Pts',(0.447466570451588,-3.90916831983204,
13.3643985010977));
#30847=CARTESIAN_POINT('Ctrl Pts',(0.332405560992506,-3.9189278563175,13.3585259868103));
#30848=CARTESIAN_POINT('Ctrl Pts',(0.300605164765652,-3.92162518296783,
13.3569029497618));
#30849=CARTESIAN_POINT('Ctrl Pts',(0.268785901636926,-3.92393423057168,
13.3552799127134));
#30850=CARTESIAN_POINT('Ctrl Pts',(0.236957985811464,-3.92585530973318,
13.3536568756649));
#30851=CARTESIAN_POINT('Ctrl Pts',(0.121805058475212,-3.93280574564309,
13.3477847516989));
#30852=CARTESIAN_POINT('Ctrl Pts',(0.00615301487782126,-3.9346970510376,
13.3419126277329));
#30853=CARTESIAN_POINT('Ctrl Pts',(-0.109516173066837,-3.93147494050729,
13.3360405037669));
#30854=CARTESIAN_POINT('Ctrl Pts',(-0.225035393612344,-3.92825700750727,
13.3301759931262));
#30855=CARTESIAN_POINT('Ctrl Pts',(-0.340571304869079,-3.91993885394681,
13.3243114824855));
#30856=CARTESIAN_POINT('Ctrl Pts',(-0.455637867853506,-3.90651803187671,
13.3184469718449));
#30857=CARTESIAN_POINT('Ctrl Pts',(-0.570586028489416,-3.893111019699,13.3125884957273));
#30858=CARTESIAN_POINT('Ctrl Pts',(-0.685065393316299,-3.87461183030031,
13.3067300196097));
#30859=CARTESIAN_POINT('Ctrl Pts',(-0.798591655524796,-3.85107002893042,
13.3008715434922));
#30860=CARTESIAN_POINT('Ctrl Pts',(-0.916594408634085,-3.826599943148,13.2947820599009));
#30861=CARTESIAN_POINT('Ctrl Pts',(-1.03356689369985,-3.79668140298915,
13.2886925763096));
#30862=CARTESIAN_POINT('Ctrl Pts',(-1.14897266828653,-3.76142935697728,
13.2826030927183));
#30863=CARTESIAN_POINT('Ctrl Pts',(-1.25987175760789,-3.72755393078278,
13.276751408198));
#30864=CARTESIAN_POINT('Ctrl Pts',(-1.36932377014591,-3.68875386908723,
13.2708997236776));
#30865=CARTESIAN_POINT('Ctrl Pts',(-1.47686561295014,-3.64518270615965,
13.2650480391572));
#30866=CARTESIAN_POINT('Ctrl Pts',(-1.58439105328567,-3.60161818878154,
13.259197247146));
#30867=CARTESIAN_POINT('Ctrl Pts',(-1.69000652011402,-3.55328417225649,
13.2533464551347));
#30868=CARTESIAN_POINT('Ctrl Pts',(-1.79326779030938,-3.50038278367365,
13.2474956631234));
#30869=CARTESIAN_POINT('Ctrl Pts',(-1.89653832185428,-3.44747665044406,
13.2416443463633));
#30870=CARTESIAN_POINT('Ctrl Pts',(-1.99745386907008,-3.39000251933692,
13.2357930296032));
#30871=CARTESIAN_POINT('Ctrl Pts',(-2.09559439821346,-3.32820869510558,
13.2299417128431));
#30872=CARTESIAN_POINT('Ctrl Pts',(-2.19376750007045,-3.26639436158458,
13.2240884540386));
#30873=CARTESIAN_POINT('Ctrl Pts',(-2.28916340280131,-3.20025770427893,
13.2182351952341));
#30874=CARTESIAN_POINT('Ctrl Pts',(-2.38139126814028,-3.13009019487063,
13.2123819364296));
#30875=CARTESIAN_POINT('Ctrl Pts',(-2.47372406066531,-3.05984285623405,
13.2065220184015));
#30876=CARTESIAN_POINT('Ctrl Pts',(-2.56288129257795,-2.98555576266533,
13.2006621003734));
#30877=CARTESIAN_POINT('Ctrl Pts',(-2.64850535321555,-2.90756055723497,
13.1948021823454));
#30878=CARTESIAN_POINT('Ctrl Pts',(-2.73418706698361,-2.8295128354007,13.1889383186668));
#30879=CARTESIAN_POINT('Ctrl Pts',(-2.81633058015719,-2.74775232106288,
13.1830744549882));
#30880=CARTESIAN_POINT('Ctrl Pts',(-2.89461650753482,-2.66264610384236,
13.1772105913096));
#30881=CARTESIAN_POINT('Ctrl Pts',(-2.97301792547758,-2.5774143344894,13.1713380770222));
#30882=CARTESIAN_POINT('Ctrl Pts',(-3.04755013455492,-2.48882732663886,
13.1654655627349));
#30883=CARTESIAN_POINT('Ctrl Pts',(-3.11793517238528,-2.39728372555331,
13.1595930484475));
#30884=CARTESIAN_POINT('Ctrl Pts',(-3.13738808786231,-2.37198303680932,
13.1579700113989));
#30885=CARTESIAN_POINT('Ctrl Pts',(-3.15652448380176,-2.34645666696216,
13.1563469743502));
#30886=CARTESIAN_POINT('Ctrl Pts',(-3.17533910233633,-2.32071337850538,
13.1547239373016));
#30887=CARTESIAN_POINT('Ctrl Pts',(-3.24341011310096,-2.22757454274115,
13.1488518133354));
#30888=CARTESIAN_POINT('Ctrl Pts',(-3.30749385624835,-2.13128203997407,
13.1429796893693));
#30889=CARTESIAN_POINT('Ctrl Pts',(-3.36728422133357,-2.03221208852767,
13.1371075654032));
#30890=CARTESIAN_POINT('Ctrl Pts',(-3.42699706702323,-1.93327058324048,
13.1312430547623));
#30891=CARTESIAN_POINT('Ctrl Pts',(-3.48242739266084,-1.83155914106754,
13.1253785441215));
#30892=CARTESIAN_POINT('Ctrl Pts',(-3.53331050837613,-1.72748541278901,
13.1195140334807));
#30893=CARTESIAN_POINT('Ctrl Pts',(-3.58414126587168,-1.62351877534124,
13.113655557363));
#30894=CARTESIAN_POINT('Ctrl Pts',(-3.63043393977614,-1.51719505586621,
13.1077970812453));
#30895=CARTESIAN_POINT('Ctrl Pts',(-3.67196854227613,-1.40894855283454,
13.1019386051276));
#30896=CARTESIAN_POINT('Ctrl Pts',(-3.71514090916976,-1.29643374680412,
13.0958491215363));
#30897=CARTESIAN_POINT('Ctrl Pts',(-3.75317201572699,-1.18184179140842,
13.0897596379451));
#30898=CARTESIAN_POINT('Ctrl Pts',(-3.78586871898737,-1.06568618391762,
13.0836701543539));
#30899=CARTESIAN_POINT('Ctrl Pts',(-3.8172885905535,-0.954066543246762,
13.0778184698334));
#30900=CARTESIAN_POINT('Ctrl Pts',(-3.84378274322947,-0.841003517854998,
13.0719667853129));
#30901=CARTESIAN_POINT('Ctrl Pts',(-3.86523013594268,-0.72696973540895,
13.0661151007924));
#30902=CARTESIAN_POINT('Ctrl Pts',(-3.88667425746228,-0.612953345593541,
13.060264308781));
#30903=CARTESIAN_POINT('Ctrl Pts',(-3.90307307311108,-0.49796689929363,
13.0544135167695));
#30904=CARTESIAN_POINT('Ctrl Pts',(-3.91435662611418,-0.382493403336624,
13.0485627247581));
#30905=CARTESIAN_POINT('Ctrl Pts',(-3.92564119112232,-0.26700955073387,
13.0427114079979));
#30906=CARTESIAN_POINT('Ctrl Pts',(-3.93180954126403,-0.151038973114173,
13.0368600912377));
#30907=CARTESIAN_POINT('Ctrl Pts',(-3.9328436462599,-0.0350692753433018,
13.0310087744774));
#30908=CARTESIAN_POINT('Ctrl Pts',(-3.93387809447388,0.08093891261901,13.0251555156728));
#30909=CARTESIAN_POINT('Ctrl Pts',(-3.9297749054669,0.196945806974127,13.0193022568682));
#30910=CARTESIAN_POINT('Ctrl Pts',(-3.92056814712845,0.312465043999806,
13.0134489980635));
#30911=CARTESIAN_POINT('Ctrl Pts',(-3.91135091430659,0.42811570668989,13.0075890800353));
#30912=CARTESIAN_POINT('Ctrl Pts',(-3.89701855578512,0.543277192321976,
13.0017291620071));
#30913=CARTESIAN_POINT('Ctrl Pts',(-3.8776568957996,0.6574693897497,12.9958692439789));
#30914=CARTESIAN_POINT('Ctrl Pts',(-3.85828219905428,0.771738476052125,
12.9900053803002));
#30915=CARTESIAN_POINT('Ctrl Pts',(-3.83387154477571,0.885036571444755,
12.9841415166214));
#30916=CARTESIAN_POINT('Ctrl Pts',(-3.80456123845042,0.996896575819474,
12.9782776529427));
#30917=CARTESIAN_POINT('Ctrl Pts',(-3.77520769237632,1.10892160059478,12.9724051386552));
#30918=CARTESIAN_POINT('Ctrl Pts',(-3.74094019009118,1.21950390676341,12.9665326243677));
#30919=CARTESIAN_POINT('Ctrl Pts',(-3.70194397204481,1.32819419809044,12.9606601100802));
#30920=CARTESIAN_POINT('Ctrl Pts',(-3.69116625342237,1.3582338643863,12.9590370730328));
#30921=CARTESIAN_POINT('Ctrl Pts',(-3.68002760666876,1.38812914418125,12.9574140359855));
#30922=CARTESIAN_POINT('Ctrl Pts',(-3.66853256383573,1.41787087849241,12.9557909989381));
#30923=CARTESIAN_POINT('Ctrl Pts',(-3.62694366935026,1.52547603212679,12.9499188749722));
#30924=CARTESIAN_POINT('Ctrl Pts',(-3.58054663655935,1.63143020888402,12.9440467510062));
#30925=CARTESIAN_POINT('Ctrl Pts',(-3.52949262520624,1.73527254591743,12.9381746270403));
#30926=CARTESIAN_POINT('Ctrl Pts',(-3.47850480639256,1.83898024929902,12.9323101163997));
#30927=CARTESIAN_POINT('Ctrl Pts',(-3.42287219685505,1.94058119035989,12.926445605759));
#30928=CARTESIAN_POINT('Ctrl Pts',(-3.36279478643395,2.03963237480009,12.9205810951184));
#30929=CARTESIAN_POINT('Ctrl Pts',(-3.30277919507061,2.13858163655672,12.9147226190009));
#30930=CARTESIAN_POINT('Ctrl Pts',(-3.23832811314525,2.23498600895748,12.9088641428834));
#30931=CARTESIAN_POINT('Ctrl Pts',(-3.16968810763422,2.32842571286313,12.9030056667659));
#30932=CARTESIAN_POINT('Ctrl Pts',(-3.09834153578124,2.4255498680696,12.8969161831746));
#30933=CARTESIAN_POINT('Ctrl Pts',(-3.02246909522505,2.51947033480564,12.8908266995833));
#30934=CARTESIAN_POINT('Ctrl Pts',(-2.94239849967909,2.60974712742178,12.884737215992));
#30935=CARTESIAN_POINT('Ctrl Pts',(-2.86545472317267,2.69649854106383,12.8788855314717));
#30936=CARTESIAN_POINT('Ctrl Pts',(-2.78463482136749,2.77988517853167,12.8730338469514));
#30937=CARTESIAN_POINT('Ctrl Pts',(-2.70027107867531,2.85954980751686,12.867182162431));
#30938=CARTESIAN_POINT('Ctrl Pts',(-2.61592020328776,2.9392022859144,12.8613313704198));
#30939=CARTESIAN_POINT('Ctrl Pts',(-2.52802686221723,3.01513360081178,12.8554805784086));
#30940=CARTESIAN_POINT('Ctrl Pts',(-2.43695967661988,3.0870238960087,12.8496297863974));
#30941=CARTESIAN_POINT('Ctrl Pts',(-2.3458843233422,3.15892063893919,12.8437784696373));
#30942=CARTESIAN_POINT('Ctrl Pts',(-2.25163488417316,3.22677538551229,12.8379271528773));
#30943=CARTESIAN_POINT('Ctrl Pts',(-2.15461190761489,3.29030948811265,12.8320758361172));
#30944=CARTESIAN_POINT('Ctrl Pts',(-2.05755672925711,3.35386467759888,12.8262225773128));
#30945=CARTESIAN_POINT('Ctrl Pts',(-1.95772652876357,3.41309614530512,12.8203693185083));
#30946=CARTESIAN_POINT('Ctrl Pts',(-1.85554896141381,3.46776975184283,12.8145160597038));
#30947=CARTESIAN_POINT('Ctrl Pts',(-1.75325514715125,3.52250556027218,12.8086561416758));
#30948=CARTESIAN_POINT('Ctrl Pts',(-1.64860900033829,3.57267296233976,12.8027962236478));
#30949=CARTESIAN_POINT('Ctrl Pts',(-1.54206088150001,3.61808474717597,12.7969363056197));
#30950=CARTESIAN_POINT('Ctrl Pts',(-1.43544102076429,3.66352710906643,12.7910724419412));
#30951=CARTESIAN_POINT('Ctrl Pts',(-1.32691702413892,3.7042073329776,12.7852085782626));
#30952=CARTESIAN_POINT('Ctrl Pts',(-1.21695558154691,3.73998771556028,12.7793447145841));
#30953=CARTESIAN_POINT('Ctrl Pts',(-1.10683191938939,3.77582088280985,12.7734722002968));
#30954=CARTESIAN_POINT('Ctrl Pts',(-0.995266975889134,3.80673967210187,
12.7675996860095));
#30955=CARTESIAN_POINT('Ctrl Pts',(-0.882738901942349,3.83265717629396,
12.7617271717222));
#30956=CARTESIAN_POINT('Ctrl Pts',(-0.851638554773166,3.83982021881182,
12.760104134673));
#30957=CARTESIAN_POINT('Ctrl Pts',(-0.820464673745179,3.84660154238882,
12.7584810976238));
#30958=CARTESIAN_POINT('Ctrl Pts',(-0.789227414493501,3.85300001144717,
12.7568580605746));
#30959=CARTESIAN_POINT('Ctrl Pts',(-0.676211473933424,3.8761495775774,12.7509859366088));
#30960=CARTESIAN_POINT('Ctrl Pts',(-0.561986667712901,3.89436127347583,
12.7451138126429));
#30961=CARTESIAN_POINT('Ctrl Pts',(-0.447022463926352,3.90751326507604,
12.7392416886771));
#30962=CARTESIAN_POINT('Ctrl Pts',(-0.332207313512615,3.92064820485801,
12.7333771780365));
#30963=CARTESIAN_POINT('Ctrl Pts',(-0.216655078864421,3.92873643926183,
12.727512667396));
#30964=CARTESIAN_POINT('Ctrl Pts',(-0.100846577966071,3.93170687713524,
12.7216481567555));
#30965=CARTESIAN_POINT('Ctrl Pts',(0.0148427571372789,3.93467425845763,
12.715789680638));
#30966=CARTESIAN_POINT('Ctrl Pts',(0.130787423199741,3.93253430735893,12.7099312045206));
#30967=CARTESIAN_POINT('Ctrl Pts',(0.246500968593963,3.92526766889625,12.7040727284031));
#30968=CARTESIAN_POINT('Ctrl Pts',(0.366777252365796,3.91771449725306,12.6979832448118));
#30969=CARTESIAN_POINT('Ctrl Pts',(0.486803361598573,3.90462196463276,12.6918937612205));
#30970=CARTESIAN_POINT('Ctrl Pts',(0.606031994606799,3.8860280778081,12.6858042776291));
#30971=CARTESIAN_POINT('Ctrl Pts',(0.720604656750912,3.86816029672769,12.6799525931089));
#30972=CARTESIAN_POINT('Ctrl Pts',(0.83444051104996,3.84521283256345,12.6741009085887));
#30973=CARTESIAN_POINT('Ctrl Pts',(0.94705941817337,3.81727225364515,12.6682492240685));
#30974=CARTESIAN_POINT('Ctrl Pts',(1.05966114846559,3.78933593627244,12.6623984320573));
#30975=CARTESIAN_POINT('Ctrl Pts',(1.17104589949739,3.75640811788417,12.6565476400462));
#30976=CARTESIAN_POINT('Ctrl Pts',(1.28074534728091,3.71862613816155,12.650696848035));
#30977=CARTESIAN_POINT('Ctrl Pts',(1.39045463384457,3.68084076982942,12.6448455312751));
#30978=CARTESIAN_POINT('Ctrl Pts',(1.49847792578075,3.63820050933438,12.6389942145151));
#30979=CARTESIAN_POINT('Ctrl Pts',(1.60436432185904,3.59089182832702,12.6331428977551));
#30980=CARTESIAN_POINT('Ctrl Pts',(1.71028586149414,3.54356744563012,12.6272896389508));
#30981=CARTESIAN_POINT('Ctrl Pts',(1.81406871775506,3.49157173000692,12.6214363801464));
#30982=CARTESIAN_POINT('Ctrl Pts',(1.91528479340871,3.43513801180351,12.615583121342));
#30983=CARTESIAN_POINT('Ctrl Pts',(2.01661602209066,3.37864008923822,12.6097232033141));
#30984=CARTESIAN_POINT('Ctrl Pts',(2.11537428020042,3.31769428767874,12.6038632852862));
#30985=CARTESIAN_POINT('Ctrl Pts',(2.21115868939502,3.25257840033302,12.5980033672582));
#30986=CARTESIAN_POINT('Ctrl Pts',(2.30700759297325,3.18741866859702,12.5921395035798));
#30987=CARTESIAN_POINT('Ctrl Pts',(2.39987833004557,3.11808350683748,12.5862756399013));
#30988=CARTESIAN_POINT('Ctrl Pts',(2.48940285641362,3.04489119977705,12.5804117762229));
#30989=CARTESIAN_POINT('Ctrl Pts',(2.57905945298267,2.97159091646589,12.5745392619357));
#30990=CARTESIAN_POINT('Ctrl Pts',(2.66535967955664,2.89442240577341,12.5686667476485));
#30991=CARTESIAN_POINT('Ctrl Pts',(2.74797204107872,2.81374104377955,12.5627942333612));
#30992=CARTESIAN_POINT('Ctrl Pts',(2.77080432670303,2.79144244502676,12.5611711963112));
#30993=CARTESIAN_POINT('Ctrl Pts',(2.79335515190305,2.76887571084539,12.5595481592612));
#30994=CARTESIAN_POINT('Ctrl Pts',(2.81561807358169,2.74604877300461,12.5579251222112));
#30995=CARTESIAN_POINT('Ctrl Pts',(2.89510692602653,2.66454612389213,12.5521301347229));
#30996=CARTESIAN_POINT('Ctrl Pts',(2.97120448473133,2.57943463234707,12.5463351472347));
#30997=CARTESIAN_POINT('Ctrl Pts',(3.04355847766435,2.49103207386767,12.5405401597464));
#30998=CARTESIAN_POINT('Ctrl Pts',(3.11579673760803,2.40277091867429,12.5347544415631));
#30999=CARTESIAN_POINT('Ctrl Pts',(3.1843030788273,2.31122949608834,12.5289687233797));
#31000=CARTESIAN_POINT('Ctrl Pts',(3.2487616329008,2.2167626964995,12.5231830051964));
#31001=CARTESIAN_POINT('Ctrl Pts',(3.31316125215976,2.12238226843098,12.5174025769274));
#31002=CARTESIAN_POINT('Ctrl Pts',(3.37352019869514,2.02508212588218,12.5116221486584));
#31003=CARTESIAN_POINT('Ctrl Pts',(3.4295626798161,1.92525032793469,12.5058417203894));
#31004=CARTESIAN_POINT('Ctrl Pts',(3.48556834691289,1.82548410899349,12.5000650892546));
#31005=CARTESIAN_POINT('Ctrl Pts',(3.53726297594805,1.72318990900058,12.4942884581199));
#31006=CARTESIAN_POINT('Ctrl Pts',(3.5844144405252,1.61878414822805,12.4885118269852));
#31007=CARTESIAN_POINT('Ctrl Pts',(3.63154706468069,1.51442010511106,12.4827375040325));
#31008=CARTESIAN_POINT('Ctrl Pts',(3.67413995891684,1.4079465657574,12.4769631810799));
#31009=CARTESIAN_POINT('Ctrl Pts',(3.71200766077777,1.29980311060067,12.4711888581273));
#31010=CARTESIAN_POINT('Ctrl Pts',(3.7498829308237,1.19163804204688,12.4654133811267));
#31011=CARTESIAN_POINT('Ctrl Pts',(3.78303097079323,1.08180278889257,12.4596379041261));
#31012=CARTESIAN_POINT('Ctrl Pts',(3.81131521201403,0.97075504359772,12.4538624271255));
#31013=CARTESIAN_POINT('Ctrl Pts',(3.83960129040054,0.859700085342571,12.4480865749863));
#31014=CARTESIAN_POINT('Ctrl Pts',(3.8630228446412,0.747432892764753,12.4423107228472));
#31015=CARTESIAN_POINT('Ctrl Pts',(3.88149410410307,0.634422981781957,12.4365348707081));
#31016=CARTESIAN_POINT('Ctrl Pts',(3.89998219168447,0.521310113862548,12.4307537565168));
#31017=CARTESIAN_POINT('Ctrl Pts',(3.91351091543769,0.407453597623295,12.4249726423256));
#31018=CARTESIAN_POINT('Ctrl Pts',(3.92204623846465,0.293329683709804,12.4191915281344));
#31019=CARTESIAN_POINT('Ctrl Pts',(3.929442095749,0.194441313888272,12.4141821927679));
#31020=CARTESIAN_POINT('Ctrl Pts',(3.93308962003901,0.0953524250593562,
12.4091728574014));
#31021=CARTESIAN_POINT('Ctrl Pts',(3.93299832708652,-0.00362755215277343,
12.404163522035));
#31022=CARTESIAN_POINT('',(3.93443448987282,0.00134968955162095,11.154163522035));
#31023=CARTESIAN_POINT('Ctrl Pts',(3.93324003457201,-0.00362777508866888,
12.404163522035));
#31024=CARTESIAN_POINT('Ctrl Pts',(3.93600258766685,-0.301163912932759,
12.3891064093059));
#31025=CARTESIAN_POINT('Ctrl Pts',(3.7690722733079,-1.90596907523995,12.3077383171222));
#31026=CARTESIAN_POINT('Ctrl Pts',(1.56812889849248,-4.38010354283667,12.1600592454845));
#31027=CARTESIAN_POINT('Ctrl Pts',(-2.83826737299349,-3.68626824908905,
11.9611263071209));
#31028=CARTESIAN_POINT('Ctrl Pts',(-4.6354315863291,0.396370150380956,11.7621933687574));
#31029=CARTESIAN_POINT('Ctrl Pts',(-2.17122253533752,4.11462367616172,11.563260430394));
#31030=CARTESIAN_POINT('Ctrl Pts',(2.28900123116229,4.05028500649437,11.3643274920306));
#31031=CARTESIAN_POINT('Ctrl Pts',(3.90396011105411,1.45381414440226,11.2279618559109));
#31032=CARTESIAN_POINT('Ctrl Pts',(3.93929569899745,0.0750487185641683,
11.1579071992457));
#31033=CARTESIAN_POINT('Ctrl Pts',(3.93896841652295,0.00135124489418437,
11.154163522035));
#31034=CARTESIAN_POINT('',(3.9329988605794,0.00299377372986385,9.90416352208001));
#31035=CARTESIAN_POINT('Ctrl Pts',(3.93299976858205,0.00134919737711916,
11.154163522035));
#31036=CARTESIAN_POINT('Ctrl Pts',(3.93303902141628,-0.113075415770322,
11.1483421609502));
#31037=CARTESIAN_POINT('Ctrl Pts',(3.92808052764153,-0.227703811320846,
11.1425207998654));
#31038=CARTESIAN_POINT('Ctrl Pts',(3.91809711475004,-0.342058473637813,
11.1366994387805));
#31039=CARTESIAN_POINT('Ctrl Pts',(3.90812625842716,-0.456269307168048,
11.1308853994724));
#31040=CARTESIAN_POINT('Ctrl Pts',(3.89314308324188,-0.570206676261325,
11.1250713601643));
#31041=CARTESIAN_POINT('Ctrl Pts',(3.87317241100323,-0.683391889506635,
11.1192573208562));
#31042=CARTESIAN_POINT('Ctrl Pts',(3.85322128602432,-0.796466317259319,
11.1134489723197));
#31043=CARTESIAN_POINT('Ctrl Pts',(3.82829244368335,-0.908789640732537,
11.1076406237833));
#31044=CARTESIAN_POINT('Ctrl Pts',(3.79846254146286,-1.0198878963413,11.1018322752469));
#31045=CARTESIAN_POINT('Ctrl Pts',(3.76865229567981,-1.13091294366752,11.0960277541263));
#31046=CARTESIAN_POINT('Ctrl Pts',(3.73394752017707,-1.24071412274453,11.0902232330057));
#31047=CARTESIAN_POINT('Ctrl Pts',(3.69447588432086,-1.34882798761429,11.0844187118851));
#31048=CARTESIAN_POINT('Ctrl Pts',(3.6550175900138,-1.45690530962457,11.0786161527127));
#31049=CARTESIAN_POINT('Ctrl Pts',(3.61079578151708,-1.56329605565847,11.0728135935403));
#31050=CARTESIAN_POINT('Ctrl Pts',(3.56198766662226,-1.6675529565297,11.0670110343678));
#31051=CARTESIAN_POINT('Ctrl Pts',(3.51318373164055,-1.7718009288695,11.0612089721249));
#31052=CARTESIAN_POINT('Ctrl Pts',(3.45979444978325,-1.87391503802175,11.055406909882));
#31053=CARTESIAN_POINT('Ctrl Pts',(3.40204441479229,-1.9734697362211,11.0496048476391));
#31054=CARTESIAN_POINT('Ctrl Pts',(3.34428475092241,-2.07304103354693,11.0438018179967));
#31055=CARTESIAN_POINT('Ctrl Pts',(3.28216310060605,-2.1700517077837,11.0379987883543));
#31056=CARTESIAN_POINT('Ctrl Pts',(3.21594865601709,-2.26410318710563,11.0321957587119));
#31057=CARTESIAN_POINT('Ctrl Pts',(3.14966538352637,-2.35825243008048,11.0263866969967));
#31058=CARTESIAN_POINT('Ctrl Pts',(3.07928106441321,-2.44943599100851,11.0205776352814));
#31059=CARTESIAN_POINT('Ctrl Pts',(3.00510669561318,-2.53728649308289,11.0147685735661));
#31060=CARTESIAN_POINT('Ctrl Pts',(2.930891994425,-2.62518476395672,11.0089563531677));
#31061=CARTESIAN_POINT('Ctrl Pts',(2.85288342588868,-2.70974605839912,11.0031441327693));
#31062=CARTESIAN_POINT('Ctrl Pts',(2.77142922418866,-2.79063954234742,10.9973319123708));
#31063=CARTESIAN_POINT('Ctrl Pts',(2.68984406177454,-2.87166308549714,10.9915103471808));
#31064=CARTESIAN_POINT('Ctrl Pts',(2.60480251344148,-2.94900675745116,10.9856887819908));
#31065=CARTESIAN_POINT('Ctrl Pts',(2.51668652332082,-3.02237951676082,10.9798672168009));
#31066=CARTESIAN_POINT('Ctrl Pts',(2.4490501969759,-3.07869919139308,10.9753986829685));
#31067=CARTESIAN_POINT('Ctrl Pts',(2.37960315685819,-3.13268008654891,10.9709301491361));
#31068=CARTESIAN_POINT('Ctrl Pts',(2.30852895187917,-3.1842083911603,10.9664616153037));
#31069=CARTESIAN_POINT('Ctrl Pts',(2.21512996297312,-3.25192200895128,10.960589491346));
#31070=CARTESIAN_POINT('Ctrl Pts',(2.11859260878961,-3.31563630408311,10.9547173673882));
#31071=CARTESIAN_POINT('Ctrl Pts',(2.01929427785213,-3.37504660996461,10.9488452434304));
#31072=CARTESIAN_POINT('Ctrl Pts',(1.92012468918109,-3.43437988919968,10.9429807327985));
#31073=CARTESIAN_POINT('Ctrl Pts',(1.81820159388882,-3.48942006589947,10.9371162221665));
#31074=CARTESIAN_POINT('Ctrl Pts',(1.7139336540081,-3.53990401418717,10.9312517115346));
#31075=CARTESIAN_POINT('Ctrl Pts',(1.60977300480953,-3.59033601498981,10.9253932354263));
#31076=CARTESIAN_POINT('Ctrl Pts',(1.50327268009245,-3.63622093358657,10.9195347593179));
#31077=CARTESIAN_POINT('Ctrl Pts',(1.39486781809373,-3.67734044793876,10.9136762832096));
#31078=CARTESIAN_POINT('Ctrl Pts',(1.28218840855007,-3.72008135930103,10.9075867996151));
#31079=CARTESIAN_POINT('Ctrl Pts',(1.16745156535847,-3.75767308877496,10.9014973160205));
#31080=CARTESIAN_POINT('Ctrl Pts',(1.05117152211228,-3.78992446245307,10.8954078324259));
#31081=CARTESIAN_POINT('Ctrl Pts',(0.939432305261353,-3.82091639483073,
10.889556147916));
#31082=CARTESIAN_POINT('Ctrl Pts',(0.826268588841986,-3.84697711368719,
10.883704463406));
#31083=CARTESIAN_POINT('Ctrl Pts',(0.71215346085846,-3.86798738986922,10.877852778896));
#31084=CARTESIAN_POINT('Ctrl Pts',(0.598055737920354,-3.88899446152599,
10.8720019868955));
#31085=CARTESIAN_POINT('Ctrl Pts',(0.483007298411011,-3.90495254727477,
10.8661511948951));
#31086=CARTESIAN_POINT('Ctrl Pts',(0.367491413672845,-3.91579354165624,
10.8603004028946));
#31087=CARTESIAN_POINT('Ctrl Pts',(0.251965168494878,-3.92663550834962,
10.8544490861457));
#31088=CARTESIAN_POINT('Ctrl Pts',(0.135971806374681,-3.93235943270659,
10.8485977693968));
#31089=CARTESIAN_POINT('Ctrl Pts',(0.019998997685629,-3.93294915300104,
10.8427464526479));
#31090=CARTESIAN_POINT('Ctrl Pts',(-0.0960123022194861,-3.93353906902284,
10.836893193855));
#31091=CARTESIAN_POINT('Ctrl Pts',(-0.21200262194024,-3.92899139051807,
10.8310399350621));
#31092=CARTESIAN_POINT('Ctrl Pts',(-0.327485731869154,-3.91934204879111,
10.8251866762692));
#31093=CARTESIAN_POINT('Ctrl Pts',(-0.443100226351587,-3.9096817290566,
10.8193267582531));
#31094=CARTESIAN_POINT('Ctrl Pts',(-0.558205947042739,-3.89490819564083,
10.8134668402371));
#31095=CARTESIAN_POINT('Ctrl Pts',(-0.672323115186839,-3.87510911185549,
10.8076069222211));
#31096=CARTESIAN_POINT('Ctrl Pts',(-0.786517121680261,-3.85529669678144,
10.8017430585549));
#31097=CARTESIAN_POINT('Ctrl Pts',(-0.899720847428843,-3.83045208184253,
10.7958791948887));
#31098=CARTESIAN_POINT('Ctrl Pts',(-1.01146771805528,-3.80071336137468,
10.7900153312225));
#31099=CARTESIAN_POINT('Ctrl Pts',(-1.12337944217693,-3.77093076914573,
10.7841428169479));
#31100=CARTESIAN_POINT('Ctrl Pts',(-1.23382962881059,-3.73623978506127,
10.7782703026733));
#31101=CARTESIAN_POINT('Ctrl Pts',(-1.34236969483216,-3.69682736983974,
10.7723977883986));
#31102=CARTESIAN_POINT('Ctrl Pts',(-1.3723678440887,-3.68593462250954,10.7707747512458));
#31103=CARTESIAN_POINT('Ctrl Pts',(-1.40222022486759,-3.67468150291626,
10.769151714093));
#31104=CARTESIAN_POINT('Ctrl Pts',(-1.4319176956174,-3.66307257817502,10.7675286769402));
#31105=CARTESIAN_POINT('Ctrl Pts',(-1.53936270136931,-3.62107166179718,
10.7616565527553));
#31106=CARTESIAN_POINT('Ctrl Pts',(-1.64513831813272,-3.57426896836526,
10.7557844285705));
#31107=CARTESIAN_POINT('Ctrl Pts',(-1.7487842656419,-3.52281742249628,10.7499123043856));
#31108=CARTESIAN_POINT('Ctrl Pts',(-1.85229583414077,-3.47143258456889,
10.7440477935253));
#31109=CARTESIAN_POINT('Ctrl Pts',(-1.95368285745297,-3.41541106249665,
10.738183282665));
#31110=CARTESIAN_POINT('Ctrl Pts',(-2.05250311084,-3.35495454216479,10.7323187718047));
#31111=CARTESIAN_POINT('Ctrl Pts',(-2.15122167918183,-3.29456023098329,
10.7264602954669));
#31112=CARTESIAN_POINT('Ctrl Pts',(-2.24737838050312,-3.22974021314422,
10.7206018191292));
#31113=CARTESIAN_POINT('Ctrl Pts',(-2.34055438353376,-3.16074266236922,
10.7147433427915));
#31114=CARTESIAN_POINT('Ctrl Pts',(-2.43740443483996,-3.08902445043473,
10.7086538592825));
#31115=CARTESIAN_POINT('Ctrl Pts',(-2.5310334788226,-3.01279267924939,10.7025643757736));
#31116=CARTESIAN_POINT('Ctrl Pts',(-2.62100278885694,-2.932376746055,10.6964748922647));
#31117=CARTESIAN_POINT('Ctrl Pts',(-2.70745873177258,-2.85510111365204,
10.6906232075242));
#31118=CARTESIAN_POINT('Ctrl Pts',(-2.79053507025231,-2.77396227746486,
10.6847715227838));
#31119=CARTESIAN_POINT('Ctrl Pts',(-2.86987584785386,-2.68929388834784,
10.6789198380434));
#31120=CARTESIAN_POINT('Ctrl Pts',(-2.94920452425714,-2.60463841300601,
10.6730690458124));
#31121=CARTESIAN_POINT('Ctrl Pts',(-3.02479849002867,-2.51645475669091,
10.6672182535815));
#31122=CARTESIAN_POINT('Ctrl Pts',(-3.09633930379688,-2.42511276351486,
10.6613674613506));
#31123=CARTESIAN_POINT('Ctrl Pts',(-3.16788653394604,-2.33376257802181,
10.6555161443714));
#31124=CARTESIAN_POINT('Ctrl Pts',(-3.23537963451814,-2.23925381804811,
10.6496648273923));
#31125=CARTESIAN_POINT('Ctrl Pts',(-3.29854149476455,-2.14198809691288,
10.6438135104132));
#31126=CARTESIAN_POINT('Ctrl Pts',(-3.36172431834001,-2.04469009342704,
10.6379602513906));
#31127=CARTESIAN_POINT('Ctrl Pts',(-3.42057281811699,-1.94463365583845,
10.6321069923679));
#31128=CARTESIAN_POINT('Ctrl Pts',(-3.47485449511554,-1.84224733349659,
10.6262537333452));
#31129=CARTESIAN_POINT('Ctrl Pts',(-3.5291979280851,-1.7397445267883,10.6203938151014));
#31130=CARTESIAN_POINT('Ctrl Pts',(-3.57896397413598,-1.63490691007829,
10.6145338968575));
#31131=CARTESIAN_POINT('Ctrl Pts',(-3.62396714946527,-1.52818555797279,
10.6086739786136));
#31132=CARTESIAN_POINT('Ctrl Pts',(-3.66900062671078,-1.42139234734957,
10.6028101147203));
#31133=CARTESIAN_POINT('Ctrl Pts',(-3.70926470424461,-1.31271326246949,
10.5969462508271));
#31134=CARTESIAN_POINT('Ctrl Pts',(-3.74462346799198,-1.20261551751327,
10.5910823869338));
#31135=CARTESIAN_POINT('Ctrl Pts',(-3.78003439439521,-1.09235535198087,
10.5852098724351));
#31136=CARTESIAN_POINT('Ctrl Pts',(-3.81052545579805,-0.980672746727933,
10.5793373579364));
#31137=CARTESIAN_POINT('Ctrl Pts',(-3.83601157787593,-0.868046182182596,
10.5734648434377));
#31138=CARTESIAN_POINT('Ctrl Pts',(-3.84305538627748,-0.836918655634727,
10.5718418084841));
#31139=CARTESIAN_POINT('Ctrl Pts',(-3.84971719775555,-0.805719058641991,
10.5702187735305));
#31140=CARTESIAN_POINT('Ctrl Pts',(-3.85599591565923,-0.774457551076468,
10.5685957385768));
#31141=CARTESIAN_POINT('Ctrl Pts',(-3.87871225158276,-0.661353742587398,
10.5627236150339));
#31142=CARTESIAN_POINT('Ctrl Pts',(-3.89648612205457,-0.547059998442666,
10.5568514914909));
#31143=CARTESIAN_POINT('Ctrl Pts',(-3.90919749281048,-0.432046250075409,
10.550979367948));
#31144=CARTESIAN_POINT('Ctrl Pts',(-3.92189238302123,-0.317181619321923,
10.5451148577301));
#31145=CARTESIAN_POINT('Ctrl Pts',(-3.92953778120365,-0.201599247850998,
10.5392503475122));
#31146=CARTESIAN_POINT('Ctrl Pts',(-3.93206443912526,-0.0857802224674986,
10.5333858372943));
#31147=CARTESIAN_POINT('Ctrl Pts',(-3.93458849714113,0.0299196262972318,
10.5275273615987));
#31148=CARTESIAN_POINT('Ctrl Pts',(-3.93200428251064,0.145855233786871,
10.5216688859032));
#31149=CARTESIAN_POINT('Ctrl Pts',(-3.9242943044177,0.261540077836615,10.5158104102076));
#31150=CARTESIAN_POINT('Ctrl Pts',(-3.91628031088973,0.381786540319882,
10.5097209264578));
#31151=CARTESIAN_POINT('Ctrl Pts',(-3.90272795529233,0.501761604293995,
10.5036314427081));
#31152=CARTESIAN_POINT('Ctrl Pts',(-3.88367734128387,0.620918117627617,
10.4975419589583));
#31153=CARTESIAN_POINT('Ctrl Pts',(-3.86537067035357,0.735421465279937,
10.4916902748555));
#31154=CARTESIAN_POINT('Ctrl Pts',(-3.8419871775853,0.849168546146305,10.4858385907527));
#31155=CARTESIAN_POINT('Ctrl Pts',(-3.81361527047577,0.961679556190125,
10.4799869066499));
#31156=CARTESIAN_POINT('Ctrl Pts',(-3.78524769068778,1.07417340590292,10.4741361150538));
#31157=CARTESIAN_POINT('Ctrl Pts',(-3.75189331040411,1.18543115889112,10.4682853234577));
#31158=CARTESIAN_POINT('Ctrl Pts',(-3.71369126282571,1.29498502092185,10.4624345318617));
#31159=CARTESIAN_POINT('Ctrl Pts',(-3.67548578894442,1.40454870872733,10.4565832155141));
#31160=CARTESIAN_POINT('Ctrl Pts',(-3.63243191959001,1.51240781139919,10.4507318991664));
#31161=CARTESIAN_POINT('Ctrl Pts',(-3.58471785281063,1.61811214560078,10.4448805828188));
#31162=CARTESIAN_POINT('Ctrl Pts',(-3.53698794976742,1.72385156299349,10.4390273244236));
#31163=CARTESIAN_POINT('Ctrl Pts',(-3.48459494375123,1.82743441325059,10.4331740660283));
#31164=CARTESIAN_POINT('Ctrl Pts',(-3.42777380377962,1.92843349642195,10.4273208076331));
#31165=CARTESIAN_POINT('Ctrl Pts',(-3.37088801860775,2.02954748587576,10.4214608900075));
#31166=CARTESIAN_POINT('Ctrl Pts',(-3.30956424684825,2.12807148047396,10.4156009723818));
#31167=CARTESIAN_POINT('Ctrl Pts',(-3.24408181575473,2.22360566933291,10.4097410547562));
#31168=CARTESIAN_POINT('Ctrl Pts',(-3.17855529342486,2.3192041841558,10.4038771914767));
#31169=CARTESIAN_POINT('Ctrl Pts',(-3.10886478410271,2.41180855519888,10.3980133281971));
#31170=CARTESIAN_POINT('Ctrl Pts',(-3.03532998044183,2.50105196064196,10.3921494649175));
#31171=CARTESIAN_POINT('Ctrl Pts',(-2.96168669515644,2.59042702169731,10.3862769510211));
#31172=CARTESIAN_POINT('Ctrl Pts',(-2.88418807245217,2.67643091546318,10.3804044371246));
#31173=CARTESIAN_POINT('Ctrl Pts',(-2.80319075601463,2.75873351112319,10.3745319232282));
#31174=CARTESIAN_POINT('Ctrl Pts',(-2.78080477818912,2.78148024104539,10.3729088822232));
#31175=CARTESIAN_POINT('Ctrl Pts',(-2.75815174411362,2.80394448378567,10.3712858412183));
#31176=CARTESIAN_POINT('Ctrl Pts',(-2.73523961024742,2.82611982664103,10.3696628002134));
#31177=CARTESIAN_POINT('Ctrl Pts',(-2.65234405084114,2.90634969356468,10.3637906761752));
#31178=CARTESIAN_POINT('Ctrl Pts',(-2.56577657936873,2.98306374184479,10.357918552137));
#31179=CARTESIAN_POINT('Ctrl Pts',(-2.47586775560022,3.05590704321632,10.3520464280989));
#31180=CARTESIAN_POINT('Ctrl Pts',(-2.38607550045775,3.1286559017601,10.3461819173894));
#31181=CARTESIAN_POINT('Ctrl Pts',(-2.29295082630594,3.19754373553336,10.34031740668));
#31182=CARTESIAN_POINT('Ctrl Pts',(-2.19686112162668,3.26225232198326,10.3344528959705));
#31183=CARTESIAN_POINT('Ctrl Pts',(-2.10087029235316,3.32689432390404,10.3285944197876));
#31184=CARTESIAN_POINT('Ctrl Pts',(-2.00192084195665,3.38736540268395,10.3227359436048));
#31185=CARTESIAN_POINT('Ctrl Pts',(-1.90041269945998,3.44338794964076,10.3168774674219));
#31186=CARTESIAN_POINT('Ctrl Pts',(-1.79490195806552,3.50161953893827,10.3107879838564));
#31187=CARTESIAN_POINT('Ctrl Pts',(-1.68662694166444,3.55504426961796,10.3046985002909));
#31188=CARTESIAN_POINT('Ctrl Pts',(-1.57606971675418,3.60340023421357,10.2986090167254));
#31189=CARTESIAN_POINT('Ctrl Pts',(-1.46982983599936,3.64986786142284,10.2927573321486));
#31190=CARTESIAN_POINT('Ctrl Pts',(-1.36148306030609,3.69165499076689,10.2869056475718));
#31191=CARTESIAN_POINT('Ctrl Pts',(-1.25148088769395,3.7285767509516,10.2810539629951));
#31192=CARTESIAN_POINT('Ctrl Pts',(-1.1414954928675,3.76549287974408,10.2752031709308));
#31193=CARTESIAN_POINT('Ctrl Pts',(-1.02985559495821,3.79754498334782,10.2693523788665));
#31194=CARTESIAN_POINT('Ctrl Pts',(-0.917029995956315,3.82459736266661,
10.2635015868022));
#31195=CARTESIAN_POINT('Ctrl Pts',(-0.804194277859957,3.8516521682573,10.2576502699924));
#31196=CARTESIAN_POINT('Ctrl Pts',(-0.690173049312679,3.87370626175716,
10.2517989531827));
#31197=CARTESIAN_POINT('Ctrl Pts',(-0.575446805842531,3.89067474529106,
10.245947636373));
#31198=CARTESIAN_POINT('Ctrl Pts',(-0.460682484949947,3.90764886063243,
10.2400943775223));
#31199=CARTESIAN_POINT('Ctrl Pts',(-0.345213092601965,3.9195339492648,10.2342411186716));
#31200=CARTESIAN_POINT('Ctrl Pts',(-0.229525057735885,3.92629688738273,
10.228387859821));
#31201=CARTESIAN_POINT('Ctrl Pts',(-0.113705405270288,3.93306751965574,
10.222527941752));
#31202=CARTESIAN_POINT('Ctrl Pts',(0.00233297325410128,3.93470434585651,
10.216668023683));
#31203=CARTESIAN_POINT('Ctrl Pts',(0.11810272632928,3.93122636667409,10.210808105614));
#31204=CARTESIAN_POINT('Ctrl Pts',(0.233950430432206,3.92774604567057,10.2049442418976));
#31205=CARTESIAN_POINT('Ctrl Pts',(0.349528737665922,3.91914409232972,10.1990803781811));
#31206=CARTESIAN_POINT('Ctrl Pts',(0.464356243540799,3.90549129804237,10.1932165144646));
#31207=CARTESIAN_POINT('Ctrl Pts',(0.579353147501274,3.89181836261203,10.1873440001441));
#31208=CARTESIAN_POINT('Ctrl Pts',(0.693596633081365,3.8730797816868,10.1814714858236));
#31209=CARTESIAN_POINT('Ctrl Pts',(0.806616202723852,3.84939726470305,10.1755989715031));
#31210=CARTESIAN_POINT('Ctrl Pts',(0.837852379002223,3.84285192678007,10.173975934952));
#31211=CARTESIAN_POINT('Ctrl Pts',(0.868995162505947,3.83592923731664,10.172352898401));
#31212=CARTESIAN_POINT('Ctrl Pts',(0.90003485814385,3.82863242609237,10.1707298618499));
#31213=CARTESIAN_POINT('Ctrl Pts',(1.01233607784,3.80223265690853,10.1648577364779));
#31214=CARTESIAN_POINT('Ctrl Pts',(1.12366304891352,3.77084342048896,10.158985611106));
#31215=CARTESIAN_POINT('Ctrl Pts',(1.23353850249376,3.73455107916138,10.153113485734));
#31216=CARTESIAN_POINT('Ctrl Pts',(1.34327150051455,3.69830579152614,10.1472489736813));
#31217=CARTESIAN_POINT('Ctrl Pts',(1.45155633457245,3.65717016914594,10.1413844616285));
#31218=CARTESIAN_POINT('Ctrl Pts',(1.55792672122676,3.61128139741112,10.1355199495758));
#31219=CARTESIAN_POINT('Ctrl Pts',(1.66418765391786,3.56543984471999,10.1296614720417));
#31220=CARTESIAN_POINT('Ctrl Pts',(1.76853768021067,3.51485503375725,10.1238029945077));
#31221=CARTESIAN_POINT('Ctrl Pts',(1.87052710768258,3.45971347649262,10.1179445169737));
#31222=CARTESIAN_POINT('Ctrl Pts',(1.97653807853306,3.40239763342211,10.1118550339117));
#31223=CARTESIAN_POINT('Ctrl Pts',(2.07999802714273,3.34015843987668,10.1057655508497));
#31224=CARTESIAN_POINT('Ctrl Pts',(2.18042609039876,3.27326000560731,10.0996760677878));
#31225=CARTESIAN_POINT('Ctrl Pts',(2.27693239144998,3.2089739860612,10.0938243818489));
#31226=CARTESIAN_POINT('Ctrl Pts',(2.37063878019018,3.14038603900235,10.08797269591));
#31227=CARTESIAN_POINT('Ctrl Pts',(2.46114573213632,3.06777617912181,10.0821210099711));
#31228=CARTESIAN_POINT('Ctrl Pts',(2.55163887978295,2.99517739384085,10.076270216543));
#31229=CARTESIAN_POINT('Ctrl Pts',(2.63893323852493,2.91855817405838,10.0704194231148));
#31230=CARTESIAN_POINT('Ctrl Pts',(2.72266130926682,2.83823966483126,10.0645686296867));
#31231=CARTESIAN_POINT('Ctrl Pts',(2.80639688940836,2.75791395200112,10.0587173115128));
#31232=CARTESIAN_POINT('Ctrl Pts',(2.88656524735549,2.673888576381,10.0528659933389));
#31233=CARTESIAN_POINT('Ctrl Pts',(2.96283531171061,2.58652197278134,10.0470146751651));
#31234=CARTESIAN_POINT('Ctrl Pts',(3.03913068993416,2.49912637239602,10.0411614149514));
#31235=CARTESIAN_POINT('Ctrl Pts',(3.1115249301235,2.40838765023391,10.0353081547378));
#31236=CARTESIAN_POINT('Ctrl Pts',(3.17972731964458,2.3146972097244,10.0294548945242));
#31237=CARTESIAN_POINT('Ctrl Pts',(3.24800730250562,2.22090017831311,10.0235949751009));
#31238=CARTESIAN_POINT('Ctrl Pts',(3.31208567237586,2.12414506021348,10.0177350556776));
#31239=CARTESIAN_POINT('Ctrl Pts',(3.37171507784118,2.02485220049723,10.0118751362543));
#31240=CARTESIAN_POINT('Ctrl Pts',(3.43138463341719,1.92549248418099,10.0060112711869));
#31241=CARTESIAN_POINT('Ctrl Pts',(3.48659906327221,1.8235919864264,10.0001474061195));
#31242=CARTESIAN_POINT('Ctrl Pts',(3.53715780830981,1.71959403322788,9.99428354105211));
#31243=CARTESIAN_POINT('Ctrl Pts',(3.58779113946049,1.61544265843847,9.98841102539611));
#31244=CARTESIAN_POINT('Ctrl Pts',(3.63375491454719,1.50918803068272,9.98253850974011));
#31245=CARTESIAN_POINT('Ctrl Pts',(3.67489731258031,1.40129181186146,9.97666599408411));
#31246=CARTESIAN_POINT('Ctrl Pts',(3.68626809200505,1.37147186544046,9.97504297055158));
#31247=CARTESIAN_POINT('Ctrl Pts',(3.69727089338434,1.34152660458722,9.97341994701905));
#31248=CARTESIAN_POINT('Ctrl Pts',(3.70790319572806,1.31146593211934,9.97179692348651));
#31249=CARTESIAN_POINT('Ctrl Pts',(3.75282647998858,1.18445448241816,9.9649393732442));
#31250=CARTESIAN_POINT('Ctrl Pts',(3.79125534051289,1.05503264886109,9.95808182300188));
#31251=CARTESIAN_POINT('Ctrl Pts',(3.82296277587289,0.923820661324593,9.95122427275956));
#31252=CARTESIAN_POINT('Ctrl Pts',(3.85452351214834,0.793215745228449,9.94439844997585));
#31253=CARTESIAN_POINT('Ctrl Pts',(3.87942477998307,0.660837308486352,9.93757262719214));
#31254=CARTESIAN_POINT('Ctrl Pts',(3.89748945725625,0.527318623392355,9.93074680440843));
#31255=CARTESIAN_POINT('Ctrl Pts',(3.91540359399889,0.39491260548778,9.92397786406815));
#31256=CARTESIAN_POINT('Ctrl Pts',(3.92659452399959,0.26138538800618,9.91720892372788));
#31257=CARTESIAN_POINT('Ctrl Pts',(3.93093689015499,0.127374116753154,9.9104399833876));
#31258=CARTESIAN_POINT('Ctrl Pts',(3.93227903490181,0.0859537212152617,
9.9083478296184));
#31259=CARTESIAN_POINT('Ctrl Pts',(3.93296727603341,0.0444872179918603,
9.90625567584921));
#31260=CARTESIAN_POINT('Ctrl Pts',(3.9329988605794,0.00299377372985386,
9.90416352208001));
#31261=CARTESIAN_POINT('',(3.93127184741014,-0.00247874324238124,8.65416299050568));
#31262=CARTESIAN_POINT('Ctrl Pts',(3.93299886058008,0.00299377283657058,
9.90416352203497));
#31263=CARTESIAN_POINT('Ctrl Pts',(3.93308723740947,-0.113109214353025,
9.89830945745726));
#31264=CARTESIAN_POINT('Ctrl Pts',(3.9280302285454,-0.229267072370521,9.89245539287955));
#31265=CARTESIAN_POINT('Ctrl Pts',(3.91783999345601,-0.344990993616612,
9.88660132830185));
#31266=CARTESIAN_POINT('Ctrl Pts',(3.90765103618284,-0.460700403528975,
9.88074799780128));
#31267=CARTESIAN_POINT('Ctrl Pts',(3.89233016843786,-0.575975574245469,
9.8748946673007));
#31268=CARTESIAN_POINT('Ctrl Pts',(3.87194153497946,-0.690331622990648,
9.86904133680013));
#31269=CARTESIAN_POINT('Ctrl Pts',(3.85155055435826,-0.80470083653492,9.86318733245746));
#31270=CARTESIAN_POINT('Ctrl Pts',(3.82609072010459,-0.91815031176996,9.85733332811479));
#31271=CARTESIAN_POINT('Ctrl Pts',(3.79567740077867,-1.03020486759578,9.85147932377211));
#31272=CARTESIAN_POINT('Ctrl Pts',(3.76525326530779,-1.14229927432729,9.84562323752056));
#31273=CARTESIAN_POINT('Ctrl Pts',(3.72987224910885,-1.25299737736529,9.83976715126901));
#31274=CARTESIAN_POINT('Ctrl Pts',(3.68969952561667,-1.36183934833156,9.83391106501746));
#31275=CARTESIAN_POINT('Ctrl Pts',(3.64947794537558,-1.4708136893336,9.82804785678585));
#31276=CARTESIAN_POINT('Ctrl Pts',(3.60445316681952,-1.57792700461605,9.82218464855424));
#31277=CARTESIAN_POINT('Ctrl Pts',(3.55483852128138,-1.68273945921941,9.81632144032263));
#31278=CARTESIAN_POINT('Ctrl Pts',(3.50518969067181,-1.78762413083063,9.81045419227193));
#31279=CARTESIAN_POINT('Ctrl Pts',(3.45094488790614,-1.89020442123878,9.80458694422123));
#31280=CARTESIAN_POINT('Ctrl Pts',(3.39236251616816,-1.99006672222245,9.79871969617053));
#31281=CARTESIAN_POINT('Ctrl Pts',(3.33368586926898,-2.09008972913596,9.79284300610273));
#31282=CARTESIAN_POINT('Ctrl Pts',(3.27065794049003,-2.18738566878382,9.78696631603493));
#31283=CARTESIAN_POINT('Ctrl Pts',(3.20357953500277,-2.28157120487427,9.78108962596713));
#31284=CARTESIAN_POINT('Ctrl Pts',(3.17228284329568,-2.3255152382018,9.77834774568578));
#31285=CARTESIAN_POINT('Ctrl Pts',(3.14010497705328,-2.36878266652459,9.77560586540443));
#31286=CARTESIAN_POINT('Ctrl Pts',(3.1070792877133,-2.41133724307966,9.77286398512307));
#31287=CARTESIAN_POINT('Ctrl Pts',(3.03635009140188,-2.50247390242771,9.76699185973954));
#31288=CARTESIAN_POINT('Ctrl Pts',(2.96148909624755,-2.59064877599629,9.761119734356));
#31289=CARTESIAN_POINT('Ctrl Pts',(2.88277340207827,-2.67546379386268,9.75524760897246));
#31290=CARTESIAN_POINT('Ctrl Pts',(2.80415976464377,-2.76016884707875,9.74938309693654));
#31291=CARTESIAN_POINT('Ctrl Pts',(2.72170164544951,-2.84152240713908,9.74351858490063));
#31292=CARTESIAN_POINT('Ctrl Pts',(2.63571778942591,-2.91915753848671,9.73765407286471));
#31293=CARTESIAN_POINT('Ctrl Pts',(2.54982241025973,-2.99671278376311,9.7317955953755));
#31294=CARTESIAN_POINT('Ctrl Pts',(2.46040881544806,-3.07055693551838,9.72593711788628));
#31295=CARTESIAN_POINT('Ctrl Pts',(2.3678337020125,-3.14035866735215,9.72007864039707));
#31296=CARTESIAN_POINT('Ctrl Pts',(2.27160826001953,-3.21291275071554,9.71398915732885));
#31297=CARTESIAN_POINT('Ctrl Pts',(2.17196715603456,-3.28109872888663,9.70789967426062));
#31298=CARTESIAN_POINT('Ctrl Pts',(2.06935061857032,-3.34458921504908,9.70181019119239));
#31299=CARTESIAN_POINT('Ctrl Pts',(1.97074130625292,-3.40560036718778,9.69595850536704));
#31300=CARTESIAN_POINT('Ctrl Pts',(1.86938496856155,-3.46227563004297,9.69010681954169));
#31301=CARTESIAN_POINT('Ctrl Pts',(1.76570245622905,-3.51436819870467,9.68425513371633));
#31302=CARTESIAN_POINT('Ctrl Pts',(1.66203575820139,-3.56645282188219,9.67840434042668));
#31303=CARTESIAN_POINT('Ctrl Pts',(1.55604396029811,-3.61395595511132,9.67255354713702));
#31304=CARTESIAN_POINT('Ctrl Pts',(1.4481719907339,-3.65667702774716,9.66670275384737));
#31305=CARTESIAN_POINT('Ctrl Pts',(1.34029034680878,-3.69940193176827,9.66085143583673));
#31306=CARTESIAN_POINT('Ctrl Pts',(1.23052858041005,-3.73734377040407,9.65500011782609));
#31307=CARTESIAN_POINT('Ctrl Pts',(1.11935037322815,-3.77035061260276,9.64914879981545));
#31308=CARTESIAN_POINT('Ctrl Pts',(1.00813526670446,-3.80336840956302,9.64329553978948));
#31309=CARTESIAN_POINT('Ctrl Pts',(0.895503180725383,-3.8314478356438,9.63744227976351));
#31310=CARTESIAN_POINT('Ctrl Pts',(0.781930985552084,-3.85448737627114,
9.63158901973754));
#31311=CARTESIAN_POINT('Ctrl Pts',(0.66822958083112,-3.87755312867169,9.62572910053695));
#31312=CARTESIAN_POINT('Ctrl Pts',(0.553586337524964,-3.89556746884632,
9.61986918133634));
#31313=CARTESIAN_POINT('Ctrl Pts',(0.43848640339453,-3.90848035354383,9.61400926213575));
#31314=CARTESIAN_POINT('Ctrl Pts',(0.323308969729893,-3.92140193279497,
9.60814539731162));
#31315=CARTESIAN_POINT('Ctrl Pts',(0.207674644412055,-3.92921518914535,
9.60228153248749));
#31316=CARTESIAN_POINT('Ctrl Pts',(0.0920700048664749,-3.93192219076165,
9.59641766766336));
#31317=CARTESIAN_POINT('Ctrl Pts',(-0.0237051783309354,-3.93463318583308,
9.5905451522788));
#31318=CARTESIAN_POINT('Ctrl Pts',(-0.139450176577184,-3.93222290045582,
9.58467263689424));
#31319=CARTESIAN_POINT('Ctrl Pts',(-0.254682016237665,-3.92474535105211,
9.57880012150967));
#31320=CARTESIAN_POINT('Ctrl Pts',(-0.286529382266794,-3.92267873254143,
9.57717709659299));
#31321=CARTESIAN_POINT('Ctrl Pts',(-0.31833760521875,-3.92022535841899,
9.57555407167632));
#31322=CARTESIAN_POINT('Ctrl Pts',(-0.350096631160233,-3.91738705629789,
9.57393104675964));
#31323=CARTESIAN_POINT('Ctrl Pts',(-0.465001345995669,-3.90711802926783,
9.56805891404481));
#31324=CARTESIAN_POINT('Ctrl Pts',(-0.579646493589882,-3.89177192615486,
9.56218678132999));
#31325=CARTESIAN_POINT('Ctrl Pts',(-0.693547389923439,-3.87136681521273,
9.55631464861516));
#31326=CARTESIAN_POINT('Ctrl Pts',(-0.807300612601107,-3.85098815970185,
9.55045012917937));
#31327=CARTESIAN_POINT('Ctrl Pts',(-0.920311099740817,-3.82556361216972,
9.54458560974357));
#31328=CARTESIAN_POINT('Ctrl Pts',(-1.03209786236774,-3.79516310617817,
9.53872109030778));
#31329=CARTESIAN_POINT('Ctrl Pts',(-1.14376959837936,-3.76479388177333,
9.53286260535948));
#31330=CARTESIAN_POINT('Ctrl Pts',(-1.25421971794834,-3.72945899101311,
9.52700412041119));
#31331=CARTESIAN_POINT('Ctrl Pts',(-1.36297668791349,-3.68927954324477,
9.52114563546289));
#31332=CARTESIAN_POINT('Ctrl Pts',(-1.4760218576683,-3.64751585219047,9.51505615516844));
#31333=CARTESIAN_POINT('Ctrl Pts',(-1.58723716410742,-3.60051779123602,
9.508966674874));
#31334=CARTESIAN_POINT('Ctrl Pts',(-1.6961092556027,-3.54847888440369,9.50287719457955));
#31335=CARTESIAN_POINT('Ctrl Pts',(-1.80073002235906,-3.49847203453807,
9.49702550119511));
#31336=CARTESIAN_POINT('Ctrl Pts',(-1.90318673160227,-3.44381082464488,
9.49117380781068));
#31337=CARTESIAN_POINT('Ctrl Pts',(-2.00304430489268,-3.38471601654216,
9.48532211442625));
#31338=CARTESIAN_POINT('Ctrl Pts',(-2.10288664770936,-3.32563022169594,
9.47947131355361));
#31339=CARTESIAN_POINT('Ctrl Pts',(-2.20013028710999,-3.26211238366864,
9.47362051268097));
#31340=CARTESIAN_POINT('Ctrl Pts',(-2.29436603792941,-3.19442850663403,
9.46776971180833));
#31341=CARTESIAN_POINT('Ctrl Pts',(-2.38861024040586,-3.12673855928205,
9.46191838619893));
#31342=CARTESIAN_POINT('Ctrl Pts',(-2.4798456822328,-3.05488207135051,9.45606706058954));
#31343=CARTESIAN_POINT('Ctrl Pts',(-2.56769397226143,-2.97916710924585,
9.45021573498014));
#31344=CARTESIAN_POINT('Ctrl Pts',(-2.65557141865656,-2.90342701775981,
9.44436246734782));
#31345=CARTESIAN_POINT('Ctrl Pts',(-2.74005916491526,-2.82382617545463,
9.43850919971549));
#31346=CARTESIAN_POINT('Ctrl Pts',(-2.82081411601947,-2.74071098856945,
9.43265593208316));
#31347=CARTESIAN_POINT('Ctrl Pts',(-2.90166094043903,-2.65750124317521,
9.42679600530368));
#31348=CARTESIAN_POINT('Ctrl Pts',(-2.97876620509092,-2.57076946958095,
9.42093607852419));
#31349=CARTESIAN_POINT('Ctrl Pts',(-3.05182565235624,-2.48089685146731,
9.41507615174471));
#31350=CARTESIAN_POINT('Ctrl Pts',(-3.12493429214566,-2.39096372015383,
9.40921227934833));
#31351=CARTESIAN_POINT('Ctrl Pts',(-3.1939914445301,-2.29788586454191,9.40334840695194));
#31352=CARTESIAN_POINT('Ctrl Pts',(-3.25873592809101,-2.20207382959082,
9.39748453455556));
#31353=CARTESIAN_POINT('Ctrl Pts',(-3.32357592389546,-2.1061204509775,9.39161201166763));
#31354=CARTESIAN_POINT('Ctrl Pts',(-3.38409033796464,-2.00742519400292,
9.38573948877969));
#31355=CARTESIAN_POINT('Ctrl Pts',(-3.44006364760443,-1.9064236413847,9.37986696589175));
#31356=CARTESIAN_POINT('Ctrl Pts',(-3.45553264184485,-1.8785104726659,9.37824401339324));
#31357=CARTESIAN_POINT('Ctrl Pts',(-3.47065508372829,-1.85042127389786,
9.37662106089472));
#31358=CARTESIAN_POINT('Ctrl Pts',(-3.48542707898021,-1.82216549114274,
9.3749981083962));
#31359=CARTESIAN_POINT('Ctrl Pts',(-3.53887451052616,-1.71993156885758,
9.36912600777014));
#31360=CARTESIAN_POINT('Ctrl Pts',(-3.58790967536027,-1.61517268576546,
9.36325390714409));
#31361=CARTESIAN_POINT('Ctrl Pts',(-3.63228587862215,-1.50830643304407,
9.35738180651803));
#31362=CARTESIAN_POINT('Ctrl Pts',(-3.67660454692182,-1.40157873534451,
9.35151731923116));
#31363=CARTESIAN_POINT('Ctrl Pts',(-3.71627610887297,-1.29274947977079,
9.3456528319443));
#31364=CARTESIAN_POINT('Ctrl Pts',(-3.75109950768657,-1.18226117395166,
9.33978834465744));
#31365=CARTESIAN_POINT('Ctrl Pts',(-3.78588707350342,-1.07188655970882,
9.33392989188073));
#31366=CARTESIAN_POINT('Ctrl Pts',(-3.81583627545891,-0.959856682742663,
9.32807143910402));
#31367=CARTESIAN_POINT('Ctrl Pts',(-3.8407942275231,-0.846633747157065,
9.32221298632732));
#31368=CARTESIAN_POINT('Ctrl Pts',(-3.86673644534915,-0.728945643168742,
9.31612349398171));
#31369=CARTESIAN_POINT('Ctrl Pts',(-3.8872854590377,-0.609968863406854,
9.31003400163611));
#31370=CARTESIAN_POINT('Ctrl Pts',(-3.90232671628392,-0.490239940617599,
9.30394450929051));
#31371=CARTESIAN_POINT('Ctrl Pts',(-3.9167805227377,-0.375187146254242,
9.29809284793505));
#31372=CARTESIAN_POINT('Ctrl Pts',(-3.92614866336008,-0.25944030638907,
9.29224118657959));
#31373=CARTESIAN_POINT('Ctrl Pts',(-3.93038180241211,-0.143484798037018,
9.28638952522413));
#31374=CARTESIAN_POINT('Ctrl Pts',(-3.9346142958907,-0.0275469734405368,
9.28053875627431));
#31375=CARTESIAN_POINT('Ctrl Pts',(-3.93371332979162,0.0885990433418262,
9.2746879873245));
#31376=CARTESIAN_POINT('Ctrl Pts',(-3.92768162855818,0.204465216324347,
9.26883721837467));
#31377=CARTESIAN_POINT('Ctrl Pts',(-3.92164938621706,0.320341783733489,
9.26298592454872));
#31378=CARTESIAN_POINT('Ctrl Pts',(-3.91048551523794,0.435938044554662,
9.25713463072277));
#31379=CARTESIAN_POINT('Ctrl Pts',(-3.89424477246337,0.550769145960201,
9.25128333689682));
#31380=CARTESIAN_POINT('Ctrl Pts',(-3.87799863896647,0.665638362776525,
9.2454301008752));
#31381=CARTESIAN_POINT('Ctrl Pts',(-3.85667234073705,0.779741506036119,
9.23957686485357));
#31382=CARTESIAN_POINT('Ctrl Pts',(-3.83037196752621,0.892602705793224,
9.23372362883195));
#31383=CARTESIAN_POINT('Ctrl Pts',(-3.8040416708739,1.00559231420364,9.22786373324835));
#31384=CARTESIAN_POINT('Ctrl Pts',(-3.7727260973294,1.11733675587199,9.22200383766475));
#31385=CARTESIAN_POINT('Ctrl Pts',(-3.73658158551186,1.2273740484521,9.21614394208114));
#31386=CARTESIAN_POINT('Ctrl Pts',(-3.70041273542503,1.33748543574599,9.21028010067812));
#31387=CARTESIAN_POINT('Ctrl Pts',(-3.65940861837551,1.44588699928753,9.2044162592751));
#31388=CARTESIAN_POINT('Ctrl Pts',(-3.61377355483072,1.55213713775754,9.19855241787208));
#31389=CARTESIAN_POINT('Ctrl Pts',(-3.5680711650671,1.65854402894175,9.1926799254398));
#31390=CARTESIAN_POINT('Ctrl Pts',(-3.51772437228785,1.76279278938837,9.18680743300753));
#31391=CARTESIAN_POINT('Ctrl Pts',(-3.46298323625927,1.86446670803939,9.18093494057526));
#31392=CARTESIAN_POINT('Ctrl Pts',(-3.44785185466565,1.8925711094611,9.17931168372776));
#31393=CARTESIAN_POINT('Ctrl Pts',(-3.43238496946287,1.92047895135816,9.17768842688026));
#31394=CARTESIAN_POINT('Ctrl Pts',(-3.41658842808763,1.94818184804646,9.17606517003276));
#31395=CARTESIAN_POINT('Ctrl Pts',(-3.35944435675326,2.04839722221729,9.17019302986713));
#31396=CARTESIAN_POINT('Ctrl Pts',(-3.29779147050594,2.1462642476224,9.1643208897015));
#31397=CARTESIAN_POINT('Ctrl Pts',(-3.23184785157092,2.24134969701214,9.15844874953588));
#31398=CARTESIAN_POINT('Ctrl Pts',(-3.1659897311995,2.33631186427887,9.15258422283698));
#31399=CARTESIAN_POINT('Ctrl Pts',(-3.09585217456309,2.4284992908329,9.14671969613809));
#31400=CARTESIAN_POINT('Ctrl Pts',(-3.02169888992021,2.51750368791289,9.1408551694392));
#31401=CARTESIAN_POINT('Ctrl Pts',(-2.94762191005517,2.60641649821045,9.13499667742116));
#31402=CARTESIAN_POINT('Ctrl Pts',(-2.86953768443757,2.69215247821757,9.12913818540312));
#31403=CARTESIAN_POINT('Ctrl Pts',(-2.78775252360083,2.77433322929261,9.12327969338508));
#31404=CARTESIAN_POINT('Ctrl Pts',(-2.70274278029786,2.85975415995852,9.11719021581359));
#31405=CARTESIAN_POINT('Ctrl Pts',(-2.61373452063478,2.94133337332348,9.11110073824211));
#31406=CARTESIAN_POINT('Ctrl Pts',(-2.52111730152547,3.01868457311275,9.10501126067062));
#31407=CARTESIAN_POINT('Ctrl Pts',(-2.43211653445608,3.09301541764889,9.09915956073699));
#31408=CARTESIAN_POINT('Ctrl Pts',(-2.33978370694337,3.16344194809958,9.09330786080336));
#31409=CARTESIAN_POINT('Ctrl Pts',(-2.24450058085828,3.22966037572479,9.08745616086973));
#31410=CARTESIAN_POINT('Ctrl Pts',(-2.14923199081137,3.29586870131379,9.08160535364962));
#31411=CARTESIAN_POINT('Ctrl Pts',(-2.05101433649171,3.35786996465837,9.07575454642951));
#31412=CARTESIAN_POINT('Ctrl Pts',(-1.95025974780192,3.41540274581251,9.06990373920939));
#31413=CARTESIAN_POINT('Ctrl Pts',(-1.84949612638668,3.47294068482419,9.06405240745996));
#31414=CARTESIAN_POINT('Ctrl Pts',(-1.74619547750079,3.52600914027372,9.05820107571052));
#31415=CARTESIAN_POINT('Ctrl Pts',(-1.64079536833043,3.5743921943829,9.05234974396108));
#31416=CARTESIAN_POINT('Ctrl Pts',(-1.53536028131871,3.62279130478276,9.04649647040196));
#31417=CARTESIAN_POINT('Ctrl Pts',(-1.42782472415334,3.66650174967328,9.04064319684283));
#31418=CARTESIAN_POINT('Ctrl Pts',(-1.31864644328848,3.70535565871923,9.0347899232837));
#31419=CARTESIAN_POINT('Ctrl Pts',(-1.20934395898276,3.74425376876521,9.0289299909211));
#31420=CARTESIAN_POINT('Ctrl Pts',(-1.09839541062445,3.77828417673352,9.0230700585585));
#31421=CARTESIAN_POINT('Ctrl Pts',(-0.986274011150539,3.80732879784883,
9.0172101261959));
#31422=CARTESIAN_POINT('Ctrl Pts',(-0.874077121646961,3.83639297436856,
9.01134624840923));
#31423=CARTESIAN_POINT('Ctrl Pts',(-0.76070621205463,3.86046459419032,9.00548237062256));
#31424=CARTESIAN_POINT('Ctrl Pts',(-0.646643273153777,3.87947695924141,
8.99961849283589));
#31425=CARTESIAN_POINT('Ctrl Pts',(-0.532412072966534,3.8985173706065,8.9937459648809));
#31426=CARTESIAN_POINT('Ctrl Pts',(-0.417487214888083,3.91248358231421,
8.98787343692592));
#31427=CARTESIAN_POINT('Ctrl Pts',(-0.302354461510855,3.92136083261978,
8.98200090897094));
#31428=CARTESIAN_POINT('Ctrl Pts',(-0.270537146075454,3.92381408996737,
8.98037801653707));
#31429=CARTESIAN_POINT('Ctrl Pts',(-0.238703942649404,3.92587900404544,
8.9787551241032));
#31430=CARTESIAN_POINT('Ctrl Pts',(-0.206865060006896,3.9275559635667,8.97713223166932));
#31431=CARTESIAN_POINT('Ctrl Pts',(-0.0916611652256139,3.93362377286796,
8.97126005545973));
#31432=CARTESIAN_POINT('Ctrl Pts',(0.0240030410320682,3.93462867854233,
8.96538787925015));
#31433=CARTESIAN_POINT('Ctrl Pts',(0.139645176672874,3.93052009594557,8.95951570304056));
#31434=CARTESIAN_POINT('Ctrl Pts',(0.255137388099245,3.92641683991958,8.95365113981217));
#31435=CARTESIAN_POINT('Ctrl Pts',(0.370607176484888,3.91721329360362,8.94778657658379));
#31436=CARTESIAN_POINT('Ctrl Pts',(0.485568490821238,3.90291073952782,8.94192201335541));
#31437=CARTESIAN_POINT('Ctrl Pts',(0.600411517643439,3.88862290182489,8.93606348437089));
#31438=CARTESIAN_POINT('Ctrl Pts',(0.714746703286442,3.86924654271268,8.93020495538637));
#31439=CARTESIAN_POINT('Ctrl Pts',(0.82809012813836,3.84483494309961,8.92434642640185));
#31440=CARTESIAN_POINT('Ctrl Pts',(0.945901389870079,3.81946107289001,8.91825696252286));
#31441=CARTESIAN_POINT('Ctrl Pts',(1.06264064041209,3.78864685009729,8.91216749864386));
#31442=CARTESIAN_POINT('Ctrl Pts',(1.17777234658628,3.75251133237685,8.90607803476486));
#31443=CARTESIAN_POINT('Ctrl Pts',(1.28840943461754,3.71778650645406,8.90022629701483));
#31444=CARTESIAN_POINT('Ctrl Pts',(1.39756170571898,3.67814820215032,8.89437455926481));
#31445=CARTESIAN_POINT('Ctrl Pts',(1.50476725107607,3.63375350293453,8.88852282151479));
#31446=CARTESIAN_POINT('Ctrl Pts',(1.61195644619781,3.58936557448585,8.88267197623063));
#31447=CARTESIAN_POINT('Ctrl Pts',(1.71719912406298,3.54022285159701,8.87682113094647));
#31448=CARTESIAN_POINT('Ctrl Pts',(1.8200526177605,3.48653086442428,8.87097028566231));
#31449=CARTESIAN_POINT('Ctrl Pts',(1.92291533591624,3.43283406186343,8.86511891564266));
#31450=CARTESIAN_POINT('Ctrl Pts',(2.02338807744833,3.37458737526685,8.85926754562302));
#31451=CARTESIAN_POINT('Ctrl Pts',(2.12105271812888,3.31204232565317,8.85341617560337));
#31452=CARTESIAN_POINT('Ctrl Pts',(2.21874977211252,3.24947651835652,8.84756286360935));
#31453=CARTESIAN_POINT('Ctrl Pts',(2.31363652414597,3.18260973425628,8.84170955161533));
#31454=CARTESIAN_POINT('Ctrl Pts',(2.40532437545746,3.11173643627319,8.8358562396213));
#31455=CARTESIAN_POINT('Ctrl Pts',(2.49711653278522,3.04078251134479,8.8299962687772));
#31456=CARTESIAN_POINT('Ctrl Pts',(2.58570219849534,2.96581322807541,8.82413629793309));
#31457=CARTESIAN_POINT('Ctrl Pts',(2.67072630827555,2.88716296496836,8.81827632708898));
#31458=CARTESIAN_POINT('Ctrl Pts',(2.75580766450286,2.80845974690372,8.81241241074622));
#31459=CARTESIAN_POINT('Ctrl Pts',(2.83732239989423,2.72607090719513,8.80654849440346));
#31460=CARTESIAN_POINT('Ctrl Pts',(2.91495394598017,2.64036597705974,8.8006845780607));
#31461=CARTESIAN_POINT('Ctrl Pts',(2.99270000784788,2.55453462193901,8.79481201174253));
#31462=CARTESIAN_POINT('Ctrl Pts',(3.06655118532422,2.46537773078405,8.78893944542437));
#31463=CARTESIAN_POINT('Ctrl Pts',(3.13623257323649,2.37329607225276,8.7830668791062));
#31464=CARTESIAN_POINT('Ctrl Pts',(3.15548481129688,2.34785487390477,8.78144435050609));
#31465=CARTESIAN_POINT('Ctrl Pts',(3.1744190083362,2.32219056727557,8.77982182190599));
#31466=CARTESIAN_POINT('Ctrl Pts',(3.19302997863455,2.29631194647876,8.77819929330588));
#31467=CARTESIAN_POINT('Ctrl Pts',(3.26096126127469,2.20185325488431,8.77227695571904));
#31468=CARTESIAN_POINT('Ctrl Pts',(3.32480947415829,2.10422199904811,8.76635461813219));
#31469=CARTESIAN_POINT('Ctrl Pts',(3.38426712749915,2.00380263741933,8.76043228054534));
#31470=CARTESIAN_POINT('Ctrl Pts',(3.44364508310638,1.90351787907683,8.75451788132904));
#31471=CARTESIAN_POINT('Ctrl Pts',(3.49864397968998,1.8004527916056,8.74860348211273));
#31472=CARTESIAN_POINT('Ctrl Pts',(3.54899787998221,1.69502302281762,8.74268908289643));
#31473=CARTESIAN_POINT('Ctrl Pts',(3.59929577739263,1.5897105114982,8.73678126158964));
#31474=CARTESIAN_POINT('Ctrl Pts',(3.64495878208342,1.48203891261819,8.73087344028286));
#31475=CARTESIAN_POINT('Ctrl Pts',(3.68576573473105,1.37245034470559,8.72496561897608));
#31476=CARTESIAN_POINT('Ctrl Pts',(3.72653238350795,1.26297001431596,8.71906363265698));
#31477=CARTESIAN_POINT('Ctrl Pts',(3.76245238819303,1.15157686122514,8.71316164633788));
#31478=CARTESIAN_POINT('Ctrl Pts',(3.79335209321593,1.03873427636443,8.70725966001879));
#31479=CARTESIAN_POINT('Ctrl Pts',(3.82423340147542,0.92595887461549,8.70136118756644));
#31480=CARTESIAN_POINT('Ctrl Pts',(3.85010025013148,0.811736146639425,8.69546271511409));
#31481=CARTESIAN_POINT('Ctrl Pts',(3.87082848282112,0.696545660083203,8.68956424266174));
#31482=CARTESIAN_POINT('Ctrl Pts',(3.89156250563976,0.581322996747287,8.68366412255728));
#31483=CARTESIAN_POINT('Ctrl Pts',(3.9071549464799,0.465132427676677,8.67776400245282));
#31484=CARTESIAN_POINT('Ctrl Pts',(3.91753252051055,0.348465135619414,8.67186388234835));
#31485=CARTESIAN_POINT('Ctrl Pts',(3.9279100945412,0.231797843562152,8.66596376224389));
#31486=CARTESIAN_POINT('Ctrl Pts',(3.93307275953401,0.114654231718768,8.66006364213943));
#31487=CARTESIAN_POINT('Ctrl Pts',(3.93299922484218,-0.00246928954045427,
8.65416352203497));
#31488=CARTESIAN_POINT('Ctrl Pts',(3.92808040047205,-0.00249620959774103,
8.65416200846926));
#31489=CARTESIAN_POINT('Ctrl Pts',(3.93089496884793,-0.497463850130089,
8.62919679062698));
#31490=CARTESIAN_POINT('Ctrl Pts',(3.61407832683064,-2.30365100072786,8.53792059333025));
#31491=CARTESIAN_POINT('Ctrl Pts',(0.898627897229635,-4.56470309825019,
8.38033341657901));
#31492=CARTESIAN_POINT('Ctrl Pts',(-3.35540415369693,-3.22274549575858,
8.18140047821557));
#31493=CARTESIAN_POINT('Ctrl Pts',(-4.52475415810096,1.08211876658719,7.98246753985213));
#31494=CARTESIAN_POINT('Ctrl Pts',(-1.53456114674909,4.39176043556087,7.78353460148871));
#31495=CARTESIAN_POINT('Ctrl Pts',(2.73011925450327,3.68738255941635,7.5907671869393));
#31496=CARTESIAN_POINT('Ctrl Pts',(3.93032929473929,1.18226324547227,7.46431075184439));
#31497=CARTESIAN_POINT('Ctrl Pts',(3.93806266851679,-0.00234938565519546,
7.40416529620395));
#31498=CARTESIAN_POINT('Origin',(0.,0.,4.68922655072688));
#31499=CARTESIAN_POINT('',(-1.83231942908391,2.65117390457541,42.));
#31500=CARTESIAN_POINT('Ctrl Pts',(-1.83231942908391,2.65117390457541,42.));
#31501=CARTESIAN_POINT('Ctrl Pts',(-1.59286454902597,2.81666958494625,41.9809759492185));
#31502=CARTESIAN_POINT('Ctrl Pts',(-1.33201263913347,2.94901901405471,41.9607686073061));
#31503=CARTESIAN_POINT('Ctrl Pts',(-0.94038760612917,3.08496026826113,41.9333795023616));
#31504=CARTESIAN_POINT('Ctrl Pts',(-0.821717533680347,3.11866883638072,
41.9254078541967));
#31505=CARTESIAN_POINT('Ctrl Pts',(-0.671731090466772,3.15211335156219,
41.9157406907206));
#31506=CARTESIAN_POINT('Ctrl Pts',(-0.641974702652182,3.15830806302118,
41.9138420609115));
#31507=CARTESIAN_POINT('Ctrl Pts',(-0.598694209464382,3.16668126009764,
41.9111075101178));
#31508=CARTESIAN_POINT('Ctrl Pts',(-0.585237524082561,3.16919579847215,
41.9102610503663));
#31509=CARTESIAN_POINT('Ctrl Pts',(-0.561656668655719,3.17344684048019,
41.9087842018925));
#31510=CARTESIAN_POINT('Ctrl Pts',(-0.551539533996479,3.17522081264738,
41.9081526455468));
#31511=CARTESIAN_POINT('Ctrl Pts',(-0.531905083053156,3.17856690831476,
41.9069309206604));
#31512=CARTESIAN_POINT('Ctrl Pts',(-0.522388860922958,3.180144727703,41.9063405801605));
#31513=CARTESIAN_POINT('Ctrl Pts',(-0.49966244361569,3.18380807496898,41.9049349411649));
#31514=CARTESIAN_POINT('Ctrl Pts',(-0.486446001051586,3.18585415738281,
41.9041208777451));
#31515=CARTESIAN_POINT('Ctrl Pts',(-0.438906241083337,3.1929112181866,41.9012044743489));
#31516=CARTESIAN_POINT('Ctrl Pts',(-0.404514505945473,3.19745037307116,
41.8991167496231));
#31517=CARTESIAN_POINT('Ctrl Pts',(-0.112663242478015,3.23118559459845,
41.8815703265869));
#31518=CARTESIAN_POINT('Ctrl Pts',(0.147375533090322,3.22979078434417,41.8671569875167));
#31519=CARTESIAN_POINT('Ctrl Pts',(0.490901260419218,3.18633410705426,41.8476740325027));
#31520=CARTESIAN_POINT('Ctrl Pts',(0.576859467941198,3.17189865197372,41.8427508154163));
#31521=CARTESIAN_POINT('Ctrl Pts',(0.755107119359493,3.13447887242855,41.8322621000324));
#31522=CARTESIAN_POINT('Ctrl Pts',(0.847173105909439,3.11085819303723,41.8266838854335));
#31523=CARTESIAN_POINT('Ctrl Pts',(0.951039404733918,3.07925736302113,41.8200673721665));
#31524=CARTESIAN_POINT('Ctrl Pts',(0.964001760132938,3.07522396727318,41.8192357783498));
#31525=CARTESIAN_POINT('Ctrl Pts',(0.982384632964249,3.06937626616702,41.8180475754683));
#31526=CARTESIAN_POINT('Ctrl Pts',(0.98782661221302,3.06762918447521,41.8176947181694));
#31527=CARTESIAN_POINT('Ctrl Pts',(0.99866925401454,3.06411644173785,41.8169894190578));
#31528=CARTESIAN_POINT('Ctrl Pts',(1.00406995132958,3.06235095622799,41.8166369882612));
#31529=CARTESIAN_POINT('Ctrl Pts',(1.01527337855022,3.05865573825014,41.8159035035219));
#31530=CARTESIAN_POINT('Ctrl Pts',(1.02107530356226,3.05672376584055,41.8155223159985));
#31531=CARTESIAN_POINT('Ctrl Pts',(1.03623404439014,3.05162811097689,41.8145229451406));
#31532=CARTESIAN_POINT('Ctrl Pts',(1.04558181125822,3.04843792662141,41.8139032416118));
#31533=CARTESIAN_POINT('Ctrl Pts',(1.08473045582555,3.03487612066088,41.811293922843));
#31534=CARTESIAN_POINT('Ctrl Pts',(1.11439169949277,3.02411047992125,41.8092828759173));
#31535=CARTESIAN_POINT('Ctrl Pts',(1.39636947860304,2.91705416425172,41.7898688269073));
#31536=CARTESIAN_POINT('Ctrl Pts',(1.63579034605531,2.78984588992295,41.7712081228864));
#31537=CARTESIAN_POINT('Ctrl Pts',(1.98606021360407,2.54298862628443,41.7425745710956));
#31538=CARTESIAN_POINT('Ctrl Pts',(2.1086889113403,2.44226742333424,41.7322130210346));
#31539=CARTESIAN_POINT('Ctrl Pts',(2.24840109434542,2.30911251730484,41.7200350503971));
#31540=CARTESIAN_POINT('Ctrl Pts',(2.27299514247021,2.28490729120114,41.7178750524692));
#31541=CARTESIAN_POINT('Ctrl Pts',(2.30723339790549,2.25011030906333,41.7148436175089));
#31542=CARTESIAN_POINT('Ctrl Pts',(2.31720235528355,2.23984276470445,41.7139579489364));
#31543=CARTESIAN_POINT('Ctrl Pts',(2.33422185681955,2.22207825785498,41.7124405286845));
#31544=CARTESIAN_POINT('Ctrl Pts',(2.34130542534912,2.21461336806681,41.7118073492769));
#31545=CARTESIAN_POINT('Ctrl Pts',(2.35476003665294,2.20029776380871,41.7106015022732));
#31546=CARTESIAN_POINT('Ctrl Pts',(2.36113723067631,2.19345299937417,41.7100285738766));
#31547=CARTESIAN_POINT('Ctrl Pts',(2.37755960094831,2.1756719442829,41.7085495201214));
#31548=CARTESIAN_POINT('Ctrl Pts',(2.38755923215579,2.16469374037955,41.7076453351494));
#31549=CARTESIAN_POINT('Ctrl Pts',(2.42100037529773,2.12746638767069,41.7046089499004));
#31550=CARTESIAN_POINT('Ctrl Pts',(2.44408824537454,2.10090191198268,41.7024915326204));
#31551=CARTESIAN_POINT('Ctrl Pts',(2.64166159662193,1.86591154459648,41.6841675428929));
#31552=CARTESIAN_POINT('Ctrl Pts',(2.78956234557991,1.63656959213224,41.6691492568824));
#31553=CARTESIAN_POINT('Ctrl Pts',(2.9631727689299,1.27385138824258,41.6466322343774));
#31554=CARTESIAN_POINT('Ctrl Pts',(3.01223664969729,1.15304600177306,41.6392887354463));
#31555=CARTESIAN_POINT('Ctrl Pts',(3.07220569088834,0.97517694271233,41.6282728120498));
#31556=CARTESIAN_POINT('Ctrl Pts',(3.08909930036871,0.920262160881826,41.6248442994261));
#31557=CARTESIAN_POINT('Ctrl Pts',(3.10766907526759,0.853609146558072,41.6206176280295));
#31558=CARTESIAN_POINT('Ctrl Pts',(3.11076093109885,0.842271972773622,41.6198964499384));
#31559=CARTESIAN_POINT('Ctrl Pts',(3.11547387240395,0.824610655429433,41.6187691205578));
#31560=CARTESIAN_POINT('Ctrl Pts',(3.11713789855208,0.818297930040075,41.6183654116117));
#31561=CARTESIAN_POINT('Ctrl Pts',(3.12018501470388,0.806594082455271,41.6176154419066));
#31562=CARTESIAN_POINT('Ctrl Pts',(3.12157332435453,0.801204418065614,41.6172694890409));
#31563=CARTESIAN_POINT('Ctrl Pts',(3.12467900035397,0.789017024318631,41.616485859968));
#31564=CARTESIAN_POINT('Ctrl Pts',(3.12638812722437,0.78221735831384,41.6160477201379));
#31565=CARTESIAN_POINT('Ctrl Pts',(3.13138179104575,0.762072518982309,41.6147470314962));
#31566=CARTESIAN_POINT('Ctrl Pts',(3.13460311498892,0.748712054829437,41.6138809568673));
#31567=CARTESIAN_POINT('Ctrl Pts',(3.15789296760548,0.649331766262787,41.6074154191471));
#31568=CARTESIAN_POINT('Ctrl Pts',(3.17450101425351,0.562547741124929,41.6016405442463));
#31569=CARTESIAN_POINT('Ctrl Pts',(3.22464291288388,0.226208853058234,41.5790382922504));
#31570=CARTESIAN_POINT('Ctrl Pts',(3.2324633839039,-0.0262809476336652,
41.5616906602602));
#31571=CARTESIAN_POINT('Ctrl Pts',(3.20317956367178,-0.36556493571607,41.5391906679312));
#31572=CARTESIAN_POINT('Ctrl Pts',(3.19189540397188,-0.453655238773622,
41.5334135218898));
#31573=CARTESIAN_POINT('Ctrl Pts',(3.16781545345881,-0.595017718556564,
41.5242586274787));
#31574=CARTESIAN_POINT('Ctrl Pts',(3.15727585998227,-0.648622055070129,
41.5208140707945));
#31575=CARTESIAN_POINT('Ctrl Pts',(3.14169025986463,-0.718461258146075,
41.5163589284154));
#31576=CARTESIAN_POINT('Ctrl Pts',(3.1378720383408,-0.734958064892181,41.5153089607166));
#31577=CARTESIAN_POINT('Ctrl Pts',(3.13141869155242,-0.761872683687758,
41.5135996460059));
#31578=CARTESIAN_POINT('Ctrl Pts',(3.12886120447845,-0.77230860125507,41.5129377892687));
#31579=CARTESIAN_POINT('Ctrl Pts',(3.12381909303895,-0.792446932153368,
41.5116622968975));
#31580=CARTESIAN_POINT('Ctrl Pts',(3.12134134101052,-0.802150922729585,
41.511048445648));
#31581=CARTESIAN_POINT('Ctrl Pts',(3.11552963277203,-0.824477475842125,
41.5096378127874));
#31582=CARTESIAN_POINT('Ctrl Pts',(3.11216411713119,-0.837091701562125,
41.5088420722497));
#31583=CARTESIAN_POINT('Ctrl Pts',(3.10293794073369,-0.870847279490467,
41.5067158154903));
#31584=CARTESIAN_POINT('Ctrl Pts',(3.09693783837874,-0.891950060372449,
41.5053898721548));
#31585=CARTESIAN_POINT('Ctrl Pts',(3.04250168004785,-1.07623138051949,41.4938362706498));
#31586=CARTESIAN_POINT('Ctrl Pts',(2.98142123927022,-1.23540656099934,41.4840513901351));
#31587=CARTESIAN_POINT('Ctrl Pts',(2.79876588818634,-1.61780993259629,41.4601749296067));
#31588=CARTESIAN_POINT('Ctrl Pts',(2.66288760855944,-1.83286666833307,41.4464315698199));
#31589=CARTESIAN_POINT('Ctrl Pts',(2.46997401387528,-2.07078139298229,41.4284117466716));
#31590=CARTESIAN_POINT('Ctrl Pts',(2.4357074177198,-2.11097982633885,41.4252540008806));
#31591=CARTESIAN_POINT('Ctrl Pts',(2.39287369072687,-2.15879658908845,41.4213318078411));
#31592=CARTESIAN_POINT('Ctrl Pts',(2.38523157577708,-2.16723730441179,41.420632965618));
#31593=CARTESIAN_POINT('Ctrl Pts',(2.37321798558272,-2.18036580380949,41.4195354796457));
#31594=CARTESIAN_POINT('Ctrl Pts',(2.36887689230881,-2.18508144308042,41.4191391286467));
#31595=CARTESIAN_POINT('Ctrl Pts',(2.36073507443293,-2.19387295194582,41.4183961095489));
#31596=CARTESIAN_POINT('Ctrl Pts',(2.35693781790056,-2.19795194250644,41.4180497072395));
#31597=CARTESIAN_POINT('Ctrl Pts',(2.34825815720645,-2.20722722652227,41.4172582474309));
#31598=CARTESIAN_POINT('Ctrl Pts',(2.34336906204687,-2.21241719372926,41.4168126760375));
#31599=CARTESIAN_POINT('Ctrl Pts',(2.32836942123389,-2.22823440496519,41.4154465353617));
#31600=CARTESIAN_POINT('Ctrl Pts',(2.31820367673029,-2.23880870536164,41.4145218481882));
#31601=CARTESIAN_POINT('Ctrl Pts',(2.17773587137418,-2.38293936435441,41.4017656477714));
#31602=CARTESIAN_POINT('Ctrl Pts',(2.03616138166091,-2.50498781788348,41.3891734371723));
#31603=CARTESIAN_POINT('Ctrl Pts',(1.76919758739966,-2.69747762768972,41.3668955958529));
#31604=CARTESIAN_POINT('Ctrl Pts',(1.6481353518135,-2.77310298544616,41.3572445852661));
#31605=CARTESIAN_POINT('Ctrl Pts',(1.43845856146293,-2.88548734928111,41.3414825842501));
#31606=CARTESIAN_POINT('Ctrl Pts',(1.35249874248371,-2.92676446122756,41.3352641694782));
#31607=CARTESIAN_POINT('Ctrl Pts',(1.21185065068668,-2.98677974816566,41.3254872890444));
#31608=CARTESIAN_POINT('Ctrl Pts',(1.15827358394486,-3.00796247610289,41.3218512408999));
#31609=CARTESIAN_POINT('Ctrl Pts',(1.08784211499233,-3.03364773520101,41.3171817336116));
#31610=CARTESIAN_POINT('Ctrl Pts',(1.07148158967866,-3.03946479999321,41.3161046579275));
#31611=CARTESIAN_POINT('Ctrl Pts',(1.04476726808361,-3.04872070100536,41.3143580854135));
#31612=CARTESIAN_POINT('Ctrl Pts',(1.03444178187883,-3.05223963046383,41.3136859409618));
#31613=CARTESIAN_POINT('Ctrl Pts',(1.01452814382783,-3.05891354696338,41.3123952110237));
#31614=CARTESIAN_POINT('Ctrl Pts',(1.00494266174938,-3.0620760429295,41.3117763836653));
#31615=CARTESIAN_POINT('Ctrl Pts',(0.982927305668118,-3.06922496104284,
41.3103606740534));
#31616=CARTESIAN_POINT('Ctrl Pts',(0.970487699424704,-3.07318102018542,
41.3095647985493));
#31617=CARTESIAN_POINT('Ctrl Pts',(0.937295142849948,-3.08351531963327,
41.3074517434146));
#31618=CARTESIAN_POINT('Ctrl Pts',(0.91650096806394,-3.08975968677057,41.3061389440187));
#31619=CARTESIAN_POINT('Ctrl Pts',(0.747870976377588,-3.13854607580705,
41.2955777682768));
#31620=CARTESIAN_POINT('Ctrl Pts',(0.597215768152055,-3.1706662929314,41.2866818168707));
#31621=CARTESIAN_POINT('Ctrl Pts',(0.227708156346183,-3.22216107032286,
41.2655431921916));
#31622=CARTESIAN_POINT('Ctrl Pts',(0.00808524222401213,-3.23018542070195,
41.2535573529878));
#31623=CARTESIAN_POINT('Ctrl Pts',(-0.275934441114121,-3.2115820863583,
41.2372117431779));
#31624=CARTESIAN_POINT('Ctrl Pts',(-0.341080213456631,-3.20531785104832,
41.2334009724467));
#31625=CARTESIAN_POINT('Ctrl Pts',(-0.430285176728102,-3.19399001368724,
41.2280440695457));
#31626=CARTESIAN_POINT('Ctrl Pts',(-0.454547759379614,-3.1906274930175,
41.226572841367));
#31627=CARTESIAN_POINT('Ctrl Pts',(-0.496295232652938,-3.18435593329998,
41.2240131928583));
#31628=CARTESIAN_POINT('Ctrl Pts',(-0.513799116560879,-3.18157855522713,
41.2229314087993));
#31629=CARTESIAN_POINT('Ctrl Pts',(-0.53889257979365,-3.17738444949102,
41.2213670956979));
#31630=CARTESIAN_POINT('Ctrl Pts',(-0.546501725615189,-3.17608454129136,
41.2208909623499));
#31631=CARTESIAN_POINT('Ctrl Pts',(-0.559699609310544,-3.17378104963471,
41.220061908618));
#31632=CARTESIAN_POINT('Ctrl Pts',(-0.565290560236526,-3.1727900002629,
41.2197096980301));
#31633=CARTESIAN_POINT('Ctrl Pts',(-0.57695212672932,-3.17069107379149,
41.2189729173542));
#31634=CARTESIAN_POINT('Ctrl Pts',(-0.583022181376876,-3.16958053635803,
41.2185882028341));
#31635=CARTESIAN_POINT('Ctrl Pts',(-0.59905364401023,-3.16659991499425,
41.217569020439));
#31636=CARTESIAN_POINT('Ctrl Pts',(-0.609009387712006,-3.16470027794517,
41.2169329051342));
#31637=CARTESIAN_POINT('Ctrl Pts',(-0.650846525681272,-3.15651268470663,
41.2142467976182));
#31638=CARTESIAN_POINT('Ctrl Pts',(-0.682639560770881,-3.14978992422111,
41.2121738855381));
#31639=CARTESIAN_POINT('Ctrl Pts',(-0.978175688202822,-3.08261326551532,
41.1926425823373));
#31640=CARTESIAN_POINT('Ctrl Pts',(-1.23341415224436,-2.98965216311244,
41.1739231776421));
#31641=CARTESIAN_POINT('Ctrl Pts',(-1.47443971851644,-2.86568408750336,
41.1558028684421));
#31642=CARTESIAN_POINT('Ctrl Pts',(-1.47484758497728,-2.86547419705606,
41.155772203341));
#31643=CARTESIAN_POINT('Ctrl Pts',(-1.47525540498233,-2.86526422037662,
41.155741540048));
#31644=CARTESIAN_POINT('',(1.87158653173903,2.62360084935058,42.));
#31645=CARTESIAN_POINT('Origin',(0.,0.,42.));
#31646=CARTESIAN_POINT('',(3.2227499802754,-0.000356559795960891,41.8107734493069));
#31647=CARTESIAN_POINT('Ctrl Pts',(3.2227499802754,-0.000356559795960942,
41.8107734493069));
#31648=CARTESIAN_POINT('Ctrl Pts',(3.22276116218653,0.100710650400674,41.8170618951482));
#31649=CARTESIAN_POINT('Ctrl Pts',(3.21801377018382,0.201942216964461,41.8233503409896));
#31650=CARTESIAN_POINT('Ctrl Pts',(3.20848744225778,0.302862832605988,41.829638786831));
#31651=CARTESIAN_POINT('Ctrl Pts',(3.19897581006305,0.403627763679155,41.8359175318399));
#31652=CARTESIAN_POINT('Ctrl Pts',(3.18469994561519,0.504082287979816,41.8421962768489));
#31653=CARTESIAN_POINT('Ctrl Pts',(3.16569147799305,0.603750800133791,41.8484750218579));
#31654=CARTESIAN_POINT('Ctrl Pts',(3.14657766864607,0.703971658389041,41.8547885626138));
#31655=CARTESIAN_POINT('Ctrl Pts',(3.1226786188447,0.803397339300133,41.8611021033697));
#31656=CARTESIAN_POINT('Ctrl Pts',(3.09407959784692,0.901548115569805,41.8674156441256));
#31657=CARTESIAN_POINT('Ctrl Pts',(3.06570847649884,0.998916748718827,41.8736788735885));
#31658=CARTESIAN_POINT('Ctrl Pts',(3.03271212563611,1.09503031405381,41.8799421030514));
#31659=CARTESIAN_POINT('Ctrl Pts',(2.99522500802737,1.18943041569797,41.8862053325142));
#31660=CARTESIAN_POINT('Ctrl Pts',(2.95776305103302,1.28376715785475,41.8924643582209));
#31661=CARTESIAN_POINT('Ctrl Pts',(2.91581647617623,1.37639233915429,41.8987233839276));
#31662=CARTESIAN_POINT('Ctrl Pts',(2.86956900111435,1.46686444852399,41.9049824096343));
#31663=CARTESIAN_POINT('Ctrl Pts',(2.82334173867697,1.55729701673447,41.9112386998115));
#31664=CARTESIAN_POINT('Ctrl Pts',(2.77281750559416,1.64557801634918,41.9174949899886));
#31665=CARTESIAN_POINT('Ctrl Pts',(2.71822707715101,1.73128828319927,41.9237512801657));
#31666=CARTESIAN_POINT('Ctrl Pts',(2.66278353997809,1.81833798223493,41.9301053401519));
#31667=CARTESIAN_POINT('Ctrl Pts',(2.60314583319936,1.90273552374361,41.9364594001381));
#31668=CARTESIAN_POINT('Ctrl Pts',(2.53960259844331,1.98407061479172,41.9428134601242));
#31669=CARTESIAN_POINT('Ctrl Pts',(2.47703075709567,2.06416232609028,41.9490703847976));
#31670=CARTESIAN_POINT('Ctrl Pts',(2.41067225600933,2.14128425585093,41.955327309471));
#31671=CARTESIAN_POINT('Ctrl Pts',(2.34084384373137,2.21507734893501,41.9615842341443));
#31672=CARTESIAN_POINT('Ctrl Pts',(2.26938935993436,2.29058883777022,41.9679868617869));
#31673=CARTESIAN_POINT('Ctrl Pts',(2.19430165238688,2.3626141854434,41.9743894894295));
#31674=CARTESIAN_POINT('Ctrl Pts',(2.11595976478563,2.43080888518788,41.9807921170721));
#31675=CARTESIAN_POINT('Ctrl Pts',(2.03761787718438,2.49900358493236,41.9871947447148));
#31676=CARTESIAN_POINT('Ctrl Pts',(1.95602218416629,2.56336736150102,41.9935973723574));
#31677=CARTESIAN_POINT('Ctrl Pts',(1.87158653173903,2.62360084935058,42.));
#31678=CARTESIAN_POINT('Ctrl Pts',(-1.47525540501187,-2.86526422036141,
41.4036966894132));
#31679=CARTESIAN_POINT('Ctrl Pts',(-1.38677849737974,-2.91081884505378,
41.4098763065341));
#31680=CARTESIAN_POINT('Ctrl Pts',(-1.29603887642405,-2.95234909938083,
41.416055923655));
#31681=CARTESIAN_POINT('Ctrl Pts',(-1.20343783800877,-2.98962454708761,
41.4222355407759));
#31682=CARTESIAN_POINT('Ctrl Pts',(-1.11095940990869,-3.02685063946888,
41.4284069756473));
#31683=CARTESIAN_POINT('Ctrl Pts',(-1.01662486189503,-3.05983296337935,
41.4345784105186));
#31684=CARTESIAN_POINT('Ctrl Pts',(-0.920859674742334,-3.0883871230682,
41.44074984539));
#31685=CARTESIAN_POINT('Ctrl Pts',(-0.825193211592798,-3.1169118463717,
41.4469149181503));
#31686=CARTESIAN_POINT('Ctrl Pts',(-0.728099454503173,-3.14101735876284,
41.4530799909106));
#31687=CARTESIAN_POINT('Ctrl Pts',(-0.630022549005479,-3.16056785249813,
41.4592450636709));
#31688=CARTESIAN_POINT('Ctrl Pts',(-0.532013907618492,-3.1801047385746,
41.4654058453781));
#31689=CARTESIAN_POINT('Ctrl Pts',(-0.433023901818505,-3.19509282494601,
41.4715666270853));
#31690=CARTESIAN_POINT('Ctrl Pts',(-0.333509615403356,-3.20544675496779,
41.4777274087925));
#31691=CARTESIAN_POINT('Ctrl Pts',(-0.234030931931769,-3.21579698069343,
41.4838859863744));
#31692=CARTESIAN_POINT('Ctrl Pts',(-0.134028770862012,-3.22151629991976,
41.4900445639562));
#31693=CARTESIAN_POINT('Ctrl Pts',(-0.0339672538064622,-3.22257099040019,
41.4962031415381));
#31694=CARTESIAN_POINT('Ctrl Pts',(0.0660850270636717,-3.22362558352734,
41.502361150652));
#31695=CARTESIAN_POINT('Ctrl Pts',(0.166196220000049,-3.22001639951388,
41.5085191597658));
#31696=CARTESIAN_POINT('Ctrl Pts',(0.265901266663934,-3.21176183408523,
41.5146771688797));
#31697=CARTESIAN_POINT('Ctrl Pts',(0.365623577575643,-3.20350583935216,
41.5208362442726));
#31698=CARTESIAN_POINT('Ctrl Pts',(0.464939170920528,-3.19060290099849,
41.5269953196655));
#31699=CARTESIAN_POINT('Ctrl Pts',(0.563388166794329,-3.17312327778423,
41.5331543950584));
#31700=CARTESIAN_POINT('Ctrl Pts',(0.661943510286706,-3.15562477254597,
41.539320123673));
#31701=CARTESIAN_POINT('Ctrl Pts',(0.75962995985247,-3.13353978619853,41.5454858522876));
#31702=CARTESIAN_POINT('Ctrl Pts',(0.855997994093369,-3.10698970011298,
41.5516515809023));
#31703=CARTESIAN_POINT('Ctrl Pts',(0.95242092520818,-3.08042448954409,41.5578208218769));
#31704=CARTESIAN_POINT('Ctrl Pts',(1.0475235335995,-3.04938924786325,41.5639900628514));
#31705=CARTESIAN_POINT('Ctrl Pts',(1.14087360958332,-3.01405457307202,41.570159303826));
#31706=CARTESIAN_POINT('Ctrl Pts',(1.23437865913814,-2.97866123801002,41.5763387865631));
#31707=CARTESIAN_POINT('Ctrl Pts',(1.32612496744316,-2.93895438515914,41.5825182693002));
#31708=CARTESIAN_POINT('Ctrl Pts',(1.41570225115083,-2.89515193013881,41.5886977520372));
#31709=CARTESIAN_POINT('Ctrl Pts',(1.48062643598534,-2.86340461019075,41.5931765424492));
#31710=CARTESIAN_POINT('Ctrl Pts',(1.54441169411802,-2.82950680768233,41.5976553328612));
#31711=CARTESIAN_POINT('Ctrl Pts',(1.60691137623422,-2.79355568969531,41.6021341232732));
#31712=CARTESIAN_POINT('Ctrl Pts',(1.69211405879109,-2.74454533332714,41.6082398336511));
#31713=CARTESIAN_POINT('Ctrl Pts',(1.7752410144947,-2.69153627101615,41.614345544029));
#31714=CARTESIAN_POINT('Ctrl Pts',(1.85588634804178,-2.63473023773823,41.6204512544069));
#31715=CARTESIAN_POINT('Ctrl Pts',(1.9364206655874,-2.57800240338883,41.6265485596915));
#31716=CARTESIAN_POINT('Ctrl Pts',(2.0144797874966,-2.51748823444475,41.6326458649761));
#31717=CARTESIAN_POINT('Ctrl Pts',(2.08968262236008,-2.45343516325708,41.6387431702607));
#31718=CARTESIAN_POINT('Ctrl Pts',(2.16480531212943,-2.38945035464794,41.6448339775309));
#31719=CARTESIAN_POINT('Ctrl Pts',(2.23707742699188,-2.32193442402454,41.6509247848011));
#31720=CARTESIAN_POINT('Ctrl Pts',(2.30614799342743,-2.25117724644476,41.6570155920713));
#31721=CARTESIAN_POINT('Ctrl Pts',(2.37517089654546,-2.18046889605718,41.6631021962764));
#31722=CARTESIAN_POINT('Ctrl Pts',(2.4409963303577,-2.10652405872705,41.6691888004816));
#31723=CARTESIAN_POINT('Ctrl Pts',(2.50330825701889,-2.02967123762471,41.6752754046868));
#31724=CARTESIAN_POINT('Ctrl Pts',(2.56559822081552,-1.95284550456462,41.681359863568));
#31725=CARTESIAN_POINT('Ctrl Pts',(2.62437685666788,-1.87311416772567,41.6874443224494));
#31726=CARTESIAN_POINT('Ctrl Pts',(2.67936742746757,-1.79083995687102,41.6935287813306));
#31727=CARTESIAN_POINT('Ctrl Pts',(2.73435407531765,-1.70857161534231,41.6996128061552));
#31728=CARTESIAN_POINT('Ctrl Pts',(2.78555294787346,-1.62376112973534,41.7056968309798));
#31729=CARTESIAN_POINT('Ctrl Pts',(2.83273045137963,-1.53680049203746,41.7117808558044));
#31730=CARTESIAN_POINT('Ctrl Pts',(2.87991785314039,-1.44982160923401,41.7178661571109));
#31731=CARTESIAN_POINT('Ctrl Pts',(2.92308199852756,-1.36069206929212,41.7239514584173));
#31732=CARTESIAN_POINT('Ctrl Pts',(2.96203563656836,-1.26982772461428,41.7300367597237));
#31733=CARTESIAN_POINT('Ctrl Pts',(3.00103710447587,-1.17885181065272,41.7361295329677));
#31734=CARTESIAN_POINT('Ctrl Pts',(3.03581756728007,-1.08613724837081,41.7422223062117));
#31735=CARTESIAN_POINT('Ctrl Pts',(3.06623833561043,-0.992118960474475,
41.7483150794557));
#31736=CARTESIAN_POINT('Ctrl Pts',(3.09667812302572,-0.898041892281014,
41.7544116619056));
#31737=CARTESIAN_POINT('Ctrl Pts',(3.12275267596171,-0.802659905221281,
41.7605082443555));
#31738=CARTESIAN_POINT('Ctrl Pts',(3.1443741138857,-0.706419842887715,41.7666048268055));
#31739=CARTESIAN_POINT('Ctrl Pts',(3.16603678529099,-0.609996244527372,
41.7727130358327));
#31740=CARTESIAN_POINT('Ctrl Pts',(3.18322930403252,-0.51271174036668,41.7788212448598));
#31741=CARTESIAN_POINT('Ctrl Pts',(3.1959154811389,-0.415020240369924,41.784929453887));
#31742=CARTESIAN_POINT('Ctrl Pts',(3.20708758025298,-0.328988088097834,
41.7903086564702));
#31743=CARTESIAN_POINT('Ctrl Pts',(3.21476558175308,-0.242640549609535,
41.7956878590534));
#31744=CARTESIAN_POINT('Ctrl Pts',(3.21895823631987,-0.156286388813851,
41.8010670616366));
#31745=CARTESIAN_POINT('Ctrl Pts',(3.22148001842556,-0.104346412844581,
41.8043025241821));
#31746=CARTESIAN_POINT('Ctrl Pts',(3.22274422707167,-0.0523565586558018,
41.8075379867276));
#31747=CARTESIAN_POINT('Ctrl Pts',(3.22274998027534,-0.000356560338852404,
41.8107734492731));
#31748=CARTESIAN_POINT('Ctrl Pts',(1.43039598794072,-2.88162839993989,6.58668234580631));
#31749=CARTESIAN_POINT('Ctrl Pts',(2.3908869304735,-2.40485547853165,6.65299332526079));
#31750=CARTESIAN_POINT('Ctrl Pts',(3.78068485083689,-0.42330470969778,6.78561528416975));
#31751=CARTESIAN_POINT('Ctrl Pts',(2.39660828659712,2.9593008547868,6.98454822253319));
#31752=CARTESIAN_POINT('Ctrl Pts',(-1.19393826692811,3.61225397709376,7.18348116089663));
#31753=CARTESIAN_POINT('Ctrl Pts',(-3.68522155716544,0.949002744436199,
7.38241409926007));
#31754=CARTESIAN_POINT('Ctrl Pts',(-2.78953196244949,-2.58902355773568,
7.5813470376235));
#31755=CARTESIAN_POINT('Ctrl Pts',(0.671039291373588,-3.74572463321816,
7.78027997598695));
#31756=CARTESIAN_POINT('Ctrl Pts',(3.51448527473695,-1.45960212386322,7.97921291435037));
#31757=CARTESIAN_POINT('Ctrl Pts',(3.12717197768531,2.16867191230057,8.17814585271383));
#31758=CARTESIAN_POINT('Ctrl Pts',(-0.135028807280012,3.80310255787661,
8.37707879107726));
#31759=CARTESIAN_POINT('Ctrl Pts',(-3.27306356366253,1.94141424541036,8.5760117294407));
#31760=CARTESIAN_POINT('Ctrl Pts',(-3.40217358758694,-1.70507215059562,
8.77494466780414));
#31761=CARTESIAN_POINT('Ctrl Pts',(-0.403640923403273,-3.78405339475958,
8.97387760616759));
#31762=CARTESIAN_POINT('Ctrl Pts',(2.96595593022244,-2.38435003081143,9.172810544531));
#31763=CARTESIAN_POINT('Ctrl Pts',(3.60893852822567,1.20730380998424,9.37174348289446));
#31764=CARTESIAN_POINT('Ctrl Pts',(0.934206293343398,3.68907429945195,9.57067642125789));
#31765=CARTESIAN_POINT('Ctrl Pts',(-2.59934534842778,2.77946388606067,9.76960935962134));
#31766=CARTESIAN_POINT('Ctrl Pts',(-3.7433073822935,-0.685321221973841,
9.96854229798476));
#31767=CARTESIAN_POINT('Ctrl Pts',(-1.4460297930754,-3.52008693042821,10.1674752363482));
#31768=CARTESIAN_POINT('Ctrl Pts',(2.18058944266648,-3.11882102941849,10.3664081747117));
#31769=CARTESIAN_POINT('Ctrl Pts',(3.80258297155867,0.14959131214445,10.5653411130751));
#31770=CARTESIAN_POINT('Ctrl Pts',(1.92884471639216,3.28048361242447,10.7642740514386));
#31771=CARTESIAN_POINT('Ctrl Pts',(-1.71808921409888,3.39561249800469,10.963206989802));
#31772=CARTESIAN_POINT('Ctrl Pts',(-3.78557595114969,0.389139407006486,
11.1621399281654));
#31773=CARTESIAN_POINT('Ctrl Pts',(-2.37296555731667,-2.97507129439684,
11.3610728665289));
#31774=CARTESIAN_POINT('Ctrl Pts',(1.2211228251491,-3.60428547773973,11.5600058048923));
#31775=CARTESIAN_POINT('Ctrl Pts',(3.69262746162031,-0.920063684940536,
11.7589387432558));
#31776=CARTESIAN_POINT('Ctrl Pts',(2.76948293800576,2.60997682152157,11.9578716816192));
#31777=CARTESIAN_POINT('Ctrl Pts',(-0.699659800874596,3.74065380890841,
12.1568046199826));
#31778=CARTESIAN_POINT('Ctrl Pts',(-3.52560211426312,1.43253079764144,12.3557375583461));
#31779=CARTESIAN_POINT('Ctrl Pts',(-3.11044242675709,-2.19252426758155,
12.5546704967095));
#31780=CARTESIAN_POINT('Ctrl Pts',(0.164161079403195,-3.8019818377298,12.7536034350729));
#31781=CARTESIAN_POINT('Ctrl Pts',(3.2878505613498,-1.91626027473385,12.9525363734364));
#31782=CARTESIAN_POINT('Ctrl Pts',(3.38900412249117,1.73108804282604,13.1514693117998));
#31783=CARTESIAN_POINT('Ctrl Pts',(0.374630835682455,3.78703927775718,13.3504022501632));
#31784=CARTESIAN_POINT('Ctrl Pts',(-2.98414227610861,2.36154814268967,13.5493351885267));
#31785=CARTESIAN_POINT('Ctrl Pts',(-3.59957987005836,-1.23492490191512,
13.7482681268901));
#31786=CARTESIAN_POINT('Ctrl Pts',(-0.905907377036315,-3.69612588780959,
13.9472010652536));
#31787=CARTESIAN_POINT('Ctrl Pts',(2.6205698730494,-2.7594615950884,14.146134003617));
#31788=CARTESIAN_POINT('Ctrl Pts',(3.73794536304987,0.713988247211487,14.3450669419804));
#31789=CARTESIAN_POINT('Ctrl Pts',(1.41901074133174,3.53106545822759,14.5439998803439));
#31790=CARTESIAN_POINT('Ctrl Pts',(-2.2044268855072,3.10201819155779,14.7429328187073));
#31791=CARTESIAN_POINT('Ctrl Pts',(-3.8013248865683,-0.178728456209389,
14.9418657570708));
#31792=CARTESIAN_POINT('Ctrl Pts',(-1.90364769271949,-3.29516922422906,
15.1407986954342));
#31793=CARTESIAN_POINT('Ctrl Pts',(1.74406145191863,-3.38234599150264,15.3397316337976));
#31794=CARTESIAN_POINT('Ctrl Pts',(3.78844700014203,-0.360116760811474,
15.5386645721611));
#31795=CARTESIAN_POINT('Ctrl Pts',(2.35009605280664,2.993169440056,15.7375975105245));
#31796=CARTESIAN_POINT('Ctrl Pts',(-1.24870884594248,3.59482141035789,15.9365304488879));
#31797=CARTESIAN_POINT('Ctrl Pts',(-3.69957004376932,0.891737767254035,
16.1354633872514));
#31798=CARTESIAN_POINT('Ctrl Pts',(-2.74939973479973,-2.63112444642698,
16.3343963256148));
#31799=CARTESIAN_POINT('Ctrl Pts',(0.728306209987826,-3.73518203288617,
16.5333292639783));
#31800=CARTESIAN_POINT('Ctrl Pts',(3.53647695542546,-1.40546984956888,16.7322622023417));
#31801=CARTESIAN_POINT('Ctrl Pts',(3.09354840927974,2.21629713570752,16.9311951407051));
#31802=CARTESIAN_POINT('Ctrl Pts',(-0.193293208732243,3.80061212040383,
17.1301280790686));
#31803=CARTESIAN_POINT('Ctrl Pts',(-3.30243950399845,1.89100715935529,17.329061017432));
#31804=CARTESIAN_POINT('Ctrl Pts',(-3.37563819737945,-1.75700925287699,
17.5279939557954));
#31805=CARTESIAN_POINT('Ctrl Pts',(-0.345597398331251,-3.78979909659722,
17.7269268941589));
#31806=CARTESIAN_POINT('Ctrl Pts',(3.00215265516693,-2.33860945636005,17.9258598325223));
#31807=CARTESIAN_POINT('Ctrl Pts',(3.5900101677383,1.26247445512302,18.1247927708858));
#31808=CARTESIAN_POINT('Ctrl Pts',(0.877555064047497,3.70295987878172,18.3237257092492));
#31809=CARTESIAN_POINT('Ctrl Pts',(-2.6416403868901,2.73929750495517,18.5226586476126));
#31810=CARTESIAN_POINT('Ctrl Pts',(-3.73236385888241,-0.742613479012362,
18.7215915859761));
#31811=CARTESIAN_POINT('Ctrl Pts',(-1.39190832123119,-3.54183652637864,
18.9205245243395));
#31812=CARTESIAN_POINT('Ctrl Pts',(2.22813484392072,-3.085033204296,19.119457462703));
#31813=CARTESIAN_POINT('Ctrl Pts',(3.79984354968653,0.20785512312247,19.3183904010664));
#31814=CARTESIAN_POINT('Ctrl Pts',(1.87833886025086,3.30966129390517,19.5173233394298));
#31815=CARTESIAN_POINT('Ctrl Pts',(-1.76993125559216,3.36888083861398,19.7162562777933));
#31816=CARTESIAN_POINT('Ctrl Pts',(-3.79109554726769,0.331072961429409,
19.9151892161567));
#31817=CARTESIAN_POINT('Ctrl Pts',(-2.32708852200922,-3.01109178954004,
20.1141221545202));
#31818=CARTESIAN_POINT('Ctrl Pts',(1.27622152733633,-3.58514621284347,20.3130550928836));
#31819=CARTESIAN_POINT('Ctrl Pts',(3.70629534307339,-0.863359475661814,
20.511988031247));
#31820=CARTESIAN_POINT('Ctrl Pts',(2.72915505388636,2.65211754003269,20.7109209696104));
#31821=CARTESIAN_POINT('Ctrl Pts',(-0.756909844210963,3.729490882418,20.9098539079739));
#31822=CARTESIAN_POINT('Ctrl Pts',(-3.54714409239226,1.37832635544315,21.1087868463373));
#31823=CARTESIAN_POINT('Ctrl Pts',(-3.07647270163572,-2.23993983633326,
21.3077197847008));
#31824=CARTESIAN_POINT('Ctrl Pts',(0.222413985566929,-3.79901918570132,
21.5066527230642));
#31825=CARTESIAN_POINT('Ctrl Pts',(3.31683448791136,-1.86564298141534,21.7055856614276));
#31826=CARTESIAN_POINT('Ctrl Pts',(3.36207401442483,1.78282727032986,21.9045185997911));
#31827=CARTESIAN_POINT('Ctrl Pts',(0.316543663368888,3.79233633311756,22.1034515381545));
#31828=CARTESIAN_POINT('Ctrl Pts',(-3.01998671192163,2.31553341891654,22.3023844765179));
#31829=CARTESIAN_POINT('Ctrl Pts',(-3.58022961709107,-1.28994986073349,
22.5013174148814));
#31830=CARTESIAN_POINT('Ctrl Pts',(-0.849151210531485,-3.70957638766954,
22.7002503532448));
#31831=CARTESIAN_POINT('Ctrl Pts',(2.66255575201821,-2.71897253051539,22.8991832916083));
#31832=CARTESIAN_POINT('Ctrl Pts',(3.72656314567699,0.771195095669392,23.0981162299717));
#31833=CARTESIAN_POINT('Ctrl Pts',(1.3647241516294,3.55239957553509,23.2970491683351));
#31834=CARTESIAN_POINT('Ctrl Pts',(-2.25171193961186,3.06786702699317,23.4959821066986));
#31835=CARTESIAN_POINT('Ctrl Pts',(-3.79813904055242,-0.236969582297126,
23.694915045062));
#31836=CARTESIAN_POINT('Ctrl Pts',(-1.85291970926293,-3.32395898069267,
23.8938479834255));
#31837=CARTESIAN_POINT('Ctrl Pts',(1.79569710773726,-3.35521782475692,24.0927809217889));
#31838=CARTESIAN_POINT('Ctrl Pts',(3.79352143592832,-0.302009717484061,
24.2917138601523));
#31839=CARTESIAN_POINT('Ctrl Pts',(2.30394431674614,3.02883729170711,24.4906467985158));
#31840=CARTESIAN_POINT('Ctrl Pts',(-1.30365925374081,3.57526045267173,24.6895797368792));
#31841=CARTESIAN_POINT('Ctrl Pts',(-3.71280296439449,0.834930477277034,
24.8885126752426));
#31842=CARTESIAN_POINT('Ctrl Pts',(-2.70875008435262,-2.67295486958203,
25.0874456136061));
#31843=CARTESIAN_POINT('Ctrl Pts',(0.785469023636781,-3.72358069164743,
25.2863785519695));
#31844=CARTESIAN_POINT('Ctrl Pts',(3.55760289864069,-1.35110190951161,25.485311490333));
#31845=CARTESIAN_POINT('Ctrl Pts',(3.05921630672578,2.26345098090627,25.6842444286964));
#31846=CARTESIAN_POINT('Ctrl Pts',(-0.251521699592702,3.79720312716301,
25.8831773670599));
#31847=CARTESIAN_POINT('Ctrl Pts',(-3.33103466763993,1.84016923060991,26.0821103054233));
#31848=CARTESIAN_POINT('Ctrl Pts',(-3.34831237027993,-1.80854057884607,
26.2810432437867));
#31849=CARTESIAN_POINT('Ctrl Pts',(-0.287471337177379,-3.79465083829908,
26.4799761821502));
#31850=CARTESIAN_POINT('Ctrl Pts',(3.03764339894311,-2.29232138566123,26.6789091205136));
#31851=CARTESIAN_POINT('Ctrl Pts',(3.57023879254785,1.31734950506271,26.877842058877));
#31852=CARTESIAN_POINT('Ctrl Pts',(0.820697484702102,3.71597502587224,27.0767749972405));
#31853=CARTESIAN_POINT('Ctrl Pts',(-2.68331474003338,2.69848786549469,27.2757079356039));
#31854=CARTESIAN_POINT('Ctrl Pts',(-3.72054356412085,-0.799731418528385,
27.4746408739674));
#31855=CARTESIAN_POINT('Ctrl Pts',(-1.3374598291058,-3.56275398530838,27.6735738123308));
#31856=CARTESIAN_POINT('Ctrl Pts',(2.27515678785163,-3.05052066785249,27.8725067506942));
#31857=CARTESIAN_POINT('Ctrl Pts',(3.79621145927515,0.266070123784241,28.0714396890576));
#31858=CARTESIAN_POINT('Ctrl Pts',(1.82739173267215,3.33806144486047,28.2703726274211));
#31859=CARTESIAN_POINT('Ctrl Pts',(-1.82135749507502,3.34135775238698,28.4693055657845));
#31860=CARTESIAN_POINT('Ctrl Pts',(-3.79572452364676,0.272928735916584,
28.668238504148));
#31861=CARTESIAN_POINT('Ctrl Pts',(-2.28066479632187,-3.04640490432913,
28.8671714425114));
#31862=CARTESIAN_POINT('Ctrl Pts',(1.33102041368457,-3.56516471045272,29.0661043808749));
#31863=CARTESIAN_POINT('Ctrl Pts',(3.71909252552727,-0.806452441790404,
29.2650373192383));
#31864=CARTESIAN_POINT('Ctrl Pts',(2.68818602462228,2.69363521125782,29.4639702576017));
#31865=CARTESIAN_POINT('Ctrl Pts',(-0.81398207092878,3.71745180769153,29.6629031959652));
#31866=CARTESIAN_POINT('Ctrl Pts',(-3.56785275990456,1.32379811071928,29.8618361343286));
#31867=CARTESIAN_POINT('Ctrl Pts',(-3.04178023805176,-2.286829188571,30.060769072692));
#31868=CARTESIAN_POINT('Ctrl Pts',(0.280614641256556,-3.79516405144956,
30.2597020110555));
#31869=CARTESIAN_POINT('Ctrl Pts',(3.34503920917982,-1.81458740306222,30.4586349494189));
#31870=CARTESIAN_POINT('Ctrl Pts',(3.33435407319303,1.83414766823269,30.6575678877823));
#31871=CARTESIAN_POINT('Ctrl Pts',(0.258382127231354,3.7967424762064,30.8565008261458));
#31872=CARTESIAN_POINT('Ctrl Pts',(-3.05512167921966,2.26897471988225,31.0554337645092));
#31873=CARTESIAN_POINT('Ctrl Pts',(-3.56003828088928,-1.34467177887595,
31.2543667028727));
#31874=CARTESIAN_POINT('Ctrl Pts',(-0.792195557702424,-3.7221554175852,
31.4532996412361));
#31875=CARTESIAN_POINT('Ctrl Pts',(2.70391613171949,-2.67784471299768,31.6522325795996));
#31876=CARTESIAN_POINT('Ctrl Pts',(3.71430546775585,0.828220771595132,31.851165517963));
#31877=CARTESIAN_POINT('Ctrl Pts',(1.31011695494754,3.57289914756372,32.0500984563264));
#31878=CARTESIAN_POINT('Ctrl Pts',(-2.29846801167811,3.03299514565962,32.2490313946898));
#31879=CARTESIAN_POINT('Ctrl Pts',(-3.79406091906533,-0.295155038451869,
32.4479643330533));
#31880=CARTESIAN_POINT('Ctrl Pts',(-1.8017564297867,-3.35196785814317,32.6468972714167));
#31881=CARTESIAN_POINT('Ctrl Pts',(1.84691091052057,-3.32730143553342,32.8458302097802));
#31882=CARTESIAN_POINT('Ctrl Pts',(3.79770468103133,-0.243831724710034,
33.0447631481436));
#31883=CARTESIAN_POINT('Ctrl Pts',(2.25725132798827,3.06379359562579,33.2436960865071));
#31884=CARTESIAN_POINT('Ctrl Pts',(-1.35830340019312,3.55485957912918,33.4426290248705));
#31885=CARTESIAN_POINT('Ctrl Pts',(-3.72516365707354,0.777927041772669,
33.6415619632339));
#31886=CARTESIAN_POINT('Ctrl Pts',(-2.66746408246281,-2.71415735046314,
33.8404949015973));
#31887=CARTESIAN_POINT('Ctrl Pts',(0.842447311459858,-3.71110459051167,
34.0394278399608));
#31888=CARTESIAN_POINT('Ctrl Pts',(3.57789307418948,-1.29641656267163,34.2383607783242));
#31889=CARTESIAN_POINT('Ctrl Pts',(3.02416551966811,2.31007308627943,34.4372937166877));
#31890=CARTESIAN_POINT('Ctrl Pts',(-0.309691101873131,3.79290207832017,
34.6362266550511));
#31891=CARTESIAN_POINT('Ctrl Pts',(-3.35884729001673,1.78889900124255,34.8351595934145));
#31892=CARTESIAN_POINT('Ctrl Pts',(-3.32019994296254,-1.85964703453407,
35.034092531778));
#31893=CARTESIAN_POINT('Ctrl Pts',(-0.229277741996502,-3.79861112399583,
35.2330254701414));
#31894=CARTESIAN_POINT('Ctrl Pts',(3.07242052621671,-2.24549479277051,35.4319584085049));
#31895=CARTESIAN_POINT('Ctrl Pts',(3.54962868121306,1.37191507747408,35.6308913468683));
#31896=CARTESIAN_POINT('Ctrl Pts',(0.763647103503218,3.72811719983819,35.8298242852317));
#31897=CARTESIAN_POINT('Ctrl Pts',(-2.72435871711047,2.65704428540604,36.0287572235952));
#31898=CARTESIAN_POINT('Ctrl Pts',(-3.70784922296926,-0.856661481574834,
36.2276901619586));
#31899=CARTESIAN_POINT('Ctrl Pts',(-1.28269713503262,-3.58283446656971,
36.426623100322));
#31900=CARTESIAN_POINT('Ctrl Pts',(2.3216442419344,-3.01529148950444,36.6255560386855));
#31901=CARTESIAN_POINT('Ctrl Pts',(3.79168754631124,0.324222617667434,36.8244889770489));
#31902=CARTESIAN_POINT('Ctrl Pts',(1.77601530605909,3.36567740459321,37.0234219154124));
#31903=CARTESIAN_POINT('Ctrl Pts',(-1.8723558529673,3.31304969821073,37.2223548537758));
#31904=CARTESIAN_POINT('Ctrl Pts',(-3.7994617923675,0.214720395742962,37.4212877921392));
#31905=CARTESIAN_POINT('Ctrl Pts',(-2.23370528574428,-3.08100234999048,
37.6202207305027));
#31906=CARTESIAN_POINT('Ctrl Pts',(1.38550660873585,-3.54434565307739,37.8191536688661));
#31907=CARTESIAN_POINT('Ctrl Pts',(3.73101600658191,-0.749355973410843,
38.0180866072295));
#31908=CARTESIAN_POINT('Ctrl Pts',(2.64658546701708,2.7345201218469,38.217019545593));
#31909=CARTESIAN_POINT('Ctrl Pts',(-0.870863058265686,3.70453933627131,
38.4159524839564));
#31910=CARTESIAN_POINT('Ctrl Pts',(-3.58772328085212,1.26895902047793,38.6148854223199));
#31911=CARTESIAN_POINT('Ctrl Pts',(-3.00637313042353,-2.33318159065596,
38.8138183606833));
#31912=CARTESIAN_POINT('Ctrl Pts',(0.338749266911483,-3.79041680024323,
39.0127512990467));
#31913=CARTESIAN_POINT('Ctrl Pts',(3.37245830401273,-1.76310657017941,39.2116842374102));
#31914=CARTESIAN_POINT('Ctrl Pts',(3.30585041806794,1.88503916744779,39.4106171757737));
#31915=CARTESIAN_POINT('Ctrl Pts',(0.200160644147806,3.80025286079382,39.609550114137));
#31916=CARTESIAN_POINT('Ctrl Pts',(-3.08954036858721,2.2218902919993,39.8084830525005));
#31917=CARTESIAN_POINT('Ctrl Pts',(-3.53900783447175,-1.39909181671731,
40.0074159908639));
#31918=CARTESIAN_POINT('Ctrl Pts',(-0.735059111694563,-3.73383314394713,
40.2063489292274));
#31919=CARTESIAN_POINT('Ctrl Pts',(2.74465148416864,-2.63613934982058,40.4052818675907));
#31920=CARTESIAN_POINT('Ctrl Pts',(3.70115567014427,0.885150728230919,40.6042148059543));
#31921=CARTESIAN_POINT('Ctrl Pts',(1.25523944945949,3.59236978650378,40.8031477443176));
#31922=CARTESIAN_POINT('Ctrl Pts',(-2.34475597191911,2.99777433843635,41.0020806826812));
#31923=CARTESIAN_POINT('Ctrl Pts',(-3.78895369938313,-0.353968922753305,
41.2010136210445));
#31924=CARTESIAN_POINT('Ctrl Pts',(-1.75043395750614,-3.37784670177234,
41.399946559408));
#31925=CARTESIAN_POINT('Ctrl Pts',(1.89819598814578,-3.30121868695718,41.5988794977715));
#31926=CARTESIAN_POINT('Ctrl Pts',(3.80045064895368,-0.179534356723371,
41.7978556019462));
#31927=CARTESIAN_POINT('Ctrl Pts',(2.74058008982409,1.99769120286346,41.9305207266665));
#31928=CARTESIAN_POINT('Ctrl Pts',(1.86660756886202,2.62022723339283,41.9968748719324));
#31929=CARTESIAN_POINT('Ctrl Pts',(1.53698740838146,-3.09636394654476,6.72509367227838));
#31930=CARTESIAN_POINT('Ctrl Pts',(2.56905300209345,-2.58406246986299,6.79140465173286));
#31931=CARTESIAN_POINT('Ctrl Pts',(4.06241702282764,-0.454848876953752,
6.92402661064182));
#31932=CARTESIAN_POINT('Ctrl Pts',(2.5752007069213,3.17982446103466,7.12295954900526));
#31933=CARTESIAN_POINT('Ctrl Pts',(-1.28290913713704,3.88143487920559,7.32189248736869));
#31934=CARTESIAN_POINT('Ctrl Pts',(-3.9598399172061,1.01972130865502,7.52082542573213));
#31935=CARTESIAN_POINT('Ctrl Pts',(-2.9974045912523,-2.78195453691917,7.71975836409557));
#31936=CARTESIAN_POINT('Ctrl Pts',(0.721044347205764,-4.02485161106244,
7.91869130245901));
#31937=CARTESIAN_POINT('Ctrl Pts',(3.776380568565,-1.56836995107503,8.11762424082243));
#31938=CARTESIAN_POINT('Ctrl Pts',(3.36020514183989,2.33027878309083,8.3165571791859));
#31939=CARTESIAN_POINT('Ctrl Pts',(-0.145090994597224,4.08650527093188,
8.51549011754931));
#31940=CARTESIAN_POINT('Ctrl Pts',(-3.51696839657934,2.08608614314127,8.71442305591277));
#31941=CARTESIAN_POINT('Ctrl Pts',(-3.65569954707234,-1.83213211442255,
8.91335599427619));
#31942=CARTESIAN_POINT('Ctrl Pts',(-0.433719768517655,-4.06603658666688,
9.11228893263964));
#31943=CARTESIAN_POINT('Ctrl Pts',(3.18697546483547,-2.5620289803853,9.31122187100306));
#31944=CARTESIAN_POINT('Ctrl Pts',(3.87787236700172,1.2972706646837,9.51015480936652));
#31945=CARTESIAN_POINT('Ctrl Pts',(1.00382224349398,3.96397976129963,9.70908774772995));
#31946=CARTESIAN_POINT('Ctrl Pts',(-2.7930454952688,2.98658625369632,9.90802068609338));
#31947=CARTESIAN_POINT('Ctrl Pts',(-4.02225422945243,-0.736390550414543,
10.1069536244569));
#31948=CARTESIAN_POINT('Ctrl Pts',(-1.55378622621903,-3.78239965302563,
10.3058865628203));
#31949=CARTESIAN_POINT('Ctrl Pts',(2.34308439375097,-3.3512318907665,10.5048195011837));
#31950=CARTESIAN_POINT('Ctrl Pts',(4.08594696565489,0.160738680133138,10.7037524395472));
#31951=CARTESIAN_POINT('Ctrl Pts',(2.07257994765896,3.52494137861565,10.9026853779106));
#31952=CARTESIAN_POINT('Ctrl Pts',(-1.84611919413145,3.64864953283978,11.101618316274));
#31953=CARTESIAN_POINT('Ctrl Pts',(-4.06767260216181,0.418137616238003,
11.3005512546375));
#31954=CARTESIAN_POINT('Ctrl Pts',(-2.54979614936507,-3.19677009518745,
11.4994841930009));
#31955=CARTESIAN_POINT('Ctrl Pts',(1.31211945654531,-3.87287257668649,11.6984171313644));
#31956=CARTESIAN_POINT('Ctrl Pts',(3.96779770091828,-0.98862574460827,11.8973500697278));
#31957=CARTESIAN_POINT('Ctrl Pts',(2.97586153717486,2.80446921318709,12.0962830080912));
#31958=CARTESIAN_POINT('Ctrl Pts',(-0.75179762328831,4.01940291491122,12.2952159464547));
#31959=CARTESIAN_POINT('Ctrl Pts',(-3.78832582184925,1.53928130158088,12.4941488848181));
#31960=CARTESIAN_POINT('Ctrl Pts',(-3.34222892452571,-2.35590858772967,
12.6930818231815));
#31961=CARTESIAN_POINT('Ctrl Pts',(0.176394169248418,-4.08530103604272,
12.892014761545));
#31962=CARTESIAN_POINT('Ctrl Pts',(3.53285730387823,-2.05905772826418,13.0909476999084));
#31963=CARTESIAN_POINT('Ctrl Pts',(3.64154870898418,1.86008668023026,13.2898806382719));
#31964=CARTESIAN_POINT('Ctrl Pts',(0.402547883306248,4.06924497414062,13.4888135766353));
#31965=CARTESIAN_POINT('Ctrl Pts',(-3.20651703574811,2.53752792247832,13.6877465149988));
#31966=CARTESIAN_POINT('Ctrl Pts',(-3.86781631267568,-1.32695004777861,
13.8866794533622));
#31967=CARTESIAN_POINT('Ctrl Pts',(-0.973414525350525,-3.97155682569729,
14.0856123917256));
#31968=CARTESIAN_POINT('Ctrl Pts',(2.81585164640969,-2.96509341561348,14.284545330089));
#31969=CARTESIAN_POINT('Ctrl Pts',(4.01649263886463,0.767193808531516,14.4834782684525));
#31970=CARTESIAN_POINT('Ctrl Pts',(1.52475374663538,3.79419628775648,14.6824112068159));
#31971=CARTESIAN_POINT('Ctrl Pts',(-2.36869817469211,3.33317692526415,14.8813441451794));
#31972=CARTESIAN_POINT('Ctrl Pts',(-4.08459512965621,-0.192047089777438,
15.0802770835428));
#31973=CARTESIAN_POINT('Ctrl Pts',(-2.04550527152725,-3.54072134487557,
15.2792100219063));
#31974=CARTESIAN_POINT('Ctrl Pts',(1.87402685245334,-3.63439442193429,15.4781429602697));
#31975=CARTESIAN_POINT('Ctrl Pts',(4.07075759833579,-0.386952236709728,
15.6770758986331));
#31976=CARTESIAN_POINT('Ctrl Pts',(2.52522243637638,3.21621689329631,15.8760088369966));
#31977=CARTESIAN_POINT('Ctrl Pts',(-1.34176115504296,3.86270325817569,16.07494177536));
#31978=CARTESIAN_POINT('Ctrl Pts',(-3.97525763609332,0.958189012974472,
16.2738747137235));
#31979=CARTESIAN_POINT('Ctrl Pts',(-2.95428175737412,-2.8271927341357,16.4728076520868));
#31980=CARTESIAN_POINT('Ctrl Pts',(0.782578728991608,-4.01352338859924,
16.6717405904503));
#31981=CARTESIAN_POINT('Ctrl Pts',(3.80001104333727,-1.51020380360336,16.8706735288137));
#31982=CARTESIAN_POINT('Ctrl Pts',(3.3240759848093,2.38145298192455,17.0696064671772));
#31983=CARTESIAN_POINT('Ctrl Pts',(-0.207697190464619,4.08382924899859,
17.2685394055406));
#31984=CARTESIAN_POINT('Ctrl Pts',(-3.54853339731083,2.03192278053888,17.4674723439041));
#31985=CARTESIAN_POINT('Ctrl Pts',(-3.62718677091157,-1.88793950825425,
17.6664052822675));
#31986=CARTESIAN_POINT('Ctrl Pts',(-0.37135090847757,-4.07221045142267,
17.8653382206309));
#31987=CARTESIAN_POINT('Ctrl Pts',(3.22586952699263,-2.51287987232251,18.0642711589944));
#31988=CARTESIAN_POINT('Ctrl Pts',(3.85753348743574,1.35655256116935,18.2632040973578));
#31989=CARTESIAN_POINT('Ctrl Pts',(0.942949431467649,3.97890007760914,18.4621370357212));
#31990=CARTESIAN_POINT('Ctrl Pts',(-2.83849231006808,2.94342672128722,18.6610699740847));
#31991=CARTESIAN_POINT('Ctrl Pts',(-4.01049520759558,-0.797952158814143,
18.8600029124481));
#31992=CARTESIAN_POINT('Ctrl Pts',(-1.49563168618331,-3.80577000319091,
19.0589358508116));
#31993=CARTESIAN_POINT('Ctrl Pts',(2.3941728221794,-3.31492623680237,19.257868789175));
#31994=CARTESIAN_POINT('Ctrl Pts',(4.08300340529871,0.223344241524889,19.4568017275385));
#31995=CARTESIAN_POINT('Ctrl Pts',(2.01831045474011,3.55629334647608,19.6557346659019));
#31996=CARTESIAN_POINT('Ctrl Pts',(-1.90182444335736,3.61992586174797,19.8546676042653));
#31997=CARTESIAN_POINT('Ctrl Pts',(-4.07360351206664,0.355744127683883,
20.0536005426287));
#31998=CARTESIAN_POINT('Ctrl Pts',(-2.5005004115443,-3.23547479510659,20.2525334809922));
#31999=CARTESIAN_POINT('Ctrl Pts',(1.37132404897559,-3.85230707636404,20.4514664193556));
#32000=CARTESIAN_POINT('Ctrl Pts',(3.98248409676232,-0.927696004593339,
20.6503993577191));
#32001=CARTESIAN_POINT('Ctrl Pts',(2.93252846673791,2.84975020829459,20.8493322960825));
#32002=CARTESIAN_POINT('Ctrl Pts',(-0.813313872270502,4.00740814031659,
21.0482652344459));
#32003=CARTESIAN_POINT('Ctrl Pts',(-3.8114730827583,1.48103760833823,21.2471981728094));
#32004=CARTESIAN_POINT('Ctrl Pts',(-3.30572781558952,-2.40685750869074,
21.4461311111728));
#32005=CARTESIAN_POINT('Ctrl Pts',(0.238988013211991,-4.0821176106825,21.6450640495362));
#32006=CARTESIAN_POINT('Ctrl Pts',(3.56400107843168,-2.00466849400123,21.8439969878997));
#32007=CARTESIAN_POINT('Ctrl Pts',(3.61261180105568,1.91568145388957,22.0429299262631));
#32008=CARTESIAN_POINT('Ctrl Pts',(0.340132123483712,4.0749367598133,22.2418628646266));
#32009=CARTESIAN_POINT('Ctrl Pts',(-3.24503255660361,2.48808423580994,22.44079580299));
#32010=CARTESIAN_POINT('Ctrl Pts',(-3.84702410170021,-1.38607540157123,
22.6397287413534));
#32011=CARTESIAN_POINT('Ctrl Pts',(-0.912428956318338,-3.98600964092851,
22.8386616797169));
#32012=CARTESIAN_POINT('Ctrl Pts',(2.86096626351498,-2.92158715374577,23.0375946180803));
#32013=CARTESIAN_POINT('Ctrl Pts',(4.00426223208981,0.828663643803887,23.2365275564438));
#32014=CARTESIAN_POINT('Ctrl Pts',(1.46642178435367,3.81712019830084,23.4354604948072));
#32015=CARTESIAN_POINT('Ctrl Pts',(-2.4195068552087,3.29648085623159,23.6343934331707));
#32016=CARTESIAN_POINT('Ctrl Pts',(-4.08117187815611,-0.254628275827654,
23.8333263715341));
#32017=CARTESIAN_POINT('Ctrl Pts',(-1.99099709862783,-3.57165648000459,
24.0322593098975));
#32018=CARTESIAN_POINT('Ctrl Pts',(1.92951033638773,-3.60524469622744,24.2311922482609));
#32019=CARTESIAN_POINT('Ctrl Pts',(4.07621017508652,-0.324515125108852,
24.4301251866244));
#32020=CARTESIAN_POINT('Ctrl Pts',(2.47563152742672,3.2545426711466,24.6290581249878));
#32021=CARTESIAN_POINT('Ctrl Pts',(-1.40080640236154,3.84168464101443,24.8279910633513));
#32022=CARTESIAN_POINT('Ctrl Pts',(-3.98947665834203,0.897148510809323,
25.0269240017147));
#32023=CARTESIAN_POINT('Ctrl Pts',(-2.91060294296254,-2.8721403110435,25.2258569400782));
#32024=CARTESIAN_POINT('Ctrl Pts',(0.844001248033056,-4.00105752910675,
25.4247898784416));
#32025=CARTESIAN_POINT('Ctrl Pts',(3.82271126690174,-1.45178442883431,25.623722816805));
#32026=CARTESIAN_POINT('Ctrl Pts',(3.28718549450203,2.43212067600246,25.8226557551684));
#32027=CARTESIAN_POINT('Ctrl Pts',(-0.270264799725342,4.08016622160577,
26.0215886935319));
#32028=CARTESIAN_POINT('Ctrl Pts',(-3.57925943879032,1.97729646935751,26.2205216318953));
#32029=CARTESIAN_POINT('Ctrl Pts',(-3.59782465543471,-1.94331088780188,
26.4194545702588));
#32030=CARTESIAN_POINT('Ctrl Pts',(-0.308893361864258,-4.07742373918868,
26.6183875086222));
#32031=CARTESIAN_POINT('Ctrl Pts',(3.26400499909824,-2.46314246923822,26.8173204469857));
#32032=CARTESIAN_POINT('Ctrl Pts',(3.83628877270618,1.41551683505063,27.016253385349));
#32033=CARTESIAN_POINT('Ctrl Pts',(0.881854892429735,3.99288509809649,27.2151863237125));
#32034=CARTESIAN_POINT('Ctrl Pts',(-2.88327218681108,2.89957599566987,27.4141192620759));
#32035=CARTESIAN_POINT('Ctrl Pts',(-3.99779407842222,-0.859326459755243,
27.6130522004394));
#32036=CARTESIAN_POINT('Ctrl Pts',(-1.43712575670111,-3.82824620646707,
27.8119851388028));
#32037=CARTESIAN_POINT('Ctrl Pts',(2.44469878586269,-3.2778418668851,28.0109180771663));
#32038=CARTESIAN_POINT('Ctrl Pts',(4.07910065579756,0.285897355313241,28.2098510155297));
#32039=CARTESIAN_POINT('Ctrl Pts',(1.96356680735725,3.58680984315424,28.4087839538932));
#32040=CARTESIAN_POINT('Ctrl Pts',(-1.95708290549785,3.59035178762629,28.6077168922566));
#32041=CARTESIAN_POINT('Ctrl Pts',(-4.07857743430098,0.293267063125026,
28.80664983062));
#32042=CARTESIAN_POINT('Ctrl Pts',(-2.45061724462188,-3.27341940152267,
29.0055827689835));
#32043=CARTESIAN_POINT('Ctrl Pts',(1.43020648364449,-3.83083657600328,29.2045157073469));
#32044=CARTESIAN_POINT('Ctrl Pts',(3.99623491014561,-0.866548325736514,
29.4034486457103));
#32045=CARTESIAN_POINT('Ctrl Pts',(2.88850647377694,2.89436172736787,29.6023815840738));
#32046=CARTESIAN_POINT('Ctrl Pts',(-0.874639053949637,3.9944719279536,29.8013145224372));
#32047=CARTESIAN_POINT('Ctrl Pts',(-3.83372493572705,1.42244598318807,30.0002474608007));
#32048=CARTESIAN_POINT('Ctrl Pts',(-3.26845011057368,-2.45724100010441,
30.1991803991641));
#32049=CARTESIAN_POINT('Ctrl Pts',(0.301525713057809,-4.07797519637728,
30.3981133375275));
#32050=CARTESIAN_POINT('Ctrl Pts',(3.59430758223343,-1.94980831422029,30.5970462758909));
#32051=CARTESIAN_POINT('Ctrl Pts',(3.58282620252664,1.97082618726046,30.7959792142544));
#32052=CARTESIAN_POINT('Ctrl Pts',(0.277636458332829,4.07967124348368,30.9949121526178));
#32053=CARTESIAN_POINT('Ctrl Pts',(-3.2827857401879,2.4380560374861,31.1938450909813));
#32054=CARTESIAN_POINT('Ctrl Pts',(-3.82532813096051,-1.44487513245452,
31.3927780293447));
#32055=CARTESIAN_POINT('Ctrl Pts',(-0.851229035476529,-3.99952604530396,
31.5917109677081));
#32056=CARTESIAN_POINT('Ctrl Pts',(2.90540876988572,-2.877394539818,31.7906439060716));
#32057=CARTESIAN_POINT('Ctrl Pts',(3.99109112648016,0.889938805780879,31.989576844435));
#32058=CARTESIAN_POINT('Ctrl Pts',(1.4077453238388,3.83914737423731,32.1885097827985));
#32059=CARTESIAN_POINT('Ctrl Pts',(-2.46974713456985,3.25901036346728,32.3874427211619));
#32060=CARTESIAN_POINT('Ctrl Pts',(-4.07678985987002,-0.317149643487198,
32.5863756595253));
#32061=CARTESIAN_POINT('Ctrl Pts',(-1.93602119196322,-3.60175254593826,
32.7853085978888));
#32062=CARTESIAN_POINT('Ctrl Pts',(1.98454053129662,-3.57524801063428,32.9842415362522));
#32063=CARTESIAN_POINT('Ctrl Pts',(4.08070515067628,-0.262001776992349,
33.1831744746156));
#32064=CARTESIAN_POINT('Ctrl Pts',(2.42545903226761,3.29210387756742,33.3821074129791));
#32065=CARTESIAN_POINT('Ctrl Pts',(-1.45952256610013,3.81976351845869,33.5810403513425));
#32066=CARTESIAN_POINT('Ctrl Pts',(-4.00275845524774,0.835897246583656,
33.7799732897059));
#32067=CARTESIAN_POINT('Ctrl Pts',(-2.86624035694998,-2.91641315216041,
33.9789062280695));
#32068=CARTESIAN_POINT('Ctrl Pts',(0.905225490601913,-3.98765172364236,
34.1778391664328));
#32069=CARTESIAN_POINT('Ctrl Pts',(3.84451344237989,-1.3930239945038,34.3767721047963));
#32070=CARTESIAN_POINT('Ctrl Pts',(3.24952276417025,2.48221700563069,34.5757050431597));
#32071=CARTESIAN_POINT('Ctrl Pts',(-0.332768917194808,4.07554466368054,
34.7746379815232));
#32072=CARTESIAN_POINT('Ctrl Pts',(-3.60914462495387,1.92220564302213,34.9735709198866));
#32073=CARTESIAN_POINT('Ctrl Pts',(-3.56761732322031,-1.99822573623664,
35.17250385825));
#32074=CARTESIAN_POINT('Ctrl Pts',(-0.246363248667963,-4.08167914070044,
35.3714367966135));
#32075=CARTESIAN_POINT('Ctrl Pts',(3.30137367684192,-2.41282641392402,35.5703697349769));
#32076=CARTESIAN_POINT('Ctrl Pts',(3.81414282020493,1.47414856950349,35.7693026733403));
#32077=CARTESIAN_POINT('Ctrl Pts',(0.820553184171816,4.00593209253256,35.9682356117038));
#32078=CARTESIAN_POINT('Ctrl Pts',(-2.9273747126076,2.8550440889171,36.1671685500672));
#32079=CARTESIAN_POINT('Ctrl Pts',(-3.98415376995365,-0.920498883894049,
36.3661014884307));
#32080=CARTESIAN_POINT('Ctrl Pts',(-1.37828221131289,-3.849823061487,36.5650344267941));
#32081=CARTESIAN_POINT('Ctrl Pts',(2.49465043014533,-3.23998745175455,36.7639673651575));
#32082=CARTESIAN_POINT('Ctrl Pts',(4.07423962618006,0.348383304391666,36.962900303521));
#32083=CARTESIAN_POINT('Ctrl Pts',(1.90836187008279,3.61648371160565,37.1618332418844));
#32084=CARTESIAN_POINT('Ctrl Pts',(-2.01188160081678,3.55993425067045,37.3607661802478));
#32085=CARTESIAN_POINT('Ctrl Pts',(-4.08259319987495,0.230721106156537,
37.5596991186113));
#32086=CARTESIAN_POINT('Ctrl Pts',(-2.40015836675168,-3.31059500799247,
37.7586320569747));
#32087=CARTESIAN_POINT('Ctrl Pts',(1.48875292563011,-3.8084661070492,37.9575649953382));
#32088=CARTESIAN_POINT('Ctrl Pts',(4.00904691493279,-0.805197095935613,
38.1564979337016));
#32089=CARTESIAN_POINT('Ctrl Pts',(2.84380589172842,2.93829333322945,38.3554308720651));
#32090=CARTESIAN_POINT('Ctrl Pts',(-0.935758745314963,3.9805972344063,38.5543638104285));
#32091=CARTESIAN_POINT('Ctrl Pts',(-3.85507618443849,1.3635203486794,38.7532967487919));
#32092=CARTESIAN_POINT('Ctrl Pts',(-3.23040450708304,-2.50704752847379,
38.9522296871554));
#32093=CARTESIAN_POINT('Ctrl Pts',(0.363992462388689,-4.07287418561517,
39.1511626255188));
#32094=CARTESIAN_POINT('Ctrl Pts',(3.62376991564507,-1.8944911904441,39.3500955638822));
#32095=CARTESIAN_POINT('Ctrl Pts',(3.55219848867015,2.02551006091971,39.5490285022457));
#32096=CARTESIAN_POINT('Ctrl Pts',(0.215076379060282,4.08344321778653,39.7479614406091));
#32097=CARTESIAN_POINT('Ctrl Pts',(-3.31976926965591,2.38746293362043,39.9468943789726));
#32098=CARTESIAN_POINT('Ctrl Pts',(-3.80273052050235,-1.50335048727303,
40.145827317336));
#32099=CARTESIAN_POINT('Ctrl Pts',(-0.789834848961668,-4.01207398204883,
40.3447602556994));
#32100=CARTESIAN_POINT('Ctrl Pts',(2.94917967271135,-2.83258134221006,40.5436931940629));
#32101=CARTESIAN_POINT('Ctrl Pts',(3.97696142147388,0.951111115579423,40.7426261324263));
#32102=CARTESIAN_POINT('Ctrl Pts',(1.34877841142462,3.86006894220613,40.9415590707897));
#32103=CARTESIAN_POINT('Ctrl Pts',(-2.51948441896513,3.22116494326784,41.1404920091532));
#32104=CARTESIAN_POINT('Ctrl Pts',(-4.07130205620617,-0.380346269017061,
41.3394249475166));
#32105=CARTESIAN_POINT('Ctrl Pts',(-1.88087422963442,-3.62955985044473,
41.5383578858801));
#32106=CARTESIAN_POINT('Ctrl Pts',(2.0396473123645,-3.54722160642478,41.7372908242435));
#32107=CARTESIAN_POINT('Ctrl Pts',(4.08365574488659,-0.19291304504628,41.9362669284183));
#32108=CARTESIAN_POINT('Ctrl Pts',(2.94480488286648,2.14655679302897,42.0689320531386));
#32109=CARTESIAN_POINT('Ctrl Pts',(2.00570496136574,2.81548347365039,42.1352861984045));
#32110=CARTESIAN_POINT('Ctrl Pts',(1.6435788288222,-3.31109949314964,6.86350499875044));
#32111=CARTESIAN_POINT('Ctrl Pts',(2.74721907371341,-2.76326946119434,6.92981597820492));
#32112=CARTESIAN_POINT('Ctrl Pts',(4.34414919481839,-0.486393044209725,
7.06243793711388));
#32113=CARTESIAN_POINT('Ctrl Pts',(2.75379312724547,3.40034806728253,7.26137087547732));
#32114=CARTESIAN_POINT('Ctrl Pts',(-1.37188000734597,4.15061578131742,7.46030381384076));
#32115=CARTESIAN_POINT('Ctrl Pts',(-4.23445827724675,1.09043987287385,7.65923675220419));
#32116=CARTESIAN_POINT('Ctrl Pts',(-3.2052772200551,-2.97488551610267,7.85816969056764));
#32117=CARTESIAN_POINT('Ctrl Pts',(0.771049403037938,-4.30397858890673,
8.05710262893107));
#32118=CARTESIAN_POINT('Ctrl Pts',(4.03827586239305,-1.67713777828685,8.25603556729451));
#32119=CARTESIAN_POINT('Ctrl Pts',(3.59323830599447,2.49188565388108,8.45496850565795));
#32120=CARTESIAN_POINT('Ctrl Pts',(-0.155153181914435,4.36990798398716,
8.65390144402138));
#32121=CARTESIAN_POINT('Ctrl Pts',(-3.76087322949614,2.23075804087219,8.85283438238483));
#32122=CARTESIAN_POINT('Ctrl Pts',(-3.90922550655774,-1.95919207824947,
9.05176732074826));
#32123=CARTESIAN_POINT('Ctrl Pts',(-0.463798613632033,-4.34801977857419,
9.2507002591117));
#32124=CARTESIAN_POINT('Ctrl Pts',(3.40799499944848,-2.73970792995919,9.44963319747514));
#32125=CARTESIAN_POINT('Ctrl Pts',(4.14680620577778,1.38723751938316,9.64856613583857));
#32126=CARTESIAN_POINT('Ctrl Pts',(1.07343819364456,4.23888522314733,9.84749907420202));
#32127=CARTESIAN_POINT('Ctrl Pts',(-2.9867456421098,3.19370862133198,10.0464320125655));
#32128=CARTESIAN_POINT('Ctrl Pts',(-4.30120107661137,-0.787459878855247,
10.2453649509289));
#32129=CARTESIAN_POINT('Ctrl Pts',(-1.66154265936265,-4.04471237562304,
10.4442978892923));
#32130=CARTESIAN_POINT('Ctrl Pts',(2.50557934483546,-3.58364275211452,10.6432308276558));
#32131=CARTESIAN_POINT('Ctrl Pts',(4.36931095975112,0.171886048121829,10.8421637660192));
#32132=CARTESIAN_POINT('Ctrl Pts',(2.21631517892575,3.76939914480685,11.0410967043827));
#32133=CARTESIAN_POINT('Ctrl Pts',(-1.97414917416402,3.90168656767488,11.2400296427461));
#32134=CARTESIAN_POINT('Ctrl Pts',(-4.34976925317394,0.447135825469514,
11.4389625811095));
#32135=CARTESIAN_POINT('Ctrl Pts',(-2.72662674141349,-3.41846889597808,
11.6378955194729));
#32136=CARTESIAN_POINT('Ctrl Pts',(1.40311608794153,-4.14145967563326,11.8368284578364));
#32137=CARTESIAN_POINT('Ctrl Pts',(4.24296794021624,-1.057187804276,12.0357613961998));
#32138=CARTESIAN_POINT('Ctrl Pts',(3.18224013634397,2.99896160485262,12.2346943345633));
#32139=CARTESIAN_POINT('Ctrl Pts',(-0.803935445702029,4.29815202091405,
12.4336272729267));
#32140=CARTESIAN_POINT('Ctrl Pts',(-4.05104952943537,1.64603180552031,12.6325602112902));
#32141=CARTESIAN_POINT('Ctrl Pts',(-3.57401542229434,-2.51929290787779,
12.8314931496536));
#32142=CARTESIAN_POINT('Ctrl Pts',(0.18862725909364,-4.36862023435567,13.030426088017));
#32143=CARTESIAN_POINT('Ctrl Pts',(3.77786404640665,-2.20185518179452,13.2293590263804));
#32144=CARTESIAN_POINT('Ctrl Pts',(3.89409329547718,1.98908531763447,13.4282919647439));
#32145=CARTESIAN_POINT('Ctrl Pts',(0.430464930930045,4.35145067052408,13.6272249031073));
#32146=CARTESIAN_POINT('Ctrl Pts',(-3.42889179538761,2.71350770226696,13.8261578414708));
#32147=CARTESIAN_POINT('Ctrl Pts',(-4.13605275529299,-1.4189751936421,14.0250907798342));
#32148=CARTESIAN_POINT('Ctrl Pts',(-1.04092167366474,-4.246987763585,14.2240237181976));
#32149=CARTESIAN_POINT('Ctrl Pts',(3.01113341976998,-3.17072523613856,14.4229566565611));
#32150=CARTESIAN_POINT('Ctrl Pts',(4.29503991467939,0.820399369851541,14.6218895949245));
#32151=CARTESIAN_POINT('Ctrl Pts',(1.63049675193903,4.05732711728536,14.820822533288));
#32152=CARTESIAN_POINT('Ctrl Pts',(-2.53296946387702,3.56433565897051,15.0197554716514));
#32153=CARTESIAN_POINT('Ctrl Pts',(-4.36786537274413,-0.205365723345486,
15.2186884100148));
#32154=CARTESIAN_POINT('Ctrl Pts',(-2.18736285033501,-3.7862734655221,15.4176213483783));
#32155=CARTESIAN_POINT('Ctrl Pts',(2.00399225298804,-3.88644285236594,15.6165542867417));
#32156=CARTESIAN_POINT('Ctrl Pts',(4.35306819652955,-0.41378771260799,15.8154872251052));
#32157=CARTESIAN_POINT('Ctrl Pts',(2.70034881994612,3.43926434653661,16.0144201634686));
#32158=CARTESIAN_POINT('Ctrl Pts',(-1.43481346414344,4.13058510599347,16.213353101832));
#32159=CARTESIAN_POINT('Ctrl Pts',(-4.25094522841732,1.02464025869492,16.4122860401955));
#32160=CARTESIAN_POINT('Ctrl Pts',(-3.15916377994851,-3.02326102184444,
16.6112189785589));
#32161=CARTESIAN_POINT('Ctrl Pts',(0.836851247995388,-4.29186474431231,
16.8101519169224));
#32162=CARTESIAN_POINT('Ctrl Pts',(4.06354513124908,-1.61493775763784,17.0090848552858));
#32163=CARTESIAN_POINT('Ctrl Pts',(3.55460356033887,2.54660882814157,17.2080177936493));
#32164=CARTESIAN_POINT('Ctrl Pts',(-0.222101172196999,4.36704637759334,
17.4069507320126));
#32165=CARTESIAN_POINT('Ctrl Pts',(-3.79462729062322,2.17283840172248,17.6058836703761));
#32166=CARTESIAN_POINT('Ctrl Pts',(-3.87873534444371,-2.0188697636315,17.8048166087395));
#32167=CARTESIAN_POINT('Ctrl Pts',(-0.397104418623892,-4.35462180624813,
18.003749547103));
#32168=CARTESIAN_POINT('Ctrl Pts',(3.44958639881833,-2.68715028828496,18.2026824854664));
#32169=CARTESIAN_POINT('Ctrl Pts',(4.12505680713318,1.45063066721568,18.4016154238299));
#32170=CARTESIAN_POINT('Ctrl Pts',(1.00834379888781,4.25484027643657,18.6005483621933));
#32171=CARTESIAN_POINT('Ctrl Pts',(-3.03534423324606,3.14755593761926,18.7994813005568));
#32172=CARTESIAN_POINT('Ctrl Pts',(-4.28862655630873,-0.853290838615923,
18.9984142389201));
#32173=CARTESIAN_POINT('Ctrl Pts',(-1.59935505113543,-4.06970348000317,
19.1973471772837));
#32174=CARTESIAN_POINT('Ctrl Pts',(2.56021080043808,-3.54481926930875,19.396280115647));
#32175=CARTESIAN_POINT('Ctrl Pts',(4.36616326091091,0.238833359927311,19.5952130540105));
#32176=CARTESIAN_POINT('Ctrl Pts',(2.15828204922935,3.802925399047,19.7941459923739));
#32177=CARTESIAN_POINT('Ctrl Pts',(-2.03371763112254,3.87097088488195,19.9930789307374));
#32178=CARTESIAN_POINT('Ctrl Pts',(-4.3561114768656,0.380415293938357,20.1920118691008));
#32179=CARTESIAN_POINT('Ctrl Pts',(-2.67391230107938,-3.45985780067314,
20.3909448074643));
#32180=CARTESIAN_POINT('Ctrl Pts',(1.46642657061485,-4.11946793988461,20.5898777458277));
#32181=CARTESIAN_POINT('Ctrl Pts',(4.25867285045125,-0.992032533524869,
20.7888106841911));
#32182=CARTESIAN_POINT('Ctrl Pts',(3.13590187958944,3.0473828765565,20.9877436225545));
#32183=CARTESIAN_POINT('Ctrl Pts',(-0.869717900330041,4.28532539821516,
21.186676560918));
#32184=CARTESIAN_POINT('Ctrl Pts',(-4.07580207312432,1.58374886123332,21.3856094992814));
#32185=CARTESIAN_POINT('Ctrl Pts',(-3.53498292954331,-2.57377518104822,
21.5845424376449));
#32186=CARTESIAN_POINT('Ctrl Pts',(0.255562040857054,-4.36521603566368,
21.7834753760083));
#32187=CARTESIAN_POINT('Ctrl Pts',(3.81116766895198,-2.14369400658712,21.9824083143717));
#32188=CARTESIAN_POINT('Ctrl Pts',(3.86314958768654,2.04853563744927,22.1813412527352));
#32189=CARTESIAN_POINT('Ctrl Pts',(0.363720583598531,4.35753718650904,22.3802741910986));
#32190=CARTESIAN_POINT('Ctrl Pts',(-3.47007840128558,2.66063505270333,22.5792071294621));
#32191=CARTESIAN_POINT('Ctrl Pts',(-4.11381858630935,-1.48220094240897,
22.7781400678255));
#32192=CARTESIAN_POINT('Ctrl Pts',(-0.975706702105193,-4.26244289418747,
22.9770730061889));
#32193=CARTESIAN_POINT('Ctrl Pts',(3.05937677501175,-3.12420177697617,23.1760059445524));
#32194=CARTESIAN_POINT('Ctrl Pts',(4.28196131850264,0.886132191938384,23.3749388829158));
#32195=CARTESIAN_POINT('Ctrl Pts',(1.56811941707795,4.08184082106659,23.5738718212792));
#32196=CARTESIAN_POINT('Ctrl Pts',(-2.58730177080555,3.52509468547,23.7728047596427));
#32197=CARTESIAN_POINT('Ctrl Pts',(-4.3642047157598,-0.272286969358187,
23.9717376980061));
#32198=CARTESIAN_POINT('Ctrl Pts',(-2.12907448799273,-3.81935397931651,
24.1706706363695));
#32199=CARTESIAN_POINT('Ctrl Pts',(2.06332356503822,-3.85527156769798,24.369603574733));
#32200=CARTESIAN_POINT('Ctrl Pts',(4.3588989142447,-0.347020532733638,24.5685365130964));
#32201=CARTESIAN_POINT('Ctrl Pts',(2.6473187381073,3.4802480505861,24.7674694514599));
#32202=CARTESIAN_POINT('Ctrl Pts',(-1.49795355098226,4.10810882935714,24.9664023898233));
#32203=CARTESIAN_POINT('Ctrl Pts',(-4.26615035228957,0.959366544341607,
25.1653353281867));
#32204=CARTESIAN_POINT('Ctrl Pts',(-3.11245580157246,-3.07132575250498,
25.3642682665502));
#32205=CARTESIAN_POINT('Ctrl Pts',(0.902533472429329,-4.27853436656609,
25.5632012049136));
#32206=CARTESIAN_POINT('Ctrl Pts',(4.0878196351628,-1.55246694815701,25.7621341432771));
#32207=CARTESIAN_POINT('Ctrl Pts',(3.51515468227829,2.60079037109864,25.9610670816405));
#32208=CARTESIAN_POINT('Ctrl Pts',(-0.289007899857984,4.36312931604853,
26.160000020004));
#32209=CARTESIAN_POINT('Ctrl Pts',(-3.8274842099407,2.11442370810511,26.3589329583674));
#32210=CARTESIAN_POINT('Ctrl Pts',(-3.8473369405895,-2.07808119675769,26.5578658967308));
#32211=CARTESIAN_POINT('Ctrl Pts',(-0.330315386551131,-4.36019664007829,
26.7567988350943));
#32212=CARTESIAN_POINT('Ctrl Pts',(3.49036659925336,-2.6339635528152,26.9557317734577));
#32213=CARTESIAN_POINT('Ctrl Pts',(4.10233875286451,1.51368416503854,27.1546647118211));
#32214=CARTESIAN_POINT('Ctrl Pts',(0.943012300157368,4.26979517032074,27.3535976501846));
#32215=CARTESIAN_POINT('Ctrl Pts',(-3.08322963358878,3.10066412584504,27.552530588548));
#32216=CARTESIAN_POINT('Ctrl Pts',(-4.27504459272359,-0.9189215009821,27.7514635269115));
#32217=CARTESIAN_POINT('Ctrl Pts',(-1.53679168429643,-4.09373842762575,
27.9503964652748));
#32218=CARTESIAN_POINT('Ctrl Pts',(2.61424078387375,-3.50516306591769,28.1493294036383));
#32219=CARTESIAN_POINT('Ctrl Pts',(4.36198985231999,0.305724586842239,28.3482623420017));
#32220=CARTESIAN_POINT('Ctrl Pts',(2.09974188204234,3.835558241448,28.5471952803652));
#32221=CARTESIAN_POINT('Ctrl Pts',(-2.09280831592068,3.83934582286561,28.7461282187286));
#32222=CARTESIAN_POINT('Ctrl Pts',(-4.36143034495521,0.313605390333471,
28.9450611570921));
#32223=CARTESIAN_POINT('Ctrl Pts',(-2.62056969292188,-3.50043389871622,
29.1439940954555));
#32224=CARTESIAN_POINT('Ctrl Pts',(1.52939255360441,-4.09650844155383,29.342927033819));
#32225=CARTESIAN_POINT('Ctrl Pts',(4.27337729476395,-0.926644209682624,
29.5418599721824));
#32226=CARTESIAN_POINT('Ctrl Pts',(3.08882692293162,3.09508824347791,29.7407929105458));
#32227=CARTESIAN_POINT('Ctrl Pts',(-0.935296036970499,4.27149204821567,
29.9397258489092));
#32228=CARTESIAN_POINT('Ctrl Pts',(-4.09959711154953,1.52109385565686,30.1386587872727));
#32229=CARTESIAN_POINT('Ctrl Pts',(-3.49511998309561,-2.62765281163783,
30.3375917256362));
#32230=CARTESIAN_POINT('Ctrl Pts',(0.322436784859063,-4.360786341305,30.5365246639996));
#32231=CARTESIAN_POINT('Ctrl Pts',(3.84357595528703,-2.08502922537836,30.735457602363));
#32232=CARTESIAN_POINT('Ctrl Pts',(3.83129833186026,2.10750470628822,30.9343905407264));
#32233=CARTESIAN_POINT('Ctrl Pts',(0.296890789434302,4.36260001076095,31.1333234790899));
#32234=CARTESIAN_POINT('Ctrl Pts',(-3.51044980115615,2.60713735508994,31.3322564174533));
#32235=CARTESIAN_POINT('Ctrl Pts',(-4.09061798103173,-1.54507848603308,
31.5311893558168));
#32236=CARTESIAN_POINT('Ctrl Pts',(-0.910262513250637,-4.27689667302272,
31.7301222941802));
#32237=CARTESIAN_POINT('Ctrl Pts',(3.10690140805196,-3.07694436663831,31.9290552325437));
#32238=CARTESIAN_POINT('Ctrl Pts',(4.26787678520448,0.951656839966625,32.127988170907));
#32239=CARTESIAN_POINT('Ctrl Pts',(1.50537369273006,4.10539560091092,32.3269211092706));
#32240=CARTESIAN_POINT('Ctrl Pts',(-2.64102625746159,3.48502558127492,32.5258540476339));
#32241=CARTESIAN_POINT('Ctrl Pts',(-4.35951880067472,-0.339144248522522,
32.7247869859974));
#32242=CARTESIAN_POINT('Ctrl Pts',(-2.07028595413972,-3.85153723373335,
32.9237199243608));
#32243=CARTESIAN_POINT('Ctrl Pts',(2.12217015207268,-3.82319458573513,33.1226528627243));
#32244=CARTESIAN_POINT('Ctrl Pts',(4.36370562032123,-0.280171829274663,
33.3215858010877));
#32245=CARTESIAN_POINT('Ctrl Pts',(2.59366673654697,3.52041415950907,33.5205187394511));
#32246=CARTESIAN_POINT('Ctrl Pts',(-1.56074173200713,4.08466745778821,33.7194516778146));
#32247=CARTESIAN_POINT('Ctrl Pts',(-4.28035325342194,0.893867451394637,
33.9183846161781));
#32248=CARTESIAN_POINT('Ctrl Pts',(-3.06501663143715,-3.11866895385767,
34.1173175545414));
#32249=CARTESIAN_POINT('Ctrl Pts',(0.968003669743968,-4.26419885677308,
34.3162504929049));
#32250=CARTESIAN_POINT('Ctrl Pts',(4.11113381057032,-1.48963142633595,34.5151834312683));
#32251=CARTESIAN_POINT('Ctrl Pts',(3.47488000867237,2.65436092498193,34.7141163696317));
#32252=CARTESIAN_POINT('Ctrl Pts',(-0.355846732516481,4.35818724904092,
34.9130493079952));
#32253=CARTESIAN_POINT('Ctrl Pts',(-3.85944195989102,2.05551228480171,35.1119822463586));
#32254=CARTESIAN_POINT('Ctrl Pts',(-3.81503470347808,-2.13680443793921,
35.3109151847221));
#32255=CARTESIAN_POINT('Ctrl Pts',(-0.263448755339423,-4.36474715740505,
35.5098481230855));
#32256=CARTESIAN_POINT('Ctrl Pts',(3.53032682746711,-2.58015803507752,35.708781061449));
#32257=CARTESIAN_POINT('Ctrl Pts',(4.07865695919681,1.5763820615329,35.9077139998124));
#32258=CARTESIAN_POINT('Ctrl Pts',(0.87745926484041,4.28374698522694,36.1066469381758));
#32259=CARTESIAN_POINT('Ctrl Pts',(-3.13039070810472,3.05304389242815,36.3055798765393));
#32260=CARTESIAN_POINT('Ctrl Pts',(-4.26045831693806,-0.984336286213261,
36.5045128149027));
#32261=CARTESIAN_POINT('Ctrl Pts',(-1.47386728759316,-4.11681165640429,
36.7034457532661));
#32262=CARTESIAN_POINT('Ctrl Pts',(2.66765661835625,-3.46468341400465,36.9023786916296));
#32263=CARTESIAN_POINT('Ctrl Pts',(4.35679170604889,0.372543991115891,37.101311629993));
#32264=CARTESIAN_POINT('Ctrl Pts',(2.04070843410648,3.86729001861809,37.3002445683564));
#32265=CARTESIAN_POINT('Ctrl Pts',(-2.15140734866625,3.80681880313016,37.4991775067199));
#32266=CARTESIAN_POINT('Ctrl Pts',(-4.3657246073824,0.246721816570115,37.6981104450834));
#32267=CARTESIAN_POINT('Ctrl Pts',(-2.56661144775907,-3.54018766599446,
37.8970433834468));
#32268=CARTESIAN_POINT('Ctrl Pts',(1.59199924252436,-4.07258656102101,38.0959763218102));
#32269=CARTESIAN_POINT('Ctrl Pts',(4.28707782328367,-0.861038218460384,
38.2949092601736));
#32270=CARTESIAN_POINT('Ctrl Pts',(3.04102631643975,3.14206654461201,38.4938421985371));
#32271=CARTESIAN_POINT('Ctrl Pts',(-1.00065443236423,4.25665513254129,38.6927751369005));
#32272=CARTESIAN_POINT('Ctrl Pts',(-4.12242908802487,1.45808167688089,38.8917080752639));
#32273=CARTESIAN_POINT('Ctrl Pts',(-3.45443588374254,-2.68091346629163,
39.0906410136274));
#32274=CARTESIAN_POINT('Ctrl Pts',(0.389235657865896,-4.35533157098711,
39.2895739519908));
#32275=CARTESIAN_POINT('Ctrl Pts',(3.8750815272774,-2.02587581070879,39.4885068903542));
#32276=CARTESIAN_POINT('Ctrl Pts',(3.79854655927238,2.16598095439164,39.6874398287178));
#32277=CARTESIAN_POINT('Ctrl Pts',(0.22999211397275,4.36663357477926,39.8863727670811));
#32278=CARTESIAN_POINT('Ctrl Pts',(-3.5499981707246,2.55303557524153,40.0853057054446));
#32279=CARTESIAN_POINT('Ctrl Pts',(-4.06645320653296,-1.60760915782874,
40.284238643808));
#32280=CARTESIAN_POINT('Ctrl Pts',(-0.844610586228765,-4.29031482015054,
40.4831715821715));
#32281=CARTESIAN_POINT('Ctrl Pts',(3.15370786125407,-3.02902333459953,40.6821045205349));
#32282=CARTESIAN_POINT('Ctrl Pts',(4.2527671728035,1.01707150292793,40.8810374588983));
#32283=CARTESIAN_POINT('Ctrl Pts',(1.44231737338975,4.12776809790848,41.0799703972618));
#32284=CARTESIAN_POINT('Ctrl Pts',(-2.69421286601115,3.44455554809932,41.2789033356252));
#32285=CARTESIAN_POINT('Ctrl Pts',(-4.3536504130292,-0.406723615280815,
41.4778362739886));
#32286=CARTESIAN_POINT('Ctrl Pts',(-2.0113145017627,-3.88127299911711,41.6767692123521));
#32287=CARTESIAN_POINT('Ctrl Pts',(2.18109863658322,-3.79322452589238,41.8757021507155));
#32288=CARTESIAN_POINT('Ctrl Pts',(4.3668608408195,-0.206291733369188,42.0746782548904));
#32289=CARTESIAN_POINT('Ctrl Pts',(3.14902967590887,2.29542238319448,42.2073433796106));
#32290=CARTESIAN_POINT('Ctrl Pts',(2.14480235386948,3.01073971390795,42.2736975248765));
#32291=CARTESIAN_POINT('Ctrl Pts',(1.75017024926294,-3.52583503975451,7.00191632522251));
#32292=CARTESIAN_POINT('Ctrl Pts',(2.92538514533336,-2.94247645252568,7.06822730467699));
#32293=CARTESIAN_POINT('Ctrl Pts',(4.62588136680913,-0.517937211465701,
7.20084926358595));
#32294=CARTESIAN_POINT('Ctrl Pts',(2.93238554756965,3.6208716735304,7.39978220194938));
#32295=CARTESIAN_POINT('Ctrl Pts',(-1.46085087755489,4.41979668342923,7.59871514031282));
#32296=CARTESIAN_POINT('Ctrl Pts',(-4.5090766372874,1.16115843709268,7.79764807867627));
#32297=CARTESIAN_POINT('Ctrl Pts',(-3.4131498488579,-3.16781649528616,7.99658101703969));
#32298=CARTESIAN_POINT('Ctrl Pts',(0.821054458870111,-4.58310556675101,
8.19551395540314));
#32299=CARTESIAN_POINT('Ctrl Pts',(4.30017115622109,-1.78590560549867,8.39444689376657));
#32300=CARTESIAN_POINT('Ctrl Pts',(3.82627147014904,2.65349252467134,8.59337983213001));
#32301=CARTESIAN_POINT('Ctrl Pts',(-0.165215369231643,4.65331069704242,
8.79231277049345));
#32302=CARTESIAN_POINT('Ctrl Pts',(-4.00477806241297,2.37542993860311,8.99124570885689));
#32303=CARTESIAN_POINT('Ctrl Pts',(-4.16275146604314,-2.0862520420764,9.19017864722033));
#32304=CARTESIAN_POINT('Ctrl Pts',(-0.493877458746418,-4.63000297048149,
9.38911158558376));
#32305=CARTESIAN_POINT('Ctrl Pts',(3.62901453406151,-2.91738687953307,9.5880445239472));
#32306=CARTESIAN_POINT('Ctrl Pts',(4.41574004455383,1.47720437408262,9.78697746231064));
#32307=CARTESIAN_POINT('Ctrl Pts',(1.14305414379514,4.513790684995,9.98591040067408));
#32308=CARTESIAN_POINT('Ctrl Pts',(-3.18044578895083,3.40083098896765,10.1848433390375));
#32309=CARTESIAN_POINT('Ctrl Pts',(-4.58014792377031,-0.838529207295953,
10.3837762774009));
#32310=CARTESIAN_POINT('Ctrl Pts',(-1.76929909250628,-4.30702509822045,
10.5827092157644));
#32311=CARTESIAN_POINT('Ctrl Pts',(2.66807429591995,-3.81605361346254,10.7816421541278));
#32312=CARTESIAN_POINT('Ctrl Pts',(4.65267495384734,0.183033416110524,10.9805750924913));
#32313=CARTESIAN_POINT('Ctrl Pts',(2.36005041019255,4.01385691099803,11.1795080308547));
#32314=CARTESIAN_POINT('Ctrl Pts',(-2.10217915419658,4.15472360250998,11.3784409692181));
#32315=CARTESIAN_POINT('Ctrl Pts',(-4.63186590418606,0.476134034701025,
11.5773739075816));
#32316=CARTESIAN_POINT('Ctrl Pts',(-2.90345733346189,-3.6401676967687,11.776306845945));
#32317=CARTESIAN_POINT('Ctrl Pts',(1.49411271933775,-4.41004677458003,11.9752397843084));
#32318=CARTESIAN_POINT('Ctrl Pts',(4.51813817951421,-1.12574986394373,12.1741727226719));
#32319=CARTESIAN_POINT('Ctrl Pts',(3.38861873551307,3.19345399651813,12.3731056610353));
#32320=CARTESIAN_POINT('Ctrl Pts',(-0.856073268115742,4.57690112691687,
12.5720385993988));
#32321=CARTESIAN_POINT('Ctrl Pts',(-4.3137732370215,1.75278230945974,12.7709715377622));
#32322=CARTESIAN_POINT('Ctrl Pts',(-3.80580192006295,-2.68267722802591,
12.9699044761256));
#32323=CARTESIAN_POINT('Ctrl Pts',(0.200860348938858,-4.6519394326686,13.1688374144891));
#32324=CARTESIAN_POINT('Ctrl Pts',(4.0228707889351,-2.34465263532486,13.3677703528525));
#32325=CARTESIAN_POINT('Ctrl Pts',(4.14663788197017,2.11808395503869,13.566703291216));
#32326=CARTESIAN_POINT('Ctrl Pts',(0.458381978553845,4.63365636690753,13.7656362295794));
#32327=CARTESIAN_POINT('Ctrl Pts',(-3.65126655502712,2.88948748205561,13.9645691679428));
#32328=CARTESIAN_POINT('Ctrl Pts',(-4.4042891979103,-1.51100033950559,14.1635021063063));
#32329=CARTESIAN_POINT('Ctrl Pts',(-1.10842882197895,-4.52241870147271,
14.3624350446697));
#32330=CARTESIAN_POINT('Ctrl Pts',(3.20641519313028,-3.37635705666365,14.5613679830331));
#32331=CARTESIAN_POINT('Ctrl Pts',(4.57358719049415,0.873604931171569,14.7603009213966));
#32332=CARTESIAN_POINT('Ctrl Pts',(1.73623975724267,4.32045794681424,14.95923385976));
#32333=CARTESIAN_POINT('Ctrl Pts',(-2.69724075306194,3.79549439267688,15.1581667981235));
#32334=CARTESIAN_POINT('Ctrl Pts',(-4.65113561583202,-0.218684356913533,
15.3570997364869));
#32335=CARTESIAN_POINT('Ctrl Pts',(-2.32922042914278,-4.03182558616862,
15.5560326748503));
#32336=CARTESIAN_POINT('Ctrl Pts',(2.13395765352274,-4.13849128279759,15.7549656132138));
#32337=CARTESIAN_POINT('Ctrl Pts',(4.63537879472331,-0.44062318850625,15.9538985515772));
#32338=CARTESIAN_POINT('Ctrl Pts',(2.87547520351587,3.66231179977693,16.1528314899406));
#32339=CARTESIAN_POINT('Ctrl Pts',(-1.52786577324392,4.39846695381126,16.3517644283041));
#32340=CARTESIAN_POINT('Ctrl Pts',(-4.52663282074132,1.09109150441536,16.5506973666675));
#32341=CARTESIAN_POINT('Ctrl Pts',(-3.36404580252289,-3.21932930955316,
16.749630305031));
#32342=CARTESIAN_POINT('Ctrl Pts',(0.891123766999176,-4.57020610002538,
16.9485632433944));
#32343=CARTESIAN_POINT('Ctrl Pts',(4.32707921916088,-1.71967171167232,17.1474961817578));
#32344=CARTESIAN_POINT('Ctrl Pts',(3.78513113586845,2.7117646743586,17.3464291201213));
#32345=CARTESIAN_POINT('Ctrl Pts',(-0.236505153929377,4.65026350618809,
17.5453620584847));
#32346=CARTESIAN_POINT('Ctrl Pts',(-4.0407211839356,2.31375402290608,17.7442949968481));
#32347=CARTESIAN_POINT('Ctrl Pts',(-4.13028391797584,-2.14980001900876,
17.9432279352116));
#32348=CARTESIAN_POINT('Ctrl Pts',(-0.422857928770215,-4.63703316107358,
18.142160873575));
#32349=CARTESIAN_POINT('Ctrl Pts',(3.67330327064404,-2.86142070424742,18.3410938119385));
#32350=CARTESIAN_POINT('Ctrl Pts',(4.39258012683063,1.544708773262,18.5400267503019));
#32351=CARTESIAN_POINT('Ctrl Pts',(1.07373816630795,4.53078047526401,18.7389596886653));
#32352=CARTESIAN_POINT('Ctrl Pts',(-3.23219615642406,3.35168515395129,18.9378926270288));
#32353=CARTESIAN_POINT('Ctrl Pts',(-4.56675790502189,-0.9086295184177,19.1368255653922));
#32354=CARTESIAN_POINT('Ctrl Pts',(-1.70307841608756,-4.33363695681545,
19.3357585037557));
#32355=CARTESIAN_POINT('Ctrl Pts',(2.72624877869676,-3.77471230181512,19.5346914421191));
#32356=CARTESIAN_POINT('Ctrl Pts',(4.6493231165231,0.254322478329726,19.7336243804825));
#32357=CARTESIAN_POINT('Ctrl Pts',(2.2982536437186,4.04955745161791,19.932557318846));
#32358=CARTESIAN_POINT('Ctrl Pts',(-2.16561081888772,4.12201590801593,20.1314902572094));
#32359=CARTESIAN_POINT('Ctrl Pts',(-4.63861944166455,0.405086460192834,
20.3304231955728));
#32360=CARTESIAN_POINT('Ctrl Pts',(-2.84732419061446,-3.68424080623969,
20.5293561339363));
#32361=CARTESIAN_POINT('Ctrl Pts',(1.56152909225411,-4.38662880340519,20.7282890722997));
#32362=CARTESIAN_POINT('Ctrl Pts',(4.53486160414019,-1.05636906245639,20.9272220106632));
#32363=CARTESIAN_POINT('Ctrl Pts',(3.33927529244099,3.24501554481841,21.1261549490266));
#32364=CARTESIAN_POINT('Ctrl Pts',(-0.926121928389577,4.56324265611374,
21.32508788739));
#32365=CARTESIAN_POINT('Ctrl Pts',(-4.34013106349035,1.68646011412841,21.5240208257534));
#32366=CARTESIAN_POINT('Ctrl Pts',(-3.76423804349709,-2.74069285340571,
21.7229537641169));
#32367=CARTESIAN_POINT('Ctrl Pts',(0.272136068502114,-4.64831446064486,
21.9218867024803));
#32368=CARTESIAN_POINT('Ctrl Pts',(4.05833425947229,-2.282719519173,22.1208196408438));
#32369=CARTESIAN_POINT('Ctrl Pts',(4.1136873743174,2.18138982100898,22.3197525792072));
#32370=CARTESIAN_POINT('Ctrl Pts',(0.387309043713353,4.64013761320478,22.5186855175706));
#32371=CARTESIAN_POINT('Ctrl Pts',(-3.69512424596756,2.83318586959673,22.7176184559341));
#32372=CARTESIAN_POINT('Ctrl Pts',(-4.38061307091849,-1.5783264832467,22.9165513942975));
#32373=CARTESIAN_POINT('Ctrl Pts',(-1.03898444789204,-4.53887614744645,
23.115484332661));
#32374=CARTESIAN_POINT('Ctrl Pts',(3.25778728650852,-3.32681640020656,23.3144172710244));
#32375=CARTESIAN_POINT('Ctrl Pts',(4.55966040491547,0.943600740072882,23.5133502093879));
#32376=CARTESIAN_POINT('Ctrl Pts',(1.66981704980222,4.34656144383233,23.7122831477513));
#32377=CARTESIAN_POINT('Ctrl Pts',(-2.7550966864024,3.75370851470842,23.9112160861147));
#32378=CARTESIAN_POINT('Ctrl Pts',(-4.6472375533635,-0.289945662888717,
24.1101490244782));
#32379=CARTESIAN_POINT('Ctrl Pts',(-2.26715187735763,-4.06705147862843,
24.3090819628416));
#32380=CARTESIAN_POINT('Ctrl Pts',(2.19713679368869,-4.10529843916849,24.508014901205));
#32381=CARTESIAN_POINT('Ctrl Pts',(4.6415876534029,-0.369525940358427,24.7069478395685));
#32382=CARTESIAN_POINT('Ctrl Pts',(2.81900594878788,3.70595343002559,24.9058807779319));
#32383=CARTESIAN_POINT('Ctrl Pts',(-1.59510069960298,4.37453301769984,25.1048137162954));
#32384=CARTESIAN_POINT('Ctrl Pts',(-4.54282404623711,1.02158457787389,25.3037466546588));
#32385=CARTESIAN_POINT('Ctrl Pts',(-3.31430866018239,-3.27051119396646,
25.5026795930222));
#32386=CARTESIAN_POINT('Ctrl Pts',(0.961065696825607,-4.55601120402541,
25.7016125313856));
#32387=CARTESIAN_POINT('Ctrl Pts',(4.35292800342385,-1.65314946747969,25.9005454697491));
#32388=CARTESIAN_POINT('Ctrl Pts',(3.74312387005455,2.76946006619482,26.0994784081125));
#32389=CARTESIAN_POINT('Ctrl Pts',(-0.307750999990631,4.64609241049128,
26.298411346476));
#32390=CARTESIAN_POINT('Ctrl Pts',(-4.0757089810911,2.25155094685271,26.4973442848394));
#32391=CARTESIAN_POINT('Ctrl Pts',(-4.09684922574428,-2.21285150571349,
26.6962772232029));
#32392=CARTESIAN_POINT('Ctrl Pts',(-0.351737411238005,-4.64296954096788,
26.8952101615663));
#32393=CARTESIAN_POINT('Ctrl Pts',(3.71672819940849,-2.8047846363922,27.0941430999298));
#32394=CARTESIAN_POINT('Ctrl Pts',(4.36838873302285,1.61185149502644,27.2930760382932));
#32395=CARTESIAN_POINT('Ctrl Pts',(1.00416970788501,4.54670524254498,27.4920089766566));
#32396=CARTESIAN_POINT('Ctrl Pts',(-3.28318708036648,3.30175225602021,27.69094191502));
#32397=CARTESIAN_POINT('Ctrl Pts',(-4.55229510702496,-0.97851654220896,
27.8898748533835));
#32398=CARTESIAN_POINT('Ctrl Pts',(-1.63645761189174,-4.35923064878442,
28.0888077917469));
#32399=CARTESIAN_POINT('Ctrl Pts',(2.78378278188482,-3.7324842649503,28.2877407301104));
#32400=CARTESIAN_POINT('Ctrl Pts',(4.6448790488424,0.32555181837124,28.4866736684738));
#32401=CARTESIAN_POINT('Ctrl Pts',(2.23591695672744,4.08430663974176,28.6856066068372));
#32402=CARTESIAN_POINT('Ctrl Pts',(-2.22853372634353,4.08833985810493,28.8845395452007));
#32403=CARTESIAN_POINT('Ctrl Pts',(-4.64428325560944,0.333943717541912,
29.0834724835641));
#32404=CARTESIAN_POINT('Ctrl Pts',(-2.79052214122188,-3.72744839590976,
29.2824054219276));
#32405=CARTESIAN_POINT('Ctrl Pts',(1.62857862356433,-4.36218030710437,29.481338360291));
#32406=CARTESIAN_POINT('Ctrl Pts',(4.55051967938229,-0.986740093628734,
29.6802712986544));
#32407=CARTESIAN_POINT('Ctrl Pts',(3.28914737208629,3.29581475958795,29.8792042370179));
#32408=CARTESIAN_POINT('Ctrl Pts',(-0.995953019991353,4.54851216847773,
30.0781371753813));
#32409=CARTESIAN_POINT('Ctrl Pts',(-4.36546928737203,1.61974172812565,30.2770701137447));
#32410=CARTESIAN_POINT('Ctrl Pts',(-3.72178985561752,-2.79806462317125,
30.4760030521082));
#32411=CARTESIAN_POINT('Ctrl Pts',(0.343347856660311,-4.64359748623272,
30.6749359904716));
#32412=CARTESIAN_POINT('Ctrl Pts',(4.09284432834063,-2.22025013653641,30.8738689288351));
#32413=CARTESIAN_POINT('Ctrl Pts',(4.07977046119387,2.24418322531598,31.0728018671985));
#32414=CARTESIAN_POINT('Ctrl Pts',(0.316145120535775,4.64552877803824,31.2717348055619));
#32415=CARTESIAN_POINT('Ctrl Pts',(-3.73811386212439,2.77621867269378,31.4706677439254));
#32416=CARTESIAN_POINT('Ctrl Pts',(-4.35590783110296,-1.64528183961164,
31.6696006822888));
#32417=CARTESIAN_POINT('Ctrl Pts',(-0.969295991024743,-4.55426730074148,
31.8685336206522));
#32418=CARTESIAN_POINT('Ctrl Pts',(3.30839404621819,-3.27649419345861,32.0674665590156));
#32419=CARTESIAN_POINT('Ctrl Pts',(4.54466244392879,1.01337487415237,32.2663994973791));
#32420=CARTESIAN_POINT('Ctrl Pts',(1.60300206162132,4.3716438275845,32.4653324357425));
#32421=CARTESIAN_POINT('Ctrl Pts',(-2.81230538035333,3.71104079908257,32.664265374106));
#32422=CARTESIAN_POINT('Ctrl Pts',(-4.64224774147941,-0.361138853557849,
32.8631983124694));
#32423=CARTESIAN_POINT('Ctrl Pts',(-2.20455071631624,-4.10132192152844,
33.0621312508329));
#32424=CARTESIAN_POINT('Ctrl Pts',(2.25979977284874,-4.07114116083598,33.2610641891963));
#32425=CARTESIAN_POINT('Ctrl Pts',(4.64670608996618,-0.298341881556976,
33.4599971275598));
#32426=CARTESIAN_POINT('Ctrl Pts',(2.76187444082632,3.74872444145071,33.6589300659231));
#32427=CARTESIAN_POINT('Ctrl Pts',(-1.66196089791414,4.34957139711773,33.8578630042867));
#32428=CARTESIAN_POINT('Ctrl Pts',(-4.55794805159614,0.951837656205623,
34.05679594265));
#32429=CARTESIAN_POINT('Ctrl Pts',(-3.26379290592433,-3.32092475555494,
34.2557288810135));
#32430=CARTESIAN_POINT('Ctrl Pts',(1.03078184888602,-4.54074598990379,34.4546618193769));
#32431=CARTESIAN_POINT('Ctrl Pts',(4.37775417876074,-1.58623885816811,34.6535947577404));
#32432=CARTESIAN_POINT('Ctrl Pts',(3.70023725317449,2.82650484433319,34.8525276961038));
#32433=CARTESIAN_POINT('Ctrl Pts',(-0.378924547838154,4.64082983440129,
35.0514606344673));
#32434=CARTESIAN_POINT('Ctrl Pts',(-4.10973929482816,2.18881892658129,35.2503935728307));
#32435=CARTESIAN_POINT('Ctrl Pts',(-4.06245208373585,-2.27538313964179,
35.4493265111941));
#32436=CARTESIAN_POINT('Ctrl Pts',(-0.280534262010886,-4.64781517410965,
35.6482594495575));
#32437=CARTESIAN_POINT('Ctrl Pts',(3.75927997809232,-2.74748965623102,35.847192387921));
#32438=CARTESIAN_POINT('Ctrl Pts',(4.34317109818868,1.67861555356232,36.0461253262844));
#32439=CARTESIAN_POINT('Ctrl Pts',(0.934365345509009,4.56156187792131,36.2450582646479));
#32440=CARTESIAN_POINT('Ctrl Pts',(-3.33340670360185,3.25104369593922,36.4439912030113));
#32441=CARTESIAN_POINT('Ctrl Pts',(-4.53676286392246,-1.04817368853247,
36.6429241413748));
#32442=CARTESIAN_POINT('Ctrl Pts',(-1.56945236387344,-4.38380025132158,
36.8418570797382));
#32443=CARTESIAN_POINT('Ctrl Pts',(2.84066280656719,-3.68937937625476,37.0407900181016));
#32444=CARTESIAN_POINT('Ctrl Pts',(4.63934378591771,0.396704677840125,37.239722956465));
#32445=CARTESIAN_POINT('Ctrl Pts',(2.17305499813018,4.11809632563053,37.4386558948285));
#32446=CARTESIAN_POINT('Ctrl Pts',(-2.29093309651572,4.05370335558988,37.6375888331919));
#32447=CARTESIAN_POINT('Ctrl Pts',(-4.64885601488985,0.262722526983691,
37.8365217715554));
#32448=CARTESIAN_POINT('Ctrl Pts',(-2.73306452876649,-3.76978032399644,
38.0354547099188));
#32449=CARTESIAN_POINT('Ctrl Pts',(1.69524555941862,-4.33670701499282,38.2343876482823));
#32450=CARTESIAN_POINT('Ctrl Pts',(4.56510873163454,-0.91687934098516,38.4333205866457));
#32451=CARTESIAN_POINT('Ctrl Pts',(3.23824674115109,3.34583975599457,38.6322535250092));
#32452=CARTESIAN_POINT('Ctrl Pts',(-1.0655501194135,4.53271303067627,38.8311864633726));
#32453=CARTESIAN_POINT('Ctrl Pts',(-4.38978199161124,1.55264300508237,39.030119401736));
#32454=CARTESIAN_POINT('Ctrl Pts',(-3.67846726040206,-2.85477940410947,
39.2290523400994));
#32455=CARTESIAN_POINT('Ctrl Pts',(0.414478853343105,-4.63778895635907,
39.4279852784629));
#32456=CARTESIAN_POINT('Ctrl Pts',(4.12639313890974,-2.15726043097348,39.6269182168263));
#32457=CARTESIAN_POINT('Ctrl Pts',(4.04489462987461,2.30645184786356,39.8258511551898));
#32458=CARTESIAN_POINT('Ctrl Pts',(0.244907848885221,4.64982393177198,40.0247840935532));
#32459=CARTESIAN_POINT('Ctrl Pts',(-3.7802270717933,2.71860821686265,40.2237170319166));
#32460=CARTESIAN_POINT('Ctrl Pts',(-4.33017589256357,-1.71186782838445,
40.4226499702801));
#32461=CARTESIAN_POINT('Ctrl Pts',(-0.899386323495868,-4.56855565825224,
40.6215829086435));
#32462=CARTESIAN_POINT('Ctrl Pts',(3.35823604979678,-3.22546532698901,40.820515847007));
#32463=CARTESIAN_POINT('Ctrl Pts',(4.52857292413312,1.08303189027643,41.0194487853703));
#32464=CARTESIAN_POINT('Ctrl Pts',(1.53585633535487,4.39546725361082,41.2183817237339));
#32465=CARTESIAN_POINT('Ctrl Pts',(-2.86894131305717,3.66794615293081,41.4173146620972));
#32466=CARTESIAN_POINT('Ctrl Pts',(-4.63599876985225,-0.433100961544568,
41.6162476004607));
#32467=CARTESIAN_POINT('Ctrl Pts',(-2.14175477389098,-4.13298614778951,
41.8151805388241));
#32468=CARTESIAN_POINT('Ctrl Pts',(2.32254996080195,-4.03922744535998,42.0141134771876));
#32469=CARTESIAN_POINT('Ctrl Pts',(4.65006593675241,-0.219670421692099,
42.2130895813624));
#32470=CARTESIAN_POINT('Ctrl Pts',(3.35325446895125,2.44428797335999,42.3457547060828));
#32471=CARTESIAN_POINT('Ctrl Pts',(2.28389974637321,3.20599595416551,42.4121088513486));
#32472=CARTESIAN_POINT('Ctrl Pts',(1.75279798770009,-3.52836018667712,42.));
#32473=CARTESIAN_POINT('Ctrl Pts',(1.82143554149094,-3.48681209294754,42.0000000000001));
#32474=CARTESIAN_POINT('Ctrl Pts',(1.8885815825096,-3.44308219441033,42.0000000000001));
#32475=CARTESIAN_POINT('Ctrl Pts',(1.95412305121373,-3.3971702788484,42.0000000000001));
#32476=CARTESIAN_POINT('Ctrl Pts',(2.05256290803176,-3.32821298381799,42.0000000000001));
#32477=CARTESIAN_POINT('Ctrl Pts',(2.14738503498556,-3.25433510156145,42.0000000000001));
#32478=CARTESIAN_POINT('Ctrl Pts',(2.23843406813092,-3.17595253897366,42.));
#32479=CARTESIAN_POINT('Ctrl Pts',(2.33061707260172,-3.09659375977688,42.));
#32480=CARTESIAN_POINT('Ctrl Pts',(2.41893285168275,-3.01261656500042,42.));
#32481=CARTESIAN_POINT('Ctrl Pts',(2.50317836884662,-2.92441884813481,42.));
#32482=CARTESIAN_POINT('Ctrl Pts',(2.58733330463444,-2.83631596207834,42.));
#32483=CARTESIAN_POINT('Ctrl Pts',(2.66742707573242,-2.74400073281455,42.));
#32484=CARTESIAN_POINT('Ctrl Pts',(2.74321006647546,-2.64784937809448,42.));
#32485=CARTESIAN_POINT('Ctrl Pts',(2.77126704941009,-2.61225145708249,42.));
#32486=CARTESIAN_POINT('Ctrl Pts',(2.79873266663842,-2.5761275893848,42.));
#32487=CARTESIAN_POINT('Ctrl Pts',(2.82559245821946,-2.53949653137926,42.));
#32488=CARTESIAN_POINT('Ctrl Pts',(2.83828839352235,-2.52218196878813,42.));
#32489=CARTESIAN_POINT('Ctrl Pts',(2.85085105627574,-2.50475098317605,42.));
#32490=CARTESIAN_POINT('Ctrl Pts',(2.86326365969319,-2.48722741801918,42.));
#32491=CARTESIAN_POINT('Ctrl Pts',(2.93259154223295,-2.38935337612672,42.));
#32492=CARTESIAN_POINT('Ctrl Pts',(2.99733691489821,-2.28846731280446,42.));
#32493=CARTESIAN_POINT('Ctrl Pts',(3.05733405014049,-2.18496333662957,42.));
#32494=CARTESIAN_POINT('Ctrl Pts',(3.1172049553746,-2.08167712598138,42.));
#32495=CARTESIAN_POINT('Ctrl Pts',(3.17234788189958,-1.975783114258,42.));
#32496=CARTESIAN_POINT('Ctrl Pts',(3.22255028201254,-1.86765340308612,42.));
#32497=CARTESIAN_POINT('Ctrl Pts',(3.27167533988857,-1.76184415278164,42.));
#32498=CARTESIAN_POINT('Ctrl Pts',(3.31606975722882,-1.65389331291347,42.));
#32499=CARTESIAN_POINT('Ctrl Pts',(3.35548570303569,-1.54414347432169,42.));
#32500=CARTESIAN_POINT('Ctrl Pts',(3.38624649344917,-1.45849306777363,41.9999999999999));
#32501=CARTESIAN_POINT('Ctrl Pts',(3.41397424609095,-1.3717467549663,42.));
#32502=CARTESIAN_POINT('Ctrl Pts',(3.43852910267749,-1.28406938692554,42.));
#32503=CARTESIAN_POINT('Ctrl Pts',(3.44533961773349,-1.25975126342081,42.));
#32504=CARTESIAN_POINT('Ctrl Pts',(3.45190592873417,-1.23536153850306,42.));
#32505=CARTESIAN_POINT('Ctrl Pts',(3.45822477341065,-1.21090379238842,42.));
#32506=CARTESIAN_POINT('Ctrl Pts',(3.46235621786795,-1.19491260653134,42.));
#32507=CARTESIAN_POINT('Ctrl Pts',(3.4663797310686,-1.17890055560633,42.));
#32508=CARTESIAN_POINT('Ctrl Pts',(3.47029389106376,-1.16287225647867,42.));
#32509=CARTESIAN_POINT('Ctrl Pts',(3.49750979687016,-1.05142441586034,42.));
#32510=CARTESIAN_POINT('Ctrl Pts',(3.5194575163352,-0.939135267477813,42.));
#32511=CARTESIAN_POINT('Ctrl Pts',(3.5359436815247,-0.826341686230967,41.9999999999999));
#32512=CARTESIAN_POINT('Ctrl Pts',(3.55198728298497,-0.716575998213669,
42.));
#32513=CARTESIAN_POINT('Ctrl Pts',(3.56285862720728,-0.606331891956589,
42.));
#32514=CARTESIAN_POINT('Ctrl Pts',(3.56833123257986,-0.495921126813228,
42.));
#32515=CARTESIAN_POINT('Ctrl Pts',(3.57365916987809,-0.388429065229428,
42.));
#32516=CARTESIAN_POINT('Ctrl Pts',(3.57387001615029,-0.280778481168261,
41.9999999999999));
#32517=CARTESIAN_POINT('Ctrl Pts',(3.56870842791254,-0.173267408887965,
42.));
#32518=CARTESIAN_POINT('Ctrl Pts',(3.5653222936604,-0.102737388366562,42.));
#32519=CARTESIAN_POINT('Ctrl Pts',(3.55962285067617,-0.0322676353425919,
42.));
#32520=CARTESIAN_POINT('Ctrl Pts',(3.55165143284768,0.0380520659533637,
42.));
#32521=CARTESIAN_POINT('Ctrl Pts',(3.54710154953435,0.0781887696624734,
42.));
#32522=CARTESIAN_POINT('Ctrl Pts',(3.54181137670787,0.118276518513767,42.));
#32523=CARTESIAN_POINT('Ctrl Pts',(3.53578772847455,0.158297966652038,42.));
#32524=CARTESIAN_POINT('Ctrl Pts',(3.53344572120281,0.173858390988625,42.));
#32525=CARTESIAN_POINT('Ctrl Pts',(3.53099300975283,0.18940721262173,42.));
#32526=CARTESIAN_POINT('Ctrl Pts',(3.52843217698487,0.204931472988267,42.));
#32527=CARTESIAN_POINT('Ctrl Pts',(3.51031326577749,0.314771794722974,42.));
#32528=CARTESIAN_POINT('Ctrl Pts',(3.48676167369221,0.42354871924747,42.));
#32529=CARTESIAN_POINT('Ctrl Pts',(3.45802915101404,0.530939049228676,42.));
#32530=CARTESIAN_POINT('Ctrl Pts',(3.42903674042542,0.639300733127319,42.));
#32531=CARTESIAN_POINT('Ctrl Pts',(3.39476873131307,0.746251421507866,42.));
#32532=CARTESIAN_POINT('Ctrl Pts',(3.35543440096621,0.851438324429188,42.));
#32533=CARTESIAN_POINT('Ctrl Pts',(3.31638563898292,0.955861567426199,42.));
#32534=CARTESIAN_POINT('Ctrl Pts',(3.27234323949019,1.05854724171231,42.));
#32535=CARTESIAN_POINT('Ctrl Pts',(3.22347219448623,1.15911873378746,42.));
#32536=CARTESIAN_POINT('Ctrl Pts',(3.18696786157772,1.23424082760639,42.));
#32537=CARTESIAN_POINT('Ctrl Pts',(3.14776858641996,1.30818275664874,42.));
#32538=CARTESIAN_POINT('Ctrl Pts',(3.10593149822866,1.3807724923263,42.));
#32539=CARTESIAN_POINT('Ctrl Pts',(3.09665122555106,1.39687429505223,42.));
#32540=CARTESIAN_POINT('Ctrl Pts',(3.08724034026875,1.41291082564143,42.));
#32541=CARTESIAN_POINT('Ctrl Pts',(3.07770186971861,1.42887599560449,42.));
#32542=CARTESIAN_POINT('Ctrl Pts',(3.02142512756762,1.52307010656646,42.));
#32543=CARTESIAN_POINT('Ctrl Pts',(2.96086891636547,1.61451905005572,42.));
#32544=CARTESIAN_POINT('Ctrl Pts',(2.8962164722944,1.70287781084587,42.));
#32545=CARTESIAN_POINT('Ctrl Pts',(2.83191557546761,1.79075612144872,42.));
#32546=CARTESIAN_POINT('Ctrl Pts',(2.76356229636571,1.87557839552669,42.));
#32547=CARTESIAN_POINT('Ctrl Pts',(2.69130548220896,1.95696485393201,42.));
#32548=CARTESIAN_POINT('Ctrl Pts',(2.66190509140716,1.9900799823945,42.));
#32549=CARTESIAN_POINT('Ctrl Pts',(2.63185812650358,2.02262576678383,42.));
#32550=CARTESIAN_POINT('Ctrl Pts',(2.60117344348306,2.05457433130465,42.));
#32551=CARTESIAN_POINT('Ctrl Pts',(2.58410938875368,2.07234124299619,42.));
#32552=CARTESIAN_POINT('Ctrl Pts',(2.56684810362444,2.08992343448043,42.));
#32553=CARTESIAN_POINT('Ctrl Pts',(2.54939103594971,2.10731591519684,42.));
#32554=CARTESIAN_POINT('Ctrl Pts',(2.53487042035394,2.12178280800183,42.));
#32555=CARTESIAN_POINT('Ctrl Pts',(2.5202196449902,2.13611310176088,42.));
#32556=CARTESIAN_POINT('Ctrl Pts',(2.50544496557298,2.15029937598748,42.));
#32557=CARTESIAN_POINT('Ctrl Pts',(2.42926706246224,2.22344347563389,42.));
#32558=CARTESIAN_POINT('Ctrl Pts',(2.34975495167501,2.29280482501271,42.));
#32559=CARTESIAN_POINT('Ctrl Pts',(2.26705277020889,2.3580370020813,42.));
#32560=CARTESIAN_POINT('Ctrl Pts',(2.18660232836131,2.42149309688814,42.));
#32561=CARTESIAN_POINT('Ctrl Pts',(2.10313261859417,2.48104212527174,42.));
#32562=CARTESIAN_POINT('Ctrl Pts',(2.01675730739135,2.53632015288963,42.));
#32563=CARTESIAN_POINT('Ctrl Pts',(1.96924090736295,2.56672945430337,42.));
#32564=CARTESIAN_POINT('Ctrl Pts',(1.9208449031706,2.59584540845355,42.));
#32565=CARTESIAN_POINT('Ctrl Pts',(1.87158653173888,2.62360084935068,42.));
#32566=CARTESIAN_POINT('Ctrl Pts',(1.87561947885753,2.62751737394877,7.));
#32567=CARTESIAN_POINT('Ctrl Pts',(1.93354269965564,2.59525298287931,7.));
#32568=CARTESIAN_POINT('Ctrl Pts',(1.9902828570607,2.5611368520897,7.));
#32569=CARTESIAN_POINT('Ctrl Pts',(2.04574146644465,2.52519262124126,7.));
#32570=CARTESIAN_POINT('Ctrl Pts',(2.13162955029859,2.46952622160611,7.));
#32571=CARTESIAN_POINT('Ctrl Pts',(2.21444518497691,2.40947818555694,7.));
#32572=CARTESIAN_POINT('Ctrl Pts',(2.29410632613084,2.34545806303941,7.));
#32573=CARTESIAN_POINT('Ctrl Pts',(2.37532784153249,2.28018393701321,7.));
#32574=CARTESIAN_POINT('Ctrl Pts',(2.45327056143154,2.2107801777211,7.));
#32575=CARTESIAN_POINT('Ctrl Pts',(2.52782839274206,2.13762915775039,7.));
#32576=CARTESIAN_POINT('Ctrl Pts',(2.58531053735377,2.08123162801354,7.));
#32577=CARTESIAN_POINT('Ctrl Pts',(2.64078037491381,2.02260559094313,7.00000000000001));
#32578=CARTESIAN_POINT('Ctrl Pts',(2.69417895438683,1.96190848496968,7.00000000000001));
#32579=CARTESIAN_POINT('Ctrl Pts',(2.72087824412334,1.93155993198295,7.00000000000001));
#32580=CARTESIAN_POINT('Ctrl Pts',(2.74705956481114,1.90069338875978,7.));
#32581=CARTESIAN_POINT('Ctrl Pts',(2.7727145409719,1.86932730444631,7.));
#32582=CARTESIAN_POINT('Ctrl Pts',(2.78884149611167,1.84961029393483,7.));
#32583=CARTESIAN_POINT('Ctrl Pts',(2.80476051079127,1.82969580151675,7.));
#32584=CARTESIAN_POINT('Ctrl Pts',(2.82046926811514,1.80958836864072,7.));
#32585=CARTESIAN_POINT('Ctrl Pts',(2.82975021226723,1.79770862807838,7.));
#32586=CARTESIAN_POINT('Ctrl Pts',(2.83895676410696,1.78576273312009,7.));
#32587=CARTESIAN_POINT('Ctrl Pts',(2.84808162916198,1.77376089666299,7.));
#32588=CARTESIAN_POINT('Ctrl Pts',(2.91426843550152,1.68670610511091,7.));
#32589=CARTESIAN_POINT('Ctrl Pts',(2.97625815391462,1.5965866592015,7.00000000000001));
#32590=CARTESIAN_POINT('Ctrl Pts',(3.03395162804767,1.5038370359648,7.));
#32591=CARTESIAN_POINT('Ctrl Pts',(3.09256315555186,1.40961152476044,7.));
#32592=CARTESIAN_POINT('Ctrl Pts',(3.14674118550069,1.31267085407981,7.));
#32593=CARTESIAN_POINT('Ctrl Pts',(3.19635279807365,1.21342385387171,7.));
#32594=CARTESIAN_POINT('Ctrl Pts',(3.24632307395247,1.11345935517188,7.));
#32595=CARTESIAN_POINT('Ctrl Pts',(3.29166123872158,1.01115432229022,7.00000000000001));
#32596=CARTESIAN_POINT('Ctrl Pts',(3.33219378964199,0.906889812914124,7.00000000000001));
#32597=CARTESIAN_POINT('Ctrl Pts',(3.36732095539704,0.816529926352442,7.00000000000001));
#32598=CARTESIAN_POINT('Ctrl Pts',(3.39883841274255,0.724697453060791,7.));
#32599=CARTESIAN_POINT('Ctrl Pts',(3.42660553724382,0.631625023031459,7.00000000000001));
#32600=CARTESIAN_POINT('Ctrl Pts',(3.4306454355836,0.618083716097167,7.00000000000001));
#32601=CARTESIAN_POINT('Ctrl Pts',(3.43460534260238,0.604517877724185,7.00000000000001));
#32602=CARTESIAN_POINT('Ctrl Pts',(3.4384824016501,0.590937153688084,7.00000000000001));
#32603=CARTESIAN_POINT('Ctrl Pts',(3.47005153049162,0.480355493316353,7.));
#32604=CARTESIAN_POINT('Ctrl Pts',(3.49618019043182,0.36862583872353,7.00000000000001));
#32605=CARTESIAN_POINT('Ctrl Pts',(3.51673404290034,0.256178310679654,7.00000000000001));
#32606=CARTESIAN_POINT('Ctrl Pts',(3.53722278462116,0.144086995303895,7.00000000000001));
#32607=CARTESIAN_POINT('Ctrl Pts',(3.55217247491514,0.0312815018845697,
7.00000000000001));
#32608=CARTESIAN_POINT('Ctrl Pts',(3.56140843844997,-0.0818418576713709,
7.00000000000001));
#32609=CARTESIAN_POINT('Ctrl Pts',(3.56994121560687,-0.186352493155338,
7.00000000000001));
#32610=CARTESIAN_POINT('Ctrl Pts',(3.57359707077813,-0.291135254734413,
7.00000000000001));
#32611=CARTESIAN_POINT('Ctrl Pts',(3.5722009810671,-0.395890897501032,7.00000000000001));
#32612=CARTESIAN_POINT('Ctrl Pts',(3.57116150285243,-0.473888183534262,
7.00000000000001));
#32613=CARTESIAN_POINT('Ctrl Pts',(3.56732059981105,-0.551870737087469,
7.00000000000001));
#32614=CARTESIAN_POINT('Ctrl Pts',(3.56075400606168,-0.629740882624065,
7.00000000000001));
#32615=CARTESIAN_POINT('Ctrl Pts',(3.55856368150232,-0.655714910974234,
7.00000000000001));
#32616=CARTESIAN_POINT('Ctrl Pts',(3.55606999420635,-0.681676435082942,
7.00000000000001));
#32617=CARTESIAN_POINT('Ctrl Pts',(3.55327544641143,-0.707621825224809,
7.00000000000001));
#32618=CARTESIAN_POINT('Ctrl Pts',(3.55068069240703,-0.731712272018656,
7.00000000000001));
#32619=CARTESIAN_POINT('Ctrl Pts',(3.54782600396051,-0.755791644275436,
7.00000000000001));
#32620=CARTESIAN_POINT('Ctrl Pts',(3.54471830098374,-0.779822457946214,
7.00000000000001));
#32621=CARTESIAN_POINT('Ctrl Pts',(3.53000284143865,-0.893612118364699,
7.00000000000001));
#32622=CARTESIAN_POINT('Ctrl Pts',(3.50960228158218,-1.00648399764322,7.));
#32623=CARTESIAN_POINT('Ctrl Pts',(3.48384809250374,-1.11812566925976,7.));
#32624=CARTESIAN_POINT('Ctrl Pts',(3.45807685458176,-1.22984124580054,7.));
#32625=CARTESIAN_POINT('Ctrl Pts',(3.42694460602159,-1.34032567693087,7.00000000000001));
#32626=CARTESIAN_POINT('Ctrl Pts',(3.39072803041029,-1.44927444241835,7.));
#32627=CARTESIAN_POINT('Ctrl Pts',(3.35380189025642,-1.5603577603764,7.));
#32628=CARTESIAN_POINT('Ctrl Pts',(3.31159010115209,-1.6698454102589,7.));
#32629=CARTESIAN_POINT('Ctrl Pts',(3.26433136408276,-1.77741247295867,7.));
#32630=CARTESIAN_POINT('Ctrl Pts',(3.21898084301654,-1.88063618661486,7.));
#32631=CARTESIAN_POINT('Ctrl Pts',(3.16898212705041,-1.98209189032465,7.));
#32632=CARTESIAN_POINT('Ctrl Pts',(3.11450263572912,-2.08148053262523,7.));
#32633=CARTESIAN_POINT('Ctrl Pts',(3.10547063707986,-2.09795789064087,7.));
#32634=CARTESIAN_POINT('Ctrl Pts',(3.09631995779018,-2.11437003247308,7.));
#32635=CARTESIAN_POINT('Ctrl Pts',(3.08705342909664,-2.13071264965695,7.));
#32636=CARTESIAN_POINT('Ctrl Pts',(3.02764224096765,-2.23549129289445,7.));
#32637=CARTESIAN_POINT('Ctrl Pts',(2.96345098277208,-2.33745331367609,7.));
#32638=CARTESIAN_POINT('Ctrl Pts',(2.89475462679644,-2.43626425908663,7.));
#32639=CARTESIAN_POINT('Ctrl Pts',(2.825598931564,-2.53573590542643,7.));
#32640=CARTESIAN_POINT('Ctrl Pts',(2.7518773740215,-2.63201502957476,7.));
#32641=CARTESIAN_POINT('Ctrl Pts',(2.67381996723917,-2.72474601970096,7.));
#32642=CARTESIAN_POINT('Ctrl Pts',(2.6386340070233,-2.76654639539699,7.));
#32643=CARTESIAN_POINT('Ctrl Pts',(2.60256637930229,-2.80762554190717,7.));
#32644=CARTESIAN_POINT('Ctrl Pts',(2.56563509704846,-2.84794923462997,7.));
#32645=CARTESIAN_POINT('Ctrl Pts',(2.54298515597624,-2.87267973972611,7.));
#32646=CARTESIAN_POINT('Ctrl Pts',(2.52000527689653,-2.89713102952822,7.));
#32647=CARTESIAN_POINT('Ctrl Pts',(2.49672981813975,-2.92126413124198,7.));
#32648=CARTESIAN_POINT('Ctrl Pts',(2.411100096883,-3.01004909545701,7.));
#32649=CARTESIAN_POINT('Ctrl Pts',(2.32140840071681,-3.09460368152808,7.));
#32650=CARTESIAN_POINT('Ctrl Pts',(2.22790870923994,-3.17457235277157,7.));
#32651=CARTESIAN_POINT('Ctrl Pts',(2.13564011139915,-3.25348809089092,7.));
#32652=CARTESIAN_POINT('Ctrl Pts',(2.03966265549336,-3.32793863516635,7.));
#32653=CARTESIAN_POINT('Ctrl Pts',(1.94017790140973,-3.39755587824315,7.));
#32654=CARTESIAN_POINT('Ctrl Pts',(1.87771921844902,-3.44126309101144,7.));
#32655=CARTESIAN_POINT('Ctrl Pts',(1.81387727843869,-3.48306464631677,7.));
#32656=CARTESIAN_POINT('Ctrl Pts',(1.74869447533099,-3.52286199445094,7.));
#32657=CARTESIAN_POINT('Ctrl Pts',(-2.28358776666034,3.20569428094324,6.5881335146371));
#32658=CARTESIAN_POINT('Ctrl Pts',(-3.35286492248133,2.44407649255814,6.65448899198165));
#32659=CARTESIAN_POINT('Ctrl Pts',(-4.64957922564859,-0.219617924792526,
6.78715544878067));
#32660=CARTESIAN_POINT('Ctrl Pts',(-2.32229699647965,-4.03879127370882,
6.98613288503415));
#32661=CARTESIAN_POINT('Ctrl Pts',(2.14152197144423,-4.13253673306908,7.18506582339759));
#32662=CARTESIAN_POINT('Ctrl Pts',(4.6354962344389,-0.433054729749735,7.38399876176103));
#32663=CARTESIAN_POINT('Ctrl Pts',(2.86863005376323,3.66754880853003,7.58293170012447));
#32664=CARTESIAN_POINT('Ctrl Pts',(-1.53568971473972,4.39499028421212,7.7818646384879));
#32665=CARTESIAN_POINT('Ctrl Pts',(-4.52808181481838,1.08291459320159,7.98079757685135));
#32666=CARTESIAN_POINT('Ctrl Pts',(-3.35787183100746,-3.22511561142074,
8.17973051521478));
#32667=CARTESIAN_POINT('Ctrl Pts',(0.899288778474051,-4.56806013476469,
8.37866345357823));
#32668=CARTESIAN_POINT('Ctrl Pts',(4.32970627742076,-1.7116822031998,8.57759639194166));
#32669=CARTESIAN_POINT('Ctrl Pts',(3.77981709720475,2.71831339521054,8.77652933030509));
#32670=CARTESIAN_POINT('Ctrl Pts',(-0.244881287865563,4.64931963845551,
8.97546226866854));
#32671=CARTESIAN_POINT('Ctrl Pts',(-4.04445595226873,2.30620171359066,9.17439520703196));
#32672=CARTESIAN_POINT('Ctrl Pts',(-4.12594562258144,-2.15702647441609,
9.37332814539542));
#32673=CARTESIAN_POINT('Ctrl Pts',(-0.414433902178747,-4.63728597633392,
9.57226108375884));
#32674=CARTESIAN_POINT('Ctrl Pts',(3.6780683225737,-2.85446979798575,9.77119402212229));
#32675=CARTESIAN_POINT('Ctrl Pts',(4.38930591019076,1.55247461807464,9.97012696048572));
#32676=CARTESIAN_POINT('Ctrl Pts',(1.06543455816436,4.53222144777138,10.1690598988492));
#32677=CARTESIAN_POINT('Ctrl Pts',(-3.23789554621589,3.34547689252468,10.3679928372126));
#32678=CARTESIAN_POINT('Ctrl Pts',(-4.56461363563294,-0.916779903504382,
10.566925775576));
#32679=CARTESIAN_POINT('Ctrl Pts',(-1.69506170633405,-4.33623668960493,
10.7658587139395));
#32680=CARTESIAN_POINT('Ctrl Pts',(2.73276812195122,-3.76937148311671,10.9647916523029));
#32681=CARTESIAN_POINT('Ctrl Pts',(4.64835183630865,0.262694034166192,11.1637245906663));
#32682=CARTESIAN_POINT('Ctrl Pts',(2.29068463981999,4.05326372260543,11.3626575290298));
#32683=CARTESIAN_POINT('Ctrl Pts',(-2.17281932557235,4.11764970909905,11.5615904673932));
#32684=CARTESIAN_POINT('Ctrl Pts',(-4.63884063895772,0.396661654349383,
11.7605234057567));
#32685=CARTESIAN_POINT('Ctrl Pts',(-2.84035473048496,-3.68897925500734,
11.9594563441201));
#32686=CARTESIAN_POINT('Ctrl Pts',(1.56928215333904,-4.38332481861607,12.1583892824835));
#32687=CARTESIAN_POINT('Ctrl Pts',(4.53627084208731,-1.04806001180736,12.357322220847));
#32688=CARTESIAN_POINT('Ctrl Pts',(3.33304518836854,3.25069111315414,12.5562551592104));
#32689=CARTESIAN_POINT('Ctrl Pts',(-0.934264011548026,4.56106716657885,
12.7551880975738));
#32690=CARTESIAN_POINT('Ctrl Pts',(-4.34270007180307,1.67843350404123,12.9541210359373));
#32691=CARTESIAN_POINT('Ctrl Pts',(-3.75887227597289,-2.74719168498093,
13.1530539743007));
#32692=CARTESIAN_POINT('Ctrl Pts',(0.280503837458128,-4.6473111084089,13.3519869126642));
#32693=CARTESIAN_POINT('Ctrl Pts',(4.0620115019401,-2.27513636937342,13.5509198510276));
#32694=CARTESIAN_POINT('Ctrl Pts',(4.10929358463094,2.18858154439125,13.749852789391));
#32695=CARTESIAN_POINT('Ctrl Pts',(0.378883452643525,4.64032652627596,13.9487857277545));
#32696=CARTESIAN_POINT('Ctrl Pts',(-3.6998359543678,2.82619830371296,14.1477186661179));
#32697=CARTESIAN_POINT('Ctrl Pts',(-4.37727940176434,-1.5860668271018,14.3466516044813));
#32698=CARTESIAN_POINT('Ctrl Pts',(-1.03067005834432,-4.54025353608988,
14.5455845428448));
#32699=CARTESIAN_POINT('Ctrl Pts',(3.26343894045982,-3.32056459401619,14.7445174812082));
#32700=CARTESIAN_POINT('Ctrl Pts',(4.55745373218093,0.951734427334463,14.9434504195717));
#32701=CARTESIAN_POINT('Ctrl Pts',(1.66178065462684,4.34909967660568,15.1423833579351));
#32702=CARTESIAN_POINT('Ctrl Pts',(-2.7615749095149,3.74831788410233,15.3413162962985));
#32703=CARTESIAN_POINT('Ctrl Pts',(-4.64620214454805,-0.298309525729033,
15.540249234662));
#32704=CARTESIAN_POINT('Ctrl Pts',(-2.25955469263049,-4.07069963669087,
15.7391821730254));
#32705=CARTESIAN_POINT('Ctrl Pts',(2.20431162797926,-4.10087712421368,15.9381151113889));
#32706=CARTESIAN_POINT('Ctrl Pts',(4.64174427957893,-0.361099687260673,
16.1370480497523));
#32707=CARTESIAN_POINT('Ctrl Pts',(2.81200037969602,3.71063832860775,16.3359809881157));
#32708=CARTESIAN_POINT('Ctrl Pts',(-1.60282821254903,4.37116971326904,16.5349139264792));
#32709=CARTESIAN_POINT('Ctrl Pts',(-4.54416956536685,1.01326497143505,16.7338468648426));
#32710=CARTESIAN_POINT('Ctrl Pts',(-3.30803524366227,-3.27613885051165,
16.932779803206));
#32711=CARTESIAN_POINT('Ctrl Pts',(0.969190868759014,-4.55377338051179,
17.1317127415695));
#32712=CARTESIAN_POINT('Ctrl Pts',(4.35543542339085,-1.6451034052046,17.3306456799329));
#32713=CARTESIAN_POINT('Ctrl Pts',(3.73770845551644,2.77591758571908,17.5295786182963));
#32714=CARTESIAN_POINT('Ctrl Pts',(-0.316110833907594,4.64502496030214,
17.7285115566598));
#32715=CARTESIAN_POINT('Ctrl Pts',(-4.07932800118232,2.24393983874646,17.9274444950232));
#32716=CARTESIAN_POINT('Ctrl Pts',(-4.09240045043936,-2.22000934556306,
18.1263774333867));
#32717=CARTESIAN_POINT('Ctrl Pts',(-0.343310619835542,-4.64309387794946,
18.3253103717501));
#32718=CARTESIAN_POINT('Ctrl Pts',(3.72138621938403,-2.79776116695515,18.5242433101136));
#32719=CARTESIAN_POINT('Ctrl Pts',(4.36499584269893,1.61956606359996,18.723176248477));
#32720=CARTESIAN_POINT('Ctrl Pts',(0.995845006712163,4.54801887240478,18.9221091868404));
#32721=CARTESIAN_POINT('Ctrl Pts',(-3.28879065687452,3.29545732128312,19.1210421252039));
#32722=CARTESIAN_POINT('Ctrl Pts',(-4.55002616559029,-0.986633079511998,
19.3199750635673));
#32723=CARTESIAN_POINT('Ctrl Pts',(-1.62840200065756,-4.36170721912855,
19.5189080019307));
#32724=CARTESIAN_POINT('Ctrl Pts',(2.79021950300484,-3.72704414599493,19.7178409402942));
#32725=CARTESIAN_POINT('Ctrl Pts',(4.64377957295296,0.333907500617121,19.9167738786576));
#32726=CARTESIAN_POINT('Ctrl Pts',(2.22829203699626,4.08789646872357,20.115706817021));
#32727=CARTESIAN_POINT('Ctrl Pts',(-2.23567446665327,4.08386368777145,20.3146397553845));
#32728=CARTESIAN_POINT('Ctrl Pts',(-4.6443753015709,0.325516511565617,20.5135726937479));
#32729=CARTESIAN_POINT('Ctrl Pts',(-2.78348087456552,-3.73207946888481,
20.7125056321114));
#32730=CARTESIAN_POINT('Ctrl Pts',(1.63628013449202,-4.35875788070528,20.9114385704748));
#32731=CARTESIAN_POINT('Ctrl Pts',(4.55180140068407,-0.978410419953773,
21.1103715088382));
#32732=CARTESIAN_POINT('Ctrl Pts',(3.28283101156097,3.30139417378129,21.3093044472017));
#32733=CARTESIAN_POINT('Ctrl Pts',(-1.00406080348858,4.54621214243697,21.5082373855651));
#32734=CARTESIAN_POINT('Ctrl Pts',(-4.36791497172966,1.61167668621328,21.7071703239285));
#32735=CARTESIAN_POINT('Ctrl Pts',(-3.71632511212236,-2.80448045137639,
21.906103262292));
#32736=CARTESIAN_POINT('Ctrl Pts',(0.351699264548243,-4.64246600078663,
22.1050362006554));
#32737=CARTESIAN_POINT('Ctrl Pts',(4.0964049135034,-2.21261151713735,22.3039691390189));
#32738=CARTESIAN_POINT('Ctrl Pts',(4.07526696155566,2.25130676123813,22.5029020773823));
#32739=CARTESIAN_POINT('Ctrl Pts',(0.307717623722685,4.64558853162805,22.7018350157458));
#32740=CARTESIAN_POINT('Ctrl Pts',(-3.74271792010062,2.76915971220537,22.9007679541091));
#32741=CARTESIAN_POINT('Ctrl Pts',(-4.35245591888036,-1.65297017981175,
23.0997008924726));
#32742=CARTESIAN_POINT('Ctrl Pts',(-0.96096146715276,-4.55551709466568,
23.298633830836));
#32743=CARTESIAN_POINT('Ctrl Pts',(3.31394921617401,-3.27015649988854,23.4975667691995));
#32744=CARTESIAN_POINT('Ctrl Pts',(4.54233136705332,1.02147378479679,23.6964997075629));
#32745=CARTESIAN_POINT('Ctrl Pts',(1.59492770745015,4.37405859004556,23.8954326459263));
#32746=CARTESIAN_POINT('Ctrl Pts',(-2.8187002214397,3.70555151128673,24.0943655842898));
#32747=CARTESIAN_POINT('Ctrl Pts',(-4.64108426309036,-0.369485864463859,
24.2932985226532));
#32748=CARTESIAN_POINT('Ctrl Pts',(-2.19689850940736,-4.10485321059198,
24.4922314610167));
#32749=CARTESIAN_POINT('Ctrl Pts',(2.26690599978809,-4.06661039801803,24.6911643993801));
#32750=CARTESIAN_POINT('Ctrl Pts',(4.64673355030702,-0.289914217648445,
24.8900973377435));
#32751=CARTESIAN_POINT('Ctrl Pts',(2.75479789015282,3.75330141682668,25.089030276107));
#32752=CARTESIAN_POINT('Ctrl Pts',(-1.66963595449858,4.34609004975612,25.2879632144704));
#32753=CARTESIAN_POINT('Ctrl Pts',(-4.55916589979193,0.943498404512721,
25.4868961528339));
#32754=CARTESIAN_POINT('Ctrl Pts',(-3.25743397236614,-3.32645559970645,
25.6858290911973));
#32755=CARTESIAN_POINT('Ctrl Pts',(1.03887176776102,-4.5383838964209,25.8847620295608));
#32756=CARTESIAN_POINT('Ctrl Pts',(4.38013798386919,-1.57815531029427,26.0836949679242));
#32757=CARTESIAN_POINT('Ctrl Pts',(3.69472350167733,2.8328786044052,26.2826279062876));
#32758=CARTESIAN_POINT('Ctrl Pts',(-0.387267039202406,4.63963438015227,
26.4815608446511));
#32759=CARTESIAN_POINT('Ctrl Pts',(-4.11324123594255,2.18115324452121,26.6804937830145));
#32760=CARTESIAN_POINT('Ctrl Pts',(-4.05789412426333,-2.28247195325872,
26.8794267213779));
#32761=CARTESIAN_POINT('Ctrl Pts',(-0.272106554751227,-4.64781034079544,
27.0783596597414));
#32762=CARTESIAN_POINT('Ctrl Pts',(3.76382980366497,-2.74039561928326,27.2772925981048));
#32763=CARTESIAN_POINT('Ctrl Pts',(4.33966036680293,1.68627721384812,27.4762255364683));
#32764=CARTESIAN_POINT('Ctrl Pts',(0.926021488444692,4.56274776248724,27.6751584748317));
#32765=CARTESIAN_POINT('Ctrl Pts',(-3.33891314074683,3.24466361579928,27.8740914131951));
#32766=CARTESIAN_POINT('Ctrl Pts',(-4.53436978850062,-1.056254496926,28.0730243515586));
#32767=CARTESIAN_POINT('Ctrl Pts',(-1.56135974101536,-4.38615306393655,
28.271957289922));
#32768=CARTESIAN_POINT('Ctrl Pts',(2.84701539209114,-3.68384124228226,28.4708902282854));
#32769=CARTESIAN_POINT('Ctrl Pts',(4.63811637326107,0.405042527682263,28.6698231666489));
#32770=CARTESIAN_POINT('Ctrl Pts',(2.16537595366717,4.12156886639343,28.8687561050123));
#32771=CARTESIAN_POINT('Ctrl Pts',(-2.29800439309459,4.04911826827293,29.0676890433758));
#32772=CARTESIAN_POINT('Ctrl Pts',(-4.64881888728275,0.254294896501576,
29.2666219817392));
#32773=CARTESIAN_POINT('Ctrl Pts',(-2.72595311106574,-3.77430292602682,
29.4655549201026));
#32774=CARTESIAN_POINT('Ctrl Pts',(1.70289371351612,-4.33316696442807,29.6644878584661));
#32775=CARTESIAN_POINT('Ctrl Pts',(4.56626263015895,-0.908530975562921,
29.8634207968295));
#32776=CARTESIAN_POINT('Ctrl Pts',(3.23184561769564,3.35132165638052,30.0623537351929));
#32777=CARTESIAN_POINT('Ctrl Pts',(-1.07362171706024,4.53028910223179,30.2612866735564));
#32778=CARTESIAN_POINT('Ctrl Pts',(-4.39210374192795,1.54454124622366,30.4602196119198));
#32779=CARTESIAN_POINT('Ctrl Pts',(-3.67290489288628,-2.86111037692635,
30.6591525502832));
#32780=CARTESIAN_POINT('Ctrl Pts',(0.422812068905003,-4.63653026470569,
30.8580854886467));
#32781=CARTESIAN_POINT('Ctrl Pts',(4.12983597966957,-2.14956686850405,31.0570184270101));
#32782=CARTESIAN_POINT('Ctrl Pts',(4.04028295890316,2.31350309123207,31.2559513653736));
#32783=CARTESIAN_POINT('Ctrl Pts',(0.236479504429024,4.64975917496042,31.454884303737));
#32784=CARTESIAN_POINT('Ctrl Pts',(-3.78472063013482,2.71147057756036,31.6538172421005));
#32785=CARTESIAN_POINT('Ctrl Pts',(-4.32660993797449,-1.71948520952171,
31.8527501804639));
#32786=CARTESIAN_POINT('Ctrl Pts',(-0.891027122681378,-4.56971045119814,
32.0516831188273));
#32787=CARTESIAN_POINT('Ctrl Pts',(3.36368096441276,-3.21898016626241,32.2506160571907));
#32788=CARTESIAN_POINT('Ctrl Pts',(4.5261418975313,1.09097317316021,32.4495489955542));
#32789=CARTESIAN_POINT('Ctrl Pts',(1.52770007286572,4.39798993046933,32.6484819339176));
#32790=CARTESIAN_POINT('Ctrl Pts',(-2.87516335195365,3.66191461406821,32.8474148722811));
#32791=CARTESIAN_POINT('Ctrl Pts',(-4.63487607777506,-0.4405754019598,33.0463478106445));
#32792=CARTESIAN_POINT('Ctrl Pts',(-2.13372622115719,-4.13804245438466,
33.245280749008));
#32793=CARTESIAN_POINT('Ctrl Pts',(2.3289678201032,-4.03138832588321,33.4442136873714));
#32794=CARTESIAN_POINT('Ctrl Pts',(4.65063119002216,-0.218660640117578,
33.6431466257348));
#32795=CARTESIAN_POINT('Ctrl Pts',(2.69694823141472,3.79508276302539,33.8420795640982));
#32796=CARTESIAN_POINT('Ctrl Pts',(-1.73605145825132,4.31998938371931,34.0410125024617));
#32797=CARTESIAN_POINT('Ctrl Pts',(-4.57309117498029,0.873510186809756,
34.2399454408251));
#32798=CARTESIAN_POINT('Ctrl Pts',(-3.20606745040362,-3.37599088337116,
34.4388783791886));
#32799=CARTESIAN_POINT('Ctrl Pts',(1.10830861045392,-4.52192823529311,34.637811317552));
#32800=CARTESIAN_POINT('Ctrl Pts',(4.4038115431333,-1.51083646822047,34.8367442559154));
#32801=CARTESIAN_POINT('Ctrl Pts',(3.65087056719927,2.88917411083122,35.0356771942789));
#32802=CARTESIAN_POINT('Ctrl Pts',(-0.458332266027874,4.63315383676036,
35.2346101326423));
#32803=CARTESIAN_POINT('Ctrl Pts',(-4.1461881700408,2.11785424421031,35.4335430710058));
#32804=CARTESIAN_POINT('Ctrl Pts',(-4.02243449981698,-2.3443983526288,35.6324760093692));
#32805=CARTESIAN_POINT('Ctrl Pts',(-0.200838565195405,-4.65143491968315,
35.8314089477326));
#32806=CARTESIAN_POINT('Ctrl Pts',(3.80538917253758,-2.68238628582457,36.0303418860961));
#32807=CARTESIAN_POINT('Ctrl Pts',(4.313305398898,1.75259221639213,36.2292748244595));
#32808=CARTESIAN_POINT('Ctrl Pts',(0.855980425100957,4.57640475199999,36.428207762823));
#32809=CARTESIAN_POINT('Ctrl Pts',(-3.3882512324144,3.19310765946044,36.6271407011864));
#32810=CARTESIAN_POINT('Ctrl Pts',(-4.51764817756711,-1.1256277739117,36.8260736395498));
#32811=CARTESIAN_POINT('Ctrl Pts',(-1.49395067955099,-4.40956849538517,
37.0250065779133));
#32812=CARTESIAN_POINT('Ctrl Pts',(2.90314244717482,-3.63977291262905,37.2239395162767));
#32813=CARTESIAN_POINT('Ctrl Pts',(4.63136356822164,0.476082396912402,37.4228724546401));
#32814=CARTESIAN_POINT('Ctrl Pts',(2.10195116827292,4.15427301369114,37.6218053930036));
#32815=CARTESIAN_POINT('Ctrl Pts',(-2.35979445756394,4.01342159940947,37.820738331367));
#32816=CARTESIAN_POINT('Ctrl Pts',(-4.6521703611112,0.183013565819844,38.0196712697305));
#32817=CARTESIAN_POINT('Ctrl Pts',(-2.66778493740627,-3.81563975427051,
38.2186042080939));
#32818=CARTESIAN_POINT('Ctrl Pts',(1.76910720810075,-4.30655799166989,38.4175371464573));
#32819=CARTESIAN_POINT('Ctrl Pts',(4.57965119683031,-0.838438267478442,
38.6164700848208));
#32820=CARTESIAN_POINT('Ctrl Pts',(3.18010086249031,3.40046216234224,38.8154030231842));
#32821=CARTESIAN_POINT('Ctrl Pts',(-1.14293017678358,4.51330115287866,39.0143359615477));
#32822=CARTESIAN_POINT('Ctrl Pts',(-4.4152611484038,1.47704417104799,39.2132688999111));
#32823=CARTESIAN_POINT('Ctrl Pts',(-3.6286209586944,-2.91707048796121,39.4122018382745));
#32824=CARTESIAN_POINT('Ctrl Pts',(0.493823895339948,-4.62950082687821,
39.6111347766379));
#32825=CARTESIAN_POINT('Ctrl Pts',(4.16230000860224,-2.08602580072547,39.8100677150015));
#32826=CARTESIAN_POINT('Ctrl Pts',(4.00434373250677,2.37517234857208,40.0090006533648));
#32827=CARTESIAN_POINT('Ctrl Pts',(0.16519745519922,4.6528059816321,40.2079335917283));
#32828=CARTESIAN_POINT('Ctrl Pts',(-3.82585650677666,2.65320484133016,40.4068665300917));
#32829=CARTESIAN_POINT('Ctrl Pts',(-4.29970479193952,-1.78571208206424,
40.6057994684551));
#32830=CARTESIAN_POINT('Ctrl Pts',(-0.820965403692237,-4.58260824249866,
40.8047324068186));
#32831=CARTESIAN_POINT('Ctrl Pts',(3.41277964200003,-3.16747340374845,41.003665345182));
#32832=CARTESIAN_POINT('Ctrl Pts',(4.50858774680517,1.16103327592888,41.2025982835454));
#32833=CARTESIAN_POINT('Ctrl Pts',(1.46069211445911,4.41931609540443,41.4015312219089));
#32834=CARTESIAN_POINT('Ctrl Pts',(-2.93206675809147,3.62048102032587,41.6004641602723));
#32835=CARTESIAN_POINT('Ctrl Pts',(-4.62538118106894,-0.517884424352666,
41.7993970986358));
#32836=CARTESIAN_POINT('Ctrl Pts',(-2.92506802252003,-2.94215747695014,
41.9320190575447));
#32837=CARTESIAN_POINT('Ctrl Pts',(-1.74998052418886,-3.52545282590189,
41.9983300369992));
#32838=CARTESIAN_POINT('Ctrl Pts',(-2.14454317821952,3.01050386677641,6.72649619915742));
#32839=CARTESIAN_POINT('Ctrl Pts',(-3.14871348584711,2.29525996140177,6.79285167650196));
#32840=CARTESIAN_POINT('Ctrl Pts',(-4.36647259874689,-0.206245684665433,
6.92551813330099));
#32841=CARTESIAN_POINT('Ctrl Pts',(-2.18089545508631,-3.7928747038927,7.12449556955447));
#32842=CARTESIAN_POINT('Ctrl Pts',(2.01112757824255,-3.88091212828921,7.32342850791792));
#32843=CARTESIAN_POINT('Ctrl Pts',(4.35324710193498,-0.406686609570857,
7.52236144628135));
#32844=CARTESIAN_POINT('Ctrl Pts',(2.69396302714936,3.44423669322017,7.7212943846448));
#32845=CARTESIAN_POINT('Ctrl Pts',(-1.44218363300452,4.12738523561646,7.92022732300823));
#32846=CARTESIAN_POINT('Ctrl Pts',(-4.25237300188823,1.01697737978396,8.11916026137167));
#32847=CARTESIAN_POINT('Ctrl Pts',(-3.15341553044576,-3.02874265855638,
8.31809319973511));
#32848=CARTESIAN_POINT('Ctrl Pts',(0.844532293999059,-4.28991709569067,
8.51702613809854));
#32849=CARTESIAN_POINT('Ctrl Pts',(4.06607628421319,-1.60746017549409,8.71595907646199));
#32850=CARTESIAN_POINT('Ctrl Pts',(3.54966911676128,2.55279894780965,8.91489201482541));
#32851=CARTESIAN_POINT('Ctrl Pts',(-0.229970795531832,4.36622881746894,
9.11382495318887));
#32852=CARTESIAN_POINT('Ctrl Pts',(-3.79819446779221,2.16578019232958,9.31275789155229));
#32853=CARTESIAN_POINT('Ctrl Pts',(-3.87472234165631,-2.02568803287688,
9.51169082991574));
#32854=CARTESIAN_POINT('Ctrl Pts',(-0.389199579151803,-4.35492786885263,
9.71062376827917));
#32855=CARTESIAN_POINT('Ctrl Pts',(3.45411568819898,-2.6806649703053,9.90955670664261));
#32856=CARTESIAN_POINT('Ctrl Pts',(4.12204697548566,1.45794652614552,10.1084896450061));
#32857=CARTESIAN_POINT('Ctrl Pts',(1.00056168057528,4.25626057815718,10.3074225833695));
#32858=CARTESIAN_POINT('Ctrl Pts',(-3.04074444030663,3.14177530310008,10.5063555217329));
#32859=CARTESIAN_POINT('Ctrl Pts',(-4.28668044925664,-0.860958407946073,
10.7052884600964));
#32860=CARTESIAN_POINT('Ctrl Pts',(-1.59185167833342,-4.07220906838072,
10.9042213984598));
#32861=CARTESIAN_POINT('Ctrl Pts',(2.56637354567592,-3.53985952206916,11.1031543368232));
#32862=CARTESIAN_POINT('Ctrl Pts',(4.36531994349343,0.246698947662476,11.3020872751867));
#32863=CARTESIAN_POINT('Ctrl Pts',(2.15120793231547,3.80646594483665,11.5010202135501));
#32864=CARTESIAN_POINT('Ctrl Pts',(-2.04051927856241,3.86693155519059,11.6999531519136));
#32865=CARTESIAN_POINT('Ctrl Pts',(-4.35638787015977,0.372509459594964,
11.898886090277));
#32866=CARTESIAN_POINT('Ctrl Pts',(-2.66740935028452,-3.46436226862834,
12.0978190286404));
#32867=CARTESIAN_POINT('Ctrl Pts',(1.47373067318826,-4.11643006453438,12.2967519670039));
#32868=CARTESIAN_POINT('Ctrl Pts',(4.2600634102983,-0.984245046982922,12.4956849053673));
#32869=CARTESIAN_POINT('Ctrl Pts',(3.13010054869347,3.05276090237982,12.6946178437308));
#32870=CARTESIAN_POINT('Ctrl Pts',(-0.877377932161288,4.28334991993443,
12.8935507820942));
#32871=CARTESIAN_POINT('Ctrl Pts',(-4.07827890392793,1.57623594491877,13.0924837204576));
#32872=CARTESIAN_POINT('Ctrl Pts',(-3.52999959753036,-2.57991887734767,
13.2914166588211));
#32873=CARTESIAN_POINT('Ctrl Pts',(0.263424335980266,-4.36434258411605,
13.4903495971845));
#32874=CARTESIAN_POINT('Ctrl Pts',(3.8146810836505,-2.1366063751491,13.6892825355479));
#32875=CARTESIAN_POINT('Ctrl Pts',(3.85908422390511,2.05532175707241,13.8882154739114));
#32876=CARTESIAN_POINT('Ctrl Pts',(0.355813748685168,4.35778328379722,14.0871484122748));
#32877=CARTESIAN_POINT('Ctrl Pts',(-3.47455791816341,2.65411488930297,14.2860813506383));
#32878=CARTESIAN_POINT('Ctrl Pts',(-4.11075274498564,-1.48949335073545,
14.4850142890017));
#32879=CARTESIAN_POINT('Ctrl Pts',(-0.967913944402505,-4.26380360341846,
14.6839472273652));
#32880=CARTESIAN_POINT('Ctrl Pts',(3.06473253162247,-3.11837988094897,14.8828801657286));
#32881=CARTESIAN_POINT('Ctrl Pts',(4.27995650269812,0.893784597822432,15.081813104092));
#32882=CARTESIAN_POINT('Ctrl Pts',(1.56059706511263,4.08428884539946,15.2807460424554));
#32883=CARTESIAN_POINT('Ctrl Pts',(-2.59342632668046,3.52008784838862,15.4796789808189));
#32884=CARTESIAN_POINT('Ctrl Pts',(-4.3633011435735,-0.280145859835127,
15.6786119191823));
#32885=CARTESIAN_POINT('Ctrl Pts',(-2.12197344575085,-3.82284020955897,
15.8775448575457));
#32886=CARTESIAN_POINT('Ctrl Pts',(2.0700940570225,-3.8511802304453,16.0764777959092));
#32887=CARTESIAN_POINT('Ctrl Pts',(4.35911471200799,-0.339112812863191,
16.2754107342726));
#32888=CARTESIAN_POINT('Ctrl Pts',(2.6407814577879,3.48470255036153,16.4743436726361));
#32889=CARTESIAN_POINT('Ctrl Pts',(-1.50523415796133,4.10501506720731,16.6732766109995));
#32890=CARTESIAN_POINT('Ctrl Pts',(-4.26748119093852,0.951568629831059,
16.8722095493629));
#32891=CARTESIAN_POINT('Ctrl Pts',(-3.10661342589027,-3.07665916122845,
17.0711424877264));
#32892=CARTESIAN_POINT('Ctrl Pts',(0.910178140001792,-4.27650024269325,
17.2700754260898));
#32893=CARTESIAN_POINT('Ctrl Pts',(4.09023881708235,-1.54493527098234,17.4690083644533));
#32894=CARTESIAN_POINT('Ctrl Pts',(3.51012441364316,2.60689569661673,17.6679413028167));
#32895=CARTESIAN_POINT('Ctrl Pts',(-0.296863270295577,4.36219563649339,
17.8668742411801));
#32896=CARTESIAN_POINT('Ctrl Pts',(-3.83094320453884,2.10730935932299,18.0658071795436));
#32897=CARTESIAN_POINT('Ctrl Pts',(-3.84321968993877,-2.08483596169087,
18.264740117907));
#32898=CARTESIAN_POINT('Ctrl Pts',(-0.322406897833154,-4.3603821351485,
18.4636730562704));
#32899=CARTESIAN_POINT('Ctrl Pts',(3.4947960165208,-2.62740925156378,18.6626059946339));
#32900=CARTESIAN_POINT('Ctrl Pts',(4.09921711531441,1.52095286376864,18.8615389329973));
#32901=CARTESIAN_POINT('Ctrl Pts',(0.935209343336036,4.27109611884696,19.0604718713608));
#32902=CARTESIAN_POINT('Ctrl Pts',(-3.08854061611436,3.09480135629163,19.2594048097242));
#32903=CARTESIAN_POINT('Ctrl Pts',(-4.27298119064957,-0.926558317996034,
19.4583377480876));
#32904=CARTESIAN_POINT('Ctrl Pts',(-1.52925079250028,-4.09612873161108,
19.6572706864511));
#32905=CARTESIAN_POINT('Ctrl Pts',(2.62032678939031,-3.50010943958843,19.8562036248145));
#32906=CARTESIAN_POINT('Ctrl Pts',(4.36102607910528,0.313576321899792,20.055136563178));
#32907=CARTESIAN_POINT('Ctrl Pts',(2.09261433118024,3.83898994961327,20.2540695015414));
#32908=CARTESIAN_POINT('Ctrl Pts',(-2.09954725462231,3.83520271927058,20.4530024399048));
#32909=CARTESIAN_POINT('Ctrl Pts',(-4.36158553460872,0.30569624888859,20.6519353782683));
#32910=CARTESIAN_POINT('Ctrl Pts',(-2.61399846697548,-3.50483816843836,
20.8508683166317));
#32911=CARTESIAN_POINT('Ctrl Pts',(1.53664923735901,-4.09335897443855,21.0498012549951));
#32912=CARTESIAN_POINT('Ctrl Pts',(4.27464833406557,-0.918836325121606,
21.2487341933586));
#32913=CARTESIAN_POINT('Ctrl Pts',(3.08294384559025,3.10037672182424,21.447667131722));
#32914=CARTESIAN_POINT('Ctrl Pts',(-0.942924891294206,4.26939939823746,
21.6466000700854));
#32915=CARTESIAN_POINT('Ctrl Pts',(-4.10195850250371,1.51354385996249,21.8455330084489));
#32916=CARTESIAN_POINT('Ctrl Pts',(-3.49004307327481,-2.63371940779178,
22.0444659468123));
#32917=CARTESIAN_POINT('Ctrl Pts',(0.330284769249194,-4.35979248858183,
22.2433988851758));
#32918=CARTESIAN_POINT('Ctrl Pts',(3.84698032663149,-2.07788857709042,22.4423318235392));
#32919=CARTESIAN_POINT('Ctrl Pts',(3.82712943615432,2.11422771981017,22.6412647619026));
#32920=CARTESIAN_POINT('Ctrl Pts',(0.288981111392786,4.36272489271909,22.8401977002661));
#32921=CARTESIAN_POINT('Ctrl Pts',(-3.51482885866484,2.6005493009342,23.0391306386295));
#32922=CARTESIAN_POINT('Ctrl Pts',(-4.08744073059509,-1.5523230482618,23.238063576993));
#32923=CARTESIAN_POINT('Ctrl Pts',(-0.902449815593572,-4.27813778443702,
23.4369965153564));
#32924=CARTESIAN_POINT('Ctrl Pts',(3.11216730456806,-3.07104106789052,23.6359294537198));
#32925=CARTESIAN_POINT('Ctrl Pts',(4.26575491804855,0.959277619585273,23.8348623920833));
#32926=CARTESIAN_POINT('Ctrl Pts',(1.4978147039944,4.10772804416148,24.0337953304467));
#32927=CARTESIAN_POINT('Ctrl Pts',(-2.64707335517684,3.47992546250712,24.2327282688101));
#32928=CARTESIAN_POINT('Ctrl Pts',(-4.35849488303591,-0.346988367013049,
24.4316612071736));
#32929=CARTESIAN_POINT('Ctrl Pts',(-2.06313231327231,-3.85491421827051,
24.630594145537));
#32930=CARTESIAN_POINT('Ctrl Pts',(2.12887714170064,-3.81899995913029,24.8295270839005));
#32931=CARTESIAN_POINT('Ctrl Pts',(4.36380019275037,-0.272261730774709,
25.0284600222639));
#32932=CARTESIAN_POINT('Ctrl Pts',(2.58706195091454,3.52476794050656,25.2273929606274));
#32933=CARTESIAN_POINT('Ctrl Pts',(-1.56797406633792,4.08146247068183,25.4263258989908));
#32934=CARTESIAN_POINT('Ctrl Pts',(-4.28156441872558,0.886050055355632,
25.6252588373542));
#32935=CARTESIAN_POINT('Ctrl Pts',(-3.05909319796137,-3.12391219122417,
25.8241917757177));
#32936=CARTESIAN_POINT('Ctrl Pts',(0.975616262761357,-4.2620478035949,26.0231247140811));
#32937=CARTESIAN_POINT('Ctrl Pts',(4.11343727186996,-1.48206355554802,26.2220576524445));
#32938=CARTESIAN_POINT('Ctrl Pts',(3.46975675584276,2.6603884354688,26.4209905908079));
#32939=CARTESIAN_POINT('Ctrl Pts',(-0.363686869931574,4.35713328152031,
26.6199235291714));
#32940=CARTESIAN_POINT('Ctrl Pts',(-3.86279150803662,2.0483457563929,26.8188564675348));
#32941=CARTESIAN_POINT('Ctrl Pts',(-3.810814407564,-2.14349530519553,27.0177894058983));
#32942=CARTESIAN_POINT('Ctrl Pts',(-0.255538352525876,-4.36481141891387,
27.2167223442617));
#32943=CARTESIAN_POINT('Ctrl Pts',(3.53465526802747,-2.57353661495193,27.4156552826252));
#32944=CARTESIAN_POINT('Ctrl Pts',(4.07542428247787,1.58360206178266,27.6145882209886));
#32945=CARTESIAN_POINT('Ctrl Pts',(0.869637285206309,4.28492818661779,27.813521159352));
#32946=CARTESIAN_POINT('Ctrl Pts',(-3.13561120934189,3.04710041123396,28.0124540977155));
#32947=CARTESIAN_POINT('Ctrl Pts',(-4.25827810930823,-0.99194058092151,
28.2113870360789));
#32948=CARTESIAN_POINT('Ctrl Pts',(-1.46629064589802,-4.11908610180032,
28.4103199744424));
#32949=CARTESIAN_POINT('Ctrl Pts',(2.67366445316185,-3.4595371025892,28.6092529128058));
#32950=CARTESIAN_POINT('Ctrl Pts',(4.35570770402749,0.380380032820054,28.8081858511692));
#32951=CARTESIAN_POINT('Ctrl Pts',(2.03352912356371,3.87061208026725,29.0071187895327));
#32952=CARTESIAN_POINT('Ctrl Pts',(-2.15808199565578,3.80257290164423,29.2060517278961));
#32953=CARTESIAN_POINT('Ctrl Pts',(-4.36575855636173,0.238811222196252,
29.4049846662595));
#32954=CARTESIAN_POINT('Ctrl Pts',(-2.55997349163937,-3.5444906960516,29.603917604623));
#32955=CARTESIAN_POINT('Ctrl Pts',(1.59920680512957,-4.06932625464213,29.8028505429864));
#32956=CARTESIAN_POINT('Ctrl Pts',(4.2882290387233,-0.853211746134946,30.0017834813498));
#32957=CARTESIAN_POINT('Ctrl Pts',(3.03506288379887,3.14726418714398,30.2007164197133));
#32958=CARTESIAN_POINT('Ctrl Pts',(-1.00825033437494,4.25444589053914,30.3996493580767));
#32959=CARTESIAN_POINT('Ctrl Pts',(-4.12467445101052,1.45049620663885,30.5985822964402));
#32960=CARTESIAN_POINT('Ctrl Pts',(-3.44926665280217,-2.68690121332354,
30.7975152348036));
#32961=CARTESIAN_POINT('Ctrl Pts',(0.397067610571902,-4.35421817148927,
30.996448173167));
#32962=CARTESIAN_POINT('Ctrl Pts',(3.87837582013254,-2.01868263233817,31.1953811115305));
#32963=CARTESIAN_POINT('Ctrl Pts',(3.7942755623814,2.17263699890429,31.3943140498939));
#32964=CARTESIAN_POINT('Ctrl Pts',(0.222080585391179,4.36664159118708,31.5932469882574));
#32965=CARTESIAN_POINT('Ctrl Pts',(-3.55427408016482,2.54637278012491,31.7921799266208));
#32966=CARTESIAN_POINT('Ctrl Pts',(-4.06316847671228,-1.61478806725346,
31.9911128649843));
#32967=CARTESIAN_POINT('Ctrl Pts',(-0.836773679318462,-4.2914669265756,
32.1900458033476));
#32968=CARTESIAN_POINT('Ctrl Pts',(3.15887095352933,-3.02298079240363,32.3889787417111));
#32969=CARTESIAN_POINT('Ctrl Pts',(4.25055120355625,1.02454528364496,32.5879116800745));
#32970=CARTESIAN_POINT('Ctrl Pts',(1.43468046968086,4.1302022374466,32.786844618438));
#32971=CARTESIAN_POINT('Ctrl Pts',(-2.70009852159804,3.43894555728302,32.9857775568014));
#32972=CARTESIAN_POINT('Ctrl Pts',(-4.3526647057765,-0.413749358162806,
33.1847104951649));
#32973=CARTESIAN_POINT('Ctrl Pts',(-2.00380650070783,-3.88608261363723,
33.3836434335282));
#32974=CARTESIAN_POINT('Ctrl Pts',(2.18716010122942,-3.7859225116057,33.5825763718918));
#32975=CARTESIAN_POINT('Ctrl Pts',(4.36746051042428,-0.205346687767176,
33.7815093102551));
#32976=CARTESIAN_POINT('Ctrl Pts',(2.53273468010832,3.56400527671735,33.9804422486186));
#32977=CARTESIAN_POINT('Ctrl Pts',(-1.63034561937406,4.05695103910325,34.179375186982));
#32978=CARTESIAN_POINT('Ctrl Pts',(-4.29464180263262,0.820323326117568,
34.3783081253455));
#32979=CARTESIAN_POINT('Ctrl Pts',(-3.01085431445013,-3.17043133807512,
34.5772410637089));
#32980=CARTESIAN_POINT('Ctrl Pts',(1.04082518947229,-4.24659410554575,34.7761740020724));
#32981=CARTESIAN_POINT('Ctrl Pts',(4.1356693799436,-1.41884366724649,34.9751069404358));
#32982=CARTESIAN_POINT('Ctrl Pts',(3.42857396757734,2.7132561842074,35.1740398787992));
#32983=CARTESIAN_POINT('Ctrl Pts',(-0.43042503065489,4.35104732970134,35.3729728171627));
#32984=CARTESIAN_POINT('Ctrl Pts',(-3.89373234762037,1.98890094709468,35.5719057555261));
#32985=CARTESIAN_POINT('Ctrl Pts',(-3.77751387196871,-2.2016510893785,35.7708386938896));
#32986=CARTESIAN_POINT('Ctrl Pts',(-0.188609775022207,-4.36821530206696,
35.969771632253));
#32987=CARTESIAN_POINT('Ctrl Pts',(3.57368414281305,-2.51905939180415,36.1687045706164));
#32988=CARTESIAN_POINT('Ctrl Pts',(4.05067403312995,1.64587923299354,36.3676375089799));
#32989=CARTESIAN_POINT('Ctrl Pts',(0.803860928027483,4.29775362040325,36.5665704473433));
#32990=CARTESIAN_POINT('Ctrl Pts',(-3.18194517095124,2.99868362775086,36.7655033857068));
#32991=CARTESIAN_POINT('Ctrl Pts',(-4.24257465477942,-1.05708981235569,
36.9644363240701));
#32992=CARTESIAN_POINT('Ctrl Pts',(-1.40298603154328,-4.14107579911404,
37.1633692624336));
#32993=CARTESIAN_POINT('Ctrl Pts',(2.72637400733384,-3.41815203427124,37.362302200797));
#32994=CARTESIAN_POINT('Ctrl Pts',(4.34936606820663,0.447094379937924,37.5612351391605));
#32995=CARTESIAN_POINT('Ctrl Pts',(1.97396618806673,3.90132491601227,37.7601680775239));
#32996=CARTESIAN_POINT('Ctrl Pts',(-2.21610974618682,3.76904975494763,37.9591010158874));
#32997=CARTESIAN_POINT('Ctrl Pts',(-4.3689059634554,0.17187011588989,38.1580339542508));
#32998=CARTESIAN_POINT('Ctrl Pts',(-2.50534709985704,-3.5833105804079,38.3569668926142));
#32999=CARTESIAN_POINT('Ctrl Pts',(1.66138864906423,-4.04433746645492,38.5558998309777));
#33000=CARTESIAN_POINT('Ctrl Pts',(4.30080239357324,-0.787386888794196,
38.7548327693411));
#33001=CARTESIAN_POINT('Ctrl Pts',(2.98646879715839,3.19341259377544,38.9537657077046));
#33002=CARTESIAN_POINT('Ctrl Pts',(-1.07333869518271,4.23849231457894,39.152698646068));
#33003=CARTESIAN_POINT('Ctrl Pts',(-4.14642183414512,1.38710893760937,39.3516315844314));
#33004=CARTESIAN_POINT('Ctrl Pts',(-3.40767910781596,-2.73945398844537,
39.5505645227949));
#33005=CARTESIAN_POINT('Ctrl Pts',(0.46375562238267,-4.34761674667882,39.7494974611583));
#33006=CARTESIAN_POINT('Ctrl Pts',(3.90886315799689,-1.9590104947349,39.9484303995218));
#33007=CARTESIAN_POINT('Ctrl Pts',(3.76052462715392,2.23055129808965,40.1473633378851));
#33008=CARTESIAN_POINT('Ctrl Pts',(0.155138804288171,4.36950288189749,40.3462962762487));
#33009=CARTESIAN_POINT('Ctrl Pts',(-3.59290524859212,2.49165476622559,40.545229214612));
#33010=CARTESIAN_POINT('Ctrl Pts',(-4.03790154884084,-1.67698247458014,
40.7441621529755));
#33011=CARTESIAN_POINT('Ctrl Pts',(-0.770977924188701,-4.3035793887071,
40.943095091339));
#33012=CARTESIAN_POINT('Ctrl Pts',(3.20498007865981,-2.97461020739956,41.1420280297023));
#33013=CARTESIAN_POINT('Ctrl Pts',(4.23406590146329,1.09033952096375,41.3409609680659));
#33014=CARTESIAN_POINT('Ctrl Pts',(1.37175253575807,4.15022988087543,41.5398939064291));
#33015=CARTESIAN_POINT('Ctrl Pts',(-2.75353715585242,3.40003479934917,41.7388268447928));
#33016=CARTESIAN_POINT('Ctrl Pts',(-4.34374794056332,-0.486351138137266,
41.9377597831561));
#33017=CARTESIAN_POINT('Ctrl Pts',(-2.74696456387898,-2.76301346440847,
42.0703817420651));
#33018=CARTESIAN_POINT('Ctrl Pts',(-1.64342656321671,-3.3107927439021,42.1366927215196));
#33019=CARTESIAN_POINT('Ctrl Pts',(-2.0054985897787,2.81531345260957,6.86485888367774));
#33020=CARTESIAN_POINT('Ctrl Pts',(-2.94456204921288,2.14644343024538,6.93121436102229));
#33021=CARTESIAN_POINT('Ctrl Pts',(-4.08336597184518,-0.19287344453834,
7.06388081782131));
#33022=CARTESIAN_POINT('Ctrl Pts',(-2.03949391369296,-3.54695813407657,
7.26285825407481));
#33023=CARTESIAN_POINT('Ctrl Pts',(1.88073318504086,-3.62928752350934,7.46179119243823));
#33024=CARTESIAN_POINT('Ctrl Pts',(4.07099796943106,-0.380318489391973,
7.66072413080168));
#33025=CARTESIAN_POINT('Ctrl Pts',(2.51929600053549,3.2209245779103,7.8596570691651));
#33026=CARTESIAN_POINT('Ctrl Pts',(-1.34867755126933,3.85978018702081,8.05859000752856));
#33027=CARTESIAN_POINT('Ctrl Pts',(-3.97666418895809,0.951040166366322,
8.25752294589198));
#33028=CARTESIAN_POINT('Ctrl Pts',(-2.94895922988404,-2.83236970569201,
8.45645588425543));
#33029=CARTESIAN_POINT('Ctrl Pts',(0.789775809524059,-4.01177405661665,
8.65538882261886));
#33030=CARTESIAN_POINT('Ctrl Pts',(3.80244629100563,-1.50323814778838,8.85432176098231));
#33031=CARTESIAN_POINT('Ctrl Pts',(3.31952113631781,2.38728450040875,9.05325469934573));
#33032=CARTESIAN_POINT('Ctrl Pts',(-0.2150603031981,4.08313799648236,9.25218763770918));
#33033=CARTESIAN_POINT('Ctrl Pts',(-3.5519329833157,2.02535867106851,9.45112057607261));
#33034=CARTESIAN_POINT('Ctrl Pts',(-3.62349906073116,-1.89434959133768,
9.65005351443604));
#33035=CARTESIAN_POINT('Ctrl Pts',(-0.363965256124856,-4.07256976137133,
9.84898645279951));
#33036=CARTESIAN_POINT('Ctrl Pts',(3.23016305382427,-2.50686014262486,10.0479193911629));
#33037=CARTESIAN_POINT('Ctrl Pts',(3.85478804078057,1.36341843421643,10.2468523295264));
#33038=CARTESIAN_POINT('Ctrl Pts',(0.93568880298618,3.98029970854296,10.4457852678898));
#33039=CARTESIAN_POINT('Ctrl Pts',(-2.84359333439737,2.9380737136755,10.6447182062533));
#33040=CARTESIAN_POINT('Ctrl Pts',(-4.00874726288035,-0.805136912387771,
10.8436511446167));
#33041=CARTESIAN_POINT('Ctrl Pts',(-1.48864165033278,-3.8081814471565,11.0425840829802));
#33042=CARTESIAN_POINT('Ctrl Pts',(2.39997896940062,-3.31034756102161,11.2415170213436));
#33043=CARTESIAN_POINT('Ctrl Pts',(4.0822880506782,0.23070386115876,11.440449959707));
#33044=CARTESIAN_POINT('Ctrl Pts',(2.01173122481096,3.55966816706786,11.6393828980705));
#33045=CARTESIAN_POINT('Ctrl Pts',(-1.90821923155247,3.61621340128212,11.8383158364339));
#33046=CARTESIAN_POINT('Ctrl Pts',(-4.07393510136182,0.34835726484055,12.0372487747973));
#33047=CARTESIAN_POINT('Ctrl Pts',(-2.49446397008411,-3.23974528224934,
12.2361817131608));
#33048=CARTESIAN_POINT('Ctrl Pts',(1.3781791930375,-3.84953531045267,12.4351146515242));
#33049=CARTESIAN_POINT('Ctrl Pts',(3.98385597850928,-0.920430082158486,
12.6340475898877));
#33050=CARTESIAN_POINT('Ctrl Pts',(2.92715590901843,2.8548306916055,12.8329805282511));
#33051=CARTESIAN_POINT('Ctrl Pts',(-0.820491852774556,4.00563267329001,
13.0319134666145));
#33052=CARTESIAN_POINT('Ctrl Pts',(-3.81385773605278,1.47403838579632,13.230846404978));
#33053=CARTESIAN_POINT('Ctrl Pts',(-3.30112691908783,-2.41264606971442,
13.4297793433414));
#33054=CARTESIAN_POINT('Ctrl Pts',(0.246344834502405,-4.0813740598232,13.6287122817048));
#33055=CARTESIAN_POINT('Ctrl Pts',(3.56735066536092,-1.99807638092479,13.8276452200683));
#33056=CARTESIAN_POINT('Ctrl Pts',(3.60887486317929,1.92206196975356,14.0265781584317));
#33057=CARTESIAN_POINT('Ctrl Pts',(0.332744044726809,4.07524004131849,14.2255110967952));
#33058=CARTESIAN_POINT('Ctrl Pts',(-3.24927988195903,2.48203147489298,14.4244440351586));
#33059=CARTESIAN_POINT('Ctrl Pts',(-3.84422608820695,-1.39291987436911,
14.623376973522));
#33060=CARTESIAN_POINT('Ctrl Pts',(-0.905157830460687,-3.98735367074704,
14.8223099118855));
#33061=CARTESIAN_POINT('Ctrl Pts',(2.86602612278512,-2.91619516788176,15.0212428502489));
#33062=CARTESIAN_POINT('Ctrl Pts',(4.00245927321531,0.835834768310396,15.2201757886123));
#33063=CARTESIAN_POINT('Ctrl Pts',(1.45941347559844,3.81947801419324,15.4191087269758));
#33064=CARTESIAN_POINT('Ctrl Pts',(-2.42527774384603,3.29185781267492,15.6180416653392));
#33065=CARTESIAN_POINT('Ctrl Pts',(-4.08040014259896,-0.261982193941216,
15.8169746037027));
#33066=CARTESIAN_POINT('Ctrl Pts',(-1.98439219887121,-3.57498078242707,
16.0159075420661));
#33067=CARTESIAN_POINT('Ctrl Pts',(1.93587648606574,-3.60148333667693,16.2148404804295));
#33068=CARTESIAN_POINT('Ctrl Pts',(4.07648514443705,-0.317125938465704,
16.413773418793));
#33069=CARTESIAN_POINT('Ctrl Pts',(2.46956253587978,3.25876677211529,16.6127063571564));
#33070=CARTESIAN_POINT('Ctrl Pts',(-1.40764010337363,3.8388604211456,16.8116392955199));
#33071=CARTESIAN_POINT('Ctrl Pts',(-3.99079281651019,0.889872288227052,
17.0105722338833));
#33072=CARTESIAN_POINT('Ctrl Pts',(-2.90519160811827,-2.87717947194522,
17.2095051722467));
#33073=CARTESIAN_POINT('Ctrl Pts',(0.851165411244564,-3.99922710487472,
17.4084381106102));
#33074=CARTESIAN_POINT('Ctrl Pts',(3.82504221077387,-1.44476713676006,17.6073710489736));
#33075=CARTESIAN_POINT('Ctrl Pts',(3.28254037176988,2.43787380751438,17.806303987337));
#33076=CARTESIAN_POINT('Ctrl Pts',(-0.277615706683554,4.07936631268466,
18.0052369257005));
#33077=CARTESIAN_POINT('Ctrl Pts',(-3.58255840789535,1.97067887989953,18.2041698640639));
#33078=CARTESIAN_POINT('Ctrl Pts',(-3.59403892943819,-1.94966257781868,
18.4031028024274));
#33079=CARTESIAN_POINT('Ctrl Pts',(-0.301503175830768,-4.07767039234755,
18.6020357407908));
#33080=CARTESIAN_POINT('Ctrl Pts',(3.26820581365757,-2.45705733617242,18.8009686791542));
#33081=CARTESIAN_POINT('Ctrl Pts',(3.83343838792988,1.42233966393734,18.9999016175177));
#33082=CARTESIAN_POINT('Ctrl Pts',(0.874573679959915,3.99417336528914,19.1988345558811));
#33083=CARTESIAN_POINT('Ctrl Pts',(-2.88829057535421,2.89414539130014,19.3977674942445));
#33084=CARTESIAN_POINT('Ctrl Pts',(-3.99593621570884,-0.866483556480068,
19.596700432608));
#33085=CARTESIAN_POINT('Ctrl Pts',(-1.43009958434302,-3.83055024409362,
19.7956333709714));
#33086=CARTESIAN_POINT('Ctrl Pts',(2.45043407577578,-3.27317473318194,19.9945663093349));
#33087=CARTESIAN_POINT('Ctrl Pts',(4.07827258525759,0.293245143182466,20.1934992476983));
#33088=CARTESIAN_POINT('Ctrl Pts',(1.95693662536422,3.59008343050296,20.3924321860618));
#33089=CARTESIAN_POINT('Ctrl Pts',(-1.96342004259136,3.58654175076973,20.5913651244252));
#33090=CARTESIAN_POINT('Ctrl Pts',(-4.07879576764655,0.285875986211559,
20.7902980627886));
#33091=CARTESIAN_POINT('Ctrl Pts',(-2.44451605938545,-3.27759686799192,
20.989231001152));
#33092=CARTESIAN_POINT('Ctrl Pts',(1.43701834022598,-3.82796006817182,21.1881639395155));
#33093=CARTESIAN_POINT('Ctrl Pts',(3.99749526744709,-0.85926223028944,21.3870968778789));
#33094=CARTESIAN_POINT('Ctrl Pts',(2.88305667961953,2.89935926986721,21.5860298162423));
#33095=CARTESIAN_POINT('Ctrl Pts',(-0.881788979099839,3.99258665403793,
21.7849627546059));
#33096=CARTESIAN_POINT('Ctrl Pts',(-3.83600203327774,1.41541103371171,21.9838956929692));
#33097=CARTESIAN_POINT('Ctrl Pts',(-3.26376103442727,-2.46295836420717,
22.1828286313327));
#33098=CARTESIAN_POINT('Ctrl Pts',(0.30887027395015,-4.07711897637704,22.3817615696961));
#33099=CARTESIAN_POINT('Ctrl Pts',(3.59755573975958,-1.94316563704349,22.5806945080596));
#33100=CARTESIAN_POINT('Ctrl Pts',(3.57899191075299,1.97714867838221,22.779627446423));
#33101=CARTESIAN_POINT('Ctrl Pts',(0.270244599062885,4.07986125381013,22.9785603847864));
#33102=CARTESIAN_POINT('Ctrl Pts',(-3.28693979722906,2.43193888966304,23.1774933231499));
#33103=CARTESIAN_POINT('Ctrl Pts',(-3.82242554230984,-1.45167591671186,
23.3764262615133));
#33104=CARTESIAN_POINT('Ctrl Pts',(-0.843938164034378,-4.00075847420837,
23.5753591998767));
#33105=CARTESIAN_POINT('Ctrl Pts',(2.91038539296211,-2.87192563589251,23.7742921382402));
#33106=CARTESIAN_POINT('Ctrl Pts',(3.98917846904379,0.897081454373756,23.9732250766036));
#33107=CARTESIAN_POINT('Ctrl Pts',(1.40070170053866,3.8413974982774,24.1721580149671));
#33108=CARTESIAN_POINT('Ctrl Pts',(-2.47544648891397,3.25429941372752,24.3710909533305));
#33109=CARTESIAN_POINT('Ctrl Pts',(-4.07590550298146,-0.324490869562239,
24.5700238916939));
#33110=CARTESIAN_POINT('Ctrl Pts',(-1.92936611713726,-3.60497522594906,
24.7689568300574));
#33111=CARTESIAN_POINT('Ctrl Pts',(1.9908482836132,-3.57138952024253,24.9678897684208));
#33112=CARTESIAN_POINT('Ctrl Pts',(4.08086683519371,-0.254609243900974,
25.1668227067842));
#33113=CARTESIAN_POINT('Ctrl Pts',(2.41932601167626,3.29623446418644,25.3657556451477));
#33114=CARTESIAN_POINT('Ctrl Pts',(-1.46631217817726,3.81683489160756,25.5646885835111));
#33115=CARTESIAN_POINT('Ctrl Pts',(-4.00396293765922,0.828601706198546,
25.7636215218746));
#33116=CARTESIAN_POINT('Ctrl Pts',(-2.86075242355659,-2.92136878274188,
25.962554460238));
#33117=CARTESIAN_POINT('Ctrl Pts',(0.912360757761685,-3.98571171076888,
26.1614873986014));
#33118=CARTESIAN_POINT('Ctrl Pts',(3.84673655987073,-1.38597180080177,26.3604203369649));
#33119=CARTESIAN_POINT('Ctrl Pts',(3.24479001000817,2.4878982665324,26.5593532753283));
#33120=CARTESIAN_POINT('Ctrl Pts',(-0.340106700660735,4.07463218288835,
26.7582862136918));
#33121=CARTESIAN_POINT('Ctrl Pts',(-3.61234178013069,1.91553826826458,26.9572191520552));
#33122=CARTESIAN_POINT('Ctrl Pts',(-3.56373469086466,-2.00451865713232,
27.1561520904186));
#33123=CARTESIAN_POINT('Ctrl Pts',(-0.238970150300533,-4.0818124970323,
27.355085028782));
#33124=CARTESIAN_POINT('Ctrl Pts',(3.30548073238998,-2.4066776106206,27.5540179671455));
#33125=CARTESIAN_POINT('Ctrl Pts',(3.81118819815281,1.4809269097172,27.7529509055089));
#33126=CARTESIAN_POINT('Ctrl Pts',(0.813253081967926,4.00710861074834,27.9518838438724));
#33127=CARTESIAN_POINT('Ctrl Pts',(-2.93230927793693,2.84953720666863,28.1508167822358));
#33128=CARTESIAN_POINT('Ctrl Pts',(-3.98218643011584,-0.927626664917013,
28.3497497205993));
#33129=CARTESIAN_POINT('Ctrl Pts',(-1.37122155078066,-3.85201913966408,
28.5486826589627));
#33130=CARTESIAN_POINT('Ctrl Pts',(2.50031351423257,-3.23523296289614,28.7476155973261));
#33131=CARTESIAN_POINT('Ctrl Pts',(4.07329903479392,0.355717537957839,28.9465485356896));
#33132=CARTESIAN_POINT('Ctrl Pts',(1.90168229346025,3.61965529414108,29.145481474053));
#33133=CARTESIAN_POINT('Ctrl Pts',(-2.01815959821697,3.55602753501551,29.3444144124164));
#33134=CARTESIAN_POINT('Ctrl Pts',(-4.08269822544072,0.223327547890934,
29.5433473507799));
#33135=CARTESIAN_POINT('Ctrl Pts',(-2.393993872213,-3.31467846607637,29.7422802891433));
#33136=CARTESIAN_POINT('Ctrl Pts',(1.49551989674303,-3.80548554485619,29.9412132275068));
#33137=CARTESIAN_POINT('Ctrl Pts',(4.01019544728766,-0.797892516706975,
30.1401461658702));
#33138=CARTESIAN_POINT('Ctrl Pts',(2.8382801499021,2.94320671790745,30.3390791042336));
#33139=CARTESIAN_POINT('Ctrl Pts',(-0.942878951689648,3.97860267884648,
30.5380120425971));
#33140=CARTESIAN_POINT('Ctrl Pts',(-3.85724516009308,1.35645116705405,30.7369449809605));
#33141=CARTESIAN_POINT('Ctrl Pts',(-3.22562841271805,-2.51269204972075,
30.935877919324));
#33142=CARTESIAN_POINT('Ctrl Pts',(0.371323152238799,-4.07190607827283,
31.1348108576874));
#33143=CARTESIAN_POINT('Ctrl Pts',(3.62691566059552,-1.88779839617231,31.3337437960508));
#33144=CARTESIAN_POINT('Ctrl Pts',(3.54826816585965,2.03177090657653,31.5326767344143));
#33145=CARTESIAN_POINT('Ctrl Pts',(0.207681666353341,4.08352400741375,31.7316096727777));
#33146=CARTESIAN_POINT('Ctrl Pts',(-3.32382753019483,2.38127498268946,31.9305426111411));
#33147=CARTESIAN_POINT('Ctrl Pts',(-3.79972701545007,-1.51009092498523,
32.1294755495046));
#33148=CARTESIAN_POINT('Ctrl Pts',(-0.782520235955546,-4.01322340195306,
32.328408487868));
#33149=CARTESIAN_POINT('Ctrl Pts',(2.9540609426459,-2.82698141854484,32.5273414262314));
#33150=CARTESIAN_POINT('Ctrl Pts',(3.97496050958118,0.958117394129718,32.7262743645949));
#33151=CARTESIAN_POINT('Ctrl Pts',(1.34166086649601,3.86241454442386,32.9252073029583));
#33152=CARTESIAN_POINT('Ctrl Pts',(-2.52503369124243,3.21597650049785,33.1241402413218));
#33153=CARTESIAN_POINT('Ctrl Pts',(-4.07045333377795,-0.38692331436581,
33.3230731796852));
#33154=CARTESIAN_POINT('Ctrl Pts',(-1.87388678025847,-3.63412277288981,
33.5220061180486));
#33155=CARTESIAN_POINT('Ctrl Pts',(2.04535238235562,-3.54045669732818,33.720939056412));
#33156=CARTESIAN_POINT('Ctrl Pts',(4.08428983082642,-0.192032735416775,
33.9198719947756));
#33157=CARTESIAN_POINT('Ctrl Pts',(2.36852112880191,3.3329277904093,34.1188049331389));
#33158=CARTESIAN_POINT('Ctrl Pts',(-1.5246397804968,3.79391269448716,34.3177378715024));
#33159=CARTESIAN_POINT('Ctrl Pts',(-4.01619243028494,0.767136465425386,
34.5166708098658));
#33160=CARTESIAN_POINT('Ctrl Pts',(-2.81564117849665,-2.96487179277909,
34.7156037482293));
#33161=CARTESIAN_POINT('Ctrl Pts',(0.973341768490662,-3.97125997579838,
34.9145366865927));
#33162=CARTESIAN_POINT('Ctrl Pts',(3.8675272167539,-1.32685086627251,35.1134696249562));
#33163=CARTESIAN_POINT('Ctrl Pts',(3.20627736795542,2.53733825758359,35.3124025633196));
#33164=CARTESIAN_POINT('Ctrl Pts',(-0.402517795281907,4.06894082264232,
35.511335501683));
#33165=CARTESIAN_POINT('Ctrl Pts',(-3.64127652519993,1.85994764997906,35.7102684400464));
#33166=CARTESIAN_POINT('Ctrl Pts',(-3.53259324412043,-2.0589038261282,35.9092013784099));
#33167=CARTESIAN_POINT('Ctrl Pts',(-0.176380984849015,-4.08499568445078,
36.1081343167733));
#33168=CARTESIAN_POINT('Ctrl Pts',(3.34197911308852,-2.35573249778373,36.3070672551368));
#33169=CARTESIAN_POINT('Ctrl Pts',(3.78804266736189,1.53916624959495,36.5060001935002));
#33170=CARTESIAN_POINT('Ctrl Pts',(0.751741430954012,4.0191024888065,36.7049331318636));
#33171=CARTESIAN_POINT('Ctrl Pts',(-2.97563910948809,2.80425959604127,36.9038660702271));
#33172=CARTESIAN_POINT('Ctrl Pts',(-3.96750113199172,-0.988551850799671,
37.1027990085905));
#33173=CARTESIAN_POINT('Ctrl Pts',(-1.31202138353558,-3.87258310284293,
37.301731946954));
#33174=CARTESIAN_POINT('Ctrl Pts',(2.54960556749285,-3.19653115591342,37.5006648853174));
#33175=CARTESIAN_POINT('Ctrl Pts',(4.06736856819161,0.418106362963447,37.6995978236809));
#33176=CARTESIAN_POINT('Ctrl Pts',(1.84598120786055,3.64837681833342,37.8985307620442));
#33177=CARTESIAN_POINT('Ctrl Pts',(-2.07242503480969,3.52467791048579,38.0974637004078));
#33178=CARTESIAN_POINT('Ctrl Pts',(-4.0856415657996,0.160726665959935,38.2963966387711));
#33179=CARTESIAN_POINT('Ctrl Pts',(-2.34290926230782,-3.3509814065453,38.4953295771346));
#33180=CARTESIAN_POINT('Ctrl Pts',(1.5536700900277,-3.78211694123996,38.694262515498));
#33181=CARTESIAN_POINT('Ctrl Pts',(4.02195359031618,-0.736335510109945,
38.8931954538615));
#33182=CARTESIAN_POINT('Ctrl Pts',(2.79283673182646,2.98636302520864,39.0921283922249));
#33183=CARTESIAN_POINT('Ctrl Pts',(-1.00374721358184,3.96368347627922,39.2910613305884));
#33184=CARTESIAN_POINT('Ctrl Pts',(-3.87758251988644,1.29717370417073,39.4899942689517));
#33185=CARTESIAN_POINT('Ctrl Pts',(-3.18673725693753,-2.56183748892951,
39.6889272073153));
#33186=CARTESIAN_POINT('Ctrl Pts',(0.433687349425391,-4.06573266647945,
39.8878601456786));
#33187=CARTESIAN_POINT('Ctrl Pts',(3.65542630739156,-1.83199518874432,40.0867930840421));
#33188=CARTESIAN_POINT('Ctrl Pts',(3.51670552180105,2.08593024760723,40.2857260224055));
#33189=CARTESIAN_POINT('Ctrl Pts',(0.145080153377126,4.08619978216286,40.484658960769));
#33190=CARTESIAN_POINT('Ctrl Pts',(-3.35995399040756,2.33010469112103,40.6835918991324));
#33191=CARTESIAN_POINT('Ctrl Pts',(-3.77609830574217,-1.56825286709605,
40.8825248374958));
#33192=CARTESIAN_POINT('Ctrl Pts',(-0.720990444685169,-4.02455053491554,
41.0814577758593));
#33193=CARTESIAN_POINT('Ctrl Pts',(2.99718051531959,-2.78174701105068,41.2803907142227));
#33194=CARTESIAN_POINT('Ctrl Pts',(3.9595440561214,1.01964576599861,41.4793236525862));
#33195=CARTESIAN_POINT('Ctrl Pts',(1.28281295705702,3.88114366634645,41.6782565909495));
#33196=CARTESIAN_POINT('Ctrl Pts',(-2.57500755361336,3.17958857837247,41.8771895293131));
#33197=CARTESIAN_POINT('Ctrl Pts',(-4.0621147000577,-0.454817851921865,
42.0761224676764));
#33198=CARTESIAN_POINT('Ctrl Pts',(-2.56886110523792,-2.5838694518668,42.2087444265854));
#33199=CARTESIAN_POINT('Ctrl Pts',(-1.53687260224456,-3.09613266190232,
42.2750554060399));
#33200=CARTESIAN_POINT('Ctrl Pts',(-1.86645400133787,2.62012303844274,7.00322156819806));
#33201=CARTESIAN_POINT('Ctrl Pts',(-2.74041061257865,1.997626899089,7.0695770455426));
#33202=CARTESIAN_POINT('Ctrl Pts',(-3.80025934494349,-0.179501204411249,
7.20224350234162));
#33203=CARTESIAN_POINT('Ctrl Pts',(-1.89809237229961,-3.30104156426044,
7.40122093859512));
#33204=CARTESIAN_POINT('Ctrl Pts',(1.75033879183918,-3.37766291872948,7.60015387695855));
#33205=CARTESIAN_POINT('Ctrl Pts',(3.78874883692714,-0.353950369213094,
7.79908681532199));
#33206=CARTESIAN_POINT('Ctrl Pts',(2.34462897392162,2.99761246260044,7.99801975368543));
#33207=CARTESIAN_POINT('Ctrl Pts',(-1.25517146953415,3.59217513842517,8.19695269204886));
#33208=CARTESIAN_POINT('Ctrl Pts',(-3.70095537602795,0.885102952948687,
8.39588563041231));
#33209=CARTESIAN_POINT('Ctrl Pts',(-2.74450292932235,-2.63599675282763,
8.59481856877575));
#33210=CARTESIAN_POINT('Ctrl Pts',(0.735019325049069,-3.73363101754262,
8.79375150713918));
#33211=CARTESIAN_POINT('Ctrl Pts',(3.53881629779805,-1.39901612008267,8.99268444550262));
#33212=CARTESIAN_POINT('Ctrl Pts',(3.08937315587434,2.22177005300786,9.19161738386606));
#33213=CARTESIAN_POINT('Ctrl Pts',(-0.200149810864368,3.80004717549578,
9.3905503222295));
#33214=CARTESIAN_POINT('Ctrl Pts',(-3.30567149883918,1.88493714980744,9.58948326059294));
#33215=CARTESIAN_POINT('Ctrl Pts',(-3.37227577980602,-1.76301114979847,
9.78841619895636));
#33216=CARTESIAN_POINT('Ctrl Pts',(-0.338730933097911,-3.79021165389004,
9.98734913731983));
#33217=CARTESIAN_POINT('Ctrl Pts',(3.00621041944956,-2.33305531494441,10.1862820756832));
#33218=CARTESIAN_POINT('Ctrl Pts',(3.58752910607548,1.26889034228732,10.3852150140467));
#33219=CARTESIAN_POINT('Ctrl Pts',(0.870815925397089,3.70433883892876,10.5841479524101));
#33220=CARTESIAN_POINT('Ctrl Pts',(-2.64644222848811,2.73437212425091,10.7830808907735));
#33221=CARTESIAN_POINT('Ctrl Pts',(-3.73081407650405,-0.749315416829459,
10.9820138291369));
#33222=CARTESIAN_POINT('Ctrl Pts',(-1.38543162233216,-3.54415382593228,
11.1809467675004));
#33223=CARTESIAN_POINT('Ctrl Pts',(2.23358439312533,-3.08083559997405,11.3798797058638));
#33224=CARTESIAN_POINT('Ctrl Pts',(3.79925615786297,0.214708774655039,11.5788126442273));
#33225=CARTESIAN_POINT('Ctrl Pts',(1.87225451730644,3.31287038929909,11.7777455825907));
#33226=CARTESIAN_POINT('Ctrl Pts',(-1.77591918454253,3.36549524737367,11.9766785209541));
#33227=CARTESIAN_POINT('Ctrl Pts',(-3.79148233256386,0.32420507008613,12.1756114593176));
#33228=CARTESIAN_POINT('Ctrl Pts',(-2.32151858988368,-3.01512829587034,
12.374544397681));
#33229=CARTESIAN_POINT('Ctrl Pts',(1.28262771288672,-3.58264055637097,12.5734773360444));
#33230=CARTESIAN_POINT('Ctrl Pts',(3.70764854672028,-0.85661511733405,12.7724102744079));
#33231=CARTESIAN_POINT('Ctrl Pts',(2.72421126934337,2.65690048083118,12.9713432127713));
#33232=CARTESIAN_POINT('Ctrl Pts',(-0.763605773387818,3.72791542664558,
13.1702761511348));
#33233=CARTESIAN_POINT('Ctrl Pts',(-3.54943656817764,1.37184082667385,13.3692090894982));
#33234=CARTESIAN_POINT('Ctrl Pts',(-3.0722542406453,-2.24537326208117,13.5681420278616));
#33235=CARTESIAN_POINT('Ctrl Pts',(0.229265333024543,-3.79840553553036,
13.7670749662251));
#33236=CARTESIAN_POINT('Ctrl Pts',(3.32002024707132,-1.85954638670049,13.9660079045885));
#33237=CARTESIAN_POINT('Ctrl Pts',(3.35866550245346,1.78880218243472,14.164940842952));
#33238=CARTESIAN_POINT('Ctrl Pts',(0.309674340768458,3.79269679883976,14.3638737813154));
#33239=CARTESIAN_POINT('Ctrl Pts',(-3.02400184575466,2.30994806048298,14.5628067196789));
#33240=CARTESIAN_POINT('Ctrl Pts',(-3.57769943142826,-1.29634639800277,
14.7617396580423));
#33241=CARTESIAN_POINT('Ctrl Pts',(-0.842401716518874,-3.71090373807563,
14.9606725964057));
#33242=CARTESIAN_POINT('Ctrl Pts',(2.66731971394778,-2.71401045481454,15.1596055347691));
#33243=CARTESIAN_POINT('Ctrl Pts',(3.72496204373251,0.777884938798361,15.3585384731326));
#33244=CARTESIAN_POINT('Ctrl Pts',(1.35822988608424,3.55466718298702,15.557471411496));
#33245=CARTESIAN_POINT('Ctrl Pts',(-2.25712916101158,3.06362777696122,15.7564043498595));
#33246=CARTESIAN_POINT('Ctrl Pts',(-3.7974991416244,-0.243818528047306,
15.9553372882229));
#33247=CARTESIAN_POINT('Ctrl Pts',(-1.84681095199157,-3.32712135529518,
16.1542702265864));
#33248=CARTESIAN_POINT('Ctrl Pts',(1.80165891510899,-3.35178644290854,16.3532031649498));
#33249=CARTESIAN_POINT('Ctrl Pts',(3.79385557686611,-0.295139064068223,
16.5521361033133));
#33250=CARTESIAN_POINT('Ctrl Pts',(2.29834361397166,3.03283099386907,16.7510690416766));
#33251=CARTESIAN_POINT('Ctrl Pts',(-1.31004604878593,3.57270577508387,16.9500019800401));
#33252=CARTESIAN_POINT('Ctrl Pts',(-3.71410444208186,0.828175946623051,
17.1489349184035));
#33253=CARTESIAN_POINT('Ctrl Pts',(-2.70376979034626,-2.677699782662,17.347867856767));
#33254=CARTESIAN_POINT('Ctrl Pts',(0.792152682487336,-3.7219539670562,17.5468007951304));
#33255=CARTESIAN_POINT('Ctrl Pts',(3.55984560446539,-1.3445990025378,17.7457337334939));
#33256=CARTESIAN_POINT('Ctrl Pts',(3.05495632989659,2.26885191841203,17.9446666718573));
#33257=CARTESIAN_POINT('Ctrl Pts',(-0.25836814307153,3.79653698887591,18.1435996102207));
#33258=CARTESIAN_POINT('Ctrl Pts',(-3.33417361125188,1.83404840047608,18.3425325485842));
#33259=CARTESIAN_POINT('Ctrl Pts',(-3.34485816893761,-1.8144891939465,18.5414654869476));
#33260=CARTESIAN_POINT('Ctrl Pts',(-0.280599453828384,-3.79495864954658,
18.740398425311));
#33261=CARTESIAN_POINT('Ctrl Pts',(3.04161561079433,-2.28670542078106,18.9393313636745));
#33262=CARTESIAN_POINT('Ctrl Pts',(3.56765966054535,1.32372646410603,19.1382643020379));
#33263=CARTESIAN_POINT('Ctrl Pts',(0.813938016583792,3.71725061173132,19.3371972404014));
#33264=CARTESIAN_POINT('Ctrl Pts',(-2.68804053459405,2.69348942630865,19.5361301787648));
#33265=CARTESIAN_POINT('Ctrl Pts',(-3.71889124076811,-0.8064087949641,19.7350631171283));
#33266=CARTESIAN_POINT('Ctrl Pts',(-1.33094837618574,-3.56497175657617,
19.9339960554916));
#33267=CARTESIAN_POINT('Ctrl Pts',(2.28054136216125,-3.04624002677545,20.1329289938551));
#33268=CARTESIAN_POINT('Ctrl Pts',(3.79551909140992,0.272913964465135,20.3318619322185));
#33269=CARTESIAN_POINT('Ctrl Pts',(1.8212589195482,3.34117691139266,20.530794870582));
#33270=CARTESIAN_POINT('Ctrl Pts',(-1.8272928305604,3.33788078226886,20.7297278089454));
#33271=CARTESIAN_POINT('Ctrl Pts',(-3.79600600068437,0.266055723534535,
20.9286607473089));
#33272=CARTESIAN_POINT('Ctrl Pts',(-2.27503365179541,-3.05035556754547,
21.1275936856723));
#33273=CARTESIAN_POINT('Ctrl Pts',(1.33738744309295,-3.56256116190508,21.3265266240357));
#33274=CARTESIAN_POINT('Ctrl Pts',(3.72034220082859,-0.799688135457281,
21.5254595623992));
#33275=CARTESIAN_POINT('Ctrl Pts',(2.6831695136488,2.69834181791016,21.7243925007626));
#33276=CARTESIAN_POINT('Ctrl Pts',(-0.820653066905469,3.7157739098384,21.923325439126));
#33277=CARTESIAN_POINT('Ctrl Pts',(-3.57004556405178,1.31727820746093,22.1222583774895));
#33278=CARTESIAN_POINT('Ctrl Pts',(-3.03747899557971,-2.29219732062257,
22.3211913158529));
#33279=CARTESIAN_POINT('Ctrl Pts',(0.287455778651096,-3.79444546417224,
22.5201242542163));
#33280=CARTESIAN_POINT('Ctrl Pts',(3.34813115288769,-1.80844269699657,22.7190571925798));
#33281=CARTESIAN_POINT('Ctrl Pts',(3.33085438535164,1.84006963695426,22.9179901309432));
#33282=CARTESIAN_POINT('Ctrl Pts',(0.251508086732996,3.79699761490117,23.1169230693067));
#33283=CARTESIAN_POINT('Ctrl Pts',(-3.0590507357933,2.26332847839188,23.3158560076701));
#33284=CARTESIAN_POINT('Ctrl Pts',(-3.55741035402456,-1.35102878516191,
23.5147889460336));
#33285=CARTESIAN_POINT('Ctrl Pts',(-0.785426512475196,-3.72337916397971,
23.7137218843969));
#33286=CARTESIAN_POINT('Ctrl Pts',(2.70860348135616,-2.67281020389449,23.9126548227604));
#33287=CARTESIAN_POINT('Ctrl Pts',(3.71260202003901,0.83488528916224,24.1115877611238));
#33288=CARTESIAN_POINT('Ctrl Pts',(1.30358869708293,3.57506695239331,24.3105206994873));
#33289=CARTESIAN_POINT('Ctrl Pts',(-2.3038196226511,3.02867336494793,24.5094536378507));
#33290=CARTESIAN_POINT('Ctrl Pts',(-3.79331612292701,-0.301993372111428,
24.7083865762142));
#33291=CARTESIAN_POINT('Ctrl Pts',(-1.7955999210022,-3.35503623362761,24.9073195145776));
#33292=CARTESIAN_POINT('Ctrl Pts',(1.85281942552575,-3.32377908135478,25.1062524529411));
#33293=CARTESIAN_POINT('Ctrl Pts',(3.79793347763706,-0.23695675702724,25.3051853913045));
#33294=CARTESIAN_POINT('Ctrl Pts',(2.25159007243797,3.06770098786632,25.5041183296679));
#33295=CARTESIAN_POINT('Ctrl Pts',(-1.36465029001659,3.55220731253327,25.7030512680313));
#33296=CARTESIAN_POINT('Ctrl Pts',(-3.72636145659287,0.771153357041461,
25.9019842063948));
#33297=CARTESIAN_POINT('Ctrl Pts',(-2.66241164915182,-2.7188253742596,26.1009171447582));
#33298=CARTESIAN_POINT('Ctrl Pts',(0.849105252762015,-3.70937561794287,
26.2998500831217));
#33299=CARTESIAN_POINT('Ctrl Pts',(3.58003584787151,-1.28988004605551,26.4987830214851));
#33300=CARTESIAN_POINT('Ctrl Pts',(3.01982326417359,2.31540809759601,26.6977159598485));
#33301=CARTESIAN_POINT('Ctrl Pts',(-0.316526531389901,3.79213108425639,
26.896648898212));
#33302=CARTESIAN_POINT('Ctrl Pts',(-3.36189205222476,1.78273078013626,27.0955818365754));
#33303=CARTESIAN_POINT('Ctrl Pts',(-3.31665497416533,-1.86554200906911,
27.294514774939));
#33304=CARTESIAN_POINT('Ctrl Pts',(-0.222401948075185,-3.79881357515075,
27.4934477133024));
#33305=CARTESIAN_POINT('Ctrl Pts',(3.07630619675248,-2.23981860628926,27.6923806516658));
#33306=CARTESIAN_POINT('Ctrl Pts',(3.54695211382774,1.37825175765173,27.8913135900291));
#33307=CARTESIAN_POINT('Ctrl Pts',(0.756868878729541,3.72928903487889,28.0902465283926));
#33308=CARTESIAN_POINT('Ctrl Pts',(-2.72900734653197,2.65197400210329,28.2891794667561));
#33309=CARTESIAN_POINT('Ctrl Pts',(-3.70609475092345,-0.863312748912513,
28.4881124051195));
#33310=CARTESIAN_POINT('Ctrl Pts',(-1.27615245566332,-3.58495217752786,
28.6870453434829));
#33311=CARTESIAN_POINT('Ctrl Pts',(2.32696257530329,-3.01092882320308,28.8859782818464));
#33312=CARTESIAN_POINT('Ctrl Pts',(3.79089036556033,0.331055043095624,29.0849112202098));
#33313=CARTESIAN_POINT('Ctrl Pts',(1.7698354633568,3.36869850801491,29.2838441585732));
#33314=CARTESIAN_POINT('Ctrl Pts',(-1.87823720077816,3.3094821683868,29.4827770969367));
#33315=CARTESIAN_POINT('Ctrl Pts',(-3.79963789451971,0.207843873585611,
29.6817100353001));
#33316=CARTESIAN_POINT('Ctrl Pts',(-2.22801425278663,-3.08486623610115,
29.8806429736635));
#33317=CARTESIAN_POINT('Ctrl Pts',(1.39183298835648,-3.54164483507025,30.079575912027));
#33318=CARTESIAN_POINT('Ctrl Pts',(3.73216185585201,-0.742573287279,30.2785088503904));
#33319=CARTESIAN_POINT('Ctrl Pts',(2.64149741600532,2.73914924867091,30.4774417887539));
#33320=CARTESIAN_POINT('Ctrl Pts',(-0.877507569004345,3.70275946715383,
30.6763747271173));
#33321=CARTESIAN_POINT('Ctrl Pts',(-3.58981586917566,1.26240612746925,30.8753076654808));
#33322=CARTESIAN_POINT('Ctrl Pts',(-3.00199017263393,-2.33848288611794,
31.0742406038442));
#33323=CARTESIAN_POINT('Ctrl Pts',(0.345578693905692,-3.78959398505641,
31.2731735422076));
#33324=CARTESIAN_POINT('Ctrl Pts',(3.37545550105851,-1.75691416000643,31.4721064805712));
#33325=CARTESIAN_POINT('Ctrl Pts',(3.3022607693379,1.89090481424875,31.6710394189345));
#33326=CARTESIAN_POINT('Ctrl Pts',(0.193282747315501,3.80040642364043,31.8699723572979));
#33327=CARTESIAN_POINT('Ctrl Pts',(-3.09338098022485,2.216177185254,32.0689052956615));
#33328=CARTESIAN_POINT('Ctrl Pts',(-3.53628555418785,-1.40539378271698,
32.2678382340249));
#33329=CARTESIAN_POINT('Ctrl Pts',(-0.728266792592632,-3.73497987733052,
32.4667711723883));
#33330=CARTESIAN_POINT('Ctrl Pts',(2.74925093176247,-2.63098204468606,32.6657041107517));
#33331=CARTESIAN_POINT('Ctrl Pts',(3.69936981560612,0.891689504614469,32.8646370491151));
#33332=CARTESIAN_POINT('Ctrl Pts',(1.24864126331116,3.59462685140112,33.0635699874787));
#33333=CARTESIAN_POINT('Ctrl Pts',(-2.34996886088683,2.99300744371268,33.262502925842));
#33334=CARTESIAN_POINT('Ctrl Pts',(-3.78824196177939,-0.360097270568816,
33.4614358642054));
#33335=CARTESIAN_POINT('Ctrl Pts',(-1.74396705980911,-3.38216293214238,
33.660368802569));
#33336=CARTESIAN_POINT('Ctrl Pts',(1.90354466348184,-3.29499088305067,33.8593017409324));
#33337=CARTESIAN_POINT('Ctrl Pts',(3.80111915122855,-0.17871878306637,34.0582346792959));
#33338=CARTESIAN_POINT('Ctrl Pts',(2.20430757749551,3.10185030410124,34.2571676176593));
#33339=CARTESIAN_POINT('Ctrl Pts',(-1.41893394161954,3.5308743498711,34.4561005560226));
#33340=CARTESIAN_POINT('Ctrl Pts',(-3.73774305793726,0.713949604733199,
34.6550334943861));
#33341=CARTESIAN_POINT('Ctrl Pts',(-2.62042804254318,-2.75931224748304,
34.8539664327496));
#33342=CARTESIAN_POINT('Ctrl Pts',(0.90585834750904,-3.69592584605102,35.052899371113));
#33343=CARTESIAN_POINT('Ctrl Pts',(3.59938505356419,-1.23485806529853,35.2518323094765));
#33344=CARTESIAN_POINT('Ctrl Pts',(2.98398076833351,2.36142033095977,35.4507652478398));
#33345=CARTESIAN_POINT('Ctrl Pts',(-0.374610559908926,3.7868343155833,35.6496981862033));
#33346=CARTESIAN_POINT('Ctrl Pts',(-3.3888207027795,1.73099435286343,35.8486311245668));
#33347=CARTESIAN_POINT('Ctrl Pts',(-3.28767261627215,-1.91615656287791,
36.0475640629301));
#33348=CARTESIAN_POINT('Ctrl Pts',(-0.164152194675816,-3.80177606683461,
36.2464970012937));
#33349=CARTESIAN_POINT('Ctrl Pts',(3.11027408336399,-2.1924056037633,36.445429939657));
#33350=CARTESIAN_POINT('Ctrl Pts',(3.52541130159383,1.43245326619635,36.6443628780206));
#33351=CARTESIAN_POINT('Ctrl Pts',(0.699621933880535,3.74045135720976,36.843295816384));
#33352=CARTESIAN_POINT('Ctrl Pts',(-2.76933304802493,2.60983556433168,37.0422287547475));
#33353=CARTESIAN_POINT('Ctrl Pts',(-3.69242760920404,-0.920013889243654,
37.2411616931107));
#33354=CARTESIAN_POINT('Ctrl Pts',(-1.22105673552787,-3.60409040657181,
37.4400946314743));
#33355=CARTESIAN_POINT('Ctrl Pts',(2.37283712765188,-2.9749102775556,37.6390275698377));
#33356=CARTESIAN_POINT('Ctrl Pts',(3.7853710681766,0.389118345988962,37.8379605082012));
#33357=CARTESIAN_POINT('Ctrl Pts',(1.71799622765437,3.39542872065456,38.0368934465646));
#33358=CARTESIAN_POINT('Ctrl Pts',(-1.92874032343257,3.28030606602396,38.235826384928));
#33359=CARTESIAN_POINT('Ctrl Pts',(-3.80237716814379,0.149583216029986,
38.4347593232914));
#33360=CARTESIAN_POINT('Ctrl Pts',(-2.1804714247586,-3.1186522326827,38.633692261655));
#33361=CARTESIAN_POINT('Ctrl Pts',(1.44595153099118,-3.51989641602498,38.8326252000182));
#33362=CARTESIAN_POINT('Ctrl Pts',(3.74310478705912,-0.685284131425703,
39.0315581383817));
#33363=CARTESIAN_POINT('Ctrl Pts',(2.59920466649454,2.77931345664184,39.2304910767451));
#33364=CARTESIAN_POINT('Ctrl Pts',(-0.934155731980976,3.68887463797949,
39.4294240151087));
#33365=CARTESIAN_POINT('Ctrl Pts',(-3.60874320562774,1.20723847073212,39.628356953472));
#33366=CARTESIAN_POINT('Ctrl Pts',(-2.9657954060591,-2.38422098941366,39.8272898918356));
#33367=CARTESIAN_POINT('Ctrl Pts',(0.403619076468115,-3.78384858628005,
40.0262228301989));
#33368=CARTESIAN_POINT('Ctrl Pts',(3.40198945678621,-1.70497988275374,40.2251557685625));
#33369=CARTESIAN_POINT('Ctrl Pts',(3.27288641644818,1.9413091971248,40.4240887069258));
#33370=CARTESIAN_POINT('Ctrl Pts',(0.135021502466078,3.80289668242824,40.6230216452892));
#33371=CARTESIAN_POINT('Ctrl Pts',(-3.12700273222302,2.16855461601647,40.8219545836528));
#33372=CARTESIAN_POINT('Ctrl Pts',(-3.51429506264349,-1.45952325961196,
41.020887522016));
#33373=CARTESIAN_POINT('Ctrl Pts',(-0.671002965181634,-3.74552168112398,
41.2198204603797));
#33374=CARTESIAN_POINT('Ctrl Pts',(2.78938095197937,-2.58888381470178,41.418753398743));
#33375=CARTESIAN_POINT('Ctrl Pts',(3.68502221077952,0.948952011033468,41.6176863371064));
#33376=CARTESIAN_POINT('Ctrl Pts',(1.19387337835599,3.61205745181745,41.8166192754698));
#33377=CARTESIAN_POINT('Ctrl Pts',(-2.39647795137431,2.95914235739577,42.0155522138333));
#33378=CARTESIAN_POINT('Ctrl Pts',(-3.78048145955207,-0.423284565706465,
42.2144851521968));
#33379=CARTESIAN_POINT('Ctrl Pts',(-2.39075764659687,-2.40472543932513,
42.3471071111058));
#33380=CARTESIAN_POINT('Ctrl Pts',(-1.43031864127241,-2.88147257990253,
42.4134180905602));
#33381=CARTESIAN_POINT('',(-1.87386922097,2.62532148205406,42.0016066797527));
#33382=CARTESIAN_POINT('Ctrl Pts',(-1.87561919562493,2.62751776731827,42.));
#33383=CARTESIAN_POINT('Ctrl Pts',(-1.93354241972396,2.5952533695629,42.));
#33384=CARTESIAN_POINT('Ctrl Pts',(-1.99028258208655,2.56113722808904,42.));
#33385=CARTESIAN_POINT('Ctrl Pts',(-2.04574119823645,2.52519298213882,42.));
#33386=CARTESIAN_POINT('Ctrl Pts',(-2.13151874516022,2.46959820791473,42.));
#33387=CARTESIAN_POINT('Ctrl Pts',(-2.21423174799282,2.40963304771824,42.));
#33388=CARTESIAN_POINT('Ctrl Pts',(-2.29379848781349,2.34570550738362,42.));
#33389=CARTESIAN_POINT('Ctrl Pts',(-2.37493421037037,2.28051737490485,42.));
#33390=CARTESIAN_POINT('Ctrl Pts',(-2.45279884777719,2.21120864124839,42.));
#33391=CARTESIAN_POINT('Ctrl Pts',(-2.52728671613257,2.13816044108625,42.));
#33392=CARTESIAN_POINT('Ctrl Pts',(-2.60344111362154,2.06347792172002,42.));
#33393=CARTESIAN_POINT('Ctrl Pts',(-2.67606653870818,1.98488624906051,42.));
#33394=CARTESIAN_POINT('Ctrl Pts',(-2.7450221352932,1.90274628377322,42.));
#33395=CARTESIAN_POINT('Ctrl Pts',(-2.7679416471307,1.87544454178317,42.));
#33396=CARTESIAN_POINT('Ctrl Pts',(-2.79045546383387,1.84775045492808,42.));
#33397=CARTESIAN_POINT('Ctrl Pts',(-2.81255757521727,1.81967632547802,42.));
#33398=CARTESIAN_POINT('Ctrl Pts',(-2.82452315241262,1.80447763439825,42.));
#33399=CARTESIAN_POINT('Ctrl Pts',(-2.83636967025138,1.78916527706112,42.));
#33400=CARTESIAN_POINT('Ctrl Pts',(-2.84808157918788,1.77376072408085,42.));
#33401=CARTESIAN_POINT('Ctrl Pts',(-2.91426840109589,1.68670588014324,42.));
#33402=CARTESIAN_POINT('Ctrl Pts',(-2.9762581387323,1.59658638019521,42.));
#33403=CARTESIAN_POINT('Ctrl Pts',(-3.03395163488204,1.50383670327667,42.));
#33404=CARTESIAN_POINT('Ctrl Pts',(-3.09256319399938,1.40961112267194,42.));
#33405=CARTESIAN_POINT('Ctrl Pts',(-3.14674125704714,1.31267038210085,42.));
#33406=CARTESIAN_POINT('Ctrl Pts',(-3.19635290330767,1.21342331376483,42.));
#33407=CARTESIAN_POINT('Ctrl Pts',(-3.246323219868,1.11345873294058,42.));
#33408=CARTESIAN_POINT('Ctrl Pts',(-3.29166142466647,1.01115361908758,42.));
#33409=CARTESIAN_POINT('Ctrl Pts',(-3.3321940140089,0.906889032325619,42.));
#33410=CARTESIAN_POINT('Ctrl Pts',(-3.36732123477664,0.816529022840346,
42.));
#33411=CARTESIAN_POINT('Ctrl Pts',(-3.39883874146856,0.724696427496403,
42.));
#33412=CARTESIAN_POINT('Ctrl Pts',(-3.42660590875194,0.631623878310208,
42.));
#33413=CARTESIAN_POINT('Ctrl Pts',(-3.43064581025193,0.618082564310531,
42.));
#33414=CARTESIAN_POINT('Ctrl Pts',(-3.43460572040773,0.604516718988522,
42.));
#33415=CARTESIAN_POINT('Ctrl Pts',(-3.43848278257111,0.590935988110032,
42.));
#33416=CARTESIAN_POINT('Ctrl Pts',(-3.47005193987078,0.480354261204366,
42.));
#33417=CARTESIAN_POINT('Ctrl Pts',(-3.49618062575215,0.368624547072095,
42.));
#33418=CARTESIAN_POINT('Ctrl Pts',(-3.51673450065987,0.256176968912335,
42.));
#33419=CARTESIAN_POINT('Ctrl Pts',(-3.53722326495676,0.144085602441787,
42.));
#33420=CARTESIAN_POINT('Ctrl Pts',(-3.55217297423634,0.0312800672726983,
42.));
#33421=CARTESIAN_POINT('Ctrl Pts',(-3.56140895218783,-0.0818433222640444,
42.));
#33422=CARTESIAN_POINT('Ctrl Pts',(-3.56994174233481,-0.186353981417057,
42.));
#33423=CARTESIAN_POINT('Ctrl Pts',(-3.57359760697331,-0.291136756602193,
42.));
#33424=CARTESIAN_POINT('Ctrl Pts',(-3.5722015224377,-0.395892400984094,
42.));
#33425=CARTESIAN_POINT('Ctrl Pts',(-3.57116204802633,-0.473889691980635,
42.));
#33426=CARTESIAN_POINT('Ctrl Pts',(-3.56732114613858,-0.551872243847325,
42.));
#33427=CARTESIAN_POINT('Ctrl Pts',(-3.56075455121097,-0.629742381860636,
42.));
#33428=CARTESIAN_POINT('Ctrl Pts',(-3.55856422692781,-0.655716399765561,
42.));
#33429=CARTESIAN_POINT('Ctrl Pts',(-3.55607053983388,-0.681677912787002,
42.));
#33430=CARTESIAN_POINT('Ctrl Pts',(-3.55327599217611,-0.707623291232608,
42.));
#33431=CARTESIAN_POINT('Ctrl Pts',(-3.55103199554422,-0.728457196742502,
42.));
#33432=CARTESIAN_POINT('Ctrl Pts',(-3.54859343660888,-0.749284406114006,
42.));
#33433=CARTESIAN_POINT('Ctrl Pts',(-3.54596521901003,-0.770076248997231,
42.));
#33434=CARTESIAN_POINT('Ctrl Pts',(-3.53185443093333,-0.881706765731404,
42.));
#33435=CARTESIAN_POINT('Ctrl Pts',(-3.51226715074755,-0.992463613106634,
42.));
#33436=CARTESIAN_POINT('Ctrl Pts',(-3.48751798321568,-1.10205172963754,
42.));
#33437=CARTESIAN_POINT('Ctrl Pts',(-3.46230882163008,-1.2136766775851,42.));
#33438=CARTESIAN_POINT('Ctrl Pts',(-3.43174398907026,-1.32408968730896,
42.));
#33439=CARTESIAN_POINT('Ctrl Pts',(-3.39610122197234,-1.43298776326768,
42.));
#33440=CARTESIAN_POINT('Ctrl Pts',(-3.35972906008411,-1.5441143331326,42.));
#33441=CARTESIAN_POINT('Ctrl Pts',(-3.31806887336794,-1.65366408568259,
42.));
#33442=CARTESIAN_POINT('Ctrl Pts',(-3.27136124123191,-1.7613134609039,42.));
#33443=CARTESIAN_POINT('Ctrl Pts',(-3.23281667986467,-1.85014900575188,
42.));
#33444=CARTESIAN_POINT('Ctrl Pts',(-3.19083369759702,-1.93769056532194,
42.));
#33445=CARTESIAN_POINT('Ctrl Pts',(-3.14552159514942,-2.02374982253641,
42.));
#33446=CARTESIAN_POINT('Ctrl Pts',(-3.1353496479755,-2.04306894857399,42.));
#33447=CARTESIAN_POINT('Ctrl Pts',(-3.12500984414154,-2.06231334028129,
42.));
#33448=CARTESIAN_POINT('Ctrl Pts',(-3.11450326876925,-2.081480800172,42.));
#33449=CARTESIAN_POINT('Ctrl Pts',(-3.10547118925435,-2.09795829314162,
42.));
#33450=CARTESIAN_POINT('Ctrl Pts',(-3.09632042674677,-2.11437056920114,
42.));
#33451=CARTESIAN_POINT('Ctrl Pts',(-3.08705381289204,-2.13071331918172,
42.));
#33452=CARTESIAN_POINT('Ctrl Pts',(-3.02769650863937,-2.23539682041853,
42.));
#33453=CARTESIAN_POINT('Ctrl Pts',(-2.9635677965333,-2.33726880643937,42.));
#33454=CARTESIAN_POINT('Ctrl Pts',(-2.89494192545328,-2.43599574081051,
42.));
#33455=CARTESIAN_POINT('Ctrl Pts',(-2.82581314326201,-2.53544617597652,
42.));
#33456=CARTESIAN_POINT('Ctrl Pts',(-2.75212073730953,-2.63170612789041,
42.));
#33457=CARTESIAN_POINT('Ctrl Pts',(-2.67409458472159,-2.72442029741163,
42.));
#33458=CARTESIAN_POINT('Ctrl Pts',(-2.63882178662635,-2.76633301607867,
42.));
#33459=CARTESIAN_POINT('Ctrl Pts',(-2.60266268502766,-2.80752084211434,
42.));
#33460=CARTESIAN_POINT('Ctrl Pts',(-2.56563543615746,-2.84794928527981,
42.));
#33461=CARTESIAN_POINT('Ctrl Pts',(-2.54453127685218,-2.87099199925564,
42.));
#33462=CARTESIAN_POINT('Ctrl Pts',(-2.52314012955761,-2.89379293748534,
42.));
#33463=CARTESIAN_POINT('Ctrl Pts',(-2.50149137216201,-2.91631875583217,
42.));
#33464=CARTESIAN_POINT('Ctrl Pts',(-2.41601150820879,-3.00526168463577,
42.));
#33465=CARTESIAN_POINT('Ctrl Pts',(-2.32646440639479,-3.08998053490754,
42.));
#33466=CARTESIAN_POINT('Ctrl Pts',(-2.23310493987845,-3.17012015379869,
42.));
#33467=CARTESIAN_POINT('Ctrl Pts',(-2.14095799804003,-3.24921894341766,
42.));
#33468=CARTESIAN_POINT('Ctrl Pts',(-2.04509659589572,-3.32385743023979,
42.));
#33469=CARTESIAN_POINT('Ctrl Pts',(-1.94572314910561,-3.39366789682963,
42.));
#33470=CARTESIAN_POINT('Ctrl Pts',(-1.88149925545439,-3.43878558296039,
42.));
#33471=CARTESIAN_POINT('Ctrl Pts',(-1.81580757706967,-3.48188610285196,
42.));
#33472=CARTESIAN_POINT('Ctrl Pts',(-1.7486944753309,-3.52286199445098,42.));
#33473=CARTESIAN_POINT('Ctrl Pts',(-1.83231942908391,2.65117390457541,42.));
#33474=CARTESIAN_POINT('Ctrl Pts',(-1.84571201009948,2.64191782131431,42.0005355599176));
#33475=CARTESIAN_POINT('Ctrl Pts',(-1.85903445318218,2.6325602558508,42.0010711198351));
#33476=CARTESIAN_POINT('Ctrl Pts',(-1.8722852285359,2.62310228270006,42.0016066797527));
#33477=CARTESIAN_POINT('Ctrl Pts',(-1.75279757044496,-3.52836060600329,
7.));
#33478=CARTESIAN_POINT('Ctrl Pts',(-1.82143513113133,-3.4868125032314,6.99999999999999));
#33479=CARTESIAN_POINT('Ctrl Pts',(-1.88858118174007,-3.44308259126114,
6.99999999999999));
#33480=CARTESIAN_POINT('Ctrl Pts',(-1.95412266298839,-3.39717065740713,
6.99999999999999));
#33481=CARTESIAN_POINT('Ctrl Pts',(-2.05256253282086,-3.32821333898428,
6.99999999999999));
#33482=CARTESIAN_POINT('Ctrl Pts',(-2.14738467987841,-3.25433542296032,
7.));
#33483=CARTESIAN_POINT('Ctrl Pts',(-2.23843373886498,-3.17595281845062,
7.));
#33484=CARTESIAN_POINT('Ctrl Pts',(-2.33061677527292,-3.09659399183901,
7.));
#33485=CARTESIAN_POINT('Ctrl Pts',(-2.41893259169034,-3.01261674070712,
6.99999999999999));
#33486=CARTESIAN_POINT('Ctrl Pts',(-2.50317815019085,-2.9244189608764,6.99999999999999));
#33487=CARTESIAN_POINT('Ctrl Pts',(-2.5873331199782,-2.8363160195573,7.));
#33488=CARTESIAN_POINT('Ctrl Pts',(-2.66742692977287,-2.74400072916138,
6.99999999999999));
#33489=CARTESIAN_POINT('Ctrl Pts',(-2.74320996257998,-2.64784930966859,
6.99999999999999));
#33490=CARTESIAN_POINT('Ctrl Pts',(-2.77126696959633,-2.61225135388067,
6.99999999999999));
#33491=CARTESIAN_POINT('Ctrl Pts',(-2.79873261100939,-2.57612745058929,
7.));
#33492=CARTESIAN_POINT('Ctrl Pts',(-2.82559242679685,-2.53949635630442,
7.));
#33493=CARTESIAN_POINT('Ctrl Pts',(-2.83828837203979,-2.52218177861299,
7.));
#33494=CARTESIAN_POINT('Ctrl Pts',(-2.85085104477547,-2.5047507777665,7.));
#33495=CARTESIAN_POINT('Ctrl Pts',(-2.86326365819409,-2.48722719727718,
7.));
#33496=CARTESIAN_POINT('Ctrl Pts',(-2.93259158933157,-2.38935308000032,
7.));
#33497=CARTESIAN_POINT('Ctrl Pts',(-2.99733701215284,-2.28846693884865,
7.));
#33498=CARTESIAN_POINT('Ctrl Pts',(-3.05733419775333,-2.18496288465553,
7.));
#33499=CARTESIAN_POINT('Ctrl Pts',(-3.11720514852066,-2.08167660429433,
7.));
#33500=CARTESIAN_POINT('Ctrl Pts',(-3.17234812152713,-1.97578252307709,
7.));
#33501=CARTESIAN_POINT('Ctrl Pts',(-3.22255056777115,-1.86765274479227,
7.));
#33502=CARTESIAN_POINT('Ctrl Pts',(-3.27167565899372,-1.76184345421906,
7.));
#33503=CARTESIAN_POINT('Ctrl Pts',(-3.31607011161638,-1.65389257738756,
7.));
#33504=CARTESIAN_POINT('Ctrl Pts',(-3.35548609359103,-1.54414270697495,
7.));
#33505=CARTESIAN_POINT('Ctrl Pts',(-3.38624690686046,-1.45849229054546,
7.));
#33506=CARTESIAN_POINT('Ctrl Pts',(-3.41397468395636,-1.37174597137287,
7.00000000000001));
#33507=CARTESIAN_POINT('Ctrl Pts',(-3.43852956617388,-1.28406860130853,
7.00000000000001));
#33508=CARTESIAN_POINT('Ctrl Pts',(-3.44534001315227,-1.25975074570902,
7.00000000000001));
#33509=CARTESIAN_POINT('Ctrl Pts',(-3.45190626155755,-1.23536129061186,
7.));
#33510=CARTESIAN_POINT('Ctrl Pts',(-3.45822504922081,-1.21090381613226,
7.));
#33511=CARTESIAN_POINT('Ctrl Pts',(-3.46235658517791,-1.19491230943548,
7.00000000000001));
#33512=CARTESIAN_POINT('Ctrl Pts',(-3.46638018579831,-1.17889993609237,
7.));
#33513=CARTESIAN_POINT('Ctrl Pts',(-3.4702944287354,-1.16287131443645,7.));
#33514=CARTESIAN_POINT('Ctrl Pts',(-3.49751037118451,-1.0514234427693,7.00000000000001));
#33515=CARTESIAN_POINT('Ctrl Pts',(-3.51945812556307,-0.939134270268195,
7.00000000000001));
#33516=CARTESIAN_POINT('Ctrl Pts',(-3.53594432284242,-0.826340673701463,
7.00000000000001));
#33517=CARTESIAN_POINT('Ctrl Pts',(-3.55198795134533,-0.716574999412837,
7.00000000000001));
#33518=CARTESIAN_POINT('Ctrl Pts',(-3.56285932263424,-0.60633091546549,
7.00000000000001));
#33519=CARTESIAN_POINT('Ctrl Pts',(-3.56833195426463,-0.495920182767021,
7.00000000000001));
#33520=CARTESIAN_POINT('Ctrl Pts',(-3.57365992657054,-0.388427962237084,
7.));
#33521=CARTESIAN_POINT('Ctrl Pts',(-3.57387078895861,-0.280777228268469,
7.00000000000001));
#33522=CARTESIAN_POINT('Ctrl Pts',(-3.56870919579919,-0.173266018235025,
7.00000000000001));
#33523=CARTESIAN_POINT('Ctrl Pts',(-3.56545218869441,-0.105425573607107,
7.00000000000001));
#33524=CARTESIAN_POINT('Ctrl Pts',(-3.56005490071492,-0.0376409163409465,
7.00000000000001));
#33525=CARTESIAN_POINT('Ctrl Pts',(-3.55255422030096,0.0300081250946052,
7.00000000000001));
#33526=CARTESIAN_POINT('Ctrl Pts',(-3.54883684376604,0.0635353446751962,
7.00000000000001));
#33527=CARTESIAN_POINT('Ctrl Pts',(-3.54460273875139,0.0970292015076146,
7.00000000000001));
#33528=CARTESIAN_POINT('Ctrl Pts',(-3.53985592740968,0.130479635249894,
7.00000000000001));
#33529=CARTESIAN_POINT('Ctrl Pts',(-3.53595669558841,0.157957237853769,
7.00000000000001));
#33530=CARTESIAN_POINT('Ctrl Pts',(-3.53171002969387,0.185413044431481,
7.00000000000001));
#33531=CARTESIAN_POINT('Ctrl Pts',(-3.52712663472941,0.212793679985835,
7.00000000000001));
#33532=CARTESIAN_POINT('Ctrl Pts',(-3.50874228151889,0.322619535942592,
7.00000000000001));
#33533=CARTESIAN_POINT('Ctrl Pts',(-3.48492824893386,0.431373726643265,
7.00000000000001));
#33534=CARTESIAN_POINT('Ctrl Pts',(-3.45593528714537,0.538732382687488,
7.00000000000001));
#33535=CARTESIAN_POINT('Ctrl Pts',(-3.42668728127143,0.647035446910703,
7.00000000000001));
#33536=CARTESIAN_POINT('Ctrl Pts',(-3.3921683075505,0.753919111921691,7.00000000000001));
#33537=CARTESIAN_POINT('Ctrl Pts',(-3.35258661736185,0.859029856172523,
7.00000000000001));
#33538=CARTESIAN_POINT('Ctrl Pts',(-3.31330346367511,0.96334782493164,7.00000000000001));
#33539=CARTESIAN_POINT('Ctrl Pts',(-3.26903306106834,1.06592021272638,7.00000000000001));
#33540=CARTESIAN_POINT('Ctrl Pts',(-3.21993945256717,1.16636974039666,7.00000000000001));
#33541=CARTESIAN_POINT('Ctrl Pts',(-3.18444216307314,1.23900009029579,7.00000000000001));
#33542=CARTESIAN_POINT('Ctrl Pts',(-3.14642243000112,1.31051997303733,7.00000000000001));
#33543=CARTESIAN_POINT('Ctrl Pts',(-3.10593191142431,1.38077323634485,7.00000000000001));
#33544=CARTESIAN_POINT('Ctrl Pts',(-3.09665163218864,1.39687502816246,7.00000000000001));
#33545=CARTESIAN_POINT('Ctrl Pts',(-3.087240740324,1.41291154782213,7.00000000000001));
#33546=CARTESIAN_POINT('Ctrl Pts',(-3.07770226318236,1.42887670683733,7.00000000000001));
#33547=CARTESIAN_POINT('Ctrl Pts',(-3.02120417669121,1.52344116628832,7.00000000000001));
#33548=CARTESIAN_POINT('Ctrl Pts',(-2.96039292042869,1.61523884970404,7.00000000000001));
#33549=CARTESIAN_POINT('Ctrl Pts',(-2.89545383187046,1.70392058416469,7.00000000000001));
#33550=CARTESIAN_POINT('Ctrl Pts',(-2.83177573858355,1.7908802857128,7.00000000000001));
#33551=CARTESIAN_POINT('Ctrl Pts',(-2.76412793568667,1.8748443953877,7.00000000000001));
#33552=CARTESIAN_POINT('Ctrl Pts',(-2.69265479824662,1.95544467162499,7.00000000000001));
#33553=CARTESIAN_POINT('Ctrl Pts',(-2.64648561361655,2.00750967350008,7.00000000000001));
#33554=CARTESIAN_POINT('Ctrl Pts',(-2.5987196386097,2.05817023396695,7.));
#33555=CARTESIAN_POINT('Ctrl Pts',(-2.54939063956779,2.10731665555531,7.00000000000001));
#33556=CARTESIAN_POINT('Ctrl Pts',(-2.5348701644819,2.12178338717555,7.00000000000001));
#33557=CARTESIAN_POINT('Ctrl Pts',(-2.52021953276182,2.13611352242801,7.));
#33558=CARTESIAN_POINT('Ctrl Pts',(-2.50544499954275,2.15029964147411,7.));
#33559=CARTESIAN_POINT('Ctrl Pts',(-2.42926702549359,2.22344373290008,7.));
#33560=CARTESIAN_POINT('Ctrl Pts',(-2.34975484372937,2.29280507614037,7.));
#33561=CARTESIAN_POINT('Ctrl Pts',(-2.26705259277626,2.35803725076561,7.));
#33562=CARTESIAN_POINT('Ctrl Pts',(-2.18660206795646,2.42149335532451,7.));
#33563=CARTESIAN_POINT('Ctrl Pts',(-2.10313227547012,2.48104239546345,7.));
#33564=CARTESIAN_POINT('Ctrl Pts',(-2.01675688329826,2.5363204381136,7.));
#33565=CARTESIAN_POINT('Ctrl Pts',(-1.96924061746609,2.56672963340872,7.));
#33566=CARTESIAN_POINT('Ctrl Pts',(-1.92084475461694,2.59584549215854,7.));
#33567=CARTESIAN_POINT('Ctrl Pts',(-1.87158653173904,2.62360084935059,7.));
#33568=CARTESIAN_POINT('Origin',(0.,0.,42.));
#33569=CARTESIAN_POINT('Origin',(0.,0.,7.));
#42651=UNCERTAINTY_MEASURE_WITH_UNIT(LENGTH_MEASURE(0.01),#42668,
'DISTANCE_ACCURACY_VALUE',
'Maximum model space distance between geometric entities at asserted c
onnectivities');
#42656=UNCERTAINTY_MEASURE_WITH_UNIT(LENGTH_MEASURE(0.01),#42668,
'DISTANCE_ACCURACY_VALUE',
'Maximum model space distance between geometric entities at asserted c
onnectivities');
#42662=(
GEOMETRIC_REPRESENTATION_CONTEXT(3)
GLOBAL_UNCERTAINTY_ASSIGNED_CONTEXT((#42651))
GLOBAL_UNIT_ASSIGNED_CONTEXT((#42668,#42670,#42671))
REPRESENTATION_CONTEXT('','3D')
);
#42667=(
GEOMETRIC_REPRESENTATION_CONTEXT(3)
GLOBAL_UNCERTAINTY_ASSIGNED_CONTEXT((#42656))
GLOBAL_UNIT_ASSIGNED_CONTEXT((#42668,#42670,#42671))
REPRESENTATION_CONTEXT('','3D')
);
#42668=(
LENGTH_UNIT()
NAMED_UNIT(*)
SI_UNIT(.MILLI.,.METRE.)
);
#42670=(
NAMED_UNIT(*)
PLANE_ANGLE_UNIT()
SI_UNIT($,.RADIAN.)
);
#42671=(
NAMED_UNIT(*)
SI_UNIT($,.STERADIAN.)
SOLID_ANGLE_UNIT()
);
#42677=SHAPE_DEFINITION_REPRESENTATION(#42687,#42706);
#42687=PRODUCT_DEFINITION_SHAPE('',$,#42717);
#42706=SHAPE_REPRESENTATION('',(#4264),#42662);
#42711=PRODUCT_DEFINITION_CONTEXT('part definition',#42743,'design');
#42717=PRODUCT_DEFINITION('Screw','Screw',#42727,#42711);
#42727=PRODUCT_DEFINITION_FORMATION('',$,#42750);
#42743=APPLICATION_CONTEXT(
'Core Data for Automotive Mechanical Design Process');
#42744=PRODUCT_CONTEXT('part definition',#42743,'mechanical');
#42750=PRODUCT('Screw','Screw',$,(#42744));
#42756=PRESENTATION_STYLE_ASSIGNMENT((#42758));
#42758=SURFACE_STYLE_USAGE(.BOTH.,#42760);
#42760=SURFACE_SIDE_STYLE('',(#42762));
#42762=SURFACE_STYLE_FILL_AREA(#42764);
#42764=FILL_AREA_STYLE('Opaque(160,160,160)',(#42766));
#42766=FILL_AREA_STYLE_COLOUR('Opaque(160,160,160)',#42768);
#42768=COLOUR_RGB('Opaque(160,160,160)', 0.09019608, 0.27058824, 0.51372549);
ENDSEC;
END-ISO-10303-21;
